ISO-10303-21;
HEADER;
FILE_DESCRIPTION (('STEP AP214'),
    '1' );
FILE_NAME ('1. Base.step',
    '2026-10-09T14:04:53',
    ( '' ),
    ( '' ),
    'SwSTEP 2.0',
    'SolidWorks 2021',
    '' );
FILE_SCHEMA (( 'AUTOMOTIVE_DESIGN' ));
ENDSEC;

DATA;
#9=CARTESIAN_POINT ( 'NONE',  ( -103.2512961873279238, -60.00000000000000711, 100.0497975478645145 ) ) ;
#17=CARTESIAN_POINT ( 'NONE',  ( -83.71287190118881938, -39.46305555311884916, 176.1778646026642150 ) ) ;
#27=CARTESIAN_POINT ( 'NONE',  ( -39.15148982810983824, -57.67118160050520004, -41.75192649668374401 ) ) ;
#32=CARTESIAN_POINT ( 'NONE',  ( 106.8726675771063981, -14.21045842199433729, 167.8793401222494595 ) ) ;
#34=CARTESIAN_POINT ( 'NONE',  ( -114.2389886898993581, -60.00000000000000000, 181.3578213617837491 ) ) ;
#35=CARTESIAN_POINT ( 'NONE',  ( -63.13573024357239660, -42.96249537661331885, 82.55452416654728154 ) ) ;
#38=CARTESIAN_POINT ( 'NONE',  ( 95.01673997733890076, -60.00000000000974865, -3.495082099215109928 ) ) ;
#40=CARTESIAN_POINT ( 'NONE',  ( 6.086195650940305374E-05, -60.35900081385168647, 33.94948342857766477 ) ) ;
#47=CARTESIAN_POINT ( 'NONE',  ( -99.61197666665466954, -60.00000000000001421, 201.9966760002100159 ) ) ;
#55=AXIS2_PLACEMENT_3D ( 'NONE', #91909, #202, #25075 ) ;
#60=CARTESIAN_POINT ( 'NONE',  ( -31.41997332126805631, -18.66943872641200741, 29.82631662943089523 ) ) ;
#63=CARTESIAN_POINT ( 'NONE',  ( 39.22965285208312736, -18.76749908013844248, 33.52532150400537603 ) ) ;
#69=CARTESIAN_POINT ( 'NONE',  ( -79.89526249746191411, -38.77347676181469183, 192.8024975868495687 ) ) ;
#82=CARTESIAN_POINT ( 'NONE',  ( 102.1624392737155205, -60.00000000000001421, 93.69283045337873261 ) ) ;
#87=CARTESIAN_POINT ( 'NONE',  ( -97.97749490832038077, -30.00000000000004619, 190.5538380573200925 ) ) ;
#102=CARTESIAN_POINT ( 'NONE',  ( 79.44807355516962843, -49.90302049612382973, 154.1158519667677069 ) ) ;
#109=CARTESIAN_POINT ( 'NONE',  ( -49.97608103696126136, -60.00000000000002132, -32.05360424975566502 ) ) ;
#115=CIRCLE ( 'NONE', #15617, 7.500000000001509015 ) ;
#118=CARTESIAN_POINT ( 'NONE',  ( 86.75557114459695640, -46.46500150678768648, 190.6000161368287138 ) ) ;
#122=CARTESIAN_POINT ( 'NONE',  ( 28.31057169221128333, -31.30877727696230295, 39.66972444408808229 ) ) ;
#130=CYLINDRICAL_SURFACE ( 'NONE', #47470, 15.00000000000000000 ) ;
#140=CARTESIAN_POINT ( 'NONE',  ( 107.5126338499654253, -57.67122577595705479, 113.4697314741770526 ) ) ;
#146=CARTESIAN_POINT ( 'NONE',  ( -77.21030068849461259, -59.99999999999998579, 191.0276050645643693 ) ) ;
#150=CARTESIAN_POINT ( 'NONE',  ( -85.33812798373763542, -39.31465026836636412, 184.9304593203771105 ) ) ;
#156=CARTESIAN_POINT ( 'NONE',  ( -84.48871104503169249, -45.26950317026464177, -6.202404481629068655 ) ) ;
#164=CARTESIAN_POINT ( 'NONE',  ( 13.60704923275002010, -1.734723475976807094E-15, -10.45706415777842935 ) ) ;
#167=CARTESIAN_POINT ( 'NONE',  ( -49.63234380517151578, -59.99999999999993605, -40.41886796471348475 ) ) ;
#169=CARTESIAN_POINT ( 'NONE',  ( -79.92941718139617535, -25.61975873786342106, 131.8724341985731314 ) ) ;
#171=CARTESIAN_POINT ( 'NONE',  ( 78.26152162121309175, -14.21045842199439946, 161.8191806974193696 ) ) ;
#173=CARTESIAN_POINT ( 'NONE',  ( 99.06310009222487167, -57.67128884157320101, 63.13715724456057643 ) ) ;
#193=CARTESIAN_POINT ( 'NONE',  ( 30.74548990976421337, -46.43177832593983112, 34.64018936480751165 ) ) ;
#202=DIRECTION ( 'NONE',  ( -0.000000000000000000, -1.000000000000000000, -0.000000000000000000 ) ) ;
#206=CARTESIAN_POINT ( 'NONE',  ( 92.56567127985995569, -60.00000000000000000, -10.67295280362520593 ) ) ;
#219=CARTESIAN_POINT ( 'NONE',  ( 84.37161269647305062, -45.28772981460180347, -2.916092811979204225 ) ) ;
#230=CARTESIAN_POINT ( 'NONE',  ( -43.74360349336041054, -60.00000000000002842, 47.43859567335308469 ) ) ;
#232=CARTESIAN_POINT ( 'NONE',  ( 64.25703057368325233, -46.43406019868007917, 87.64572675471643493 ) ) ;
#236=CARTESIAN_POINT ( 'NONE',  ( -101.8692865417259696, -57.67122770170253432, 80.25822756173465677 ) ) ;
#254=CARTESIAN_POINT ( 'NONE',  ( -98.86384284808873701, -30.00000000000000000, 189.1376879781174694 ) ) ;
#257=CARTESIAN_POINT ( 'NONE',  ( 70.33310829152424049, -57.68251784491140199, 156.7550977623263861 ) ) ;
#261=CARTESIAN_POINT ( 'NONE',  ( 15.09152706886165340, -24.11201641507069482, -38.52986768641943627 ) ) ;
#263=CARTESIAN_POINT ( 'NONE',  ( -43.52531999574927113, -60.00000000000001421, 57.80899546987902227 ) ) ;
#266=CARTESIAN_POINT ( 'NONE',  ( -86.58262807044705767, -46.48364591595048267, 190.3714820317854617 ) ) ;
#271=CARTESIAN_POINT ( 'NONE',  ( -8.111617385471721065, -32.51280704258433474, 29.30143946630584040 ) ) ;
#286=CARTESIAN_POINT ( 'NONE',  ( 109.5675852999991662, -29.99999999999999645, 170.1819856699497961 ) ) ;
#307=CARTESIAN_POINT ( 'NONE',  ( -29.44801773522681643, -60.00000000000494538, 45.39224945972397052 ) ) ;
#310=CARTESIAN_POINT ( 'NONE',  ( 107.0172663714162553, -60.00000000000002132, 197.1060892900004546 ) ) ;
#312=CARTESIAN_POINT ( 'NONE',  ( -109.2896413415886485, -29.99999999999996092, 180.5615511752786233 ) ) ;
#313=CARTESIAN_POINT ( 'NONE',  ( 18.09412890605399227, -49.91541348027277536, 32.54674071594174478 ) ) ;
#316=CARTESIAN_POINT ( 'NONE',  ( -41.05697111444229819, -36.06893584801743202, 38.79370462227291227 ) ) ;
#329=CARTESIAN_POINT ( 'NONE',  ( 76.44072697005394446, -30.00000000006936318, 169.7891841772097052 ) ) ;
#330=CARTESIAN_POINT ( 'NONE',  ( -1.544427540536530316E-15, -4.285714285714290916, 25.22241582816893057 ) ) ;
#333=CARTESIAN_POINT ( 'NONE',  ( 90.70948918873676803, -30.00000000000000000, 92.63632137647867637 ) ) ;
#349=CARTESIAN_POINT ( 'NONE',  ( 78.80651474684775337, -38.66927030591594416, 190.4702765846127477 ) ) ;
#372=CARTESIAN_POINT ( 'NONE',  ( 85.94098261277883921, -35.59794438537343808, 185.2097674715711833 ) ) ;
#375=CARTESIAN_POINT ( 'NONE',  ( 87.67975675995961637, -57.66951933457082191, -24.82267382768696251 ) ) ;
#380=CARTESIAN_POINT ( 'NONE',  ( -81.08062976773315711, -30.00000000000001421, 2.674856533068522779 ) ) ;
#396=CARTESIAN_POINT ( 'NONE',  ( -100.1961331157895785, -37.99999999999996447, 190.2810200694672744 ) ) ;
#401=CARTESIAN_POINT ( 'NONE',  ( -58.10004709386434740, -28.99893100057961703, -25.62387168749792465 ) ) ;
#410=CARTESIAN_POINT ( 'NONE',  ( -90.00834054549592622, -60.00000000000000711, -18.84511867618155634 ) ) ;
#412=CARTESIAN_POINT ( 'NONE',  ( 18.45432732700360390, -25.80688170520882352, -30.46384464344198406 ) ) ;
#414=CARTESIAN_POINT ( 'NONE',  ( 101.1404883722410517, -52.73811232283483008, 193.2266567730409292 ) ) ;
#415=CARTESIAN_POINT ( 'NONE',  ( 3.816988791951658744, -18.99760367465201938, 27.04954382783872546 ) ) ;
#417=ORIENTED_EDGE ( 'NONE', *, *, #61734, .F. ) ;
#430=CARTESIAN_POINT ( 'NONE',  ( -14.02841258157142690, -57.67128452586098319, 41.71853563109401364 ) ) ;
#435=CARTESIAN_POINT ( 'NONE',  ( 8.555192725956649369, -60.00000000000006395, -44.87746236044966253 ) ) ;
#436=CARTESIAN_POINT ( 'NONE',  ( -17.10644827616429708, -60.00000000000001421, 42.25319189086976479 ) ) ;
#437=CARTESIAN_POINT ( 'NONE',  ( -51.13187347197568755, -25.65488839008201438, 47.91772828370423554 ) ) ;
#440=CARTESIAN_POINT ( 'NONE',  ( -99.38087883715134296, -60.32317553465453841, 196.1180290444751222 ) ) ;
#446=CARTESIAN_POINT ( 'NONE',  ( 89.04072021948540794, -38.53165156231079891, 200.3084838905402592 ) ) ;
#451=CARTESIAN_POINT ( 'NONE',  ( 85.77043248607724024, -30.00000000000001066, 176.9767547045051685 ) ) ;
#459=CARTESIAN_POINT ( 'NONE',  ( 52.85568683939615653, -25.63927253738310341, 50.79666856344920234 ) ) ;
#465=CARTESIAN_POINT ( 'NONE',  ( -92.64914355384837563, -38.35495843336040878, 40.51828768684245574 ) ) ;
#468=CARTESIAN_POINT ( 'NONE',  ( 98.81766897887224843, -38.35584203838750739, 81.49447246300090342 ) ) ;
#470=CARTESIAN_POINT ( 'NONE',  ( 87.19055186570717808, -60.14788264809187979, 31.77688151689448404 ) ) ;
#475=CARTESIAN_POINT ( 'NONE',  ( 75.45569487463558289, -60.00000000000000711, 184.2290690944641369 ) ) ;
#479=CARTESIAN_POINT ( 'NONE',  ( 59.37731412860715352, -46.43601160270981154, 73.85368140583713625 ) ) ;
#483=CARTESIAN_POINT ( 'NONE',  ( -66.20132703361541360, -30.00000000008030909, 112.2256356094896432 ) ) ;
#493=CARTESIAN_POINT ( 'NONE',  ( 84.47996738200173183, -35.89428493999452030, 177.6417994544143539 ) ) ;
#506=CARTESIAN_POINT ( 'NONE',  ( 47.40960664892755005, -60.00000000000000000, 65.69262840591406416 ) ) ;
#507=STYLED_ITEM ( 'NONE', ( #43636 ), #21377 ) ;
#509=CARTESIAN_POINT ( 'NONE',  ( 11.66830085788263105, -14.19238082999582851, 31.80802733702232388 ) ) ;
#512=CARTESIAN_POINT ( 'NONE',  ( -6.915205664888873116, -19.09113298351051569, 35.17258881450032959 ) ) ;
#524=CARTESIAN_POINT ( 'NONE',  ( 51.46559081915259526, -60.22828912016439773, -31.80537533325271937 ) ) ;
#537=CARTESIAN_POINT ( 'NONE',  ( -101.1691898682323227, -59.99999999999998579, 87.89072118495219854 ) ) ;
#544=CARTESIAN_POINT ( 'NONE',  ( -81.41457456882541521, -53.45414052628666468, 177.1216105972638672 ) ) ;
#551=DIRECTION ( 'NONE',  ( 0.000000000000000000, -0.000000000000000000, 1.000000000000000000 ) ) ;
#557=CARTESIAN_POINT ( 'NONE',  ( 106.6845404271915925, -14.21045842199438525, 180.1433801272770836 ) ) ;
#558=CARTESIAN_POINT ( 'NONE',  ( -106.4002951517535536, -14.21045842199431242, 159.7122570458138284 ) ) ;
#560=CARTESIAN_POINT ( 'NONE',  ( -62.70045667444673398, -49.91596129396690174, 84.84719086326107629 ) ) ;
#563=CARTESIAN_POINT ( 'NONE',  ( 98.58876825478586170, -59.99999999996099831, 57.54132604300040299 ) ) ;
#565=CARTESIAN_POINT ( 'NONE',  ( 8.282570541373461381, -53.39685655951549847, 32.78284559411562071 ) ) ;
#566=CARTESIAN_POINT ( 'NONE',  ( -101.9291513569354350, -37.82052686412928466, 156.3387055009734752 ) ) ;
#576=CARTESIAN_POINT ( 'NONE',  ( -31.79882010337384912, -60.00000000000000000, 44.03261922666757044 ) ) ;
#587=CARTESIAN_POINT ( 'NONE',  ( 87.01147726110801273, -59.99999999999995737, -6.889873257858575961 ) ) ;
#588=CARTESIAN_POINT ( 'NONE',  ( -33.42055755381959159, -49.90302826338683673, 36.47865937243805234 ) ) ;
#590=CARTESIAN_POINT ( 'NONE',  ( 45.25892614766976862, -18.78593732984838738, 38.35189378481528877 ) ) ;
#595=CARTESIAN_POINT ( 'NONE',  ( -83.62175913889684864, -38.78254028569615741, 197.4759616008079206 ) ) ;
#606=CARTESIAN_POINT ( 'NONE',  ( 101.6859781841139920, -60.00000000000000711, 90.91199205705245845 ) ) ;
#613=CARTESIAN_POINT ( 'NONE',  ( -98.40393905160468080, -30.00000000000002132, 190.0006876441828751 ) ) ;
#624=CARTESIAN_POINT ( 'NONE',  ( 84.12715833974999668, -25.58911834355439652, 158.2829670055756139 ) ) ;
#632=CARTESIAN_POINT ( 'NONE',  ( -3.823683356083669160, -59.99999999999998579, -36.85499309513409116 ) ) ;
#636=ORIENTED_EDGE ( 'NONE', *, *, #30453, .T. ) ;
#641=CARTESIAN_POINT ( 'NONE',  ( 86.90843919687902996, -31.72564875591590905, 187.1486806339965199 ) ) ;
#660=CARTESIAN_POINT ( 'NONE',  ( 111.8874950267952499, -57.67106131057807517, 191.6777584699202635 ) ) ;
#666=CARTESIAN_POINT ( 'NONE',  ( -85.92822421211859307, -60.00000000000001421, 200.5408493071717544 ) ) ;
#671=CARTESIAN_POINT ( 'NONE',  ( -86.40833561382129346, -17.71286793965802886, 176.2748628663870250 ) ) ;
#675=( BOUNDED_CURVE ( )  B_SPLINE_CURVE ( 2, ( #7646, #83148, #8722 ),
 .UNSPECIFIED., .F., .F. ) 
 B_SPLINE_CURVE_WITH_KNOTS ( ( 3, 3 ),
 ( 0.000000000000000000, 1.000000000000000000 ),
 .UNSPECIFIED. ) 
 CURVE ( )  GEOMETRIC_REPRESENTATION_ITEM ( )  RATIONAL_B_SPLINE_CURVE ( ( 1.000000000000000000, 1.857142857142858317, 1.000000000000000000 ) ) 
 REPRESENTATION_ITEM ( '' )  );
#681=MECHANICAL_DESIGN_GEOMETRIC_PRESENTATION_REPRESENTATION('',(#33473),#83255);
#682=CARTESIAN_POINT ( 'NONE',  ( -83.23302758787693278, -37.79703903699630985, -5.212852745124933129 ) ) ;
#690=CARTESIAN_POINT ( 'NONE',  ( -47.47011933289886088, -14.21045842199439946, -33.05967481147064291 ) ) ;
#691=CARTESIAN_POINT ( 'NONE',  ( -75.77454316836929138, -42.96621770076318825, 126.5407752095937326 ) ) ;
#693=CARTESIAN_POINT ( 'NONE',  ( 67.17255777190595722, -60.00000000000001421, 138.9727001947898941 ) ) ;
#695=CARTESIAN_POINT ( 'NONE',  ( 114.0253014678331596, -57.67114145616815080, 179.0545312471846557 ) ) ;
#715=CARTESIAN_POINT ( 'NONE',  ( 29.11974998906863377, -25.58802340656078655, 30.36905162638436906 ) ) ;
#724=CARTESIAN_POINT ( 'NONE',  ( -4.871453668401689791E-08, -12.57758911513053413, 32.18678843846154081 ) ) ;
#732=CARTESIAN_POINT ( 'NONE',  ( 92.74300446008587073, -59.99999999999999289, -7.104999719762539634 ) ) ;
#746=CARTESIAN_POINT ( 'NONE',  ( 84.47252406500750510, -45.28770036745071081, -5.144395108280352069 ) ) ;
#756=CARTESIAN_POINT ( 'NONE',  ( 66.93286271214273597, -25.57999363339980192, 84.51815215314977081 ) ) ;
#762=CARTESIAN_POINT ( 'NONE',  ( -113.9839795500101332, -57.67115229137139210, 179.6907882865009185 ) ) ;
#767=CARTESIAN_POINT ( 'NONE',  ( 106.5260298931462160, -60.15149297030401243, 172.9218580926358584 ) ) ;
#781=CARTESIAN_POINT ( 'NONE',  ( 8.568842943812819968, -60.00000000000002132, 39.63676292489870434 ) ) ;
#782=CARTESIAN_POINT ( 'NONE',  ( -95.46185265749743110, -30.00000000000000000, 191.3287857896271191 ) ) ;
#787=CARTESIAN_POINT ( 'NONE',  ( 66.29758781432747128, -57.68034428469994879, 132.1174182233373813 ) ) ;
#789=CARTESIAN_POINT ( 'NONE',  ( 6.955314659475122951, -21.96029575818983304, -38.54528801990171161 ) ) ;
#792=CARTESIAN_POINT ( 'NONE',  ( -41.32172643392373601, -59.99999999999997868, 54.07094069856850638 ) ) ;
#800=CARTESIAN_POINT ( 'NONE',  ( -86.86786266847680338, -50.11060889839860977, 191.7888452930998255 ) ) ;
#803=CARTESIAN_POINT ( 'NONE',  ( -10.33879959434646700, -46.43938644275853278, 31.64223682635364199 ) ) ;
#818=CARTESIAN_POINT ( 'NONE',  ( 109.5811936024938120, -29.99999999999993250, 174.3369879458943217 ) ) ;
#838=CARTESIAN_POINT ( 'NONE',  ( 104.5071319395805176, -60.00000000000001421, 199.6225049996390055 ) ) ;
#839=CARTESIAN_POINT ( 'NONE',  ( -91.09862910994078788, -14.21045842199425380, 197.8399937059591309 ) ) ;
#840=CARTESIAN_POINT ( 'NONE',  ( 19.17772706616747769, -46.43459562844415700, 32.07223590092135623 ) ) ;
#843=CARTESIAN_POINT ( 'NONE',  ( -41.58646596321217004, -49.89193559009187595, 42.49270283408452542 ) ) ;
#857=CARTESIAN_POINT ( 'NONE',  ( 75.18194444360641171, -30.00000000000002132, -17.88826170105039992 ) ) ;
#862=CARTESIAN_POINT ( 'NONE',  ( 81.15738970259414486, -30.00000000000000000, 23.70005024620699885 ) ) ;
#878=CARTESIAN_POINT ( 'NONE',  ( 73.95169229206069872, -38.32650620814214903, 159.8841706720717468 ) ) ;
#901=CARTESIAN_POINT ( 'NONE',  ( 85.35156438166434612, -42.92490405308009827, 186.7151393938520130 ) ) ;
#905=CARTESIAN_POINT ( 'NONE',  ( 93.45479798572706898, -57.65424997624518966, -16.00303676217793836 ) ) ;
#909=CARTESIAN_POINT ( 'NONE',  ( -80.98777655177451607, -30.00000000000000000, 4.227689634766996996 ) ) ;
#916=CARTESIAN_POINT ( 'NONE',  ( 2.500000000000002220, -8.000000000000000000, -14.79019945774903988 ) ) ;
#920=CARTESIAN_POINT ( 'NONE',  ( -55.38798599899330810, -36.77553162784465002, -26.88172734773499428 ) ) ;
#928=CARTESIAN_POINT ( 'NONE',  ( -47.39373218408801591, -26.88155139983819453, -28.62974718684898434 ) ) ;
#941=CARTESIAN_POINT ( 'NONE',  ( -88.00960923584342765, -60.00000000000001421, -21.57056747520839224 ) ) ;
#947=CARTESIAN_POINT ( 'NONE',  ( 100.6323957723895859, -45.27888482481586152, 191.8799519755351071 ) ) ;
#962=CARTESIAN_POINT ( 'NONE',  ( -2.832419495711385515, -59.99999999997088906, -44.99999822275857753 ) ) ;
#967=CARTESIAN_POINT ( 'NONE',  ( -89.52600508066183238, -29.99999999999992539, 22.05060892610427814 ) ) ;
#968=CARTESIAN_POINT ( 'NONE',  ( -29.53202096672922039, -60.00000000000010658, 45.26681583358117678 ) ) ;
#969=CARTESIAN_POINT ( 'NONE',  ( -50.44932658885322496, -29.12285630001392178, 48.00120133921549836 ) ) ;
#977=CARTESIAN_POINT ( 'NONE',  ( 77.84046923451541034, -38.55292655321335360, 187.7603890749101083 ) ) ;
#984=CARTESIAN_POINT ( 'NONE',  ( 85.95410577112431838, -30.00000000000000000, 178.2824706394331713 ) ) ;
#991=CARTESIAN_POINT ( 'NONE',  ( 53.62918214583260834, -18.70049265220536938, 49.64637026124001551 ) ) ;
#996=CARTESIAN_POINT ( 'NONE',  ( -108.7293852557766058, -38.35617175010320068, 143.3098564186624628 ) ) ;
#998=CARTESIAN_POINT ( 'NONE',  ( 108.2472851096807318, -38.35600094170354168, 139.5562851490066976 ) ) ;
#1000=CARTESIAN_POINT ( 'NONE',  ( 93.38248521992973394, -60.15121612030061726, 76.38266335057042511 ) ) ;
#1005=CARTESIAN_POINT ( 'NONE',  ( 73.94769450610063188, -60.00000000000001421, 171.6900336431731375 ) ) ;
#1010=ORIENTED_EDGE ( 'NONE', *, *, #18362, .T. ) ;
#1011=CARTESIAN_POINT ( 'NONE',  ( 62.66139505928889974, -39.48355879806769053, 79.44996130265079159 ) ) ;
#1018=B_SPLINE_CURVE_WITH_KNOTS ( 'NONE', 3,
 ( #64522, #7320, #40232, #97390, #31640, #82820, #99519, #25143, #49371, #82279, #75243, #789, #58559, #48837, #98976, #97936, #24087, #89329, #41294, #32705, #73647, #15422, #50434, #33762, #74180, #17573, #33228, #83346, #89852, #15957, #57459, #8918, #261, #23552, #81725, #7854, #40758, #9436, #65573, #56392, #57999, #48308, #66636, #98459, #24611, #81204, #41824, #25698, #91457, #106014, #90379, #66102, #90923, #17036, #49911, #74711, #3506, #2426, #34306, #51510, #1343, #19205, #45042, #77392, #36446, #28339, #52039, #101666, #69313, #91973, #84953, #53120, #100592, #35370, #11573, #26751, #68785, #34838, #67183, #93581, #92498, #52568, #93042, #44502, #102192, #50965, #75790, #1885, #9991, #84426, #83877, #26227, #27824, #19732, #61217, #67710, #94103, #43959, #18650, #59088, #20270, #18106, #42896, #11040, #60174, #86038, #12112, #60695, #100061, #85492, #59628, #10517, #43433, #76849, #2955, #35913, #76313, #68238, #101131, #27292, #70889, #53639 ),
 .UNSPECIFIED., .F., .F.,
 ( 4, 2, 2, 2, 1, 1, 1, 2, 2, 2, 2, 1, 1, 1, 1, 2, 1, 1, 1, 2, 2, 1, 1, 2, 2, 1, 1, 2, 2, 1, 1, 1, 2, 2, 1, 2, 2, 1, 1, 2, 2, 2, 1, 2, 2, 1, 1, 1, 1, 1, 2, 2, 2, 2, 1, 1, 2, 2, 2, 2, 2, 1, 1, 1, 2, 2, 2, 2, 2, 2, 2, 2, 2, 1, 2, 2, 4 ),
 ( 0.4975915512072818236, 0.5289920792568175711, 0.5309546122599135831, 0.5314452455106876139, 0.5319358787614616446, 0.5329171452630095951, 0.5368422112692015080, 0.5446923432815854449, 0.5603926073063532076, 0.5623551403094491086, 0.5628457735602231393, 0.5633364068109970590, 0.5643176733125451205, 0.5682427393187369224, 0.5760928713311206373, 0.5917931353558881780, 0.5927744018574361284, 0.5932650351082101592, 0.5935103517335971191, 0.5936330100462905435, 0.5937556683589840789, 0.5957182013620797578, 0.5996432673682712267, 0.6074933993806540533, 0.6231936634054197066, 0.6241749299069676571, 0.6246655631577415768, 0.6249108797831286477, 0.6250335380958220721, 0.6251561964085156076, 0.6271187294116120636, 0.6310437954178048647, 0.6388939274301904669, 0.6545941914549617824, 0.6555754579565099549, 0.6560660912072839857, 0.6563114078326710565, 0.6565567244580581274, 0.6585192574611541394, 0.6624443234673463854, 0.6702944554797307664, 0.6859947195044996393, 0.6869759860060478118, 0.6874666192568217316, 0.6875892775695152670, 0.6877119358822088024, 0.6879572525075958733, 0.6899197855106924404, 0.6938448515168855746, 0.7016949835292720650, 0.7173952475540448237, 0.7487957756035905632, 0.7497770421051389578, 0.7507583086066873523, 0.7527208416097839194, 0.7566459076159772756, 0.7644960396283637660, 0.7801963036531369688, 0.8115968317026831524, 0.8120874649534575163, 0.8125780982042316580, 0.8135593647057801636, 0.8155218977088771748, 0.8194469637150711971, 0.8272970957274592418, 0.8429973597522353312, 0.8743978878017877321, 0.8783229538079817544, 0.8822480198141758878, 0.8900981518265640435, 0.9057984158513401329, 0.9371989439008926448, 0.9411240099070868892, 0.9450490759132811336, 0.9528992079256695114, 0.9685994719504462669, 1.000000000000000000 ),
 .UNSPECIFIED. ) ;
#1019=CARTESIAN_POINT ( 'NONE',  ( -83.56878833267877837, -38.35732955512302311, -24.05591699864107014 ) ) ;
#1034=CARTESIAN_POINT ( 'NONE',  ( 86.29990591153305957, -18.16420165869689640, 170.9052643593855407 ) ) ;
#1044=CARTESIAN_POINT ( 'NONE',  ( -13.85649155559951673, -23.71556875437013190, -38.53520488289465362 ) ) ;
#1047=CARTESIAN_POINT ( 'NONE',  ( 54.43804780095958762, -60.00000000000001421, 83.66271491324665988 ) ) ;
#1050=CARTESIAN_POINT ( 'NONE',  ( 16.25118221408220265, -15.62697450488209228, 31.58037248904192040 ) ) ;
#1051=CARTESIAN_POINT ( 'NONE',  ( -15.58516397110831520, -23.01955332296469692, 36.01882826759725020 ) ) ;
#1065=CARTESIAN_POINT ( 'NONE',  ( 18.69608613214362336, -21.77036281612506485, -29.76801956564477081 ) ) ;
#1073=CARTESIAN_POINT ( 'NONE',  ( -102.3034211283397354, -60.00000000000000000, 94.51454494009686869 ) ) ;
#1082=CARTESIAN_POINT ( 'NONE',  ( -84.21860900825973317, -32.47513773243782964, 170.3689398041517506 ) ) ;
#1102=CARTESIAN_POINT ( 'NONE',  ( 109.2895958250431931, -30.00000000000001776, 180.5620058458624442 ) ) ;
#1103=CARTESIAN_POINT ( 'NONE',  ( -114.5103415054848170, -60.00000000000004263, 177.0886483751272351 ) ) ;
#1104=CARTESIAN_POINT ( 'NONE',  ( -60.10583360727262914, -46.44061193372358787, 75.82408097508675837 ) ) ;
#1106=CARTESIAN_POINT ( 'NONE',  ( 94.24355000539094362, -59.99999999999023714, 9.059983527071823417 ) ) ;
#1108=CARTESIAN_POINT ( 'NONE',  ( 5.103942930757551899, -46.43457032225082770, 31.61858307196456508 ) ) ;
#1110=CARTESIAN_POINT ( 'NONE',  ( -103.8570207266811849, -45.26542059613050384, 165.7338815625408870 ) ) ;
#1118=CARTESIAN_POINT ( 'NONE',  ( -24.62151441998206991, -60.00000000000002842, 41.06435363319492637 ) ) ;
#1130=CARTESIAN_POINT ( 'NONE',  ( 101.3080640753006350, -60.00000000000000711, 123.4091116514592414 ) ) ;
#1131=CARTESIAN_POINT ( 'NONE',  ( -28.95202798812907830, -22.11406365714871924, 29.69911553587598974 ) ) ;
#1132=CARTESIAN_POINT ( 'NONE',  ( 2.083846472846741813E-15, -8.673617379884035472E-16, 17.01589776168603407 ) ) ;
#1133=CARTESIAN_POINT ( 'NONE',  ( 46.31338397479791524, -42.98337749828782250, 46.26860352693638845 ) ) ;
#1138=CARTESIAN_POINT ( 'NONE',  ( -76.05157118273700689, -38.38104278720037144, 178.7388989767962926 ) ) ;
#1140=CARTESIAN_POINT ( 'NONE',  ( 2.499999999999997335, -17.18733286780618386, 25.31895441490158660 ) ) ;
#1141=CARTESIAN_POINT ( 'NONE',  ( 54.39905599971908146, -60.00000000000002132, 67.33650783362674019 ) ) ;
#1149=CARTESIAN_POINT ( 'NONE',  ( 108.9289463635939939, -60.00000000000000711, 135.4717115545318507 ) ) ;
#1154=CARTESIAN_POINT ( 'NONE',  ( -88.74229694790767553, -29.99999999999991473, 188.3111048629079676 ) ) ;
#1165=CARTESIAN_POINT ( 'NONE',  ( 80.43333148890700102, -60.41558019800816481, 179.0669228154336281 ) ) ;
#1183=CARTESIAN_POINT ( 'NONE',  ( 87.17785765982114299, -39.07126277053915686, 189.3859673183815175 ) ) ;
#1193=ORIENTED_EDGE ( 'NONE', *, *, #9570, .T. ) ;
#1202=CARTESIAN_POINT ( 'NONE',  ( 111.1322596926232791, -57.67055516791452874, 193.7673871897310960 ) ) ;
#1209=CARTESIAN_POINT ( 'NONE',  ( -86.47079280586432048, -60.00000000000000000, 200.7835212895751908 ) ) ;
#1215=CARTESIAN_POINT ( 'NONE',  ( -85.04835365382125190, -35.79626639874415872, 181.2982241859634769 ) ) ;
#1223=CARTESIAN_POINT ( 'NONE',  ( -85.33191461124319233, -52.75079290529370724, -11.76315019629209502 ) ) ;
#1231=CARTESIAN_POINT ( 'NONE',  ( 31.98199460507809277, -29.99999999999994316, 41.00477363309762779 ) ) ;
#1233=CARTESIAN_POINT ( 'NONE',  ( -41.39220545275658480, -29.99999999999999289, -36.78659115423995729 ) ) ;
#1234=CARTESIAN_POINT ( 'NONE',  ( -67.53808867432213958, -36.01100032359511971, 91.97886330798218069 ) ) ;
#1236=CARTESIAN_POINT ( 'NONE',  ( 72.40119513776858184, -29.99999999999997868, 139.7542682952119719 ) ) ;
#1238=CARTESIAN_POINT ( 'NONE',  ( 95.90504079892977529, -57.67160311991111143, 40.96731908205725148 ) ) ;
#1249=CARTESIAN_POINT ( 'NONE',  ( 25.22241582816893057, -4.285714285714296246, 1.650803255657552482 ) ) ;
#1259=CARTESIAN_POINT ( 'NONE',  ( 31.45708034808273368, -36.01777946066211911, 33.04625429053564289 ) ) ;
#1270=CARTESIAN_POINT ( 'NONE',  ( 2.727751707655953116E-05, -39.99999999999999289, 30.55631662626905154 ) ) ;
#1278=CARTESIAN_POINT ( 'NONE',  ( 92.74240834403246936, -60.00000000000001421, -6.770989331620668850 ) ) ;
#1290=CARTESIAN_POINT ( 'NONE',  ( 85.75148193301690469, -52.74700210787339216, -7.196367400198823816 ) ) ;
#1305=CARTESIAN_POINT ( 'NONE',  ( 73.95717139486286840, -53.37645863163115934, 126.4388429052782641 ) ) ;
#1306=ORIENTED_EDGE ( 'NONE', *, *, #69525, .T. ) ;
#1309=CARTESIAN_POINT ( 'NONE',  ( -94.41342216801938036, -57.67108681604360498, -0.2751897739404595700 ) ) ;
#1314=CARTESIAN_POINT ( 'NONE',  ( 105.4036389870676373, -60.15118156600056665, 186.0926753555523021 ) ) ;
#1316=FACE_OUTER_BOUND ( 'NONE', #66260, .T. ) ;
#1330=CARTESIAN_POINT ( 'NONE',  ( 8.612678335079275271, -60.00000000000001421, 39.63706026226171986 ) ) ;
#1331=CARTESIAN_POINT ( 'NONE',  ( -89.07735706832592371, -30.00000000000000355, 188.8167402104235180 ) ) ;
#1337=CARTESIAN_POINT ( 'NONE',  ( 72.47680246399455939, -57.66589478774676536, 176.7310626288513902 ) ) ;
#1343=CARTESIAN_POINT ( 'NONE',  ( 26.08484759583986090, -28.11660871352809821, -38.33721129155797769 ) ) ;
#1346=CARTESIAN_POINT ( 'NONE',  ( -38.90638701791922216, -60.00000000000000000, 50.62404636354061438 ) ) ;
#1351=CARTESIAN_POINT ( 'NONE',  ( -86.43059533877344336, -24.51652298365282689, 183.3697959701796094 ) ) ;
#1354=CARTESIAN_POINT ( 'NONE',  ( -7.205479452658297035, -49.92090683998103628, 32.20013795827138381 ) ) ;
#1368=CARTESIAN_POINT ( 'NONE',  ( 108.5047413589249032, -30.00000000000003197, 153.5997199437166785 ) ) ;
#1369=CARTESIAN_POINT ( 'NONE',  ( -80.21561207987609521, -49.91266703426506979, 160.3608070185047723 ) ) ;
#1376=VECTOR ( 'NONE', #72788, 1000.000000000000000 ) ;
#1389=CARTESIAN_POINT ( 'NONE',  ( 108.1486474569906591, -60.00000000000001421, 129.9490626958306052 ) ) ;
#1390=CARTESIAN_POINT ( 'NONE',  ( -70.85198506086598513, -59.99999999999993605, 164.3657034848495186 ) ) ;
#1391=CARTESIAN_POINT ( 'NONE',  ( 19.73958029447546281, -22.07186201797325964, 28.03297876132052835 ) ) ;
#1393=CARTESIAN_POINT ( 'NONE',  ( 82.92278159110408353, -38.00000000000002132, -11.29934189521478416 ) ) ;
#1397=CARTESIAN_POINT ( 'NONE',  ( -39.55842790402597586, -25.68830429364345136, 35.29869333941604026 ) ) ;
#1413=CARTESIAN_POINT ( 'NONE',  ( 51.82200911525481501, -29.99999999993400834, 69.17902143724853659 ) ) ;
#1417=CARTESIAN_POINT ( 'NONE',  ( 81.07391525874288618, -30.00000000000001066, 22.29763315622286868 ) ) ;
#1436=CARTESIAN_POINT ( 'NONE',  ( 63.48417968370426223, -38.33937475606958145, 107.9424513483785688 ) ) ;
#1459=CARTESIAN_POINT ( 'NONE',  ( 84.15625878038136420, -57.42679397882895387, 190.9228678296396708 ) ) ;
#1464=CARTESIAN_POINT ( 'NONE',  ( 92.25064720835594301, -57.65936633065353334, -18.85860424735002994 ) ) ;
#1468=CARTESIAN_POINT ( 'NONE',  ( -91.50145128248362880, -30.00000000000000000, 97.27245082254961517 ) ) ;
#1482=CARTESIAN_POINT ( 'NONE',  ( 44.68310115566336549, -26.19546418128159360, -29.27681102373194832 ) ) ;
#1484=CARTESIAN_POINT ( 'NONE',  ( -21.59838042582818574, -49.91976248583917908, 32.92827807905565862 ) ) ;
#1489=CARTESIAN_POINT ( 'NONE',  ( -55.65965000038991661, -28.60422584645425914, -26.38104815732392439 ) ) ;
#1492=CARTESIAN_POINT ( 'NONE',  ( -73.91452718666039345, -47.40888132954707856, -22.31150090410597642 ) ) ;
#1499=CARTESIAN_POINT ( 'NONE',  ( -43.30146564658384278, -60.00000000000000711, -39.13498028926473893 ) ) ;
#1503=CARTESIAN_POINT ( 'NONE',  ( 100.5526317174083886, -45.27816195441151592, 191.9872936527002594 ) ) ;
#1517=CARTESIAN_POINT ( 'NONE',  ( -65.18805258578451856, -57.67964089302213893, 127.3758707571902846 ) ) ;
#1522=CARTESIAN_POINT ( 'NONE',  ( -87.61621634008581339, -14.21045842199436571, -10.69165924380367372 ) ) ;
#1524=CARTESIAN_POINT ( 'NONE',  ( -51.33256727740138103, -39.51242535013955859, 53.05575148282086673 ) ) ;
#1535=CARTESIAN_POINT ( 'NONE',  ( 83.71607977213993479, -38.77881177540385949, 197.5599962973940364 ) ) ;
#1540=CARTESIAN_POINT ( 'NONE',  ( 89.35610039075180566, -30.00000000000000355, 189.1959864005116003 ) ) ;
#1548=CARTESIAN_POINT ( 'NONE',  ( 50.83651537935279663, -56.83343471464645091, 58.27782394269261346 ) ) ;
#1552=CARTESIAN_POINT ( 'NONE',  ( -90.66125720047617165, -38.34385643748635886, 8.951488509635131763 ) ) ;
#1555=CARTESIAN_POINT ( 'NONE',  ( 110.3663729943234273, -38.35605026316035548, 158.8586429886188967 ) ) ;
#1557=CARTESIAN_POINT ( 'NONE',  ( 86.28824347430642661, -52.71555702371639285, 35.16861034268297459 ) ) ;
#1567=CARTESIAN_POINT ( 'NONE',  ( 59.78093605258602139, -25.59731411256743527, 65.24099791815997662 ) ) ;
#1579=STYLED_ITEM ( 'NONE', ( #94435 ), #102410 ) ;
#1582=CARTESIAN_POINT ( 'NONE',  ( 84.05033357701425700, -42.97894289604104046, 182.1071465539960172 ) ) ;
#1587=EDGE_CURVE ( 'NONE', #80603, #84468, #68497, .T. ) ;
#1591=CARTESIAN_POINT ( 'NONE',  ( -27.10508918418226898, -28.49923914006959080, -38.30058658043027719 ) ) ;
#1594=CARTESIAN_POINT ( 'NONE',  ( 43.73109350357475478, -60.00000000000000711, 58.18588980859811244 ) ) ;
#1597=CARTESIAN_POINT ( 'NONE',  ( 13.32650251567469724, -14.66737781475426416, 31.72147017887533949 ) ) ;
#1598=CARTESIAN_POINT ( 'NONE',  ( -44.47534256803313468, -38.31161230092084224, 57.00189278798902137 ) ) ;
#1607=CARTESIAN_POINT ( 'NONE',  ( -40.04958995022020929, -32.98584746607007645, -37.46495261379590858 ) ) ;
#1613=CARTESIAN_POINT ( 'NONE',  ( 40.94348386959299546, -34.58951997928637212, -29.39300229961106581 ) ) ;
#1624=CARTESIAN_POINT ( 'NONE',  ( -103.9547180768905008, -60.00000000000000000, 104.1795586391435791 ) ) ;
#1633=CARTESIAN_POINT ( 'NONE',  ( -83.58190473302030910, -35.99179951698813085, 169.8173457906621877 ) ) ;
#1644=DIRECTION ( 'NONE',  ( -0.000000000000000000, -1.000000000000000000, -0.000000000000000000 ) ) ;
#1651=CARTESIAN_POINT ( 'NONE',  ( 95.23263947746859515, -60.00000000000000000, 30.92889862699057701 ) ) ;
#1652=CARTESIAN_POINT ( 'NONE',  ( -96.06797501213969781, -14.21045842199444564, 198.0637310406154938 ) ) ;
#1654=CARTESIAN_POINT ( 'NONE',  ( -57.59724535810557455, -36.02309701339866166, 64.66795058115701522 ) ) ;
#1657=CARTESIAN_POINT ( 'NONE',  ( 14.02564712579228434, -60.00000000000000000, -44.59530358871077027 ) ) ;
#1658=ORIENTED_EDGE ( 'NONE', *, *, #78441, .T. ) ;
#1659=CARTESIAN_POINT ( 'NONE',  ( 7.080836988906568763, -32.51043656205519028, 29.29839389023845087 ) ) ;
#1661=CARTESIAN_POINT ( 'NONE',  ( -102.7591849661067585, -37.82055285979338777, 174.7714434000731387 ) ) ;
#1667=CARTESIAN_POINT ( 'NONE',  ( -30.55841257715690062, -60.00000000000000000, 43.32489242905028703 ) ) ;
#1679=CARTESIAN_POINT ( 'NONE',  ( 86.88755769280966490, -60.00000000000002132, -3.487599879275609105 ) ) ;
#1681=CARTESIAN_POINT ( 'NONE',  ( -30.23497050974513201, -36.01572923412079774, 32.58813699357081362 ) ) ;
#1684=CARTESIAN_POINT ( 'NONE',  ( 44.36345712709423594, -18.78927584261837680, 37.46452360639921864 ) ) ;
#1689=CARTESIAN_POINT ( 'NONE',  ( -79.44558119418380215, -38.73421251888159844, 191.9379437533855821 ) ) ;
#1693=CARTESIAN_POINT ( 'NONE',  ( 71.97178132980937448, -59.99999999999997868, 122.5137839838858866 ) ) ;
#1701=CARTESIAN_POINT ( 'NONE',  ( 109.9795466629233118, -59.99999999999998579, 143.2892139239177425 ) ) ;
#1706=CARTESIAN_POINT ( 'NONE',  ( -88.09576673204246333, -30.00000000000004619, 187.0129754708849816 ) ) ;
#1722=CARTESIAN_POINT ( 'NONE',  ( 81.94408366797206611, -39.49612657794242665, 160.0900498601838819 ) ) ;
#1736=CARTESIAN_POINT ( 'NONE',  ( 86.98622367796362198, -24.32005973283799705, 186.4277034656624039 ) ) ;
#1757=CARTESIAN_POINT ( 'NONE',  ( -90.88092632026551598, -60.00000000000000711, 202.1567407304452502 ) ) ;
#1761=CARTESIAN_POINT ( 'NONE',  ( -86.20286142257957351, -21.32224752070146323, 177.4588804251129375 ) ) ;
#1769=CARTESIAN_POINT ( 'NONE',  ( -86.97516054069694746, -60.21813631295302827, -9.169555333803231179 ) ) ;
#1777=CARTESIAN_POINT ( 'NONE',  ( 68.01663869669266660, -29.99999999999994316, 119.4502877181080862 ) ) ;
#1780=CARTESIAN_POINT ( 'NONE',  ( -94.55497525217361954, -59.99999999999993605, 22.39874202688834615 ) ) ;
#1781=CARTESIAN_POINT ( 'NONE',  ( -75.39866320161442559, -36.02139133080472533, 119.8324419168973378 ) ) ;
#1783=CARTESIAN_POINT ( 'NONE',  ( 74.04755006654457361, -14.21045842199432307, 133.5027151116648838 ) ) ;
#1785=CARTESIAN_POINT ( 'NONE',  ( 42.88790708626195425, -60.00000000000487432, 61.60924055822990653 ) ) ;
#1797=DIRECTION ( 'NONE',  ( 8.673617379884035472E-17, 0.000000000000000000, 1.000000000000000000 ) ) ;
#1804=CARTESIAN_POINT ( 'NONE',  ( 32.43724909693664671, -42.96036988411042046, 34.72672468598132411 ) ) ;
#1819=CARTESIAN_POINT ( 'NONE',  ( 81.10482683381307822, -59.99999999999998579, -27.27273203502905119 ) ) ;
#1835=CARTESIAN_POINT ( 'NONE',  ( 86.89782702116733049, -60.22147714030394638, -10.09549994484113888 ) ) ;
#1847=CARTESIAN_POINT ( 'NONE',  ( 75.40505029639432166, -56.84436558962719488, 136.0568600359671905 ) ) ;
#1854=CARTESIAN_POINT ( 'NONE',  ( -93.98392372475152001, -57.65316015971099972, -14.13389826495936141 ) ) ;
#1857=DIRECTION ( 'NONE',  ( 8.673617379884035472E-17, 0.000000000000000000, 1.000000000000000000 ) ) ;
#1859=CARTESIAN_POINT ( 'NONE',  ( 102.7627937065603732, -45.28273124251436599, 186.5622291220291231 ) ) ;
#1875=CARTESIAN_POINT ( 'NONE',  ( -85.55157992948998924, -29.99999999999999645, 175.2523284361330411 ) ) ;
#1880=CARTESIAN_POINT ( 'NONE',  ( 71.28015635268077688, -57.68069394656665594, 164.9132661665504145 ) ) ;
#1885=CARTESIAN_POINT ( 'NONE',  ( 43.63372982999123195, -33.99649851277516888, -37.05616739551991401 ) ) ;
#1888=CARTESIAN_POINT ( 'NONE',  ( -43.51410555626048904, -60.00000000000003553, 57.78858762630559909 ) ) ;
#1891=CARTESIAN_POINT ( 'NONE',  ( -86.37715061851159248, -28.18947634940464297, 184.3000902350322008 ) ) ;
#1892=EDGE_LOOP ( 'NONE', ( #55785, #65651, #67466, #82236, #54519 ) ) ;
#1894=CARTESIAN_POINT ( 'NONE',  ( -1.003950229922949244, -39.47608679182096125, 30.46899775823919754 ) ) ;
#1910=CARTESIAN_POINT ( 'NONE',  ( 114.0746655879125200, -59.99999999999997158, 159.9914145889356121 ) ) ;
#1911=CARTESIAN_POINT ( 'NONE',  ( -81.44491109756651781, -39.50132863999797195, 155.9728766274752161 ) ) ;
#1919=CARTESIAN_POINT ( 'NONE',  ( 44.47534377888507606, -38.31160956920668070, 57.00192013341546016 ) ) ;
#1933=CARTESIAN_POINT ( 'NONE',  ( 104.6021310401891782, -60.00000000000001421, 107.7617790675090390 ) ) ;
#1935=CARTESIAN_POINT ( 'NONE',  ( -74.38379737572475392, -29.99999999999997513, 152.0617010018234794 ) ) ;
#1936=CARTESIAN_POINT ( 'NONE',  ( 23.35041436762913136, -29.03775181700250840, 29.66908870611247906 ) ) ;
#1937=CARTESIAN_POINT ( 'NONE',  ( 81.98192093697382177, -38.00000000001091394, -13.86368299876859567 ) ) ;
#1939=CARTESIAN_POINT ( 'NONE',  ( -42.58793732781356312, -53.34669846594655240, 44.38150804302040342 ) ) ;
#1952=CARTESIAN_POINT ( 'NONE',  ( 77.69923846652405075, -29.99999999995701572, 180.6369940188211842 ) ) ;
#1957=CARTESIAN_POINT ( 'NONE',  ( 86.72630328678319245, -30.00000000000000711, 68.79586718995930994 ) ) ;
#1977=CARTESIAN_POINT ( 'NONE',  ( 76.23961518655661962, -38.39423639178605185, 180.1051403894379632 ) ) ;
#1997=CARTESIAN_POINT ( 'NONE',  ( 86.39493283625975550, -17.42247157107316013, 179.1641491230458314 ) ) ;
#2008=CARTESIAN_POINT ( 'NONE',  ( -81.88499113863680634, -29.99999999999998934, 32.76904490412169935 ) ) ;
#2023=CARTESIAN_POINT ( 'NONE',  ( 47.90406143040812736, -27.00548834118202990, -28.50430916820407390 ) ) ;
#2024=CARTESIAN_POINT ( 'NONE',  ( -25.00494464352431123, -42.95926918693982799, 32.33779692008577200 ) ) ;
#2029=CARTESIAN_POINT ( 'NONE',  ( -47.33572465232198567, -26.86733324311558846, -28.64391245175660572 ) ) ;
#2043=CARTESIAN_POINT ( 'NONE',  ( 98.90275021636469432, -37.79594797260679684, 191.9678992726249191 ) ) ;
#2057=CARTESIAN_POINT ( 'NONE',  ( -72.68483858684419374, -57.66063987133676960, 178.6659478268091163 ) ) ;
#2061=CARTESIAN_POINT ( 'NONE',  ( -91.01451176774321539, -60.00000000000003553, -21.65129702257078392 ) ) ;
#2063=CARTESIAN_POINT ( 'NONE',  ( -48.95121697330014143, -60.29223702220649983, 55.82659700904435596 ) ) ;
#2065=ORIENTED_EDGE ( 'NONE', *, *, #46622, .F. ) ;
#2071=CARTESIAN_POINT ( 'NONE',  ( 75.04363187477058261, -38.33897610751563434, 169.9345625973519418 ) ) ;
#2077=CARTESIAN_POINT ( 'NONE',  ( 93.01758433144732408, -30.00000000000000355, 191.1199583869153287 ) ) ;
#2083=CARTESIAN_POINT ( 'NONE',  ( 51.62032401756362532, -29.11406301577443401, 49.91969295013280572 ) ) ;
#2089=CARTESIAN_POINT ( 'NONE',  ( -87.97618656098680390, -38.37017363619033006, -19.60761191172759155 ) ) ;
#2091=CARTESIAN_POINT ( 'NONE',  ( 110.2902390756780733, -38.35602141471932924, 184.0508174503084433 ) ) ;
#2093=CARTESIAN_POINT ( 'NONE',  ( 85.58843428916756579, -52.71458237231213673, 27.65246598081628804 ) ) ;
#2112=CARTESIAN_POINT ( 'NONE',  ( 41.54461699769327510, -26.98090085330345644, 36.99557725161058386 ) ) ;
#2116=CARTESIAN_POINT ( 'NONE',  ( 81.99421977229519598, -57.10237923831468265, 184.9719132876309970 ) ) ;
#2124=CARTESIAN_POINT ( 'NONE',  ( -43.82550334199506636, -34.04363078587874014, -37.02915632368206644 ) ) ;
#2126=CARTESIAN_POINT ( 'NONE',  ( 55.24550608235244908, -60.00000000000001421, 85.96734175474250605 ) ) ;
#2127=CARTESIAN_POINT ( 'NONE',  ( 29.65525632516439103, -32.22057144229324166, 40.37876903116406169 ) ) ;
#2129=CARTESIAN_POINT ( 'NONE',  ( 25.50276709395012631, -19.53775645589208665, 31.59196450892726915 ) ) ;
#2130=CARTESIAN_POINT ( 'NONE',  ( -29.91573279547425557, -32.39459060425171089, 40.52592436092722039 ) ) ;
#2142=UNCERTAINTY_MEASURE_WITH_UNIT (LENGTH_MEASURE( 1.000000000000000082E-05 ), #89430, 'distance_accuracy_value', 'NONE');
#2148=CARTESIAN_POINT ( 'NONE',  ( 44.60714091412001636, -47.40887810288958093, -30.95114210435581725 ) ) ;
#2157=CARTESIAN_POINT ( 'NONE',  ( -92.03933232207216975, -60.00000000000000711, 19.29454771163106486 ) ) ;
#2164=CARTESIAN_POINT ( 'NONE',  ( -81.65897383743494231, -53.48041058990561680, 179.0445688183182824 ) ) ;
#2176=FILL_AREA_STYLE_COLOUR ( '', #68490 ) ;
#2183=CARTESIAN_POINT ( 'NONE',  ( 96.66679845751455957, -59.99999999999993605, 43.68127598107410847 ) ) ;
#2184=CARTESIAN_POINT ( 'NONE',  ( -109.5584880022855998, -59.99999999999993605, 197.6571416747650574 ) ) ;
#2185=CARTESIAN_POINT ( 'NONE',  ( -60.91996879675399157, -32.54063067540256782, 71.34513968801962847 ) ) ;
#2189=CARTESIAN_POINT ( 'NONE',  ( -103.9196169064778985, -60.15914586142672960, 191.0476149618794750 ) ) ;
#2190=CARTESIAN_POINT ( 'NONE',  ( 109.3513501059324255, -30.00000000000000000, 179.6549720493207190 ) ) ;
#2197=CARTESIAN_POINT ( 'NONE',  ( -52.56211189760216485, -60.00000000000001421, 78.42721256930607865 ) ) ;
#2208=CARTESIAN_POINT ( 'NONE',  ( -29.78904055858565059, -39.48797846605977924, 33.06079419891941029 ) ) ;
#2210=CARTESIAN_POINT ( 'NONE',  ( 45.52105560327908762, -39.52714366401688295, 44.31032762745270759 ) ) ;
#2213=CARTESIAN_POINT ( 'NONE',  ( -86.93198415347136176, -38.59779612754854128, 199.5132169019792912 ) ) ;
#2215=CARTESIAN_POINT ( 'NONE',  ( 79.34455092495568351, -38.35611032209237692, -26.90405483085318039 ) ) ;
#2217=CARTESIAN_POINT ( 'NONE',  ( 20.85090658074709324, -60.00000000000000711, 34.52371470500510497 ) ) ;
#2225=CARTESIAN_POINT ( 'NONE',  ( 110.0463146278414683, -60.00000000000000000, 143.8199656869762464 ) ) ;
#2233=CARTESIAN_POINT ( 'NONE',  ( -91.54332115524630353, -30.00000000000000000, 97.26594229145295856 ) ) ;
#2245=CARTESIAN_POINT ( 'NONE',  ( 80.88940320574509713, -49.91559681877727428, 166.5735459904898619 ) ) ;
#2262=CARTESIAN_POINT ( 'NONE',  ( 86.53852868639081919, -17.00621220630052477, 184.4929596998693739 ) ) ;
#2285=CARTESIAN_POINT ( 'NONE',  ( -76.81430757441975743, -59.99999999999999289, 189.9012580596375699 ) ) ;
#2291=CARTESIAN_POINT ( 'NONE',  ( -85.21415449681325072, -35.76165008134817214, 182.1678819788450880 ) ) ;
#2299=CARTESIAN_POINT ( 'NONE',  ( -85.54679910649467445, -52.71797009601630890, -1.685581303667236908 ) ) ;
#2309=CARTESIAN_POINT ( 'NONE',  ( 69.27313422356952799, -59.99999999999999289, 151.6321682696899984 ) ) ;
#2311=CARTESIAN_POINT ( 'NONE',  ( -88.92180072262880230, -30.00000000000001421, -15.18793788064705197 ) ) ;
#2313=CARTESIAN_POINT ( 'NONE',  ( -71.21937153047667834, -36.01495328744242386, 103.8040231744988802 ) ) ;
#2315=CARTESIAN_POINT ( 'NONE',  ( 72.11378188144121282, -59.99999999999999289, 177.1381934468311670 ) ) ;
#2318=CARTESIAN_POINT ( 'NONE',  ( 11.20998319195465776, -57.67118707559646396, -44.35019014734187692 ) ) ;
#2320=ORIENTED_EDGE ( 'NONE', *, *, #103922, .F. ) ;
#2330=CARTESIAN_POINT ( 'NONE',  ( -42.13804600684559887, -59.99999999998057376, 60.14875204916594953 ) ) ;
#2347=CARTESIAN_POINT ( 'NONE',  ( 33.64991883386763050, -60.30412654068202727, 38.51323943821249429 ) ) ;
#2348=CARTESIAN_POINT ( 'NONE',  ( 20.16952962162617879, -4.285714285716217375, 15.50035291838605467 ) ) ;
#2349=ORIENTED_EDGE ( 'NONE', *, *, #84634, .T. ) ;
#2360=CARTESIAN_POINT ( 'NONE',  ( 91.76855862128167018, -60.00000000000000000, -14.78760871838603741 ) ) ;
#2367=CARTESIAN_POINT ( 'NONE',  ( -80.67925139857744909, -29.99999999998416200, 191.9698402685723977 ) ) ;
#2374=CARTESIAN_POINT ( 'NONE',  ( 83.39873523156931867, -45.27648495923967431, -13.67455449466119966 ) ) ;
#2388=CARTESIAN_POINT ( 'NONE',  ( 76.97083215510561160, -29.07873089524411725, 121.1780571378874640 ) ) ;
#2394=CARTESIAN_POINT ( 'NONE',  ( -93.89173215636174064, -57.65323629495627245, -14.51111636511549996 ) ) ;
#2400=CARTESIAN_POINT ( 'NONE',  ( 106.0465130611873974, -60.15137259862576968, 181.9139942087800534 ) ) ;
#2408=CARTESIAN_POINT ( 'NONE',  ( 96.81745522565726958, -37.99999999999980815, 192.8977754549547967 ) ) ;
#2417=CARTESIAN_POINT ( 'NONE',  ( -85.27768309077019637, -30.00000000000000711, 172.8990738933071327 ) ) ;
#2422=CARTESIAN_POINT ( 'NONE',  ( 78.99859466470238090, -57.50609917691477335, 197.8297617738492704 ) ) ;
#2426=CARTESIAN_POINT ( 'NONE',  ( 24.48579885659522404, -27.51483317846157206, -38.38701603259436013 ) ) ;
#2428=CARTESIAN_POINT ( 'NONE',  ( -40.70962269998187821, -59.99999999999999289, 53.12857981522989803 ) ) ;
#2431=CARTESIAN_POINT ( 'NONE',  ( -86.11174981640101578, -53.81160830264160211, 192.0627294854906211 ) ) ;
#2434=CARTESIAN_POINT ( 'NONE',  ( -3.040491613002718196, -42.95758431452577497, 31.04430139814011724 ) ) ;
#2449=CARTESIAN_POINT ( 'NONE',  ( 95.99465422657044655, -14.21045842199428222, 88.91344185009528189 ) ) ;
#2450=CARTESIAN_POINT ( 'NONE',  ( -78.67339649595623996, -56.84650683190278642, 157.0027717221539660 ) ) ;
#2452=CARTESIAN_POINT ( 'NONE',  ( 80.00000000000000000, -60.00000000000000000, -21.09707704303352926 ) ) ;
#2458=MECHANICAL_DESIGN_GEOMETRIC_PRESENTATION_REPRESENTATION('',(#35220),#33445);
#2469=CARTESIAN_POINT ( 'NONE',  ( 92.47524522096102828, -60.00000000000000000, -0.8168806114483707637 ) ) ;
#2470=CARTESIAN_POINT ( 'NONE',  ( -77.72307990868957006, -60.00000000000013500, 197.5629538559897469 ) ) ;
#2471=CARTESIAN_POINT ( 'NONE',  ( 23.10491929295638869, -60.35294240224059337, 34.93602920169672643 ) ) ;
#2475=CARTESIAN_POINT ( 'NONE',  ( -42.51571275536706196, -22.24532317153370187, 36.74399635000383313 ) ) ;
#2487=CARTESIAN_POINT ( 'NONE',  ( 95.78288065149338593, -30.00000000000000711, 191.3120139408427463 ) ) ;
#2491=CARTESIAN_POINT ( 'NONE',  ( 81.26282277270112786, -30.00000000000000000, 25.32439451913061390 ) ) ;
#2511=CARTESIAN_POINT ( 'NONE',  ( 77.13440917754967074, -38.47324727432590663, 185.0008781656527788 ) ) ;
#2536=CARTESIAN_POINT ( 'NONE',  ( 86.21552468565893435, -35.53747912697327394, 186.1477005681167043 ) ) ;
#2547=CARTESIAN_POINT ( 'NONE',  ( -90.19056545505544875, -30.00000000000000000, 89.60777242590961578 ) ) ;
#2550=CARTESIAN_POINT ( 'NONE',  ( -2.499999999999963141, -18.83381654053417620, 27.02533567785737034 ) ) ;
#2554=CARTESIAN_POINT ( 'NONE',  ( 22.68445741908610458, -19.34685978730561828, -33.34832530438864495 ) ) ;
#2555=CARTESIAN_POINT ( 'NONE',  ( -22.30031860479850891, -32.51783567543096609, 30.11000684557585316 ) ) ;
#2559=CARTESIAN_POINT ( 'NONE',  ( -21.50683366985505529, -46.43907677105036669, 32.33084832063442349 ) ) ;
#2560=CARTESIAN_POINT ( 'NONE',  ( -47.12618484245456330, -26.81580167950459170, -28.69496456390906758 ) ) ;
#2577=CARTESIAN_POINT ( 'NONE',  ( 98.60524411875431383, -37.77932106365781095, 192.1824683179078761 ) ) ;
#2591=CARTESIAN_POINT ( 'NONE',  ( -61.39119026585446193, -59.99999999998052402, -37.72981658969594321 ) ) ;
#2596=CARTESIAN_POINT ( 'NONE',  ( -89.66254536497091010, -30.00000000000007461, 1.293233577394788725 ) ) ;
#2598=CARTESIAN_POINT ( 'NONE',  ( -49.28595117375603962, -56.83155379549049968, 55.29437192555985803 ) ) ;
#2610=CARTESIAN_POINT ( 'NONE',  ( 109.6017100556251052, -29.99999999998994582, 173.2570657943911101 ) ) ;
#2615=CARTESIAN_POINT ( 'NONE',  ( 86.72120758077696223, -30.00000000000000355, 182.5673864577368306 ) ) ;
#2620=ORIENTED_EDGE ( 'NONE', *, *, #83208, .T. ) ;
#2622=CARTESIAN_POINT ( 'NONE',  ( 51.04619832299282223, -29.11810138070153897, 48.95650004900380736 ) ) ;
#2628=CARTESIAN_POINT ( 'NONE',  ( -85.44393953219409354, -38.35987823094075111, -22.43841095247546846 ) ) ;
#2631=CARTESIAN_POINT ( 'NONE',  ( 106.4348537030854942, -38.37040168822593955, 195.7536246194525233 ) ) ;
#2633=CARTESIAN_POINT ( 'NONE',  ( 86.97191705326012823, -60.14714815928688552, 29.24646490916457253 ) ) ;
#2651=( NAMED_UNIT ( * ) SI_UNIT ( $, .STERADIAN. ) SOLID_ANGLE_UNIT ( ) );
#2654=CARTESIAN_POINT ( 'NONE',  ( 82.22664787600508873, -53.54757062451568572, 182.7241912098365333 ) ) ;
#2655=EDGE_CURVE ( 'NONE', #74273, #71336, #85851, .T. ) ;
#2660=CARTESIAN_POINT ( 'NONE',  ( -87.99615528876792325, -45.26544677176889309, 58.11335563032940144 ) ) ;
#2664=CARTESIAN_POINT ( 'NONE',  ( -25.04254350662498396, -27.72387814640729786, -38.37349969813231354 ) ) ;
#2666=CARTESIAN_POINT ( 'NONE',  ( 51.08421898080068502, -60.00000000000001421, 74.55324466403668282 ) ) ;
#2668=CARTESIAN_POINT ( 'NONE',  ( 29.78312297350667492, -32.30613403230655933, 40.45056335855814211 ) ) ;
#2670=CARTESIAN_POINT ( 'NONE',  ( -4.871453668401689791E-08, -12.57758911513053413, 32.18678843846154081 ) ) ;
#2671=CARTESIAN_POINT ( 'NONE',  ( -29.94728110026810342, -32.41561811289711414, 40.54398215057806709 ) ) ;
#2690=CARTESIAN_POINT ( 'NONE',  ( 29.14228781303362936, -60.22829445328315501, -35.25039815003416521 ) ) ;
#2696=EDGE_CURVE ( 'NONE', #94469, #35136, #82320, .T. ) ;
#2700=CARTESIAN_POINT ( 'NONE',  ( -93.93600680990350327, -59.99999999999999289, 40.82566283017103359 ) ) ;
#2707=CARTESIAN_POINT ( 'NONE',  ( -84.32039038253493857, -32.46127920068834527, 171.3701678123200907 ) ) ;
#2720=CARTESIAN_POINT ( 'NONE',  ( -72.13200937809398283, -57.67118076099990986, -33.88443861317198724 ) ) ;
#2725=CARTESIAN_POINT ( 'NONE',  ( 90.94603201905546541, -14.21045842199432663, 57.96280492189741551 ) ) ;
#2726=CARTESIAN_POINT ( 'NONE',  ( -105.0772696006729632, -59.99999999999994316, 202.2127603465211223 ) ) ;
#2727=CARTESIAN_POINT ( 'NONE',  ( -59.57600778041714307, -42.96618104056574339, 72.74187206144701179 ) ) ;
#2731=CARTESIAN_POINT ( 'NONE',  ( -102.8035547126978884, -37.82057828177080694, 172.5329001939995237 ) ) ;
#2736=CARTESIAN_POINT ( 'NONE',  ( -42.86245485551749823, -60.00000000000001421, 56.60147671463673191 ) ) ;
#2741=CARTESIAN_POINT ( 'NONE',  ( 10.38447319516995115, -0.000000000000000000, 13.52495681779773484 ) ) ;
#2749=CARTESIAN_POINT ( 'NONE',  ( -30.13293448531765151, -22.12503195913166110, 30.04311387844209946 ) ) ;
#2751=CARTESIAN_POINT ( 'NONE',  ( 43.22147467150615796, -46.43435577793969316, 43.42933933853470307 ) ) ;
#2755=CARTESIAN_POINT ( 'NONE',  ( -97.76083068359459105, -38.48065516424733801, 201.0208589095672949 ) ) ;
#2760=CARTESIAN_POINT ( 'NONE',  ( 43.68778998544354408, -60.00000000000005684, 47.36496327955963181 ) ) ;
#2770=CARTESIAN_POINT ( 'NONE',  ( 112.0087755282777380, -60.00000000000000000, 164.6420903483667360 ) ) ;
#2776=CARTESIAN_POINT ( 'NONE',  ( -59.44538817165069844, -38.34335046808914882, 94.60634109114953105 ) ) ;
#2789=CARTESIAN_POINT ( 'NONE',  ( 81.31019069296409896, -49.92858064726677014, 170.6618749361798280 ) ) ;
#2806=CARTESIAN_POINT ( 'NONE',  ( 86.80848714680104194, -20.64835433331844783, 185.6727037537062586 ) ) ;
#2827=CARTESIAN_POINT ( 'NONE',  ( -93.50040392359746022, -60.00000000000000000, 202.5177011504292466 ) ) ;
#2833=CARTESIAN_POINT ( 'NONE',  ( -82.95741313463533118, -57.28139562845189658, 188.3880023493264275 ) ) ;
#2841=CARTESIAN_POINT ( 'NONE',  ( -85.42014498610673456, -52.71254651111112111, 0.1204113182908394392 ) ) ;
#2847=CARTESIAN_POINT ( 'NONE',  ( 72.11378188144121282, -59.99999999999999289, 177.1381934468311670 ) ) ;
#2848=CARTESIAN_POINT ( 'NONE',  ( -87.24749885984873288, -14.21045842199425024, -0.3946065656837255964 ) ) ;
#2849=CARTESIAN_POINT ( 'NONE',  ( -72.91763775797275571, -42.96435045428120958, 114.3462633838142892 ) ) ;
#2851=CARTESIAN_POINT ( 'NONE',  ( 109.5593579388806091, -60.00000000000008527, 197.6560947019162597 ) ) ;
#2853=CARTESIAN_POINT ( 'NONE',  ( 51.50543603504199552, -57.67116266638129218, -39.62106952943562277 ) ) ;
#2864=CARTESIAN_POINT ( 'NONE',  ( -35.02057590403620679, -60.00000000000246558, 49.66482031158606958 ) ) ;
#2867=CARTESIAN_POINT ( 'NONE',  ( -10.00000000000000178, -15.00000000000000000, -9.999999999999998224 ) ) ;
#2874=CARTESIAN_POINT ( 'NONE',  ( 33.01644511546025740, -60.30961634571765018, 38.16996237056868324 ) ) ;
#2887=CARTESIAN_POINT ( 'NONE',  ( 92.56471944205797797, -60.00000000000000711, -2.224637919256570395 ) ) ;
#2895=CARTESIAN_POINT ( 'NONE',  ( -93.89469422640124208, -30.00000000003503686, 199.9082004840001332 ) ) ;
#2901=CARTESIAN_POINT ( 'NONE',  ( 83.19333843231504488, -37.80199420799200993, -9.185050932785989275 ) ) ;
#2918=CARTESIAN_POINT ( 'NONE',  ( 76.37327748893468993, -36.02034588710548491, 123.8589219231648855 ) ) ;
#2926=CARTESIAN_POINT ( 'NONE',  ( -104.5387911149144600, -57.64184148030879840, 201.9936694370400971 ) ) ;
#2930=CARTESIAN_POINT ( 'NONE',  ( 104.0473560679520801, -45.28269839500234895, 172.6637801801720684 ) ) ;
#2948=CARTESIAN_POINT ( 'NONE',  ( -88.78165138298567172, -30.00000000000001066, 188.3707320087108030 ) ) ;
#2951=CARTESIAN_POINT ( 'NONE',  ( 81.60669281017756305, -57.51821468741594856, 200.2139519186157770 ) ) ;
#2955=CARTESIAN_POINT ( 'NONE',  ( 66.88170049462542011, -38.03301857054354684, -32.23619581494182995 ) ) ;
#2958=CARTESIAN_POINT ( 'NONE',  ( -51.02129726669660670, -60.00000000000000000, 74.38172674847689336 ) ) ;
#2963=CARTESIAN_POINT ( 'NONE',  ( -85.92024107957429635, -53.82049793324690512, 191.8561986361768277 ) ) ;
#2966=CARTESIAN_POINT ( 'NONE',  ( -4.115265312743041193, -56.88410095382541698, 33.36240466207844690 ) ) ;
#2984=CARTESIAN_POINT ( 'NONE',  ( 95.66379843407523254, -59.99999999999997158, 35.18487050012404893 ) ) ;
#2985=CARTESIAN_POINT ( 'NONE',  ( -82.92168442201257506, -18.68762057716829617, 141.1249244015832005 ) ) ;
#2990=CARTESIAN_POINT ( 'NONE',  ( 38.37663786125177978, -57.69558054003382352, 53.18690643716654876 ) ) ;
#3011=CARTESIAN_POINT ( 'NONE',  ( 47.02104799127375401, -59.99999999999997868, -38.48628389369286396 ) ) ;
#3012=CARTESIAN_POINT ( 'NONE',  ( -76.70274796309844589, -29.99999999999996447, 172.7051753936532066 ) ) ;
#3013=CARTESIAN_POINT ( 'NONE',  ( 22.29962909612223498, -32.51552189962478678, 30.10951381722811249 ) ) ;
#3015=CARTESIAN_POINT ( 'NONE',  ( -33.84603987176726747, -46.43407376650471718, 36.05494947502590009 ) ) ;
#3030=CARTESIAN_POINT ( 'NONE',  ( 98.32497725137756106, -30.00000000000000711, 190.1228518036747630 ) ) ;
#3035=CARTESIAN_POINT ( 'NONE',  ( 82.00736216671209888, -29.99999999999999645, 34.01753071249959959 ) ) ;
#3053=CARTESIAN_POINT ( 'NONE',  ( 72.53904111559185708, -38.32615141910980583, 149.3261510640276697 ) ) ;
#3077=CARTESIAN_POINT ( 'NONE',  ( 86.23413113060379942, -28.25917168182434125, 183.4403566737863969 ) ) ;
#3083=CARTESIAN_POINT ( 'NONE',  ( 9.953686224012043837, -16.20368524395693655, -34.82632026490023236 ) ) ;
#3087=CARTESIAN_POINT ( 'NONE',  ( -87.74588082317708881, -29.99999999999998934, 75.10738559680038406 ) ) ;
#3090=CARTESIAN_POINT ( 'NONE',  ( 0.009260245579808886948, -57.67120202535643614, 41.61186695095138788 ) ) ;
#3100=CARTESIAN_POINT ( 'NONE',  ( 56.00069051983414425, -28.66156656293939875, -26.27684122581554860 ) ) ;
#3103=CARTESIAN_POINT ( 'NONE',  ( -25.83922611890834986, -32.52481888390300924, 30.74902383434352515 ) ) ;
#3106=CARTESIAN_POINT ( 'NONE',  ( -16.37657220773485989, -18.58804370566180353, 27.19384971940823448 ) ) ;
#3122=CARTESIAN_POINT ( 'NONE',  ( 100.8769579830505592, -45.28053191621518891, 191.5263513813913789 ) ) ;
#3124=SURFACE_SIDE_STYLE ('',( #77006 ) ) ;
#3138=CARTESIAN_POINT ( 'NONE',  ( -47.54236909243191889, -59.99999999996124700, -40.79170333304822549 ) ) ;
#3140=AXIS2_PLACEMENT_3D ( 'NONE', #79796, #80849, #64683 ) ;
#3145=CARTESIAN_POINT ( 'NONE',  ( -95.02173393737120932, -60.00000000000007105, -3.234914688897275070 ) ) ;
#3147=CARTESIAN_POINT ( 'NONE',  ( -47.88475624650544660, -56.82326849868364604, 52.80298889764087278 ) ) ;
#3158=CARTESIAN_POINT ( 'NONE',  ( 90.08055447028598905, -30.00000000002782841, -8.126024404956387670 ) ) ;
#3162=CARTESIAN_POINT ( 'NONE',  ( 89.34851512668548423, -30.00000000000000355, 189.1863861107025286 ) ) ;
#3168=CARTESIAN_POINT ( 'NONE',  ( 54.15937250249886148, -32.56281511288196384, 55.81529859889931089 ) ) ;
#3172=CARTESIAN_POINT ( 'NONE',  ( -91.47181070595220831, -38.38037305410311717, -6.014377416796397924 ) ) ;
#3176=CARTESIAN_POINT ( 'NONE',  ( 108.3599484846729695, -38.35745757732994576, 191.9951766408777019 ) ) ;
#3178=CARTESIAN_POINT ( 'NONE',  ( 85.12609559102118340, -52.70885996367997706, 4.505813679903315716 ) ) ;
#3200=CARTESIAN_POINT ( 'NONE',  ( 16.05552553557446060, -15.52039114152552735, 31.56705366141566316 ) ) ;
#3206=CARTESIAN_POINT ( 'NONE',  ( 83.88774053950423593, -50.14893828415973331, 186.5792076936381534 ) ) ;
#3211=CARTESIAN_POINT ( 'NONE',  ( -88.45092629199805856, -52.70969016536442098, 52.48989280492887843 ) ) ;
#3216=CARTESIAN_POINT ( 'NONE',  ( -23.57853350939547354, -27.17268373882357224, -38.41116532901637726 ) ) ;
#3217=CARTESIAN_POINT ( 'NONE',  ( 23.81365055911821216, -60.00000000000000000, 40.86761593640069634 ) ) ;
#3218=CARTESIAN_POINT ( 'NONE',  ( 35.44951030812982395, -35.74875123850512892, 44.64175081870536133 ) ) ;
#3221=CARTESIAN_POINT ( 'NONE',  ( 45.12508949386340618, -28.33865188907569532, 40.20852945013428581 ) ) ;
#3235=CARTESIAN_POINT ( 'NONE',  ( -18.94239008060200291, -34.58964377142442004, -31.89223463875953613 ) ) ;
#3237=ORIENTED_EDGE ( 'NONE', *, *, #21665, .T. ) ;
#3249=CARTESIAN_POINT ( 'NONE',  ( -93.42203525153540511, -59.99999999999998579, 36.32810924189196555 ) ) ;
#3256=CARTESIAN_POINT ( 'NONE',  ( -83.91177200283225091, -32.50788753430207834, 167.3447669332486214 ) ) ;
#3267=CARTESIAN_POINT ( 'NONE',  ( -80.00483118099813851, -57.67118036264142944, -30.22182926596574148 ) ) ;
#3274=CARTESIAN_POINT ( 'NONE',  ( 94.62301060094824834, -14.21045842199438525, 80.84833697736402769 ) ) ;
#3276=CARTESIAN_POINT ( 'NONE',  ( -77.72307990868957006, -60.00000000000013500, 197.5629538559897469 ) ) ;
#3277=CARTESIAN_POINT ( 'NONE',  ( -54.36348728659673668, -49.91102849765379545, 63.10952282595231821 ) ) ;
#3281=CARTESIAN_POINT ( 'NONE',  ( -102.8828697075181680, -52.71162264969420619, 190.2909648261160953 ) ) ;
#3285=CARTESIAN_POINT ( 'NONE',  ( -22.53767922124185574, -59.99999999999998579, 40.61082087230103355 ) ) ;
#3295=CARTESIAN_POINT ( 'NONE',  ( -30.66975189450997163, -32.54514858898122043, 32.11485851461230112 ) ) ;
#3297=CARTESIAN_POINT ( 'NONE',  ( 47.71926515674179115, -36.06417799759196186, 46.18337568543712734 ) ) ;
#3301=CARTESIAN_POINT ( 'NONE',  ( -85.95206158600240087, -38.64469160019880434, 199.0332504256811603 ) ) ;
#3303=CARTESIAN_POINT ( 'NONE',  ( 84.58395683528345899, -38.35848370293111032, -23.21156260195221677 ) ) ;
#3312=CARTESIAN_POINT ( 'NONE',  ( 106.5873745654861580, -59.99999999999999289, 197.6168797630004406 ) ) ;
#3318=CARTESIAN_POINT ( 'NONE',  ( -80.60042778259895613, -30.00000000000000711, -12.84585300385902684 ) ) ;
#3320=CARTESIAN_POINT ( 'NONE',  ( -85.21905093902094563, -38.68651908961214758, 198.6209921461202725 ) ) ;
#3334=CARTESIAN_POINT ( 'NONE',  ( 85.11568698743305106, -25.45901852875848093, 167.9889055482516369 ) ) ;
#3347=B_SPLINE_SURFACE_WITH_KNOTS ( 'NONE', 3, 1, ( 
 ( #38181, #80180, #58983 ),
 ( #42245, #91871, #105006 ),
 ( #31148, #55369, #14374 ),
 ( #72626, #88817, #15990 ),
 ( #88299, #32191, #65070 ),
 ( #97419, #6287, #56426 ),
 ( #31668, #30609, #40262 ),
 ( #75135, #23046, #23580 ),
 ( #22526, #48868, #55882 ),
 ( #39224, #1231, #48340 ),
 ( #38690, #72099, #81760 ),
 ( #106040, #47805, #34201 ),
 ( #80708, #89359, #9335 ),
 ( #79659, #71556, #6826 ),
 ( #73136, #39745, #46763 ),
 ( #81235, #97968, #67073 ),
 ( #63498, #24118, #96396 ),
 ( #26129, #18536, #100485 ),
 ( #44934, #44389, #69208 ),
 ( #68678, #19089, #67606 ),
 ( #75678, #26643, #52460 ),
 ( #85931, #28778, #12001 ),
 ( #93478, #28238, #60589 ),
 ( #101019, #102076, #84842 ),
 ( #59516, #1777, #11462 ),
 ( #92925, #36338, #84312 ),
 ( #77818, #51400, #92389 ),
 ( #10409, #61659, #34735 ),
 ( #17997, #76205, #43323 ),
 ( #2309, #35256, #101558 ),
 ( #60065, #61109, #19627 ),
 ( #9874, #53008, #3928 ),
 ( #68123, #20158, #27175 ),
 ( #93996, #43846, #51929 ),
 ( #10925, #76736, #36860 ),
 ( #2847, #69729, #35800 ),
 ( #102619, #27715, #85378 ),
 ( #77285, #50858, #3395 ),
 ( #83764, #42786, #87509 ),
 ( #46503, #22788, #104196 ),
 ( #6029, #79398, #103156 ),
 ( #39490, #96126, #37393 ),
 ( #95593, #4991, #94548 ),
 ( #38952, #71829, #86467 ),
 ( #37921, #20699, #30885 ),
 ( #72365, #105271, #5514 ),
 ( #53538, #12525, #70783 ),
 ( #14117, #78863, #31416 ),
 ( #38438, #95075, #96652 ),
 ( #45459, #103678, #78333 ),
 ( #62701, #21208, #70255 ),
 ( #14642, #47019, #104734 ),
 ( #71303, #21729, #29301 ),
 ( #4450, #62190, #22259 ),
 ( #13588, #54038, #86983 ),
 ( #13052, #63764, #29823 ),
 ( #55624, #30340, #54570 ),
 ( #55106, #88561, #45984 ),
 ( #63233, #47550, #88037 ),
 ( #80447, #79921, #6557 ),
 ( #97691, #75006, #48076 ),
 ( #64809, #42120, #90684 ),
 ( #23855, #97165, #25456 ),
 ( #80976, #1102, #557 ),
 ( #49680, #82587, #7093 ),
 ( #56700, #73952, #83116 ),
 ( #15187, #24905, #64293 ),
 ( #7612, #16252, #41068 ),
 ( #74482, #81493, #58310 ),
 ( #91235, #33004, #32 ),
 ( #89623, #33525, #65871 ),
 ( #73410, #17341, #57228 ),
 ( #40009, #16794, #66398 ),
 ( #105792, #41598, #40531 ),
 ( #9212, #98750, #72880 ),
 ( #65342, #57759, #15722 ),
 ( #31931, #50216, #23312 ),
 ( #48607, #106307, #32472 ),
 ( #8161, #90147, #98232 ),
 ( #8692, #99279, #24388 ),
 ( #56148, #89091, #49136 ),
 ( #82037, #92803, #91753 ),
 ( #44809, #28116, #84190 ),
 ( #10805, #9740, #44267 ),
 ( #60990, #100359, #93877 ),
 ( #76612, #99828, #34610 ),
 ( #51267, #93352, #43197 ),
 ( #27053, #18411, #18963 ),
 ( #43722, #17872, #52338 ),
 ( #42657, #35675, #3274 ),
 ( #36215, #11881, #52880 ),
 ( #34076, #77158, #85251 ),
 ( #26000, #10286, #2725 ),
 ( #35132, #11334, #76082 ),
 ( #2183, #75556, #19503 ),
 ( #100887, #68551, #69082 ),
 ( #101438, #27590, #50725 ),
 ( #1651, #101955, #68002 ),
 ( #20036, #60472, #85807 ),
 ( #84718, #59937, #83636 ),
 ( #77697, #66948, #51807 ),
 ( #58861, #67481, #26523 ),
 ( #59395, #92256, #54440 ),
 ( #103556, #4866, #14516 ),
 ( #22128, #53422, #104074 ),
 ( #13993, #70663, #46386 ),
 ( #88443, #63646, #104608 ),
 ( #46900, #21093, #30760 ),
 ( #96535, #79276, #5397 ),
 ( #4332, #79805, #38319 ),
 ( #3807, #38833, #71180 ),
 ( #62579, #71697, #13464 ),
 ( #54980, #95463, #12406 ),
 ( #55504, #30217, #86340 ),
 ( #37802, #53929, #36746 ),
 ( #87911, #5902, #102501 ),
 ( #63102, #22666, #29705 ),
 ( #86860, #45337, #78730 ),
 ( #96004, #21609, #87390 ),
 ( #47427, #69608, #28644 ),
 ( #94421, #61529, #78216 ),
 ( #20584, #37265, #70130 ),
 ( #103036, #29193, #62069 ),
 ( #94956, #12936, #45857 ),
 ( #40405, #7489, #41467 ),
 ( #74357, #39368, #49011 ),
 ( #16128, #49556, #56577 ),
 ( #91107, #81912, #98632 ),
 ( #73832, #72246, #90556 ),
 ( #8028, #24783, #58181 ),
 ( #435, #106182, #106726 ),
 ( #33405, #17215, #31803 ),
 ( #64691, #88965, #47950 ),
 ( #32346, #15595, #16665 ),
 ( #24260, #48486, #105148 ),
 ( #66275, #40939, #97563 ),
 ( #89501, #15063, #82463 ),
 ( #23187, #6970, #23725 ),
 ( #32876, #99163, #80857 ),
 ( #39888, #80318, #65752 ),
 ( #72761, #6431, #25320 ),
 ( #31290, #8566, #105668 ),
 ( #57632, #56034, #98110 ),
 ( #90022, #64177, #65216 ),
 ( #97047, #81381, #73287 ),
 ( #57108, #26928, #25877 ),
 ( #67356, #44141, #9618 ),
 ( #18835, #92679, #9091 ),
 ( #93218, #51680, #27996 ),
 ( #85124, #84600, #27463 ),
 ( #66817, #76487, #60342 ),
 ( #2061, #58734, #10682 ),
 ( #59801, #52212, #60863 ),
 ( #101831, #59266, #1522 ),
 ( #19380, #42000, #100234 ),
 ( #77025, #51142, #101315 ),
 ( #91632, #18288, #17743 ),
 ( #35010, #10162, #43598 ),
 ( #3145, #2596, #35545 ),
 ( #11208, #50602, #68420 ),
 ( #84061, #36088, #68959 ),
 ( #43075, #93752, #99706 ),
 ( #50090, #82995, #74879 ),
 ( #75963, #967, #33948 ),
 ( #83517, #42528, #75430 ),
 ( #34489, #26402, #92140 ),
 ( #67876, #100760, #77568 ),
 ( #87261, #94828, #38200 ),
 ( #71059, #104482, #79679 ),
 ( #45727, #61396, #45215 ),
 ( #30629, #46263, #21479 ),
 ( #70540, #78608, #61938 ),
 ( #62452, #103431, #20975 ),
 ( #54859, #46786, #95344 ),
 ( #22005, #29069, #94285 ),
 ( #4739, #69480, #53292 ),
 ( #53808, #103951, #71576 ),
 ( #5789, #37679, #86738 ),
 ( #12812, #20452, #70004 ),
 ( #30096, #37138, #79148 ),
 ( #13871, #29581, #4208 ),
 ( #54315, #3684, #62980 ),
 ( #28513, #13336, #95881 ),
 ( #87788, #63518, #38711 ),
 ( #5274, #78090, #19905 ),
 ( #52747, #85670, #11745 ),
 ( #44681, #36615, #102904 ),
 ( #102365, #86213, #12285 ),
 ( #81256, #96928, #98509 ),
 ( #22547, #72645, #14392 ),
 ( #64571, #23063, #72119 ),
 ( #16537, #16008, #40807 ),
 ( #40281, #97438, #39244 ),
 ( #47304, #105028, #24139 ),
 ( #15470, #74235, #33278 ),
 ( #65088, #106603, #32210 ),
 ( #105547, #73701, #56447 ),
 ( #31169, #80200, #89897 ),
 ( #23599, #7901, #55902 ),
 ( #49427, #88838, #64053 ),
 ( #14932, #312, #6304 ),
 ( #56982, #96416, #90433 ),
 ( #48364, #73158, #47824 ),
 ( #6846, #82331, #80728 ),
 ( #97985, #48884, #55389 ),
 ( #32753, #81778, #88318 ),
 ( #24658, #65627, #57510 ),
 ( #39771, #8441, #41342 ),
 ( #31685, #89380, #7370 ),
 ( #106059, #68289, #44011 ),
 ( #11085, #75297, #17620 ),
 ( #43481, #58051, #9490 ),
 ( #60222, #67232, #10565 ),
 ( #74759, #34357, #839 ),
 ( #51012, #26275, #100640 ),
 ( #93090, #34886, #26800 ),
 ( #101184, #33812, #51556 ),
 ( #100110, #19262, #92552 ),
 ( #67753, #10039, #59137 ),
 ( #18700, #17084, #8966 ),
 ( #41871, #92019, #76899 ),
 ( #25194, #59671, #76357 ),
 ( #2470, #18155, #83928 ),
 ( #84470, #35418, #66688 ),
 ( #90973, #27345, #42946 ),
 ( #52090, #3012, #85001 ),
 ( #75837, #66148, #99030 ),
 ( #91506, #99569, #49961 ),
 ( #82869, #25748, #58603 ),
 ( #50481, #83393, #42402 ),
 ( #1390, #1935, #54201 ),
 ( #78491, #20327, #38083 ),
 ( #87140, #13217, #27880 ),
 ( #45619, #29977, #37016 ),
 ( #86089, #44555, #4088 ),
 ( #95230, #20858, #102780 ),
 ( #21361, #68834, #12161 ),
 ( #79031, #69884, #36495 ),
 ( #53691, #46145, #94709 ),
 ( #70940, #28942, #103832 ),
 ( #52617, #35964, #95750 ),
 ( #11625, #61816, #13748 ),
 ( #46659, #102242, #5150 ),
 ( #86624, #62865, #12687 ),
 ( #79557, #37552, #21892 ),
 ( #29464, #101713, #54733 ),
 ( #4622, #87669, #60745 ),
 ( #93633, #70420, #62335 ),
 ( #77442, #61267, #69363 ),
 ( #19784, #103316, #28394 ),
 ( #85545, #77971, #3557 ),
 ( #94157, #53172, #45092 ),
 ( #23477, #71998, #15349 ),
 ( #64451, #63404, #73033 ),
 ( #106471, #55782, #97324 ),
 ( #88193, #15883, #22947 ),
 ( #104910, #32629, #81138 ),
 ( #71457, #6186, #48759 ),
 ( #90302, #5671, #40682 ),
 ( #89779, #56858, #22422 ),
 ( #81652, #39652, #47177 ),
 ( #7247, #7777, #89251 ),
 ( #16411, #24540, #57390 ) ),
 .UNSPECIFIED., .T., .F., .F.,
 ( 4, 1, 1, 1, 1, 1, 1, 1, 1, 1, 1, 1, 1, 1, 1, 1, 1, 1, 1, 1, 1, 1, 1, 1, 1, 1, 1, 1, 1, 1, 1, 1, 1, 1, 1, 1, 1, 1, 1, 1, 1, 1, 1, 1, 1, 1, 1, 1, 1, 1, 1, 1, 1, 1, 1, 1, 1, 1, 1, 1, 1, 1, 1, 1, 1, 1, 1, 1, 1, 1, 1, 1, 1, 1, 1, 1, 1, 1, 1, 1, 1, 1, 1, 1, 1, 1, 1, 1, 1, 1, 1, 1, 1, 1, 1, 1, 1, 1, 1, 1, 1, 1, 1, 1, 1, 1, 1, 1, 1, 1, 1, 1, 1, 1, 1, 1, 1, 1, 1, 1, 1, 1, 1, 1, 1, 1, 1, 1, 1, 1, 2, 1, 1, 1, 1, 1, 1, 1, 1, 1, 1, 1, 1, 1, 1, 1, 1, 1, 1, 1, 1, 1, 1, 1, 1, 1, 1, 1, 1, 1, 1, 1, 1, 1, 1, 1, 1, 1, 1, 1, 1, 1, 1, 1, 1, 1, 1, 1, 1, 1, 1, 1, 1, 1, 1, 1, 1, 1, 1, 1, 1, 1, 1, 1, 1, 1, 1, 1, 1, 1, 1, 1, 1, 1, 1, 1, 1, 1, 1, 1, 1, 1, 1, 1, 1, 1, 1, 1, 1, 1, 1, 1, 1, 1, 1, 1, 1, 1, 1, 1, 1, 1, 1, 1, 1, 1, 1, 1, 1, 1, 1, 1, 1, 1, 1, 1, 1, 1, 1, 1, 1, 1, 1, 1, 1, 1, 1, 1, 1, 4 ),
 ( 2, 1, 2 ),
 ( 0.000000000000000000, 0.003906146814772826562, 0.007812293629545653123, 0.01171844044431847968, 0.01562458725909130625, 0.01953073407386413107, 0.02343688088863695937, 0.02734302770340978420, 0.03124917451818261249, 0.03320224792556902144, 0.03515532133295543732, 0.03710839474034185320, 0.03906146814772826215, 0.04296761496250108697, 0.04687376177727391874, 0.05468605540681956839, 0.06249834903636522498, 0.07031064266591087464, 0.07812293629545652429, 0.08593522992500217395, 0.09374752355454783748, 0.1015598171840934594, 0.1093721108136391368, 0.1132782576284119685, 0.1171844044431848003, 0.1210905512579576043, 0.1249966980727304500, 0.1289028448875032540, 0.1328089917022760857, 0.1367151385170488620, 0.1406212853318217493, 0.1445274321465945810, 0.1484335789613673851, 0.1523397257761402168, 0.1562458725909130486, 0.1601520194056858248, 0.1640581662204587121, 0.1679643130352315439, 0.1718704598500043479, 0.1757766066647771797, 0.1796827534795499559, 0.1816358268869364412, 0.1835889002943228432, 0.1855419737017092452, 0.1874950471090956750, 0.1914011939238684790, 0.1933542673312549365, 0.1953073407386413107, 0.1992134875534140870, 0.2011665609608005445, 0.2031196343681869187, 0.2050727077755734040, 0.2060492444792665356, 0.2070257811829598060, 0.2089788545903461525, 0.2109319279977326378, 0.2128850014051190120, 0.2148380748125054418, 0.2167911482198918716, 0.2187442216272782736, 0.2206972950346647311, 0.2226503684420510498, 0.2246034418494375351, 0.2265565152568239371, 0.2285095886642103391, 0.2304626620715967689, 0.2324157354789831431, 0.2343688088863696006, 0.2363218822937560304, 0.2382749557011424046, 0.2402280291085288344, 0.2421811025159151809, 0.2441341759233016939, 0.2460872493306880127, 0.2499933961454608999, 0.2538995429602335929, 0.2578056897750065080, 0.2617118365897793675, 0.2656179834045521715, 0.2695241302193249755, 0.2734302770340977240, 0.2773364238488707501, 0.2812425706636434986, 0.2851487174784163581, 0.2890548642931891621, 0.2968671579227347701, 0.3046794515522804336, 0.3124917451818260972, 0.3203040388113716497, 0.3281163324409174242, 0.3359286260704630878, 0.3437409197000086958, 0.3476470665147816108, 0.3515532133295543593, 0.3554593601443271633, 0.3593655069590999118, 0.3632716537738728824, 0.3671778005886456864, 0.3710839474034184904, 0.3749900942181913499, 0.3788962410329640984, 0.3828023878477369579, 0.3867085346625097619, 0.3906146814772826215, 0.3945208282920554810, 0.3984269751068281740, 0.4023331219216010890, 0.4042861953289875743, 0.4062392687363738375, 0.4081923421437603228, 0.4101454155511468080, 0.4120984889585330713, 0.4140515623659196121, 0.4160046357733060973, 0.4179577091806923050, 0.4199107825880789013, 0.4218638559954652756, 0.4257700028102379686, 0.4296761496250108836, 0.4335822964397836876, 0.4374884432545565471, 0.4413945900693294067, 0.4453007368841020996, 0.4492068836988750702, 0.4531130305136478742, 0.4609253241431935377, 0.4687376177727392013, 0.4765499114022848093, 0.4843622050318303618, 0.4921744986613760253, 0.4999867922909217999, 0.5077994986613761919, 0.5156122050318305838, 0.5234249114022848648, 0.5312376177727392568, 0.5390503241431936488, 0.5468630305136479297, 0.5507693836988751812, 0.5546757368841022107, 0.5585820900693294622, 0.5624884432545566026, 0.5663947964397838541, 0.5703011496250109946, 0.5742075028102381351, 0.5781138559954652756, 0.5800670325880789013, 0.5820202091806925271, 0.5839733857733060418, 0.5859265623659195565, 0.5878797389585332933, 0.5898329155511468080, 0.5917860921437604338, 0.5937392687363740595, 0.5956924453289873522, 0.5976456219216012000, 0.6015519751068284515, 0.6054583282920554810, 0.6093646814772826215, 0.6132710346625098730, 0.6171773878477370134, 0.6210837410329641539, 0.6249900942181914054, 0.6288964474034186569, 0.6328028005886456864, 0.6367091537738729379, 0.6406155069591000784, 0.6445218601443273299, 0.6484282133295544703, 0.6523345665147814998, 0.6562409197000087513, 0.6640536260704632543, 0.6718663324409175353, 0.6796790388113718162, 0.6874917451818260972, 0.6953044515522806002, 0.7031171579227348811, 0.7109298642931891621, 0.7148362174784161915, 0.7187425706636435541, 0.7226489238488706945, 0.7265552770340979460, 0.7304616302193250865, 0.7343679834045522270, 0.7382743365897792565, 0.7421806897750065080, 0.7460870429602337595, 0.7499933961454610110, 0.7538997493306882625, 0.7558529259233015551, 0.7578061025159152919, 0.7597592791085288066, 0.7617124557011423214, 0.7636656322937560581, 0.7656188088863695729, 0.7675719854789833096, 0.7695251620715968244, 0.7714783386642103391, 0.7734315152568238538, 0.7753846918494375906, 0.7773378684420511053, 0.7792910450346646201, 0.7812442216272783568, 0.7831973982198916495, 0.7851505748125056083, 0.7871037514051189010, 0.7890569279977326378, 0.7910101045903461525, 0.7929632811829598893, 0.7949164577755734040, 0.7968696343681870298, 0.7988228109608006555, 0.8007759875534141703, 0.8046823407386413107, 0.8066355173312547144, 0.8085886939238684512, 0.8124950471090957027, 0.8144482237017094395, 0.8164014002943229542, 0.8183545768869363579, 0.8203077534795502057, 0.8242141066647772352, 0.8281204598500044867, 0.8320268130352314051, 0.8359331662204587676, 0.8398395194056857971, 0.8437458725909130486, 0.8476522257761403001, 0.8515585789613675516, 0.8554649321465945810, 0.8593712853318218325, 0.8632776385170490840, 0.8671839917022761135, 0.8710903448875033650, 0.8749966980727305055, 0.8789030512579574239, 0.8828094044431848975, 0.8867157576284119269, 0.8906221108136391784, 0.8984348171840934594, 0.9062475235545479624, 0.9140602299250022433, 0.9218729362954565243, 0.9296856426659108052, 0.9374983490363653083, 0.9453110554068195892, 0.9531237617772740922, 0.9570301149625010106, 0.9609364681477282621, 0.9628896447403418879, 0.9648428213329554026, 0.9667959979255691394, 0.9687491745181826541, 0.9726555277034099056, 0.9765618808886369351, 0.9804682340738641866, 0.9843745872590914381, 0.9882809404443185786, 0.9921872936295457190, 0.9960936468147727485, 1.000000000000000000 ),
 ( 0.000000000000000000, 1.000000000000000000, 1.526318052600188269 ),
 .UNSPECIFIED. ) ;
#3352=CARTESIAN_POINT ( 'NONE',  ( -81.05938286033433826, -29.99999999999999645, -11.75216569974085523 ) ) ;
#3354=CARTESIAN_POINT ( 'NONE',  ( 86.68749933009506492, -17.00766437030456402, 185.5393203993762370 ) ) ;
#3370=ORIENTED_EDGE ( 'NONE', *, *, #60706, .F. ) ;
#3377=CARTESIAN_POINT ( 'NONE',  ( -111.1352917996996013, -60.00000000000000000, 186.5960929966779815 ) ) ;
#3382=CARTESIAN_POINT ( 'NONE',  ( -85.94455300974112788, -21.71266392783007504, 172.2523347831352964 ) ) ;
#3387=CARTESIAN_POINT ( 'NONE',  ( -86.46969771635572499, -60.13837812595784982, 2.720957838497157333 ) ) ;
#3395=CARTESIAN_POINT ( 'NONE',  ( 78.54417320222145804, -14.21045842199432307, 165.9036888455924270 ) ) ;
#3399=CARTESIAN_POINT ( 'NONE',  ( -94.69971540129887444, -59.99999999999987921, 1.030331952319396782 ) ) ;
#3400=CARTESIAN_POINT ( 'NONE',  ( -69.47556247483554159, -25.58659212672100125, 92.27640143973368936 ) ) ;
#3402=CARTESIAN_POINT ( 'NONE',  ( 86.51021125171571668, -60.00000000000013500, 203.5141634203183685 ) ) ;
#3404=CARTESIAN_POINT ( 'NONE',  ( 22.37633122833116417, -57.67115084601979191, -43.62954971562658812 ) ) ;
#3409=EDGE_CURVE ( 'NONE', #53391, #17004, #65304, .T. ) ;
#3416=CARTESIAN_POINT ( 'NONE',  ( 2.936182742933428427E-09, -59.99999999999998579, 41.99999999999666755 ) ) ;
#3420=CARTESIAN_POINT ( 'NONE',  ( 23.93420880016848074, -4.285714285714296246, -8.127057321558242009 ) ) ;
#3428=CARTESIAN_POINT ( 'NONE',  ( 32.92851612125411975, -46.42981575483278078, 35.59486626606223325 ) ) ;
#3429=FILL_AREA_STYLE ('',( #28812 ) ) ;
#3443=CARTESIAN_POINT ( 'NONE',  ( 92.27650878891940067, -59.99999999999999289, 1.835041955732973351 ) ) ;
#3449=CARTESIAN_POINT ( 'NONE',  ( -109.5905853243550467, -30.00000000000664357, 171.0618735817303104 ) ) ;
#3456=CARTESIAN_POINT ( 'NONE',  ( 84.22572678630466214, -52.73862619169806720, -14.84760467275862972 ) ) ;
#3468=CARTESIAN_POINT ( 'NONE',  ( 72.11924800345758513, -53.37899342557430060, 118.2001781568277750 ) ) ;
#3474=CARTESIAN_POINT ( 'NONE',  ( -93.91996415714238822, -57.61928231945634593, 204.5092364001214946 ) ) ;
#3486=CARTESIAN_POINT ( 'NONE',  ( -51.48836687262417655, -29.91056394135168262, 49.15659163052040270 ) ) ;
#3498=CARTESIAN_POINT ( 'NONE',  ( -57.05541872896377242, -28.84113649674122115, -25.95661199123281548 ) ) ;
#3499=CARTESIAN_POINT ( 'NONE',  ( -87.75496598979771079, -29.99999999999999289, 186.1453428037212632 ) ) ;
#3502=CARTESIAN_POINT ( 'NONE',  ( 83.57756196019212780, -57.54177920181132322, 201.5121743845033393 ) ) ;
#3506=CARTESIAN_POINT ( 'NONE',  ( 24.04396523262633067, -27.34829711589978984, -38.39905134658587826 ) ) ;
#3509=CARTESIAN_POINT ( 'NONE',  ( -56.06363120456222049, -60.00000000000000711, 88.36825490483376200 ) ) ;
#3511=AXIS2_PLACEMENT_3D ( 'NONE', #6834, #39754, #56434 ) ;
#3513=CARTESIAN_POINT ( 'NONE',  ( -85.68179626072733868, -57.45883239149054589, 192.8351143831483512 ) ) ;
#3516=CARTESIAN_POINT ( 'NONE',  ( -2.999853627381086518, -29.03101188044279368, 28.72356160493805532 ) ) ;
#3530=CARTESIAN_POINT ( 'NONE',  ( -3.301606509414613644, -4.285714285714286476, 25.22241582816893413 ) ) ;
#3532=CARTESIAN_POINT ( 'NONE',  ( 104.6755681235317326, -59.99999999999997158, 94.38101796850538960 ) ) ;
#3534=CARTESIAN_POINT ( 'NONE',  ( -83.18631812101111223, -22.15354509450119025, 146.6237897504154546 ) ) ;
#3538=CARTESIAN_POINT ( 'NONE',  ( 46.71400118704798388, -57.68116600608826161, 69.02050771961488351 ) ) ;
#3549=EDGE_CURVE ( 'NONE', #71545, #17004, #72925, .T. ) ;
#3556=CARTESIAN_POINT ( 'NONE',  ( 51.11362513016616305, -59.99999999999997868, -37.68753618808192840 ) ) ;
#3557=CARTESIAN_POINT ( 'NONE',  ( -37.63111671575072137, -14.21045842199439235, 41.24562198507008759 ) ) ;
#3558=CARTESIAN_POINT ( 'NONE',  ( 23.12828282194952578, -22.07908306402419996, 28.45182989271827978 ) ) ;
#3560=CARTESIAN_POINT ( 'NONE',  ( -36.41141080624493753, -49.89788766448109669, 38.20003062495130308 ) ) ;
#3573=CARTESIAN_POINT ( 'NONE',  ( 90.37091339520917188, -30.00000000000016698, 190.1441424001023393 ) ) ;
#3578=CARTESIAN_POINT ( 'NONE',  ( 76.79371475606434672, -30.00000000000000711, -16.79878599767251046 ) ) ;
#3596=CARTESIAN_POINT ( 'NONE',  ( 60.37599435018250915, -38.34251099049790668, 97.59093692943510234 ) ) ;
#3602=CARTESIAN_POINT ( 'NONE',  ( 59.77473313328942339, -39.48835101806282921, 71.62691032963155635 ) ) ;
#3620=CARTESIAN_POINT ( 'NONE',  ( 86.45121968906420307, -35.49061221823143342, 186.8395049817269467 ) ) ;
#3621=DIRECTION ( 'NONE',  ( 0.000000000000000000, 0.000000000000000000, -1.000000000000000000 ) ) ;
#3628=CARTESIAN_POINT ( 'NONE',  ( -96.78478928627799860, -29.99999999999999645, 129.2502935530884258 ) ) ;
#3631=CARTESIAN_POINT ( 'NONE',  ( 2.316771770790045260, -57.67120512461058013, 41.60859164704628199 ) ) ;
#3636=CARTESIAN_POINT ( 'NONE',  ( -5.141721953570575820, -19.24029832776622939, 27.08744995826211976 ) ) ;
#3640=CARTESIAN_POINT ( 'NONE',  ( 28.44949503909961663, -21.18434267548764893, -32.45319859116707306 ) ) ;
#3643=CARTESIAN_POINT ( 'NONE',  ( -26.49644935441500238, -49.91621229936360749, 33.89336801046082570 ) ) ;
#3648=CARTESIAN_POINT ( 'NONE',  ( -19.02339800640524814, -39.47694344028838032, 30.89218607398163741 ) ) ;
#3664=CARTESIAN_POINT ( 'NONE',  ( 101.3732779641561734, -45.28196344093066728, 190.6380055777363509 ) ) ;
#3678=CARTESIAN_POINT ( 'NONE',  ( -94.68899862568390802, -60.00000000000000000, 1.161127854999643105 ) ) ;
#3680=CARTESIAN_POINT ( 'NONE',  ( 29.75767506032096676, -59.99999999999997868, 42.91511451735463112 ) ) ;
#3684=CARTESIAN_POINT ( 'NONE',  ( -104.6655502547336738, -29.99999999999993250, 124.7729330896767408 ) ) ;
#3685=CARTESIAN_POINT ( 'NONE',  ( 7.130718316848325244, -39.47255126203687325, 30.45876176605233709 ) ) ;
#3688=CARTESIAN_POINT ( 'NONE',  ( -48.04142550409461165, -39.52501460404417344, 47.69088070168321281 ) ) ;
#3699=DIRECTION ( 'NONE',  ( -0.000000000000000000, -1.000000000000000000, -0.000000000000000000 ) ) ;
#3701=CARTESIAN_POINT ( 'NONE',  ( 108.2638972020982067, -29.99999999998661693, 151.1580933454320927 ) ) ;
#3707=CARTESIAN_POINT ( 'NONE',  ( 95.82107296712156597, -30.00000000000000355, 191.3050472533331572 ) ) ;
#3713=CARTESIAN_POINT ( 'NONE',  ( 54.43224963993771581, -25.62617297809076078, 53.68705043744507321 ) ) ;
#3717=CARTESIAN_POINT ( 'NONE',  ( -91.11385766084679005, -38.35479298179576801, 0.5733152911744004987 ) ) ;
#3720=CARTESIAN_POINT ( 'NONE',  ( 108.2770287625986754, -38.35766625322560941, 192.2059017873136497 ) ) ;
#3722=CARTESIAN_POINT ( 'NONE',  ( 82.44406999259793167, -37.85557453133404948, 14.49103131622133311 ) ) ;
#3740=CARTESIAN_POINT ( 'NONE',  ( 40.60998584173464820, -26.59100105118786317, 36.33122594000368366 ) ) ;
#3747=CARTESIAN_POINT ( 'NONE',  ( 84.56613401024672783, -39.39959700902200979, 181.6695324457707557 ) ) ;
#3750=CARTESIAN_POINT ( 'NONE',  ( -84.82029566994467018, -37.82138604335175103, 44.26793484215674113 ) ) ;
#3754=CARTESIAN_POINT ( 'NONE',  ( -4.429919089265682786, -21.58035052029104151, -38.54841997176323787 ) ) ;
#3757=CARTESIAN_POINT ( 'NONE',  ( 21.33042875005117267, -59.99999999999998579, 40.41048302378931822 ) ) ;
#3759=CARTESIAN_POINT ( 'NONE',  ( -87.14767027655014431, -37.99999999998310329, 189.0874028505847662 ) ) ;
#3760=CARTESIAN_POINT ( 'NONE',  ( 51.37606068035684359, -29.89807750398198394, 48.95549095964486241 ) ) ;
#3775=CARTESIAN_POINT ( 'NONE',  ( 3.088936762904795241, -21.77034166220828837, -30.49860928398698690 ) ) ;
#3783=CARTESIAN_POINT ( 'NONE',  ( -92.23621273581470348, -60.00000000000000000, 2.391921308898584453 ) ) ;
#3790=CARTESIAN_POINT ( 'NONE',  ( -82.17221523199479805, -46.46580854769393909, 173.2050682668972854 ) ) ;
#3800=CARTESIAN_POINT ( 'NONE',  ( -91.04381008827128596, -57.66401771476134996, -20.86613467659797649 ) ) ;
#3807=CARTESIAN_POINT ( 'NONE',  ( 93.17370000506844008, -59.99999999999994316, -17.95777172718301173 ) ) ;
#3810=CARTESIAN_POINT ( 'NONE',  ( -94.89844962927027439, -60.00000000000001421, 205.0338773334991060 ) ) ;
#3811=CARTESIAN_POINT ( 'NONE',  ( -54.48342840945926469, -56.85295987972201459, 66.24415397588745691 ) ) ;
#3814=CARTESIAN_POINT ( 'NONE',  ( -102.9797039820129072, -45.26540897849420020, 185.6133583916170267 ) ) ;
#3819=( NAMED_UNIT ( * ) SI_UNIT ( $, .STERADIAN. ) SOLID_ANGLE_UNIT ( ) );
#3832=CARTESIAN_POINT ( 'NONE',  ( -27.39369750312375729, -56.87079340815250106, 35.32494246014085348 ) ) ;
#3835=CARTESIAN_POINT ( 'NONE',  ( 47.01967600138543446, -39.52544382475996798, 46.22899997382759096 ) ) ;
#3841=CARTESIAN_POINT ( 'NONE',  ( -91.91261139602251262, -38.50135474963098403, 200.9741384565720637 ) ) ;
#3852=CARTESIAN_POINT ( 'NONE',  ( 103.5957000756554578, -60.00000000000001421, 200.2558930352217317 ) ) ;
#3857=CARTESIAN_POINT ( 'NONE',  ( -81.34740007214244883, -30.00000000000000711, -10.45134090017297446 ) ) ;
#3859=PRESENTATION_STYLE_ASSIGNMENT (( #19553 ) ) ;
#3870=CARTESIAN_POINT ( 'NONE',  ( 83.58220805307611556, -35.98891138001182810, 169.8156018569172545 ) ) ;
#3910=CARTESIAN_POINT ( 'NONE',  ( -108.5746306176662301, -59.99999999999999289, 194.5749993497246635 ) ) ;
#3916=CARTESIAN_POINT ( 'NONE',  ( -84.96410193910523390, -32.32224907966426741, 177.2623289152436996 ) ) ;
#3922=CARTESIAN_POINT ( 'NONE',  ( -82.46448073435685444, -37.83313065937878861, 8.731117919795149618 ) ) ;
#3928=CARTESIAN_POINT ( 'NONE',  ( 75.56757797150578426, -14.21045842199434439, 141.5459454228812319 ) ) ;
#3931=CARTESIAN_POINT ( 'NONE',  ( -94.49493096136262693, -59.99999999999997158, -13.89135613746328701 ) ) ;
#3932=CARTESIAN_POINT ( 'NONE',  ( -64.47854645191701195, -42.96210629927422531, 86.48441421252113059 ) ) ;
#3934=CARTESIAN_POINT ( 'NONE',  ( 111.5326445490954228, -59.99999999999995737, 193.8609935400126005 ) ) ;
#3935=CARTESIAN_POINT ( 'NONE',  ( 19.58390667205444657, -59.99999999998016165, 42.52723830633056679 ) ) ;
#3946=CARTESIAN_POINT ( 'NONE',  ( -44.37565758691186346, -59.99999999999997868, -38.94428251963324072 ) ) ;
#3960=CARTESIAN_POINT ( 'NONE',  ( 34.65411374088593988, -18.71485586463119333, 31.05683867045650715 ) ) ;
#3961=CARTESIAN_POINT ( 'NONE',  ( 15.50035291838412199, -4.285714285712356464, 20.16952962162429941 ) ) ;
#3974=CARTESIAN_POINT ( 'NONE',  ( 92.01456011641386112, -59.99999999999999289, 18.73852019385518020 ) ) ;
#3984=CARTESIAN_POINT ( 'NONE',  ( -104.9152107932271463, -30.00000000010609469, 126.1345714984008737 ) ) ;
#3990=CARTESIAN_POINT ( 'NONE',  ( 84.33012706832269600, -45.28231600066910545, -10.05877812763055523 ) ) ;
#4001=CARTESIAN_POINT ( 'NONE',  ( 78.28673168894357559, -60.30906236363500028, 158.4437153918191825 ) ) ;
#4005=CARTESIAN_POINT ( 'NONE',  ( -106.5151323516585649, -57.65184864013982491, 200.5412705504392079 ) ) ;
#4012=CARTESIAN_POINT ( 'NONE',  ( -42.05067302585612055, -27.18224454527997480, 37.40642595164874962 ) ) ;
#4026=CARTESIAN_POINT ( 'NONE',  ( -32.75612034570598041, -24.60049146598317904, -37.04625446625190222 ) ) ;
#4027=CARTESIAN_POINT ( 'NONE',  ( -59.21483274588983647, -29.99999999999999645, 65.04807226357009142 ) ) ;
#4032=CARTESIAN_POINT ( 'NONE',  ( 78.02157272649068886, -57.51171903303600885, 196.6038749271185111 ) ) ;
#4037=CARTESIAN_POINT ( 'NONE',  ( -69.29604869819449675, -60.00000000000000711, 137.6211246123437206 ) ) ;
#4040=CARTESIAN_POINT ( 'NONE',  ( -86.04699626542492297, -31.95447380513247282, 184.0172807620984656 ) ) ;
#4044=CARTESIAN_POINT ( 'NONE',  ( -1.981107828036278606, -22.06778036923262931, 27.56548919790143870 ) ) ;
#4060=CARTESIAN_POINT ( 'NONE',  ( -6.601913983200961233, -4.285714285712858285, -24.56594385547797543 ) ) ;
#4063=CARTESIAN_POINT ( 'NONE',  ( 90.56091889802806350, -29.99999999999993960, 34.47026654395114775 ) ) ;
#4064=CARTESIAN_POINT ( 'NONE',  ( -79.63233721077718030, -32.55990623632270342, 136.6957858042794385 ) ) ;
#4065=ORIENTED_EDGE ( 'NONE', *, *, #33055, .F. ) ;
#4068=CARTESIAN_POINT ( 'NONE',  ( 30.89728992616315750, -57.68649126897638268, 45.79953151277155143 ) ) ;
#4087=CARTESIAN_POINT ( 'NONE',  ( 83.46915560824537295, -60.00000000000000000, -25.72054130885968704 ) ) ;
#4088=CARTESIAN_POINT ( 'NONE',  ( -73.20747738243755975, -14.21045842199437992, 129.5005664428163641 ) ) ;
#4089=CARTESIAN_POINT ( 'NONE',  ( 26.98664971853731487, -46.43314927939716341, 33.41725387913556489 ) ) ;
#4092=CARTESIAN_POINT ( 'NONE',  ( -38.45575393299976241, -46.43411444215534090, 38.95968530998309376 ) ) ;
#4095=CARTESIAN_POINT ( 'NONE',  ( -22.67073868809949033, -4.285714285714295357, 11.17734400176826526 ) ) ;
#4102=CARTESIAN_POINT ( 'NONE',  ( -67.77671069964115702, -38.33437092114629507, 124.5516907683609418 ) ) ;
#4104=CARTESIAN_POINT ( 'NONE',  ( 99.43643474579640440, -30.00000000000000000, 187.6780440051967958 ) ) ;
#4108=CARTESIAN_POINT ( 'NONE',  ( 76.98249430118629277, -30.00000000000000000, -16.66152498815789684 ) ) ;
#4129=CARTESIAN_POINT ( 'NONE',  ( 63.59325793215686673, -46.43410071035751230, 85.67174166192037887 ) ) ;
#4134=CARTESIAN_POINT ( 'NONE',  ( -64.54403517473807028, -37.84143551314759435, -32.95252873240283975 ) ) ;
#4148=CARTESIAN_POINT ( 'NONE',  ( 86.32370369321748171, -31.85974275469703088, 185.2292116863652609 ) ) ;
#4156=DIRECTION ( 'NONE',  ( 0.000000000000000000, 0.000000000000000000, -1.000000000000000000 ) ) ;
#4158=CARTESIAN_POINT ( 'NONE',  ( -99.16808899320049875, -30.00000000000000355, 146.3606151617508431 ) ) ;
#4161=CARTESIAN_POINT ( 'NONE',  ( 19.23758136976156052, -57.67182727287845267, 42.11656184680051496 ) ) ;
#4174=CARTESIAN_POINT ( 'NONE',  ( -18.16430329042714931, -53.40190210536660231, 33.13507712519638204 ) ) ;
#4185=CARTESIAN_POINT ( 'NONE',  ( 101.2091753172953190, -45.28154215804822513, 190.9441895052663938 ) ) ;
#4186=CARTESIAN_POINT ( 'NONE',  ( 46.25537882904671250, -37.26716345494458693, 44.48526200656858265 ) ) ;
#4191=EDGE_CURVE ( 'NONE', #62746, #32321, #21589, .T. ) ;
#4203=CARTESIAN_POINT ( 'NONE',  ( -95.16212988580207366, -60.00000000004876455, 30.21691017251174216 ) ) ;
#4205=CARTESIAN_POINT ( 'NONE',  ( 81.11166217577948601, -59.99999999999026556, -30.02696344982326337 ) ) ;
#4208=CARTESIAN_POINT ( 'NONE',  ( -101.4323841882945771, -14.21045842199443499, 121.1831906623697677 ) ) ;
#4209=CARTESIAN_POINT ( 'NONE',  ( 7.030933152283679100, -25.54832196774594522, 28.13802627504265885 ) ) ;
#4211=CARTESIAN_POINT ( 'NONE',  ( -48.21680793553016287, -53.36514319048075805, 52.27612587481558393 ) ) ;
#4221=CARTESIAN_POINT ( 'NONE',  ( 89.33888981624761527, -30.00000000000353850, -13.70441906546611044 ) ) ;
#4225=CARTESIAN_POINT ( 'NONE',  ( 101.2094742396540425, -30.00000000000000000, 175.1259804473514521 ) ) ;
#4231=CARTESIAN_POINT ( 'NONE',  ( 54.29581107121828865, -29.09449404548636409, 54.75117451817219205 ) ) ;
#4235=CARTESIAN_POINT ( 'NONE',  ( -87.51990533283513685, -38.36637924240768172, -20.20941912294309262 ) ) ;
#4239=CARTESIAN_POINT ( 'NONE',  ( 105.2106280407045631, -38.39002650047679310, 197.2706458416391797 ) ) ;
#4242=CARTESIAN_POINT ( 'NONE',  ( 83.97326503874400316, -45.28715381657895733, 3.105619776616419969 ) ) ;
#4264=CARTESIAN_POINT ( 'NONE',  ( -40.30924518282468227, -28.68040258788349561, 47.69910574250469182 ) ) ;
#4267=CARTESIAN_POINT ( 'NONE',  ( 83.89774654829980705, -46.54964297292601572, 184.2018487009828789 ) ) ;
#4272=CARTESIAN_POINT ( 'NONE',  ( -95.59733413037783123, -37.82076376832549158, 111.4287389431865734 ) ) ;
#4279=CARTESIAN_POINT ( 'NONE',  ( 15.20944265188900424, -22.80677179166491797, 35.96349324364335587 ) ) ;
#4280=CARTESIAN_POINT ( 'NONE',  ( 33.62703971678629955, -23.41653139858035360, 33.03092013152653550 ) ) ;
#4297=CARTESIAN_POINT ( 'NONE',  ( 1.581782531941442027, -47.40884548514188168, -34.79113668873367260 ) ) ;
#4304=CARTESIAN_POINT ( 'NONE',  ( -91.96777462086218691, -60.00000000000000000, 17.71638642338550795 ) ) ;
#4312=CARTESIAN_POINT ( 'NONE',  ( -80.97806908835234196, -53.42006643256369358, 173.1435725716072227 ) ) ;
#4315=CARTESIAN_POINT ( 'NONE',  ( -17.01584901091793967, 0.000000000000000000, -1.113195845621204993 ) ) ;
#4325=CARTESIAN_POINT ( 'NONE',  ( -53.00838388237266940, -57.67116150918030115, -39.31046371713402721 ) ) ;
#4332=CARTESIAN_POINT ( 'NONE',  ( 93.93995408072316877, -60.00000000000007816, -15.95669063232190155 ) ) ;
#4333=CARTESIAN_POINT ( 'NONE',  ( -74.93456164446882894, -30.00000000000001421, 156.1801137937684985 ) ) ;
#4334=CARTESIAN_POINT ( 'NONE',  ( -58.48862033019764084, -18.66108675706986730, 59.20230775497523013 ) ) ;
#4338=CARTESIAN_POINT ( 'NONE',  ( -99.23041091440894945, -37.78869810946568464, 191.6572301050025260 ) ) ;
#4343=CARTESIAN_POINT ( 'NONE',  ( -23.93160351366482885, -59.99999999999998579, 40.89972924297317292 ) ) ;
#4354=CARTESIAN_POINT ( 'NONE',  ( -28.82410583165911078, -60.34270495868832285, 36.38275433194883135 ) ) ;
#4356=CARTESIAN_POINT ( 'NONE',  ( 48.50248592037799966, -25.67881720222466413, 44.08540501476609563 ) ) ;
#4359=CARTESIAN_POINT ( 'NONE',  ( -86.84248034292065199, -38.60144547145630867, 199.4726879763670411 ) ) ;
#4362=CARTESIAN_POINT ( 'NONE',  ( 90.78374300502272831, -38.34267589133914100, 5.711982823473677584 ) ) ;
#4370=CARTESIAN_POINT ( 'NONE',  ( 112.1326292210085853, -59.99999999999997868, 177.2482590370370588 ) ) ;
#4376=CARTESIAN_POINT ( 'NONE',  ( -80.80298817501201825, -30.00000000000003197, 8.170653238303200894 ) ) ;
#4378=CARTESIAN_POINT ( 'NONE',  ( -81.36991943370300362, -38.84403975064132908, 195.1307900073841211 ) ) ;
#4392=CARTESIAN_POINT ( 'NONE',  ( 80.86826994178642281, -56.92707617347908666, 177.6008734011382160 ) ) ;
#4406=CARTESIAN_POINT ( 'NONE',  ( -80.64775485730676508, -30.00000000000000355, -12.74855559745246225 ) ) ;
#4424=LINE ( 'NONE', #37362, #84292 ) ;
#4430=CARTESIAN_POINT ( 'NONE',  ( -102.6181093806218456, -60.00000000000000711, 200.8243356994102271 ) ) ;
#4435=CARTESIAN_POINT ( 'NONE',  ( -82.00017004842651147, -60.72289651137820954, 187.9292513951569674 ) ) ;
#4443=CARTESIAN_POINT ( 'NONE',  ( -84.42099871513350706, -45.26547612325662584, 28.59035868857876039 ) ) ;
#4450=CARTESIAN_POINT ( 'NONE',  ( 107.5269304809499431, -60.00000000000002132, 200.1385401206229062 ) ) ;
#4452=CARTESIAN_POINT ( 'NONE',  ( -95.66383100604464573, -60.00000000000002132, 35.18327952992021324 ) ) ;
#4453=CARTESIAN_POINT ( 'NONE',  ( -62.37994538018725166, -60.34609847077623357, 89.28735657275996118 ) ) ;
#4456=CARTESIAN_POINT ( 'NONE',  ( 102.0109750195309175, -30.00000000000007816, 198.2012210982776708 ) ) ;
#4458=CARTESIAN_POINT ( 'NONE',  ( 78.54918379967675435, -59.99999999999753442, 198.2828222273666086 ) ) ;
#4466=VERTEX_POINT ( 'NONE', #55370 ) ;
#4472=CARTESIAN_POINT ( 'NONE',  ( -51.23217687371317197, -59.99999999999998579, -37.66347443025715336 ) ) ;
#4489=CARTESIAN_POINT ( 'NONE',  ( 38.04275141536665927, -60.26973243953698045, 41.50661353697247336 ) ) ;
#4500=CARTESIAN_POINT ( 'NONE',  ( 91.87991718087357640, -60.00000000000000711, 9.797106062246539793 ) ) ;
#4507=CARTESIAN_POINT ( 'NONE',  ( -87.30396544109028412, -29.99999999998607336, 198.3586875667010645 ) ) ;
#4520=CARTESIAN_POINT ( 'NONE',  ( 79.94750706239578619, -25.61877512049329297, 131.8648424581376730 ) ) ;
#4527=CARTESIAN_POINT ( 'NONE',  ( -108.9175987578229297, -57.66477069964600588, 197.8260142395344303 ) ) ;
#4540=CARTESIAN_POINT ( 'NONE',  ( -49.56313789510318202, -29.60261757400662574, 45.92228025562707927 ) ) ;
#4549=ORIENTED_EDGE ( 'NONE', *, *, #62264, .T. ) ;
#4556=CARTESIAN_POINT ( 'NONE',  ( -61.19724114412970550, -29.40090490056691408, -24.55535741776452596 ) ) ;
#4557=CARTESIAN_POINT ( 'NONE',  ( -66.40962216726373413, -30.00000000000000000, 84.31724798585034364 ) ) ;
#4562=CARTESIAN_POINT ( 'NONE',  ( 75.82261830597555274, -57.55065031891655991, 192.7782113498394381 ) ) ;
#4563=VECTOR ( 'NONE', #19813, 1000.000000000000000 ) ;
#4569=CARTESIAN_POINT ( 'NONE',  ( -50.52593252671915991, -60.00000000000000711, 73.12709640751428708 ) ) ;
#4574=CARTESIAN_POINT ( 'NONE',  ( -85.56608911191202083, -39.28323613089826694, 185.6737815819577406 ) ) ;
#4577=CARTESIAN_POINT ( 'NONE',  ( 2.066990665002553832E-05, -35.99444419889723434, 29.88872399275190972 ) ) ;
#4592=CARTESIAN_POINT ( 'NONE',  ( -6.601913983209747983, -4.285714285713511096, 24.56594385547482418 ) ) ;
#4594=CARTESIAN_POINT ( 'NONE',  ( 87.30924545702741568, -14.21045842199429998, 28.19131950638903206 ) ) ;
#4595=CARTESIAN_POINT ( 'NONE',  ( -81.46110316675287777, -22.15507786611714636, 136.5093758021127996 ) ) ;
#4598=( LENGTH_UNIT ( ) NAMED_UNIT ( * ) SI_UNIT ( .MILLI., .METRE. ) );
#4605=ORIENTED_EDGE ( 'NONE', *, *, #25954, .F. ) ;
#4622=CARTESIAN_POINT ( 'NONE',  ( -46.52099778141491271, -60.00000000000009948, 69.35786614446448084 ) ) ;
#4623=CARTESIAN_POINT ( 'NONE',  ( 27.94074522160097018, -39.48070956748559723, 32.48135008067870189 ) ) ;
#4629=CARTESIAN_POINT ( 'NONE',  ( -12.64023069600374249, -4.285714285714296246, -21.88880945939638778 ) ) ;
#4639=CARTESIAN_POINT ( 'NONE',  ( 91.77464836895023836, -29.99999999999999289, 98.58162192422200576 ) ) ;
#4643=CARTESIAN_POINT ( 'NONE',  ( 81.59421194845130287, -30.00000000000000355, -6.849562237453022284 ) ) ;
#4664=CARTESIAN_POINT ( 'NONE',  ( 64.22169963983361640, -25.57819097122271756, 76.81871742320117846 ) ) ;
#4668=CARTESIAN_POINT ( 'NONE',  ( -46.45064480349970637, -34.72776456001106737, -36.68816489433520189 ) ) ;
#4681=CARTESIAN_POINT ( 'NONE',  ( 85.01337858154622040, -61.07969618245190446, 193.5080867132440687 ) ) ;
#4691=CARTESIAN_POINT ( 'NONE',  ( -100.3761925564723754, -29.99999999999999289, 157.7587148953477652 ) ) ;
#4694=CARTESIAN_POINT ( 'NONE',  ( 8.463560105336789263, -57.67125183312073489, 41.60408020090174119 ) ) ;
#4709=CARTESIAN_POINT ( 'NONE',  ( -14.66631300009641947, -46.43930650983597985, 31.75654908330537296 ) ) ;
#4734=CARTESIAN_POINT ( 'NONE',  ( -44.76546953684172792, -60.00000000001929834, -41.27300769871817465 ) ) ;
#4736=CARTESIAN_POINT ( 'NONE',  ( 36.34800668462530382, -60.00000000000000000, -42.52793270410367654 ) ) ;
#4739=CARTESIAN_POINT ( 'NONE',  ( -103.2297580319645220, -60.00000000000001421, 85.94764253490394879 ) ) ;
#4740=CARTESIAN_POINT ( 'NONE',  ( 7.997113486846998853, -18.58630230906148739, 26.97986963482658496 ) ) ;
#4743=CARTESIAN_POINT ( 'NONE',  ( -47.98399617180434262, -46.44468898856910499, 49.73485108116536679 ) ) ;
#4754=CARTESIAN_POINT ( 'NONE',  ( 88.54209716525605245, -30.00000000000043698, -15.94097299020626579 ) ) ;
#4758=CARTESIAN_POINT ( 'NONE',  ( 97.41881973446541565, -29.99999999999999645, 190.9256256769457138 ) ) ;
#4763=CARTESIAN_POINT ( 'NONE',  ( 53.74627874984997788, -42.96783881181733022, 59.00685369471283792 ) ) ;
#4767=DIRECTION ( 'NONE',  ( 0.000000000000000000, 0.000000000000000000, 1.000000000000000000 ) ) ;
#4772=CARTESIAN_POINT ( 'NONE',  ( 101.6454106623534130, -38.44960037453935087, 199.8551154696798449 ) ) ;
#4775=CARTESIAN_POINT ( 'NONE',  ( 83.74695688753641321, -45.28417006571125825, 7.588987474943079903 ) ) ;
#4780=AXIS2_PLACEMENT_3D ( 'NONE', #63257, #88582, #96148 ) ;
#4786=ORIENTED_EDGE ( 'NONE', *, *, #17565, .T. ) ;
#4795=CARTESIAN_POINT ( 'NONE',  ( -41.42724453868126488, -29.06770635680324588, 49.23312051806635736 ) ) ;
#4799=CARTESIAN_POINT ( 'NONE',  ( 82.86076466567399734, -60.89105270492382260, 190.2892942670303285 ) ) ;
#4803=CARTESIAN_POINT ( 'NONE',  ( -100.0262352094438114, -60.15499860873356397, 115.3325505367406265 ) ) ;
#4808=CARTESIAN_POINT ( 'NONE',  ( -9.343143414270016933, -22.46350855537282953, -38.54324068240695311 ) ) ;
#4814=CARTESIAN_POINT ( 'NONE',  ( 40.16194943996363520, -26.39549351810784472, 36.06414978926066794 ) ) ;
#4829=CARTESIAN_POINT ( 'NONE',  ( 3.129901519903563578, -34.58960633113510141, -32.63490336102687195 ) ) ;
#4840=CARTESIAN_POINT ( 'NONE',  ( -92.73391705501121862, -59.99999999999999289, -6.016779592986783776 ) ) ;
#4844=DIRECTION ( 'NONE',  ( 0.000000000000000000, -1.000000000000000000, 0.000000000000000000 ) ) ;
#4849=CARTESIAN_POINT ( 'NONE',  ( -84.46793043747848628, -25.56582313524723915, 161.3502830699509616 ) ) ;
#4851=CARTESIAN_POINT ( 'NONE',  ( 0.000000000000000000, -8.673617379884035472E-16, -17.01589776168603407 ) ) ;
#4862=CARTESIAN_POINT ( 'NONE',  ( -106.6432006776756083, -57.67119647726944009, 107.9924613694791589 ) ) ;
#4866=CARTESIAN_POINT ( 'NONE',  ( 89.21410497458975897, -29.99999999999997513, 9.589292377912048693 ) ) ;
#4867=CARTESIAN_POINT ( 'NONE',  ( -74.38379737572475392, -29.99999999999997513, 152.0617010018234794 ) ) ;
#4868=CARTESIAN_POINT ( 'NONE',  ( -57.09792055977870007, -29.08279639372222647, 60.54515176239379315 ) ) ;
#4873=CARTESIAN_POINT ( 'NONE',  ( -103.3953119595051788, -60.16512775842720373, 192.1477606830822822 ) ) ;
#4879=CARTESIAN_POINT ( 'NONE',  ( 2.377971214860273304E-07, -59.99999999999998579, 39.63907915656436387 ) ) ;
#4885=CARTESIAN_POINT ( 'NONE',  ( 69.77518918526168079, -29.99999999999999645, 94.60611941633173672 ) ) ;
#4892=CARTESIAN_POINT ( 'NONE',  ( -28.19790697388618383, -18.63285467839684983, 28.87379585876446697 ) ) ;
#4896=CARTESIAN_POINT ( 'NONE',  ( 47.00367278406724125, -22.23533693108482723, 41.16701144914247834 ) ) ;
#4900=CARTESIAN_POINT ( 'NONE',  ( -108.8824160030044652, -38.35653676688028213, 190.5054770832236954 ) ) ;
#4902=CARTESIAN_POINT ( 'NONE',  ( 90.63064853328148729, -38.34546238407526175, 14.30285600733137485 ) ) ;
#4903=CARTESIAN_POINT ( 'NONE',  ( 82.86271956844252884, -60.00000000000014211, 189.8647660441692437 ) ) ;
#4911=CARTESIAN_POINT ( 'NONE',  ( 102.7341935722522805, -60.00000000000002842, 200.7825474415656686 ) ) ;
#4919=CARTESIAN_POINT ( 'NONE',  ( -96.94769293072555172, -38.48349360550125198, 201.1369200050914685 ) ) ;
#4932=CARTESIAN_POINT ( 'NONE',  ( 81.23237909639242105, -56.97435546150522612, 180.4903185276303361 ) ) ;
#4938=FACE_OUTER_BOUND ( 'NONE', #68012, .T. ) ;
#4972=CARTESIAN_POINT ( 'NONE',  ( -98.90204163354637501, -60.00000000000000711, 202.1654228340109967 ) ) ;
#4979=CARTESIAN_POINT ( 'NONE',  ( -83.88175480885155366, -42.98347005089964767, 181.2433426847502176 ) ) ;
#4985=CARTESIAN_POINT ( 'NONE',  ( -83.48701994937339066, -37.82282612950775302, 31.99776073991571934 ) ) ;
#4991=CARTESIAN_POINT ( 'NONE',  ( 79.87681789614374850, -30.00000000000000711, 191.0754539389706395 ) ) ;
#4993=CARTESIAN_POINT ( 'NONE',  ( -87.68152309050471160, -14.21045842199426801, 32.26861779447729361 ) ) ;
#4994=CARTESIAN_POINT ( 'NONE',  ( -66.93347199945957016, -25.58110973058455784, 84.52057819029118946 ) ) ;
#4997=CARTESIAN_POINT ( 'NONE',  ( 49.49803543560198449, -60.00000000002933831, 76.94089586485750942 ) ) ;
#5008=CARTESIAN_POINT ( 'NONE',  ( -92.63142467325774021, -60.00000000000000000, -3.230052685997783612 ) ) ;
#5011=CARTESIAN_POINT ( 'NONE',  ( 83.88447113947664491, -60.00000000000000000, 191.6821499555289847 ) ) ;
#5023=CARTESIAN_POINT ( 'NONE',  ( 33.08419194243336392, -32.55809666592025309, 33.08005832449853756 ) ) ;
#5024=CARTESIAN_POINT ( 'NONE',  ( 5.820808985959283532, -2.898778190268130493E-12, -21.65942590380460686 ) ) ;
#5038=CARTESIAN_POINT ( 'NONE',  ( 92.00383831918911426, -59.99999999999999289, 6.129265091283676803 ) ) ;
#5044=CARTESIAN_POINT ( 'NONE',  ( -89.67601645498943697, -30.00000000002656364, 1.152961518554983078 ) ) ;
#5057=ORIENTED_EDGE ( 'NONE', *, *, #5071, .T. ) ;
#5058=CARTESIAN_POINT ( 'NONE',  ( 78.61532337604826637, -46.43317018272926333, 144.3717807119670624 ) ) ;
#5065=CARTESIAN_POINT ( 'NONE',  ( -87.17917008083185237, -57.58863837343483283, 203.1758066736668980 ) ) ;
#5071=EDGE_CURVE ( 'NONE', #81125, #40837, #23438, .T. ) ;
#5075=CARTESIAN_POINT ( 'NONE',  ( -5.978393154364650464, -13.00690510473827644, 32.07137290849176026 ) ) ;
#5088=CARTESIAN_POINT ( 'NONE',  ( 4.093755603727620596, -17.90092510166400430, -37.94411461619921511 ) ) ;
#5089=CARTESIAN_POINT ( 'NONE',  ( -82.56376108564677452, -30.00000000000000711, 149.7403354104212951 ) ) ;
#5092=B_SPLINE_CURVE_WITH_KNOTS ( 'NONE', 3,
 ( #50724, #76080, #60471, #11333, #51265, #83115 ),
 .UNSPECIFIED., .F., .F.,
 ( 4, 2, 4 ),
 ( 2.275079091765669941E-15, 0.01116218283128518791, 0.02232436566256810334 ),
 .UNSPECIFIED. ) ;
#5093=COLOUR_RGB ( '', 0.09019608, 0.27058824, 0.51372549) ;
#5096=CARTESIAN_POINT ( 'NONE',  ( 101.8121882041653805, -57.63159399422936957, 203.3427569746260986 ) ) ;
#5102=CARTESIAN_POINT ( 'NONE',  ( -70.60798716468931957, -60.00000000000000711, 144.8513084279401255 ) ) ;
#5107=CARTESIAN_POINT ( 'NONE',  ( -85.74525919723035372, -39.25732588298068038, 186.2133864294523562 ) ) ;
#5115=CARTESIAN_POINT ( 'NONE',  ( -82.65297077345887544, -37.77213538829948192, -12.24075959479144515 ) ) ;
#5122=CARTESIAN_POINT ( 'NONE',  ( 3.088855081073062209E-15, -4.285714285714286476, 25.22241582816893413 ) ) ;
#5125=CARTESIAN_POINT ( 'NONE',  ( 82.54285424309888697, -59.99999999999997868, -29.20801037391389698 ) ) ;
#5126=CARTESIAN_POINT ( 'NONE',  ( -80.01308992809121889, -36.03078623675013858, 142.1897297268717182 ) ) ;
#5130=CARTESIAN_POINT ( 'NONE',  ( 85.39890529347994175, -57.56671838092738369, 202.4583528846124807 ) ) ;
#5143=EDGE_CURVE ( 'NONE', #60348, #84468, #98885, .T. ) ;
#5150=CARTESIAN_POINT ( 'NONE',  ( -61.00210428163805432, -14.21045842199449005, 86.20094954650318186 ) ) ;
#5151=CARTESIAN_POINT ( 'NONE',  ( 28.23832643585050661, -46.43268247453659825, 33.77938694114138940 ) ) ;
#5158=CARTESIAN_POINT ( 'NONE',  ( -25.22241582816893413, -4.285714285714295357, 1.650803255657545376 ) ) ;
#5166=CARTESIAN_POINT ( 'NONE',  ( 88.35295536199733135, -29.99999999999992539, 187.5720053298597918 ) ) ;
#5170=CARTESIAN_POINT ( 'NONE',  ( 77.60255351419164072, -29.99999999999999645, -16.19249867753874739 ) ) ;
#5176=ORIENTED_EDGE ( 'NONE', *, *, #104320, .F. ) ;
#5192=CARTESIAN_POINT ( 'NONE',  ( 63.47440578363637798, -42.95821100843742357, 83.53516802226259585 ) ) ;
#5196=CARTESIAN_POINT ( 'NONE',  ( -65.57582204172831553, -37.93122577949567642, -32.64385588336286759 ) ) ;
#5204=CARTESIAN_POINT ( 'NONE',  ( -61.96882301508342294, -60.00000000000000000, -29.16134989615447282 ) ) ;
#5210=CARTESIAN_POINT ( 'NONE',  ( 86.86677769205006427, -24.33857869492717896, 185.9205046572136268 ) ) ;
#5214=CARTESIAN_POINT ( 'NONE',  ( 33.74163818581530450, -22.91772919730411928, -31.53376869490962520 ) ) ;
#5218=CARTESIAN_POINT ( 'NONE',  ( -100.7601573074881856, -30.00000000000000711, 180.6867523902226651 ) ) ;
#5222=CARTESIAN_POINT ( 'NONE',  ( 22.78484890785721007, -57.67311484157481516, 42.64563236796616508 ) ) ;
#5238=CARTESIAN_POINT ( 'NONE',  ( -13.66789640398582506, -53.40249338299810233, 32.88025485198195952 ) ) ;
#5239=CARTESIAN_POINT ( 'NONE',  ( -106.4066146825508525, -59.99999999999998579, 177.3607894768842357 ) ) ;
#5268=CARTESIAN_POINT ( 'NONE',  ( -93.10945532521039070, -59.99999999999134559, 204.9187477655829923 ) ) ;
#5271=CARTESIAN_POINT ( 'NONE',  ( 52.96195712877477746, -59.99999999999034372, -39.71698208206965575 ) ) ;
#5274=CARTESIAN_POINT ( 'NONE',  ( -111.4777060157506128, -60.00000000000003553, 136.6114436209108760 ) ) ;
#5275=CARTESIAN_POINT ( 'NONE',  ( 11.52855662273420201, -56.87783920999704890, 33.40081634995917881 ) ) ;
#5279=CARTESIAN_POINT ( 'NONE',  ( -48.68168605414437167, -60.29016101526869420, 55.32621818811512071 ) ) ;
#5291=CARTESIAN_POINT ( 'NONE',  ( 103.7884372076644013, -30.00000000000040501, 196.7705344244245111 ) ) ;
#5296=CARTESIAN_POINT ( 'NONE',  ( 95.92227023446287149, -29.99999999999999645, 191.2948881066602098 ) ) ;
#5297=DIRECTION ( 'NONE',  ( 0.000000000000000000, -1.000000000000000000, 0.000000000000000000 ) ) ;
#5310=CARTESIAN_POINT ( 'NONE',  ( 88.55857370903616754, -38.54383131503518456, 200.1465328989446562 ) ) ;
#5312=CARTESIAN_POINT ( 'NONE',  ( 84.94965200653656723, -52.70721121321142988, 8.412351094543845775 ) ) ;
#5329=CARTESIAN_POINT ( 'NONE',  ( -38.11555372032616873, -36.98165116605179037, 47.45724135341656336 ) ) ;
#5335=CARTESIAN_POINT ( 'NONE',  ( 83.99905227920338291, -46.55430364312917391, 184.5977050623376954 ) ) ;
#5340=CARTESIAN_POINT ( 'NONE',  ( 94.39577478536416777, -57.67124450908064404, -0.09368570482560956147 ) ) ;
#5349=AXIS2_PLACEMENT_3D ( 'NONE', #6421, #75953, #9607 ) ;
#5351=CARTESIAN_POINT ( 'NONE',  ( 32.46779435786267243, -22.86540350073456906, 32.67550843060059407 ) ) ;
#5360=CARTESIAN_POINT ( 'NONE',  ( -102.2638839044604708, -37.99999999999999289, 159.8928815567210791 ) ) ;
#5367=CARTESIAN_POINT ( 'NONE',  ( -0.001407372325411601578, -47.40884528607705306, -34.79112416808659702 ) ) ;
#5369=CARTESIAN_POINT ( 'NONE',  ( 57.19142787028389563, -60.00000000000000000, 91.73163585818134891 ) ) ;
#5375=CARTESIAN_POINT ( 'NONE',  ( -92.16884015762632032, -60.00000000000000000, -13.23401553576926126 ) ) ;
#5382=CARTESIAN_POINT ( 'NONE',  ( -84.03169659675084802, -29.04760639451814441, 162.8244371882715313 ) ) ;
#5384=CARTESIAN_POINT ( 'NONE',  ( -4.418225343294782448, -0.000000000000000000, -16.46939662769500856 ) ) ;
#5392=CARTESIAN_POINT ( 'NONE',  ( -87.17917008083185237, -57.58863837343483283, 203.1758066736668980 ) ) ;
#5397=CARTESIAN_POINT ( 'NONE',  ( 87.76937946118395928, -14.21045842199442433, -6.551255600857777139 ) ) ;
#5399=CARTESIAN_POINT ( 'NONE',  ( -70.85198506086598513, -59.99999999999993605, 164.3657034848495186 ) ) ;
#5401=CARTESIAN_POINT ( 'NONE',  ( -55.90002588988700438, -53.38502262911126905, 68.14443619204867275 ) ) ;
#5405=CARTESIAN_POINT ( 'NONE',  ( -101.3229872063272126, -52.72700633799254888, 193.0131086346895302 ) ) ;
#5418=CARTESIAN_POINT ( 'NONE',  ( -28.36237863811216897, -22.10885024312786129, 29.53413804810376675 ) ) ;
#5421=CARTESIAN_POINT ( 'NONE',  ( 47.61335411246825089, -53.35666067661759371, 51.28262531696475435 ) ) ;
#5426=CARTESIAN_POINT ( 'NONE',  ( -110.8605419238568999, -38.35619012346779755, 166.9666919078160277 ) ) ;
#5428=CARTESIAN_POINT ( 'NONE',  ( 91.33513191089157601, -38.39909729304942232, -10.01622609513604978 ) ) ;
#5429=CARTESIAN_POINT ( 'NONE',  ( 82.14211595064963944, -60.00000000000011369, 187.9158604088532911 ) ) ;
#5437=CARTESIAN_POINT ( 'NONE',  ( 95.33093839319907659, -60.00000000000000711, 202.5686516758067910 ) ) ;
#5440=CARTESIAN_POINT ( 'NONE',  ( 56.66478156921341025, -18.67503977128396642, 55.37327426273083830 ) ) ;
#5445=CARTESIAN_POINT ( 'NONE',  ( -91.30009454865734142, -38.40134775628936836, -10.51120872120718097 ) ) ;
#5453=ADVANCED_FACE ( 'NONE', ( #97172 ), #33422, .F. ) ;
#5457=CARTESIAN_POINT ( 'NONE',  ( 84.44844196884631060, -29.00443322529857682, 166.8952161098262934 ) ) ;
#5469=CARTESIAN_POINT ( 'NONE',  ( -76.42400522962535092, -29.99999999999999645, -17.06061772383467101 ) ) ;
#5472=CARTESIAN_POINT ( 'NONE',  ( -0.08974973093378038613, -18.03000550220510334, 35.00499666190406600 ) ) ;
#5498=CARTESIAN_POINT ( 'NONE',  ( -112.1962952311318134, -60.00000000000000000, 169.8889608969054734 ) ) ;
#5501=CARTESIAN_POINT ( 'NONE',  ( -84.23719628859713282, -42.98023119072136211, 182.9348151746076496 ) ) ;
#5508=CARTESIAN_POINT ( 'NONE',  ( -87.19071514201230855, -60.15150547609031406, 31.77301145132557636 ) ) ;
#5512=PLANE ( 'NONE',  #47637 ) ;
#5514=CARTESIAN_POINT ( 'NONE',  ( 81.10520000301197285, -14.21045842199436926, 192.6066858413676925 ) ) ;
#5515=CARTESIAN_POINT ( 'NONE',  ( -97.37795077744138439, -14.21045842199441722, 96.97852642953840530 ) ) ;
#5517=CARTESIAN_POINT ( 'NONE',  ( -66.25603766433088992, -36.00965392168274803, 88.05982369710793023 ) ) ;
#5520=CARTESIAN_POINT ( 'NONE',  ( 74.18019383371068898, -60.00000000000248690, 189.7622998913098229 ) ) ;
#5528=CARTESIAN_POINT ( 'NONE',  ( -92.13623215974652680, -60.00000000000000000, 3.793454175199357792 ) ) ;
#5541=CARTESIAN_POINT ( 'NONE',  ( 35.45451790554718485, -32.57629471585633496, 34.20714003089912580 ) ) ;
#5542=CARTESIAN_POINT ( 'NONE',  ( 2.083846472846741813E-15, -1.734723475976807094E-15, 17.01589776168603407 ) ) ;
#5554=CARTESIAN_POINT ( 'NONE',  ( 98.00624854155054777, -59.99999999999999289, 68.96488094194445750 ) ) ;
#5562=CARTESIAN_POINT ( 'NONE',  ( -89.53105629151139055, -30.00000000001332623, 3.004387943588768373 ) ) ;
#5577=CARTESIAN_POINT ( 'NONE',  ( 80.03392445538010236, -32.55901999570951233, 138.7251254010801915 ) ) ;
#5580=EDGE_LOOP ( 'NONE', ( #51468, #55203, #82744, #64999, #84871, #98218 ) ) ;
#5587=EDGE_CURVE ( 'NONE', #38016, #70795, #11956, .T. ) ;
#5597=CARTESIAN_POINT ( 'NONE',  ( -33.77811757699123518, -23.48828957687707231, 33.07784126555895199 ) ) ;
#5609=CARTESIAN_POINT ( 'NONE',  ( 63.34140952676320069, -30.10174061359070663, -32.02184817817584417 ) ) ;
#5610=CARTESIAN_POINT ( 'NONE',  ( -84.01570479851304185, -30.00000000000000000, 161.1131640044202129 ) ) ;
#5615=CARTESIAN_POINT ( 'NONE',  ( 106.9698911830091816, -57.65429730927083796, 200.0955121608643026 ) ) ;
#5621=CARTESIAN_POINT ( 'NONE',  ( -73.50155193450905244, -59.99999999999998579, 167.2054298968465957 ) ) ;
#5627=CARTESIAN_POINT ( 'NONE',  ( -84.81894751370330710, -50.19651377637536172, 188.8560073178213941 ) ) ;
#5634=CARTESIAN_POINT ( 'NONE',  ( -84.05617864326320898, -52.72894240072567129, -15.15459004269859911 ) ) ;
#5641=CARTESIAN_POINT ( 'NONE',  ( -20.16952962162108065, -4.285714285713656757, 15.50035291838862683 ) ) ;
#5643=CARTESIAN_POINT ( 'NONE',  ( 69.60540008574220394, -30.00000000000001421, -29.89027719438221453 ) ) ;
#5644=CARTESIAN_POINT ( 'NONE',  ( -80.71693047659314857, -32.56228764399944708, 142.8125308610640047 ) ) ;
#5646=CARTESIAN_POINT ( 'NONE',  ( 1.295095875561511761E-05, -30.00000000000000000, 37.00000000000000711 ) ) ;
#5648=CARTESIAN_POINT ( 'NONE',  ( 93.62081204623362396, -57.61897985685533286, 204.5015724136271444 ) ) ;
#5657=CARTESIAN_POINT ( 'NONE',  ( -100.9117355037075754, -37.82075919422305077, 146.9395316649864753 ) ) ;
#5671=CARTESIAN_POINT ( 'NONE',  ( -12.46506237085073110, -30.00000000000006395, 37.03826559298295251 ) ) ;
#5672=CARTESIAN_POINT ( 'NONE',  ( 24.88419958317715341, -39.47653737364599635, 31.71990145829097685 ) ) ;
#5683=CARTESIAN_POINT ( 'NONE',  ( 30.90300773556078084, -60.00000000000000000, -40.80305823694001077 ) ) ;
#5687=CARTESIAN_POINT ( 'NONE',  ( 81.51344701192068953, -29.99999999999999645, -9.040800538730334068 ) ) ;
#5707=CARTESIAN_POINT ( 'NONE',  ( -82.68571612615870947, -60.00000000000005684, 189.3854813724193491 ) ) ;
#5708=CARTESIAN_POINT ( 'NONE',  ( 62.14462952195434298, -53.38719692732349387, 84.99936359579984924 ) ) ;
#5712=CARTESIAN_POINT ( 'NONE',  ( -65.16315667887181462, -37.89597709104619128, -32.76824749171753837 ) ) ;
#5715=CARTESIAN_POINT ( 'NONE',  ( -47.47329288218261922, -57.67116814553164517, -40.40967777935767202 ) ) ;
#5720=CARTESIAN_POINT ( 'NONE',  ( 43.15338089903108454, -60.00000000000001421, -33.32712317583224149 ) ) ;
#5721=COLOUR_RGB ( '', 0.31764706, 0.68627451, 0.89019608) ;
#5725=CARTESIAN_POINT ( 'NONE',  ( 86.49766297946776206, -46.48553392096007997, 190.2538031942813461 ) ) ;
#5732=CARTESIAN_POINT ( 'NONE',  ( 25.54149015966096670, -60.00000000000000000, 41.31963070409977234 ) ) ;
#5734=CARTESIAN_POINT ( 'NONE',  ( -98.93669197873286691, -30.00000000000000355, 188.9772157868254965 ) ) ;
#5740=CARTESIAN_POINT ( 'NONE',  ( 40.07782535012948699, -57.69200939151943430, 55.80417300162885397 ) ) ;
#5750=CARTESIAN_POINT ( 'NONE',  ( -87.19032044583666163, -28.00046754097470725, 187.4561909348103370 ) ) ;
#5755=CARTESIAN_POINT ( 'NONE',  ( -11.08525313475499630, -18.58645957121905212, 27.00989044373123349 ) ) ;
#5756=CARTESIAN_POINT ( 'NONE',  ( -86.09965174442223201, -60.00000000000002132, 13.47334620854856624 ) ) ;
#5761=DIRECTION ( 'NONE',  ( 0.000000000000000000, -1.000000000000000000, 0.000000000000000000 ) ) ;
#5763=CARTESIAN_POINT ( 'NONE',  ( 72.09784563428850390, -59.99999999999999289, 155.0115803735216389 ) ) ;
#5784=CARTESIAN_POINT ( 'NONE',  ( -78.84470549551073759, -60.00000000000486722, 198.6068565147943161 ) ) ;
#5786=CARTESIAN_POINT ( 'NONE',  ( 75.21146677271600822, -60.00000000000000000, 182.8225648044053173 ) ) ;
#5789=CARTESIAN_POINT ( 'NONE',  ( -106.1205840060921730, -60.00000000000004263, 102.8126256328862667 ) ) ;
#5790=CARTESIAN_POINT ( 'NONE',  ( 11.12509248473755541, -22.06751002638328174, 27.59088369308159017 ) ) ;
#5793=CARTESIAN_POINT ( 'NONE',  ( -46.33873388880254396, -49.90047875932729227, 48.28660123752720068 ) ) ;
#5802=CARTESIAN_POINT ( 'NONE',  ( 108.4933579148305114, -30.00000000000335731, 186.4703362515614629 ) ) ;
#5805=CARTESIAN_POINT ( 'NONE',  ( 99.09352263291532381, -30.00000000000000000, 188.6044529824486062 ) ) ;
#5814=CARTESIAN_POINT ( 'NONE',  ( 0.000000000000000000, -30.00000000000000000, 0.000000000000000000 ) ) ;
#5822=CARTESIAN_POINT ( 'NONE',  ( 104.6793613277272925, -38.39935806952897224, 197.8364302557836538 ) ) ;
#5824=CARTESIAN_POINT ( 'NONE',  ( 83.26448648960058563, -37.81913187090151496, -6.272588225319124966 ) ) ;
#5826=CARTESIAN_POINT ( 'NONE',  ( 79.27568089365161086, -37.99999999999995737, 139.8675762540388803 ) ) ;
#5841=CARTESIAN_POINT ( 'NONE',  ( -15.49740174064447196, -17.95698503203060170, 35.11441465487863667 ) ) ;
#5845=CARTESIAN_POINT ( 'NONE',  ( 85.90364017214238856, -28.44064950339577180, 181.2095016147336537 ) ) ;
#5850=CARTESIAN_POINT ( 'NONE',  ( 94.23549906357385453, -57.67250308052000918, 23.25353176600918559 ) ) ;
#5854=EDGE_CURVE ( 'NONE', #22652, #105826, #68749, .T. ) ;
#5856=CARTESIAN_POINT ( 'NONE',  ( 7.016496648689620308, -19.12693412541480598, 35.17887506390064800 ) ) ;
#5864=CARTESIAN_POINT ( 'NONE',  ( -83.11375064820144587, -38.00000000000003553, -10.17571340337245545 ) ) ;
#5872=CARTESIAN_POINT ( 'NONE',  ( -59.17052589201637147, -60.22831900904334645, -29.94874486158233751 ) ) ;
#5879=CARTESIAN_POINT ( 'NONE',  ( -90.61290675944017892, -60.00000000000000711, -17.71793535203029180 ) ) ;
#5885=CARTESIAN_POINT ( 'NONE',  ( -80.67482880870019812, -49.91654882987682385, 164.5101345921526104 ) ) ;
#5886=ORIENTED_EDGE ( 'NONE', *, *, #47720, .F. ) ;
#5897=CARTESIAN_POINT ( 'NONE',  ( -91.62307993511501536, -57.61497437271354727, 204.2871689995596967 ) ) ;
#5902=CARTESIAN_POINT ( 'NONE',  ( 84.06490631893382215, -29.99999999999999645, -21.85721834217820714 ) ) ;
#5904=CARTESIAN_POINT ( 'NONE',  ( -39.04695011312426800, -60.00000000000001421, 54.77420429098338417 ) ) ;
#5906=CARTESIAN_POINT ( 'NONE',  ( -52.28272210538586506, -42.97553591916267379, 56.06210961058410192 ) ) ;
#5912=CARTESIAN_POINT ( 'NONE',  ( -103.5726650996749356, -60.16286882071497644, 191.7881775096330443 ) ) ;
#5918=CARTESIAN_POINT ( 'NONE',  ( 87.17001200814932815, -38.36464134849014584, -20.67025014127871785 ) ) ;
#5923=CARTESIAN_POINT ( 'NONE',  ( 62.38470394483648818, -29.99999999999999645, 73.04314485712862393 ) ) ;
#5924=DIRECTION ( 'NONE',  ( 0.000000000000000000, -0.000000000000000000, -1.000000000000000000 ) ) ;
#5931=CARTESIAN_POINT ( 'NONE',  ( 50.78782189071710462, -39.51075776922833427, 52.07867872815624111 ) ) ;
#5934=CARTESIAN_POINT ( 'NONE',  ( -110.5479244313631710, -38.35611966620975011, 181.9352924883354206 ) ) ;
#5936=CARTESIAN_POINT ( 'NONE',  ( 91.21740072965818058, -38.35861323033353187, -0.9391089420829346057 ) ) ;
#5947=CARTESIAN_POINT ( 'NONE',  ( 95.21542849279514087, -60.00000000000001421, 202.5699345040212904 ) ) ;
#5952=CARTESIAN_POINT ( 'NONE',  ( 58.95658943640736993, -25.60101595818816023, 63.31392996776931170 ) ) ;
#5959=CARTESIAN_POINT ( 'NONE',  ( -91.27412109437786114, -38.35458256084967132, 28.31964854624011352 ) ) ;
#5967=CARTESIAN_POINT ( 'NONE',  ( 84.52692572873411336, -32.42336717775761201, 173.3565263439695343 ) ) ;
#5980=CARTESIAN_POINT ( 'NONE',  ( -81.34045205995600725, -30.00000000000000711, -10.45056096668239043 ) ) ;
#5984=CARTESIAN_POINT ( 'NONE',  ( -1.246384481104801489, -18.05976919417167537, 35.00911013355869272 ) ) ;
#6010=CARTESIAN_POINT ( 'NONE',  ( -110.2852303711805746, -60.00000000000000000, 145.7623735510408665 ) ) ;
#6015=CARTESIAN_POINT ( 'NONE',  ( -85.88231755690129887, -21.77401794985988204, 171.2094949271552764 ) ) ;
#6018=CIRCLE ( 'NONE', #26722, 8.000000000000000000 ) ;
#6020=CARTESIAN_POINT ( 'NONE',  ( -0.01402285133662556187, -30.00000000000000000, -39.99999948934169680 ) ) ;
#6023=CARTESIAN_POINT ( 'NONE',  ( -86.14801153885079543, -60.13788232086688623, 9.933174785324942135 ) ) ;
#6029=CARTESIAN_POINT ( 'NONE',  ( 77.72372478688149045, -60.00000000000015632, 197.5639835283903381 ) ) ;
#6031=CARTESIAN_POINT ( 'NONE',  ( -101.8002770060248139, -59.99999999999998579, 77.51242708015574578 ) ) ;
#6032=CARTESIAN_POINT ( 'NONE',  ( -64.03467178915637703, -49.91529051540093320, 88.80954775168983417 ) ) ;
#6035=CARTESIAN_POINT ( 'NONE',  ( 62.33054962693324086, -60.00000000003888800, 116.7585282323999110 ) ) ;
#6037=CARTESIAN_POINT ( 'NONE',  ( 1.987573926653205314, -25.54829021846704862, 28.14551609985228708 ) ) ;
#6046=CARTESIAN_POINT ( 'NONE',  ( -92.96207233507917067, -60.00000000000000000, 202.4679484878635378 ) ) ;
#6056=CARTESIAN_POINT ( 'NONE',  ( 105.0433157361263596, -60.00000000000000711, 187.5698151985990307 ) ) ;
#6057=CARTESIAN_POINT ( 'NONE',  ( -37.74004406342657347, -32.59350783026462750, 35.55426695422483618 ) ) ;
#6060=CARTESIAN_POINT ( 'NONE',  ( 34.08083780335558544, -29.09990395782033801, 32.84435087873961834 ) ) ;
#6062=CARTESIAN_POINT ( 'NONE',  ( -5.820808985953483727, -9.668376379147026354E-13, -21.65942590380073085 ) ) ;
#6065=B_SPLINE_CURVE_WITH_KNOTS ( 'NONE', 3,
 ( #46980, #63727, #5472, #38395, #71260, #104154, #63188, #22213, #5984, #55063, #14071, #87993, #47509, #80401, #64255, #41547, #57184, #65824, #106263, #512, #66899, #82539, #8108, #65295, #16206, #25952, #98186, #58812, #90100, #49088, #98703, #81990, #83588, #33477, #73903, #24858, #66350, #41022, #31884, #74433, #42606, #9696, #25403, #99235, #1051, #58263, #23810, #55895, #91187, #16743, #91705, #99783, #74959, #57708, #17822, #105748, #50673, #49633, #17294, #64768, #97643, #42076, #90635, #56655, #81454, #89580, #8643, #7568, #50168, #15673, #83071, #48563, #34026, #40485, #73364, #9162, #24341, #32425, #32954, #76560, #68498, #92206, #76034, #59882, #100309, #59342, #92755, #75504, #67954, #94367, #2130, #2671, #85198, #18912, #20530, #60938, #51214, #27001, #43151, #53367, #85754, #18363, #93828, #35084, #36164, #51757, #34560, #52826, #69556, #101907, #84671, #12359, #19981, #60419, #10755, #93297, #86287, #84140, #43672, #26471, #11827, #100837, #11283, #1598 ),
 .UNSPECIFIED., .F., .F.,
 ( 4, 2, 2, 2, 1, 2, 2, 2, 2, 1, 2, 2, 1, 2, 2, 1, 1, 2, 2, 1, 2, 2, 1, 1, 2, 2, 1, 2, 2, 1, 2, 2, 2, 2, 2, 2, 1, 1, 2, 2, 2, 2, 2, 2, 2, 1, 1, 1, 2, 2, 1, 1, 2, 2, 1, 2, 2, 1, 1, 1, 2, 2, 2, 1, 1, 2, 2, 2, 2, 1, 2, 2, 2, 4 ),
 ( 0.4962367771140062667, 0.4972206896587050839, 0.4982046022034038457, 0.5001724272928014248, 0.5041080774715966939, 0.5119793778291871211, 0.5277219785443679756, 0.5296898036337656102, 0.5316576287231631337, 0.5355932789019584028, 0.5434645792595488301, 0.5592071799747297955, 0.5611750050641273191, 0.5621589176088261919, 0.5626508738811756283, 0.5631428301535250647, 0.5670784803323204448, 0.5749497806899113161, 0.5906923814050930588, 0.5926602064944908044, 0.5936441190391896772, 0.5941360753115390025, 0.5946280315838885500, 0.5985636817626840411, 0.6064349821202751345, 0.6221775828354573212, 0.6241454079248550668, 0.6246373641972045032, 0.6251293204695539396, 0.6261132330142528124, 0.6300488831930485256, 0.6379201835506397300, 0.6536627842658222498, 0.6851479856961874004, 0.6871158107855852570, 0.6876077670579346934, 0.6880997233302842409, 0.6890836358749831136, 0.6930192860537787158, 0.7008905864113700313, 0.7166331871265524400, 0.7205688373053480422, 0.7245044874841436444, 0.7323757878417348488, 0.7481183885569173686, 0.7491023011016164634, 0.7495942573739660109, 0.7498402355101407846, 0.7499632245782281714, 0.7500862136463155583, 0.7520540387357136369, 0.7559896889145101273, 0.7638609892721028860, 0.7796035899872886255, 0.7805875025319877203, 0.7810794588043372677, 0.7813254369405121524, 0.7815714150766870372, 0.7835392401660863371, 0.7874748903448847148, 0.7953461907024816924, 0.8110887914176753144, 0.8130566165070745033, 0.8150244415964736922, 0.8189600917752720699, 0.8268313921328689364, 0.8425739928480624474, 0.8740591942784496915, 0.8779948444572482913, 0.8819304946360466690, 0.8898017949936435356, 0.9055443957088372686, 0.9370295971392248457, 1.000000000000000000 ),
 .UNSPECIFIED. ) ;
#6066=CARTESIAN_POINT ( 'NONE',  ( -67.90781492711421663, -38.33416998424474542, 125.1147017743826382 ) ) ;
#6082=CARTESIAN_POINT ( 'NONE',  ( 97.90254053569493919, -60.00000000000000711, 68.32195872189682007 ) ) ;
#6090=CARTESIAN_POINT ( 'NONE',  ( -86.86330325217545578, -30.00000000000164846, -18.79756195431963661 ) ) ;
#6094=CARTESIAN_POINT ( 'NONE',  ( 82.62819499073798113, -45.27882038833382694, -15.10946084058340411 ) ) ;
#6100=CARTESIAN_POINT ( 'NONE',  ( 81.05849975536304441, -32.56051081393310653, 144.8530755112767565 ) ) ;
#6107=CARTESIAN_POINT ( 'NONE',  ( -15.40724846713353813, -57.67135988443339301, 41.78154393163084279 ) ) ;
#6112=DIRECTION ( 'NONE',  ( -0.000000000000000000, -1.000000000000000000, -0.000000000000000000 ) ) ;
#6117=CARTESIAN_POINT ( 'NONE',  ( -28.27173859142850176, -20.85003346561162374, 31.88408023871041408 ) ) ;
#6130=CARTESIAN_POINT ( 'NONE',  ( -62.79708356444599104, -30.00000000000000000, 74.14398739475227273 ) ) ;
#6136=CARTESIAN_POINT ( 'NONE',  ( 104.5422953853447581, -57.64203673969820585, 202.0104448647194602 ) ) ;
#6137=AXIS2_PLACEMENT_3D ( 'NONE', #88202, #14284, #72007 ) ;
#6138=CARTESIAN_POINT ( 'NONE',  ( 67.74083062384904963, -34.58965796570005580, -22.72020771579463272 ) ) ;
#6142=CARTESIAN_POINT ( 'NONE',  ( -73.13094403033801427, -59.99999999999999289, 163.6547797536228472 ) ) ;
#6146=CARTESIAN_POINT ( 'NONE',  ( -85.38396510212227497, -46.56038326034761354, 188.3815645333082216 ) ) ;
#6153=CARTESIAN_POINT ( 'NONE',  ( -84.90132116126285666, -60.19215146778790881, -16.22236961991315596 ) ) ;
#6162=CARTESIAN_POINT ( 'NONE',  ( 76.02438791174152755, -14.21045842199433729, -24.18563911012876844 ) ) ;
#6163=CARTESIAN_POINT ( 'NONE',  ( -80.73742772600893147, -29.09286051066668577, 139.3498210207160639 ) ) ;
#6165=CARTESIAN_POINT ( 'NONE',  ( 8.180516222381777780, -14.21045842199445630, 34.35482301558341334 ) ) ;
#6167=CARTESIAN_POINT ( 'NONE',  ( 76.35456037190438394, -57.53670657966636526, 193.9177342501030807 ) ) ;
#6175=CARTESIAN_POINT ( 'NONE',  ( -105.6705936910478698, -60.15501511360662334, 156.3715117094907612 ) ) ;
#6186=CARTESIAN_POINT ( 'NONE',  ( -16.61716630718971643, -29.99999999999995026, 37.21284229651715947 ) ) ;
#6187=CARTESIAN_POINT ( 'NONE',  ( 25.87815429224528785, -18.61428468264773528, 28.34824171517409752 ) ) ;
#6198=CARTESIAN_POINT ( 'NONE',  ( 14.21314216640385908, -60.00000000000000711, -42.20886373635748612 ) ) ;
#6225=CARTESIAN_POINT ( 'NONE',  ( 64.30440556324268186, -18.62726074519799724, 73.56828063249902527 ) ) ;
#6239=CARTESIAN_POINT ( 'NONE',  ( 86.39719173753884718, -50.13946290863540156, 191.2655366294524981 ) ) ;
#6249=CARTESIAN_POINT ( 'NONE',  ( 21.44740118747756341, -59.99999999999999289, 40.42893638695045411 ) ) ;
#6250=CARTESIAN_POINT ( 'NONE',  ( -99.84481721452227987, -29.99999999999999645, 186.2371469292183406 ) ) ;
#6253=CARTESIAN_POINT ( 'NONE',  ( 35.36861649463124735, -57.69554417999864171, 49.52702078849532086 ) ) ;
#6254=EDGE_CURVE ( 'NONE', #35136, #62746, #28852, .T. ) ;
#6261=CARTESIAN_POINT ( 'NONE',  ( -18.78363382869726195, -60.00000000000001421, 40.07425195021468767 ) ) ;
#6264=CARTESIAN_POINT ( 'NONE',  ( -87.15827005838086450, -24.32436580448878516, 187.0120937654315014 ) ) ;
#6268=CARTESIAN_POINT ( 'NONE',  ( -13.47192767882545539, -39.47621330262420258, 30.55147369851395212 ) ) ;
#6269=CARTESIAN_POINT ( 'NONE',  ( -106.2097612562338753, -59.99999999999998579, 163.7908689420960400 ) ) ;
#6279=CARTESIAN_POINT ( 'NONE',  ( 66.96457860869179513, -60.00000000000000000, 126.4729726693442302 ) ) ;
#6287=CARTESIAN_POINT ( 'NONE',  ( 16.61664997849939240, -30.00000000000006395, 37.21280938527437598 ) ) ;
#6299=CARTESIAN_POINT ( 'NONE',  ( -113.3259981442381275, -59.99999999999020872, 187.7190709742288277 ) ) ;
#6301=CARTESIAN_POINT ( 'NONE',  ( 79.18097233721817929, -60.00000000000002132, 194.8823859941057037 ) ) ;
#6304=CARTESIAN_POINT ( 'NONE',  ( -106.6847104835838564, -14.21045842199429288, 180.1424598013736329 ) ) ;
#6305=CARTESIAN_POINT ( 'NONE',  ( 9.152592288502010121, -32.51055960119349209, 29.30987820687813894 ) ) ;
#6308=CARTESIAN_POINT ( 'NONE',  ( -44.90547982323007403, -49.89649444956833690, 46.32591069718235843 ) ) ;
#6321=CARTESIAN_POINT ( 'NONE',  ( 104.1025144181177211, -30.00000000000091305, 196.4537446789288708 ) ) ;
#6323=CARTESIAN_POINT ( 'NONE',  ( 97.95630416740392832, -30.00000000000000000, 137.2274071578905250 ) ) ;
#6337=CARTESIAN_POINT ( 'NONE',  ( 89.78679446632952477, -38.52166357420221487, 200.5186810406769666 ) ) ;
#6339=CARTESIAN_POINT ( 'NONE',  ( 84.01433852174905326, -45.28719617900539163, 2.480345902927773238 ) ) ;
#6340=CARTESIAN_POINT ( 'NONE',  ( 67.06464718582454054, -38.00000000000002132, 91.54358707406134954 ) ) ;
#6361=CARTESIAN_POINT ( 'NONE',  ( -37.42621287545377129, -36.69657090219475037, 46.66406363766312637 ) ) ;
#6368=CARTESIAN_POINT ( 'NONE',  ( 86.40507261641900527, -17.60714839840921186, 177.3339586084961752 ) ) ;
#6373=CARTESIAN_POINT ( 'NONE',  ( 94.51533167486907416, -57.67223201566687862, 27.17635600706317689 ) ) ;
#6390=CARTESIAN_POINT ( 'NONE',  ( -5.452796619269896006, -22.28572503460438625, -30.53339323392108895 ) ) ;
#6392=CARTESIAN_POINT ( 'NONE',  ( -83.28104296813326357, -38.00000000000002842, 29.79366431696643147 ) ) ;
#6398=CARTESIAN_POINT ( 'NONE',  ( -8.888168502148841910, -16.05798408390882770, -34.89684864719075819 ) ) ;
#6400=CARTESIAN_POINT ( 'NONE',  ( -21.82264282896743879, -21.77046146735031584, -29.53569673438909149 ) ) ;
#6407=CARTESIAN_POINT ( 'NONE',  ( -92.31848817267784568, -60.00000000000000711, 1.263419265082847520 ) ) ;
#6411=CARTESIAN_POINT ( 'NONE',  ( 97.19053058376982790, -37.72816749976003337, 192.7922990471952005 ) ) ;
#6414=CARTESIAN_POINT ( 'NONE',  ( -84.99204860051307264, -18.63719649618825969, 155.3315940931620105 ) ) ;
#6421=CARTESIAN_POINT ( 'NONE',  ( 0.000000000000000000, -8.000000000000000000, 0.000000000000000000 ) ) ;
#6422=ORIENTED_EDGE ( 'NONE', *, *, #69819, .F. ) ;
#6424=CARTESIAN_POINT ( 'NONE',  ( -76.05665976993959987, -57.54410268428485153, 193.2876952671887523 ) ) ;
#6431=CARTESIAN_POINT ( 'NONE',  ( -57.68513734192992359, -30.00000000000002487, -33.51766283710919225 ) ) ;
#6432=CARTESIAN_POINT ( 'NONE',  ( -52.56680815376439853, -59.99999999999999289, 85.36473592189453541 ) ) ;
#6433=CARTESIAN_POINT ( 'NONE',  ( -52.87296361776452613, -53.37811214081175848, 61.20528467236419345 ) ) ;
#6439=CARTESIAN_POINT ( 'NONE',  ( -102.4347604686928292, -60.19196468994024940, 193.6661079742802372 ) ) ;
#6442=VERTEX_POINT ( 'NONE', #50418 ) ;
#6445=CARTESIAN_POINT ( 'NONE',  ( 105.3163565900507734, -38.35599845780108552, 119.8810476205262319 ) ) ;
#6450=CARTESIAN_POINT ( 'NONE',  ( 62.34328654791936941, -30.00000000000000355, 72.93326640765459956 ) ) ;
#6460=CARTESIAN_POINT ( 'NONE',  ( 49.86853440584077646, -25.66414929712663096, 46.00440597202735660 ) ) ;
#6462=CARTESIAN_POINT ( 'NONE',  ( 80.00000000000000000, 500000.0000000000582, -21.09707704303352926 ) ) ;
#6464=CARTESIAN_POINT ( 'NONE',  ( -104.2819284261560142, -38.40732750122956674, 198.1583120562690965 ) ) ;
#6467=CARTESIAN_POINT ( 'NONE',  ( 90.74859279193630357, -38.34261006322929433, 6.457795357414656046 ) ) ;
#6471=CARTESIAN_POINT ( 'NONE',  ( 102.1416586219354627, -37.84845812144148169, 158.6799647160197253 ) ) ;
#6478=CARTESIAN_POINT ( 'NONE',  ( 97.69789586047579633, -60.00000000000000711, 202.4097175802237132 ) ) ;
#6483=CARTESIAN_POINT ( 'NONE',  ( 57.28223379198149701, -56.85411367214971534, 73.21148081599464774 ) ) ;
#6488=CARTESIAN_POINT ( 'NONE',  ( -109.6873753914951095, -38.35590170415876798, 187.5827713266319847 ) ) ;
#6496=CARTESIAN_POINT ( 'NONE',  ( 81.09017685471619075, -60.52596391356583894, 183.7721125982857302 ) ) ;
#6527=ORIENTED_EDGE ( 'NONE', *, *, #19211, .F. ) ;
#6537=CARTESIAN_POINT ( 'NONE',  ( -106.4915674334330191, -59.99999999999998579, 119.4613221490214272 ) ) ;
#6543=CARTESIAN_POINT ( 'NONE',  ( -82.41309296567457920, -50.00852957772184482, 179.9562645980678042 ) ) ;
#6549=CARTESIAN_POINT ( 'NONE',  ( -83.04985898644524411, -37.82368260205146981, 27.05149038700534447 ) ) ;
#6557=CARTESIAN_POINT ( 'NONE',  ( 105.3887446370168135, -14.21045842199438347, 188.2131443117102663 ) ) ;
#6559=CARTESIAN_POINT ( 'NONE',  ( -99.88998825557715122, -14.21045842199445808, 111.7645417027540304 ) ) ;
#6560=CARTESIAN_POINT ( 'NONE',  ( -64.08967996622652663, -22.10365852731207781, 74.71439323467923543 ) ) ;
#6563=CARTESIAN_POINT ( 'NONE',  ( 74.39743302387351775, -60.00000000001976019, 190.5079982696796890 ) ) ;
#6565=CARTESIAN_POINT ( 'NONE',  ( 2.007425432336742421, -35.99147847551537183, 29.88588737300932507 ) ) ;
#6575=CARTESIAN_POINT ( 'NONE',  ( -105.2092481652586144, -60.00000000000000000, 199.0630387942247808 ) ) ;
#6586=CARTESIAN_POINT ( 'NONE',  ( -32.92861475816587813, -46.43446236043871522, 35.59579179906526036 ) ) ;
#6591=CARTESIAN_POINT ( 'NONE',  ( 38.12793368476380351, -18.75744117181308113, 32.82679780025620175 ) ) ;
#6592=CARTESIAN_POINT ( 'NONE',  ( 5.820808985963070725, 3.863013742957921305E-12, 21.65942590380143074 ) ) ;
#6598=CARTESIAN_POINT ( 'NONE',  ( -70.94375269799076023, -38.32938429878745268, 139.5278196086539992 ) ) ;
#6606=EDGE_CURVE ( 'NONE', #89859, #6703, #80159, .T. ) ;
#6611=CARTESIAN_POINT ( 'NONE',  ( 94.29218632224478824, -59.99999999999999289, 43.67174873413125624 ) ) ;
#6615=CARTESIAN_POINT ( 'NONE',  ( -2.499999999999999556, -8.980731864869721193, 18.56355538366596747 ) ) ;
#6618=CARTESIAN_POINT ( 'NONE',  ( -87.15276554055643032, -29.99999999999880984, -18.40125190494982377 ) ) ;
#6629=ORIENTED_EDGE ( 'NONE', *, *, #85837, .T. ) ;
#6635=CARTESIAN_POINT ( 'NONE',  ( 82.53639495069484155, -22.15581645431107560, 142.5669552073890713 ) ) ;
#6642=CARTESIAN_POINT ( 'NONE',  ( -2.832004189415751050, -57.67120204282113605, 41.61186672541032294 ) ) ;
#6653=CARTESIAN_POINT ( 'NONE',  ( -33.91219190039863207, -23.55191230016975013, 33.12023192167306007 ) ) ;
#6671=CARTESIAN_POINT ( 'NONE',  ( 91.14659984513072288, -57.61327065490866772, 204.1982474754030932 ) ) ;
#6677=CARTESIAN_POINT ( 'NONE',  ( -72.99129151139911187, -60.00000000000001421, 162.3848276614833708 ) ) ;
#6682=CARTESIAN_POINT ( 'NONE',  ( -86.14149206422753480, -24.77051094580461665, 180.5811988458752921 ) ) ;
#6688=CARTESIAN_POINT ( 'NONE',  ( -83.26091089620432228, -52.71980576326409107, -16.35630072882100094 ) ) ;
#6697=CARTESIAN_POINT ( 'NONE',  ( 16.57301948837259786, 0.000000000000000000, 4.453875240779975542 ) ) ;
#6700=CARTESIAN_POINT ( 'NONE',  ( 87.19843643122861465, -14.21045842199432307, -12.73007766572366606 ) ) ;
#6701=CARTESIAN_POINT ( 'NONE',  ( -77.56842044869100050, -22.13782245202111199, 118.4993958490866248 ) ) ;
#6703=VERTEX_POINT ( 'NONE', #27277 ) ;
#6704=CARTESIAN_POINT ( 'NONE',  ( 37.54937173058232247, -29.99999999999994671, 45.10736187702755018 ) ) ;
#6706=CARTESIAN_POINT ( 'NONE',  ( 71.41732950648065525, -57.68013501089347272, 166.1457025563863681 ) ) ;
#6716=CARTESIAN_POINT ( 'NONE',  ( -106.2188175271023454, -60.15512191887798821, 163.5221892134918278 ) ) ;
#6730=CARTESIAN_POINT ( 'NONE',  ( 29.95010272283230535, -18.65120705511333909, 29.35495255050972219 ) ) ;
#6741=CARTESIAN_POINT ( 'NONE',  ( 33.13150386023963989, -60.00000000000000000, -40.54080046662263470 ) ) ;
#6769=CARTESIAN_POINT ( 'NONE',  ( -57.52277648265613408, -60.00000000000000711, 75.19842801418919009 ) ) ;
#6770=CARTESIAN_POINT ( 'NONE',  ( 65.68943055205097892, -18.62638644426881385, 77.38610594788109154 ) ) ;
#6783=CARTESIAN_POINT ( 'NONE',  ( 86.48456354109262634, -17.02907541486232645, 183.8954425549199243 ) ) ;
#6792=CARTESIAN_POINT ( 'NONE',  ( 33.26116186592400936, -60.00000000000000711, 45.03127399487921423 ) ) ;
#6793=CARTESIAN_POINT ( 'NONE',  ( -98.86309202372207494, -30.00000000000000000, 189.1393124449016625 ) ) ;
#6796=CARTESIAN_POINT ( 'NONE',  ( 35.34307722619001879, -57.69551862194811065, 49.50014266750830672 ) ) ;
#6804=CARTESIAN_POINT ( 'NONE',  ( -25.16295877377567436, -60.00000000000000711, 41.21436381525774095 ) ) ;
#6807=CARTESIAN_POINT ( 'NONE',  ( -86.79095994919661905, -24.35916602586322810, 185.5609027488455354 ) ) ;
#6811=CARTESIAN_POINT ( 'NONE',  ( -13.61893567220048773, -49.92092318789549665, 32.29805822840884844 ) ) ;
#6820=CARTESIAN_POINT ( 'NONE',  ( 73.07582179318477245, -60.00000000000000711, 163.1513601165613068 ) ) ;
#6826=CARTESIAN_POINT ( 'NONE',  ( 39.73542184579525838, -14.21045842199450782, 43.02758494329003014 ) ) ;
#6834=CARTESIAN_POINT ( 'NONE',  ( 0.000000000000000000, 0.000000000000000000, 0.000000000000000000 ) ) ;
#6841=CARTESIAN_POINT ( 'NONE',  ( -79.72833642093169715, -59.99999999999754863, 199.4660593480937791 ) ) ;
#6843=CARTESIAN_POINT ( 'NONE',  ( 78.42325447905815849, -60.00000000000002842, 193.6655075910977359 ) ) ;
#6846=CARTESIAN_POINT ( 'NONE',  ( -113.3391396720030428, -60.00000000000005684, 187.7090405971777898 ) ) ;
#6847=CARTESIAN_POINT ( 'NONE',  ( 9.055366547345554906, -22.06741143183647225, 27.56839278369679747 ) ) ;
#6849=CARTESIAN_POINT ( 'NONE',  ( 93.54169269461303315, -38.00000000000000000, 99.15423023452258633 ) ) ;
#6852=CARTESIAN_POINT ( 'NONE',  ( -44.95452292836267816, -53.35130017089566223, 47.31599179322356719 ) ) ;
#6857=CARTESIAN_POINT ( 'NONE',  ( 2.500000000000002220, -10.61161631886071000, -19.67321533785385412 ) ) ;
#6863=CARTESIAN_POINT ( 'NONE',  ( 107.4906260354581349, -29.99999999999830536, 190.3131457271783518 ) ) ;
#6868=CARTESIAN_POINT ( 'NONE',  ( 94.33119406073718949, -29.99999999999999645, 113.9538965140871198 ) ) ;
#6884=CARTESIAN_POINT ( 'NONE',  ( 79.09286514343337160, -38.69997524062500815, 191.1501546668640117 ) ) ;
#6886=CARTESIAN_POINT ( 'NONE',  ( 85.54804277169388627, -52.72484354478569202, -1.684791068517219381 ) ) ;
#6903=CARTESIAN_POINT ( 'NONE',  ( 25.37876591545637339, -29.29967622782716319, 38.35509702236433327 ) ) ;
#6907=CARTESIAN_POINT ( 'NONE',  ( 86.05773094049673944, -24.85131605070118255, 179.6131699954536316 ) ) ;
#6911=ORIENTED_EDGE ( 'NONE', *, *, #42907, .T. ) ;
#6912=CARTESIAN_POINT ( 'NONE',  ( 93.83752300881383235, -57.67474270103812728, 11.11646394693934248 ) ) ;
#6919=CARTESIAN_POINT ( 'NONE',  ( -84.15743021832903992, -38.00000000000000000, 177.7979622954009358 ) ) ;
#6934=CARTESIAN_POINT ( 'NONE',  ( -9.355518002030276392, -16.12908517271025133, -34.86275573499951008 ) ) ;
#6937=CARTESIAN_POINT ( 'NONE',  ( -54.57924045077913178, -60.22828080784039173, -31.12148306891128868 ) ) ;
#6945=CARTESIAN_POINT ( 'NONE',  ( -92.38040701271825128, -60.00000000000000000, 0.4176965262226800535 ) ) ;
#6948=CARTESIAN_POINT ( 'NONE',  ( 3.983571028020258975, -22.12038543825604364, -30.53674616711531087 ) ) ;
#6950=CARTESIAN_POINT ( 'NONE',  ( 96.63576135145862622, -37.72004133599708098, 192.9127721459992699 ) ) ;
#6954=CARTESIAN_POINT ( 'NONE',  ( -83.05174168264076684, -36.01502199835699258, 164.7559579327255221 ) ) ;
#6964=CARTESIAN_POINT ( 'NONE',  ( -113.3548229410037465, -57.67117998536030399, 185.4730977758015911 ) ) ;
#6970=CARTESIAN_POINT ( 'NONE',  ( -41.39220545275658480, -29.99999999999999289, -36.78659115423995729 ) ) ;
#6971=CARTESIAN_POINT ( 'NONE',  ( -8.555246586836847911, -60.00000000000005684, 41.98716887921269603 ) ) ;
#6972=CARTESIAN_POINT ( 'NONE',  ( -54.17978373078881305, -18.69462178154748244, 50.60429759934945793 ) ) ;
#6976=CARTESIAN_POINT ( 'NONE',  ( -99.94433702487522453, -52.76369124458621229, 194.2390971257265733 ) ) ;
#6980=CARTESIAN_POINT ( 'NONE',  ( 83.63364292175512560, -38.35741735095676574, -24.00537533077424968 ) ) ;
#6985=CARTESIAN_POINT ( 'NONE',  ( 85.15477469677583144, -29.99999999999999645, 171.7644904280243452 ) ) ;
#6994=CARTESIAN_POINT ( 'NONE',  ( 49.74300220995602473, -60.29126617275993283, 57.32551668852249094 ) ) ;
#6999=CARTESIAN_POINT ( 'NONE',  ( -108.9262910262880268, -38.35648934207953431, 190.3667217115266226 ) ) ;
#7001=CARTESIAN_POINT ( 'NONE',  ( 101.4849516909198428, -38.35588639963484781, 97.13440198566154038 ) ) ;
#7005=CARTESIAN_POINT ( 'NONE',  ( 102.3119119459010449, -37.84840099971084726, 161.0091571851309027 ) ) ;
#7010=CARTESIAN_POINT ( 'NONE',  ( 80.22574947771531129, -60.00000000000001421, 196.2602844723502358 ) ) ;
#7015=CARTESIAN_POINT ( 'NONE',  ( 56.41533150989165080, -42.96560079021762846, 64.88708484893876971 ) ) ;
#7022=CARTESIAN_POINT ( 'NONE',  ( -108.2151194096256006, -38.35755553628541747, 192.4188466880123656 ) ) ;
#7034=CARTESIAN_POINT ( 'NONE',  ( 86.10674275497149210, -18.36954599775684827, 167.2017617639139360 ) ) ;
#7072=CARTESIAN_POINT ( 'NONE',  ( -110.1353205782709495, -60.00000000000000711, 144.5369955810122065 ) ) ;
#7079=CARTESIAN_POINT ( 'NONE',  ( -81.01496773232567250, -60.51907568041632146, 183.3200419029122941 ) ) ;
#7093=CARTESIAN_POINT ( 'NONE',  ( 106.8235258757864869, -14.21045842199432307, 178.1026719309843429 ) ) ;
#7095=CARTESIAN_POINT ( 'NONE',  ( -106.2142031390243488, -14.21045842199427867, 184.2056779555663582 ) ) ;
#7096=CARTESIAN_POINT ( 'NONE',  ( -62.91815421806131070, -46.43920947130374799, 83.70092769440094571 ) ) ;
#7099=CARTESIAN_POINT ( 'NONE',  ( 102.1655696349906037, -59.99999999999998579, 79.68160258763181503 ) ) ;
#7101=CARTESIAN_POINT ( 'NONE',  ( 2.047183246720497340, -56.87785484247199719, 33.36663002190862670 ) ) ;
#7109=CARTESIAN_POINT ( 'NONE',  ( -111.3575414531999002, -60.00000000000002132, 155.6755428621777639 ) ) ;
#7119=CARTESIAN_POINT ( 'NONE',  ( -33.16678848657432610, -39.49658583418889890, 34.42063352927269193 ) ) ;
#7122=CARTESIAN_POINT ( 'NONE',  ( 38.10111135957357220, -39.51109722829941973, 37.25237634264367159 ) ) ;
#7124=CARTESIAN_POINT ( 'NONE',  ( -13.60704923275180711, -1.734723475976807094E-15, 10.45706415777857679 ) ) ;
#7129=MECHANICAL_DESIGN_GEOMETRIC_PRESENTATION_REPRESENTATION('',(#14053),#41633);
#7130=CARTESIAN_POINT ( 'NONE',  ( -73.92879853447317373, -38.32663868724161915, 159.7524117896638529 ) ) ;
#7140=CARTESIAN_POINT ( 'NONE',  ( 96.40273327088657140, -60.00000000000000711, 58.78147464121637711 ) ) ;
#7145=CARTESIAN_POINT ( 'NONE',  ( -93.63610435622004502, -29.99999999996020605, 58.27751359658407182 ) ) ;
#7159=CARTESIAN_POINT ( 'NONE',  ( 79.83490250164462054, -46.43441910742400580, 152.6729557515090221 ) ) ;
#7168=CARTESIAN_POINT ( 'NONE',  ( -18.14395573440383203, -57.67158919250769600, 41.98617601139094546 ) ) ;
#7170=ORIENTED_EDGE ( 'NONE', *, *, #36957, .T. ) ;
#7179=CARTESIAN_POINT ( 'NONE',  ( -19.56313861856585135, -16.92226382200795953, 31.48483935735937322 ) ) ;
#7182=PLANE ( 'NONE',  #79725 ) ;
#7190=CARTESIAN_POINT ( 'NONE',  ( 40.56629821760718357, -33.14137426171819811, -37.41307075545274330 ) ) ;
#7197=CARTESIAN_POINT ( 'NONE',  ( 101.5234275403970230, -57.63077336659093675, 203.4510901792717448 ) ) ;
#7206=CARTESIAN_POINT ( 'NONE',  ( -74.29762348972462860, -60.00000000000000711, 175.1860712289616799 ) ) ;
#7210=CARTESIAN_POINT ( 'NONE',  ( -84.86190328036930453, -42.95973281295992763, 185.2921246785317635 ) ) ;
#7217=CARTESIAN_POINT ( 'NONE',  ( -83.26222442445862271, -45.25913346788161817, -13.97201566420315366 ) ) ;
#7222=CARTESIAN_POINT ( 'NONE',  ( 19.43146043914768129, -2.896176105056903703E-12, 11.19959342721819695 ) ) ;
#7224=CARTESIAN_POINT ( 'NONE',  ( 90.14752496014264693, -29.99999999999995026, -6.310861463900848456 ) ) ;
#7225=CARTESIAN_POINT ( 'NONE',  ( -77.90030443299963281, -29.08352689348323850, 125.1943772946299589 ) ) ;
#7227=CARTESIAN_POINT ( 'NONE',  ( 20.43634719630433594, -14.21045842199429998, 34.90381869870211062 ) ) ;
#7229=CARTESIAN_POINT ( 'NONE',  ( 70.47149586861833370, -57.68248580236559064, 157.7590444366918803 ) ) ;
#7247=CARTESIAN_POINT ( 'NONE',  ( -1.425880015568740777, -60.00000000000000711, 42.00000000000002132 ) ) ;
#7248=CARTESIAN_POINT ( 'NONE',  ( 30.40514414639649132, -39.48589796098298876, 33.27119446255795054 ) ) ;
#7252=AXIS2_PLACEMENT_3D ( 'NONE', #32155, #39188, #72066 ) ;
#7261=CARTESIAN_POINT ( 'NONE',  ( 63.78324300990938411, -60.00000000000002842, -34.57572711317787650 ) ) ;
#7262=CARTESIAN_POINT ( 'NONE',  ( 84.85176311637069091, -30.00000000000000711, 168.9139284579673301 ) ) ;
#7264=CARTESIAN_POINT ( 'NONE',  ( 75.38474497803707663, -29.99999999999999645, -17.81191432453914913 ) ) ;
#7288=CARTESIAN_POINT ( 'NONE',  ( -20.84632109279829493, -59.99999999999998579, 34.49850619988961142 ) ) ;
#7289=CARTESIAN_POINT ( 'NONE',  ( 67.76856916487194837, -32.53299590129649488, 90.77966141860517268 ) ) ;
#7311=CARTESIAN_POINT ( 'NONE',  ( -95.50364921585600086, -30.00000000000000711, 191.3268544109589300 ) ) ;
#7315=CARTESIAN_POINT ( 'NONE',  ( 37.94872683402551417, -57.69547342295989978, 52.59817782003744924 ) ) ;
#7320=CARTESIAN_POINT ( 'NONE',  ( 1.641472239120435717, -21.31623762121044052, -38.55282611630758538 ) ) ;
#7323=CARTESIAN_POINT ( 'NONE',  ( -7.370567298740709816, -60.00000000000000711, 39.63063440146133587 ) ) ;
#7326=CARTESIAN_POINT ( 'NONE',  ( -86.90850660987527476, -31.72843720894637087, 187.1496124096579763 ) ) ;
#7330=CARTESIAN_POINT ( 'NONE',  ( -6.036298205140932183, -29.03102288755636806, 28.71854023455634319 ) ) ;
#7347=CARTESIAN_POINT ( 'NONE',  ( 71.07052165988230286, -60.00000000000000711, 147.7243966094672487 ) ) ;
#7352=( LENGTH_UNIT ( ) NAMED_UNIT ( * ) SI_UNIT ( .MILLI., .METRE. ) );
#7365=CARTESIAN_POINT ( 'NONE',  ( -111.3949278518088306, -60.00000000000000000, 194.2500860083519285 ) ) ;
#7367=CARTESIAN_POINT ( 'NONE',  ( 88.17925955597732468, -60.00000000000002132, 201.4489170471512693 ) ) ;
#7370=CARTESIAN_POINT ( 'NONE',  ( -101.7136998165503883, -14.21045842199435150, 195.4607583018654395 ) ) ;
#7371=CARTESIAN_POINT ( 'NONE',  ( 15.89902062379011660, -53.39644330016152907, 32.98550796398789942 ) ) ;
#7372=CARTESIAN_POINT ( 'NONE',  ( 102.5622483503262288, -37.99999999999999289, 164.2734793211291731 ) ) ;
#7374=CARTESIAN_POINT ( 'NONE',  ( -43.99789167439523396, -42.98520829747947403, 43.39751293111646646 ) ) ;
#7383=ORIENTED_EDGE ( 'NONE', *, *, #12903, .T. ) ;
#7386=CARTESIAN_POINT ( 'NONE',  ( 98.13275984205787950, -29.99999999995851852, 199.6471406849189520 ) ) ;
#7391=CARTESIAN_POINT ( 'NONE',  ( 97.92220087128177397, -29.99999999999999645, 136.9860503619559040 ) ) ;
#7406=CARTESIAN_POINT ( 'NONE',  ( 85.62566950274205624, -38.66289190168809853, 198.8555151629249735 ) ) ;
#7408=CARTESIAN_POINT ( 'NONE',  ( 64.24779899988634213, -38.00000000000000711, 83.19840595776713599 ) ) ;
#7423=CARTESIAN_POINT ( 'NONE',  ( -3.380110533491807345, -18.24605901591677792, 35.03526125595637097 ) ) ;
#7427=CARTESIAN_POINT ( 'NONE',  ( 86.28470205846313945, -21.13264878163486316, 179.4900229914080683 ) ) ;
#7431=CARTESIAN_POINT ( 'NONE',  ( 93.97991700648807978, -57.67305785691176823, 18.55496576499952610 ) ) ;
#7433=CARTESIAN_POINT ( 'NONE',  ( -2.499999999999996447, -30.00000000000000000, -13.00000000000000000 ) ) ;
#7454=CARTESIAN_POINT ( 'NONE',  ( -11.08507223468469682, -16.42258121883788391, -34.72272924400278526 ) ) ;
#7457=CARTESIAN_POINT ( 'NONE',  ( -65.15265132078000931, -60.22826349054815154, -28.17547081302746648 ) ) ;
#7463=CARTESIAN_POINT ( 'NONE',  ( -66.30537473500707790, -60.00000000000000711, -33.79319030883430486 ) ) ;
#7467=CARTESIAN_POINT ( 'NONE',  ( 96.11581706050769469, -52.82288690486888783, 195.4413948441345212 ) ) ;
#7470=CARTESIAN_POINT ( 'NONE',  ( -80.03050186129850374, -56.86872676409061000, 169.5269957069628219 ) ) ;
#7484=CARTESIAN_POINT ( 'NONE',  ( -109.5878728966581832, -57.66746364524283308, 196.8330158634452118 ) ) ;
#7489=CARTESIAN_POINT ( 'NONE',  ( 53.63839714946880832, -30.00000000000003553, -34.46733499188162853 ) ) ;
#7491=CARTESIAN_POINT ( 'NONE',  ( -31.98280533637225176, -29.99999999999996447, 41.00520926490388263 ) ) ;
#7493=CARTESIAN_POINT ( 'NONE',  ( -51.22124617248039158, -60.30834877352122447, 60.32251114123462798 ) ) ;
#7496=CARTESIAN_POINT ( 'NONE',  ( -96.46940560253773356, -52.81427625367515333, 195.4040124156118168 ) ) ;
#7500=CARTESIAN_POINT ( 'NONE',  ( 94.02105730861428867, -38.35588314265653764, 51.42162103336989531 ) ) ;
#7501=CARTESIAN_POINT ( 'NONE',  ( 80.00000000000000000, -52.00000000000000000, -19.09707704303353282 ) ) ;
#7505=CARTESIAN_POINT ( 'NONE',  ( 75.34613995108148288, -30.00000000000000000, 113.5060042757550463 ) ) ;
#7514=CARTESIAN_POINT ( 'NONE',  ( 48.95925862278320295, -42.97824454139764327, 50.18280914362345868 ) ) ;
#7518=CARTESIAN_POINT ( 'NONE',  ( -90.65873703400211525, -38.34395918042547891, 9.055193890183026895 ) ) ;
#7521=CARTESIAN_POINT ( 'NONE',  ( 93.42341124740551095, -38.35510331151919416, 46.74005875555363332 ) ) ;
#7524=CARTESIAN_POINT ( 'NONE',  ( 104.3685752548006462, -60.15138688519091659, 144.3650627233956527 ) ) ;
#7529=CARTESIAN_POINT ( 'NONE',  ( 77.80177750690549487, -60.00000000000000711, 192.4143508859149279 ) ) ;
#7535=CARTESIAN_POINT ( 'NONE',  ( 58.62522138716740727, -46.43623924511926049, 71.88277463636357822 ) ) ;
#7542=CARTESIAN_POINT ( 'NONE',  ( -90.93871753736571861, -38.40505638326484927, -12.93646735681355864 ) ) ;
#7553=CARTESIAN_POINT ( 'NONE',  ( 85.66145762413124487, -21.90510868169506509, 168.0986262888999647 ) ) ;
#7568=CARTESIAN_POINT ( 'NONE',  ( -23.47407494167467945, -28.00280731361893771, 37.76335220153635674 ) ) ;
#7591=CARTESIAN_POINT ( 'NONE',  ( -110.1325006654252689, -60.00000000000000711, 144.5141837704236991 ) ) ;
#7598=CARTESIAN_POINT ( 'NONE',  ( -82.69763864773811690, -46.48872540907822781, 177.5893064810508122 ) ) ;
#7612=CARTESIAN_POINT ( 'NONE',  ( 114.5925949185997439, -60.00000000000001421, 172.8113841322393682 ) ) ;
#7613=CARTESIAN_POINT ( 'NONE',  ( -114.5724197576058714, -60.00000000000000000, 174.9505165961822684 ) ) ;
#7615=CARTESIAN_POINT ( 'NONE',  ( -62.23155850973583370, -46.43999065396062775, 81.73006897967107420 ) ) ;
#7618=CARTESIAN_POINT ( 'NONE',  ( 107.8446305798313887, -59.99999999999507594, 199.8152282391069150 ) ) ;
#7629=CARTESIAN_POINT ( 'NONE',  ( -111.9904110614580190, -59.99999999999998579, 164.0997730435657047 ) ) ;
#7641=CARTESIAN_POINT ( 'NONE',  ( 87.00825156440252783, -60.00000000000000000, -8.027590136533380161 ) ) ;
#7643=CARTESIAN_POINT ( 'NONE',  ( -32.66505120407880725, -53.37625315817673766, 36.73532806000678619 ) ) ;
#7645=CARTESIAN_POINT ( 'NONE',  ( 39.50165778835835084, -46.43035749859290462, 39.79999272029177604 ) ) ;
#7646=CARTESIAN_POINT ( 'NONE',  ( 76.12557658274099026, -38.35599704320051018, -28.58424740099938077 ) ) ;
#7649=CARTESIAN_POINT ( 'NONE',  ( -80.19950985152857470, -38.79610194437496062, 193.3420121686260700 ) ) ;
#7660=CARTESIAN_POINT ( 'NONE',  ( 92.01769393557711396, -60.00000000000000000, 18.81140579558686454 ) ) ;
#7666=CARTESIAN_POINT ( 'NONE',  ( -92.80508788735930636, -29.99999999999979039, 191.0773401206811286 ) ) ;
#7684=CARTESIAN_POINT ( 'NONE',  ( 79.19591562604769308, -60.32219928206144743, 166.8364905889302747 ) ) ;
#7695=CARTESIAN_POINT ( 'NONE',  ( -53.00057554449748665, -60.00000000000002842, -31.41244228210902278 ) ) ;
#7696=CARTESIAN_POINT ( 'NONE',  ( -36.61061158941262761, -57.69633519219438966, 50.91350493295865931 ) ) ;
#7705=CARTESIAN_POINT ( 'NONE',  ( 44.47534377888507606, -38.31160956920668070, 57.00192013341546016 ) ) ;
#7708=EDGE_CURVE ( 'NONE', #80843, #6442, #98853, .T. ) ;
#7717=CARTESIAN_POINT ( 'NONE',  ( 62.84259819506511491, -37.71647027193530732, -33.49470327681527948 ) ) ;
#7725=CARTESIAN_POINT ( 'NONE',  ( 112.0160167646016163, -57.67108196866938385, 191.2727973919889166 ) ) ;
#7731=CARTESIAN_POINT ( 'NONE',  ( -73.05323961714354652, -60.00000000000000000, 162.9460430220049716 ) ) ;
#7735=CARTESIAN_POINT ( 'NONE',  ( -84.26296102854614389, -50.17790333388872170, 187.6082884815264151 ) ) ;
#7743=CARTESIAN_POINT ( 'NONE',  ( -85.74469220476173348, -52.74251783766182911, -7.704084915169921111 ) ) ;
#7749=CARTESIAN_POINT ( 'NONE',  ( 21.65942590380565491, 2.899645552008857721E-12, 5.820808985964478488 ) ) ;
#7751=CARTESIAN_POINT ( 'NONE',  ( 52.80879785486305167, -14.21045842199441722, -31.95559855168728092 ) ) ;
#7752=CARTESIAN_POINT ( 'NONE',  ( -79.18173105286311397, -29.08793685032101806, 131.2448686397106599 ) ) ;
#7755=CARTESIAN_POINT ( 'NONE',  ( 55.43986775084101737, -14.21045842199435860, 70.80752230913886081 ) ) ;
#7757=CARTESIAN_POINT ( 'NONE',  ( 93.02311254871766266, -57.65591657365690281, -17.17379135556295111 ) ) ;
#7777=CARTESIAN_POINT ( 'NONE',  ( -1.385021579957316007, -30.00000000000000000, 37.00000000000000711 ) ) ;
#7778=CARTESIAN_POINT ( 'NONE',  ( 28.55559703281400985, -39.48181379216788400, 32.65655774942846534 ) ) ;
#7790=CARTESIAN_POINT ( 'NONE',  ( 49.70935196047673088, -60.00000000000000711, -37.96160376868289887 ) ) ;
#7817=CARTESIAN_POINT ( 'NONE',  ( 65.02905820690668293, -29.05409441471111975, 80.86375735356135408 ) ) ;
#7823=CARTESIAN_POINT ( 'NONE',  ( -55.77313467663169888, -57.67115539668835567, -38.70230501811910528 ) ) ;
#7845=CARTESIAN_POINT ( 'NONE',  ( -92.60287565247158170, -30.00000000000000000, 191.0277603200695751 ) ) ;
#7849=CARTESIAN_POINT ( 'NONE',  ( 45.07112015427507856, -57.68308583978475923, 65.31626219697243130 ) ) ;
#7854=CARTESIAN_POINT ( 'NONE',  ( 17.35462159048412545, -24.88231629494887187, -38.51483657780791958 ) ) ;
#7856=CARTESIAN_POINT ( 'NONE',  ( -28.73687143290147361, -60.00000000000000000, 42.44963378108809593 ) ) ;
#7859=CARTESIAN_POINT ( 'NONE',  ( -86.51918189808866089, -17.01178005999074827, 184.3026545482127290 ) ) ;
#7863=CARTESIAN_POINT ( 'NONE',  ( -9.249882429003642770, -42.95773840073744765, 31.05202513958081312 ) ) ;
#7865=CARTESIAN_POINT ( 'NONE',  ( -103.2741708893823898, -60.00000000000002842, 192.3304520135565951 ) ) ;
#7875=CARTESIAN_POINT ( 'NONE',  ( 69.60542681594449732, -59.99999999999999289, 139.2651478594983701 ) ) ;
#7876=CARTESIAN_POINT ( 'NONE',  ( 113.3390500081078613, -59.99999999999998579, 187.7085336688584221 ) ) ;
#7898=CARTESIAN_POINT ( 'NONE',  ( -47.33438562141003558, -59.99999999996092015, 71.44327096003375743 ) ) ;
#7900=CARTESIAN_POINT ( 'NONE',  ( 91.63563106630719801, -60.00000000000001421, 202.3019666817567099 ) ) ;
#7901=CARTESIAN_POINT ( 'NONE',  ( -109.5313977869038098, -29.99999999999998934, 176.4136249138144876 ) ) ;
#7902=CARTESIAN_POINT ( 'NONE',  ( 15.78057381398083336, -46.43467002123828991, 31.81701378920458012 ) ) ;
#7904=CARTESIAN_POINT ( 'NONE',  ( 98.14827422455367412, -37.99999999999972999, 192.4855505147021688 ) ) ;
#7906=CARTESIAN_POINT ( 'NONE',  ( -47.01862296229795390, -42.98688433404485920, 47.24448534941780053 ) ) ;
#7923=CARTESIAN_POINT ( 'NONE',  ( 80.72706426431642512, -30.00000000000003553, 14.39622326674284203 ) ) ;
#7927=CARTESIAN_POINT ( 'NONE',  ( 92.38323657685867829, -30.00000000000000000, 102.4159884044749873 ) ) ;
#7941=CARTESIAN_POINT ( 'NONE',  ( 82.78759144455818841, -38.81844165587003914, 196.7277647683693260 ) ) ;
#7963=CARTESIAN_POINT ( 'NONE',  ( 84.09387693237994199, -53.78933109331524776, 189.0839742466992561 ) ) ;
#7968=CARTESIAN_POINT ( 'NONE',  ( 83.03225564478651677, -57.67107390234919251, -28.38291099116899829 ) ) ;
#7973=CARTESIAN_POINT ( 'NONE',  ( -81.02059387440468186, -29.99999999999999645, 21.32526539110572728 ) ) ;
#7976=CARTESIAN_POINT ( 'NONE',  ( -76.43706498987678799, -37.99999999999996447, 125.5496669823371860 ) ) ;
#7987=CARTESIAN_POINT ( 'NONE',  ( -22.64062017603108501, -27.31223983661013222, -30.38885495092308986 ) ) ;
#7991=AXIS2_PLACEMENT_3D ( 'NONE', #18961, #83114, #28113 ) ;
#7992=CARTESIAN_POINT ( 'NONE',  ( -100.8624366425310512, -38.00000000000002132, 188.7450187321335022 ) ) ;
#7997=CARTESIAN_POINT ( 'NONE',  ( 8.061685236282825271E-09, -15.39512265162600535, -35.22781471665102515 ) ) ;
#7999=CARTESIAN_POINT ( 'NONE',  ( -35.59171129655433674, -60.22815248269157706, -34.49232045672559366 ) ) ;
#8000=ORIENTED_EDGE ( 'NONE', *, *, #80652, .T. ) ;
#8005=CARTESIAN_POINT ( 'NONE',  ( -47.29246454944256328, -59.99999999999999289, -38.43485023766499609 ) ) ;
#8007=CARTESIAN_POINT ( 'NONE',  ( 3.241669456190960030, -22.04828166566017345, -30.53834172389159818 ) ) ;
#8009=CARTESIAN_POINT ( 'NONE',  ( 98.41711723305866144, -52.80332669457988004, 194.9895706369884749 ) ) ;
#8015=VECTOR ( 'NONE', #3699, 1000.000000000000000 ) ;
#8023=CARTESIAN_POINT ( 'NONE',  ( -72.09688937032439071, -57.67332965070641393, 173.0313604384042776 ) ) ;
#8028=CARTESIAN_POINT ( 'NONE',  ( 17.10006063058271053, -59.99999999999996447, -44.43597027717249404 ) ) ;
#8029=CARTESIAN_POINT ( 'NONE',  ( -20.75616973061526949, -30.00000000000004263, 37.60198765588109637 ) ) ;
#8031=CARTESIAN_POINT ( 'NONE',  ( -52.40170964977422585, -53.37735564585817372, 60.21222595448364956 ) ) ;
#8035=CARTESIAN_POINT ( 'NONE',  ( -99.38960187038392746, -45.25186168038769097, 193.0844496258347931 ) ) ;
#8043=CARTESIAN_POINT ( 'NONE',  ( 109.8608637664040515, -38.35600155330774186, 186.7385511336370314 ) ) ;
#8048=CARTESIAN_POINT ( 'NONE',  ( 80.64605670160975137, -30.00000000000000000, 138.0219786762299918 ) ) ;
#8055=CARTESIAN_POINT ( 'NONE',  ( 48.89013321113019117, -22.21369756360278203, 43.54071997640996017 ) ) ;
#8062=CARTESIAN_POINT ( 'NONE',  ( -93.44691131992647115, -38.35488852157141082, 46.93959257640000970 ) ) ;
#8065=CARTESIAN_POINT ( 'NONE',  ( 92.04617479045300854, -38.35408004050898256, 35.18142690402697781 ) ) ;
#8069=CARTESIAN_POINT ( 'NONE',  ( 103.7134520183080326, -60.15124960079525351, 139.5371650122951621 ) ) ;
#8071=DIRECTION ( 'NONE',  ( 0.000000000000000000, 1.000000000000000000, 0.000000000000000000 ) ) ;
#8075=CARTESIAN_POINT ( 'NONE',  ( 74.36397108531809863, -59.99999999999999289, 175.8240678876071570 ) ) ;
#8081=CARTESIAN_POINT ( 'NONE',  ( 60.91963193027662982, -32.53835347950492718, 71.34319023294183637 ) ) ;
#8086=CARTESIAN_POINT ( 'NONE',  ( -86.45048231984965525, -38.36235641012063979, -21.45451331935682049 ) ) ;
#8094=CARTESIAN_POINT ( 'NONE',  ( 82.21186757432916181, -49.98570124988022201, 178.5498643125555702 ) ) ;
#8108=CARTESIAN_POINT ( 'NONE',  ( -8.467721648720655025, -19.61993625497054694, 35.26688575358691935 ) ) ;
#8123=CARTESIAN_POINT ( 'NONE',  ( 65.50959194424925158, -21.77022000568248927, -21.27195586255206194 ) ) ;
#8133=CARTESIAN_POINT ( 'NONE',  ( -98.13052083946277548, -59.99999999999999289, 69.73258326240120653 ) ) ;
#8138=CARTESIAN_POINT ( 'NONE',  ( -2.303522549047186516E-06, -22.06787374684229874, 27.56762891740942578 ) ) ;
#8145=CARTESIAN_POINT ( 'NONE',  ( -84.12058219282783966, -35.94476431650669213, 174.7674332474302048 ) ) ;
#8148=VERTEX_POINT ( 'NONE', #85778 ) ;
#8156=CARTESIAN_POINT ( 'NONE',  ( -14.05937931246655026, -57.67120694556813731, -44.20476115079929258 ) ) ;
#8161=CARTESIAN_POINT ( 'NONE',  ( 112.0515757376121542, -60.00000000000002842, 140.8507904390172598 ) ) ;
#8162=CARTESIAN_POINT ( 'NONE',  ( -109.5675793427969040, -29.99999999999999289, 170.1817020036065742 ) ) ;
#8163=CARTESIAN_POINT ( 'NONE',  ( -62.60069042062036004, -29.05980936889960020, 74.09822019150450956 ) ) ;
#8167=CARTESIAN_POINT ( 'NONE',  ( 113.9027919867113923, -60.00000000001953282, 157.6317976075506238 ) ) ;
#8169=CARTESIAN_POINT ( 'NONE',  ( 0.9942926288455912198, -29.02944133723623921, 28.72789018247508608 ) ) ;
#8177=CARTESIAN_POINT ( 'NONE',  ( -110.5340683299488234, -60.00000000000001421, 189.3070748394261500 ) ) ;
#8189=CARTESIAN_POINT ( 'NONE',  ( -33.54301527992964793, -46.43411393437603607, 35.89697790901694674 ) ) ;
#8190=CARTESIAN_POINT ( 'NONE',  ( 40.77236552497750921, -29.15239929701842669, 36.95769491155581932 ) ) ;
#8195=CARTESIAN_POINT ( 'NONE',  ( -80.08624693268845363, -38.78840980346092238, 193.1431129205759305 ) ) ;
#8206=CARTESIAN_POINT ( 'NONE',  ( 110.9949313104018529, -60.00000000000000711, 152.0878044361085699 ) ) ;
#8212=CARTESIAN_POINT ( 'NONE',  ( -87.91185205471116149, -30.00000000000008171, 186.5683232776123930 ) ) ;
#8228=CARTESIAN_POINT ( 'NONE',  ( 80.86233901923861822, -46.43849059710549199, 160.9666562290477430 ) ) ;
#8235=CARTESIAN_POINT ( 'NONE',  ( -48.45695174840996344, -59.99999999999997158, -32.35430574311584451 ) ) ;
#8245=CARTESIAN_POINT ( 'NONE',  ( 22.50849985115188545, -27.35376444295244625, 37.47483747969673118 ) ) ;
#8246=CARTESIAN_POINT ( 'NONE',  ( 2.500000000000013767, -30.00000000000000355, -31.87333685190803223 ) ) ;
#8252=FACE_OUTER_BOUND ( 'NONE', #11027, .T. ) ;
#8260=CARTESIAN_POINT ( 'NONE',  ( 112.0975676531185030, -57.67108666598051059, 191.0081396353801040 ) ) ;
#8266=CARTESIAN_POINT ( 'NONE',  ( -76.28233775379571568, -60.00000000000000000, 188.0959844134463310 ) ) ;
#8271=CARTESIAN_POINT ( 'NONE',  ( -86.06194670869818708, -28.35369527726857442, 182.3419248918959852 ) ) ;
#8279=CARTESIAN_POINT ( 'NONE',  ( -85.48360261714907438, -52.75149282529780947, -10.94374517246983025 ) ) ;
#8288=CARTESIAN_POINT ( 'NONE',  ( 4.453875240779016309, -1.734723475976807094E-15, -16.57301948837565675 ) ) ;
#8290=CARTESIAN_POINT ( 'NONE',  ( 53.63839714946880832, -30.00000000000003553, -34.46733499188162853 ) ) ;
#8291=CARTESIAN_POINT ( 'NONE',  ( -77.45270157673813571, -42.96733943251651056, 134.7326920116138922 ) ) ;
#8293=CARTESIAN_POINT ( 'NONE',  ( 77.87328754808491738, -14.21045842199420228, 157.7472683744473159 ) ) ;
#8295=CARTESIAN_POINT ( 'NONE',  ( 113.0765498504955247, -57.67120308272065898, 186.9763648898224915 ) ) ;
#8314=CARTESIAN_POINT ( 'NONE',  ( 29.95423130063162986, -42.95837386160915372, 33.73428810424631763 ) ) ;
#8329=CARTESIAN_POINT ( 'NONE',  ( 87.60640540356948236, -60.00000000000002132, -22.02487886544127704 ) ) ;
#8357=CARTESIAN_POINT ( 'NONE',  ( -47.21131606613124632, -59.99999999999997868, 52.59714937887711272 ) ) ;
#8359=CARTESIAN_POINT ( 'NONE',  ( 69.72252812878896577, -56.85553266303294606, 111.2983125885081392 ) ) ;
#8364=CARTESIAN_POINT ( 'NONE',  ( -110.1907765348834403, -57.67120634471875462, 130.2639824976604643 ) ) ;
#8382=CARTESIAN_POINT ( 'NONE',  ( -97.58700215924690724, -30.00000000000000000, 190.8409573115993112 ) ) ;
#8387=CARTESIAN_POINT ( 'NONE',  ( 70.36692166205514809, -57.68251006697582284, 157.0214156919219022 ) ) ;
#8395=CARTESIAN_POINT ( 'NONE',  ( -10.39312431003531856, -60.00000000000000711, 39.65367113221718398 ) ) ;
#8399=CARTESIAN_POINT ( 'NONE',  ( -86.73280396411435333, -42.80135120255732772, 189.5378547483240368 ) ) ;
#8403=CARTESIAN_POINT ( 'NONE',  ( -7.130835401559076026, -39.47599328887858405, 30.45931887943757133 ) ) ;
#8417=CARTESIAN_POINT ( 'NONE',  ( 113.7193001496157052, -60.00000000000001421, 185.6034734595149871 ) ) ;
#8437=CARTESIAN_POINT ( 'NONE',  ( -25.93098123902086982, -59.99999999999020872, 43.86977658264649449 ) ) ;
#8440=CARTESIAN_POINT ( 'NONE',  ( 109.4462915750694236, -60.00000000000001421, 192.7655176299684001 ) ) ;
#8441=CARTESIAN_POINT ( 'NONE',  ( -105.6361520504002840, -30.00000000000002132, 194.5259906914266139 ) ) ;
#8442=CARTESIAN_POINT ( 'NONE',  ( 13.27489365765825191, -25.54879520240182345, 28.22250578733302717 ) ) ;
#8446=CARTESIAN_POINT ( 'NONE',  ( -42.25929233593898715, -42.98302630092105403, 41.54187495367473559 ) ) ;
#8459=CARTESIAN_POINT ( 'NONE',  ( 80.89399687007842488, -29.99999999999999289, -12.17736764248747861 ) ) ;
#8463=CARTESIAN_POINT ( 'NONE',  ( 94.31146389850853495, -30.00000000000000355, 113.8352357902896586 ) ) ;
#8479=CARTESIAN_POINT ( 'NONE',  ( 79.03758757855014494, -38.69423318788795996, 191.0234865722444511 ) ) ;
#8495=SURFACE_STYLE_FILL_AREA ( #40336 ) ;
#8497=CARTESIAN_POINT ( 'NONE',  ( -13.53089024472542334, -21.84174497847139662, 35.70596031949021665 ) ) ;
#8501=CARTESIAN_POINT ( 'NONE',  ( 86.39215313046445033, -17.36952503152258842, 179.6808971095037748 ) ) ;
#8502=CARTESIAN_POINT ( 'NONE',  ( -76.12537862032631608, -38.35598417008158378, -28.58435412235099804 ) ) ;
#8505=CARTESIAN_POINT ( 'NONE',  ( 91.85898906140822362, -57.66094271643867586, -19.56282458869456775 ) ) ;
#8509=CARTESIAN_POINT ( 'NONE',  ( -81.37858232197777397, -30.00000000000001421, -1.651955541798732385 ) ) ;
#8526=DIRECTION ( 'NONE',  ( -0.000000000000000000, 1.000000000000000000, -0.000000000000000000 ) ) ;
#8527=CARTESIAN_POINT ( 'NONE',  ( -55.09674501162535876, -28.50739436101074276, -26.55108529303278075 ) ) ;
#8529=CARTESIAN_POINT ( 'NONE',  ( -66.87664816687141922, -21.77013672081559292, -20.76364936843571130 ) ) ;
#8538=CARTESIAN_POINT ( 'NONE',  ( 1.078140322363270668E-05, -30.00000000000000000, 28.88964995960238014 ) ) ;
#8539=CARTESIAN_POINT ( 'NONE',  ( -30.64178597908914625, -60.00000000000001421, -40.84433097566444815 ) ) ;
#8543=CARTESIAN_POINT ( 'NONE',  ( 100.2342046845623855, -45.27551373043147720, 192.3669307444947094 ) ) ;
#8560=CARTESIAN_POINT ( 'NONE',  ( -57.91314980999670325, -57.67646044164155228, 100.3416927154360536 ) ) ;
#8566=CARTESIAN_POINT ( 'NONE',  ( -61.70175965769652748, -30.00000000000001066, -32.45223383460360367 ) ) ;
#8568=CARTESIAN_POINT ( 'NONE',  ( -49.82526758650133303, -56.83439142156854729, 56.29054524400240922 ) ) ;
#8569=AXIS2_PLACEMENT_3D ( 'NONE', #41618, #65888, #65363 ) ;
#8572=CARTESIAN_POINT ( 'NONE',  ( -98.68288091466004630, -37.75495276146958901, 192.1257439368163489 ) ) ;
#8578=CARTESIAN_POINT ( 'NONE',  ( 90.84051608033718139, -38.50738636110989432, 200.7712009872789167 ) ) ;
#8584=CARTESIAN_POINT ( 'NONE',  ( 81.59702955527144752, -30.00000000000000000, 143.4499623754424533 ) ) ;
#8590=CARTESIAN_POINT ( 'NONE',  ( 52.50523195933924114, -18.71259018865586654, 47.73583290201036533 ) ) ;
#8596=CARTESIAN_POINT ( 'NONE',  ( -99.29559146798845859, -38.35572756809536088, 84.31528695177730981 ) ) ;
#8599=CARTESIAN_POINT ( 'NONE',  ( 98.48521771324512031, -38.35583637768242227, 79.51923348961499016 ) ) ;
#8601=CARTESIAN_POINT ( 'NONE',  ( 92.22087313427753941, -52.71700789290898825, 76.94303511423174768 ) ) ;
#8607=CARTESIAN_POINT ( 'NONE',  ( 76.36385995988143804, -59.99999999999999289, 188.3995559568122360 ) ) ;
#8610=EDGE_LOOP ( 'NONE', ( #47719, #68315, #103042, #23791 ) ) ;
#8611=CARTESIAN_POINT ( 'NONE',  ( 62.60020664644493138, -29.05810901319667394, 74.09607312414506453 ) ) ;
#8616=CARTESIAN_POINT ( 'NONE',  ( -48.99521034380500595, -29.99999999995976552, 62.69765256684991073 ) ) ;
#8627=CARTESIAN_POINT ( 'NONE',  ( 85.41191359320438892, -28.71737910575176400, 176.9201489232353026 ) ) ;
#8640=CARTESIAN_POINT ( 'NONE',  ( 39.30609551598629281, -60.00000000000000000, 51.14711558221264198 ) ) ;
#8643=CARTESIAN_POINT ( 'NONE',  ( -22.78844821391956188, -27.54187850787782565, 37.55836683131646225 ) ) ;
#8646=B_SPLINE_CURVE_WITH_KNOTS ( 'NONE', 3,
 ( #26988, #20518, #27526, #19441, #53352, #51201, #12346, #45272 ),
 .UNSPECIFIED., .F., .F.,
 ( 4, 2, 2, 4 ),
 ( 0.02058604435327386628, 0.02618835850023638195, 0.03179067264719889763, 0.04299530094112392897 ),
 .UNSPECIFIED. ) ;
#8649=ORIENTED_EDGE ( 'NONE', *, *, #87986, .T. ) ;
#8655=CARTESIAN_POINT ( 'NONE',  ( 34.70318342342385165, -34.58950113560386086, -30.29887370229810628 ) ) ;
#8664=ADVANCED_FACE ( 'NONE', ( #63892 ), #30777, .F. ) ;
#8668=CARTESIAN_POINT ( 'NONE',  ( -100.3149285850330159, -60.00000000000000711, 82.88046306574433686 ) ) ;
#8676=CARTESIAN_POINT ( 'NONE',  ( -85.91925276215749818, -18.46748765878107434, 164.5932108442251547 ) ) ;
#8686=CARTESIAN_POINT ( 'NONE',  ( 109.3513501059324255, -38.00000000000000000, 179.6549720493207190 ) ) ;
#8692=CARTESIAN_POINT ( 'NONE',  ( 111.4777457387739048, -59.99999999999993605, 136.6117272317642630 ) ) ;
#8693=CARTESIAN_POINT ( 'NONE',  ( -113.5293469826316084, -59.99999999999994316, 153.5981017735323633 ) ) ;
#8694=CARTESIAN_POINT ( 'NONE',  ( -61.80134322767651867, -53.39308551080091547, 84.00808285357440752 ) ) ;
#8697=CARTESIAN_POINT ( 'NONE',  ( 110.6310860903329285, -59.99999999998527045, 195.7736967744526737 ) ) ;
#8699=CARTESIAN_POINT ( 'NONE',  ( 5.016252133114435630, -29.02926342023009454, 28.71829084836867452 ) ) ;
#8700=CARTESIAN_POINT ( 'NONE',  ( -103.3843560967306701, -45.26539566788723334, 158.7060436347484824 ) ) ;
#8705=ORIENTED_EDGE ( 'NONE', *, *, #94307, .T. ) ;
#8707=CARTESIAN_POINT ( 'NONE',  ( -37.19345962173282771, -60.00000000000000000, 48.57494274058771566 ) ) ;
#8717=CARTESIAN_POINT ( 'NONE',  ( 86.44524746911137925, -60.00000000000003553, 22.58426570472127182 ) ) ;
#8718=CARTESIAN_POINT ( 'NONE',  ( -32.39963873073048717, -25.61850230709818277, 31.48490130413751587 ) ) ;
#8720=CARTESIAN_POINT ( 'NONE',  ( -1.544427540536530316E-15, -4.285714285714290916, 25.22241582816893057 ) ) ;
#8721=CARTESIAN_POINT ( 'NONE',  ( 40.48067620657982957, -46.43136235810992218, 40.68172795048424462 ) ) ;
#8722=CARTESIAN_POINT ( 'NONE',  ( 71.80342808059909032, -30.00000000000000000, -19.71766482350836469 ) ) ;
#8726=CARTESIAN_POINT ( 'NONE',  ( -82.83498824252026793, -38.82036250731917448, 196.8018683164616789 ) ) ;
#8730=CARTESIAN_POINT ( 'NONE',  ( 35.47391375821870696, -59.99999999999999289, 39.53917635555357890 ) ) ;
#8737=CARTESIAN_POINT ( 'NONE',  ( 109.9064092654975155, -60.00000000000000711, 142.7128145035794375 ) ) ;
#8742=CARTESIAN_POINT ( 'NONE',  ( -91.63847879749884839, -29.99999999999996447, 190.7599629194617421 ) ) ;
#8757=CARTESIAN_POINT ( 'NONE',  ( 85.23626010823490162, -18.61825805347759655, 157.3731097714332634 ) ) ;
#8765=CARTESIAN_POINT ( 'NONE',  ( 5.430765937255434217, -60.00000000000000000, -36.83649123861827945 ) ) ;
#8775=CARTESIAN_POINT ( 'NONE',  ( 86.74269761982320404, -39.11688401941764681, 188.5944613561505321 ) ) ;
#8793=CARTESIAN_POINT ( 'NONE',  ( 105.5514723802492512, -57.67109349774979421, 101.8026348850644638 ) ) ;
#8800=CARTESIAN_POINT ( 'NONE',  ( -82.70757079118186539, -59.99999999999999289, 198.6122815915291255 ) ) ;
#8804=CARTESIAN_POINT ( 'NONE',  ( -85.78836534190880059, -32.04508190827686320, 182.7537413317583912 ) ) ;
#8812=CARTESIAN_POINT ( 'NONE',  ( -86.78291921055377145, -60.23020244905906395, -10.97695437812392782 ) ) ;
#8821=CARTESIAN_POINT ( 'NONE',  ( -17.09952670627316706, -60.00000000000001421, -44.43607591113852351 ) ) ;
#8823=CARTESIAN_POINT ( 'NONE',  ( -78.52260771847107890, -22.14211393470201017, 122.4770835781163782 ) ) ;
#8825=CARTESIAN_POINT ( 'NONE',  ( 76.24208907273079205, -14.21045842199436571, 145.5826741442930086 ) ) ;
#8827=CARTESIAN_POINT ( 'NONE',  ( 95.00826987541751123, -57.67190437205294984, 32.63624362569164106 ) ) ;
#8844=CARTESIAN_POINT ( 'NONE',  ( 28.86447232581024025, -46.43248914764336632, 33.96989350538401453 ) ) ;
#8852=DIRECTION ( 'NONE',  ( 1.871721906610600077E-16, 0.000000000000000000, -1.000000000000000000 ) ) ;
#8857=CARTESIAN_POINT ( 'NONE',  ( 92.20132009836827081, -60.00000000000002132, -13.14806591022434290 ) ) ;
#8862=MECHANICAL_DESIGN_GEOMETRIC_PRESENTATION_REPRESENTATION('',(#79548),#38240);
#8874=CARTESIAN_POINT ( 'NONE',  ( 83.16664753440134916, -37.83434465694476501, -3.567909543517462367 ) ) ;
#8882=CARTESIAN_POINT ( 'NONE',  ( -75.45824100956336622, -38.34912970864160542, 173.9041770547032968 ) ) ;
#8884=CARTESIAN_POINT ( 'NONE',  ( -76.77023017917504433, -60.00000000000002842, 146.8812870064044489 ) ) ;
#8886=CARTESIAN_POINT ( 'NONE',  ( 66.25591572988753342, -36.00678726784801142, 88.05794226510028011 ) ) ;
#8891=CARTESIAN_POINT ( 'NONE',  ( -113.5700743903323087, -57.67116359713492812, 158.3188924881959849 ) ) ;
#8912=CARTESIAN_POINT ( 'NONE',  ( -95.21340098042236377, -29.99999999999999645, 191.3393382648713441 ) ) ;
#8915=CARTESIAN_POINT ( 'NONE',  ( 62.96112565841632858, -57.67852246553200501, 118.3385123048287397 ) ) ;
#8918=CARTESIAN_POINT ( 'NONE',  ( 14.84396807590208311, -24.03113400032698621, -38.53105962718119315 ) ) ;
#8921=CARTESIAN_POINT ( 'NONE',  ( -38.99177359176184865, -60.00000000000002132, 50.73434467415564342 ) ) ;
#8924=CARTESIAN_POINT ( 'NONE',  ( -86.12441050467187154, -61.04151491554013376, 194.3981187559223827 ) ) ;
#8929=CARTESIAN_POINT ( 'NONE',  ( -7.081050772456690012, -32.51271769174685033, 29.29877307394730224 ) ) ;
#8932=CARTESIAN_POINT ( 'NONE',  ( 87.14793098496349444, -38.00000000001091394, 189.0872956505646414 ) ) ;
#8946=CARTESIAN_POINT ( 'NONE',  ( 106.4003153237399459, -14.21045842199437281, 159.7124754531589019 ) ) ;
#8961=CARTESIAN_POINT ( 'NONE',  ( -35.47086896947185153, -60.00000000000493827, 50.14652216712747190 ) ) ;
#8964=CARTESIAN_POINT ( 'NONE',  ( 111.5499265342648840, -60.00000000000001421, 157.8294912153404255 ) ) ;
#8966=CARTESIAN_POINT ( 'NONE',  ( -78.82101707352518360, -14.21045842199447584, 187.8153594499050882 ) ) ;
#8967=CARTESIAN_POINT ( 'NONE',  ( 13.47176107517659638, -39.47274912387565848, 30.55088658083724695 ) ) ;
#8970=CARTESIAN_POINT ( 'NONE',  ( -42.69126397430579800, -56.80055262131805449, 45.33095584542797241 ) ) ;
#8985=CARTESIAN_POINT ( 'NONE',  ( 60.59444657107560772, -30.00000000001982059, 93.60444982598512809 ) ) ;
#8989=CARTESIAN_POINT ( 'NONE',  ( 80.76851621713109353, -30.00000000000000355, 10.64488254787337063 ) ) ;
#8991=EDGE_CURVE ( 'NONE', #17004, #34393, #97768, .T. ) ;
#9006=CARTESIAN_POINT ( 'NONE',  ( 71.58809529799425775, -38.32751537232760342, 143.4284849665567094 ) ) ;
#9020=CARTESIAN_POINT ( 'NONE',  ( 41.97104496162273790, -38.13452990356884698, 52.68411854546428685 ) ) ;
#9025=CARTESIAN_POINT ( 'NONE',  ( 86.20875240452089372, -24.70518494214491767, 181.2918537991968435 ) ) ;
#9029=CARTESIAN_POINT ( 'NONE',  ( 85.73719764786143571, -57.67053834193623629, -26.44931048121824091 ) ) ;
#9035=CARTESIAN_POINT ( 'NONE',  ( -81.36514358934235247, -30.00000000000001066, -1.450368654527133039 ) ) ;
#9055=CARTESIAN_POINT ( 'NONE',  ( -63.92444039710895254, -29.66271673368065365, -23.50404950011429506 ) ) ;
#9058=EDGE_CURVE ( 'NONE', #89315, #24456, #49575, .T. ) ;
#9062=CARTESIAN_POINT ( 'NONE',  ( -2.499999999999995559, -30.00000000000000000, -14.79019945774903810 ) ) ;
#9063=EDGE_CURVE ( 'NONE', #84468, #80603, #54724, .T. ) ;
#9066=CARTESIAN_POINT ( 'NONE',  ( -19.54990280911475509, -60.00000000000001421, -41.86024675016059859 ) ) ;
#9070=CARTESIAN_POINT ( 'NONE',  ( 101.6834587361868927, -52.72719984991043418, 192.5473745686417715 ) ) ;
#9085=CARTESIAN_POINT ( 'NONE',  ( -5.651997800604014799, -57.67124204504380458, 41.59089347824649252 ) ) ;
#9091=CARTESIAN_POINT ( 'NONE',  ( -81.17775171884230190, -14.21045842199422005, -20.84891578014651259 ) ) ;
#9092=CARTESIAN_POINT ( 'NONE',  ( 1.295095875561511761E-05, -30.00000000000000000, 37.00000000000000711 ) ) ;
#9094=CARTESIAN_POINT ( 'NONE',  ( -49.49064989153462335, -46.44333672598879303, 52.19747830327506222 ) ) ;
#9097=CARTESIAN_POINT ( 'NONE',  ( -100.5716031806942397, -52.74657777821607851, 193.7722495540973568 ) ) ;
#9102=CARTESIAN_POINT ( 'NONE',  ( 78.23225470723293995, -38.60547359199907191, 189.0516081268614244 ) ) ;
#9107=CARTESIAN_POINT ( 'NONE',  ( 90.60055052440634427, -30.00000000000000000, 190.2884839676575268 ) ) ;
#9114=CARTESIAN_POINT ( 'NONE',  ( 51.71506308164819643, -25.64903502818010139, 48.87485861820827182 ) ) ;
#9119=CARTESIAN_POINT ( 'NONE',  ( -109.8761471886628414, -38.35606193139696529, 153.1324815485978093 ) ) ;
#9122=CARTESIAN_POINT ( 'NONE',  ( 109.6530265699404509, -38.35603087673744938, 151.1878659942163949 ) ) ;
#9124=CARTESIAN_POINT ( 'NONE',  ( 95.06247054295488397, -60.15120782134928845, 86.15213186706492365 ) ) ;
#9129=CARTESIAN_POINT ( 'NONE',  ( 73.97498551117102750, -60.00000000000000000, 171.9667912108089922 ) ) ;
#9130=CARTESIAN_POINT ( 'NONE',  ( -2.499999999999963141, -18.83381654053417620, 27.02533567785737034 ) ) ;
#9133=CARTESIAN_POINT ( 'NONE',  ( 58.97917396427931891, -53.38380800473449739, 76.07987900925265023 ) ) ;
#9138=CARTESIAN_POINT ( 'NONE',  ( -74.98372929288009914, -30.00000000032233416, 156.5717653030027918 ) ) ;
#9149=CARTESIAN_POINT ( 'NONE',  ( 84.10407772408511562, -39.43706024606296978, 178.9938989443399748 ) ) ;
#9158=CARTESIAN_POINT ( 'NONE',  ( -15.69138703980276262, -24.30991770495803905, -38.52719090127629897 ) ) ;
#9160=CARTESIAN_POINT ( 'NONE',  ( 56.79672723872580775, -60.00000000000000000, 90.54572580908420321 ) ) ;
#9162=CARTESIAN_POINT ( 'NONE',  ( -26.71188838280077960, -30.21239539108677619, 38.94092172635536997 ) ) ;
#9173=CARTESIAN_POINT ( 'NONE',  ( 44.04518021092881952, -34.58949428284888228, -28.87998162211279052 ) ) ;
#9174=EDGE_CURVE ( 'NONE', #86580, #4466, #57982, .T. ) ;
#9187=CARTESIAN_POINT ( 'NONE',  ( -95.54720156996677360, -59.99999999999999289, 52.92735314107190447 ) ) ;
#9194=CARTESIAN_POINT ( 'NONE',  ( -82.39419631509804276, -46.47357755561642989, 175.1841951907930479 ) ) ;
#9198=( BOUNDED_CURVE ( )  B_SPLINE_CURVE ( 2, ( #80835, #31783, #65194 ),
 .UNSPECIFIED., .F., .F. ) 
 B_SPLINE_CURVE_WITH_KNOTS ( ( 3, 3 ),
 ( 0.000000000000000000, 1.000000000000000000 ),
 .UNSPECIFIED. ) 
 CURVE ( )  GEOMETRIC_REPRESENTATION_ITEM ( )  RATIONAL_B_SPLINE_CURVE ( ( 1.000000000000000000, 1.857142857142858317, 1.000000000000000000 ) ) 
 REPRESENTATION_ITEM ( '' )  );
#9206=CARTESIAN_POINT ( 'NONE',  ( -2.499999999999963141, -18.83381654053417620, 27.02533567785737034 ) ) ;
#9212=CARTESIAN_POINT ( 'NONE',  ( 113.8520663817495233, -59.99999999999995026, 157.1483003829898450 ) ) ;
#9214=CARTESIAN_POINT ( 'NONE',  ( -109.0818456041877766, -30.00000000000003908, 182.6288557207085148 ) ) ;
#9215=CARTESIAN_POINT ( 'NONE',  ( -59.14235056471916607, -22.12910259080065600, 62.21584231372889917 ) ) ;
#9218=CARTESIAN_POINT ( 'NONE',  ( 94.49474166934638220, -59.99999999997076117, 21.48900165056691591 ) ) ;
#9220=CARTESIAN_POINT ( 'NONE',  ( 7.230429965541936177, -53.39678090435286606, 32.77949809094599232 ) ) ;
#9221=CARTESIAN_POINT ( 'NONE',  ( -104.6318941305285932, -52.71024081308034681, 158.7339107473082152 ) ) ;
#9224=ADVANCED_FACE ( 'NONE', ( #32094, #105950, #15356, #96304, #31059, #14817 ), #64972, .T. ) ;
#9230=CARTESIAN_POINT ( 'NONE',  ( -29.60599819566758129, -60.00000000000002132, 42.84210040572467904 ) ) ;
#9235=CARTESIAN_POINT ( 'NONE',  ( 15.29459302239697216, 0.000000000000000000, 7.540142361539030169 ) ) ;
#9241=CARTESIAN_POINT ( 'NONE',  ( 86.95153870091223780, -59.99999999999995737, -4.620851249272444505 ) ) ;
#9242=CARTESIAN_POINT ( 'NONE',  ( -31.08105070400566916, -53.38287997746494540, 36.01393495271150869 ) ) ;
#9244=CARTESIAN_POINT ( 'NONE',  ( 46.27822564134725525, -36.07043649651712514, 44.25496614335602885 ) ) ;
#9248=CARTESIAN_POINT ( 'NONE',  ( -80.07567166459625696, -38.78766219017933992, 193.1244021680591345 ) ) ;
#9252=CARTESIAN_POINT ( 'NONE',  ( 42.70433196527829978, -60.00000000000005684, 46.14154939129071664 ) ) ;
#9259=CARTESIAN_POINT ( 'NONE',  ( 106.2279738410354071, -60.00000000000002842, 117.8309344228806168 ) ) ;
#9267=CARTESIAN_POINT ( 'NONE',  ( -101.1191644727027352, -29.99999999999999289, 171.1750318645146649 ) ) ;
#9280=CARTESIAN_POINT ( 'NONE',  ( 83.03340579700397939, -32.54870090252141779, 159.1926985072703928 ) ) ;
#9285=CARTESIAN_POINT ( 'NONE',  ( 10.00000000000000000, 0.000000000000000000, 10.00000000000000178 ) ) ;
#9310=CARTESIAN_POINT ( 'NONE',  ( 107.5610214307659476, -57.67122956308984527, 113.7628399357034397 ) ) ;
#9314=CARTESIAN_POINT ( 'NONE',  ( -2.499999999999999556, -8.000000000000000000, 17.89626171146327493 ) ) ;
#9316=CARTESIAN_POINT ( 'NONE',  ( -82.35766411969579792, -59.99999999999999289, 198.3413902865526381 ) ) ;
#9320=CARTESIAN_POINT ( 'NONE',  ( -82.59538156006668430, -60.84729630826085867, 189.6675515197301252 ) ) ;
#9328=CARTESIAN_POINT ( 'NONE',  ( -85.75585748537427833, -52.73827868327173007, -6.687191420894485816 ) ) ;
#9335=CARTESIAN_POINT ( 'NONE',  ( 37.62958953315902022, -14.21045842199429288, 41.24408864243086015 ) ) ;
#9337=CARTESIAN_POINT ( 'NONE',  ( -59.37491258674359784, -59.99999999999998579, -38.24906085379748788 ) ) ;
#9338=CARTESIAN_POINT ( 'NONE',  ( -66.84523826069663244, -46.43835352555290541, 95.56956660544847182 ) ) ;
#9340=CARTESIAN_POINT ( 'NONE',  ( 70.38659604113041723, -14.21045842199445808, 117.5484250040930050 ) ) ;
#9342=CARTESIAN_POINT ( 'NONE',  ( 94.71150925245034102, -57.65915928951965697, -7.875939490799622966 ) ) ;
#9361=CARTESIAN_POINT ( 'NONE',  ( 31.57827475542996609, -32.54814147035259708, 32.45590311695885788 ) ) ;
#9376=CARTESIAN_POINT ( 'NONE',  ( 81.07743897483196349, -60.00000000000000711, -27.28973066995784436 ) ) ;
#9388=CARTESIAN_POINT ( 'NONE',  ( 84.49172617919205663, -45.28678258021372471, -6.204812034688317546 ) ) ;
#9400=CARTESIAN_POINT ( 'NONE',  ( 75.39868036955950004, -36.01852124489236218, 119.8304219598088309 ) ) ;
#9407=CARTESIAN_POINT ( 'NONE',  ( -94.30414684669057124, -57.67279326051714605, 1.132156541063573441 ) ) ;
#9412=CARTESIAN_POINT ( 'NONE',  ( 106.2181247233446300, -60.15136654602780197, 163.5236569256875043 ) ) ;
#9416=DIRECTION ( 'NONE',  ( 0.000000000000000000, -1.000000000000000000, 0.000000000000000000 ) ) ;
#9428=CARTESIAN_POINT ( 'NONE',  ( -90.03084723851439719, -30.00000000000000000, 189.8964335926784770 ) ) ;
#9432=CARTESIAN_POINT ( 'NONE',  ( 71.49051955128589952, -57.67963396668447729, 166.9361842711434747 ) ) ;
#9434=CARTESIAN_POINT ( 'NONE',  ( -96.81748461682487061, -38.00000000001091394, 192.8978395531862020 ) ) ;
#9436=CARTESIAN_POINT ( 'NONE',  ( 19.07582147746917300, -25.49993130453409407, -38.49573148241584164 ) ) ;
#9440=CARTESIAN_POINT ( 'NONE',  ( -41.05948510805755802, -59.99999999999999289, 53.66256863961316981 ) ) ;
#9449=CARTESIAN_POINT ( 'NONE',  ( -86.45611204286437612, -17.05227200858531234, 183.4756348703512572 ) ) ;
#9452=CARTESIAN_POINT ( 'NONE',  ( -6.099882006367853826, -39.47594237312841869, 30.45917207147936168 ) ) ;
#9455=CARTESIAN_POINT ( 'NONE',  ( 86.23711656224473643, -45.40185197806301431, 189.5298877258528023 ) ) ;
#9467=CARTESIAN_POINT ( 'NONE',  ( 106.5496036037455809, -14.21045842199433373, 161.7522804960935900 ) ) ;
#9468=CARTESIAN_POINT ( 'NONE',  ( -81.09901249779620969, -49.92721230687652678, 168.6194323894324896 ) ) ;
#9489=CARTESIAN_POINT ( 'NONE',  ( 112.2483500844232651, -60.00000000000000000, 174.7240955042347821 ) ) ;
#9490=CARTESIAN_POINT ( 'NONE',  ( -96.06797501213969781, -14.21045842199444564, 198.0637310406154938 ) ) ;
#9491=CARTESIAN_POINT ( 'NONE',  ( 16.50575907406394549, -25.54973315577406723, 28.36482997719511445 ) ) ;
#9495=CARTESIAN_POINT ( 'NONE',  ( -40.90326834193143668, -56.80365015598610512, 43.40273101573804837 ) ) ;
#9498=UNCERTAINTY_MEASURE_WITH_UNIT (LENGTH_MEASURE( 1.000000000000000082E-05 ), #37526, 'distance_accuracy_value', 'NONE');
#9500=CARTESIAN_POINT ( 'NONE',  ( -3.301565691951523718, -4.285714285714295357, 25.05982991920904368 ) ) ;
#9509=CARTESIAN_POINT ( 'NONE',  ( 80.48472413805814085, -30.00000000000003197, -13.06866816408327381 ) ) ;
#9515=CARTESIAN_POINT ( 'NONE',  ( 83.28278898132033703, -30.00000000000000711, 45.15681117069227923 ) ) ;
#9527=EDGE_LOOP ( 'NONE', ( #95964, #40541 ) ) ;
#9531=CARTESIAN_POINT ( 'NONE',  ( 75.48692410520401097, -38.35222609583806275, 174.0895271288090100 ) ) ;
#9556=CARTESIAN_POINT ( 'NONE',  ( 86.25580709159085302, -24.66185776332405766, 181.7623954071263199 ) ) ;
#9560=CARTESIAN_POINT ( 'NONE',  ( 94.58869087161561140, -57.65564386714318346, -10.20074617627543212 ) ) ;
#9562=DIRECTION ( 'NONE',  ( 1.000000000000000000, 0.000000000000000000, 0.000000000000000000 ) ) ;
#9565=CARTESIAN_POINT ( 'NONE',  ( -81.40749646105963677, -30.00000000000000711, -10.00555188706439580 ) ) ;
#9570=EDGE_CURVE ( 'NONE', #49798, #85237, #66347, .T. ) ;
#9577=CARTESIAN_POINT ( 'NONE',  ( 14.70186166385661686, -17.16666514262621845, -34.37153611367288164 ) ) ;
#9581=LINE ( 'NONE', #43039, #30136 ) ;
#9582=CARTESIAN_POINT ( 'NONE',  ( -52.11016065996651037, -27.94326923599848911, -27.40981600032927190 ) ) ;
#9592=CARTESIAN_POINT ( 'NONE',  ( -49.87223528229673519, -60.00000000000000711, -37.92974157021075143 ) ) ;
#9597=CARTESIAN_POINT ( 'NONE',  ( 99.16506380945328658, -37.81309594716023526, 191.7295361414442709 ) ) ;
#9607=DIRECTION ( 'NONE',  ( 0.000000000000000000, 0.000000000000000000, -1.000000000000000000 ) ) ;
#9612=CARTESIAN_POINT ( 'NONE',  ( -5.653151814788443197, -60.00000000000000000, -44.93963918615513364 ) ) ;
#9618=CARTESIAN_POINT ( 'NONE',  ( -78.96607584984282369, -14.21045842199439946, -22.44766605243856361 ) ) ;
#9621=CARTESIAN_POINT ( 'NONE',  ( -50.61134058422784676, -46.44362122540161408, 54.16156104182443443 ) ) ;
#9630=CARTESIAN_POINT ( 'NONE',  ( 104.9507826212073951, -38.39463534192324801, 197.5418619574190870 ) ) ;
#9636=CARTESIAN_POINT ( 'NONE',  ( 91.73269967366050537, -29.99999999999999289, 190.7761219706676172 ) ) ;
#9642=CARTESIAN_POINT ( 'NONE',  ( 52.74211290327268387, -29.10573497541706089, 51.84957213115916375 ) ) ;
#9646=CARTESIAN_POINT ( 'NONE',  ( -105.0815908665296945, -38.35658034820646378, 118.4378099064370105 ) ) ;
#9649=CARTESIAN_POINT ( 'NONE',  ( 110.8582216372020923, -38.35606662024349589, 166.2350381741399019 ) ) ;
#9651=CARTESIAN_POINT ( 'NONE',  ( 84.26382309112767643, -37.84986900746150695, 39.36842225124562589 ) ) ;
#9655=CARTESIAN_POINT ( 'NONE',  ( 74.83933575179801778, -60.00000000000000000, 180.0232458328126199 ) ) ;
#9660=CARTESIAN_POINT ( 'NONE',  ( 61.52822294692849425, -22.11542171271097601, 67.98225717687230940 ) ) ;
#9670=( LENGTH_UNIT ( ) NAMED_UNIT ( * ) SI_UNIT ( .MILLI., .METRE. ) );
#9678=CARTESIAN_POINT ( 'NONE',  ( 85.58339654611728520, -25.25876667343988657, 173.5966304797753423 ) ) ;
#9689=CARTESIAN_POINT ( 'NONE',  ( -18.64887156299073823, -25.34552484672397910, -38.50094829128359208 ) ) ;
#9692=CARTESIAN_POINT ( 'NONE',  ( 46.76626013676900584, -60.00000000000000711, 64.25575086454696816 ) ) ;
#9695=CARTESIAN_POINT ( 'NONE',  ( 5.358783066250208726, -12.92270511644005460, 32.09298117868684841 ) ) ;
#9696=CARTESIAN_POINT ( 'NONE',  ( -14.21687706511438876, -22.25485696289420190, 35.82459387298590059 ) ) ;
#9710=CARTESIAN_POINT ( 'NONE',  ( 53.22521075176659622, -34.58939553375807918, -27.04733313792341676 ) ) ;
#9717=CARTESIAN_POINT ( 'NONE',  ( -102.8043655696301641, -60.00000000000000000, 97.43818821035735311 ) ) ;
#9724=CARTESIAN_POINT ( 'NONE',  ( -85.11569458792331488, -25.46023517225657784, 167.9907940485576887 ) ) ;
#9733=CARTESIAN_POINT ( 'NONE',  ( -73.19784523472750948, -56.33007067409605639, -24.31537338432895012 ) ) ;
#9738=SURFACE_STYLE_USAGE ( .BOTH. , #75553 ) ;
#9740=CARTESIAN_POINT ( 'NONE',  ( 104.0150978814680940, -30.00000000000001421, 120.6686366764556766 ) ) ;
#9742=CARTESIAN_POINT ( 'NONE',  ( -79.57248154261856143, -14.21045842199419873, 190.0114072710836979 ) ) ;
#9743=CARTESIAN_POINT ( 'NONE',  ( -58.95728471227350553, -25.60210830145040717, 63.31610968965730990 ) ) ;
#9746=CARTESIAN_POINT ( 'NONE',  ( 63.92811455585417946, -60.00000000001919176, -37.02723835566183652 ) ) ;
#9749=CARTESIAN_POINT ( 'NONE',  ( 5.068871021964256762, -39.47244754689903345, 30.45846616484312008 ) ) ;
#9751=CARTESIAN_POINT ( 'NONE',  ( -101.0703404440478153, -37.82018982836708432, 188.0744957792581715 ) ) ;
#9758=CARTESIAN_POINT ( 'NONE',  ( -36.70586056242206041, -60.00000000000001421, 48.05235279427500927 ) ) ;
#9772=CARTESIAN_POINT ( 'NONE',  ( -31.81784266628647018, -42.96403268502453443, 34.45923875972478356 ) ) ;
#9774=CARTESIAN_POINT ( 'NONE',  ( 43.84264430761513154, -36.07170451123901955, 41.44757837376981513 ) ) ;
#9778=CARTESIAN_POINT ( 'NONE',  ( -81.35954770826289462, -38.84021855358666642, 195.0925015028629730 ) ) ;
#9790=CARTESIAN_POINT ( 'NONE',  ( 108.7801334214385776, -60.00000000000002842, 134.4245170770223297 ) ) ;
#9796=CARTESIAN_POINT ( 'NONE',  ( -97.45253354081053487, -29.99999999999991118, 190.9130999118634691 ) ) ;
#9809=CARTESIAN_POINT ( 'NONE',  ( 81.96495203190069390, -42.96965882988520491, 165.6653473756363724 ) ) ;
#9826=CARTESIAN_POINT ( 'NONE',  ( 87.08998920831058399, -28.00350159148703710, 187.1668149538881494 ) ) ;
#9852=CARTESIAN_POINT ( 'NONE',  ( -76.28990388871434902, -60.00000000000000711, 188.1246153785924093 ) ) ;
#9857=CARTESIAN_POINT ( 'NONE',  ( -83.48188574608597889, -57.36243674763982625, 189.6665432021039521 ) ) ;
#9865=CARTESIAN_POINT ( 'NONE',  ( -85.75146761789847005, -52.73616787743888068, -6.162650518953375567 ) ) ;
#9874=CARTESIAN_POINT ( 'NONE',  ( 70.37902863207267501, -59.99999999999998579, 160.1157867729151576 ) ) ;
#9877=CARTESIAN_POINT ( 'NONE',  ( 24.89419722466787022, -30.00000000000004974, -38.80375014483585261 ) ) ;
#9878=CARTESIAN_POINT ( 'NONE',  ( -75.11045228325910728, -39.49349330803696034, 121.1541899256156256 ) ) ;
#9880=CARTESIAN_POINT ( 'NONE',  ( 65.47680943546976096, -59.99999999999998579, 130.5870305019238913 ) ) ;
#9882=CARTESIAN_POINT ( 'NONE',  ( 2.852950387436009816, -60.00000000016757440, 42.00000030345589153 ) ) ;
#9897=CARTESIAN_POINT ( 'NONE',  ( 19.00223544648544660, -4.285714285714296246, -16.66764709352487017 ) ) ;
#9904=( GEOMETRIC_REPRESENTATION_CONTEXT ( 3 ) GLOBAL_UNCERTAINTY_ASSIGNED_CONTEXT ( ( #9498 ) ) GLOBAL_UNIT_ASSIGNED_CONTEXT ( ( #37526, #63373, #12135 ) ) REPRESENTATION_CONTEXT ( 'NONE', 'WORKASPACE' ) );
#9906=CARTESIAN_POINT ( 'NONE',  ( 32.48674833035018850, -49.90044203452471550, 36.01891768520543735 ) ) ;
#9922=CARTESIAN_POINT ( 'NONE',  ( 92.53276982938558604, -59.99999999999997868, -10.97258584023427375 ) ) ;
#9937=CARTESIAN_POINT ( 'NONE',  ( 84.30433287656845209, -52.73991272358569660, -14.69517893486082727 ) ) ;
#9951=CARTESIAN_POINT ( 'NONE',  ( 75.68650039582325917, -32.54705830725040983, 118.5082925635865081 ) ) ;
#9954=MECHANICAL_DESIGN_GEOMETRIC_PRESENTATION_REPRESENTATION('',(#47809),#46081);
#9957=CARTESIAN_POINT ( 'NONE',  ( -88.38279035983548226, -57.66943555457145720, -24.13713039724196818 ) ) ;
#9963=CARTESIAN_POINT ( 'NONE',  ( 101.5505671214599914, -37.84846131813309000, 186.3044032585196135 ) ) ;
#9981=CARTESIAN_POINT ( 'NONE',  ( -87.91521282718065322, -29.99999999999999289, 186.5625098616759487 ) ) ;
#9986=CARTESIAN_POINT ( 'NONE',  ( 70.41623196469389256, -57.68248939742788650, 157.4130776120266546 ) ) ;
#9991=CARTESIAN_POINT ( 'NONE',  ( 45.16523152280084474, -34.40758779083247987, -36.86626960789413232 ) ) ;
#9993=CARTESIAN_POINT ( 'NONE',  ( -44.15351406616127861, -60.00000000000000711, 58.95332731642092483 ) ) ;
#9998=CARTESIAN_POINT ( 'NONE',  ( -86.31883211543134848, -39.17431195792791243, 187.7266355625923495 ) ) ;
#10001=CARTESIAN_POINT ( 'NONE',  ( -4.101533912778845270, -53.40245796095344843, 32.78225363056029806 ) ) ;
#10016=CARTESIAN_POINT ( 'NONE',  ( 106.6793784964389289, -14.21045842199433729, 163.7934217252150972 ) ) ;
#10017=CARTESIAN_POINT ( 'NONE',  ( -81.98242152828360929, -32.56195222614032758, 150.9971016278573188 ) ) ;
#10038=CARTESIAN_POINT ( 'NONE',  ( 107.4330949502293464, -60.00000000000000000, 196.5277503695512564 ) ) ;
#10039=CARTESIAN_POINT ( 'NONE',  ( -81.96434049221993234, -29.99999999999993250, 194.6677479149438454 ) ) ;
#10040=CARTESIAN_POINT ( 'NONE',  ( 21.68997527405830184, -53.39465657004741672, 33.52469154556025188 ) ) ;
#10045=CARTESIAN_POINT ( 'NONE',  ( -41.95185451917502206, -60.25535463032460370, 45.28364850313863599 ) ) ;
#10058=CARTESIAN_POINT ( 'NONE',  ( 81.06325062923930602, -30.00000000000000000, 2.799235988874741565 ) ) ;
#10062=CARTESIAN_POINT ( 'NONE',  ( 80.82096024282435565, -30.00000000000000000, 17.00536050008537003 ) ) ;
#10080=CARTESIAN_POINT ( 'NONE',  ( 77.53117718845349771, -38.51705233716531751, 186.5868546221014412 ) ) ;
#10099=CARTESIAN_POINT ( 'NONE',  ( 84.89364056863026065, -50.19228796424612682, 188.9982818557025723 ) ) ;
#10110=CARTESIAN_POINT ( 'NONE',  ( -86.92488039023091062, -30.00000000000000711, 70.05807166599328184 ) ) ;
#10123=CARTESIAN_POINT ( 'NONE',  ( 56.17098950358883513, -28.68981958306524049, -26.22444997023189828 ) ) ;
#10126=CARTESIAN_POINT ( 'NONE',  ( -25.43960792238905100, -22.08944486031660759, 28.86612087644610725 ) ) ;
#10131=CARTESIAN_POINT ( 'NONE',  ( -65.27364549594882703, -29.77031089310590772, -22.95100066570442010 ) ) ;
#10138=CARTESIAN_POINT ( 'NONE',  ( -97.47674776263787066, -60.00000000000000000, 196.6139650356533934 ) ) ;
#10141=DIRECTION ( 'NONE',  ( 1.871721906610600077E-16, 0.000000000000000000, -1.000000000000000000 ) ) ;
#10142=CARTESIAN_POINT ( 'NONE',  ( 102.4337014127728054, -60.18830211168408084, 193.6666088890698632 ) ) ;
#10157=CARTESIAN_POINT ( 'NONE',  ( -42.46252528007325111, -57.68686955033432895, 59.97785686028149854 ) ) ;
#10162=CARTESIAN_POINT ( 'NONE',  ( -89.98348853342757536, -29.99999999999992184, -2.848863062743723695 ) ) ;
#10164=CARTESIAN_POINT ( 'NONE',  ( -49.92868248732877134, -22.20187048435544241, 44.97503486679070761 ) ) ;
#10171=CARTESIAN_POINT ( 'NONE',  ( 75.66773936237699161, -38.35839768494054880, 175.7330108619280793 ) ) ;
#10176=CARTESIAN_POINT ( 'NONE',  ( 91.68272017985721334, -30.00000000000000711, 190.7589576344717557 ) ) ;
#10185=CARTESIAN_POINT ( 'NONE',  ( 51.13096205315856224, -25.65380906861201993, 47.91585540195683990 ) ) ;
#10189=CARTESIAN_POINT ( 'NONE',  ( -91.21237190957077701, -38.40264986056752861, -11.26304677710397328 ) ) ;
#10193=CARTESIAN_POINT ( 'NONE',  ( 108.2638565580548971, -38.35770216212828387, 192.2389173063952228 ) ) ;
#10195=CARTESIAN_POINT ( 'NONE',  ( 86.75328224081307837, -60.14641367048189835, 26.71604830143463616 ) ) ;
#10203=CARTESIAN_POINT ( 'NONE',  ( 62.81177132629515825, -25.58257438566387876, 72.96335641850546949 ) ) ;
#10214=CARTESIAN_POINT ( 'NONE',  ( 34.49754285437400370, -23.83101018980520180, 33.28975017431508121 ) ) ;
#10220=CARTESIAN_POINT ( 'NONE',  ( 85.12060041149554479, -28.84484196787844468, 173.9512315299091938 ) ) ;
#10228=CARTESIAN_POINT ( 'NONE',  ( -18.66309977023624356, -25.35065258291380985, -38.50078107122106985 ) ) ;
#10231=CARTESIAN_POINT ( 'NONE',  ( 50.68031002952036346, -60.00000000000001421, 73.51902701646098137 ) ) ;
#10233=CARTESIAN_POINT ( 'NONE',  ( 32.12416968186654032, -33.82503823335301263, 41.92710291939467027 ) ) ;
#10235=CARTESIAN_POINT ( 'NONE',  ( 21.71774177896430302, -17.82916512352614546, 31.46925418864567092 ) ) ;
#10237=CARTESIAN_POINT ( 'NONE',  ( -2.499999999999996891, -8.000000000000000000, -17.89626171146327493 ) ) ;
#10252=CARTESIAN_POINT ( 'NONE',  ( 37.34004865435771592, -21.77016028096032230, -27.75726658366467703 ) ) ;
#10261=CARTESIAN_POINT ( 'NONE',  ( -101.9681297424606896, -60.00000000000000000, 92.55871325212498846 ) ) ;
#10269=CARTESIAN_POINT ( 'NONE',  ( -84.97744388938244242, -25.49483301205029662, 166.4590254830890785 ) ) ;
#10279=CARTESIAN_POINT ( 'NONE',  ( -89.99999999999997158, -52.00000000000000000, 198.0238439516549818 ) ) ;
#10284=AXIS2_PLACEMENT_3D ( 'NONE', #30033, #62923, #3621 ) ;
#10286=CARTESIAN_POINT ( 'NONE',  ( 93.38347165230982228, -30.00000000000000711, 56.44843285056885662 ) ) ;
#10287=CARTESIAN_POINT ( 'NONE',  ( -75.88739805180117060, -29.99999999999992895, 164.4352692622292409 ) ) ;
#10288=CARTESIAN_POINT ( 'NONE',  ( -58.57938139866309513, -60.33867871034321695, 78.30623259849073747 ) ) ;
#10292=CARTESIAN_POINT ( 'NONE',  ( -103.4779138909778027, -45.26536958372710018, 182.5772158687078388 ) ) ;
#10298=CARTESIAN_POINT ( 'NONE',  ( -74.19888714062773261, -60.00000000000002842, 174.2398114387819419 ) ) ;
#10303=CARTESIAN_POINT ( 'NONE',  ( 7.540179673759326739, -0.000000000000000000, 15.29468310207052362 ) ) ;
#10309=CARTESIAN_POINT ( 'NONE',  ( -29.95449917297849396, -42.96243585709494539, 33.73512318794586662 ) ) ;
#10311=CARTESIAN_POINT ( 'NONE',  ( 42.72751150375061258, -29.15843491787571296, 38.64392542651763307 ) ) ;
#10315=CARTESIAN_POINT ( 'NONE',  ( -94.17984850184487300, -38.49173615782690661, 201.2012723578915256 ) ) ;
#10320=CARTESIAN_POINT ( 'NONE',  ( 76.76980298920247492, -59.99999999999994316, 146.8786135127453178 ) ) ;
#10328=CARTESIAN_POINT ( 'NONE',  ( 106.8925583917160083, -59.99999999999999289, 121.9434126937530891 ) ) ;
#10347=CARTESIAN_POINT ( 'NONE',  ( 80.03137391603202389, -56.86261681419952652, 169.5251337316609579 ) ) ;
#10363=CARTESIAN_POINT ( 'NONE',  ( 87.48442578725276064, -35.36902786773393359, 189.1140711639433221 ) ) ;
#10385=CARTESIAN_POINT ( 'NONE',  ( -86.49296547713275629, -59.99999999999998579, 200.7931037995327870 ) ) ;
#10390=CARTESIAN_POINT ( 'NONE',  ( -83.81516214089008088, -53.77059041807098083, 188.4648016043023517 ) ) ;
#10398=CARTESIAN_POINT ( 'NONE',  ( -82.81177915581980642, -37.82586872126953637, 1.744547249875558093 ) ) ;
#10409=CARTESIAN_POINT ( 'NONE',  ( 67.93272126786412457, -60.00000000000005684, 143.1824220594335770 ) ) ;
#10411=CARTESIAN_POINT ( 'NONE',  ( -94.85933876937251341, -60.00000000000005684, 26.66572952598730595 ) ) ;
#10412=CARTESIAN_POINT ( 'NONE',  ( -70.22133738824466320, -49.91278461913130116, 108.8011977758523301 ) ) ;
#10413=ORIENTED_EDGE ( 'NONE', *, *, #1587, .F. ) ;
#10414=CARTESIAN_POINT ( 'NONE',  ( 67.93272126786412457, -60.00000000000005684, 143.1824220594335770 ) ) ;
#10416=CARTESIAN_POINT ( 'NONE',  ( 11.32007523880735178, -59.99999999999015898, 42.02588058645514479 ) ) ;
#10435=ORIENTED_EDGE ( 'NONE', *, *, #47720, .T. ) ;
#10438=CARTESIAN_POINT ( 'NONE',  ( 31.09166453561272547, -29.07463850443421904, 31.63965989746132834 ) ) ;
#10440=CARTESIAN_POINT ( 'NONE',  ( 20.16952962162183738, -4.285714285713005722, -15.50035291838722884 ) ) ;
#10452=CARTESIAN_POINT ( 'NONE',  ( 87.58642902445230050, -60.00000000000000000, -22.04675162796464960 ) ) ;
#10458=CARTESIAN_POINT ( 'NONE',  ( -101.0993648165865295, -30.00000000001622524, 198.6624016725467357 ) ) ;
#10466=CARTESIAN_POINT ( 'NONE',  ( 85.67655332170797067, -52.75487301146129937, -9.150629182708584608 ) ) ;
#10477=CARTESIAN_POINT ( 'NONE',  ( 75.77493148631056386, -42.96215371644679237, 126.5390892215617100 ) ) ;
#10485=CARTESIAN_POINT ( 'NONE',  ( -94.14808112328414325, -57.65316219711669987, -13.38331396264917394 ) ) ;
#10492=CARTESIAN_POINT ( 'NONE',  ( 103.9750665207554476, -52.71699900044285414, 186.8198939251532238 ) ) ;
#10510=CARTESIAN_POINT ( 'NONE',  ( -84.97248593416721008, -29.99999999999999645, 170.0635220576484699 ) ) ;
#10513=CARTESIAN_POINT ( 'NONE',  ( 72.74531393631698961, -57.65900400693993788, 179.1409299794756862 ) ) ;
#10517=CARTESIAN_POINT ( 'NONE',  ( 64.43482812103761148, -37.84152687303451756, -32.99898107021154914 ) ) ;
#10520=CARTESIAN_POINT ( 'NONE',  ( -30.87182542889072323, -60.00000000000001421, 43.47827688693090664 ) ) ;
#10523=CARTESIAN_POINT ( 'NONE',  ( -86.12452592232807547, -50.16182726635322098, 190.9343274795246828 ) ) ;
#10526=CARTESIAN_POINT ( 'NONE',  ( -2.033835829640177284, -49.92092604325223704, 32.20724000701986256 ) ) ;
#10542=CARTESIAN_POINT ( 'NONE',  ( 106.1195120942077494, -59.99999999999999289, 102.8136370513695397 ) ) ;
#10543=CARTESIAN_POINT ( 'NONE',  ( -81.76550668722990167, -29.09399621363404975, 145.4573940219550821 ) ) ;
#10564=CARTESIAN_POINT ( 'NONE',  ( 94.67064643570367366, -59.99999999999998579, 46.77569099326773028 ) ) ;
#10565=CARTESIAN_POINT ( 'NONE',  ( -93.93757927471676794, -14.21045842199439946, 198.1409199811383246 ) ) ;
#10566=CARTESIAN_POINT ( 'NONE',  ( 19.10045511374297078, -42.95404717622270141, 31.48189410863279392 ) ) ;
#10569=CARTESIAN_POINT ( 'NONE',  ( -39.87592166654171422, -32.60641129436071850, 37.08344799359745991 ) ) ;
#10583=CARTESIAN_POINT ( 'NONE',  ( 97.79383724715447102, -30.00000000000014921, 190.7107357665381642 ) ) ;
#10586=CARTESIAN_POINT ( 'NONE',  ( 81.97066485211418296, -30.00000000000000000, 33.64756664518507279 ) ) ;
#10603=CARTESIAN_POINT ( 'NONE',  ( 77.52093042597508088, -38.51585880812307749, 186.5480975061236109 ) ) ;
#10623=CARTESIAN_POINT ( 'NONE',  ( 86.37697157886478294, -28.18731561469257940, 184.2989669348581288 ) ) ;
#10631=CARTESIAN_POINT ( 'NONE',  ( -86.45571998004572833, -29.99999999999999645, 67.09524892540846963 ) ) ;
#10636=AXIS2_PLACEMENT_3D ( 'NONE', #91440, #9416, #82800 ) ;
#10638=CARTESIAN_POINT ( 'NONE',  ( -11.42066797802348077, -21.20489296322393002, 27.45196823644660000 ) ) ;
#10642=CARTESIAN_POINT ( 'NONE',  ( 55.98375673512529715, -28.65874727311520687, -26.28204123211169829 ) ) ;
#10643=CARTESIAN_POINT ( 'NONE',  ( -24.76425723927362554, -36.00077592485400402, 31.10340529209751637 ) ) ;
#10647=CARTESIAN_POINT ( 'NONE',  ( -16.70090518186424333, -35.99505156839033759, 30.12198634049419965 ) ) ;
#10648=CARTESIAN_POINT ( 'NONE',  ( -63.90368348448107128, -29.66094596946048512, -23.51237261270683021 ) ) ;
#10663=CARTESIAN_POINT ( 'NONE',  ( 100.3691303487159416, -52.75941910667004464, 193.9373745264102240 ) ) ;
#10678=CARTESIAN_POINT ( 'NONE',  ( -102.2519545932779010, -60.00000000013668000, 80.19353485699372186 ) ) ;
#10682=CARTESIAN_POINT ( 'NONE',  ( -86.47621369144106040, -14.21045842199425735, -14.66750133381012589 ) ) ;
#10684=CARTESIAN_POINT ( 'NONE',  ( -50.93686057180333648, -53.37436350439492116, 57.23435777560519000 ) ) ;
#10695=CARTESIAN_POINT ( 'NONE',  ( 96.06728777640114458, -38.48540547217477581, 201.2030628861659807 ) ) ;
#10698=AXIS2_PLACEMENT_3D ( 'NONE', #11410, #13003, #44335 ) ;
#10701=CARTESIAN_POINT ( 'NONE',  ( 86.13034586361173695, -29.99999999999999645, 179.4755604668315812 ) ) ;
#10702=CIRCLE ( 'NONE', #96807, 2.000000000000001776 ) ;
#10706=CARTESIAN_POINT ( 'NONE',  ( 51.90082211129554679, -18.71876729291939512, 46.78542853416100655 ) ) ;
#10712=CARTESIAN_POINT ( 'NONE',  ( -91.25706933832147172, -38.36172668882709758, -1.507939045793343702 ) ) ;
#10715=CARTESIAN_POINT ( 'NONE',  ( 106.8950883828628946, -38.36540791790844196, 195.0233813272650139 ) ) ;
#10717=CARTESIAN_POINT ( 'NONE',  ( 85.13574873232160201, -45.28282078271436717, 36.04402567606572916 ) ) ;
#10721=APPLICATION_CONTEXT ( 'automotive_design' ) ;
#10728=AXIS2_PLACEMENT_3D ( 'NONE', #14983, #57033, #47878 ) ;
#10737=SURFACE_SIDE_STYLE ('',( #51735 ) ) ;
#10741=CARTESIAN_POINT ( 'NONE',  ( 85.31399179591240056, -28.76387208470135093, 175.9376541799884421 ) ) ;
#10745=CARTESIAN_POINT ( 'NONE',  ( -89.59862634610074394, -60.15398014766234525, 51.74679006964829142 ) ) ;
#10750=CARTESIAN_POINT ( 'NONE',  ( -23.21907688075229714, -27.03733090009978213, -38.42007954425987037 ) ) ;
#10752=CARTESIAN_POINT ( 'NONE',  ( 41.55847581142891300, -60.00000000000000000, 54.44581446459392282 ) ) ;
#10753=CARTESIAN_POINT ( 'NONE',  ( 26.92113802654871435, -30.35670355970656686, 39.03432911242002490 ) ) ;
#10755=CARTESIAN_POINT ( 'NONE',  ( -37.01124464218769106, -36.50269617998545613, 46.22989763715360567 ) ) ;
#10769=CARTESIAN_POINT ( 'NONE',  ( 12.77004905764128928, -47.40885985275529180, -34.44498021351899553 ) ) ;
#10778=CARTESIAN_POINT ( 'NONE',  ( -93.65395957099387658, -59.99999999999999289, 38.40458741383176289 ) ) ;
#10785=CARTESIAN_POINT ( 'NONE',  ( -83.05624746893637678, -42.97990360462496540, 175.6772798865610525 ) ) ;
#10786=ORIENTED_EDGE ( 'NONE', *, *, #7708, .T. ) ;
#10798=CARTESIAN_POINT ( 'NONE',  ( -111.7589076751911392, -57.67119524614439285, 141.4413276519820784 ) ) ;
#10801=( GEOMETRIC_REPRESENTATION_CONTEXT ( 3 ) GLOBAL_UNCERTAINTY_ASSIGNED_CONTEXT ( ( #51332 ) ) GLOBAL_UNIT_ASSIGNED_CONTEXT ( ( #68050, #84771, #76664 ) ) REPRESENTATION_CONTEXT ( 'NONE', 'WORKASPACE' ) );
#10803=FILL_AREA_STYLE_COLOUR ( '', #35603 ) ;
#10805=CARTESIAN_POINT ( 'NONE',  ( 108.9225596800844897, -59.99999999999995737, 119.6931403564588123 ) ) ;
#10806=CARTESIAN_POINT ( 'NONE',  ( -77.40171858393368609, -14.21045842199445630, 153.6868182409262431 ) ) ;
#10807=CARTESIAN_POINT ( 'NONE',  ( -57.84207542031359139, -46.44074207334602278, 69.91486170460251515 ) ) ;
#10811=CARTESIAN_POINT ( 'NONE',  ( -103.1567554067950141, -45.26542592305720802, 184.6143969872866819 ) ) ;
#10816=CARTESIAN_POINT ( 'NONE',  ( -54.47032963692922891, -60.00000000000001421, 83.72682086598487672 ) ) ;
#10821=CARTESIAN_POINT ( 'NONE',  ( 16.14659623658357290, 0.000000000000000000, -5.483224646668203306 ) ) ;
#10828=CARTESIAN_POINT ( 'NONE',  ( -29.96432046203353394, -56.86175435685562718, 36.18131803398338064 ) ) ;
#10829=CARTESIAN_POINT ( 'NONE',  ( 43.12828152119622160, -42.98012150843932488, 42.46846544478599839 ) ) ;
#10833=CARTESIAN_POINT ( 'NONE',  ( -90.57426512392396489, -38.51016351068651744, 200.7127688951560174 ) ) ;
#10837=CARTESIAN_POINT ( 'NONE',  ( 2.087952376091057438, -59.99999999999998579, 33.88964995960238014 ) ) ;
#10846=CARTESIAN_POINT ( 'NONE',  ( 106.6141358215111268, -59.99999999999999289, 197.5847826952339688 ) ) ;
#10854=CARTESIAN_POINT ( 'NONE',  ( -81.48499160583682510, -29.99999999999999289, -3.293153312921696330 ) ) ;
#10856=CARTESIAN_POINT ( 'NONE',  ( -74.02947286502273982, -38.32606267584065307, 160.4867843101843903 ) ) ;
#10866=CARTESIAN_POINT ( 'NONE',  ( 83.92759608957032924, -29.05489278753509552, 161.8030344486882086 ) ) ;
#10883=FACE_BOUND ( 'NONE', #25900, .T. ) ;
#10886=CARTESIAN_POINT ( 'NONE',  ( 87.22190787708925086, -35.38180814089842841, 188.6303834557791390 ) ) ;
#10905=CARTESIAN_POINT ( 'NONE',  ( -106.1836608158888424, -60.00000000000001421, 198.0778789678093972 ) ) ;
#10911=CARTESIAN_POINT ( 'NONE',  ( -85.34260332515654568, -32.20242061357984653, 180.0776980316103391 ) ) ;
#10919=CARTESIAN_POINT ( 'NONE',  ( -83.85874690879670368, -45.26861737670255792, 5.011569712850605818 ) ) ;
#10925=CARTESIAN_POINT ( 'NONE',  ( 71.69540001792421435, -59.99999999999999289, 172.8810247122642352 ) ) ;
#10927=CARTESIAN_POINT ( 'NONE',  ( -86.74711523299461646, -14.21045842199446518, 20.03206905870895227 ) ) ;
#10928=CARTESIAN_POINT ( 'NONE',  ( -71.96658176269305329, -25.59195321872661211, 100.0548059226765787 ) ) ;
#10930=CARTESIAN_POINT ( 'NONE',  ( 104.4175052224803864, -30.00000000000007105, 196.2185630211469629 ) ) ;
#10932=CARTESIAN_POINT ( 'NONE',  ( 83.42010501496858410, -57.67103833101577948, -28.15582197385028707 ) ) ;
#10943=CARTESIAN_POINT ( 'NONE',  ( -37.96692578069663426, -60.00000000000488853, 53.22380867697400220 ) ) ;
#10955=CIRCLE ( 'NONE', #93598, 74.46152422706630603 ) ;
#10960=CARTESIAN_POINT ( 'NONE',  ( 31.76254636305852941, -36.01904366976002336, 33.16591156249626948 ) ) ;
#10961=CARTESIAN_POINT ( 'NONE',  ( -3.301606509414613644, -4.285714285714286476, 25.22241582816893413 ) ) ;
#10976=CARTESIAN_POINT ( 'NONE',  ( 92.35555844375753054, -59.99999999999999289, 0.7610974540291322032 ) ) ;
#10977=B_SPLINE_CURVE_WITH_KNOTS ( 'NONE', 3,
 ( #8246, #71385, #104285, #105878 ),
 .UNSPECIFIED., .F., .F.,
 ( 4, 4 ),
 ( 0.000000000000000000, 0.005000000000000029594 ),
 .UNSPECIFIED. ) ;
#10985=CARTESIAN_POINT ( 'NONE',  ( -98.51253199265957505, -29.99999999997342570, 199.5684000351004954 ) ) ;
#10991=CARTESIAN_POINT ( 'NONE',  ( 84.79553490237442759, -52.74953656108841216, -13.56258598970848972 ) ) ;
#11004=CARTESIAN_POINT ( 'NONE',  ( 74.87613309056551714, -53.37519123465959581, 130.5581752795035300 ) ) ;
#11010=CARTESIAN_POINT ( 'NONE',  ( -72.09688937032439071, -57.67332965070641393, 173.0313604384042776 ) ) ;
#11014=CARTESIAN_POINT ( 'NONE',  ( 103.9524479304479883, -45.28272538064109654, 177.1755535782787661 ) ) ;
#11020=CARTESIAN_POINT ( 'NONE',  ( -51.39591267744368253, -29.90029742506343169, 48.99010193482668996 ) ) ;
#11025=VECTOR ( 'NONE', #9562, 1000.000000000000000 ) ;
#11027=EDGE_LOOP ( 'NONE', ( #5057, #40923, #103190, #63088 ) ) ;
#11032=CARTESIAN_POINT ( 'NONE',  ( -85.52168577127288529, -30.00000000000000711, 175.0049642106293390 ) ) ;
#11037=CARTESIAN_POINT ( 'NONE',  ( 82.19213530885137686, -57.52430221361731810, 200.6401692809732538 ) ) ;
#11040=CARTESIAN_POINT ( 'NONE',  ( 56.66881868820166090, -36.84070694962797177, -34.92016498303262750 ) ) ;
#11043=CARTESIAN_POINT ( 'NONE',  ( -42.91031540250999399, -60.00000000000000711, 56.70723876392563056 ) ) ;
#11045=CARTESIAN_POINT ( 'NONE',  ( -86.39907952452841755, -17.11962503844113215, 182.3896902915995497 ) ) ;
#11048=CARTESIAN_POINT ( 'NONE',  ( -5.086419386595018466, -42.95753334118048627, 31.03917363720831091 ) ) ;
#11061=CARTESIAN_POINT ( 'NONE',  ( 91.50784380495012726, -29.99999999999993960, 42.72614900145088512 ) ) ;
#11062=CARTESIAN_POINT ( 'NONE',  ( -79.70987173175713281, -49.90920779543258590, 156.1999154600009092 ) ) ;
#11066=CARTESIAN_POINT ( 'NONE',  ( 34.00423421181317707, -57.69387838581924655, 48.14221580456336369 ) ) ;
#11084=CARTESIAN_POINT ( 'NONE',  ( -71.80342408229677176, -30.00000000000000000, -19.71767938363507966 ) ) ;
#11085=CARTESIAN_POINT ( 'NONE',  ( -106.7759996721837297, -60.00000000000014211, 200.9056163170290858 ) ) ;
#11086=CARTESIAN_POINT ( 'NONE',  ( 23.90148031990576882, -46.43417030711851368, 32.71422033971168730 ) ) ;
#11089=CARTESIAN_POINT ( 'NONE',  ( -34.39935170888136895, -56.83658484021449908, 38.30124131949656174 ) ) ;
#11092=CARTESIAN_POINT ( 'NONE',  ( -12.64023069600375138, -4.285714285714295357, 21.88880945939638423 ) ) ;
#11101=CARTESIAN_POINT ( 'NONE',  ( 98.18183449922635475, -29.99999999999996447, 190.3207026146189946 ) ) ;
#11102=CARTESIAN_POINT ( 'NONE',  ( 80.00000000000000000, -60.00000000000000000, -23.09707704303352926 ) ) ;
#11106=CARTESIAN_POINT ( 'NONE',  ( 80.76909324667138890, -30.00000000000000000, 10.58948054053466770 ) ) ;
#11124=CARTESIAN_POINT ( 'NONE',  ( 71.10593052259025626, -38.32839063090802512, 140.6717657492907279 ) ) ;
#11147=CARTESIAN_POINT ( 'NONE',  ( 85.38455353301951334, -46.55565056629794896, 188.3801272255345793 ) ) ;
#11157=CARTESIAN_POINT ( 'NONE',  ( -86.43767908690688273, -29.99999999999999645, 66.98128119464180941 ) ) ;
#11160=CARTESIAN_POINT ( 'NONE',  ( 34.42460263732258596, -57.69442024241028832, 48.56685808796169823 ) ) ;
#11165=CARTESIAN_POINT ( 'NONE',  ( -44.65110393089528884, -36.78960268062586181, 42.54015205027794622 ) ) ;
#11171=CARTESIAN_POINT ( 'NONE',  ( 21.71031025268755243, -19.05264385521112658, -33.48785545119387308 ) ) ;
#11172=CARTESIAN_POINT ( 'NONE',  ( -26.85002416475204257, -42.96004896817819230, 32.78313945162506116 ) ) ;
#11175=CARTESIAN_POINT ( 'NONE',  ( -20.86068844919981302, -22.07412597659780218, 28.15033270248965991 ) ) ;
#11188=CARTESIAN_POINT ( 'NONE',  ( 102.2803054478323190, -45.28266389599684771, 188.3718694929765718 ) ) ;
#11204=CARTESIAN_POINT ( 'NONE',  ( -94.29220476078621971, -59.99999999999877076, -14.61292367681898341 ) ) ;
#11208=CARTESIAN_POINT ( 'NONE',  ( -94.69971540129887444, -59.99999999999987921, 1.030331952319396782 ) ) ;
#11211=CARTESIAN_POINT ( 'NONE',  ( -48.92667392005618154, -18.75201781075177010, 42.51917512051642944 ) ) ;
#11226=CARTESIAN_POINT ( 'NONE',  ( 87.28426567074583886, -30.00000000000508393, -18.21208458236663219 ) ) ;
#11233=CARTESIAN_POINT ( 'NONE',  ( 87.80209714494544926, -29.99999999999999289, 186.2705117335520697 ) ) ;
#11238=CARTESIAN_POINT ( 'NONE',  ( 54.92320801914589623, -25.62319343846946040, 54.64829759656625896 ) ) ;
#11242=CARTESIAN_POINT ( 'NONE',  ( -84.96323215186174593, -38.35906192739592058, -22.88021158659245913 ) ) ;
#11244=CARTESIAN_POINT ( 'NONE',  ( 108.5962463409214109, -38.35700097774115847, 191.3600774737103336 ) ) ;
#11246=CARTESIAN_POINT ( 'NONE',  ( 84.98339600688585449, -52.71227180090472331, 17.49894070180983618 ) ) ;
#11257=DIRECTION ( 'NONE',  ( -0.000000000000000000, -1.000000000000000000, -0.000000000000000000 ) ) ;
#11264=CARTESIAN_POINT ( 'NONE',  ( 8.208016662565434274, -13.37663391665104662, 31.98074858385048458 ) ) ;
#11268=CARTESIAN_POINT ( 'NONE',  ( 86.37194580826782442, -18.00985568670380843, 173.0435977549529696 ) ) ;
#11272=CARTESIAN_POINT ( 'NONE',  ( -88.73957585412472326, -45.26530870161231945, 62.97202553129596936 ) ) ;
#11276=CARTESIAN_POINT ( 'NONE',  ( -27.77384242259211433, -28.75021021836514734, -38.27450564851195480 ) ) ;
#11280=CARTESIAN_POINT ( 'NONE',  ( 36.39487064310255704, -59.99999999999998579, 47.74500844687908341 ) ) ;
#11282=CARTESIAN_POINT ( 'NONE',  ( 19.19339060673821251, -16.77195851612492206, 31.49183225866399738 ) ) ;
#11283=CARTESIAN_POINT ( 'NONE',  ( -43.25681043230515144, -38.30618596757071970, 54.80884264012910734 ) ) ;
#11303=CARTESIAN_POINT ( 'NONE',  ( -15.77836386018752890, -34.58954351035645658, -32.12809626525399409 ) ) ;
#11311=CARTESIAN_POINT ( 'NONE',  ( -91.97475618974988265, -60.00000000000000711, 6.756679468872493821 ) ) ;
#11318=CARTESIAN_POINT ( 'NONE',  ( -80.31716401001155248, -60.40697784079697641, 178.0905699403173514 ) ) ;
#11328=CARTESIAN_POINT ( 'NONE',  ( -55.77313467663169888, -57.67115539668835567, -38.70230501811910528 ) ) ;
#11333=CARTESIAN_POINT ( 'NONE',  ( -97.24366422982762970, -45.35372475475530507, 193.9806419842749676 ) ) ;
#11334=CARTESIAN_POINT ( 'NONE',  ( 92.59918368926680898, -29.99999999999998224, 50.96418643717338881 ) ) ;
#11336=CARTESIAN_POINT ( 'NONE',  ( -93.93757927471676794, -14.21045842199439946, 198.1409199811383246 ) ) ;
#11337=CARTESIAN_POINT ( 'NONE',  ( -61.73170311023775270, -18.64112613040916244, 66.86421780239220425 ) ) ;
#11340=CARTESIAN_POINT ( 'NONE',  ( -100.7907627686642655, -37.81985441028579942, 188.8871514420389701 ) ) ;
#11354=CARTESIAN_POINT ( 'NONE',  ( 83.13703396460537931, -45.33804159704407510, -14.25699536724285110 ) ) ;
#11362=CARTESIAN_POINT ( 'NONE',  ( -32.12776895466944183, -42.96425948997189437, 34.59058220734644351 ) ) ;
#11364=CARTESIAN_POINT ( 'NONE',  ( 45.55829705881837555, -42.98293676978153144, 45.30720637935260697 ) ) ;
#11367=CARTESIAN_POINT ( 'NONE',  ( -86.18829832611947950, -38.63105478832063966, 199.1571653378964584 ) ) ;
#11372=CARTESIAN_POINT ( 'NONE',  ( 83.88447113947664491, -60.00000000000000000, 191.6821499555289847 ) ) ;
#11381=CARTESIAN_POINT ( 'NONE',  ( 112.1264442912419241, -59.99999999999999289, 177.3897674384393781 ) ) ;
#11386=CARTESIAN_POINT ( 'NONE',  ( -95.32476753328225527, -30.00000000000000000, 119.8948401030209965 ) ) ;
#11388=CARTESIAN_POINT ( 'NONE',  ( -76.19933201318396243, -38.38804777193976037, 180.0097251488151358 ) ) ;
#11401=CARTESIAN_POINT ( 'NONE',  ( 84.26967318104641436, -32.46622938755235310, 170.8684416685377698 ) ) ;
#11404=B_SPLINE_CURVE_WITH_KNOTS ( 'NONE', 3,
 ( #38123, #103357, #46180, #87707, #5707, #29504, #71496, #104396, #95269, #21398, #62901, #30545, #96338, #55307, #39688, #16449, #49877, #32129, #8884, #49336, #25104, #73070, #56894, #65008, #40725, #15390, #82782, #82242, #6769, #89295, #105467, #41789, #41259, #90344, #74146, #8357, #56359, #48276, #230, #73612, #15925, #33194, #89821, #17000, #72564, #81177, #74672, #66066, #24054, #24580, #7288, #55819, #98943, #105979, #48802, #40194, #31607, #57963 ),
 .UNSPECIFIED., .F., .F.,
 ( 4, 2, 2, 2, 2, 2, 2, 2, 2, 2, 2, 2, 2, 2, 2, 2, 2, 2, 2, 2, 2, 2, 2, 2, 2, 2, 2, 2, 4 ),
 ( 0.3785283831463345794, 0.3800322516953381635, 0.3815361202443417477, 0.3845438573423488049, 0.3875515944403558621, 0.3905593315383629749, 0.3965748057343771449, 0.4025902799303912594, 0.4146212283224195994, 0.4266521767144478838, 0.4386831251064762238, 0.4507140734985045638, 0.4747759702825611328, 0.4868069186745894728, 0.4988378670666178127, 0.5048533412626319272, 0.5108688154586461527, 0.5168842896546603782, 0.5228997638506744927, 0.5259075009486815500, 0.5289152380466886072, 0.5349307122427028327, 0.5379384493407098899, 0.5409461864387169472, 0.5469616606347311727, 0.5529771348307452872, 0.5589926090267594017, 0.5650080832227735161, 0.5710235574187877416 ),
 .UNSPECIFIED. ) ;
#11410=CARTESIAN_POINT ( 'NONE',  ( -89.99999999999997158, 500000.0000000000582, 196.0238439516549818 ) ) ;
#11415=CARTESIAN_POINT ( 'NONE',  ( -80.63290903287661138, -30.00000000000000711, -12.77866334089981670 ) ) ;
#11417=CARTESIAN_POINT ( 'NONE',  ( 86.62891540500523035, -16.99681948805599774, 185.2243898127639739 ) ) ;
#11441=CARTESIAN_POINT ( 'NONE',  ( -98.88275070081830620, -60.00000000000000711, 202.1696466176894660 ) ) ;
#11450=CARTESIAN_POINT ( 'NONE',  ( -82.85955728807176968, -60.89795309201070950, 190.2906973079219881 ) ) ;
#11456=CARTESIAN_POINT ( 'NONE',  ( -86.60779780715820664, -60.14586139666025133, 0.8348040731936827719 ) ) ;
#11462=CARTESIAN_POINT ( 'NONE',  ( 69.35339668739648289, -14.21045842199427511, 113.5888189438209537 ) ) ;
#11464=CARTESIAN_POINT ( 'NONE',  ( -94.21206122632280255, -59.99999999999995737, 9.571777650087724965 ) ) ;
#11465=CARTESIAN_POINT ( 'NONE',  ( -68.52812349397821379, -39.48763755164299027, 97.13502983046556949 ) ) ;
#11467=CARTESIAN_POINT ( 'NONE',  ( 101.7112553140276390, -14.21045842199441367, 195.4619641463733615 ) ) ;
#11468=CARTESIAN_POINT ( 'NONE',  ( 32.79512188131152328, -59.99999999999019451, 47.57302644083591048 ) ) ;
#11479=CARTESIAN_POINT ( 'NONE',  ( -91.84069786539126312, -59.99999999999998579, 13.61882742409930458 ) ) ;
#11485=CARTESIAN_POINT ( 'NONE',  ( 20.05453516056601515, -4.285714285714294469, -15.38541618194246752 ) ) ;
#11493=CARTESIAN_POINT ( 'NONE',  ( 32.37148614391195167, -36.02175558211217066, 33.41981937705683947 ) ) ;
#11494=CARTESIAN_POINT ( 'NONE',  ( 25.22241582816893413, -4.285714285714286476, -3.301606509414618973 ) ) ;
#11507=CARTESIAN_POINT ( 'NONE',  ( 91.87144242711445941, -60.00000000000000711, 10.36148848589531646 ) ) ;
#11514=CARTESIAN_POINT ( 'NONE',  ( -106.1473986865280352, -29.99999999999119282, 193.5445986010597608 ) ) ;
#11521=CARTESIAN_POINT ( 'NONE',  ( 82.37929189246122519, -37.80917422459863531, -12.96937234471123190 ) ) ;
#11536=CARTESIAN_POINT ( 'NONE',  ( 75.97406738546011695, -29.07565650354853659, 117.1859408371087881 ) ) ;
#11542=CARTESIAN_POINT ( 'NONE',  ( -90.87004379432312362, -57.61277171722555579, 204.1615020926832358 ) ) ;
#11547=CARTESIAN_POINT ( 'NONE',  ( 103.9399051704855736, -45.28278063994613234, 168.0512949665413771 ) ) ;
#11563=CARTESIAN_POINT ( 'NONE',  ( 45.32577667521739784, -27.72066794804566570, -35.73301877889856826 ) ) ;
#11564=CARTESIAN_POINT ( 'NONE',  ( -85.41469452698387954, -30.00000000000000355, 174.1069072483980165 ) ) ;
#11569=CARTESIAN_POINT ( 'NONE',  ( 77.44455754849047935, -57.51855352125810583, 195.7701994778959431 ) ) ;
#11573=CARTESIAN_POINT ( 'NONE',  ( 32.25685646263797679, -30.38137028985621413, -38.05272615982493534 ) ) ;
#11576=CARTESIAN_POINT ( 'NONE',  ( -72.00682906772283332, -60.00000000000000000, 154.3286074057541555 ) ) ;
#11581=CARTESIAN_POINT ( 'NONE',  ( -86.54352349054052240, -24.44773404303954578, 184.2160000694978237 ) ) ;
#11584=CARTESIAN_POINT ( 'NONE',  ( -0.9846993451217399551, -18.58623111607190026, 26.98735514561435522 ) ) ;
#11588=EDGE_LOOP ( 'NONE', ( #84877, #67715, #48142, #58819, #57644, #80225 ) ) ;
#11598=CARTESIAN_POINT ( 'NONE',  ( 89.52590460267296635, -30.00000000000006395, 22.04891038916446888 ) ) ;
#11599=CARTESIAN_POINT ( 'NONE',  ( -79.56974465040984512, -53.38012466183634075, 159.7390108954374455 ) ) ;
#11604=PRESENTATION_STYLE_ASSIGNMENT (( #45071 ) ) ;
#11624=CARTESIAN_POINT ( 'NONE',  ( 89.42130242191619516, -60.00000000000001421, -19.83448431725998518 ) ) ;
#11625=CARTESIAN_POINT ( 'NONE',  ( -60.31416392689769879, -59.99999999999997158, 109.8312514449790456 ) ) ;
#11626=CARTESIAN_POINT ( 'NONE',  ( 23.57173127243913413, -35.99637045962803228, 30.88673654114889544 ) ) ;
#11629=CARTESIAN_POINT ( 'NONE',  ( -36.95781401624343943, -60.28554291635620643, 40.61646249653143315 ) ) ;
#11642=CARTESIAN_POINT ( 'NONE',  ( 91.28451791618600453, -29.99999999999999289, 190.6136022142257502 ) ) ;
#11646=CARTESIAN_POINT ( 'NONE',  ( 80.98167351161701788, -29.99999999999999645, 4.326988430357994631 ) ) ;
#11683=CARTESIAN_POINT ( 'NONE',  ( 85.68274303767356059, -57.45247238031033987, 192.8335385098638994 ) ) ;
#11687=CARTESIAN_POINT ( 'NONE',  ( -7.233900571379007438, -15.80755961705004609, -35.01922747709534889 ) ) ;
#11691=CARTESIAN_POINT ( 'NONE',  ( -94.80346114260228774, -30.00000000000000711, 116.7752331319604906 ) ) ;
#11695=CARTESIAN_POINT ( 'NONE',  ( 1.463027203524020825, -57.67120326094947558, 41.61038173843766685 ) ) ;
#11701=CARTESIAN_POINT ( 'NONE',  ( -80.00000000000000000, 500000.0000000000582, -21.09707704303352926 ) ) ;
#11704=CARTESIAN_POINT ( 'NONE',  ( 32.85093540130672807, -22.62736283781948288, -31.69982964332332998 ) ) ;
#11706=CARTESIAN_POINT ( 'NONE',  ( -26.62684460577862566, -53.39439586559441153, 34.52290616355812602 ) ) ;
#11707=EDGE_CURVE ( 'NONE', #41900, #73170, #44007, .T. ) ;
#11710=CARTESIAN_POINT ( 'NONE',  ( -20.49954036836691174, -53.40101138645616885, 33.37275672667104232 ) ) ;
#11723=CARTESIAN_POINT ( 'NONE',  ( 100.3444285902703683, -37.84519586678835879, 189.9254009749505485 ) ) ;
#11737=CARTESIAN_POINT ( 'NONE',  ( -28.06723731321121562, -60.00000000007723600, -43.53660501072154432 ) ) ;
#11740=CARTESIAN_POINT ( 'NONE',  ( 14.20386879384134637, -60.00000000000001421, 39.75101514688974902 ) ) ;
#11745=CARTESIAN_POINT ( 'NONE',  ( -104.4271118349969498, -14.21045842199436926, 141.4138186051453090 ) ) ;
#11746=CARTESIAN_POINT ( 'NONE',  ( 4.005264604613198109, -29.02925082544549795, 28.72090773042863887 ) ) ;
#11750=CARTESIAN_POINT ( 'NONE',  ( -49.24971250091634545, -22.20977592223509234, 44.01979842293178535 ) ) ;
#11761=CARTESIAN_POINT ( 'NONE',  ( 88.65969019626136571, -29.99999999999445777, -15.66969482918002932 ) ) ;
#11766=CARTESIAN_POINT ( 'NONE',  ( 97.71307967711325659, -30.00000000000000000, 190.7721930600256712 ) ) ;
#11774=CARTESIAN_POINT ( 'NONE',  ( 54.95523992838832328, -46.43685162509488151, 63.01994253229578646 ) ) ;
#11779=CARTESIAN_POINT ( 'NONE',  ( -88.95530016575696663, -38.38408534947410544, -18.14653258153979820 ) ) ;
#11783=CARTESIAN_POINT ( 'NONE',  ( 107.4446830570735898, -38.36127121959084008, 194.0442666557358962 ) ) ;
#11785=CARTESIAN_POINT ( 'NONE',  ( 84.91903829920845226, -52.70721903688826160, 9.721747065421782352 ) ) ;
#11790=CARTESIAN_POINT ( 'NONE',  ( 2.083846472846741813E-15, -8.673617379884035472E-16, 17.01589776168603407 ) ) ;
#11803=CARTESIAN_POINT ( 'NONE',  ( 9.041496991692591578, -13.54857058825676575, 31.94122638330012265 ) ) ;
#11808=CARTESIAN_POINT ( 'NONE',  ( 84.42999968110919440, -42.97261461009923522, 183.7496894034296702 ) ) ;
#11813=CARTESIAN_POINT ( 'NONE',  ( -90.66722646538110553, -52.70996686316394886, 67.18204429113762899 ) ) ;
#11817=CARTESIAN_POINT ( 'NONE',  ( -0.8336975375668531640, -21.31741200790257906, -38.55284189565394115 ) ) ;
#11820=CARTESIAN_POINT ( 'NONE',  ( 17.06298066294603188, -60.00000000000001421, 39.92720215783332094 ) ) ;
#11821=CARTESIAN_POINT ( 'NONE',  ( 21.02493137415513758, -26.37324912420831780, 37.08244595263487042 ) ) ;
#11824=CARTESIAN_POINT ( 'NONE',  ( 49.49725558192223929, -29.58889863815145915, 45.82038523203005553 ) ) ;
#11827=CARTESIAN_POINT ( 'NONE',  ( -40.06514717946188853, -37.64732419053277823, 49.94544317564937330 ) ) ;
#11842=CARTESIAN_POINT ( 'NONE',  ( -22.39027729576407921, -47.40902575964246779, -33.77704283917025663 ) ) ;
#11845=CARTESIAN_POINT ( 'NONE',  ( -2.499999999999996003, -8.000000000000000000, 9.184850993605129949E-17 ) ) ;
#11853=CARTESIAN_POINT ( 'NONE',  ( -92.62866349064093185, -59.99999999999999289, 28.48677841314170323 ) ) ;
#11862=CARTESIAN_POINT ( 'NONE',  ( -80.64663750670202091, -56.90986277982133856, 175.6256103212931521 ) ) ;
#11865=CARTESIAN_POINT ( 'NONE',  ( -17.01594651245413203, -0.000000000000000000, 1.113195845621175684 ) ) ;
#11874=CARTESIAN_POINT ( 'NONE',  ( -93.89056551065039002, -57.67583025180931600, 8.072597750090290347 ) ) ;
#11881=CARTESIAN_POINT ( 'NONE',  ( 95.73610373016691710, -30.00000000000000355, 71.50072510963239836 ) ) ;
#11883=CARTESIAN_POINT ( 'NONE',  ( -88.35884389454342625, -14.21045842199434794, 197.0605769606054594 ) ) ;
#11884=CARTESIAN_POINT ( 'NONE',  ( -56.34788879306677956, -25.61643386706129988, 57.53393736018574600 ) ) ;
#11888=CARTESIAN_POINT ( 'NONE',  ( -104.0447889127541856, -45.26551436310554521, 172.6622363546740360 ) ) ;
#11906=CARTESIAN_POINT ( 'NONE',  ( -28.38553437247551514, -49.91375019981702366, 34.43038532363013360 ) ) ;
#11908=CARTESIAN_POINT ( 'NONE',  ( 48.40637997785970725, -36.06001625196908122, 47.15397699203993653 ) ) ;
#11913=CARTESIAN_POINT ( 'NONE',  ( -84.38815364029120758, -38.74013734265176367, 198.0659774401191271 ) ) ;
#11923=CARTESIAN_POINT ( 'NONE',  ( 103.8573764746737709, -60.00000000000000711, 200.0859602348770920 ) ) ;
#11928=CARTESIAN_POINT ( 'NONE',  ( -75.95768708191903329, -30.00000000000000000, -17.39747055666823172 ) ) ;
#11930=CARTESIAN_POINT ( 'NONE',  ( -84.11778948446114157, -38.75649915743333906, 197.8756380803732213 ) ) ;
#11942=CARTESIAN_POINT ( 'NONE',  ( 81.96385036426019610, -49.96436916644401549, 176.6379167989905739 ) ) ;
#11954=CARTESIAN_POINT ( 'NONE',  ( -74.08841422782842301, -29.99999999999999645, -18.54496149897586932 ) ) ;
#11956=LINE ( 'NONE', #14070, #54486 ) ;
#11983=CARTESIAN_POINT ( 'NONE',  ( -94.11619913633441570, -60.00000000000000711, 202.5510252723167355 ) ) ;
#11989=CARTESIAN_POINT ( 'NONE',  ( -86.38951205727846627, -17.91597735529700586, 174.1201453181821250 ) ) ;
#11994=CARTESIAN_POINT ( 'NONE',  ( -85.05563323462654068, -52.70063638665980932, 5.797456579206149208 ) ) ;
#12001=CARTESIAN_POINT ( 'NONE',  ( 63.58274112560721392, -14.21045842199431242, 93.96243211080884805 ) ) ;
#12004=CARTESIAN_POINT ( 'NONE',  ( -87.60281504538382080, -14.21045842199439946, -3.799590761493521374 ) ) ;
#12005=CARTESIAN_POINT ( 'NONE',  ( -64.92204483014883465, -36.00903953999379326, 84.15884882200457184 ) ) ;
#12007=CARTESIAN_POINT ( 'NONE',  ( 83.30384756245543088, -14.21045842199437992, 194.5080389997825137 ) ) ;
#12009=CARTESIAN_POINT ( 'NONE',  ( 75.77503827602937747, -57.67118947225861803, -32.31848336751978934 ) ) ;
#12020=CARTESIAN_POINT ( 'NONE',  ( -36.11448103554893407, -60.00000000000002132, -40.17722562108524187 ) ) ;
#12024=CARTESIAN_POINT ( 'NONE',  ( 11.17734400176826348, -4.285714285714295357, 22.67073868809949033 ) ) ;
#12036=CARTESIAN_POINT ( 'NONE',  ( 32.00609611073077332, -18.67737511809503204, 30.02820132365625483 ) ) ;
#12037=CARTESIAN_POINT ( 'NONE',  ( 25.22241582816893413, -4.285714285714286476, 3.301606509414615420 ) ) ;
#12049=CARTESIAN_POINT ( 'NONE',  ( 92.31046174747429234, -59.99999999999999289, 1.374785491484104005 ) ) ;
#12057=CARTESIAN_POINT ( 'NONE',  ( -99.88428596410730620, -29.99999999998460609, 199.1606248856587058 ) ) ;
#12063=CARTESIAN_POINT ( 'NONE',  ( 84.38025208974687530, -52.74135128307990072, -14.53858364661402547 ) ) ;
#12075=CARTESIAN_POINT ( 'NONE',  ( 80.62408886127033725, -18.68107705517183348, 129.0749382031092409 ) ) ;
#12080=CARTESIAN_POINT ( 'NONE',  ( -85.03051761340829273, -57.56200303720294897, 202.2882931814572487 ) ) ;
#12089=CARTESIAN_POINT ( 'NONE',  ( -48.03847873877180064, -29.24902813972587978, 43.67456182833235090 ) ) ;
#12102=CARTESIAN_POINT ( 'NONE',  ( 4.998341000544551882, -17.97620282888080112, -37.93689352612668131 ) ) ;
#12103=CARTESIAN_POINT ( 'NONE',  ( -62.52821090568615148, -30.00000000000000711, 73.42485873602892354 ) ) ;
#12109=CARTESIAN_POINT ( 'NONE',  ( 75.25576489772180366, -57.56749894965461323, 191.3623090674220180 ) ) ;
#12112=CARTESIAN_POINT ( 'NONE',  ( 57.89164812746757605, -37.03233184154265700, -34.65406527698851136 ) ) ;
#12115=CARTESIAN_POINT ( 'NONE',  ( -65.70695785853703796, -59.99999999999998579, 121.1804584992903528 ) ) ;
#12119=CARTESIAN_POINT ( 'NONE',  ( -83.91826887416667091, -61.04048265323336153, 192.1982429797399163 ) ) ;
#12122=CARTESIAN_POINT ( 'NONE',  ( -3.070984519260819834, -53.40251359550288157, 32.78485625322804253 ) ) ;
#12135=( NAMED_UNIT ( * ) SI_UNIT ( $, .STERADIAN. ) SOLID_ANGLE_UNIT ( ) );
#12137=CARTESIAN_POINT ( 'NONE',  ( 99.89428240326108721, -30.00000000000003908, 96.08155976150675315 ) ) ;
#12138=CARTESIAN_POINT ( 'NONE',  ( -81.17881172582528393, -39.50116433889217404, 153.9116840188365813 ) ) ;
#12142=CARTESIAN_POINT ( 'NONE',  ( 26.18764921593997030, -57.67624503786063883, 43.55245106248555231 ) ) ;
#12160=CARTESIAN_POINT ( 'NONE',  ( 63.27042206663746526, -60.00000000000000000, -34.75888330929602432 ) ) ;
#12161=CARTESIAN_POINT ( 'NONE',  ( -71.37516729659446924, -14.21045842199439946, 121.5232625957608974 ) ) ;
#12162=CARTESIAN_POINT ( 'NONE',  ( 27.33918801737314297, -25.57593558123391375, 29.89066338960705593 ) ) ;
#12164=CARTESIAN_POINT ( 'NONE',  ( -35.84365847796291860, -39.50733013384240877, 35.79938607260854155 ) ) ;
#12174=CARTESIAN_POINT ( 'NONE',  ( -76.00050994787578418, -38.37788238259345519, 178.3583240899461941 ) ) ;
#12176=CARTESIAN_POINT ( 'NONE',  ( 89.04598776754650657, -29.99999999999999289, 83.36196907162633352 ) ) ;
#12180=CARTESIAN_POINT ( 'NONE',  ( 80.71453622594903266, -30.00000000000000711, -12.60762180172875624 ) ) ;
#12182=EDGE_CURVE ( 'NONE', #95473, #24767, #79369, .T. ) ;
#12206=CARTESIAN_POINT ( 'NONE',  ( 64.78375808736633701, -22.10194954420784086, 76.63010471250390765 ) ) ;
#12220=CARTESIAN_POINT ( 'NONE',  ( 86.70382925515318107, -35.44956032792972422, 187.4678705349916470 ) ) ;
#12224=CARTESIAN_POINT ( 'NONE',  ( 75.12731958518588726, -57.67118848584987489, -32.59161320420232499 ) ) ;
#12228=CARTESIAN_POINT ( 'NONE',  ( -83.17155174494244818, -30.00000000000000000, 44.27485665655420632 ) ) ;
#12232=CARTESIAN_POINT ( 'NONE',  ( 0.002498436923358977966, -57.67120202537410734, 41.61186700447464659 ) ) ;
#12243=CARTESIAN_POINT ( 'NONE',  ( -87.37974545749381150, -46.42099736837836588, 191.3367129492426102 ) ) ;
#12249=CARTESIAN_POINT ( 'NONE',  ( -21.04607429833048471, -29.03556388439810121, 29.34454004103736580 ) ) ;
#12261=EDGE_CURVE ( 'NONE', #69966, #45998, #115, .T. ) ;
#12266=CARTESIAN_POINT ( 'NONE',  ( 102.3885618088003042, -52.72063632800296773, 191.3672504949884114 ) ) ;
#12280=CARTESIAN_POINT ( 'NONE',  ( -95.07610051239151971, -60.00000000000000000, -4.532845324902508466 ) ) ;
#12282=CARTESIAN_POINT ( 'NONE',  ( 31.95254591819974976, -59.99999999999998579, 44.12862274816207275 ) ) ;
#12285=CARTESIAN_POINT ( 'NONE',  ( -105.4253011914250067, -14.21045842199428222, 149.5333493894512458 ) ) ;
#12286=CARTESIAN_POINT ( 'NONE',  ( 5.156537703247399129, -56.87775452844108770, 33.35875848516817399 ) ) ;
#12288=CARTESIAN_POINT ( 'NONE',  ( -47.61298378469552972, -53.36243106413825643, 51.28367574756582314 ) ) ;
#12299=CARTESIAN_POINT ( 'NONE',  ( 76.53963492301289762, -29.99999999999329603, -26.83307303577876013 ) ) ;
#12304=CARTESIAN_POINT ( 'NONE',  ( 98.56603916130582377, -30.00000000000000355, 189.7319824347792405 ) ) ;
#12311=CARTESIAN_POINT ( 'NONE',  ( 54.48416669372233656, -56.84658666858351950, 66.24332653280961836 ) ) ;
#12316=CARTESIAN_POINT ( 'NONE',  ( -88.01924983139112157, -38.37074707933226847, -19.54877242889350342 ) ) ;
#12319=CARTESIAN_POINT ( 'NONE',  ( 101.3911668549956033, -38.45380319144855008, 199.9736433382965402 ) ) ;
#12321=CARTESIAN_POINT ( 'NONE',  ( 84.89893217423146154, -52.70949330645067477, 12.33567577723670006 ) ) ;
#12339=CARTESIAN_POINT ( 'NONE',  ( 31.24472784702464523, -24.80329577077787206, 39.51072433048258858 ) ) ;
#12343=CARTESIAN_POINT ( 'NONE',  ( 82.59652397065522678, -60.84044193784809806, 189.6660346993927817 ) ) ;
#12346=CARTESIAN_POINT ( 'NONE',  ( -84.44653569564452766, -56.38255921961517458, 190.8904429900520370 ) ) ;
#12348=CARTESIAN_POINT ( 'NONE',  ( -95.06236187663560600, -60.15485587419004787, 86.14958005658115781 ) ) ;
#12355=CARTESIAN_POINT ( 'NONE',  ( 7.822060438254271553, -19.39240910821929376, 35.22573232888181138 ) ) ;
#12357=CARTESIAN_POINT ( 'NONE',  ( 40.55314487144148217, -26.56230035094428743, 36.32082278398921460 ) ) ;
#12359=CARTESIAN_POINT ( 'NONE',  ( -35.99893469198357110, -36.03401585327518575, 45.16313413558417977 ) ) ;
#12374=CARTESIAN_POINT ( 'NONE',  ( 7.961997598232706252, -47.40891911902998856, -34.64489477109410132 ) ) ;
#12381=CARTESIAN_POINT ( 'NONE',  ( -92.03800156008944100, -60.00000000000000000, 19.26534363413594164 ) ) ;
#12388=CARTESIAN_POINT ( 'NONE',  ( -83.04203994682778500, -39.48694556830105284, 170.2747023245005096 ) ) ;
#12399=CARTESIAN_POINT ( 'NONE',  ( -89.88826151057727998, -57.66708741322880627, -22.42023280972025390 ) ) ;
#12406=CARTESIAN_POINT ( 'NONE',  ( 86.47489896066092285, -14.21045842199428932, -14.67047700064687987 ) ) ;
#12408=CARTESIAN_POINT ( 'NONE',  ( -75.56794833712217496, -14.21045842199431597, 141.5492349273399952 ) ) ;
#12409=CARTESIAN_POINT ( 'NONE',  ( -55.71125761005164634, -18.68150336790142418, 53.46817653840955131 ) ) ;
#12413=CARTESIAN_POINT ( 'NONE',  ( -98.82905336773379190, -37.76367048180233610, 192.0201691225735772 ) ) ;
#12414=CARTESIAN_POINT ( 'NONE',  ( 102.7253656032815030, -38.00000000000000000, 177.4132030967784033 ) ) ;
#12424=CARTESIAN_POINT ( 'NONE',  ( 62.38085580266044872, -29.99999999999999289, 73.03293077709649594 ) ) ;
#12430=CARTESIAN_POINT ( 'NONE',  ( -29.47180296636225449, -60.33975193709323293, 36.60485071960074066 ) ) ;
#12432=CARTESIAN_POINT ( 'NONE',  ( 48.47115896583378003, -29.13930102312053094, 45.10802347286871594 ) ) ;
#12438=CARTESIAN_POINT ( 'NONE',  ( -93.57730620611623351, -38.49396005077335303, 201.1642509031951249 ) ) ;
#12440=CARTESIAN_POINT ( 'NONE',  ( 85.52540355899250812, -38.36029101926790474, -22.36776190553080923 ) ) ;
#12441=CARTESIAN_POINT ( 'NONE',  ( 83.30308154782368035, -60.00000000000006395, 190.8048519435806440 ) ) ;
#12449=CARTESIAN_POINT ( 'NONE',  ( 110.9799143117941043, -60.00000000000001421, 187.5157448101569173 ) ) ;
#12452=EDGE_LOOP ( 'NONE', ( #74843, #76469, #42771, #85446 ) ) ;
#12456=CARTESIAN_POINT ( 'NONE',  ( -72.55053978524345837, -38.32605109717405867, 149.3030407648667222 ) ) ;
#12465=CARTESIAN_POINT ( 'NONE',  ( 81.41541248120216778, -53.44831681439456617, 177.1204070320672201 ) ) ;
#12502=ORIENTED_EDGE ( 'NONE', *, *, #86694, .T. ) ;
#12508=CARTESIAN_POINT ( 'NONE',  ( -112.0710918845811364, -59.99999999999999289, 178.4928572454104483 ) ) ;
#12514=CARTESIAN_POINT ( 'NONE',  ( -83.34697557531410439, -46.52569824882559857, 181.7021836014866949 ) ) ;
#12519=CARTESIAN_POINT ( 'NONE',  ( -86.98955879380979184, -60.18195689495087208, -5.047257192535347770 ) ) ;
#12523=LINE ( 'NONE', #70252, #66598 ) ;
#12525=CARTESIAN_POINT ( 'NONE',  ( 86.31905819422470927, -30.00000000000006750, 198.0863690661441296 ) ) ;
#12527=CARTESIAN_POINT ( 'NONE',  ( -86.47621369144106040, -14.21045842199425735, -14.66750133381012589 ) ) ;
#12528=CARTESIAN_POINT ( 'NONE',  ( -66.02922395999594585, -18.62684786674785187, 78.34317924958739354 ) ) ;
#12530=CARTESIAN_POINT ( 'NONE',  ( 91.09720049356627669, -14.21045842199416143, 197.8400994950010272 ) ) ;
#12532=CARTESIAN_POINT ( 'NONE',  ( 71.72808885978980697, -60.00000000001963940, 173.2180474971540605 ) ) ;
#12544=CARTESIAN_POINT ( 'NONE',  ( -13.94972454548224405, -60.00000000000000000, -42.23494151491821924 ) ) ;
#12561=CARTESIAN_POINT ( 'NONE',  ( 32.97681988584721324, -36.02474376031975822, 33.68276379229053674 ) ) ;
#12574=CARTESIAN_POINT ( 'NONE',  ( 91.89176552790895869, -59.99999999999999289, 9.187668761806360607 ) ) ;
#12583=CARTESIAN_POINT ( 'NONE',  ( -103.8379607931385777, -30.00000000000037303, 196.7236767739510128 ) ) ;
#12597=CARTESIAN_POINT ( 'NONE',  ( 81.09557302793662359, -22.15391159154729195, 134.4882534712255904 ) ) ;
#12602=CARTESIAN_POINT ( 'NONE',  ( -80.15954706948889452, -57.50857130571672826, 199.0044224626226139 ) ) ;
#12624=CARTESIAN_POINT ( 'NONE',  ( -65.25607705482885024, -29.77640809674063860, -22.97023434858075319 ) ) ;
#12625=CARTESIAN_POINT ( 'NONE',  ( -79.77046542224586290, -30.00000000000000355, 132.9793268207660333 ) ) ;
#12632=CARTESIAN_POINT ( 'NONE',  ( 77.76963947670292043, -57.51447515414862011, 196.2475803584244147 ) ) ;
#12633=CARTESIAN_POINT ( 'NONE',  ( 69.47333816740184886, -60.22837470586443231, -26.63215147159283802 ) ) ;
#12637=CARTESIAN_POINT ( 'NONE',  ( -52.62616307540574212, -60.00000000000000711, 78.63067357585181583 ) ) ;
#12642=CARTESIAN_POINT ( 'NONE',  ( -85.09823223632439237, -46.56888121716310280, 187.7722408975631652 ) ) ;
#12660=CARTESIAN_POINT ( 'NONE',  ( 22.03900363279368690, -4.285714285714963268, -12.70248734011530622 ) ) ;
#12662=CARTESIAN_POINT ( 'NONE',  ( 90.16383085397569630, -14.21045842199434084, 52.56522323202336366 ) ) ;
#12663=CARTESIAN_POINT ( 'NONE',  ( -77.52747395753381454, -56.84636302205639424, 148.6058317181106077 ) ) ;
#12666=PRESENTATION_STYLE_ASSIGNMENT (( #35942 ) ) ;
#12668=CARTESIAN_POINT ( 'NONE',  ( 18.26666949864142353, -57.67159702739868266, 41.99773675405111106 ) ) ;
#12687=CARTESIAN_POINT ( 'NONE',  ( -58.28906562901213562, -14.21045842199421294, 78.48115787639689245 ) ) ;
#12688=CARTESIAN_POINT ( 'NONE',  ( 26.36601463560733194, -46.43337520415909125, 33.26297091638029713 ) ) ;
#12694=CARTESIAN_POINT ( 'NONE',  ( -1.650803255657547375, -4.285714285714296246, -25.22241582816893057 ) ) ;
#12702=CARTESIAN_POINT ( 'NONE',  ( 98.43072231738531741, -29.99999999999995737, 140.5709701892116072 ) ) ;
#12707=CARTESIAN_POINT ( 'NONE',  ( 81.57847679930965512, -29.99999999999999645, -5.537912221079761999 ) ) ;
#12732=CARTESIAN_POINT ( 'NONE',  ( 63.70598834999947968, -49.91021569056980667, 87.81644791561008390 ) ) ;
#12736=CARTESIAN_POINT ( 'NONE',  ( -57.73274652580165878, -37.01956164141905958, -34.70034953516653786 ) ) ;
#12750=CARTESIAN_POINT ( 'NONE',  ( 86.49757777737477227, -42.81999918254669524, 189.1461807675101738 ) ) ;
#12757=CARTESIAN_POINT ( 'NONE',  ( -97.94054855731607745, -30.00000000000000355, 137.0914856574075884 ) ) ;
#12759=COLOUR_RGB ( '', 0.31764706, 0.68627451, 0.89019608) ;
#12760=CARTESIAN_POINT ( 'NONE',  ( 28.06569167955347055, -57.67949617772409709, 44.31129476918351884 ) ) ;
#12776=CARTESIAN_POINT ( 'NONE',  ( -18.71324380705060975, -25.55240577479218445, 28.53076995190656362 ) ) ;
#12778=CARTESIAN_POINT ( 'NONE',  ( -86.14485785028760745, -59.99999999999995026, 15.73779263674076212 ) ) ;
#12789=CARTESIAN_POINT ( 'NONE',  ( 104.6932645544404750, -60.15174171467819519, 188.9584721480441658 ) ) ;
#12807=CARTESIAN_POINT ( 'NONE',  ( -94.62662591020489344, -60.00000000000486011, -13.08416834391727512 ) ) ;
#12809=CARTESIAN_POINT ( 'NONE',  ( 88.33048940779720226, -60.00000000001467271, -24.74029235082771194 ) ) ;
#12812=CARTESIAN_POINT ( 'NONE',  ( -107.3073691194147443, -59.99999999999994316, 109.8427349246714613 ) ) ;
#12813=CARTESIAN_POINT ( 'NONE',  ( 11.56881156677787814, -60.35887278456814187, 33.98181144888569349 ) ) ;
#12815=CARTESIAN_POINT ( 'NONE',  ( -48.33525847096109374, -42.98408013933313754, 49.20298293444408699 ) ) ;
#12823=CARTESIAN_POINT ( 'NONE',  ( 90.02033453618058445, -29.99999999997217159, -9.423705806685745756 ) ) ;
#12827=CARTESIAN_POINT ( 'NONE',  ( 97.98369069848891399, -30.00000000000000000, 190.5473186706665842 ) ) ;
#12834=CARTESIAN_POINT ( 'NONE',  ( 54.64156605188832572, -53.37664899715956324, 65.16901697101967272 ) ) ;
#12839=CARTESIAN_POINT ( 'NONE',  ( -81.87992184396165385, -38.35665926185938446, -25.31435275803445251 ) ) ;
#12842=CARTESIAN_POINT ( 'NONE',  ( 105.2162103339291264, -38.38992852922254428, 197.2646886752842761 ) ) ;
#12845=CARTESIAN_POINT ( 'NONE',  ( 83.67122112447796667, -45.28247169777900893, 12.12148471621375556 ) ) ;
#12864=CARTESIAN_POINT ( 'NONE',  ( 51.98481497594274714, -29.99999999999999645, 49.99891310834441782 ) ) ;
#12869=CARTESIAN_POINT ( 'NONE',  ( 85.62023018141502462, -28.60500254207639159, 178.8567084087247849 ) ) ;
#12875=CARTESIAN_POINT ( 'NONE',  ( -93.88781582325293584, -52.71009071215733854, 86.64102402054331264 ) ) ;
#12882=CARTESIAN_POINT ( 'NONE',  ( 10.82237006604675145, -20.57234134931101011, 35.45079542051080779 ) ) ;
#12884=CARTESIAN_POINT ( 'NONE',  ( 51.58436202480620381, -29.92082885799144876, 49.33144644358862507 ) ) ;
#12891=CARTESIAN_POINT ( 'NONE',  ( -87.09641169487616708, -38.00000000000000000, 60.23192446987157211 ) ) ;
#12896=CARTESIAN_POINT ( 'NONE',  ( 9.320906537292072969, -21.77036391677812688, -30.31143086060786374 ) ) ;
#12903=EDGE_CURVE ( 'NONE', #59296, #80603, #101741, .T. ) ;
#12907=CARTESIAN_POINT ( 'NONE',  ( -92.14734929965659660, -59.99999999999999289, 21.43942582026355836 ) ) ;
#12917=CARTESIAN_POINT ( 'NONE',  ( -80.43218294797944168, -60.42267903133028284, 179.0676953134927203 ) ) ;
#12920=CARTESIAN_POINT ( 'NONE',  ( -15.29468310206709347, -0.000000000000000000, 7.540179673766518320 ) ) ;
#12930=CARTESIAN_POINT ( 'NONE',  ( -93.85239982658497127, -57.67543968518839392, 9.450824874790988872 ) ) ;
#12936=CARTESIAN_POINT ( 'NONE',  ( 57.68379620845067279, -29.99999999999995026, -33.51799637603287607 ) ) ;
#12937=CARTESIAN_POINT ( 'NONE',  ( -52.32131825073019371, -14.21045842199420584, 63.24190059944674402 ) ) ;
#12938=CARTESIAN_POINT ( 'NONE',  ( -54.49468904511509493, -36.03252814681875549, 57.85336393633966168 ) ) ;
#12942=CARTESIAN_POINT ( 'NONE',  ( -102.0386490841828078, -52.71615882625160765, 192.0067383440280935 ) ) ;
#12946=CARTESIAN_POINT ( 'NONE',  ( -5.646069974130150548, -59.99999999999998579, 39.61802077795142907 ) ) ;
#12952=CARTESIAN_POINT ( 'NONE',  ( 62.36520093333108861, -30.00000000000001421, 72.99138914944688850 ) ) ;
#12955=ADVANCED_FACE ( 'NONE', ( #50125 ), #24818, .F. ) ;
#12957=CARTESIAN_POINT ( 'NONE',  ( -27.61222033232023776, -46.43752918860366208, 33.58974296575833307 ) ) ;
#12960=CARTESIAN_POINT ( 'NONE',  ( 47.68197102969904222, -42.98161286699893679, 48.22189115465704390 ) ) ;
#12964=CARTESIAN_POINT ( 'NONE',  ( -110.2894375318718829, -38.35608233796805422, 184.0685881230607492 ) ) ;
#12966=CARTESIAN_POINT ( 'NONE',  ( 90.65944472992794090, -38.34295313743801614, 8.876429703253217340 ) ) ;
#12974=CARTESIAN_POINT ( 'NONE',  ( 109.2852756154741201, -60.00000000000002132, 193.0479011121091730 ) ) ;
#12982=CARTESIAN_POINT ( 'NONE',  ( -106.1106007292416251, -38.37460074271928079, 196.2185828438378792 ) ) ;
#12995=CARTESIAN_POINT ( 'NONE',  ( 82.51382183231068268, -46.47490132111590810, 176.1494215204247951 ) ) ;
#13003=DIRECTION ( 'NONE',  ( 0.000000000000000000, -1.000000000000000000, 0.000000000000000000 ) ) ;
#13034=CARTESIAN_POINT ( 'NONE',  ( -106.1675901372213531, -59.99999999999999289, 198.0953892983058040 ) ) ;
#13035=DIRECTION ( 'NONE',  ( -0.000000000000000000, 0.000000000000000000, 1.000000000000000000 ) ) ;
#13039=CARTESIAN_POINT ( 'NONE',  ( -84.35187283706933670, -35.91723947740675271, 176.6996256281102546 ) ) ;
#13047=CARTESIAN_POINT ( 'NONE',  ( -86.42387036193130712, -60.14814614128767545, 21.61025827088693063 ) ) ;
#13052=CARTESIAN_POINT ( 'NONE',  ( 109.5593579388806091, -60.00000000000008527, 197.6560947019162597 ) ) ;
#13054=CARTESIAN_POINT ( 'NONE',  ( -105.2983529938406519, -30.00000000000006750, 128.8794261209098124 ) ) ;
#13055=CARTESIAN_POINT ( 'NONE',  ( -65.00259538333476428, -18.62595769467823814, 75.48159003049013904 ) ) ;
#13059=CARTESIAN_POINT ( 'NONE',  ( 81.98093513041146707, -59.99999999999619860, 201.2291763324874125 ) ) ;
#13071=CARTESIAN_POINT ( 'NONE',  ( -11.16652874660464789, -60.00000000000000000, -42.37729182859549582 ) ) ;
#13087=CARTESIAN_POINT ( 'NONE',  ( 37.34060288484600676, -46.42986010551973663, 38.17736329578391974 ) ) ;
#13088=CARTESIAN_POINT ( 'NONE',  ( -8.569529079651847070, -1.734723475976807094E-15, 14.86825985028331942 ) ) ;
#13102=CARTESIAN_POINT ( 'NONE',  ( 92.69363537619402393, -60.00000000000000711, -4.651207231870288616 ) ) ;
#13110=CARTESIAN_POINT ( 'NONE',  ( -54.99362396314259627, -30.00000000000000711, 55.63568590878308839 ) ) ;
#13125=CARTESIAN_POINT ( 'NONE',  ( 79.97645733512185018, -39.49688154037509236, 145.6660021679025760 ) ) ;
#13131=CARTESIAN_POINT ( 'NONE',  ( -76.58308308725453628, -57.53248158402972479, 194.3307878365576187 ) ) ;
#13141=CARTESIAN_POINT ( 'NONE',  ( -51.40127918372997584, -29.90090478647314498, 48.99973797973098044 ) ) ;
#13154=CARTESIAN_POINT ( 'NONE',  ( -3.265580259469881064, -17.82470403459646136, -37.95109814934059500 ) ) ;
#13155=CARTESIAN_POINT ( 'NONE',  ( -84.24772247247709345, -30.00000000000000711, 163.2342536007591320 ) ) ;
#13161=CARTESIAN_POINT ( 'NONE',  ( 84.69200348729471273, -57.55678680253502932, 202.1247301444829532 ) ) ;
#13162=CARTESIAN_POINT ( 'NONE',  ( 65.77516868540070050, -47.40891819904962290, -25.69697480624873620 ) ) ;
#13168=CARTESIAN_POINT ( 'NONE',  ( -50.53956664665770404, -60.00000000000000711, 73.16161570676207759 ) ) ;
#13173=CARTESIAN_POINT ( 'NONE',  ( -86.39152420209940431, -17.34348802733059713, 179.9401184627342332 ) ) ;
#13181=CARTESIAN_POINT ( 'NONE',  ( -83.96832662571230799, -52.72755687222642962, -15.30586875041439932 ) ) ;
#13187=CARTESIAN_POINT ( 'NONE',  ( 22.03900363279161567, -4.285714285712638016, 12.70248734011606828 ) ) ;
#13189=CARTESIAN_POINT ( 'NONE',  ( 86.84200744108139247, -14.21045842199445630, 3.673032677714961558 ) ) ;
#13190=CARTESIAN_POINT ( 'NONE',  ( -77.89482686549987989, -49.90756091378847970, 143.7070462317983583 ) ) ;
#13194=CARTESIAN_POINT ( 'NONE',  ( 78.03174936499274850, -57.51149409110730204, 196.6180056380835310 ) ) ;
#13196=UNCERTAINTY_MEASURE_WITH_UNIT (LENGTH_MEASURE( 1.000000000000000082E-05 ), #58303, 'distance_accuracy_value', 'NONE');
#13217=CARTESIAN_POINT ( 'NONE',  ( -73.11793949506163415, -30.00000000000001776, 143.8487384131749423 ) ) ;
#13218=CARTESIAN_POINT ( 'NONE',  ( 26.01855909204189743, -22.09186832850629045, 28.98036754413648808 ) ) ;
#13234=CARTESIAN_POINT ( 'NONE',  ( 90.21985533091218201, -30.00000000000004619, 190.0404579620991115 ) ) ;
#13238=CARTESIAN_POINT ( 'NONE',  ( 80.70865640423915011, -30.00000000000000355, -12.62041422021882475 ) ) ;
#13260=CARTESIAN_POINT ( 'NONE',  ( 63.44158566079609329, -32.53091779288278218, 78.14191095953113120 ) ) ;
#13269=CARTESIAN_POINT ( 'NONE',  ( -8.647636768531977935, -60.00000000000002842, -36.71923688686057119 ) ) ;
#13273=CARTESIAN_POINT ( 'NONE',  ( 86.20424334727701421, -57.42790586652574092, 193.3016074490970482 ) ) ;
#13278=CARTESIAN_POINT ( 'NONE',  ( 44.97663383827099182, -26.29691875582094340, -29.22557715210724893 ) ) ;
#13281=CARTESIAN_POINT ( 'NONE',  ( -100.6459466783282579, -30.00000000000000000, 181.8192848642643469 ) ) ;
#13284=CARTESIAN_POINT ( 'NONE',  ( 26.51134585607502103, -57.67681482525394898, 43.69224471368552543 ) ) ;
#13290=CYLINDRICAL_SURFACE ( 'NONE', #17017, 1.999999999999998224 ) ;
#13297=CARTESIAN_POINT ( 'NONE',  ( -87.29625452526420304, -42.75230380456551416, 190.3644472096953848 ) ) ;
#13302=CARTESIAN_POINT ( 'NONE',  ( -11.56863480372296848, -60.36581770793299739, 33.98298590360514027 ) ) ;
#13317=CARTESIAN_POINT ( 'NONE',  ( 48.47273764080328817, -37.70810654209444124, 47.74218356993235801 ) ) ;
#13331=CARTESIAN_POINT ( 'NONE',  ( -76.25153216073499607, -60.00000000000000711, 194.9697643434355427 ) ) ;
#13333=CARTESIAN_POINT ( 'NONE',  ( 90.43359995430249398, -59.99999999998527045, -22.43322211268118593 ) ) ;
#13336=CARTESIAN_POINT ( 'NONE',  ( -105.2983529938406519, -30.00000000000006750, 128.8794261209098124 ) ) ;
#13337=CARTESIAN_POINT ( 'NONE',  ( 8.082812510549141294, -29.02946823534357890, 28.72076172514474734 ) ) ;
#13341=CARTESIAN_POINT ( 'NONE',  ( -48.74031821977154522, -56.82868487743887442, 54.29775784473008571 ) ) ;
#13351=CARTESIAN_POINT ( 'NONE',  ( 101.4679014012201890, -30.00000000000100542, 198.4634389564624257 ) ) ;
#13355=CARTESIAN_POINT ( 'NONE',  ( 100.4793545649653908, -30.00000000000000711, 182.9758932259915127 ) ) ;
#13369=CARTESIAN_POINT ( 'NONE',  ( 94.03355356640217622, -38.49242504296974232, 201.1935302665664267 ) ) ;
#13371=CARTESIAN_POINT ( 'NONE',  ( 84.93372689366950112, -52.71121740197983030, 14.92205009592277243 ) ) ;
#13394=CARTESIAN_POINT ( 'NONE',  ( 5.095333818548398064, -15.20659882116594197, 34.52546233959761679 ) ) ;
#13397=CARTESIAN_POINT ( 'NONE',  ( 83.55767777431796617, -53.73583656280342069, 187.8032102058423618 ) ) ;
#13403=CARTESIAN_POINT ( 'NONE',  ( 93.91931937583731838, -57.67556979900897574, 7.281222044530942128 ) ) ;
#13407=CARTESIAN_POINT ( 'NONE',  ( -2.064720489383732094, -21.35870767192724173, -38.55174460350388443 ) ) ;
#13409=CARTESIAN_POINT ( 'NONE',  ( 20.58069253160714851, -26.08373819371554347, 36.97345864217716382 ) ) ;
#13411=CARTESIAN_POINT ( 'NONE',  ( 51.67980559806123608, -29.93021853868486915, 49.50601613781095978 ) ) ;
#13420=CARTESIAN_POINT ( 'NONE',  ( -97.86738100951825459, -38.00000000000002842, 125.1133639519820804 ) ) ;
#13429=CARTESIAN_POINT ( 'NONE',  ( 4.704252628927049429, -34.58962660028700498, -32.59883165265136995 ) ) ;
#13439=CARTESIAN_POINT ( 'NONE',  ( -92.54188115047482199, -60.00000000000000000, -10.97361708650449330 ) ) ;
#13443=CIRCLE ( 'NONE', #89309, 1.999999999999998224 ) ;
#13447=CARTESIAN_POINT ( 'NONE',  ( -85.34039993398450008, -18.60225220077080976, 158.4019857972550653 ) ) ;
#13458=CARTESIAN_POINT ( 'NONE',  ( -88.64096389254642361, -57.60155557764662149, 203.6424623121221487 ) ) ;
#13464=CARTESIAN_POINT ( 'NONE',  ( 87.19843643122861465, -14.21045842199432307, -12.73007766572366606 ) ) ;
#13465=CARTESIAN_POINT ( 'NONE',  ( -57.89926771889555113, -60.00000000000002132, 101.6232698676003139 ) ) ;
#13467=CARTESIAN_POINT ( 'NONE',  ( -54.92400839910345667, -25.62426591033550238, 54.65035495193780690 ) ) ;
#13471=CARTESIAN_POINT ( 'NONE',  ( -98.96223960978490197, -37.77284757735001364, 191.9112265713812064 ) ) ;
#13476=CARTESIAN_POINT ( 'NONE',  ( -19.73380473719229755, -59.99999999999997868, 40.16716399201472854 ) ) ;
#13482=CARTESIAN_POINT ( 'NONE',  ( 61.68718524083860189, -30.00000000000000000, 71.20902493795223620 ) ) ;
#13488=CARTESIAN_POINT ( 'NONE',  ( -27.03615454696757681, -18.62292616071563955, 28.59941848166171141 ) ) ;
#13492=CARTESIAN_POINT ( 'NONE',  ( 48.40635062956359747, -60.28088182408914264, 54.82487149384981961 ) ) ;
#13495=CARTESIAN_POINT ( 'NONE',  ( -110.5675750054071642, -38.35612456673099047, 181.7435868639444436 ) ) ;
#13497=CARTESIAN_POINT ( 'NONE',  ( 91.23346586961952198, -38.40218125908411650, -11.00096301738425453 ) ) ;
#13507=CARTESIAN_POINT ( 'NONE',  ( 103.4063488952136822, -59.99999999999999289, 200.3742664542178886 ) ) ;
#13511=EDGE_CURVE ( 'NONE', #25171, #53605, #50290, .T. ) ;
#13516=CARTESIAN_POINT ( 'NONE',  ( -91.43843089045226691, -38.39238805426494139, -8.451921997045049650 ) ) ;
#13531=CARTESIAN_POINT ( 'NONE',  ( 83.42202203922076365, -39.47238757521779462, 173.7499749762425267 ) ) ;
#13571=CARTESIAN_POINT ( 'NONE',  ( -109.0438932907287182, -59.99999999999999289, 136.2887194836895617 ) ) ;
#13576=CARTESIAN_POINT ( 'NONE',  ( -83.13834745119730485, -50.08347900195551716, 183.9098975223591310 ) ) ;
#13582=CARTESIAN_POINT ( 'NONE',  ( -84.87627867855697161, -45.26544462712148231, 33.56767573986881814 ) ) ;
#13588=CARTESIAN_POINT ( 'NONE',  ( 108.4902253387283793, -59.99999999999992184, 199.0859659658876524 ) ) ;
#13589=CARTESIAN_POINT ( 'NONE',  ( -103.8766418169371093, -14.21045842199435860, 137.3606855625607182 ) ) ;
#13591=CARTESIAN_POINT ( 'NONE',  ( -65.57779507755935811, -46.43844589625626895, 91.59816456652244199 ) ) ;
#13594=CARTESIAN_POINT ( 'NONE',  ( 88.92543633794424807, -59.99999999998018296, 204.2227067804597027 ) ) ;
#13606=CARTESIAN_POINT ( 'NONE',  ( -92.54656138765464846, -60.00000000000001421, -10.92108962363814051 ) ) ;
#13620=CARTESIAN_POINT ( 'NONE',  ( 34.39988281114163016, -56.83016256492278728, 38.30024153359905625 ) ) ;
#13621=CARTESIAN_POINT ( 'NONE',  ( 4.453875240779016309, -1.734723475976807094E-15, -16.57301948837565675 ) ) ;
#13636=CARTESIAN_POINT ( 'NONE',  ( 95.45105784953814521, -60.00000000000000000, 52.25429896273150376 ) ) ;
#13644=CARTESIAN_POINT ( 'NONE',  ( -74.36474976291079031, -30.00000000000002132, 110.0129636005011946 ) ) ;
#13661=CARTESIAN_POINT ( 'NONE',  ( 79.40402211849792025, -22.14576379642964810, 126.4721508377499788 ) ) ;
#13669=CARTESIAN_POINT ( 'NONE',  ( -46.61116709543701120, -57.68144024183414587, 68.72738526911024337 ) ) ;
#13678=CARTESIAN_POINT ( 'NONE',  ( -17.75574951819011105, -16.19080177579213498, 31.52114076861774095 ) ) ;
#13689=CARTESIAN_POINT ( 'NONE',  ( -72.36027791898858652, -30.15764493038331295, -28.80863952084724389 ) ) ;
#13690=CARTESIAN_POINT ( 'NONE',  ( -66.53608649180739576, -30.00000000000000000, 84.68920165401893030 ) ) ;
#13696=CARTESIAN_POINT ( 'NONE',  ( 96.35553945990194791, -57.62197075410178826, 204.4943201522608547 ) ) ;
#13703=CARTESIAN_POINT ( 'NONE',  ( -61.36110657752745112, -60.00000000000001421, 105.0795332954127161 ) ) ;
#13708=CARTESIAN_POINT ( 'NONE',  ( -84.89290109919227234, -50.19755532556953881, 188.9997143009229319 ) ) ;
#13715=CARTESIAN_POINT ( 'NONE',  ( -85.00188143483111958, -60.19486081470527949, -16.06405287040371022 ) ) ;
#13723=CARTESIAN_POINT ( 'NONE',  ( 12.70248734011628500, -4.285714285714347760, 22.03900363279280583 ) ) ;
#13726=CARTESIAN_POINT ( 'NONE',  ( 71.63670194497801447, -60.00000000000009948, -34.46961289685300045 ) ) ;
#13727=CARTESIAN_POINT ( 'NONE',  ( -79.92344898003078413, -42.96984901787218547, 149.1617487676861060 ) ) ;
#13730=CARTESIAN_POINT ( 'NONE',  ( 99.10278221369861740, -57.62556558655981576, 204.1493198101848918 ) ) ;
#13738=CARTESIAN_POINT ( 'NONE',  ( -104.4234376084712750, -52.71018726599390902, 156.3605036308566980 ) ) ;
#13748=CARTESIAN_POINT ( 'NONE',  ( -63.58375344335239987, -14.21045842199425024, 93.96584349151677884 ) ) ;
#13749=CARTESIAN_POINT ( 'NONE',  ( 27.18724732262417731, -22.09952160911303665, 29.24440674777745386 ) ) ;
#13766=CARTESIAN_POINT ( 'NONE',  ( 81.13768354825626261, -29.99999999999999645, 1.847970586771182644 ) ) ;
#13788=CARTESIAN_POINT ( 'NONE',  ( 62.48344698558671695, -53.38692339959598598, 85.99248783803911067 ) ) ;
#13793=CARTESIAN_POINT ( 'NONE',  ( -65.78405188338429355, -37.94845061455978907, -32.58029113018389467 ) ) ;
#13802=CARTESIAN_POINT ( 'NONE',  ( -25.56287369367873197, -60.00000000000002132, -35.59544240314404107 ) ) ;
#13806=CARTESIAN_POINT ( 'NONE',  ( 85.77546328330258518, -61.05395614131151660, 194.1409842555038097 ) ) ;
#13815=CARTESIAN_POINT ( 'NONE',  ( 12.95434620903975365, -59.99999999999999289, 39.71337736509555327 ) ) ;
#13816=CARTESIAN_POINT ( 'NONE',  ( -99.12369170486120140, -29.99999999999999289, 145.9994480237029961 ) ) ;
#13819=CARTESIAN_POINT ( 'NONE',  ( 61.52046739279862209, -57.67782001033483397, 112.8653612915162086 ) ) ;
#13836=CARTESIAN_POINT ( 'NONE',  ( -15.78049985857718163, -46.43928016077322951, 31.81775410195077924 ) ) ;
#13840=AXIS2_PLACEMENT_3D ( 'NONE', #15475, #64056, #40285 ) ;
#13845=CARTESIAN_POINT ( 'NONE',  ( 61.63246250162482909, -59.99999999999999289, 106.0070534118292755 ) ) ;
#13865=CARTESIAN_POINT ( 'NONE',  ( -80.03450769258309094, -60.00000000000743228, 199.7433096331160698 ) ) ;
#13868=CARTESIAN_POINT ( 'NONE',  ( 74.50860608132113327, -60.00000000000000000, 177.2089907105977886 ) ) ;
#13871=CARTESIAN_POINT ( 'NONE',  ( -108.9224886339666085, -60.00000000000004263, 119.6925845435806650 ) ) ;
#13872=CARTESIAN_POINT ( 'NONE',  ( 9.120188071644534489, -29.02951018409794770, 28.72938299554262542 ) ) ;
#13874=CARTESIAN_POINT ( 'NONE',  ( -45.55848940769042343, -42.98694371728178254, 45.30845615562359541 ) ) ;
#13883=CARTESIAN_POINT ( 'NONE',  ( 84.08753936534863271, -30.00000000001337952, 196.4773746771908236 ) ) ;
#13886=CARTESIAN_POINT ( 'NONE',  ( 99.09030147775226283, -29.99999999999999645, 188.6124528200056432 ) ) ;
#13903=CARTESIAN_POINT ( 'NONE',  ( 105.2827503557284530, -38.38876419932554285, 197.1931609343118055 ) ) ;
#13905=CARTESIAN_POINT ( 'NONE',  ( 86.97481562723852733, -60.21415714265000929, -9.168737641558012186 ) ) ;
#13906=CARTESIAN_POINT ( 'NONE',  ( 56.96819746998301781, -37.99999999999999289, 64.01309078521055085 ) ) ;
#13926=CARTESIAN_POINT ( 'NONE',  ( -45.71963733757689852, -30.00000000000002842, 56.30991746768104633 ) ) ;
#13929=CARTESIAN_POINT ( 'NONE',  ( 84.44843645170369939, -46.56741310714842541, 186.0904281661588300 ) ) ;
#13933=CARTESIAN_POINT ( 'NONE',  ( 94.08407939083754457, -57.67277868574831245, 20.70298615612919946 ) ) ;
#13937=CARTESIAN_POINT ( 'NONE',  ( -11.52459393585250069, -23.01655209608192720, -38.54135265537715327 ) ) ;
#13942=CARTESIAN_POINT ( 'NONE',  ( 8.790745035565722176, -19.73282221811500037, 35.28722622678527898 ) ) ;
#13954=CARTESIAN_POINT ( 'NONE',  ( -102.8326201182668029, -37.99999999999999289, 173.0413610677699694 ) ) ;
#13959=CARTESIAN_POINT ( 'NONE',  ( -50.82590375189641207, -47.40886325391449674, -29.75599597189977530 ) ) ;
#13967=CARTESIAN_POINT ( 'NONE',  ( -91.90010039950615806, -60.00000000000001421, -14.32662728741797054 ) ) ;
#13976=CARTESIAN_POINT ( 'NONE',  ( -80.44522044428813956, -49.91460793207095037, 162.4354708053286913 ) ) ;
#13978=CARTESIAN_POINT ( 'NONE',  ( -13.52487676487832680, 0.000000000000000000, -10.38441970549514970 ) ) ;
#13989=CARTESIAN_POINT ( 'NONE',  ( -108.9175987578229297, -57.66477069964600588, 197.8260142395344303 ) ) ;
#13993=CARTESIAN_POINT ( 'NONE',  ( 95.02194560458454475, -59.99999999999987210, -3.233414228271875857 ) ) ;
#13994=CARTESIAN_POINT ( 'NONE',  ( -44.76022593139747840, -29.99999999999992539, 54.38475608328532473 ) ) ;
#13995=CARTESIAN_POINT ( 'NONE',  ( -56.19539967535489922, -18.67843576544961337, 54.42036842179090428 ) ) ;
#13999=CARTESIAN_POINT ( 'NONE',  ( -99.09551672418950830, -37.78131862766355198, 191.7927793575313160 ) ) ;
#14003=B_SPLINE_CURVE_WITH_KNOTS ( 'NONE', 3,
 ( #16103, #58708, #49529, #8538 ),
 .UNSPECIFIED., .F., .F.,
 ( 4, 4 ),
 ( 0.000000000000000000, 0.002500010780266304685 ),
 .UNSPECIFIED. ) ;
#14004=CARTESIAN_POINT ( 'NONE',  ( 90.24191362537470695, -38.39941249341406859, -15.35752588949901210 ) ) ;
#14011=CARTESIAN_POINT ( 'NONE',  ( 59.60496295899294950, -30.00000000000001066, 65.94430785219442726 ) ) ;
#14019=CARTESIAN_POINT ( 'NONE',  ( 50.52129209761249484, -49.90308930700556544, 55.20093448208132969 ) ) ;
#14024=CARTESIAN_POINT ( 'NONE',  ( -109.0363367054505233, -38.35639537931302812, 190.0084180073488938 ) ) ;
#14026=CARTESIAN_POINT ( 'NONE',  ( 91.43679786253925101, -38.39287896914650844, -8.456874844154592452 ) ) ;
#14036=CARTESIAN_POINT ( 'NONE',  ( 100.6213230593580050, -60.00000000000000000, 201.6927024307212548 ) ) ;
#14039=CARTESIAN_POINT ( 'NONE',  ( 56.50624196457695803, -22.14518791754317206, 56.45264507296375456 ) ) ;
#14046=CARTESIAN_POINT ( 'NONE',  ( -95.01326126541965778, -38.35584031613350930, 58.06921072743757861 ) ) ;
#14053=STYLED_ITEM ( 'NONE', ( #101630 ), #104040 ) ;
#14057=CARTESIAN_POINT ( 'NONE',  ( 83.47826123857470293, -39.47038229126598452, 174.2395583309989036 ) ) ;
#14068=CARTESIAN_POINT ( 'NONE',  ( -81.03185928260310789, -30.00000000000000000, 21.53690394037695555 ) ) ;
#14070=CARTESIAN_POINT ( 'NONE',  ( 2.499999999999999556, -30.00000000000000000, 14.79019945774903633 ) ) ;
#14071=CARTESIAN_POINT ( 'NONE',  ( -2.843030712961830186, -18.20086595765178927, 35.02953871394988283 ) ) ;
#14095=CARTESIAN_POINT ( 'NONE',  ( -112.0805244979449924, -60.00000000000000000, 178.3222598195121407 ) ) ;
#14100=ADVANCED_FACE ( 'NONE', ( #56782 ), #47101, .F. ) ;
#14101=CARTESIAN_POINT ( 'NONE',  ( -82.27752543006228336, -49.99667767229193771, 179.0212925606178374 ) ) ;
#14108=CARTESIAN_POINT ( 'NONE',  ( -83.78263966539077501, -45.26573403153773256, 18.52797371739886145 ) ) ;
#14117=CARTESIAN_POINT ( 'NONE',  ( 94.89952817683000319, -60.00000000000002842, 205.0337064426678921 ) ) ;
#14118=CARTESIAN_POINT ( 'NONE',  ( -90.16416446821634167, -14.21045842199442077, 52.56827875477732448 ) ) ;
#14120=CARTESIAN_POINT ( 'NONE',  ( -64.91042575604046760, -25.57878275972089099, 78.74603656798815621 ) ) ;
#14123=CARTESIAN_POINT ( 'NONE',  ( 71.04344271742604633, -59.99999999997053379, 166.1842289479795056 ) ) ;
#14125=CARTESIAN_POINT ( 'NONE',  ( 2.000806171155364410, -32.51041572883302422, 29.30576361108121120 ) ) ;
#14134=CARTESIAN_POINT ( 'NONE',  ( -111.0127739589412101, -60.00000000000000000, 187.2454623874871800 ) ) ;
#14143=CARTESIAN_POINT ( 'NONE',  ( 105.1762604897960642, -60.00000000000003553, 187.0183921652874233 ) ) ;
#14144=CARTESIAN_POINT ( 'NONE',  ( -36.03617376588638166, -42.97141350977175733, 36.59660582833075182 ) ) ;
#14147=CARTESIAN_POINT ( 'NONE',  ( 32.78518692970002490, -32.55594928816752542, 32.94813001952291387 ) ) ;
#14148=CARTESIAN_POINT ( 'NONE',  ( 16.57301948837259786, 0.000000000000000000, 4.453875240779975542 ) ) ;
#14151=CARTESIAN_POINT ( 'NONE',  ( -73.95166045995811999, -38.32671827097075834, 159.9448648323593432 ) ) ;
#14158=CARTESIAN_POINT ( 'NONE',  ( 2.500000000000041300, -26.27793508735800643, 28.26590473652897018 ) ) ;
#14161=CARTESIAN_POINT ( 'NONE',  ( 97.17610485295698197, -60.00000000000001421, 63.76203667182203816 ) ) ;
#14169=CARTESIAN_POINT ( 'NONE',  ( -84.65603397918647488, -29.99999999999999289, 167.0549101427932044 ) ) ;
#14185=CARTESIAN_POINT ( 'NONE',  ( 80.68051088453421471, -36.02887340626132584, 146.2889946952470837 ) ) ;
#14194=ORIENTED_EDGE ( 'NONE', *, *, #39322, .F. ) ;
#14204=CARTESIAN_POINT ( 'NONE',  ( -26.97617564603512008, -20.23387011012641068, 31.73410695181273766 ) ) ;
#14217=CARTESIAN_POINT ( 'NONE',  ( 59.59397680088719085, -37.32224043100899991, -34.30598283333988974 ) ) ;
#14218=CARTESIAN_POINT ( 'NONE',  ( -70.01690189409367804, -30.00000000000000000, 95.37921460274809249 ) ) ;
#14223=CARTESIAN_POINT ( 'NONE',  ( 86.66021973090251151, -57.58270229864219658, 202.9715953032458913 ) ) ;
#14224=CARTESIAN_POINT ( 'NONE',  ( 71.33015776002258690, -47.40890048900647713, -23.55054361855370715 ) ) ;
#14228=CARTESIAN_POINT ( 'NONE',  ( -72.04210314899036405, -60.00000000000000711, 154.5921861510713882 ) ) ;
#14233=CARTESIAN_POINT ( 'NONE',  ( -85.62538340443454388, -39.27472187846874618, 185.8546422728782943 ) ) ;
#14241=CARTESIAN_POINT ( 'NONE',  ( -83.32935752366911686, -45.25870497630614153, -13.82694917655253342 ) ) ;
#14249=CARTESIAN_POINT ( 'NONE',  ( -22.23822744035697241, -8.673617379884035472E-16, 2.910977163147204116 ) ) ;
#14251=CARTESIAN_POINT ( 'NONE',  ( 87.78053949331578565, -14.21045842199421294, -8.623972743651103556 ) ) ;
#14252=CARTESIAN_POINT ( 'NONE',  ( -81.82243040554628521, -18.68629064860443378, 135.0887551966091564 ) ) ;
#14254=CARTESIAN_POINT ( 'NONE',  ( 31.71028148999514329, -14.21045842199427156, 37.70122135646843731 ) ) ;
#14256=CARTESIAN_POINT ( 'NONE',  ( 106.9737785243404176, -57.65419793449832753, 200.1203704123164471 ) ) ;
#14266=CARTESIAN_POINT ( 'NONE',  ( -103.6844849286397334, -52.71031556485471725, 149.2130235818372626 ) ) ;
#14274=CARTESIAN_POINT ( 'NONE',  ( 2.499999999999984457, -21.99834388059804269, -30.53959902372158908 ) ) ;
#14280=CARTESIAN_POINT ( 'NONE',  ( 26.75709676130376025, -56.86611455124082681, 35.15177554598145804 ) ) ;
#14284=DIRECTION ( 'NONE',  ( 0.000000000000000000, -1.000000000000000000, 0.000000000000000000 ) ) ;
#14289=CARTESIAN_POINT ( 'NONE',  ( 7.063177057909296508, -60.00000000000000000, -42.52329933592234568 ) ) ;
#14292=CARTESIAN_POINT ( 'NONE',  ( -84.71861686120296042, -56.33758301279731029, -15.23115818338405170 ) ) ;
#14312=FACE_OUTER_BOUND ( 'NONE', #70797, .T. ) ;
#14316=CARTESIAN_POINT ( 'NONE',  ( 63.91119737789728816, -36.00602109814766294, 81.23386328541809576 ) ) ;
#14322=DIRECTION ( 'NONE',  ( 0.000000000000000000, 0.000000000000000000, -1.000000000000000000 ) ) ;
#14323=ADVANCED_FACE ( 'NONE', ( #84799, #10883 ), #43798, .T. ) ;
#14331=CARTESIAN_POINT ( 'NONE',  ( 86.00510000878230699, -61.04220111983610053, 194.3129011386755849 ) ) ;
#14339=CARTESIAN_POINT ( 'NONE',  ( 21.61050315576346392, -60.00000000000001421, 40.45514523058442791 ) ) ;
#14341=CARTESIAN_POINT ( 'NONE',  ( -99.15827349551238967, -30.00000000000000000, 146.2805621499050517 ) ) ;
#14346=CARTESIAN_POINT ( 'NONE',  ( 44.35530419813503755, -57.68391187086034932, 63.77888240609519244 ) ) ;
#14352=CARTESIAN_POINT ( 'NONE',  ( -4.157015784815857984, -59.99999999999999289, 39.63100293437526034 ) ) ;
#14356=CARTESIAN_POINT ( 'NONE',  ( -13.76569456190042118, -60.36563448930260734, 34.04465315501506240 ) ) ;
#14357=CARTESIAN_POINT ( 'NONE',  ( -86.44151251292561255, -59.99999999999997868, 22.52580379535574906 ) ) ;
#14368=CARTESIAN_POINT ( 'NONE',  ( 61.50711823914146947, -59.99999999999999289, 105.5777055690388977 ) ) ;
#14374=CARTESIAN_POINT ( 'NONE',  ( 4.090242245409069888, -14.21045842199428932, 34.36068907045891763 ) ) ;
#14388=CARTESIAN_POINT ( 'NONE',  ( -105.4638592052966146, -59.99999999998518518, 201.8892716500855045 ) ) ;
#14390=CARTESIAN_POINT ( 'NONE',  ( 79.59154323555446808, -60.00000000000002132, 195.4646099998837769 ) ) ;
#14392=CARTESIAN_POINT ( 'NONE',  ( -106.1779193982466580, -14.21045842199435860, 156.9944278011976451 ) ) ;
#14393=CARTESIAN_POINT ( 'NONE',  ( 12.22020185172853601, -25.54866882569812603, 28.19719061603959176 ) ) ;
#14394=CARTESIAN_POINT ( 'NONE',  ( 83.69899461553025333, -37.99999999999997158, 34.12667946149305465 ) ) ;
#14396=CARTESIAN_POINT ( 'NONE',  ( -45.44394288432073381, -32.61731379389950547, 42.31964681332677003 ) ) ;
#14407=B_SPLINE_CURVE_WITH_KNOTS ( 'NONE', 3,
 ( #53699, #62344, #21368, #77451 ),
 .UNSPECIFIED., .F., .F.,
 ( 4, 4 ),
 ( 0.3748654421220272703, 0.3763434592322586481 ),
 .UNSPECIFIED. ) ;
#14408=CARTESIAN_POINT ( 'NONE',  ( 109.3806035902058795, -29.99999999998653166, 179.6279394377761776 ) ) ;
#14413=CARTESIAN_POINT ( 'NONE',  ( 89.66112378212690714, -30.00000000000000355, 86.53036795368753076 ) ) ;
#14417=EDGE_CURVE ( 'NONE', #85237, #49798, #100326, .T. ) ;
#14431=CARTESIAN_POINT ( 'NONE',  ( 88.61011283327033539, -38.54255348427882666, 200.1637712349269975 ) ) ;
#14433=CARTESIAN_POINT ( 'NONE',  ( 85.70353180741470567, -52.75305998193952917, -8.674284238902059130 ) ) ;
#14434=CARTESIAN_POINT ( 'NONE',  ( 82.85623877874613186, -38.00000000000004974, 166.0433923026292007 ) ) ;
#14443=COLOUR_RGB ( '', 0.72549020, 0.75294118, 0.79215686) ;
#14451=CARTESIAN_POINT ( 'NONE',  ( 44.63371705108917809, -29.90653276422889917, 54.31444785595910929 ) ) ;
#14455=CARTESIAN_POINT ( 'NONE',  ( 83.28920025294588925, -60.95966722623995793, 191.1640505686548295 ) ) ;
#14459=CARTESIAN_POINT ( 'NONE',  ( 95.56805927552339597, -57.67170252440953959, 37.76800136122525231 ) ) ;
#14463=CARTESIAN_POINT ( 'NONE',  ( -63.29526267904824266, -38.00000000000001421, 80.45729844939860698 ) ) ;
#14479=CARTESIAN_POINT ( 'NONE',  ( -37.04855517154567224, -23.96599618594476766, -30.89117867367345127 ) ) ;
#14481=CARTESIAN_POINT ( 'NONE',  ( -62.88590845438242383, -47.40890540049978341, -26.65507182869829350 ) ) ;
#14490=CARTESIAN_POINT ( 'NONE',  ( -92.73154865952776049, -60.00000000000000000, -5.894050899535240085 ) ) ;
#14493=CARTESIAN_POINT ( 'NONE',  ( 98.75509859307410920, -60.33206540521932482, 196.3354318149040409 ) ) ;
#14497=CARTESIAN_POINT ( 'NONE',  ( -79.80068360959039353, -60.35772941472219344, 173.0473014186353851 ) ) ;
#14509=PLANE ( 'NONE',  #3140 ) ;
#14511=CARTESIAN_POINT ( 'NONE',  ( -89.37884834614470719, -57.60609784898206698, 203.8391154356046115 ) ) ;
#14516=CARTESIAN_POINT ( 'NONE',  ( 86.49463782384169974, -14.21045842199436215, 11.84774393978288742 ) ) ;
#14517=CARTESIAN_POINT ( 'NONE',  ( -66.64776185298879341, -30.00000000000000711, 114.0837597745640721 ) ) ;
#14519=CARTESIAN_POINT ( 'NONE',  ( -53.38980839664982625, -25.63582924091855375, 51.76195856533456663 ) ) ;
#14524=AXIS2_PLACEMENT_3D ( 'NONE', #30778, #54998, #5924 ) ;
#14525=CARTESIAN_POINT ( 'NONE',  ( -100.1530219422562453, -45.25741937776533774, 192.4508485111738310 ) ) ;
#14531=CARTESIAN_POINT ( 'NONE',  ( 107.4777185979739045, -38.36096664182583993, 193.9906563548574070 ) ) ;
#14536=CARTESIAN_POINT ( 'NONE',  ( 63.94887954703639110, -30.00000000000000711, 77.26283590874240303 ) ) ;
#14543=EDGE_LOOP ( 'NONE', ( #16545, #47221, #38740, #8649 ) ) ;
#14544=CARTESIAN_POINT ( 'NONE',  ( 49.20350849749573996, -25.67110830728586635, 45.04464490564094348 ) ) ;
#14546=DIRECTION ( 'NONE',  ( 0.000000000000000000, -1.000000000000000000, 0.000000000000000000 ) ) ;
#14548=CARTESIAN_POINT ( 'NONE',  ( -108.8331786921338704, -38.35659805241468945, 190.6592588805922901 ) ) ;
#14550=CARTESIAN_POINT ( 'NONE',  ( 84.61307093322078288, -38.35852348009560586, -23.18649592206343257 ) ) ;
#14554=CARTESIAN_POINT ( 'NONE',  ( 99.13832651037952814, -45.28277757653744118, 125.4540675598559432 ) ) ;
#14559=CARTESIAN_POINT ( 'NONE',  ( 99.48401045806168952, -60.00000000000000711, 202.0262045926570806 ) ) ;
#14565=CARTESIAN_POINT ( 'NONE',  ( 56.24403759451723772, -46.43678935591641022, 65.97268512243753946 ) ) ;
#14572=CARTESIAN_POINT ( 'NONE',  ( -98.79614853170117783, -38.47643861779322805, 200.8458920591413914 ) ) ;
#14581=CARTESIAN_POINT ( 'NONE',  ( 81.85826472627840644, -53.49893263140352673, 180.4516800555814484 ) ) ;
#14618=CARTESIAN_POINT ( 'NONE',  ( -2.499999999999963141, -18.83381654053417620, 27.02533567785737034 ) ) ;
#14622=CARTESIAN_POINT ( 'NONE',  ( -106.5148633137519738, -60.00000000000000000, 119.6060780682273474 ) ) ;
#14626=CARTESIAN_POINT ( 'NONE',  ( -85.42087258937787908, -25.35191051116863648, 171.5620230697320778 ) ) ;
#14635=CARTESIAN_POINT ( 'NONE',  ( -85.39439480315969888, -52.70747882121834493, 25.13064204089321052 ) ) ;
#14640=FILL_AREA_STYLE_COLOUR ( '', #64822 ) ;
#14642=CARTESIAN_POINT ( 'NONE',  ( 105.0775402602081954, -59.99999999999994316, 202.2121962084956976 ) ) ;
#14643=CARTESIAN_POINT ( 'NONE',  ( -98.01432676219248208, -59.99999999999999289, 53.56972733528865405 ) ) ;
#14644=CARTESIAN_POINT ( 'NONE',  ( -61.71058082456869442, -60.34646374257998502, 87.28499776601393023 ) ) ;
#14647=CARTESIAN_POINT ( 'NONE',  ( 93.59144555981008295, -60.00000000002452794, 204.9629604458358187 ) ) ;
#14649=CARTESIAN_POINT ( 'NONE',  ( 3.040510621938483649, -42.95355241522654666, 31.04364016054148934 ) ) ;
#14658=CARTESIAN_POINT ( 'NONE',  ( -104.3750103821752191, -60.00000000000000000, 199.7222116143482538 ) ) ;
#14669=CARTESIAN_POINT ( 'NONE',  ( -38.30955110355977666, -22.21941382654016905, 33.68855472650722049 ) ) ;
#14672=CARTESIAN_POINT ( 'NONE',  ( 38.28027864600694130, -42.97064924050712165, 38.10376371723102551 ) ) ;
#14674=CARTESIAN_POINT ( 'NONE',  ( 14.86825985028009711, -3.469446951953614189E-15, -8.569529079650944681 ) ) ;
#14678=CARTESIAN_POINT ( 'NONE',  ( -74.34775434501226243, -38.32892518166006823, 163.3919322230082969 ) ) ;
#14692=CARTESIAN_POINT ( 'NONE',  ( 93.72088428965379592, -60.00000000000000711, 39.00990964174581421 ) ) ;
#14701=CARTESIAN_POINT ( 'NONE',  ( -89.32516398097905608, -29.99999999998676259, 6.631855125688738362 ) ) ;
#14707=CARTESIAN_POINT ( 'NONE',  ( 82.13300407177993634, -37.81708028406786326, -13.51745076886380659 ) ) ;
#14715=CARTESIAN_POINT ( 'NONE',  ( 80.37524443596792878, -46.43599209193401123, 156.8239579507224448 ) ) ;
#14722=DIRECTION ( 'NONE',  ( 0.000000000000000000, 0.000000000000000000, 1.000000000000000000 ) ) ;
#14724=CARTESIAN_POINT ( 'NONE',  ( -44.31189620312834876, -57.68384900168454976, 63.67342368891909388 ) ) ;
#14748=CARTESIAN_POINT ( 'NONE',  ( 53.11664595332064209, -36.25651953744597478, -35.66653243501286852 ) ) ;
#14753=CARTESIAN_POINT ( 'NONE',  ( 95.17612642465779516, -57.62056889977026941, 204.5393882615723271 ) ) ;
#14759=CARTESIAN_POINT ( 'NONE',  ( -72.22471733123828130, -60.00000000000000000, 155.9617568056963819 ) ) ;
#14765=CARTESIAN_POINT ( 'NONE',  ( -86.30709385375372733, -21.08530101006160606, 179.9897705061360682 ) ) ;
#14784=CARTESIAN_POINT ( 'NONE',  ( 2.227375807148842313, -1.734723475976807094E-15, -17.01589776168603407 ) ) ;
#14786=CARTESIAN_POINT ( 'NONE',  ( 78.96299857857128757, -14.21045842199439946, -22.44940295094700033 ) ) ;
#14787=CARTESIAN_POINT ( 'NONE',  ( -81.05843653766993384, -32.56278768442193439, 144.8551522210765370 ) ) ;
#14789=CARTESIAN_POINT ( 'NONE',  ( 4.154910845142357978, -29.99999999999994316, 36.99135396797706932 ) ) ;
#14791=CARTESIAN_POINT ( 'NONE',  ( 78.27301562901895693, -57.50947999237905606, 196.9356207485391224 ) ) ;
#14793=DIRECTION ( 'NONE',  ( 0.000000000000000000, 0.000000000000000000, 1.000000000000000000 ) ) ;
#14801=CARTESIAN_POINT ( 'NONE',  ( -105.4329160415097562, -60.15501871978297288, 153.9737639351797327 ) ) ;
#14811=CARTESIAN_POINT ( 'NONE',  ( 31.71700056584302629, -53.37470450013292123, 36.28623570309412116 ) ) ;
#14817=FACE_BOUND ( 'NONE', #103894, .T. ) ;
#14819=DIRECTION ( 'NONE',  ( 0.000000000000000000, -1.000000000000000000, 0.000000000000000000 ) ) ;
#14824=CARTESIAN_POINT ( 'NONE',  ( 32.68672512615790993, -60.00000000000000711, -40.59438170049026695 ) ) ;
#14827=CARTESIAN_POINT ( 'NONE',  ( 2.936182742933428427E-09, -59.99999999999998579, 41.99999999999667466 ) ) ;
#14854=CARTESIAN_POINT ( 'NONE',  ( 65.57816012826067720, -46.43382891351115660, 91.59682735943974308 ) ) ;
#14859=CARTESIAN_POINT ( 'NONE',  ( -22.45002021702217121, -57.67118433041228798, -43.66150106997372404 ) ) ;
#14868=CARTESIAN_POINT ( 'NONE',  ( 86.09607050833426456, -57.43433071910509113, 193.2105974690565802 ) ) ;
#14877=CARTESIAN_POINT ( 'NONE',  ( 34.08754861723457452, -59.99999999999998579, 45.65693729473046147 ) ) ;
#14878=CARTESIAN_POINT ( 'NONE',  ( -100.1431153105590823, -30.00000000000001066, 184.9454591299870856 ) ) ;
#14880=CARTESIAN_POINT ( 'NONE',  ( 40.40776752368557112, -57.69128819681711917, 56.34745769540169391 ) ) ;
#14886=CARTESIAN_POINT ( 'NONE',  ( -25.02205373457694648, -60.00000000000000711, 41.17636800131604247 ) ) ;
#14889=CARTESIAN_POINT ( 'NONE',  ( -86.74851537548293834, -20.66079247287741794, 185.3133297257026015 ) ) ;
#14893=CARTESIAN_POINT ( 'NONE',  ( -11.24664110559554153, -32.51291048916622373, 29.33424993359241739 ) ) ;
#14906=CARTESIAN_POINT ( 'NONE',  ( 62.83177751537848366, -60.00000000000000000, 110.1979811477270204 ) ) ;
#14927=CARTESIAN_POINT ( 'NONE',  ( -80.99729387517955104, -59.99999999999265299, 200.5325947112515337 ) ) ;
#14929=CARTESIAN_POINT ( 'NONE',  ( 86.19853216617802616, -60.00000000000000000, 200.6758986416989785 ) ) ;
#14932=CARTESIAN_POINT ( 'NONE',  ( -114.2389886898993581, -60.00000000000000000, 181.3578213617837491 ) ) ;
#14933=CARTESIAN_POINT ( 'NONE',  ( 9.314459442565317104, -49.91580766175264472, 32.21235667255560031 ) ) ;
#14934=CARTESIAN_POINT ( 'NONE',  ( 102.0814292656478983, -38.00000000000000000, 157.7111269564730094 ) ) ;
#14936=CARTESIAN_POINT ( 'NONE',  ( -45.31002847039886916, -22.24445591861224258, 39.34227033862079992 ) ) ;
#14937=EDGE_CURVE ( 'NONE', #105449, #85237, #21855, .T. ) ;
#14948=CARTESIAN_POINT ( 'NONE',  ( 84.40333236755373036, -29.99999999999844746, 196.7259491443398929 ) ) ;
#14953=CARTESIAN_POINT ( 'NONE',  ( 94.31238871030012660, -30.00000000000000711, 113.8407967138806924 ) ) ;
#14966=CARTESIAN_POINT ( 'NONE',  ( 85.15627926326807540, -38.69159677318751989, 198.5762613391925413 ) ) ;
#14968=CARTESIAN_POINT ( 'NONE',  ( 85.73051029312144067, -52.75124695241775896, -8.197939295095531875 ) ) ;
#14969=CARTESIAN_POINT ( 'NONE',  ( 83.15040716801659926, -38.00000000000005684, 168.9672039349142949 ) ) ;
#14983=CARTESIAN_POINT ( 'NONE',  ( 0.000000000000000000, 0.000000000000000000, 0.000000000000000000 ) ) ;
#14987=SURFACE_SIDE_STYLE ('',( #8495 ) ) ;
#14991=CARTESIAN_POINT ( 'NONE',  ( -1.943011881543717845, -18.06865899137350340, 35.01031080251575389 ) ) ;
#14997=CARTESIAN_POINT ( 'NONE',  ( 86.40712283630125512, -17.65985353466466279, 176.8060135199089018 ) ) ;
#15001=CARTESIAN_POINT ( 'NONE',  ( 93.83458408931859651, -57.67449834134204423, 11.79857076260040216 ) ) ;
#15006=CARTESIAN_POINT ( 'NONE',  ( -84.35947751489756286, -37.99999999999994316, 179.2493818773862131 ) ) ;
#15016=CARTESIAN_POINT ( 'NONE',  ( -3.976861647037802427, -22.09778810902588830, -30.53710112390729137 ) ) ;
#15018=CARTESIAN_POINT ( 'NONE',  ( -82.24209943865865569, -37.99999999999997158, -13.36826342095787368 ) ) ;
#15026=CARTESIAN_POINT ( 'NONE',  ( -59.18075469557353330, -34.58949886300455745, -25.51696680825630992 ) ) ;
#15035=CARTESIAN_POINT ( 'NONE',  ( -92.70286745887267443, -59.99999999999997868, -4.853674443702933772 ) ) ;
#15039=CARTESIAN_POINT ( 'NONE',  ( 95.20707830180857911, -45.27064899011855914, 194.1781096548304788 ) ) ;
#15043=CARTESIAN_POINT ( 'NONE',  ( -83.48750810316161619, -32.53526638036854024, 163.2801944554805118 ) ) ;
#15056=CARTESIAN_POINT ( 'NONE',  ( -78.78539465073522763, -57.50642106797575082, 197.5849804933186817 ) ) ;
#15063=CARTESIAN_POINT ( 'NONE',  ( -33.15890210479862787, -30.00000000000000711, -37.92163678030271967 ) ) ;
#15065=CARTESIAN_POINT ( 'NONE',  ( -1.385021579957316007, -30.00000000000000000, 37.00000000000000711 ) ) ;
#15066=CARTESIAN_POINT ( 'NONE',  ( -53.79344265758010124, -29.09963908877845284, 53.78559824726266925 ) ) ;
#15072=CARTESIAN_POINT ( 'NONE',  ( -97.79127707065502761, -52.80354280853628524, 195.1513629227311242 ) ) ;
#15077=CARTESIAN_POINT ( 'NONE',  ( 106.7250614457355198, -38.36694503808185175, 195.3045705398520511 ) ) ;
#15078=CARTESIAN_POINT ( 'NONE',  ( -80.00000000000000000, -52.00000000000000000, -19.09707704303353282 ) ) ;
#15081=CARTESIAN_POINT ( 'NONE',  ( 80.77650999055178715, -30.00000000000000711, 138.7427449783301370 ) ) ;
#15087=AXIS2_PLACEMENT_3D ( 'NONE', #44900, #53507, #86432 ) ;
#15090=CARTESIAN_POINT ( 'NONE',  ( 49.54155134396112459, -25.66740930363953410, 45.52487917608116419 ) ) ;
#15093=CARTESIAN_POINT ( 'NONE',  ( -107.4879495132023095, -38.36268515545186375, 194.0533311958894842 ) ) ;
#15096=CARTESIAN_POINT ( 'NONE',  ( 110.2348944668668622, -38.35604625147674085, 157.2622168874477779 ) ) ;
#15100=CARTESIAN_POINT ( 'NONE',  ( 93.99242027173671943, -37.84847618451019002, 101.9190371959758181 ) ) ;
#15106=CARTESIAN_POINT ( 'NONE',  ( 88.01504803064270277, -59.99999999999999289, 201.3865903595551572 ) ) ;
#15110=CARTESIAN_POINT ( 'NONE',  ( 58.58608388584831062, -32.54594335739298572, 65.51434834299064391 ) ) ;
#15115=ORIENTED_EDGE ( 'NONE', *, *, #86694, .F. ) ;
#15116=CARTESIAN_POINT ( 'NONE',  ( -93.90547544503390043, -38.35568117715248349, 50.59712527411566896 ) ) ;
#15129=CARTESIAN_POINT ( 'NONE',  ( 80.94188275191889659, -60.49855713378364186, 182.8649140336319761 ) ) ;
#15168=CARTESIAN_POINT ( 'NONE',  ( -106.4896240607370572, -60.00000000000000000, 119.4492507493957305 ) ) ;
#15176=CARTESIAN_POINT ( 'NONE',  ( -85.66159904005490944, -21.90579002698637723, 168.1005346913126743 ) ) ;
#15187=CARTESIAN_POINT ( 'NONE',  ( 114.5718218735923131, -60.00000000000004974, 174.9501719601325078 ) ) ;
#15188=CARTESIAN_POINT ( 'NONE',  ( -99.89444227931625164, -30.00000000000003197, 96.08249125629401988 ) ) ;
#15189=CARTESIAN_POINT ( 'NONE',  ( -62.17707188868673285, -36.01208718166724765, 76.36316336690838114 ) ) ;
#15192=CARTESIAN_POINT ( 'NONE',  ( 94.51406953657293286, -59.99999999999998579, 3.554358192505464586 ) ) ;
#15205=CARTESIAN_POINT ( 'NONE',  ( -110.3478029491143104, -60.00000000000001421, 189.9910190477876597 ) ) ;
#15215=CARTESIAN_POINT ( 'NONE',  ( 100.8709588495254508, -60.00000000000001421, 195.1801793387124633 ) ) ;
#15216=CARTESIAN_POINT ( 'NONE',  ( -31.61288136673854510, -22.14119122292571618, 30.54124083663120004 ) ) ;
#15221=CARTESIAN_POINT ( 'NONE',  ( 38.30783514898087816, -22.21897967646507865, 33.68727933474853842 ) ) ;
#15222=CARTESIAN_POINT ( 'NONE',  ( 11.19959342721965179, -3.864748466433897305E-12, 19.43146043915186993 ) ) ;
#15227=CARTESIAN_POINT ( 'NONE',  ( -57.42639478918781037, -38.34440198517998510, 88.53404947109167722 ) ) ;
#15238=CARTESIAN_POINT ( 'NONE',  ( 93.20221228412790992, -60.00000000000000711, 34.27167064687595399 ) ) ;
#15245=CARTESIAN_POINT ( 'NONE',  ( -79.69840623192676787, -30.00000000000000711, 132.5680624720444314 ) ) ;
#15256=ADVANCED_FACE ( 'NONE', ( #15306 ), #72992, .T. ) ;
#15263=CARTESIAN_POINT ( 'NONE',  ( 82.26387345944664276, -32.55838572498345940, 153.0448389433394993 ) ) ;
#15271=CARTESIAN_POINT ( 'NONE',  ( -47.68231610104891871, -57.68007204195236426, 71.30078553503261674 ) ) ;
#15281=CARTESIAN_POINT ( 'NONE',  ( -27.20181548915192948, -20.34077866823755798, 31.75751083479892856 ) ) ;
#15293=CARTESIAN_POINT ( 'NONE',  ( -67.60950767405599038, -38.09528385293550201, -32.01701373524668526 ) ) ;
#15297=CARTESIAN_POINT ( 'NONE',  ( 91.26148061703614189, -57.61363950115104160, 204.2176009484390136 ) ) ;
#15303=CARTESIAN_POINT ( 'NONE',  ( -73.49543186908600489, -60.00000000000001421, 167.1451735809920081 ) ) ;
#15306=FACE_OUTER_BOUND ( 'NONE', #65775, .T. ) ;
#15308=CARTESIAN_POINT ( 'NONE',  ( -85.96492870306816769, -28.40779642704074348, 181.6674700888168275 ) ) ;
#15315=CARTESIAN_POINT ( 'NONE',  ( -84.58417382167392873, -60.18425325025634720, -16.69743988867924500 ) ) ;
#15322=CARTESIAN_POINT ( 'NONE',  ( 2.083846472846741813E-15, -1.734723475976807094E-15, 17.01589776168603407 ) ) ;
#15326=CARTESIAN_POINT ( 'NONE',  ( 77.20805073229469428, -29.99999999999999289, -26.53535389768476449 ) ) ;
#15327=CARTESIAN_POINT ( 'NONE',  ( -78.91132512760897555, -36.02857813642251728, 136.0548663355014867 ) ) ;
#15330=CARTESIAN_POINT ( 'NONE',  ( 105.7047805233263063, -57.64761371320827266, 201.1859495630244226 ) ) ;
#15333=CIRCLE ( 'NONE', #101498, 2.000000000000001776 ) ;
#15349=CARTESIAN_POINT ( 'NONE',  ( -34.17891763260271887, -14.21045842199440301, 38.95228509905292924 ) ) ;
#15350=CARTESIAN_POINT ( 'NONE',  ( 29.01731335256807398, -49.90763980309816361, 34.62778969272466156 ) ) ;
#15356=FACE_BOUND ( 'NONE', #70114, .T. ) ;
#15363=CARTESIAN_POINT ( 'NONE',  ( 15.96501273729558257, -60.00000000000000000, -42.10368348739202560 ) ) ;
#15365=CARTESIAN_POINT ( 'NONE',  ( 89.67317295579802305, -30.00000000000008882, 189.5710670903794721 ) ) ;
#15390=CARTESIAN_POINT ( 'NONE',  ( -62.94953480991654970, -59.99999999999994316, 90.76860819568858574 ) ) ;
#15391=CARTESIAN_POINT ( 'NONE',  ( 68.52817887026473898, -39.48419332027852846, 97.13330144592191573 ) ) ;
#15397=CARTESIAN_POINT ( 'NONE',  ( -51.62523913740291448, -57.67116585372185966, -39.59675499642695939 ) ) ;
#15414=CARTESIAN_POINT ( 'NONE',  ( 12.80896177052940388, -60.00000000000000711, 39.70888688113913645 ) ) ;
#15415=CARTESIAN_POINT ( 'NONE',  ( -94.05504825925655155, -30.00000000000000000, 191.2807258966970210 ) ) ;
#15418=CARTESIAN_POINT ( 'NONE',  ( 45.11600752062921060, -57.68303782434002613, 65.41414365635188233 ) ) ;
#15422=CARTESIAN_POINT ( 'NONE',  ( 11.11178199064544536, -22.91032599454487695, -38.54163065549817446 ) ) ;
#15425=CARTESIAN_POINT ( 'NONE',  ( -24.73795869524107616, -60.00000000000000000, 41.10165728384131967 ) ) ;
#15429=CARTESIAN_POINT ( 'NONE',  ( -87.09031288375886959, -28.00572983669372107, 187.1676684957507177 ) ) ;
#15433=CARTESIAN_POINT ( 'NONE',  ( -15.66209394986200287, -39.47634415140716868, 30.64911114313175133 ) ) ;
#15444=CARTESIAN_POINT ( 'NONE',  ( 73.52739441614612304, -60.00000000000000000, 167.4607074514827332 ) ) ;
#15464=CARTESIAN_POINT ( 'NONE',  ( -105.8057338367873399, -59.99999999999877076, 201.6387488181161700 ) ) ;
#15467=CARTESIAN_POINT ( 'NONE',  ( 85.55794531748325937, -60.00000000000000000, 200.3757775331295079 ) ) ;
#15470=CARTESIAN_POINT ( 'NONE',  ( -114.5289996431801853, -60.00000000000001421, 168.5344195898668715 ) ) ;
#15471=CARTESIAN_POINT ( 'NONE',  ( 17.74185477829191981, -32.51177142622724148, 29.60969788138565661 ) ) ;
#15474=CARTESIAN_POINT ( 'NONE',  ( 97.09147383894379857, -38.00000000000009237, 192.8437217724261359 ) ) ;
#15475=CARTESIAN_POINT ( 'NONE',  ( 0.000000000000000000, -8.000000000000000000, 0.000000000000000000 ) ) ;
#15477=CARTESIAN_POINT ( 'NONE',  ( -44.56587912721629152, -29.16193315628479610, 40.40586370753838708 ) ) ;
#15492=CARTESIAN_POINT ( 'NONE',  ( 95.01775444805275583, -29.99999999999331735, 199.9312514212468272 ) ) ;
#15496=CARTESIAN_POINT ( 'NONE',  ( 94.47209748978787047, -30.00000000000000000, 114.8027109744303687 ) ) ;
#15510=CARTESIAN_POINT ( 'NONE',  ( 81.59129191571777540, -38.84187913677770609, 195.3900936346319952 ) ) ;
#15525=CARTESIAN_POINT ( 'NONE',  ( 44.47534377888506185, -38.31160956920666649, 57.00192013341545305 ) ) ;
#15531=CARTESIAN_POINT ( 'NONE',  ( 85.09804983725459238, -42.94247291440246528, 186.0227739267606637 ) ) ;
#15535=CARTESIAN_POINT ( 'NONE',  ( 95.57137203408007053, -57.67170117783086880, 37.79708907818724128 ) ) ;
#15554=CARTESIAN_POINT ( 'NONE',  ( -101.3870858685743173, -38.00000000000002132, 187.1511826377679881 ) ) ;
#15560=CARTESIAN_POINT ( 'NONE',  ( -10.85172174320315541, -16.38067545052308915, -34.74268429604064323 ) ) ;
#15563=CARTESIAN_POINT ( 'NONE',  ( -62.18019193066977124, -60.22836170466317185, -29.09066113803248044 ) ) ;
#15572=CARTESIAN_POINT ( 'NONE',  ( -92.72847056440254221, -59.99999999999998579, -5.749582770862643244 ) ) ;
#15574=CARTESIAN_POINT ( 'NONE',  ( 42.42558281948700483, -34.00733088751519517, -29.05298797978474212 ) ) ;
#15576=CARTESIAN_POINT ( 'NONE',  ( 98.44225398900675827, -60.33831865521403870, 196.4443166631917563 ) ) ;
#15579=CARTESIAN_POINT ( 'NONE',  ( -84.74748497845986606, -18.65607540284239718, 153.2878044841931455 ) ) ;
#15590=CARTESIAN_POINT ( 'NONE',  ( -99.73481241717010448, -57.62673548571369508, 203.9935789388791250 ) ) ;
#15595=CARTESIAN_POINT ( 'NONE',  ( -8.309739744518550353, -29.99999999999999289, -39.88085837097889197 ) ) ;
#15596=ADVANCED_FACE ( 'NONE', ( #78845 ), #79903, .F. ) ;
#15598=CARTESIAN_POINT ( 'NONE',  ( -53.02381676432123214, -36.03889879312533395, 54.93151352944263266 ) ) ;
#15601=CARTESIAN_POINT ( 'NONE',  ( -98.75596714119691910, -37.75931162163595900, 192.0729565296949772 ) ) ;
#15605=CARTESIAN_POINT ( 'NONE',  ( 85.34762539502915502, -38.35938083958861711, -22.54931118768901754 ) ) ;
#15612=CARTESIAN_POINT ( 'NONE',  ( 85.25593731491920835, -30.00000000000000355, 172.6945922388917438 ) ) ;
#15617=AXIS2_PLACEMENT_3D ( 'NONE', #57398, #73581, #90313 ) ;
#15620=CARTESIAN_POINT ( 'NONE',  ( 50.44857603004569313, -29.12119561422500524, 47.99944827896294441 ) ) ;
#15624=CARTESIAN_POINT ( 'NONE',  ( -108.1290187186095437, -38.35627294540438470, 138.7757913829071299 ) ) ;
#15627=CARTESIAN_POINT ( 'NONE',  ( 90.86461683327247840, -38.35179314048024679, 20.70149138315537840 ) ) ;
#15629=CARTESIAN_POINT ( 'NONE',  ( 101.9339513551239378, -37.84836680173732759, 156.3405949689792749 ) ) ;
#15634=CARTESIAN_POINT ( 'NONE',  ( 77.82654327636778646, -60.00000000000000000, 192.4673928146949891 ) ) ;
#15638=CARTESIAN_POINT ( 'NONE',  ( 57.84234124985879788, -46.43614486156029386, 69.91354623974028470 ) ) ;
#15640=B_SPLINE_CURVE_WITH_KNOTS ( 'NONE', 3,
 ( #77882, #85443, #36921, #61173, #94059, #54106 ),
 .UNSPECIFIED., .F., .F.,
 ( 4, 2, 4 ),
 ( 0.02044294606936548214, 0.03157470899999220704, 0.04270647193061893887 ),
 .UNSPECIFIED. ) ;
#15646=CARTESIAN_POINT ( 'NONE',  ( -73.36661343314580108, -29.99999999991936761, 145.3711930596387845 ) ) ;
#15656=CARTESIAN_POINT ( 'NONE',  ( 84.42314394957541879, -32.44248152629501902, 172.3652158902926601 ) ) ;
#15673=CARTESIAN_POINT ( 'NONE',  ( -24.75015538639915746, -28.86932137373848661, 38.18840044054004323 ) ) ;
#15696=CARTESIAN_POINT ( 'NONE',  ( -112.2059321623641495, -60.00000000000000000, 170.3870518237542342 ) ) ;
#15704=CARTESIAN_POINT ( 'NONE',  ( -84.63106176657737478, -32.40589074336656950, 174.3468092685627369 ) ) ;
#15722=CARTESIAN_POINT ( 'NONE',  ( 105.8603286302927984, -14.21045842199436571, 153.6005582235227678 ) ) ;
#15724=CARTESIAN_POINT ( 'NONE',  ( -109.1953414053527780, -30.00000000000001066, 161.8807222540328894 ) ) ;
#15725=CARTESIAN_POINT ( 'NONE',  ( -63.35317981673050980, -39.48581946695038170, 81.40797789241049998 ) ) ;
#15728=CARTESIAN_POINT ( 'NONE',  ( 110.4834380140601695, -59.99999999996104805, 129.5980811341964056 ) ) ;
#15739=CARTESIAN_POINT ( 'NONE',  ( -97.18990194766369939, -60.00000000000000000, 63.92461308931969910 ) ) ;
#15749=CARTESIAN_POINT ( 'NONE',  ( 106.4731662889862349, -60.00000000000002132, 174.0751867897438103 ) ) ;
#15750=CARTESIAN_POINT ( 'NONE',  ( -31.12606138324045446, -18.66557501722132528, 29.72691873377532445 ) ) ;
#15753=CARTESIAN_POINT ( 'NONE',  ( 41.03672742457499822, -60.25176818595546280, 44.31207356424504695 ) ) ;
#15759=CARTESIAN_POINT ( 'NONE',  ( -74.04571983938727442, -38.32706951796213701, 160.7403410287773227 ) ) ;
#15769=CARTESIAN_POINT ( 'NONE',  ( 100.7796288034784169, -60.00000000000002132, 85.60714601047209271 ) ) ;
#15776=CARTESIAN_POINT ( 'NONE',  ( -90.13898955460108198, -29.99999999999991473, 189.9826003834946562 ) ) ;
#15792=CARTESIAN_POINT ( 'NONE',  ( 80.10507346880626756, -46.43520559967900851, 154.7484568511157477 ) ) ;
#15802=CARTESIAN_POINT ( 'NONE',  ( -68.42433815231228778, -57.68192485334662933, 143.8276693603407068 ) ) ;
#15812=CARTESIAN_POINT ( 'NONE',  ( -29.12521271972553194, -21.25831152097612886, 32.00366296159075574 ) ) ;
#15824=CARTESIAN_POINT ( 'NONE',  ( -59.10698846045011834, -30.00000000000000000, 64.79178358224362455 ) ) ;
#15828=CARTESIAN_POINT ( 'NONE',  ( 112.0288779015512119, -57.67108280594192138, 191.2312896774432147 ) ) ;
#15834=CARTESIAN_POINT ( 'NONE',  ( -75.37500990013671753, -60.00000000000000000, 183.7553592533116955 ) ) ;
#15838=CARTESIAN_POINT ( 'NONE',  ( -84.39447898885444488, -50.18442846096746024, 187.9382864958523669 ) ) ;
#15841=( BOUNDED_CURVE ( )  B_SPLINE_CURVE ( 2, ( #100410, #26572, #98802 ),
 .UNSPECIFIED., .F., .F. ) 
 B_SPLINE_CURVE_WITH_KNOTS ( ( 3, 3 ),
 ( 0.000000000000000000, 1.000000000000000000 ),
 .UNSPECIFIED. ) 
 CURVE ( )  GEOMETRIC_REPRESENTATION_ITEM ( )  RATIONAL_B_SPLINE_CURVE ( ( 1.000000000000000000, 1.857142857142858317, 1.000000000000000000 ) ) 
 REPRESENTATION_ITEM ( '' )  );
#15846=CARTESIAN_POINT ( 'NONE',  ( -86.24397153928001103, -60.23073308139314719, -13.36445785299144440 ) ) ;
#15854=CARTESIAN_POINT ( 'NONE',  ( 2.910977163135976653, -8.673617379884035472E-16, -22.23822744035697241 ) ) ;
#15857=CARTESIAN_POINT ( 'NONE',  ( 17.10006063058271053, -59.99999999999996447, -44.43597027717249404 ) ) ;
#15858=CARTESIAN_POINT ( 'NONE',  ( -76.14763078889043868, -56.84898049809550713, 140.2345650644058992 ) ) ;
#15860=CARTESIAN_POINT ( 'NONE',  ( 24.85181238201470322, -30.00000000000000000, 38.32581332381749206 ) ) ;
#15862=CARTESIAN_POINT ( 'NONE',  ( 86.94765383177332296, -57.67023441083929214, -25.46996265147350869 ) ) ;
#15883=CARTESIAN_POINT ( 'NONE',  ( -24.85253352225967660, -29.99999999999996092, 38.32597638696945097 ) ) ;
#15884=CARTESIAN_POINT ( 'NONE',  ( 28.95048640063493295, -22.11353157157453353, 29.69856830660305391 ) ) ;
#15915=ORIENTED_EDGE ( 'NONE', *, *, #77201, .F. ) ;
#15924=ADVANCED_FACE ( 'NONE', ( #56555 ), #42016, .F. ) ;
#15925=CARTESIAN_POINT ( 'NONE',  ( -41.76078508741669992, -59.99999999999995026, 45.02266864589306294 ) ) ;
#15926=CARTESIAN_POINT ( 'NONE',  ( 67.57980059920171811, -53.38336469478974067, 101.9910149677482565 ) ) ;
#15950=CARTESIAN_POINT ( 'NONE',  ( 1.421012265766256721, -59.99999999999999289, 39.63907929704831190 ) ) ;
#15951=CARTESIAN_POINT ( 'NONE',  ( -98.89902882238894222, -29.99999999999999645, 189.0609296686858158 ) ) ;
#15954=CARTESIAN_POINT ( 'NONE',  ( 47.36048362120468624, -57.68077050285960894, 70.51996143053239052 ) ) ;
#15957=CARTESIAN_POINT ( 'NONE',  ( 14.74954138962861627, -24.00043886548641936, -38.53150145719773434 ) ) ;
#15960=UNCERTAINTY_MEASURE_WITH_UNIT (LENGTH_MEASURE( 1.000000000000000082E-05 ), #96358, 'distance_accuracy_value', 'NONE');
#15962=CARTESIAN_POINT ( 'NONE',  ( -27.03817179307704421, -60.00000000000001421, 41.77503236863146441 ) ) ;
#15965=CARTESIAN_POINT ( 'NONE',  ( -86.71815218704666961, -20.66647618804140407, 185.1331831730891224 ) ) ;
#15969=CARTESIAN_POINT ( 'NONE',  ( -6.057497750955408655, -32.51266269460595737, 29.29875079916816105 ) ) ;
#15983=CARTESIAN_POINT ( 'NONE',  ( 73.51782150160397578, -60.00000000000000711, 167.3661187031590316 ) ) ;
#15984=CARTESIAN_POINT ( 'NONE',  ( 105.4249980201500136, -14.21045842199437992, 149.5332359265665900 ) ) ;
#15990=CARTESIAN_POINT ( 'NONE',  ( 8.180516222381777780, -14.21045842199445630, 34.35482301558341334 ) ) ;
#16005=CARTESIAN_POINT ( 'NONE',  ( -32.66239298923139245, -59.99999999999511147, 47.46693911184033254 ) ) ;
#16007=CARTESIAN_POINT ( 'NONE',  ( 73.38123138194130490, -59.99999999999997868, 165.9433868892914461 ) ) ;
#16008=CARTESIAN_POINT ( 'NONE',  ( -109.1953414053527780, -30.00000000000001066, 161.8807222540328894 ) ) ;
#16009=CARTESIAN_POINT ( 'NONE',  ( 13.37339337037409415, -32.51077182928822396, 29.38669317182240803 ) ) ;
#16010=CARTESIAN_POINT ( 'NONE',  ( 99.45413243311152485, -38.00000000000002842, 191.4610151428277049 ) ) ;
#16011=CARTESIAN_POINT ( 'NONE',  ( -44.74673245019804568, -39.53078959506873957, 43.36019415930032750 ) ) ;
#16022=CARTESIAN_POINT ( 'NONE',  ( 80.75544287417717726, -30.00000000000002132, -12.51947141605529090 ) ) ;
#16026=CARTESIAN_POINT ( 'NONE',  ( 94.63127039864093604, -30.00000000000000000, 115.7646022404933461 ) ) ;
#16041=CARTESIAN_POINT ( 'NONE',  ( 85.16262797248658956, -38.69119117541009700, 198.5801802344664111 ) ) ;
#16054=( LENGTH_UNIT ( ) NAMED_UNIT ( * ) SI_UNIT ( .MILLI., .METRE. ) );
#16060=CARTESIAN_POINT ( 'NONE',  ( -7.422993619742127791, -19.22976363275861900, 35.19469004974323667 ) ) ;
#16064=CARTESIAN_POINT ( 'NONE',  ( 83.95501332274635331, -53.77704049164677969, 188.7737198488325134 ) ) ;
#16069=CARTESIAN_POINT ( 'NONE',  ( 92.89556986967913588, -57.65649627823201229, -17.47502724792872186 ) ) ;
#16075=CARTESIAN_POINT ( 'NONE',  ( -81.00880480115741022, -29.99999999999999645, 21.10007109864825736 ) ) ;
#16076=CARTESIAN_POINT ( 'NONE',  ( -72.14820142673382009, -37.99999999999997158, 108.4616125675222094 ) ) ;
#16084=CARTESIAN_POINT ( 'NONE',  ( -12.74625527888247944, -23.93263146839674604, -30.51339262294724008 ) ) ;
#16095=CARTESIAN_POINT ( 'NONE',  ( -35.84592417077619331, -23.58871961031537978, -31.12588894592865785 ) ) ;
#16097=CARTESIAN_POINT ( 'NONE',  ( -56.21085237342701646, -34.58943223605337636, -26.29373296556804362 ) ) ;
#16098=VERTEX_POINT ( 'NONE', #84775 ) ;
#16103=CARTESIAN_POINT ( 'NONE',  ( -2.499999999999978684, -29.99999999999999645, 28.88619816519791073 ) ) ;
#16104=CARTESIAN_POINT ( 'NONE',  ( -81.49343273877569516, -60.00000000000002132, -27.02824350414386245 ) ) ;
#16106=CARTESIAN_POINT ( 'NONE',  ( 8.431489367831275672, -22.82219903641888337, -30.52630000682834677 ) ) ;
#16107=CARTESIAN_POINT ( 'NONE',  ( 100.7081988093182190, -60.27117616117514132, 195.3567347834335806 ) ) ;
#16122=CARTESIAN_POINT ( 'NONE',  ( -31.30247466046573379, -57.68739127208316120, 46.06264550376279487 ) ) ;
#16128=CARTESIAN_POINT ( 'NONE',  ( 42.61132677773223065, -60.00000000000003553, -41.65900251181847125 ) ) ;
#16130=CARTESIAN_POINT ( 'NONE',  ( -54.15982943992869281, -32.56507362313620746, 55.81706142454490305 ) ) ;
#16134=CARTESIAN_POINT ( 'NONE',  ( -97.87568255775092041, -37.71879727302795970, 192.5524585354622786 ) ) ;
#16138=CARTESIAN_POINT ( 'NONE',  ( 106.5513553430678684, -38.35592835780060739, 127.5841831557265067 ) ) ;
#16145=CARTESIAN_POINT ( 'NONE',  ( 83.63598298596150471, -30.00000000000000000, 157.8859991142867614 ) ) ;
#16151=CARTESIAN_POINT ( 'NONE',  ( 50.61148790639070683, -46.43901393920370424, 54.16023664066702281 ) ) ;
#16155=CARTESIAN_POINT ( 'NONE',  ( -110.3885816063411767, -38.35608404332607790, 159.0436535490340759 ) ) ;
#16159=CARTESIAN_POINT ( 'NONE',  ( 92.04552895760792808, -38.35407921060832592, 35.17533269925505124 ) ) ;
#16162=CARTESIAN_POINT ( 'NONE',  ( 96.37451246332086896, -52.71696751734791064, 101.1475834991004348 ) ) ;
#16168=CARTESIAN_POINT ( 'NONE',  ( 75.46832707863339351, -60.00000000000002132, 184.3015218829329172 ) ) ;
#16174=CARTESIAN_POINT ( 'NONE',  ( 59.14149476428188734, -22.12859458409723601, 62.21351809755216777 ) ) ;
#16179=CARTESIAN_POINT ( 'NONE',  ( -78.30510816835224830, -30.00000000001010036, 184.2198921887762140 ) ) ;
#16188=CARTESIAN_POINT ( 'NONE',  ( 83.05676702380381471, -42.97589841844901315, 175.6755486148402099 ) ) ;
#16206=CARTESIAN_POINT ( 'NONE',  ( -8.658620422836460051, -19.69050060409069758, 35.27988606632377611 ) ) ;
#16225=CARTESIAN_POINT ( 'NONE',  ( -103.7468799687159873, -59.99999999999999289, 102.9567143256649189 ) ) ;
#16234=CARTESIAN_POINT ( 'NONE',  ( -81.24902549186542444, -60.56381191490225291, 184.6567455024997457 ) ) ;
#16252=CARTESIAN_POINT ( 'NONE',  ( 109.5916899561874942, -30.00000000000003197, 172.2594225519244446 ) ) ;
#16253=CARTESIAN_POINT ( 'NONE',  ( -105.6361520504002840, -30.00000000000002132, 194.5259906914266139 ) ) ;
#16254=CARTESIAN_POINT ( 'NONE',  ( -60.20847870758737486, -56.86770172147161873, 81.17039900336807534 ) ) ;
#16257=CARTESIAN_POINT ( 'NONE',  ( 114.5004563705182221, -60.00000000000000000, 167.5904344248802431 ) ) ;
#16267=CARTESIAN_POINT ( 'NONE',  ( -111.6028829027016940, -59.99999999999997158, 183.7673010694335574 ) ) ;
#16278=CARTESIAN_POINT ( 'NONE',  ( 85.18902050349326771, -60.00000000000000000, -15.68190703514374107 ) ) ;
#16280=CARTESIAN_POINT ( 'NONE',  ( -33.11049135242710406, -49.90384961613743542, 36.32409600320708165 ) ) ;
#16282=CARTESIAN_POINT ( 'NONE',  ( 39.55699615616754272, -25.68728013176338365, 35.29738370701448247 ) ) ;
#16286=CARTESIAN_POINT ( 'NONE',  ( -81.55799083263947580, -38.84168887015896132, 195.3484558550406405 ) ) ;
#16296=CARTESIAN_POINT ( 'NONE',  ( 104.9332722526575168, -60.00000000000000711, 109.9670046731016697 ) ) ;
#16302=CARTESIAN_POINT ( 'NONE',  ( -98.27005700444449587, -30.00000000000002132, 190.2025997981200476 ) ) ;
#16318=CARTESIAN_POINT ( 'NONE',  ( 79.61275247625323459, -56.85118161666118652, 165.3693179662261912 ) ) ;
#16327=CARTESIAN_POINT ( 'NONE',  ( 2.272164087111425257, -60.00000000000000000, -36.90211091601013749 ) ) ;
#16335=SHAPE_REPRESENTATION ( '1. Base', ( #10728 ), #103758 ) ;
#16340=CARTESIAN_POINT ( 'NONE',  ( 23.92965011663618213, -28.31131868122402295, 37.91106159048879931 ) ) ;
#16351=CARTESIAN_POINT ( 'NONE',  ( -58.62616826898538847, -30.00000000000000000, 63.65786219019150849 ) ) ;
#16356=CARTESIAN_POINT ( 'NONE',  ( 97.43174647595270699, -57.67122121763508602, 52.28073263135593862 ) ) ;
#16361=CARTESIAN_POINT ( 'NONE',  ( -76.88100059106110962, -59.99999999999998579, 190.1002214371410162 ) ) ;
#16365=CARTESIAN_POINT ( 'NONE',  ( -84.09290747704537239, -53.79517231171755043, 189.0853069011170362 ) ) ;
#16368=VERTEX_POINT ( 'NONE', #21146 ) ;
#16373=CARTESIAN_POINT ( 'NONE',  ( -86.01413558773862178, -60.22748779183664425, -14.08703606452684376 ) ) ;
#16381=CARTESIAN_POINT ( 'NONE',  ( 8.569529079650926917, -1.734723475976807094E-15, 14.86825985027943808 ) ) ;
#16383=CARTESIAN_POINT ( 'NONE',  ( 42.61132677773223065, -60.00000000000003553, -41.65900251181847125 ) ) ;
#16384=CARTESIAN_POINT ( 'NONE',  ( -78.83331469179402973, -18.67150368877627997, 121.1180772619996162 ) ) ;
#16387=CARTESIAN_POINT ( 'NONE',  ( 31.98199460507809277, -29.99999999999994316, 41.00477363309762779 ) ) ;
#16389=CARTESIAN_POINT ( 'NONE',  ( 112.4234441501388204, -57.67115680235927755, 189.8840207355380585 ) ) ;
#16393=CARTESIAN_POINT ( 'NONE',  ( -89.99999999999997158, -52.00000000000000000, 198.0238439516549818 ) ) ;
#16411=CARTESIAN_POINT ( 'NONE',  ( 6.243930039575695118E-05, -60.00000000000000000, 42.00000000000000711 ) ) ;
#16412=CARTESIAN_POINT ( 'NONE',  ( 29.49176342059628197, -46.43232445692602539, 34.17932786961914360 ) ) ;
#16415=EDGE_CURVE ( 'NONE', #95473, #16098, #56633, .T. ) ;
#16421=DIRECTION ( 'NONE',  ( 0.000000000000000000, 0.000000000000000000, -1.000000000000000000 ) ) ;
#16425=CARTESIAN_POINT ( 'NONE',  ( 11.77556225125753642, -59.99999999999999289, -42.34068502047673377 ) ) ;
#16435=ORIENTED_EDGE ( 'NONE', *, *, #71644, .T. ) ;
#16449=CARTESIAN_POINT ( 'NONE',  ( -78.89501011019794419, -59.99999999999995737, 163.3001588117704159 ) ) ;
#16450=CARTESIAN_POINT ( 'NONE',  ( 66.84561192680622810, -46.43373246685565903, 95.56824384552960794 ) ) ;
#16451=CIRCLE ( 'NONE', #35436, 7.499999999992679633 ) ;
#16467=( GEOMETRIC_REPRESENTATION_CONTEXT ( 3 ) GLOBAL_UNCERTAINTY_ASSIGNED_CONTEXT ( ( #73304 ) ) GLOBAL_UNIT_ASSIGNED_CONTEXT ( ( #7352, #105528, #47283 ) ) REPRESENTATION_CONTEXT ( 'NONE', 'WORKASPACE' ) );
#16485=CARTESIAN_POINT ( 'NONE',  ( -92.77811343242147757, -29.99999999999999645, 191.0689905325092184 ) ) ;
#16487=CARTESIAN_POINT ( 'NONE',  ( 62.75430164509801756, -57.67841677346302021, 117.5347977078399140 ) ) ;
#16493=CARTESIAN_POINT ( 'NONE',  ( -5.044614528818932797, -59.99999999999999289, 39.62871590938365784 ) ) ;
#16495=CARTESIAN_POINT ( 'NONE',  ( -87.03184277043726524, -39.08917807867680239, 189.1309292593449243 ) ) ;
#16498=CARTESIAN_POINT ( 'NONE',  ( -9.023399056601082435, -18.58633034970281273, 26.98791154383341251 ) ) ;
#16500=DIRECTION ( 'NONE',  ( 0.000000000000000000, 1.000000000000000000, 0.000000000000000000 ) ) ;
#16501=CARTESIAN_POINT ( 'NONE',  ( -101.5568998084323056, -60.00000000000000000, 194.6300538685317463 ) ) ;
#16512=CARTESIAN_POINT ( 'NONE',  ( 114.3489886862215883, -60.00000000000002842, 164.2602920347584359 ) ) ;
#16524=ORIENTED_EDGE ( 'NONE', *, *, #89297, .T. ) ;
#16532=CARTESIAN_POINT ( 'NONE',  ( -49.37845040383849238, -60.00000000003905853, 76.62573825319901744 ) ) ;
#16535=CARTESIAN_POINT ( 'NONE',  ( 91.88848222090017259, -59.99999999999997158, 9.002118979807052668 ) ) ;
#16537=CARTESIAN_POINT ( 'NONE',  ( -114.2223820868815380, -59.99999999999997868, 162.1253058113985048 ) ) ;
#16538=CARTESIAN_POINT ( 'NONE',  ( 17.81248185889901592, -35.99250062930340732, 30.19708477161321269 ) ) ;
#16543=CARTESIAN_POINT ( 'NONE',  ( -41.52699401632758480, -22.24292886909580957, 35.91547177849930961 ) ) ;
#16545=ORIENTED_EDGE ( 'NONE', *, *, #99307, .T. ) ;
#16547=DIRECTION ( 'NONE',  ( -0.000000000000000000, -1.000000000000000000, -0.000000000000000000 ) ) ;
#16552=CARTESIAN_POINT ( 'NONE',  ( 2.499999999999984457, -21.99834388059804269, -30.53959902372158908 ) ) ;
#16559=CARTESIAN_POINT ( 'NONE',  ( 72.67119523410620729, -30.00000000000000000, -19.29465872568861684 ) ) ;
#16561=AXIS2_PLACEMENT_3D ( 'NONE', #105924, #32074, #14793 ) ;
#16565=CARTESIAN_POINT ( 'NONE',  ( 98.02403481859347778, -29.99999999999999645, 137.7085981003935444 ) ) ;
#16579=CARTESIAN_POINT ( 'NONE',  ( 79.85416194052990591, -38.77095264444343314, 192.7203380926642069 ) ) ;
#16601=CARTESIAN_POINT ( 'NONE',  ( 86.27972295779851208, -24.64005545529337127, 181.9969923761166513 ) ) ;
#16605=CARTESIAN_POINT ( 'NONE',  ( 94.56681692940503581, -57.65518366666022132, -10.45629857477335456 ) ) ;
#16607=LINE ( 'NONE', #7433, #35240 ) ;
#16610=CARTESIAN_POINT ( 'NONE',  ( -80.98592521388407306, -29.99999999999999645, 20.65126904418409026 ) ) ;
#16641=CARTESIAN_POINT ( 'NONE',  ( -33.37378058036343731, -60.00000000000000000, -40.51130621461524584 ) ) ;
#16643=CARTESIAN_POINT ( 'NONE',  ( 71.17283260602091843, -38.00000000000000000, -21.88484610531455488 ) ) ;
#16645=CARTESIAN_POINT ( 'NONE',  ( 99.38078780120881106, -60.31955890522991126, 196.1176621183285818 ) ) ;
#16660=CARTESIAN_POINT ( 'NONE',  ( -9.856791769558052252, -57.67120557387264768, 41.61776228975389813 ) ) ;
#16664=DIRECTION ( 'NONE',  ( 0.000000000000000000, 0.000000000000000000, -1.000000000000000000 ) ) ;
#16665=CARTESIAN_POINT ( 'NONE',  ( -8.180708021844917965, -14.21045842199436926, -37.25108655295423432 ) ) ;
#16667=CARTESIAN_POINT ( 'NONE',  ( -53.88432441057622668, -39.50293457858858659, 57.94454880366763661 ) ) ;
#16670=CARTESIAN_POINT ( 'NONE',  ( -99.48109555172277396, -45.25232648423930470, 193.0206739817450625 ) ) ;
#16675=VERTEX_POINT ( 'NONE', #60394 ) ;
#16678=CARTESIAN_POINT ( 'NONE',  ( 71.73296838179494728, -38.32718984392275985, 144.1581809263412879 ) ) ;
#16683=CARTESIAN_POINT ( 'NONE',  ( 85.25629243111305300, -30.00000000000000000, 172.6978005289113298 ) ) ;
#16690=CARTESIAN_POINT ( 'NONE',  ( 51.69300476518706944, -60.30369315783265449, 61.32240503668131026 ) ) ;
#16696=CARTESIAN_POINT ( 'NONE',  ( -110.7188736420333299, -38.35613913791396357, 163.9771080353006596 ) ) ;
#16699=CARTESIAN_POINT ( 'NONE',  ( 90.82053129898724819, -38.35077124885843602, 19.83685144799958877 ) ) ;
#16701=CARTESIAN_POINT ( 'NONE',  ( 103.1792978025558369, -45.28266199700388484, 156.3515883262585930 ) ) ;
#16707=CARTESIAN_POINT ( 'NONE',  ( 77.51769761606085751, -60.00000000000000711, 191.8023382803138475 ) ) ;
#16713=CARTESIAN_POINT ( 'NONE',  ( 61.96504965809006649, -39.48483385517126720, 77.49375403494420311 ) ) ;
#16717=CARTESIAN_POINT ( 'NONE',  ( -88.93458861890022149, -38.38101198339035136, -18.16568902887404491 ) ) ;
#16727=CARTESIAN_POINT ( 'NONE',  ( 85.88214304176412384, -21.77332349503629416, 171.2076137571639549 ) ) ;
#16743=CARTESIAN_POINT ( 'NONE',  ( -15.92201275013530726, -23.21266242509823741, 36.07010217149083076 ) ) ;
#16755=CARTESIAN_POINT ( 'NONE',  ( 45.16937095488047760, -60.22825610313712019, -33.02226515330256973 ) ) ;
#16765=CARTESIAN_POINT ( 'NONE',  ( -95.60614214828055424, -60.00000000000000711, 53.33793432721193284 ) ) ;
#16775=CARTESIAN_POINT ( 'NONE',  ( -84.78841041186234406, -28.94319752679387392, 170.4401308887547373 ) ) ;
#16786=FACE_OUTER_BOUND ( 'NONE', #65415, .T. ) ;
#16787=SURFACE_SIDE_STYLE ('',( #74475 ) ) ;
#16794=CARTESIAN_POINT ( 'NONE',  ( 109.1953510978495956, -29.99999999999998934, 161.8808647345001646 ) ) ;
#16795=CARTESIAN_POINT ( 'NONE',  ( -106.6034117734591860, -29.99999999999999645, 192.6833206840571791 ) ) ;
#16796=CARTESIAN_POINT ( 'NONE',  ( -62.29161391638449885, -22.11170671976271862, 69.90898424290641344 ) ) ;
#16800=CARTESIAN_POINT ( 'NONE',  ( 113.6477508017368194, -59.99999999999997158, 154.8077346558557679 ) ) ;
#16802=CARTESIAN_POINT ( 'NONE',  ( 4.998710019538861182, -25.54820205286554469, 28.13823241950028020 ) ) ;
#16803=CARTESIAN_POINT ( 'NONE',  ( -105.8794421244064097, -60.15508394961005934, 158.7618641718036088 ) ) ;
#16812=CARTESIAN_POINT ( 'NONE',  ( -78.29652527090244973, -60.00000000000002132, 193.4105370956309002 ) ) ;
#16825=CARTESIAN_POINT ( 'NONE',  ( -32.06874758335647613, -36.02319553862302115, 33.29146392800486609 ) ) ;
#16827=CARTESIAN_POINT ( 'NONE',  ( 42.58818415145629643, -53.34091589762581265, 44.38045783418311174 ) ) ;
#16833=CARTESIAN_POINT ( 'NONE',  ( -76.00620243949536814, -38.37823116147261260, 178.4010451240498867 ) ) ;
#16838=CARTESIAN_POINT ( 'NONE',  ( 68.96826172936565058, -59.99999999999997158, 110.4669535869814467 ) ) ;
#16847=CARTESIAN_POINT ( 'NONE',  ( 106.3832165010686737, -59.99999999999999289, 118.7897376084098369 ) ) ;
#16853=CARTESIAN_POINT ( 'NONE',  ( -89.59768141200925129, -30.00000000000018474, 189.4893437224044987 ) ) ;
#16870=CARTESIAN_POINT ( 'NONE',  ( 79.71048774950203608, -49.90412405833568243, 156.1982597888667499 ) ) ;
#16877=CARTESIAN_POINT ( 'NONE',  ( 14.89431991952050538, -60.00000000000000711, -36.42525387037616724 ) ) ;
#16886=CARTESIAN_POINT ( 'NONE',  ( 86.79590143382110057, -31.74670322683050117, 186.8222491938091423 ) ) ;
#16890=CARTESIAN_POINT ( 'NONE',  ( 21.52054819351988613, -26.69862200661779994, 37.20882657828786222 ) ) ;
#16892=CARTESIAN_POINT ( 'NONE',  ( -72.50181434431193850, -38.00000000001091394, -21.26203725901419261 ) ) ;
#16893=CIRCLE ( 'NONE', #77170, 1.999999999999998224 ) ;
#16905=CARTESIAN_POINT ( 'NONE',  ( 113.3004268891054522, -57.67143715891052125, 155.2604439073490425 ) ) ;
#16912=CARTESIAN_POINT ( 'NONE',  ( -75.55177680087479075, -60.00000000000000000, 184.7945938706629931 ) ) ;
#16919=CARTESIAN_POINT ( 'NONE',  ( -85.67931066178286414, -35.66015517622967224, 184.2351685365583478 ) ) ;
#16926=CARTESIAN_POINT ( 'NONE',  ( -86.84696613357556316, -60.22825968734050406, -10.54492661878714443 ) ) ;
#16935=CARTESIAN_POINT ( 'NONE',  ( 60.74900604410193239, -14.21045842199440301, -29.98664384297035213 ) ) ;
#16936=CARTESIAN_POINT ( 'NONE',  ( -75.82081383092520355, -60.31953473974737534, 141.6095240737906238 ) ) ;
#16938=CARTESIAN_POINT ( 'NONE',  ( 66.01776342811430709, -14.21045842199433373, 101.7751388943407989 ) ) ;
#16940=CARTESIAN_POINT ( 'NONE',  ( 112.3945400198572884, -57.67111632160943913, 146.4074606690158760 ) ) ;
#16959=CARTESIAN_POINT ( 'NONE',  ( 30.49012212078099893, -29.07017293858438478, 31.42300344396308631 ) ) ;
#16962=EDGE_CURVE ( 'NONE', #84319, #59024, #48939, .T. ) ;
#16974=CARTESIAN_POINT ( 'NONE',  ( 91.58819796920066381, -60.00000000000000000, -15.36446433908737319 ) ) ;
#16987=CARTESIAN_POINT ( 'NONE',  ( 84.09803781733121752, -45.28736737590700301, 1.238215950073735527 ) ) ;
#16991=MANIFOLD_SOLID_BREP ( 'Cut-Extrude3', #77348 ) ;
#16995=EDGE_LOOP ( 'NONE', ( #54580, #96182, #636, #29609 ) ) ;
#16997=CARTESIAN_POINT ( 'NONE',  ( -91.09125006954968740, -38.50546275171844712, 200.8230852611536932 ) ) ;
#17000=CARTESIAN_POINT ( 'NONE',  ( -35.51287843845796033, -60.00000000000001421, 39.56491211972655009 ) ) ;
#17002=CARTESIAN_POINT ( 'NONE',  ( 65.14337256760538253, -32.53026157264622498, 82.99388498196113062 ) ) ;
#17004=VERTEX_POINT ( 'NONE', #47881 ) ;
#17007=CARTESIAN_POINT ( 'NONE',  ( -83.74719587345013849, -57.67098913794580994, -27.91190304260424071 ) ) ;
#17017=AXIS2_PLACEMENT_3D ( 'NONE', #46218, #58416, #83733 ) ;
#17027=CARTESIAN_POINT ( 'NONE',  ( -91.19955518054493382, -29.99999999999999645, 190.5738738779320158 ) ) ;
#17031=CARTESIAN_POINT ( 'NONE',  ( 71.85927879119853401, -57.67665524272614164, 170.6229705935681409 ) ) ;
#17036=CARTESIAN_POINT ( 'NONE',  ( 23.83070367701998649, -27.26789081566746020, -38.40467348746060594 ) ) ;
#17039=CARTESIAN_POINT ( 'NONE',  ( -47.23625786575815511, -60.00000000000000000, 65.30679591831491848 ) ) ;
#17043=CARTESIAN_POINT ( 'NONE',  ( -86.96091939859486786, -35.41414515093074300, 188.0763737881594579 ) ) ;
#17046=CARTESIAN_POINT ( 'NONE',  ( -8.168619677412065627, -39.47607859267740338, 30.46221458393393888 ) ) ;
#17047=CARTESIAN_POINT ( 'NONE',  ( -102.3236051589763207, -60.00000000000002132, 193.7633069716393095 ) ) ;
#17059=CARTESIAN_POINT ( 'NONE',  ( 114.0149080866908946, -60.00000000000002132, 183.4845764411877553 ) ) ;
#17063=FACE_OUTER_BOUND ( 'NONE', #38412, .T. ) ;
#17079=B_SPLINE_CURVE_WITH_KNOTS ( 'NONE', 3,
 ( #83630, #9733, #42650, #67473, #59930, #92795 ),
 .UNSPECIFIED., .F., .F.,
 ( 4, 2, 4 ),
 ( 2.103915656028635642E-15, 0.01115854487611434888, 0.02231708975222659180 ),
 .UNSPECIFIED. ) ;
#17080=CARTESIAN_POINT ( 'NONE',  ( -40.83166867234564279, -60.00000000001944755, 57.76263198987851410 ) ) ;
#17083=CARTESIAN_POINT ( 'NONE',  ( 91.93227393908065892, -60.00000000000002842, 7.599392352668481010 ) ) ;
#17084=CARTESIAN_POINT ( 'NONE',  ( -80.78871696068775066, -30.00000000000004974, 192.9492619026495390 ) ) ;
#17085=CARTESIAN_POINT ( 'NONE',  ( 14.39634327219153143, -29.02992103934742474, 28.84133556504098905 ) ) ;
#17090=CARTESIAN_POINT ( 'NONE',  ( -43.50443149440654622, -22.24771747397159061, 37.57252092150835665 ) ) ;
#17093=CARTESIAN_POINT ( 'NONE',  ( -19.00223544648545015, -4.285714285714296246, 16.66764709352487017 ) ) ;
#17103=CARTESIAN_POINT ( 'NONE',  ( 78.27425760720375081, -30.00000000000000711, -15.63494901230772349 ) ) ;
#17109=CARTESIAN_POINT ( 'NONE',  ( 80.87643365138157492, -30.00000000000000711, 6.461220206471677052 ) ) ;
#17126=CARTESIAN_POINT ( 'NONE',  ( 81.60207891900830646, -38.84190146155946621, 195.4036435249389854 ) ) ;
#17141=UNCERTAINTY_MEASURE_WITH_UNIT (LENGTH_MEASURE( 1.000000000000000082E-05 ), #9670, 'distance_accuracy_value', 'NONE');
#17148=AXIS2_PLACEMENT_3D ( 'NONE', #101580, #27195, #36361 ) ;
#17150=CARTESIAN_POINT ( 'NONE',  ( 85.09886940956974399, -46.56413427295240837, 187.7708649785900832 ) ) ;
#17153=AXIS2_PLACEMENT_3D ( 'NONE', #79648, #5761, #48331 ) ;
#17156=CARTESIAN_POINT ( 'NONE',  ( 93.03188089276335404, -57.65588774053570376, -17.14181286654005376 ) ) ;
#17158=LINE ( 'NONE', #59741, #11025 ) ;
#17160=CARTESIAN_POINT ( 'NONE',  ( -81.59247734337886016, -30.00000000000000000, -7.117116539340933024 ) ) ;
#17173=EDGE_CURVE ( 'NONE', #4466, #105449, #33322, .T. ) ;
#17174=CARTESIAN_POINT ( 'NONE',  ( -96.81748461682487061, -38.00000000001091394, 192.8978395531862020 ) ) ;
#17179=CARTESIAN_POINT ( 'NONE',  ( -67.34689840167415298, -29.89196498055581230, -22.02968126997568632 ) ) ;
#17190=CARTESIAN_POINT ( 'NONE',  ( -76.04298135053677754, -59.99999999999997868, -30.12288092604498146 ) ) ;
#17194=CARTESIAN_POINT ( 'NONE',  ( 99.74981209804160187, -45.27117877547765801, 192.8220496481170585 ) ) ;
#17195=CARTESIAN_POINT ( 'NONE',  ( 31.97977251168731527, -31.54705716108501790, 32.42483364381936184 ) ) ;
#17209=CARTESIAN_POINT ( 'NONE',  ( -32.88842731267402542, -57.69106633777249016, 47.18465683205923966 ) ) ;
#17215=CARTESIAN_POINT ( 'NONE',  ( 2.769948622550640671, -30.00000000000000000, -40.00000000000000000 ) ) ;
#17217=CARTESIAN_POINT ( 'NONE',  ( -51.84566471874714466, -38.00000000000001421, 53.44666163652544100 ) ) ;
#17219=CARTESIAN_POINT ( 'NONE',  ( -49.20250961229047704, -46.44356504767149119, 51.70527583391724136 ) ) ;
#17223=CARTESIAN_POINT ( 'NONE',  ( -101.1758500044991820, -60.25291044919993055, 194.9948784670219766 ) ) ;
#17230=CARTESIAN_POINT ( 'NONE',  ( 80.05853955895231877, -38.78746072163605163, 193.1034648313674893 ) ) ;
#17237=CARTESIAN_POINT ( 'NONE',  ( 85.91789968996276627, -30.00000000000000000, 178.0337372095932835 ) ) ;
#17243=CARTESIAN_POINT ( 'NONE',  ( 53.00628815327823418, -49.90450768202155274, 60.14456217209944100 ) ) ;
#17248=CARTESIAN_POINT ( 'NONE',  ( -92.73019748878142821, -38.35494930991703200, 41.19300550259715266 ) ) ;
#17251=CARTESIAN_POINT ( 'NONE',  ( 98.52895140874336732, -38.35583712414237567, 79.77947616707253076 ) ) ;
#17253=CARTESIAN_POINT ( 'NONE',  ( 83.90565905403732927, -45.28278352932714768, 21.05830037911174202 ) ) ;
#17258=CARTESIAN_POINT ( 'NONE',  ( 75.51285980042941048, -59.99999999999997868, 184.5535044986175706 ) ) ;
#17261=CARTESIAN_POINT ( 'NONE',  ( 62.01696980690892502, -49.91133272125355091, 82.86793255174956130 ) ) ;
#17265=CARTESIAN_POINT ( 'NONE',  ( -83.01601276650154659, -38.35698986964714408, -24.47564496195118977 ) ) ;
#17276=CARTESIAN_POINT ( 'NONE',  ( 85.81319990892043847, -21.82339626730217930, 170.1690506418119355 ) ) ;
#17285=CARTESIAN_POINT ( 'NONE',  ( -18.75852657729457107, -25.38507213530491669, -38.49965030021739665 ) ) ;
#17291=CARTESIAN_POINT ( 'NONE',  ( 56.62629245603895356, -60.00000000000001421, 90.03670186600696468 ) ) ;
#17293=CARTESIAN_POINT ( 'NONE',  ( 29.05774046782589437, -21.22587610620614740, 31.99305267930822794 ) ) ;
#17294=CARTESIAN_POINT ( 'NONE',  ( -21.88691883039211561, -26.94070025036754856, 37.30577011176958990 ) ) ;
#17307=CARTESIAN_POINT ( 'NONE',  ( 19.18395041998931205, -47.40891687610037053, -34.01679967311604713 ) ) ;
#17317=CARTESIAN_POINT ( 'NONE',  ( -95.84732615451282811, -59.99999999999999289, 55.00258849229039981 ) ) ;
#17323=CARTESIAN_POINT ( 'NONE',  ( -82.57273120623599993, -46.48239456925677615, 176.6345680876003712 ) ) ;
#17341=CARTESIAN_POINT ( 'NONE',  ( 109.3240791159541345, -30.00000000000000000, 163.9544119406666596 ) ) ;
#17343=CARTESIAN_POINT ( 'NONE',  ( -106.9542266815933829, -14.21045842199434084, 174.0135369018153995 ) ) ;
#17344=CARTESIAN_POINT ( 'NONE',  ( -59.20415057809159265, -36.01949179644289956, 68.56425315889141814 ) ) ;
#17347=CARTESIAN_POINT ( 'NONE',  ( 105.9609827248825269, -59.99999999999754863, 201.5202930408333657 ) ) ;
#17350=CARTESIAN_POINT ( 'NONE',  ( 6.099794669406291447, -39.47249940446795335, 30.45861396544772859 ) ) ;
#17351=CARTESIAN_POINT ( 'NONE',  ( -99.88241335914844399, -45.26548971045986036, 130.2270573400364242 ) ) ;
#17357=CARTESIAN_POINT ( 'NONE',  ( -30.87285025321662602, -60.00000000000000000, 43.49705760221775819 ) ) ;
#17363=CARTESIAN_POINT ( 'NONE',  ( 8.521464936441633498, -0.000000000000000000, -14.76977913854613789 ) ) ;
#17369=CARTESIAN_POINT ( 'NONE',  ( 87.35463798683012726, -60.00000000000003553, 33.86768253245171678 ) ) ;
#17370=CARTESIAN_POINT ( 'NONE',  ( -32.97757523807047164, -36.02761452523677832, 33.68363220189284135 ) ) ;
#17372=CARTESIAN_POINT ( 'NONE',  ( 46.33896657480098469, -49.89527275971956755, 48.28554634053408989 ) ) ;
#17377=CARTESIAN_POINT ( 'NONE',  ( -80.00263769476747200, -38.78215726861950685, 192.9944101463111394 ) ) ;
#17381=CARTESIAN_POINT ( 'NONE',  ( 44.30795271925991585, -59.99999999999998579, 48.19995158061011153 ) ) ;
#17388=CARTESIAN_POINT ( 'NONE',  ( 110.0156358204719140, -59.99999999999999289, 143.5755394574415504 ) ) ;
#17392=CARTESIAN_POINT ( 'NONE',  ( -98.64861594025600766, -30.00000000000004619, 189.5816746752348365 ) ) ;
#17400=CARTESIAN_POINT ( 'NONE',  ( 80.00000000000000000, -52.00000000000000000, -21.09707704303352926 ) ) ;
#17406=CARTESIAN_POINT ( 'NONE',  ( 83.89049488352652872, -25.60224597872077013, 156.2394836556818518 ) ) ;
#17420=CARTESIAN_POINT ( 'NONE',  ( 87.01900733993701920, -57.36609141436630210, 193.9082884220253220 ) ) ;
#17443=CARTESIAN_POINT ( 'NONE',  ( 110.3719848560278365, -57.66928927736454114, 195.3984882421133307 ) ) ;
#17451=CARTESIAN_POINT ( 'NONE',  ( -75.41928457129522201, -60.00000000000000000, 184.0178555490668373 ) ) ;
#17454=CARTESIAN_POINT ( 'NONE',  ( -85.85852585477157106, -25.04863950330571143, 177.1364756427148848 ) ) ;
#17461=CARTESIAN_POINT ( 'NONE',  ( -83.10302969860578060, -37.77014383597931868, -10.04599949963776595 ) ) ;
#17471=CARTESIAN_POINT ( 'NONE',  ( -63.50642133866089978, -59.99999999999999289, -37.13819210229684842 ) ) ;
#17473=CARTESIAN_POINT ( 'NONE',  ( -70.96999627002507793, -39.48937251510619006, 105.0534544120589118 ) ) ;
#17475=CARTESIAN_POINT ( 'NONE',  ( 63.58274112560721392, -14.21045842199431242, 93.96243211080884805 ) ) ;
#17477=CARTESIAN_POINT ( 'NONE',  ( 94.69573144448894197, -57.66415873669975412, -4.953024160301185752 ) ) ;
#17487=CARTESIAN_POINT ( 'NONE',  ( 8.127057321558247338, -4.285714285714295357, -23.93420880016849139 ) ) ;
#17498=CARTESIAN_POINT ( 'NONE',  ( 32.84200068835146880, -56.84013278135907399, 37.45145004404182032 ) ) ;
#17502=CARTESIAN_POINT ( 'NONE',  ( 9.797174393178825657E-16, -15.00000000000000000, 8.000000000000000000 ) ) ;
#17505=CARTESIAN_POINT ( 'NONE',  ( 4.377363093174522650E-05, -49.99999999999997868, 32.22298329293570873 ) ) ;
#17511=CARTESIAN_POINT ( 'NONE',  ( 92.70420653547968470, -60.00000000000001421, -9.023355465272066667 ) ) ;
#17524=CARTESIAN_POINT ( 'NONE',  ( 87.03145172370204818, -60.20135443965438071, -7.696256136449998841 ) ) ;
#17537=ORIENTED_EDGE ( 'NONE', *, *, #14937, .F. ) ;
#17538=CARTESIAN_POINT ( 'NONE',  ( 76.34208424054833131, -46.43307427196572235, 131.9837883314934572 ) ) ;
#17542=CARTESIAN_POINT ( 'NONE',  ( -93.33808876947477984, -57.65441397348698160, -16.37300446327261128 ) ) ;
#17549=CARTESIAN_POINT ( 'NONE',  ( 106.2885998856441745, -60.15149245731204530, 179.7510284545313937 ) ) ;
#17563=CARTESIAN_POINT ( 'NONE',  ( 12.82717339738770512, -60.00000000000000000, 39.70944106662322781 ) ) ;
#17564=CARTESIAN_POINT ( 'NONE',  ( -88.45143479841831891, -29.99999999999999645, 187.7855393631011225 ) ) ;
#17565=EDGE_CURVE ( 'NONE', #35775, #25464, #42865, .T. ) ;
#17569=CARTESIAN_POINT ( 'NONE',  ( 70.40948563225279599, -57.68249254348480548, 157.3593782098396900 ) ) ;
#17573=CARTESIAN_POINT ( 'NONE',  ( 14.58136264770422130, -23.94594737508124993, -38.53227127598449187 ) ) ;
#17575=CARTESIAN_POINT ( 'NONE',  ( -46.72192845272360273, -59.99999999999999289, 64.17803650344802691 ) ) ;
#17578=CARTESIAN_POINT ( 'NONE',  ( -86.05365282663042592, -39.21241181629545736, 187.0849633868903084 ) ) ;
#17583=CARTESIAN_POINT ( 'NONE',  ( -10.08550511080940915, -22.06801976977802227, 27.57672000808223700 ) ) ;
#17594=DIRECTION ( 'NONE',  ( -0.000000000000000000, -1.000000000000000000, -0.000000000000000000 ) ) ;
#17598=CARTESIAN_POINT ( 'NONE',  ( 109.3240791159541345, -30.00000000000000000, 163.9544119406666596 ) ) ;
#17599=CARTESIAN_POINT ( 'NONE',  ( -83.92326679681109169, -29.05553059583932907, 161.8043818697931897 ) ) ;
#17618=CARTESIAN_POINT ( 'NONE',  ( 96.95221799863543310, -60.00000000000002132, 202.4789020112573610 ) ) ;
#17620=CARTESIAN_POINT ( 'NONE',  ( -98.15060533238310825, -14.21045842199422715, 197.6136055373540614 ) ) ;
#17621=CARTESIAN_POINT ( 'NONE',  ( 14.50450630449079092, -35.99182772622528859, 30.00711302977329709 ) ) ;
#17625=CARTESIAN_POINT ( 'NONE',  ( -42.47994433708600326, -49.89231707659487824, 43.43423702368624362 ) ) ;
#17639=CARTESIAN_POINT ( 'NONE',  ( 69.85629772084516276, -29.99999999999997868, 125.7656138327989481 ) ) ;
#17643=CARTESIAN_POINT ( 'NONE',  ( 80.91584140846381956, -30.00000000000000000, 5.600791395715724263 ) ) ;
#17656=CARTESIAN_POINT ( 'NONE',  ( 74.78018824853795365, -38.33359745921677586, 167.4195336213977328 ) ) ;
#17660=ORIENTED_EDGE ( 'NONE', *, *, #6606, .F. ) ;
#17669=DIRECTION ( 'NONE',  ( 1.000000000000000000, -0.000000000000000000, 1.224646799147353207E-16 ) ) ;
#17677=CARTESIAN_POINT ( 'NONE',  ( 84.08575072203289835, -61.04859098016596874, 192.4284686294917321 ) ) ;
#17680=CARTESIAN_POINT ( 'NONE',  ( 83.51201917109111150, -57.67104594142430329, -28.06691757407987708 ) ) ;
#17685=CARTESIAN_POINT ( 'NONE',  ( -80.78186281600028451, -30.00000000000000000, 9.678833486316271717 ) ) ;
#17707=CARTESIAN_POINT ( 'NONE',  ( -38.88645629453070285, -24.53144980621419080, -30.52333081557608097 ) ) ;
#17709=CARTESIAN_POINT ( 'NONE',  ( -71.72561805443079663, -34.58960680145646194, -21.02611375570996444 ) ) ;
#17715=CARTESIAN_POINT ( 'NONE',  ( -63.73407763263179504, -60.00000000000000711, -34.61716371171238649 ) ) ;
#17719=CARTESIAN_POINT ( 'NONE',  ( 102.1330484602042787, -60.20162503959858213, 194.0437069272821873 ) ) ;
#17737=CARTESIAN_POINT ( 'NONE',  ( -71.68202686650683120, -57.67896093159416893, 168.8233993379761557 ) ) ;
#17743=CARTESIAN_POINT ( 'NONE',  ( -87.60281504538382080, -14.21045842199439946, -3.799590761493521374 ) ) ;
#17747=CARTESIAN_POINT ( 'NONE',  ( -49.98625063665457446, -18.73833733594818085, 43.94435920909415927 ) ) ;
#17755=CARTESIAN_POINT ( 'NONE',  ( 84.77133682389549563, -38.71704634458406957, 198.3318700654770339 ) ) ;
#17760=CARTESIAN_POINT ( 'NONE',  ( 92.71251373007059726, -30.00000000000000355, 191.0549262315104784 ) ) ;
#17770=CARTESIAN_POINT ( 'NONE',  ( 51.29641226325185954, -18.72494439718292369, 45.83502416631164067 ) ) ;
#17775=CARTESIAN_POINT ( 'NONE',  ( -90.68311849838809735, -38.34324579396269428, 8.149761933289237703 ) ) ;
#17776=ORIENTED_EDGE ( 'NONE', *, *, #81707, .T. ) ;
#17778=CARTESIAN_POINT ( 'NONE',  ( 108.4115401993842340, -38.35734607969845911, 191.8602404080995996 ) ) ;
#17780=CARTESIAN_POINT ( 'NONE',  ( 87.59251117718669377, -37.84866951032316251, 63.63991520629491561 ) ) ;
#17786=CARTESIAN_POINT ( 'NONE',  ( 74.84415321082225603, -59.99999999999998579, 180.0616514280479805 ) ) ;
#17790=CARTESIAN_POINT ( 'NONE',  ( 61.45962890681138902, -36.01090048717188097, 74.41309228244647045 ) ) ;
#17803=CARTESIAN_POINT ( 'NONE',  ( 83.33281023015626943, -50.09872871951235851, 184.7185439448685429 ) ) ;
#17806=ORIENTED_EDGE ( 'NONE', *, *, #22347, .F. ) ;
#17813=CARTESIAN_POINT ( 'NONE',  ( -36.94718896193312219, -31.97723873816721962, -37.72039704602598675 ) ) ;
#17817=CARTESIAN_POINT ( 'NONE',  ( 53.83222069280748201, -59.99999999999999289, 81.95787437923988250 ) ) ;
#17822=CARTESIAN_POINT ( 'NONE',  ( -17.86182390064972481, -24.36647526511750073, 36.39771317331339162 ) ) ;
#17830=CARTESIAN_POINT ( 'NONE',  ( 6.976419320225629050, -21.93239868286991978, -38.54500339651450247 ) ) ;
#17839=CARTESIAN_POINT ( 'NONE',  ( 31.96770739188477251, -47.40888721812473960, -32.79511155121236499 ) ) ;
#17848=CARTESIAN_POINT ( 'NONE',  ( -95.31672547844928545, -59.99999999999999289, 51.31686920618464143 ) ) ;
#17855=CARTESIAN_POINT ( 'NONE',  ( -85.16085110908363731, -25.44750803484134138, 168.5012799068713321 ) ) ;
#17872=CARTESIAN_POINT ( 'NONE',  ( 98.48959774644481513, -29.99999999999997158, 87.89110648026155559 ) ) ;
#17874=CARTESIAN_POINT ( 'NONE',  ( -78.82101707352518360, -14.21045842199447584, 187.8153594499050882 ) ) ;
#17875=CARTESIAN_POINT ( 'NONE',  ( -57.46856647868230539, -53.38719169883287208, 72.11333812933901299 ) ) ;
#17877=CARTESIAN_POINT ( 'NONE',  ( 19.61534071737431617, -60.00000000000000000, -44.23451022601076232 ) ) ;
#17879=CARTESIAN_POINT ( 'NONE',  ( 7.255345346424188158, -56.87783837489315886, 33.35968231048251909 ) ) ;
#17880=CARTESIAN_POINT ( 'NONE',  ( -106.4736054431515839, -60.15535417407983232, 175.2096886785453478 ) ) ;
#17889=CARTESIAN_POINT ( 'NONE',  ( -51.57713148613659371, -59.99999999999998579, 75.78954276384915545 ) ) ;
#17900=CARTESIAN_POINT ( 'NONE',  ( 86.12345145597880958, -60.00000000000003553, 8.975931401546647592 ) ) ;
#17902=CARTESIAN_POINT ( 'NONE',  ( -30.84686216097265898, -36.01813085627019007, 32.80772232543694145 ) ) ;
#17903=CARTESIAN_POINT ( 'NONE',  ( 45.00016045444848345, -56.79933079351206970, 48.30642181785263034 ) ) ;
#17908=CARTESIAN_POINT ( 'NONE',  ( -80.97742334477548809, -38.83260288647188219, 194.5685436216422204 ) ) ;
#17918=CARTESIAN_POINT ( 'NONE',  ( 108.9248648557860975, -60.00000000000000000, 135.4428396493478886 ) ) ;
#17925=CARTESIAN_POINT ( 'NONE',  ( -89.28786161495364126, -30.00000000000018474, 189.1170264501615463 ) ) ;
#17933=PRODUCT_DEFINITION ( 'UNKNOWN', '', #54222, #75839 ) ;
#17937=CARTESIAN_POINT ( 'NONE',  ( 80.20348483770095527, -60.38397368176433133, 177.1131073836802159 ) ) ;
#17951=CARTESIAN_POINT ( 'NONE',  ( 87.35329077437620526, -35.37253959560227656, 188.8831662968735827 ) ) ;
#17962=DIRECTION ( 'NONE',  ( 0.000000000000000000, 1.000000000000000000, 0.000000000000000000 ) ) ;
#17972=CARTESIAN_POINT ( 'NONE',  ( 112.5994561246894818, -57.67111607657447081, 189.2784257370963701 ) ) ;
#17976=CARTESIAN_POINT ( 'NONE',  ( -76.90050140379315735, -60.00000000000000000, 190.1576257827158827 ) ) ;
#17980=CARTESIAN_POINT ( 'NONE',  ( -84.00592508910983724, -50.16348015376611613, 186.9351520424663704 ) ) ;
#17990=CARTESIAN_POINT ( 'NONE',  ( -86.89782577854842316, -60.22521776081720901, -10.09765860210499788 ) ) ;
#17997=CARTESIAN_POINT ( 'NONE',  ( 68.63284294399571195, -59.99999999999999289, 147.4025539660169954 ) ) ;
#18000=CARTESIAN_POINT ( 'NONE',  ( 2.769948622550640671, -30.00000000000000000, -40.00000000000000000 ) ) ;
#18001=CARTESIAN_POINT ( 'NONE',  ( -68.23005283090677153, -25.58391158071819405, 88.38719919826223759 ) ) ;
#18003=CARTESIAN_POINT ( 'NONE',  ( 78.64960161195060095, -14.21045842199435860, 174.1843170503133251 ) ) ;
#18005=CARTESIAN_POINT ( 'NONE',  ( 94.33413934944054802, -57.67234579118471061, 0.7340641395501579236 ) ) ;
#18024=CARTESIAN_POINT ( 'NONE',  ( 32.29284039994544742, -29.08409890041876977, 32.09482466030329562 ) ) ;
#18043=CARTESIAN_POINT ( 'NONE',  ( 80.91250902992011618, -60.00000000000000000, -27.39157300925418781 ) ) ;
#18058=CARTESIAN_POINT ( 'NONE',  ( 82.43496726913153339, -37.80750666079145361, -12.82402668043966720 ) ) ;
#18070=CARTESIAN_POINT ( 'NONE',  ( 77.27749820069621478, -36.02219164018512743, 127.9092550732632816 ) ) ;
#18076=CARTESIAN_POINT ( 'NONE',  ( -94.13300556333170732, -57.67265947060198528, 21.91134835779649137 ) ) ;
#18079=CARTESIAN_POINT ( 'NONE',  ( 105.1830448132046030, -52.71715498403217026, 168.1466463903639976 ) ) ;
#18087=CARTESIAN_POINT ( 'NONE',  ( 97.53417911421176711, -56.34822196449098897, 195.8862142079233024 ) ) ;
#18095=CARTESIAN_POINT ( 'NONE',  ( -84.27187814110018849, -30.00000000000000355, 163.4558213934668061 ) ) ;
#18102=CARTESIAN_POINT ( 'NONE',  ( 70.53489761712432937, -57.68241810049395468, 158.3663422263703637 ) ) ;
#18106=CARTESIAN_POINT ( 'NONE',  ( 54.68240138874981682, -36.51280362385794120, -35.33638688103538072 ) ) ;
#18109=CARTESIAN_POINT ( 'NONE',  ( -32.93660888375947593, -60.00000000000000711, 44.79872838179039007 ) ) ;
#18115=CARTESIAN_POINT ( 'NONE',  ( -86.52299692828317745, -31.80693871344314516, 185.9752520618245057 ) ) ;
#18118=CARTESIAN_POINT ( 'NONE',  ( -10.15792624425911050, -29.03126705412632447, 28.73829528188013072 ) ) ;
#18132=CARTESIAN_POINT ( 'NONE',  ( 106.8726675771063981, -14.21045842199433729, 167.8793401222494595 ) ) ;
#18133=CARTESIAN_POINT ( 'NONE',  ( -82.67280634349272361, -29.09043949173138444, 151.5834487444393517 ) ) ;
#18147=CARTESIAN_POINT ( 'NONE',  ( -89.99999999999997158, -52.00000000000000000, 196.0238439516549818 ) ) ;
#18154=CARTESIAN_POINT ( 'NONE',  ( 99.73874981799322370, -59.99999999999998579, 201.9620565075520062 ) ) ;
#18155=CARTESIAN_POINT ( 'NONE',  ( -78.18420296597048491, -29.99999999999999645, 185.0796872551976548 ) ) ;
#18156=CARTESIAN_POINT ( 'NONE',  ( 23.68178223146766470, -39.47564461994503660, 31.49583778405278522 ) ) ;
#18159=CARTESIAN_POINT ( 'NONE',  ( -42.72860860146450790, -29.16005040975862883, 38.64535797928981964 ) ) ;
#18170=ORIENTED_EDGE ( 'NONE', *, *, #21665, .F. ) ;
#18172=CARTESIAN_POINT ( 'NONE',  ( 79.32260940021335216, -29.99999999999999289, -14.62515576484859459 ) ) ;
#18176=CARTESIAN_POINT ( 'NONE',  ( 80.76767570714686428, -30.00000000000000355, 10.72804306168430344 ) ) ;
#18177=EDGE_CURVE ( 'NONE', #81125, #27380, #16607, .T. ) ;
#18195=CARTESIAN_POINT ( 'NONE',  ( 69.20520435146650584, -38.33177068396069131, 130.8227709917701986 ) ) ;
#18218=DIRECTION ( 'NONE',  ( 0.000000000000000000, -1.000000000000000000, 0.000000000000000000 ) ) ;
#18221=CARTESIAN_POINT ( 'NONE',  ( 85.88695608651612190, -35.61023455811969285, 185.0182596836982043 ) ) ;
#18224=CARTESIAN_POINT ( 'NONE',  ( 90.07482630527962897, -57.66626241257390006, -22.18633397614781799 ) ) ;
#18229=CARTESIAN_POINT ( 'NONE',  ( -81.90312948688070094, -29.99999999999999645, 32.95728417534301968 ) ) ;
#18242=CARTESIAN_POINT ( 'NONE',  ( 12.17407353652991908, -16.62868128721872196, -34.62501512136454807 ) ) ;
#18244=CARTESIAN_POINT ( 'NONE',  ( -24.11972882727333456, -53.39844759095379345, 33.93414205717319732 ) ) ;
#18249=CARTESIAN_POINT ( 'NONE',  ( -66.76684803170716975, -29.86276467274606361, -22.29546326141434065 ) ) ;
#18251=CARTESIAN_POINT ( 'NONE',  ( -65.51163020881617172, -21.77008787170778703, -21.27136415489606236 ) ) ;
#18266=CARTESIAN_POINT ( 'NONE',  ( 100.1542774294340887, -45.27487897115133109, 192.4539520511120827 ) ) ;
#18283=CARTESIAN_POINT ( 'NONE',  ( -49.73192663144240555, -57.67846088945594829, 76.49129250627629517 ) ) ;
#18288=CARTESIAN_POINT ( 'NONE',  ( -90.14748428319414586, -30.00000000000004263, -6.309121115244137101 ) ) ;
#18290=CARTESIAN_POINT ( 'NONE',  ( -52.30004809150737799, -25.64534318506951038, 49.83580167134282135 ) ) ;
#18298=CARTESIAN_POINT ( 'NONE',  ( 76.35497413732163352, -38.40080420323430133, 180.8501158277027798 ) ) ;
#18304=CARTESIAN_POINT ( 'NONE',  ( 85.96311599642660894, -30.00000000000000000, 178.3436844846160909 ) ) ;
#18311=CARTESIAN_POINT ( 'NONE',  ( 53.53308456940848004, -36.03345146573957436, 55.90449180736266044 ) ) ;
#18316=CARTESIAN_POINT ( 'NONE',  ( -91.45024945953299778, -38.38939539467013873, -7.873147340154297957 ) ) ;
#18320=CARTESIAN_POINT ( 'NONE',  ( 108.5189666034069660, -38.35713193670694210, 191.5735787013350375 ) ) ;
#18322=CARTESIAN_POINT ( 'NONE',  ( 84.87915795533969288, -45.28284344526540650, 33.56703465616141102 ) ) ;
#18325=CARTESIAN_POINT ( 'NONE',  ( 0.000000000000000000, -8.000000000000000000, 0.000000000000000000 ) ) ;
#18330=CARTESIAN_POINT ( 'NONE',  ( 61.87539551481160771, -29.06099552529470031, 72.15998440305089900 ) ) ;
#18341=CARTESIAN_POINT ( 'NONE',  ( -29.46142920806810395, -21.41144172159147985, 31.99227660533023609 ) ) ;
#18347=CARTESIAN_POINT ( 'NONE',  ( 85.94436667923068285, -21.71192462058850836, 172.2505468594992806 ) ) ;
#18356=CARTESIAN_POINT ( 'NONE',  ( -29.75089728405549749, -29.48423827979404876, -38.19276141328201390 ) ) ;
#18358=CARTESIAN_POINT ( 'NONE',  ( 43.93350074023148011, -60.00000000000001421, 58.56064191452826151 ) ) ;
#18361=CARTESIAN_POINT ( 'NONE',  ( 10.44871243568134922, -13.87974197187156555, 31.87097697359232740 ) ) ;
#18362=EDGE_CURVE ( 'NONE', #25464, #98077, #17158, .T. ) ;
#18363=CARTESIAN_POINT ( 'NONE',  ( -31.88880264354962435, -33.67810866067220843, 41.75912053304347182 ) ) ;
#18376=CARTESIAN_POINT ( 'NONE',  ( 37.82333364650842356, -34.58951055744512360, -29.84593800095458604 ) ) ;
#18379=DIRECTION ( 'NONE',  ( -3.673940397442057649E-17, 0.000000000000000000, -1.000000000000000000 ) ) ;
#18386=CARTESIAN_POINT ( 'NONE',  ( -103.7190351099681891, -59.99999999999999289, 102.7930850803005711 ) ) ;
#18394=CARTESIAN_POINT ( 'NONE',  ( -80.66956869714498168, -60.45664881771811139, 181.0067086544060260 ) ) ;
#18411=CARTESIAN_POINT ( 'NONE',  ( 99.89428240326108721, -30.00000000000003908, 96.08155976150675315 ) ) ;
#18412=CARTESIAN_POINT ( 'NONE',  ( -100.5643661290868209, -60.00000000000009237, 204.3458358344470582 ) ) ;
#18413=CARTESIAN_POINT ( 'NONE',  ( -58.02850647072168755, -42.96756333752487933, 68.81541298771311688 ) ) ;
#18416=CARTESIAN_POINT ( 'NONE',  ( 44.67209098260076416, -60.00000000002891198, -41.28851062587111898 ) ) ;
#18419=CARTESIAN_POINT ( 'NONE',  ( -104.0167802882961610, -45.26538512285915772, 170.3650450961504248 ) ) ;
#18426=CARTESIAN_POINT ( 'NONE',  ( -79.00733982898046293, -60.00000000000002132, 194.6382242294647824 ) ) ;
#18433=CARTESIAN_POINT ( 'NONE',  ( 81.98192093697382177, -38.00000000001091394, -13.86368299876859567 ) ) ;
#18439=CARTESIAN_POINT ( 'NONE',  ( -31.37200766108269434, -46.43604509162865668, 34.89251725904698276 ) ) ;
#18441=CARTESIAN_POINT ( 'NONE',  ( 44.74630639848560065, -39.52738033063129564, 43.35887041975919942 ) ) ;
#18445=CARTESIAN_POINT ( 'NONE',  ( -81.76979430546906258, -38.84151416488224129, 195.6111116689327218 ) ) ;
#18449=CARTESIAN_POINT ( 'NONE',  ( 80.12066730003955684, -60.00000000000016342, 175.6537320670710187 ) ) ;
#18457=CARTESIAN_POINT ( 'NONE',  ( 103.6220394604206092, -60.00000000000001421, 102.2245821222708315 ) ) ;
#18464=CARTESIAN_POINT ( 'NONE',  ( -81.01065487345596239, -30.00000000000003197, -11.84759136933223012 ) ) ;
#18474=CARTESIAN_POINT ( 'NONE',  ( 82.82994579733494334, -36.01735634948035170, 162.7126334183690517 ) ) ;
#18491=CARTESIAN_POINT ( 'NONE',  ( 87.06637252711929875, -50.08904605173307090, 191.9841204601254958 ) ) ;
#18492=EDGE_CURVE ( 'NONE', #44460, #18895, #33467, .T. ) ;
#18497=CARTESIAN_POINT ( 'NONE',  ( -10.00000000000000178, 0.000000000000000000, -9.999999999999998224 ) ) ;
#18502=DIRECTION ( 'NONE',  ( 0.000000000000000000, 0.000000000000000000, 1.000000000000000000 ) ) ;
#18517=CARTESIAN_POINT ( 'NONE',  ( -85.35784636269366388, -60.00000000000000000, 200.2676956853971717 ) ) ;
#18522=CARTESIAN_POINT ( 'NONE',  ( -85.13125407531725841, -35.77895824004616543, 181.7330530824042967 ) ) ;
#18528=CARTESIAN_POINT ( 'NONE',  ( -86.27499340120317584, -60.13461745695511951, 5.971924282842688392 ) ) ;
#18536=CARTESIAN_POINT ( 'NONE',  ( 51.40679407232553899, -29.99999999999998934, 68.09281640667435909 ) ) ;
#18538=CARTESIAN_POINT ( 'NONE',  ( -87.30967359867977962, -14.21045842199447229, 28.19474181966119275 ) ) ;
#18539=CARTESIAN_POINT ( 'NONE',  ( -76.54952089020632400, -22.13347653070191257, 114.5436684493959660 ) ) ;
#18541=CARTESIAN_POINT ( 'NONE',  ( 62.45579587598661675, -29.99999999999998934, 99.43503315974342627 ) ) ;
#18544=CARTESIAN_POINT ( 'NONE',  ( 55.63191178850256335, -57.67115282173337931, -38.73449349589243695 ) ) ;
#18569=CARTESIAN_POINT ( 'NONE',  ( 31.61125088838073793, -22.14068077173801541, 30.54052087820161887 ) ) ;
#18585=CARTESIAN_POINT ( 'NONE',  ( 82.44953616767962501, -60.00000000000000711, -26.43629379952842839 ) ) ;
#18600=CARTESIAN_POINT ( 'NONE',  ( 84.20945289264685130, -45.27999795687735940, -10.90044817620680284 ) ) ;
#18606=ORIENTED_EDGE ( 'NONE', *, *, #66304, .F. ) ;
#18612=CARTESIAN_POINT ( 'NONE',  ( 70.72083910363338077, -42.95977585387966968, 106.3012996167854141 ) ) ;
#18617=CARTESIAN_POINT ( 'NONE',  ( -89.88826151057727998, -57.66708741322880627, -22.42023280972025390 ) ) ;
#18622=CARTESIAN_POINT ( 'NONE',  ( 101.9416562456032267, -37.84849355845468466, 184.3864726907910097 ) ) ;
#18640=CARTESIAN_POINT ( 'NONE',  ( -88.08998614599749999, -29.99999999999999645, 186.9891332546852141 ) ) ;
#18646=CARTESIAN_POINT ( 'NONE',  ( 70.60288179947629317, -57.68235211279129260, 158.9257230075169502 ) ) ;
#18650=CARTESIAN_POINT ( 'NONE',  ( 49.88420474661570836, -35.54202973682257038, -36.18076981765180733 ) ) ;
#18654=CARTESIAN_POINT ( 'NONE',  ( -32.71478493902962725, -59.99999999999998579, 44.64407865478428761 ) ) ;
#18661=CARTESIAN_POINT ( 'NONE',  ( -85.99455140606450243, -46.52813070295108133, 189.5206154160531185 ) ) ;
#18664=CARTESIAN_POINT ( 'NONE',  ( -3.030330602040952392, -39.47594121070261508, 30.46411644868683766 ) ) ;
#18666=CARTESIAN_POINT ( 'NONE',  ( 85.08140087618613734, -52.74747956140128480, 190.3168375061761424 ) ) ;
#18679=CARTESIAN_POINT ( 'NONE',  ( 101.4322121444104852, -14.21045842199439235, 121.1820579999150738 ) ) ;
#18680=CARTESIAN_POINT ( 'NONE',  ( -81.58075026974830735, -36.03152022319830650, 152.4545240145561422 ) ) ;
#18684=CARTESIAN_POINT ( 'NONE',  ( 47.79234619673301410, -57.68000456042641844, 71.60442412587305228 ) ) ;
#18699=CARTESIAN_POINT ( 'NONE',  ( 96.25432131042047956, -59.99999999999998579, 57.89339241846288076 ) ) ;
#18700=CARTESIAN_POINT ( 'NONE',  ( -84.52733067048065152, -59.99999999999991473, 202.7036346196431111 ) ) ;
#18701=CARTESIAN_POINT ( 'NONE',  ( 21.32256896959740899, -39.47421529476722668, 31.13554192005910792 ) ) ;
#18703=CARTESIAN_POINT ( 'NONE',  ( 82.11590029501883237, -38.00000000000000000, -13.62443290218705627 ) ) ;
#18706=CARTESIAN_POINT ( 'NONE',  ( -39.71717478528384504, -29.14735779400208671, 36.19107066650675364 ) ) ;
#18710=CARTESIAN_POINT ( 'NONE',  ( -11.17734400176827414, -4.285714285714296246, 22.67073868809948678 ) ) ;
#18721=CARTESIAN_POINT ( 'NONE',  ( 96.97070535361069687, -30.00000000000008882, 191.0996011186520320 ) ) ;
#18725=CARTESIAN_POINT ( 'NONE',  ( 81.98815504130990917, -30.00000000000000355, 33.82435566842140418 ) ) ;
#18746=CARTESIAN_POINT ( 'NONE',  ( 74.34077940264843676, -38.32857108130681922, 163.3424694308657763 ) ) ;
#18770=CARTESIAN_POINT ( 'NONE',  ( 86.16337931003708661, -28.29594558851139041, 183.0065083202355538 ) ) ;
#18774=ORIENTED_EDGE ( 'NONE', *, *, #83208, .F. ) ;
#18775=CARTESIAN_POINT ( 'NONE',  ( 2.435347819570957628E-07, -57.67120202539301488, -44.61186700419775519 ) ) ;
#18776=DIRECTION ( 'NONE',  ( 0.000000000000000000, 1.000000000000000000, 0.000000000000000000 ) ) ;
#18779=CARTESIAN_POINT ( 'NONE',  ( -81.82247036775113713, -30.00000000000000355, 32.11225174614141054 ) ) ;
#18788=CARTESIAN_POINT ( 'NONE',  ( -47.03242928956601787, -37.42254165723339554, 45.62446206611129895 ) ) ;
#18793=CARTESIAN_POINT ( 'NONE',  ( 54.41739748717052549, -28.39686699294333749, -26.76204183714953544 ) ) ;
#18796=CARTESIAN_POINT ( 'NONE',  ( -22.40161616653207233, -35.99812881269021148, 30.71311989447094959 ) ) ;
#18800=CARTESIAN_POINT ( 'NONE',  ( -16.95911990754058607, -49.92065424304449550, 32.46463353416660880 ) ) ;
#18801=CARTESIAN_POINT ( 'NONE',  ( -47.26583134274487463, -26.85017121223957659, -28.66095955266838757 ) ) ;
#18804=CARTESIAN_POINT ( 'NONE',  ( -72.96315109214474148, -34.58961219393635389, -20.39832908442921422 ) ) ;
#18817=CARTESIAN_POINT ( 'NONE',  ( 99.43428100118596547, -37.82682717057377886, 191.4305896544213681 ) ) ;
#18818=CARTESIAN_POINT ( 'NONE',  ( 11.37552658721364196, -21.18656163614519627, 27.44809313948756113 ) ) ;
#18821=EDGE_CURVE ( 'NONE', #26612, #105826, #10955, .T. ) ;
#18831=CARTESIAN_POINT ( 'NONE',  ( -94.82011412385188009, -59.99999999999028688, -11.94472248813712589 ) ) ;
#18835=CARTESIAN_POINT ( 'NONE',  ( -84.89308075164642275, -60.00000000000002842, -27.59301604020478038 ) ) ;
#18838=CARTESIAN_POINT ( 'NONE',  ( -50.73354104550973886, -60.30528530471388393, 59.32307533831818347 ) ) ;
#18842=CARTESIAN_POINT ( 'NONE',  ( -94.84365371199864114, -45.25270723803333084, 194.1674599023730536 ) ) ;
#18848=CARTESIAN_POINT ( 'NONE',  ( 102.9968910219542693, -38.42918772397359817, 199.1158771562406571 ) ) ;
#18853=CARTESIAN_POINT ( 'NONE',  ( 85.96011442332530805, -30.00000000000000000, 178.3233229589895643 ) ) ;
#18860=CARTESIAN_POINT ( 'NONE',  ( 52.27629109544965758, -56.83866631114189971, 61.26715463662765870 ) ) ;
#18865=CARTESIAN_POINT ( 'NONE',  ( -85.43365283625350060, -38.35985798731113050, -22.44808446743328290 ) ) ;
#18869=CARTESIAN_POINT ( 'NONE',  ( 106.8967157683483720, -38.36539324343537061, 195.0206876434428409 ) ) ;
#18871=CARTESIAN_POINT ( 'NONE',  ( 86.56679986176000341, -60.14582403643369446, 24.17458394031839930 ) ) ;
#18872=DIRECTION ( 'NONE',  ( 0.000000000000000000, 1.000000000000000000, 0.000000000000000000 ) ) ;
#18895=VERTEX_POINT ( 'NONE', #71391 ) ;
#18896=CARTESIAN_POINT ( 'NONE',  ( 81.41390920051752289, -60.59005278335753530, 185.5272298782579128 ) ) ;
#18899=CARTESIAN_POINT ( 'NONE',  ( -86.56297675702614924, -52.70887369560592361, 37.65507028047760940 ) ) ;
#18903=CARTESIAN_POINT ( 'NONE',  ( -22.71182892702813660, -26.84646812124476156, -38.43211124454622762 ) ) ;
#18907=CARTESIAN_POINT ( 'NONE',  ( 41.69006022411431189, -59.99999999999999289, 54.65678614846827088 ) ) ;
#18909=CARTESIAN_POINT ( 'NONE',  ( 25.87313031554646514, -29.63673128196639084, 38.60121535671525095 ) ) ;
#18912=CARTESIAN_POINT ( 'NONE',  ( -29.99396172607142574, -32.44667869317692777, 40.57082760664052756 ) ) ;
#18928=CARTESIAN_POINT ( 'NONE',  ( 15.77584606617254614, -34.58953296166827585, -32.12825160005380098 ) ) ;
#18939=CARTESIAN_POINT ( 'NONE',  ( -92.23598523486838019, -60.00000000000001421, 2.395111321838569118 ) ) ;
#18946=CARTESIAN_POINT ( 'NONE',  ( -81.53213380329533777, -53.46540947967974233, 178.0948321718499017 ) ) ;
#18957=CARTESIAN_POINT ( 'NONE',  ( 2.435348425596516081E-07, -57.67120202539301488, -44.61186700419774098 ) ) ;
#18961=CARTESIAN_POINT ( 'NONE',  ( 0.000000000000000000, 30.00000000000000000, 0.000000000000000000 ) ) ;
#18963=CARTESIAN_POINT ( 'NONE',  ( 97.37780541404315215, -14.21045842199443143, 96.97658560636448044 ) ) ;
#18964=CARTESIAN_POINT ( 'NONE',  ( -75.52856519143354319, -59.99999999999994316, 193.8568173627997737 ) ) ;
#18965=CARTESIAN_POINT ( 'NONE',  ( -60.37025287372667748, -29.06875052076281563, 68.28797770161614267 ) ) ;
#18969=CARTESIAN_POINT ( 'NONE',  ( -106.0471509648365043, -60.15506806661914396, 181.9131953650650360 ) ) ;
#18974=CARTESIAN_POINT ( 'NONE',  ( -48.42784265545724764, -59.99999999999998579, 67.95292345526354438 ) ) ;
#18979=CARTESIAN_POINT ( 'NONE',  ( 16.90642566761063748, 0.000000000000000000, -2.220638482676887460 ) ) ;
#18987=CARTESIAN_POINT ( 'NONE',  ( -29.28896430935111184, -29.06400796251119445, 31.04148615219279250 ) ) ;
#18991=CARTESIAN_POINT ( 'NONE',  ( 45.59211296353198861, -46.43827376306629162, 46.30565985479245228 ) ) ;
#18996=CARTESIAN_POINT ( 'NONE',  ( -97.05521031604199322, -38.48254110268376849, 201.1230655224092629 ) ) ;
#19000=CARTESIAN_POINT ( 'NONE',  ( 74.61050274188295361, -60.00000000000002132, 134.6572766532755452 ) ) ;
#19007=CARTESIAN_POINT ( 'NONE',  ( 112.1757562388903722, -59.99999999999998579, 169.0180869050140302 ) ) ;
#19015=CARTESIAN_POINT ( 'NONE',  ( -80.36397934127951714, -30.00000000000006040, -13.26667358045050271 ) ) ;
#19018=CARTESIAN_POINT ( 'NONE',  ( -80.12540570148722452, -38.79873096281602329, 193.2784058327983416 ) ) ;
#19030=CARTESIAN_POINT ( 'NONE',  ( 82.39744891461782572, -39.49350758968277830, 164.1889903970027262 ) ) ;
#19046=CARTESIAN_POINT ( 'NONE',  ( 87.13380744255303512, -42.76071740017988532, 190.1415511809839245 ) ) ;
#19071=CARTESIAN_POINT ( 'NONE',  ( -111.0088745510421262, -60.00000000000000000, 187.2406379443718833 ) ) ;
#19075=CARTESIAN_POINT ( 'NONE',  ( -85.67509731226019198, -28.57511156689592724, 179.3357466346379852 ) ) ;
#19082=CARTESIAN_POINT ( 'NONE',  ( -85.20477662574127464, -52.70491138971408418, 3.232116785323828623 ) ) ;
#19089=CARTESIAN_POINT ( 'NONE',  ( 57.26188992556405566, -30.00000000000000355, 83.64747613098029433 ) ) ;
#19091=CARTESIAN_POINT ( 'NONE',  ( -85.55948822751662419, -29.99999999999991829, -20.40846083852196813 ) ) ;
#19092=CARTESIAN_POINT ( 'NONE',  ( -72.46402628313448702, -18.64347544987403182, 97.55464540977230570 ) ) ;
#19094=CARTESIAN_POINT ( 'NONE',  ( 100.7999351731576354, -29.99999999999990763, 198.8735152728553999 ) ) ;
#19096=CARTESIAN_POINT ( 'NONE',  ( 38.84142322586829721, -60.00000000000980549, 54.50522279198219167 ) ) ;
#19103=PRODUCT ( '1. Base', '1. Base', '', ( #74044 ) ) ;
#19108=CARTESIAN_POINT ( 'NONE',  ( -36.33885736213258610, -59.99999999999506173, 51.14030269516670302 ) ) ;
#19121=CARTESIAN_POINT ( 'NONE',  ( 33.60426306485480552, -53.36599767116988602, 37.21245143418115475 ) ) ;
#19123=CARTESIAN_POINT ( 'NONE',  ( 12.70248734011628500, -4.285714285714347760, 22.03900363279280583 ) ) ;
#19137=CARTESIAN_POINT ( 'NONE',  ( 92.56598272418166573, -60.00000000000000000, -2.244544293399764356 ) ) ;
#19144=CARTESIAN_POINT ( 'NONE',  ( -107.8347873283999263, -30.00000000001003997, 189.1745601741373264 ) ) ;
#19152=CARTESIAN_POINT ( 'NONE',  ( 82.54631802247214978, -37.80417153317709023, -12.53333535189654846 ) ) ;
#19166=CARTESIAN_POINT ( 'NONE',  ( 74.77612988998848209, -18.65171555483784971, 105.3432223141187762 ) ) ;
#19173=CARTESIAN_POINT ( 'NONE',  ( -95.95698421656685184, -57.67166530053860640, 41.39248336299490916 ) ) ;
#19178=CARTESIAN_POINT ( 'NONE',  ( 104.3768403531009881, -52.71698490578736340, 184.8465504898348968 ) ) ;
#19179=CARTESIAN_POINT ( 'NONE',  ( -80.00000000000000000, -52.00000000000000000, -21.09707704303352926 ) ) ;
#19182=CARTESIAN_POINT ( 'NONE',  ( -52.44185982314375849, -29.98747349849042720, 50.93426759498176182 ) ) ;
#19190=DIRECTION ( 'NONE',  ( 0.000000000000000000, 0.000000000000000000, 1.000000000000000000 ) ) ;
#19192=CARTESIAN_POINT ( 'NONE',  ( -87.08109489273023485, -30.00000000000000000, 184.1098654863104400 ) ) ;
#19199=CARTESIAN_POINT ( 'NONE',  ( 73.91422987116176557, -57.61663468891570972, 186.6107994588369081 ) ) ;
#19205=CARTESIAN_POINT ( 'NONE',  ( 27.28396264558442752, -28.56679706456900902, -38.29477899011715891 ) ) ;
#19210=CARTESIAN_POINT ( 'NONE',  ( -36.17094327262719844, -60.00000000000000000, 47.52071233496300096 ) ) ;
#19211=EDGE_CURVE ( 'NONE', #40814, #73170, #72473, .T. ) ;
#19212=CARTESIAN_POINT ( 'NONE',  ( -86.32881076508184037, -46.50315659945954394, 190.0124563228725378 ) ) ;
#19216=CARTESIAN_POINT ( 'NONE',  ( -1.007163654173327982, -42.95772940445374388, 31.04927152701133153 ) ) ;
#19220=CARTESIAN_POINT ( 'NONE',  ( 83.88447113947664491, -60.00000000000000000, 191.6821499555289847 ) ) ;
#19234=CARTESIAN_POINT ( 'NONE',  ( 109.5930103617047422, -60.00000000000001421, 123.9179654958789456 ) ) ;
#19235=CARTESIAN_POINT ( 'NONE',  ( -83.58713925656184074, -18.68419755623315126, 145.1655856526831201 ) ) ;
#19239=CARTESIAN_POINT ( 'NONE',  ( 27.41618788073706270, -57.67796933674075177, 43.99820381704387984 ) ) ;
#19262=CARTESIAN_POINT ( 'NONE',  ( -83.90898588706018302, -30.00000000000009592, 196.6629347554013520 ) ) ;
#19263=CARTESIAN_POINT ( 'NONE',  ( 19.90934191524716468, -29.03263091507375648, 29.21916946763769829 ) ) ;
#19267=CARTESIAN_POINT ( 'NONE',  ( -33.47853446770369601, -18.69755159962205227, 30.56496980470470604 ) ) ;
#19281=CARTESIAN_POINT ( 'NONE',  ( 98.93841510732947597, -30.00000000000001066, 144.4000381891304130 ) ) ;
#19284=CARTESIAN_POINT ( 'NONE',  ( 80.76542010163649365, -30.00000000000000355, 13.70105158619666419 ) ) ;
#19300=ORIENTED_EDGE ( 'NONE', *, *, #3549, .T. ) ;
#19302=CARTESIAN_POINT ( 'NONE',  ( 71.49141929022891873, -38.32768232336286474, 142.8628847782384810 ) ) ;
#19322=CARTESIAN_POINT ( 'NONE',  ( 84.56215681354241553, -57.45443045189220754, 191.5346530351454533 ) ) ;
#19331=CARTESIAN_POINT ( 'NONE',  ( -83.18363256083800650, -30.00000000000000355, 44.37128110272426795 ) ) ;
#19334=CARTESIAN_POINT ( 'NONE',  ( 32.95144866765099323, -57.69153774002047186, 47.28118679687395343 ) ) ;
#19339=CARTESIAN_POINT ( 'NONE',  ( -51.20800334721975133, -38.00000000000002132, 52.28430389016808988 ) ) ;
#19343=CARTESIAN_POINT ( 'NONE',  ( 39.82383024057768495, -24.81360042265481169, -30.33102204919740785 ) ) ;
#19344=CARTESIAN_POINT ( 'NONE',  ( -26.88564424253746665, -60.35060106910436417, 35.78314768987581118 ) ) ;
#19348=CARTESIAN_POINT ( 'NONE',  ( -17.95371827100986195, -42.95797721961560001, 31.37255097494336908 ) ) ;
#19362=CARTESIAN_POINT ( 'NONE',  ( 101.4140146818485988, -52.73191828097732525, 192.9060813891788655 ) ) ;
#19376=CARTESIAN_POINT ( 'NONE',  ( -90.68113043260497363, -59.99999999999998579, -22.06029277779147790 ) ) ;
#19380=CARTESIAN_POINT ( 'NONE',  ( -93.94019401501873290, -59.99999999999992895, -15.95863606727341022 ) ) ;
#19383=CARTESIAN_POINT ( 'NONE',  ( -48.50691641643196306, -53.36615341440958105, 52.77268722834218551 ) ) ;
#19392=CARTESIAN_POINT ( 'NONE',  ( 79.62312256247624020, -29.99999999999502975, -25.10596286033261748 ) ) ;
#19398=CARTESIAN_POINT ( 'NONE',  ( 87.75391236170332832, -30.00000000000000000, 186.1424029422745434 ) ) ;
#19405=CARTESIAN_POINT ( 'NONE',  ( 53.66335548193523408, -32.56571110302638772, 54.84416711442435144 ) ) ;
#19410=CARTESIAN_POINT ( 'NONE',  ( -85.36887401862720992, -38.35973107371995638, -22.50894793657372261 ) ) ;
#19411=ORIENTED_EDGE ( 'NONE', *, *, #30939, .T. ) ;
#19412=CARTESIAN_POINT ( 'NONE',  ( 110.4849111511414606, -38.35604559967232774, 182.5406385957329292 ) ) ;
#19414=CARTESIAN_POINT ( 'NONE',  ( 85.24431148756310961, -52.71368398924936827, 22.59386177874363710 ) ) ;
#19435=CARTESIAN_POINT ( 'NONE',  ( -9.393209957245337804, -13.60606480366886473, 31.92530073092069642 ) ) ;
#19439=CARTESIAN_POINT ( 'NONE',  ( 83.68344101230451315, -53.75102016957082895, 188.1393155033960056 ) ) ;
#19440=CARTESIAN_POINT ( 'NONE',  ( -10.00000000000000178, -15.00000000000000000, -9.999999999999998224 ) ) ;
#19441=CARTESIAN_POINT ( 'NONE',  ( -86.23550558450645553, -45.41061243867311958, 189.5308106279269396 ) ) ;
#19444=CARTESIAN_POINT ( 'NONE',  ( -86.15561449557901597, -37.82113771879615172, 53.97651405801602209 ) ) ;
#19448=CARTESIAN_POINT ( 'NONE',  ( -13.98520082896717653, -23.75605607105831396, -38.53473594684242443 ) ) ;
#19449=CARTESIAN_POINT ( 'NONE',  ( 39.83354149937073174, -60.00000000000000711, 51.86226764490275087 ) ) ;
#19450=CARTESIAN_POINT ( 'NONE',  ( 29.71740142289437614, -32.26218012251615619, 40.41358957572558808 ) ) ;
#19452=CARTESIAN_POINT ( 'NONE',  ( 10.38014692360259872, -13.86296647480986977, 31.87445430327215234 ) ) ;
#19453=CARTESIAN_POINT ( 'NONE',  ( -2.499999999999996447, -13.08383949353407516, -21.61544600755649626 ) ) ;
#19461=CARTESIAN_POINT ( 'NONE',  ( -2.106019827721631099, -60.00000000000000000, 39.63609690567994903 ) ) ;
#19468=CARTESIAN_POINT ( 'NONE',  ( -12.61036987039059909, -34.58958934473714208, -32.31355602543667516 ) ) ;
#19477=CARTESIAN_POINT ( 'NONE',  ( -91.89519763986371004, -59.99999999999999289, 15.53214387827562248 ) ) ;
#19482=CARTESIAN_POINT ( 'NONE',  ( -80.87283484261959643, -53.41399119864235701, 172.1343020383144449 ) ) ;
#19495=CARTESIAN_POINT ( 'NONE',  ( -61.29065067449151627, -57.67115771167040350, -37.35479649122906665 ) ) ;
#19503=CARTESIAN_POINT ( 'NONE',  ( 89.60175727050132366, -14.21045842199443143, 48.51353285324994147 ) ) ;
#19504=CARTESIAN_POINT ( 'NONE',  ( -88.91591484687975822, -30.00000000000007105, 199.0554621605764680 ) ) ;
#19506=CARTESIAN_POINT ( 'NONE',  ( -57.09409901914469998, -60.33378115074653891, 74.31118004153825041 ) ) ;
#19510=CARTESIAN_POINT ( 'NONE',  ( -101.3127191661065893, -37.82044097410556560, 187.1967937974196445 ) ) ;
#19521=CARTESIAN_POINT ( 'NONE',  ( 16.46930219882285584, 0.000000000000000000, 4.418206560245473646 ) ) ;
#19527=CARTESIAN_POINT ( 'NONE',  ( -31.88729338067515684, -56.85255422488128829, 36.98592566769335832 ) ) ;
#19529=CARTESIAN_POINT ( 'NONE',  ( 44.90564540012300654, -49.89129374844679177, 46.32480369452557767 ) ) ;
#19532=CARTESIAN_POINT ( 'NONE',  ( -98.37152973009548873, -38.47865734070185084, 200.9152500599649613 ) ) ;
#19544=CARTESIAN_POINT ( 'NONE',  ( 111.2710224913295605, -59.99999999999998579, 185.8464216051011135 ) ) ;
#19551=CARTESIAN_POINT ( 'NONE',  ( -81.58798209278842251, -30.00000000000000000, -7.591802554973769546 ) ) ;
#19553=SURFACE_STYLE_USAGE ( .BOTH. , #102007 ) ;
#19565=CARTESIAN_POINT ( 'NONE',  ( 83.69477321491778810, -29.06518311407809563, 159.7595627650821655 ) ) ;
#19585=CARTESIAN_POINT ( 'NONE',  ( 86.89309887720403935, -60.97679280612473462, 194.8801408971697811 ) ) ;
#19598=B_SPLINE_CURVE_WITH_KNOTS ( 'NONE', 3,
 ( #37273, #15474, #48887, #31171, #7904, #48366, #24142, #30631, #16010, #64055, #28652, #20591, #31688, #56984, #53430, #72648, #86348, #40809, #61538, #70139, #12414, #81259, #55391, #88321, #7372, #64574, #14934, #47827, #106062, #94430, #45345, #78224, #23066, #72121, #6849, #23601, #81780, #73704, #63521, #65091, #96418, #14394, #22549, #32212, #47306, #80202, #80732, #97988, #39247, #89900, #105030, #97440, #96930, #55904, #88840, #39773, #56450, #89383, #42405, #58053, #66690, #50483, #92554, #1393, #51559, #99032, #90976, #25750, #18703, #1937 ),
 .UNSPECIFIED., .F., .F.,
 ( 4, 2, 2, 2, 2, 2, 2, 2, 2, 2, 2, 2, 2, 2, 2, 2, 2, 2, 2, 2, 2, 2, 2, 2, 2, 2, 2, 2, 2, 2, 2, 2, 2, 2, 4 ),
 ( 0.1516340706156730500, 0.1524580149623166181, 0.1532819593089602139, 0.1541059036556037820, 0.1549298480022473501, 0.1565777366955345140, 0.1582256253888216779, 0.1598735140821088418, 0.1615214027753959780, 0.1648171801619703891, 0.1714087349351192668, 0.1780002897082681723, 0.1845918444814170500, 0.1911833992545659555, 0.2043665088008637110, 0.2175496183471614942, 0.2307327278934592774, 0.2570989469860547327, 0.2834651660786502436, 0.2966482756249478880, 0.3098313851712456435, 0.3230144947175433434, 0.3296060494906922211, 0.3361976042638411544, 0.3394933816504155377, 0.3427891590369899766, 0.3460849364235644154, 0.3493807138101388543, 0.3526764911967132932, 0.3559722685832876765, 0.3576201572765749237, 0.3592680459698621709, 0.3609159346631494181, 0.3617398790097929862, 0.3625638233564366097 ),
 .UNSPECIFIED. ) ;
#19607=CARTESIAN_POINT ( 'NONE',  ( -98.33757392241099637, -59.99999999999999289, 202.2807768545189901 ) ) ;
#19614=CARTESIAN_POINT ( 'NONE',  ( -86.40361593247554595, -17.81809089641515698, 175.1979029344232401 ) ) ;
#19621=CARTESIAN_POINT ( 'NONE',  ( -85.02495788024697276, -52.70069914093267016, 6.451521919501416846 ) ) ;
#19622=FACE_OUTER_BOUND ( 'NONE', #67272, .T. ) ;
#19627=CARTESIAN_POINT ( 'NONE',  ( 74.83543306973328413, -14.21045842199438347, 137.5190812362815791 ) ) ;
#19629=CARTESIAN_POINT ( 'NONE',  ( -89.66619014120909981, -60.00000000000001421, -23.31631894612182521 ) ) ;
#19630=CARTESIAN_POINT ( 'NONE',  ( -73.98086237266396381, -29.07117432108940491, 109.2040377524712937 ) ) ;
#19632=CARTESIAN_POINT ( 'NONE',  ( 103.2152402541460248, -59.99999999999995026, 203.2731761476304655 ) ) ;
#19634=CARTESIAN_POINT ( 'NONE',  ( 77.07421096609712663, -57.67120363626943202, -31.72031775925474761 ) ) ;
#19645=CARTESIAN_POINT ( 'NONE',  ( -29.73016315324071712, -60.00000000000618172, 45.54566534438918524 ) ) ;
#19649=CARTESIAN_POINT ( 'NONE',  ( 16.66764709352487728, -4.285714285714295357, -19.00223544648543950 ) ) ;
#19660=CARTESIAN_POINT ( 'NONE',  ( 30.72324318598429116, -22.13081174256386419, 30.23699920491905857 ) ) ;
#19661=FACE_OUTER_BOUND ( 'NONE', #21259, .T. ) ;
#19665=FACE_OUTER_BOUND ( 'NONE', #16995, .T. ) ;
#19670=CARTESIAN_POINT ( 'NONE',  ( 92.60551233582847885, -60.00000000000001421, -2.887494206137121822 ) ) ;
#19677=CARTESIAN_POINT ( 'NONE',  ( -108.1305341385797192, -30.00000000011948842, 149.1718095810573459 ) ) ;
#19683=CARTESIAN_POINT ( 'NONE',  ( 84.43992632049143765, -45.28489048329945632, -8.688217668655392245 ) ) ;
#19698=CARTESIAN_POINT ( 'NONE',  ( 72.46319062493193996, -18.64354067297488626, 97.55174160385824678 ) ) ;
#19703=CARTESIAN_POINT ( 'NONE',  ( -82.32950074003311158, -57.52534511946047502, 200.7509962287250573 ) ) ;
#19706=CARTESIAN_POINT ( 'NONE',  ( 105.2866863118581904, -52.71709848458299064, 172.7927270732103011 ) ) ;
#19710=CARTESIAN_POINT ( 'NONE',  ( -49.54953808143496730, -29.59979831508751502, 45.90118066601930735 ) ) ;
#19723=CARTESIAN_POINT ( 'NONE',  ( -87.78673640380277732, -29.99999999999999645, 186.2301084186935043 ) ) ;
#19728=CARTESIAN_POINT ( 'NONE',  ( 75.21600497976655220, -57.56879808408343990, 191.2544865931707818 ) ) ;
#19732=CARTESIAN_POINT ( 'NONE',  ( 46.86030329039765974, -34.82990584059800909, -36.63149063538335781 ) ) ;
#19735=CARTESIAN_POINT ( 'NONE',  ( -71.71190387867660831, -60.00000000000000711, 152.1791357730885181 ) ) ;
#19738=CARTESIAN_POINT ( 'NONE',  ( -86.65346022717083940, -42.80895526278556673, 189.4114321490026782 ) ) ;
#19739=EDGE_LOOP ( 'NONE', ( #61165, #82720, #3370, #69486, #98137 ) ) ;
#19741=CARTESIAN_POINT ( 'NONE',  ( -0.9879027795118733302, -22.06787372868864594, 27.56762891438381402 ) ) ;
#19759=CARTESIAN_POINT ( 'NONE',  ( 104.0150978814680940, -30.00000000000001421, 120.6686366764556766 ) ) ;
#19760=CARTESIAN_POINT ( 'NONE',  ( -82.07466008940585311, -29.09322732867462946, 147.4984060422640368 ) ) ;
#19765=FILL_AREA_STYLE_COLOUR ( '', #85087 ) ;
#19776=ORIENTED_EDGE ( 'NONE', *, *, #72763, .F. ) ;
#19783=CARTESIAN_POINT ( 'NONE',  ( 91.19629277837930204, -59.99999999999997868, -16.43493217179371513 ) ) ;
#19784=CARTESIAN_POINT ( 'NONE',  ( -39.04695011312426800, -60.00000000000001421, 54.77420429098338417 ) ) ;
#19785=CARTESIAN_POINT ( 'NONE',  ( 22.19785761497768917, -29.03579384637624372, 29.50662452699125993 ) ) ;
#19787=CARTESIAN_POINT ( 'NONE',  ( -36.97264161332481791, -39.51093519734542525, 36.52640270433840186 ) ) ;
#19797=ORIENTED_EDGE ( 'NONE', *, *, #90712, .F. ) ;
#19798=CARTESIAN_POINT ( 'NONE',  ( 94.09021974688658929, -30.00000000000000000, 191.2958226932782395 ) ) ;
#19802=CARTESIAN_POINT ( 'NONE',  ( 79.66186223668852051, -30.00000000000000000, -14.34090231030551443 ) ) ;
#19806=VECTOR ( 'NONE', #63577, 1000.000000000000000 ) ;
#19813=DIRECTION ( 'NONE',  ( -0.000000000000000000, -1.000000000000000000, -0.000000000000000000 ) ) ;
#19822=CARTESIAN_POINT ( 'NONE',  ( 77.52501956836729846, -38.51633467271251732, 186.5635750154488903 ) ) ;
#19843=CARTESIAN_POINT ( 'NONE',  ( 86.49248487488796400, -20.77465731842720231, 183.3202939029210370 ) ) ;
#19848=CARTESIAN_POINT ( 'NONE',  ( 39.18061350182468772, -57.67079139730139303, -41.79049676620926590 ) ) ;
#19849=CARTESIAN_POINT ( 'NONE',  ( -1.531369966231251212, -15.38254760766061580, -35.23445425113402507 ) ) ;
#19854=CARTESIAN_POINT ( 'NONE',  ( -94.05566740925665670, -30.00000000000000711, 112.3003052795253751 ) ) ;
#19857=CARTESIAN_POINT ( 'NONE',  ( 33.93441569500630095, -57.69361011669973749, 48.11240463317153626 ) ) ;
#19863=CARTESIAN_POINT ( 'NONE',  ( -46.26773511477994560, -37.24076651715746777, 44.57266266732312943 ) ) ;
#19867=CARTESIAN_POINT ( 'NONE',  ( 64.03281346377859506, -29.67188817540662171, -23.46043575699671635 ) ) ;
#19868=CARTESIAN_POINT ( 'NONE',  ( -23.12949768660158156, -22.07965379576427978, 28.45208980778609131 ) ) ;
#19872=CARTESIAN_POINT ( 'NONE',  ( -19.40877383843934822, -56.88258129937103291, 33.84440115307146613 ) ) ;
#19882=CARTESIAN_POINT ( 'NONE',  ( -2.629942617601558563, -60.00000000000000000, -42.63907760742034014 ) ) ;
#19886=CARTESIAN_POINT ( 'NONE',  ( 102.2172463571572081, -52.72165632411573455, 191.7000982784959717 ) ) ;
#19900=CARTESIAN_POINT ( 'NONE',  ( -76.26250048646183188, -60.00000000000972733, -32.52427117533751755 ) ) ;
#19905=CARTESIAN_POINT ( 'NONE',  ( -103.8766418169371093, -14.21045842199435860, 137.3606855625607182 ) ) ;
#19906=CARTESIAN_POINT ( 'NONE',  ( 4.046579032613510485, -39.47243836725472477, 30.46108599521819826 ) ) ;
#19908=CARTESIAN_POINT ( 'NONE',  ( -48.55441502850074897, -49.90519047855075740, 51.74626393089475584 ) ) ;
#19923=CARTESIAN_POINT ( 'NONE',  ( 89.30802776495242767, -29.99999999999331379, 17.92124857685668360 ) ) ;
#19929=CARTESIAN_POINT ( 'NONE',  ( 86.39127330366721935, -29.99999999999999645, 181.0099429049296589 ) ) ;
#19935=CARTESIAN_POINT ( 'NONE',  ( 53.46816772670749884, -49.90459927595630063, 61.13385163798207600 ) ) ;
#19940=CARTESIAN_POINT ( 'NONE',  ( -90.95001345222152622, -38.40481687849002412, -12.83308699341175618 ) ) ;
#19944=CARTESIAN_POINT ( 'NONE',  ( 110.2491967804197657, -38.35601177350259405, 184.3369562795453476 ) ) ;
#19946=CARTESIAN_POINT ( 'NONE',  ( 86.14744280574011270, -60.13430353365158254, 9.937224624942581741 ) ) ;
#19964=CARTESIAN_POINT ( 'NONE',  ( 84.89452607104252024, -35.82308226578413013, 180.4058047747997762 ) ) ;
#19970=CARTESIAN_POINT ( 'NONE',  ( -89.14489647802798800, -52.70987939842911629, 57.40709364672285631 ) ) ;
#19974=CARTESIAN_POINT ( 'NONE',  ( -6.469245887355936198, -21.86882241383921155, -38.54580312982461265 ) ) ;
#19976=CARTESIAN_POINT ( 'NONE',  ( 39.13724550554672987, -60.00000000000000000, 50.92405014926310969 ) ) ;
#19978=CARTESIAN_POINT ( 'NONE',  ( 42.00932080603077168, -38.13850585723300668, 52.74428052397462352 ) ) ;
#19980=CARTESIAN_POINT ( 'NONE',  ( 45.12088577198531425, -28.33719382385789842, 40.20412836573458293 ) ) ;
#19981=CARTESIAN_POINT ( 'NONE',  ( -36.74903329801482244, -36.38333104526201822, 45.94992449520283628 ) ) ;
#20003=CARTESIAN_POINT ( 'NONE',  ( -8.066124028907301735, -60.22817720597890911, -36.77925220922959682 ) ) ;
#20010=CARTESIAN_POINT ( 'NONE',  ( -91.86514296420848780, -60.00000000000002132, 10.95446608244987097 ) ) ;
#20018=CARTESIAN_POINT ( 'NONE',  ( -82.06274044418753988, -46.46213096741415427, 172.2108392399005652 ) ) ;
#20021=CARTESIAN_POINT ( 'NONE',  ( -14.76977913854937796, -0.000000000000000000, -8.521464936439098636 ) ) ;
#20030=CARTESIAN_POINT ( 'NONE',  ( -93.81425292840387442, -57.67376786465794680, 13.59058164905135513 ) ) ;
#20036=CARTESIAN_POINT ( 'NONE',  ( 94.85921371064608820, -60.00000000000004263, 26.66736809083038651 ) ) ;
#20037=CARTESIAN_POINT ( 'NONE',  ( -99.17463707058834643, -30.00000000000003908, 199.4944348318372818 ) ) ;
#20038=CARTESIAN_POINT ( 'NONE',  ( -56.18806491820092930, -29.08722365262319087, 58.61279431429321818 ) ) ;
#20042=CARTESIAN_POINT ( 'NONE',  ( -102.7148152195156143, -37.82052743781596860, 177.0099866061467822 ) ) ;
#20043=CARTESIAN_POINT ( 'NONE',  ( -3.672464763049774796E-06, -18.02989419364509516, 35.00496915990722613 ) ) ;
#20044=EDGE_LOOP ( 'NONE', ( #10413, #26305 ) ) ;
#20047=CARTESIAN_POINT ( 'NONE',  ( -18.32916183804282895, -60.00000000000000000, 40.02166413529950262 ) ) ;
#20059=CARTESIAN_POINT ( 'NONE',  ( -32.05612036281008415, -60.32439009662663665, 37.68584545065578340 ) ) ;
#20061=CARTESIAN_POINT ( 'NONE',  ( 48.11622830880407520, -29.14282674110490134, 44.62614721453967093 ) ) ;
#20065=CARTESIAN_POINT ( 'NONE',  ( -86.06810362144429405, -38.63750899286093698, 199.0947428394257486 ) ) ;
#20077=CARTESIAN_POINT ( 'NONE',  ( 111.4401660675299865, -59.99999999999997868, 184.8140296056671730 ) ) ;
#20085=CARTESIAN_POINT ( 'NONE',  ( -98.73364301279765698, -29.99999999999999645, 142.5754916489613322 ) ) ;
#20098=CARTESIAN_POINT ( 'NONE',  ( 81.84886303975771682, -49.95657649133486444, 175.6591428596718174 ) ) ;
#20136=CARTESIAN_POINT ( 'NONE',  ( -105.9855091700707703, -60.00000000000000000, 198.2901911838892488 ) ) ;
#20143=CARTESIAN_POINT ( 'NONE',  ( -85.81946245793210437, -25.08273551360057141, 176.6337755868447061 ) ) ;
#20151=CARTESIAN_POINT ( 'NONE',  ( -82.52728043534214919, -37.83368342240796522, 6.799488428291162734 ) ) ;
#20158=CARTESIAN_POINT ( 'NONE',  ( 74.38357847894150154, -30.00000000000000711, 152.0601407382578429 ) ) ;
#20159=CARTESIAN_POINT ( 'NONE',  ( -90.14748428319414586, -30.00000000000004263, -6.309121115244137101 ) ) ;
#20160=CARTESIAN_POINT ( 'NONE',  ( -65.36515674848668311, -29.05609114770573953, 81.83284678706763771 ) ) ;
#20162=CARTESIAN_POINT ( 'NONE',  ( 78.25600647866326653, -14.21045842199443499, 182.3349015425907851 ) ) ;
#20164=CARTESIAN_POINT ( 'NONE',  ( 40.95489678083415441, -59.99999999999998579, 57.97946709036114044 ) ) ;
#20176=CARTESIAN_POINT ( 'NONE',  ( -92.81214216858748500, -60.00000000000000000, 30.43431760843921907 ) ) ;
#20189=CARTESIAN_POINT ( 'NONE',  ( 35.43533760671546418, -53.35864796427840417, 38.23550249976548798 ) ) ;
#20190=CARTESIAN_POINT ( 'NONE',  ( -22.03900363278799190, -4.285714285715346072, 12.70248734012972669 ) ) ;
#20202=CARTESIAN_POINT ( 'NONE',  ( 92.70591394858523415, -60.00000000000000711, -4.971626050221717996 ) ) ;
#20212=CARTESIAN_POINT ( 'NONE',  ( -83.01077121088147237, -30.00000000006739143, 195.4859236386342332 ) ) ;
#20219=CARTESIAN_POINT ( 'NONE',  ( 86.84721542904824787, -60.22473763668222091, -10.54107096568754365 ) ) ;
#20235=CARTESIAN_POINT ( 'NONE',  ( 78.49326029233736790, -53.37114656867112217, 151.3752469050666889 ) ) ;
#20241=CARTESIAN_POINT ( 'NONE',  ( -112.4426759231622270, -57.67115411723771956, 189.8075418672916044 ) ) ;
#20248=CARTESIAN_POINT ( 'NONE',  ( -49.59036903429539933, -29.60824657159849238, 45.96457809154073004 ) ) ;
#20261=CARTESIAN_POINT ( 'NONE',  ( 24.13407075184041872, -22.09882246145749818, -37.53491456946041893 ) ) ;
#20262=CARTESIAN_POINT ( 'NONE',  ( -62.54040768055548227, -29.99999999999999645, 73.45737685867385380 ) ) ;
#20267=CARTESIAN_POINT ( 'NONE',  ( 75.26462255869792273, -57.56720986738325507, 191.3862757953040443 ) ) ;
#20270=CARTESIAN_POINT ( 'NONE',  ( 53.08967281450005515, -36.21579350601970759, -35.63781967302410436 ) ) ;
#20273=CARTESIAN_POINT ( 'NONE',  ( -56.23870092848233071, -59.99999999999999289, 88.88512022102443666 ) ) ;
#20276=CARTESIAN_POINT ( 'NONE',  ( -86.39046867320946888, -17.31727863270868895, 180.1964746379083522 ) ) ;
#20279=CARTESIAN_POINT ( 'NONE',  ( -4.128997488399893889, -60.36574394313192471, 33.94255568994992700 ) ) ;
#20295=CARTESIAN_POINT ( 'NONE',  ( -11.19959342722916951, 9.651029144387260302E-13, -19.43146043915260179 ) ) ;
#20297=CARTESIAN_POINT ( 'NONE',  ( 94.55541571559547265, -59.99999999999990763, 22.40038052076814878 ) ) ;
#20298=CARTESIAN_POINT ( 'NONE',  ( -81.03537519357652741, -42.97169953517784080, 157.4357695269996213 ) ) ;
#20303=CARTESIAN_POINT ( 'NONE',  ( 31.44210964184475898, -57.68773756896033689, 46.15593347035913041 ) ) ;
#20326=CARTESIAN_POINT ( 'NONE',  ( 78.09008153237981276, -60.00000000000002132, -28.99347257546710210 ) ) ;
#20327=CARTESIAN_POINT ( 'NONE',  ( -73.77866262884730020, -30.00000000000000711, 147.9509455049667395 ) ) ;
#20328=CARTESIAN_POINT ( 'NONE',  ( 20.95262001139231600, -25.55370161815428176, 28.74710842965579261 ) ) ;
#20330=CARTESIAN_POINT ( 'NONE',  ( -36.40588522426740070, -29.12245875214614088, 34.06417451330221269 ) ) ;
#20341=CARTESIAN_POINT ( 'NONE',  ( -75.97346622875217292, -38.37623792979642445, 178.1546702465331862 ) ) ;
#20343=CARTESIAN_POINT ( 'NONE',  ( 97.84284621570628815, -29.99999999999976907, 190.6742164480843087 ) ) ;
#20347=CARTESIAN_POINT ( 'NONE',  ( 81.30983963799556591, -30.00000000000000355, -0.6510870460054363207 ) ) ;
#20372=CARTESIAN_POINT ( 'NONE',  ( 58.58033085486675162, -60.33174129239029782, 78.30550325338386131 ) ) ;
#20388=CARTESIAN_POINT ( 'NONE',  ( 85.76763381879807469, -50.17746128774981429, 190.4771001175396634 ) ) ;
#20396=CARTESIAN_POINT ( 'NONE',  ( -89.87360357950815626, -30.00000000000000355, 87.74932085497819401 ) ) ;
#20399=CARTESIAN_POINT ( 'NONE',  ( 28.45062504421127869, -57.68029023625437191, 44.48305370826658844 ) ) ;
#20404=CARTESIAN_POINT ( 'NONE',  ( -50.55323482659543544, -37.96401913402925032, 51.13833031541544472 ) ) ;
#20408=CARTESIAN_POINT ( 'NONE',  ( 15.53065903970252037, -17.36263754172462015, -34.27975487217998563 ) ) ;
#20411=CARTESIAN_POINT ( 'NONE',  ( -26.29831070025733553, -29.04849030947340793, 30.24692729650839951 ) ) ;
#20415=CARTESIAN_POINT ( 'NONE',  ( -17.81292157518379327, -35.99535881907262080, 30.19758427183107230 ) ) ;
#20425=CARTESIAN_POINT ( 'NONE',  ( -8.979652892184141422, -60.00000000000000711, -42.45601304278074650 ) ) ;
#20429=CARTESIAN_POINT ( 'NONE',  ( 101.4379291727228036, -37.84844671077693334, 186.7608123887999909 ) ) ;
#20432=CARTESIAN_POINT ( 'NONE',  ( 44.66113381551566874, -36.82664275380086139, 42.44229676395095652 ) ) ;
#20444=CARTESIAN_POINT ( 'NONE',  ( -93.72600522304895776, -59.99999999999028688, -16.51119016088236080 ) ) ;
#20447=CARTESIAN_POINT ( 'NONE',  ( 91.37614370737277625, -59.99999999998070876, -21.18689035136125298 ) ) ;
#20452=CARTESIAN_POINT ( 'NONE',  ( -102.4477130004285499, -30.00000000000004974, 111.1018478433771151 ) ) ;
#20453=CARTESIAN_POINT ( 'NONE',  ( 6.163491381871265773, -49.91567759485347011, 32.19897774480319441 ) ) ;
#20454=AXIS2_PLACEMENT_3D ( 'NONE', #56074, #106233, #32393 ) ;
#20456=CARTESIAN_POINT ( 'NONE',  ( -49.59501341947334652, -22.20558386076936941, 44.49776195370446885 ) ) ;
#20466=CARTESIAN_POINT ( 'NONE',  ( 100.1190857666780261, -30.00000000013407586, 97.11980566123828851 ) ) ;
#20471=CARTESIAN_POINT ( 'NONE',  ( 98.43868682546687410, -30.00000000000000355, 189.9420339001966340 ) ) ;
#20479=CARTESIAN_POINT ( 'NONE',  ( 54.35033192401171931, -39.49854378541087385, 58.91923346858290245 ) ) ;
#20486=CARTESIAN_POINT ( 'NONE',  ( -88.47893304564723849, -38.37741962354056824, -18.89372368499410371 ) ) ;
#20490=CARTESIAN_POINT ( 'NONE',  ( 101.6090991099778336, -38.45020037725543460, 199.8721891155738035 ) ) ;
#20492=CARTESIAN_POINT ( 'NONE',  ( 86.60698052122229740, -60.14205719110204029, 0.8374838849679312469 ) ) ;
#20509=CARTESIAN_POINT ( 'NONE',  ( -30.81281672544767858, -32.99113872632139532, 41.04263858266035214 ) ) ;
#20514=CARTESIAN_POINT ( 'NONE',  ( 86.06137632241674851, -21.58008244112160057, 174.3352827979300912 ) ) ;
#20518=CARTESIAN_POINT ( 'NONE',  ( -86.96108843841854252, -39.85768485184852494, 189.1641270546835187 ) ) ;
#20520=CARTESIAN_POINT ( 'NONE',  ( -96.80243442732822245, -45.26554055243965280, 111.1114493365296454 ) ) ;
#20525=CARTESIAN_POINT ( 'NONE',  ( 32.53666910739249829, -59.99999999999999289, 44.50982780536016037 ) ) ;
#20526=CARTESIAN_POINT ( 'NONE',  ( 18.87214478678923157, -24.99265787794756477, 36.59434658705920640 ) ) ;
#20528=CARTESIAN_POINT ( 'NONE',  ( 33.61216083118301157, -23.40945894981453534, 33.02634255258320195 ) ) ;
#20530=CARTESIAN_POINT ( 'NONE',  ( -29.99900812854675891, -32.45003448039427951, 40.57373401099567900 ) ) ;
#20546=CARTESIAN_POINT ( 'NONE',  ( -12.44840434870106449, -21.77031870854123241, -30.18225557512956314 ) ) ;
#20559=CARTESIAN_POINT ( 'NONE',  ( -93.51973230106480628, -60.00000000000000711, 37.21323270788247584 ) ) ;
#20565=CARTESIAN_POINT ( 'NONE',  ( -81.30226012367107558, -53.44438453014575430, 176.1360694353149938 ) ) ;
#20567=CARTESIAN_POINT ( 'NONE',  ( -16.46939662768732049, -0.000000000000000000, 4.418225343323818777 ) ) ;
#20576=CARTESIAN_POINT ( 'NONE',  ( -94.60030117187078247, -57.66721437216608592, -3.115894729640209526 ) ) ;
#20584=CARTESIAN_POINT ( 'NONE',  ( 67.59883368830136874, -59.99999999999988631, -35.88524404060949990 ) ) ;
#20585=CARTESIAN_POINT ( 'NONE',  ( -37.39630343064651186, -60.00000000000003553, 52.44675545814470041 ) ) ;
#20586=CARTESIAN_POINT ( 'NONE',  ( -55.73313709741204036, -29.08943728207367130, 57.64661559024293780 ) ) ;
#20589=CARTESIAN_POINT ( 'NONE',  ( -99.91311621068668103, -45.25511269195838082, 192.6816207345183614 ) ) ;
#20591=CARTESIAN_POINT ( 'NONE',  ( 100.6609828699545091, -38.00000000000000711, 189.2800559844043846 ) ) ;
#20595=CARTESIAN_POINT ( 'NONE',  ( -14.10784364328131879, -60.00000000000002132, 39.74721978056663119 ) ) ;
#20601=CARTESIAN_POINT ( 'NONE',  ( 60.99018172453023823, -30.00000000000000355, 69.41130770961356689 ) ) ;
#20606=CARTESIAN_POINT ( 'NONE',  ( -27.75390804783276621, -49.91462102057435146, 34.23205770176554097 ) ) ;
#20607=CARTESIAN_POINT ( 'NONE',  ( 48.17782170722597357, -18.76230026711737509, 41.56796169131970231 ) ) ;
#20612=CARTESIAN_POINT ( 'NONE',  ( -91.41481866688960167, -38.50420980943239613, 200.8848493538998525 ) ) ;
#20621=CARTESIAN_POINT ( 'NONE',  ( 111.2626209470261784, -60.00000000000000000, 185.8948156968612864 ) ) ;
#20629=SURFACE_STYLE_FILL_AREA ( #61579 ) ;
#20640=CARTESIAN_POINT ( 'NONE',  ( 82.71567603574061422, -42.97295659647987520, 172.7369150664174242 ) ) ;
#20666=CARTESIAN_POINT ( 'NONE',  ( 2.435347819570957628E-07, -57.67120202539301488, -44.61186700419775519 ) ) ;
#20680=CARTESIAN_POINT ( 'NONE',  ( -97.74358396739806665, -60.00000000000000000, 202.3837098231268499 ) ) ;
#20685=CARTESIAN_POINT ( 'NONE',  ( -85.08241398762224605, -32.28766595076764645, 178.2151489888117055 ) ) ;
#20692=CARTESIAN_POINT ( 'NONE',  ( -84.09493881211557209, -45.27002118742259995, 1.240083160534475759 ) ) ;
#20697=( NAMED_UNIT ( * ) SI_UNIT ( $, .STERADIAN. ) SOLID_ANGLE_UNIT ( ) );
#20699=CARTESIAN_POINT ( 'NONE',  ( 81.96363334812492951, -30.00000000000004263, 194.6668941393791386 ) ) ;
#20702=CARTESIAN_POINT ( 'NONE',  ( -92.19364677446148448, -60.00000000000002842, -19.86446420722052153 ) ) ;
#20703=CARTESIAN_POINT ( 'NONE',  ( -64.03236696410434092, -39.48531855383056666, 83.36438480388000016 ) ) ;
#20705=CARTESIAN_POINT ( 'NONE',  ( 84.52829458723479661, -59.99999999999986500, 202.7046071135156069 ) ) ;
#20707=CARTESIAN_POINT ( 'NONE',  ( 39.07151204532090105, -57.67118256652997843, -41.76327104003939183 ) ) ;
#20717=CARTESIAN_POINT ( 'NONE',  ( -90.66602546307569810, -59.99999999999997868, -17.63937689681369392 ) ) ;
#20731=CARTESIAN_POINT ( 'NONE',  ( 37.69778303256208574, -53.35051267955863352, 39.83820104574851939 ) ) ;
#20739=CYLINDRICAL_SURFACE ( 'NONE', #64665, 1.999999999999998224 ) ;
#20745=CARTESIAN_POINT ( 'NONE',  ( 92.54596869004491566, -60.00000000000000711, -1.929604771320055701 ) ) ;
#20753=CARTESIAN_POINT ( 'NONE',  ( -91.34471721603175354, -30.00000000002426148, 199.5624097827029573 ) ) ;
#20767=CARTESIAN_POINT ( 'NONE',  ( 79.67959528545318904, -36.02748385560343536, 140.1370599864249584 ) ) ;
#20773=CARTESIAN_POINT ( 'NONE',  ( -77.81697554521740301, -57.51284286114859157, 196.3444844341304929 ) ) ;
#20783=CARTESIAN_POINT ( 'NONE',  ( -39.92758536453102636, -26.29482751352448133, 35.91463579594280731 ) ) ;
#20797=CARTESIAN_POINT ( 'NONE',  ( -44.53895079744618357, -26.18090992505588943, -29.32626096537978100 ) ) ;
#20798=CARTESIAN_POINT ( 'NONE',  ( -70.04522862247988257, -30.00000000000000711, 95.47013614611103094 ) ) ;
#20803=CARTESIAN_POINT ( 'NONE',  ( 79.53896493954057689, -57.50597618960500057, 198.4139380564783437 ) ) ;
#20809=CARTESIAN_POINT ( 'NONE',  ( -61.33683733235092461, -59.99999999999999289, 104.9969710539504746 ) ) ;
#20814=CARTESIAN_POINT ( 'NONE',  ( -86.30461461627585606, -24.61979355009274073, 182.2308408382141351 ) ) ;
#20831=CARTESIAN_POINT ( 'NONE',  ( 25.22241582816893413, -4.285714285714286476, 3.301606509414615420 ) ) ;
#20833=CARTESIAN_POINT ( 'NONE',  ( 98.75715858346298148, -14.21045842199428222, 105.0403869495405331 ) ) ;
#20835=CARTESIAN_POINT ( 'NONE',  ( -79.23476292317855041, -46.43852501042891134, 148.5225104870177688 ) ) ;
#20839=SURFACE_STYLE_FILL_AREA ( #37533 ) ;
#20857=CARTESIAN_POINT ( 'NONE',  ( 92.65361671693909784, -60.00000000000000000, -3.623317284051360776 ) ) ;
#20858=CARTESIAN_POINT ( 'NONE',  ( -70.80424915565322408, -29.99999999999997513, 131.6008933728038528 ) ) ;
#20859=CARTESIAN_POINT ( 'NONE',  ( 28.17714236523514515, -60.33865966952142657, 36.15954811534652436 ) ) ;
#20872=CARTESIAN_POINT ( 'NONE',  ( 98.00245574399852444, -30.00000000000002132, 190.5288581759436966 ) ) ;
#20876=CARTESIAN_POINT ( 'NONE',  ( 81.57104778221477659, -29.99999999999999645, -8.220818473322141884 ) ) ;
#20896=CARTESIAN_POINT ( 'NONE',  ( 55.14648603844897679, -38.34252558323068882, 81.89861063354169346 ) ) ;
#20900=CARTESIAN_POINT ( 'NONE',  ( 63.04335118806904603, -60.33862346574463231, 91.29151592764401357 ) ) ;
#20903=CARTESIAN_POINT ( 'NONE',  ( -49.70730529349785343, -35.51104931314910829, -36.21594116302647137 ) ) ;
#20917=CARTESIAN_POINT ( 'NONE',  ( 86.36492701509820336, -20.96249612347034486, 181.2249750320262365 ) ) ;
#20925=CARTESIAN_POINT ( 'NONE',  ( -100.7640968642291028, -30.00000000000000000, 180.6473348120972275 ) ) ;
#20928=CARTESIAN_POINT ( 'NONE',  ( 0.1301286458300882076, -57.67120203291111125, 41.61185487318789455 ) ) ;
#20933=CARTESIAN_POINT ( 'NONE',  ( 11.89091310976916382, -16.57373600184161688, -34.65102486210439281 ) ) ;
#20934=DIRECTION ( 'NONE',  ( 1.000000000000000000, 0.000000000000000000, 0.000000000000000000 ) ) ;
#20939=CARTESIAN_POINT ( 'NONE',  ( -17.60110216499754188, -25.55142791915394085, 28.43521521110582384 ) ) ;
#20941=CARTESIAN_POINT ( 'NONE',  ( -85.46309781643650183, -60.00000000000000000, -15.18018135029764970 ) ) ;
#20957=CARTESIAN_POINT ( 'NONE',  ( 104.4029495770615910, -60.15230426517445039, 189.8444650207596851 ) ) ;
#20969=CARTESIAN_POINT ( 'NONE',  ( -90.19250537024298353, -59.99999999999759126, -22.67060294277911225 ) ) ;
#20971=CARTESIAN_POINT ( 'NONE',  ( 34.27131652679207718, -60.00000000000002132, 45.75654928052989590 ) ) ;
#20975=CARTESIAN_POINT ( 'NONE',  ( -91.97835729869039767, -14.21045842199439591, 64.70454208516892436 ) ) ;
#20976=CARTESIAN_POINT ( 'NONE',  ( 10.48337731409090701, -60.35894641967450980, 33.96424879542498587 ) ) ;
#20978=CARTESIAN_POINT ( 'NONE',  ( -48.73406339952293109, -36.06067253240158266, 47.64192311054786444 ) ) ;
#20988=CARTESIAN_POINT ( 'NONE',  ( 85.53273786284641744, -30.00000000000759570, -20.40353017611455044 ) ) ;
#20992=CARTESIAN_POINT ( 'NONE',  ( 97.87774770175602157, -30.00000000000000000, 190.6451874487673877 ) ) ;
#20997=CARTESIAN_POINT ( 'NONE',  ( 55.11151443560458318, -42.96699192481832341, 61.94517765222524019 ) ) ;
#21004=CARTESIAN_POINT ( 'NONE',  ( 94.26160709180628317, -38.49159546897875828, 201.2047994037039018 ) ) ;
#21006=CARTESIAN_POINT ( 'NONE',  ( 83.67118919527318610, -45.28250476704045724, 13.41276670706853658 ) ) ;
#21022=CARTESIAN_POINT ( 'NONE',  ( 2.500000000000000444, -30.00000000000000000, 28.88619651857252535 ) ) ;
#21025=CARTESIAN_POINT ( 'NONE',  ( -39.45711635436059339, -37.46255045984162280, 49.12914128638639255 ) ) ;
#21032=CARTESIAN_POINT ( 'NONE',  ( 85.72993351955908281, -28.54124513701082222, 179.8117750706674371 ) ) ;
#21036=CARTESIAN_POINT ( 'NONE',  ( -87.11468308431049934, -52.70903455444622665, 42.62993231004110584 ) ) ;
#21042=CARTESIAN_POINT ( 'NONE',  ( 11.61272280578022098, -20.93722706496040331, 35.52699528997413836 ) ) ;
#21044=CARTESIAN_POINT ( 'NONE',  ( 38.75764833851163615, -25.78963212653746240, 35.18533521607095338 ) ) ;
#21052=CARTESIAN_POINT ( 'NONE',  ( -83.27438428636391166, -38.00000000000004263, -5.225543532278351222 ) ) ;
#21058=CARTESIAN_POINT ( 'NONE',  ( -6.362823198315364692, -47.40890495455883524, -34.69792613639604184 ) ) ;
#21067=CARTESIAN_POINT ( 'NONE',  ( -94.39340477423540676, -59.99999999999999289, 44.46429842255393083 ) ) ;
#21075=CARTESIAN_POINT ( 'NONE',  ( -83.47692913927937752, -35.99746531496888480, 168.8096269909763691 ) ) ;
#21086=CARTESIAN_POINT ( 'NONE',  ( -83.13494729127086202, -57.67105474064026538, -28.32277909022158724 ) ) ;
#21093=CARTESIAN_POINT ( 'NONE',  ( 90.14752496014264693, -29.99999999999995026, -6.310861463900848456 ) ) ;
#21095=CIRCLE ( 'NONE', #7252, 2.000000000000001776 ) ;
#21096=CARTESIAN_POINT ( 'NONE',  ( -63.58375344335239987, -14.21045842199425024, 93.96584349151677884 ) ) ;
#21097=CARTESIAN_POINT ( 'NONE',  ( -56.04191766312286660, -22.14874848805373375, 55.49595916207043445 ) ) ;
#21100=CARTESIAN_POINT ( 'NONE',  ( -101.8270732106297345, -60.22023256173742567, 194.3861460195847712 ) ) ;
#21106=( LENGTH_UNIT ( ) NAMED_UNIT ( * ) SI_UNIT ( .MILLI., .METRE. ) );
#21117=CARTESIAN_POINT ( 'NONE',  ( -28.23837029583884828, -46.43733527002056150, 33.78025300252188146 ) ) ;
#21121=CARTESIAN_POINT ( 'NONE',  ( 47.01065226741122416, -25.69391163712711190, 42.17763454979905902 ) ) ;
#21124=FACE_OUTER_BOUND ( 'NONE', #66385, .T. ) ;
#21126=CARTESIAN_POINT ( 'NONE',  ( -85.18710009866828159, -38.69275026109524163, 198.6025544802344598 ) ) ;
#21128=CARTESIAN_POINT ( 'NONE',  ( 91.21471444279342222, -38.35841293779726158, -0.8993804321188152429 ) ) ;
#21135=CARTESIAN_POINT ( 'NONE',  ( 108.8511657955034906, -59.99999999999997868, 194.0146055469417661 ) ) ;
#21139=ADVANCED_FACE ( 'NONE', ( #69645, #28687 ), #37307, .T. ) ;
#21142=CARTESIAN_POINT ( 'NONE',  ( -91.26961475985454797, -38.36108261039323963, -1.705770521583544586 ) ) ;
#21146=CARTESIAN_POINT ( 'NONE',  ( -2.499999999999978684, -29.99999999999999645, 28.88619816519791073 ) ) ;
#21154=CARTESIAN_POINT ( 'NONE',  ( 84.21880853279326118, -32.47281885837850268, 170.3671019177896824 ) ) ;
#21192=CARTESIAN_POINT ( 'NONE',  ( -110.5629728245914833, -60.00000000000001421, 189.2218377042151474 ) ) ;
#21198=CARTESIAN_POINT ( 'NONE',  ( -84.10365043901819604, -39.44059402239971490, 178.9954971936382435 ) ) ;
#21201=CARTESIAN_POINT ( 'NONE',  ( -10.00000000000000178, 0.000000000000000000, -9.999999999999998224 ) ) ;
#21203=CARTESIAN_POINT ( 'NONE',  ( -82.50477553219911897, -37.82685549418413729, 17.02917934263369304 ) ) ;
#21208=CARTESIAN_POINT ( 'NONE',  ( 97.13532076618713518, -30.00000000000002842, 199.9107784265496264 ) ) ;
#21211=CARTESIAN_POINT ( 'NONE',  ( -109.5929118004772818, -60.00000000000001421, 123.9174817212569621 ) ) ;
#21212=CARTESIAN_POINT ( 'NONE',  ( -63.92638894657200410, -46.43873725858485102, 86.65927405268175221 ) ) ;
#21214=CARTESIAN_POINT ( 'NONE',  ( 94.36203364593035303, -29.99999999999990763, 200.0833959884570845 ) ) ;
#21216=CARTESIAN_POINT ( 'NONE',  ( 76.83195493398949338, -60.00000000000498801, 195.9604342644627479 ) ) ;
#21228=CARTESIAN_POINT ( 'NONE',  ( -89.98621656989941187, -59.99999999999998579, -18.86310507760501665 ) ) ;
#21233=CARTESIAN_POINT ( 'NONE',  ( 8.127057321558243785, -4.285714285714296246, 23.93420880016848074 ) ) ;
#21241=CARTESIAN_POINT ( 'NONE',  ( 35.05776305746996258, -25.64668665561590188, 32.62633962402455978 ) ) ;
#21242=CARTESIAN_POINT ( 'NONE',  ( 22.23822744035697241, -8.673617379884035472E-16, -2.910977163136222678 ) ) ;
#21249=CARTESIAN_POINT ( 'NONE',  ( 2.499999999999997780, -18.83380486180452706, 27.02532357426314036 ) ) ;
#21253=CARTESIAN_POINT ( 'NONE',  ( 92.26678742429547242, -60.00000000000001421, 1.966542298145190326 ) ) ;
#21259=EDGE_LOOP ( 'NONE', ( #21351, #1306, #90105, #81875 ) ) ;
#21261=CARTESIAN_POINT ( 'NONE',  ( -105.7409267090946372, -30.00000000000445510, 194.2571602938600392 ) ) ;
#21275=CARTESIAN_POINT ( 'NONE',  ( 78.26004437794522062, -49.90185765714640098, 145.7829001237711850 ) ) ;
#21282=CARTESIAN_POINT ( 'NONE',  ( -73.72791963761318357, -57.62431822613736898, 185.7849209195708227 ) ) ;
#21289=CARTESIAN_POINT ( 'NONE',  ( -46.57764780881405642, -28.81936281876300754, 41.83085013884056735 ) ) ;
#21303=CARTESIAN_POINT ( 'NONE',  ( 67.85746092694749620, -30.20841432806020421, -30.53995510508960720 ) ) ;
#21304=CARTESIAN_POINT ( 'NONE',  ( -81.04558864123690398, -30.00000000000000711, 140.2587397602939348 ) ) ;
#21308=CARTESIAN_POINT ( 'NONE',  ( 83.92145523934827622, -57.54641214311970998, 201.7057418963653959 ) ) ;
#21309=CARTESIAN_POINT ( 'NONE',  ( 66.60435403501256246, -60.22831153350267641, -27.67107985133044679 ) ) ;
#21314=CARTESIAN_POINT ( 'NONE',  ( -50.42178165167939596, -60.00000000000000711, 72.86386456530777878 ) ) ;
#21318=CARTESIAN_POINT ( 'NONE',  ( -86.39403411959629864, -17.39645492706551622, 179.4242455222010335 ) ) ;
#21328=CARTESIAN_POINT ( 'NONE',  ( -82.43052579600562524, -37.77911483926543923, -12.82222265178975462 ) ) ;
#21335=CARTESIAN_POINT ( 'NONE',  ( -3.301606509414339641, -4.285714285714286476, -25.22241582816893413 ) ) ;
#21336=CARTESIAN_POINT ( 'NONE',  ( 86.55961277372783513, -14.21045842199431597, 7.754469001180375187 ) ) ;
#21337=CARTESIAN_POINT ( 'NONE',  ( -82.19152542213547008, -22.15616930489894187, 140.5469334434418727 ) ) ;
#21341=CARTESIAN_POINT ( 'NONE',  ( 73.76777583395416116, -57.62289582277519884, 185.9891449441927307 ) ) ;
#21351=ORIENTED_EDGE ( 'NONE', *, *, #32136, .F. ) ;
#21360=CARTESIAN_POINT ( 'NONE',  ( 11.11919979409320014, -59.99999999999998579, -42.37939734519866875 ) ) ;
#21361=CARTESIAN_POINT ( 'NONE',  ( -67.17213121490354411, -60.00000000000000000, 138.9710117141604826 ) ) ;
#21362=CARTESIAN_POINT ( 'NONE',  ( 27.03795841298799374, -32.52614811046257870, 31.02465613286181068 ) ) ;
#21367=CARTESIAN_POINT ( 'NONE',  ( -11.17734400176825993, -4.285714285714295357, -22.67073868809949744 ) ) ;
#21368=CARTESIAN_POINT ( 'NONE',  ( 71.61875643530994751, -38.00000000000000000, -21.68328091587414264 ) ) ;
#21375=CARTESIAN_POINT ( 'NONE',  ( 86.61592898532583717, -30.00000000000007461, 182.1137437502129046 ) ) ;
#21377=ADVANCED_FACE ( 'NONE', ( #75998 ), #29854, .F. ) ;
#21379=CARTESIAN_POINT ( 'NONE',  ( 81.59414243538543587, -30.00000000000000355, -6.877237798308948769 ) ) ;
#21384=B_SPLINE_CURVE_WITH_KNOTS ( 'NONE', 3,
 ( #30911, #64839, #56178, #89118, #48103, #63793, #47577, #15215, #95618, #21759, #55650, #87533, #81004, #40033, #79423, #105818, #104223, #30371, #31958, #55134, #88063, #6056, #14143, #79945, #40558, #65369, #98262, #106335, #73976, #73441, #15749, #91259, #90175, #48633, #42685, #82069, #98780, #42147, #66424, #50241, #24416, #81517, #1130, #75582, #97717, #32499, #57254, #23883, #56726, #75032, #58887, #17369, #82615, #8717, #34637, #66975, #99854, #17900, #41625, #83144, #26028, #1679, #9241, #587, #7641, #57786, #89648, #99308, #24933, #41095, #58336, #16278 ),
 .UNSPECIFIED., .F., .F.,
 ( 4, 2, 2, 2, 2, 2, 2, 2, 2, 2, 2, 2, 2, 2, 2, 2, 2, 2, 2, 2, 2, 2, 2, 2, 2, 2, 2, 2, 2, 2, 2, 2, 2, 2, 2, 4 ),
 ( 0.7782500970722819877, 0.7790724996784590406, 0.7798949022846362045, 0.7815397074969903102, 0.7823621101031673630, 0.7831845127093445269, 0.7840069153155215798, 0.7848293179216986326, 0.7864741231340527383, 0.7881189283464068440, 0.7897637335587609497, 0.7914085387711150554, 0.7946981491958233779, 0.7979877596205315893, 0.8012773700452399117, 0.8045669804699481231, 0.8111462013193646570, 0.8177254221687813018, 0.8243046430181978357, 0.8308838638676143695, 0.8440423055664473262, 0.8572007472652803939, 0.8835176306629464182, 0.9098345140606124426, 0.9229929557594453993, 0.9361513974582784670, 0.9493098391571115346, 0.9558890600065279575, 0.9624682808559444913, 0.9690475017053610252, 0.9756267225547775590, 0.9789163329794857704, 0.9822059434041939818, 0.9854955538289023043, 0.9871403590412564100, 0.9887851642536105157 ),
 .UNSPECIFIED. ) ;
#21398=CARTESIAN_POINT ( 'NONE',  ( -80.86886930798023343, -59.99999999999999289, 181.8382583209386212 ) ) ;
#21399=CARTESIAN_POINT ( 'NONE',  ( 63.35320627527596571, -39.48236604681514450, 81.40631686326936745 ) ) ;
#21410=CARTESIAN_POINT ( 'NONE',  ( -70.67923476944599770, -59.99999999999996447, -26.10759862510926510 ) ) ;
#21415=CARTESIAN_POINT ( 'NONE',  ( 86.32949698655070847, -24.59755161587166938, 182.4574572108609516 ) ) ;
#21419=CARTESIAN_POINT ( 'NONE',  ( 70.54732098882475100, -29.99999999999997868, -20.45443121223284777 ) ) ;
#21423=CARTESIAN_POINT ( 'NONE',  ( -100.0855808037712364, -29.99999999999999645, 154.6059760397357365 ) ) ;
#21427=CARTESIAN_POINT ( 'NONE',  ( 19.23263920009527084, -57.67182620447307784, 42.11598537107099105 ) ) ;
#21436=CARTESIAN_POINT ( 'NONE',  ( 11.81369408999756132, -16.55887885820839500, -34.65806031955098376 ) ) ;
#21440=CARTESIAN_POINT ( 'NONE',  ( -86.62109302441706404, -61.00656027186597186, 194.7265321822163457 ) ) ;
#21444=CARTESIAN_POINT ( 'NONE',  ( -14.28891041865645661, -22.06856204435137059, 27.67569685217618058 ) ) ;
#21445=CARTESIAN_POINT ( 'NONE',  ( -85.82110451813760221, -59.99999999999992895, -14.40634215571435561 ) ) ;
#21474=CARTESIAN_POINT ( 'NONE',  ( -80.67090657556497035, -59.99999999999261036, 200.2785666839474743 ) ) ;
#21476=CARTESIAN_POINT ( 'NONE',  ( 18.45572942341445000, -60.00000000000000000, 40.03357716053164239 ) ) ;
#21479=CARTESIAN_POINT ( 'NONE',  ( -90.16416446821634167, -14.21045842199442077, 52.56827875477732448 ) ) ;
#21480=CARTESIAN_POINT ( 'NONE',  ( 10.26626668568163403, -39.47268289290210674, 30.48008405508823415 ) ) ;
#21483=CARTESIAN_POINT ( 'NONE',  ( -48.60191364056953489, -46.44422754269193376, 50.71984063344733329 ) ) ;
#21494=CARTESIAN_POINT ( 'NONE',  ( 88.16768356981283716, -29.99999999999916156, -16.73627450970226249 ) ) ;
#21498=CARTESIAN_POINT ( 'NONE',  ( 99.78582084211559788, -30.00000000000000000, 186.6030678800591147 ) ) ;
#21512=CARTESIAN_POINT ( 'NONE',  ( 105.6313430892477356, -38.38280832454254465, 196.7987401768915845 ) ) ;
#21515=CARTESIAN_POINT ( 'NONE',  ( 82.50935014594617201, -37.85473763363789601, 17.02533865044420835 ) ) ;
#21535=CARTESIAN_POINT ( 'NONE',  ( -43.25590865262737594, -38.30618195179057039, 54.80721966442113313 ) ) ;
#21539=CARTESIAN_POINT ( 'NONE',  ( 83.43191453633141919, -53.72065295603601953, 187.4671049082887464 ) ) ;
#21543=CARTESIAN_POINT ( 'NONE',  ( 94.06712173148491729, -57.67497447195143678, 4.449674835890252922 ) ) ;
#21552=CARTESIAN_POINT ( 'NONE',  ( 7.992336736730297098, -19.45074496869593261, 35.23616762893431087 ) ) ;
#21553=CARTESIAN_POINT ( 'NONE',  ( 45.26904958275400048, -28.38839725260003277, 40.36013178830350512 ) ) ;
#21566=CARTESIAN_POINT ( 'NONE',  ( 1.561251481115253359, -34.58958075603053572, -32.65459240829875398 ) ) ;
#21580=CARTESIAN_POINT ( 'NONE',  ( -92.61469415333380084, -60.00000000000000000, -10.15781130840770707 ) ) ;
#21589=B_SPLINE_CURVE_WITH_KNOTS ( 'NONE', 3,
 ( #81359, #58161, #73267, #74861 ),
 .UNSPECIFIED., .F., .F.,
 ( 4, 4 ),
 ( 0.000000000000000000, 1.408790152747863330E-05 ),
 .UNSPECIFIED. ) ;
#21590=CARTESIAN_POINT ( 'NONE',  ( -82.39333457580713116, -42.97489278574533955, 169.7347533911100470 ) ) ;
#21603=CARTESIAN_POINT ( 'NONE',  ( -91.67701774657527380, -57.66167918384760327, -19.87712626951747552 ) ) ;
#21609=CARTESIAN_POINT ( 'NONE',  ( 77.20805073229469428, -29.99999999999999289, -26.53535389768476449 ) ) ;
#21611=CARTESIAN_POINT ( 'NONE',  ( -60.31416392689769879, -59.99999999999997158, 109.8312514449790456 ) ) ;
#21612=CARTESIAN_POINT ( 'NONE',  ( -56.66586820654334389, -18.67493726981144775, 55.37565512294952441 ) ) ;
#21616=CARTESIAN_POINT ( 'NONE',  ( -101.6828279354359665, -52.72024364583853639, 192.5462694633920648 ) ) ;
#21631=CARTESIAN_POINT ( 'NONE',  ( -27.18871072888273943, -22.10006771587053720, 29.24485317054519484 ) ) ;
#21634=CARTESIAN_POINT ( 'NONE',  ( 46.99422950215318195, -18.77626701132429332, 40.15805432195738689 ) ) ;
#21637=CARTESIAN_POINT ( 'NONE',  ( -105.5600001555610277, -38.38496021441782347, 196.8991584141934936 ) ) ;
#21639=CARTESIAN_POINT ( 'NONE',  ( 90.90468814451379842, -38.40428968624316752, -13.09899789428958883 ) ) ;
#21648=CARTESIAN_POINT ( 'NONE',  ( 86.16588619706764973, -59.99999999999999289, 200.6625549664367441 ) ) ;
#21658=CARTESIAN_POINT ( 'NONE',  ( -90.58636909219461586, -38.34954571021286540, 13.76841356955266171 ) ) ;
#21665=EDGE_CURVE ( 'NONE', #45998, #25171, #15640, .T. ) ;
#21666=VECTOR ( 'NONE', #87892, 1000.000000000000000 ) ;
#21672=CARTESIAN_POINT ( 'NONE',  ( 82.57334049262250630, -46.47784298928625901, 176.6328590447577369 ) ) ;
#21686=CARTESIAN_POINT ( 'NONE',  ( -76.72318010411292732, -30.00000000000000711, -16.84941602192575516 ) ) ;
#21710=CARTESIAN_POINT ( 'NONE',  ( -112.1573604782814328, -60.00000000000000711, 176.8690052302545155 ) ) ;
#21711=CARTESIAN_POINT ( 'NONE',  ( -10.00000000000000000, -15.00000000000000000, 10.00000000000000178 ) ) ;
#21715=CARTESIAN_POINT ( 'NONE',  ( -82.18871635490596361, -57.14381643118496612, 185.7790063223330321 ) ) ;
#21723=CARTESIAN_POINT ( 'NONE',  ( -85.24306519959390016, -52.70679759000483244, 22.59225849838333744 ) ) ;
#21727=( LENGTH_UNIT ( ) NAMED_UNIT ( * ) SI_UNIT ( .MILLI., .METRE. ) );
#21729=CARTESIAN_POINT ( 'NONE',  ( 100.7999351731576354, -29.99999999999990763, 198.8735152728553999 ) ) ;
#21731=CARTESIAN_POINT ( 'NONE',  ( -91.01385585952614576, -29.99999999999999289, 38.60219201899132457 ) ) ;
#21732=CARTESIAN_POINT ( 'NONE',  ( -63.70546524352059237, -49.91541863491629982, 87.81759370848021717 ) ) ;
#21736=CARTESIAN_POINT ( 'NONE',  ( 100.3830179364247783, -59.99999999999631228, 204.2895793215106437 ) ) ;
#21749=CARTESIAN_POINT ( 'NONE',  ( -92.70901343235634329, -59.99999999999998579, -4.635296546728438827 ) ) ;
#21755=CARTESIAN_POINT ( 'NONE',  ( 19.00223544648544305, -4.285714285714295357, 16.66764709352488083 ) ) ;
#21759=CARTESIAN_POINT ( 'NONE',  ( 101.5344860084426415, -60.00000000000007105, 194.6295455690923859 ) ) ;
#21762=CARTESIAN_POINT ( 'NONE',  ( 9.999999999999998224, 0.000000000000000000, -9.999999999999998224 ) ) ;
#21763=CARTESIAN_POINT ( 'NONE',  ( 32.88952925475911115, -29.08932276880856804, 32.34176666536721712 ) ) ;
#21764=CARTESIAN_POINT ( 'NONE',  ( -16.57301948837645256, -1.734723475976807094E-15, 4.453875240771298039 ) ) ;
#21777=CARTESIAN_POINT ( 'NONE',  ( 101.2378610160001529, -59.99999999999999289, 88.29373084620047507 ) ) ;
#21785=CARTESIAN_POINT ( 'NONE',  ( -83.82331579519006937, -29.99999999999999645, 159.3544112921956923 ) ) ;
#21797=APPLICATION_CONTEXT ( 'automotive_design' ) ;
#21800=CARTESIAN_POINT ( 'NONE',  ( 78.12193372058688112, -56.83984770602898351, 152.8020783963501970 ) ) ;
#21803=ORIENTED_EDGE ( 'NONE', *, *, #33055, .T. ) ;
#21807=CARTESIAN_POINT ( 'NONE',  ( -5.651997800604014799, -57.67124204504380458, 41.59089347824649252 ) ) ;
#21819=CARTESIAN_POINT ( 'NONE',  ( -35.72250249440244829, -24.40408281891684084, 33.76365376224248394 ) ) ;
#21832=CARTESIAN_POINT ( 'NONE',  ( 33.33710378954599207, -24.76289289388104464, -37.00238709877101684 ) ) ;
#21833=CARTESIAN_POINT ( 'NONE',  ( -71.02231249463051199, -30.00000000000000000, 98.64568665504826583 ) ) ;
#21838=CARTESIAN_POINT ( 'NONE',  ( 96.53708244649047288, -57.62217743364686839, 204.4821657146100051 ) ) ;
#21839=CARTESIAN_POINT ( 'NONE',  ( 68.60688657586096895, -47.40901989918412340, -24.67624544561557087 ) ) ;
#21844=CARTESIAN_POINT ( 'NONE',  ( -50.48252356805748775, -60.00000000000000711, 73.01728160295303383 ) ) ;
#21849=CARTESIAN_POINT ( 'NONE',  ( -86.16350626793575884, -28.29804646221614206, 183.0077501213199298 ) ) ;
#21855=B_SPLINE_CURVE_WITH_KNOTS ( 'NONE', 3,
 ( #7997, #105631, #80285, #89467, #88932, #6398, #6934, #22636, #104571, #72728, #30724, #31771, #15560, #63612, #7454, #73247, #39333, #72213, #106151, #32839, #105115, #64652, #32307, #79765, #55471, #65180, #81871, #88408, #98073, #48974, #89987, #57073, #16095, #14479, #82960, #92643, #50566, #91596, #17707, #74324, #51108, #83482, #59767, #41433, #50050, #99122, #66783, #2560, #18801, #2029, #59233, #928, #76452, #100203, #9582, #74846, #33368, #67840, #8527, #51646, #43565, #99670, #1489, #91072, #58144, #401, #84568, #26368, #33913, #75392, #75929, #25288, #100730, #42496, #84025, #34453, #10648, #9055, #66237, #10131, #67323, #18249, #17179, #92106, #41963, #43041, #34977, #65717, #57595, #26892 ),
 .UNSPECIFIED., .F., .F.,
 ( 4, 2, 2, 2, 1, 1, 2, 2, 2, 2, 2, 2, 1, 2, 2, 1, 2, 2, 2, 1, 1, 2, 2, 1, 2, 2, 1, 1, 1, 2, 2, 1, 2, 2, 1, 1, 1, 2, 2, 1, 2, 2, 2, 1, 1, 1, 2, 2, 1, 2, 1, 1, 1, 2, 2, 4 ),
 ( 0.5023353322599047877, 0.5334393739936618140, 0.5489913948605402716, 0.5567674052939795004, 0.5606554105106991148, 0.5616274118148790739, 0.5621134124669689980, 0.5625994131190590331, 0.5645434157274189513, 0.5956474574611777539, 0.6111994783280572108, 0.6189754887614968837, 0.6228634939782167201, 0.6248074965865767494, 0.6257794978907567085, 0.6267514991949366676, 0.6889595826624540509, 0.7200636243962127425, 0.7356156452630919773, 0.7433916556965316502, 0.7472796609132515977, 0.7492236635216116269, 0.7501956648257915861, 0.7511676661299715452, 0.7822717078637267951, 0.7978237287306044756, 0.8055997391640433714, 0.8094877443807628747, 0.8114317469891225709, 0.8124037482933024190, 0.8128897489453923431, 0.8133757495974822671, 0.8444797913312427351, 0.8600318121981230801, 0.8678078226315633081, 0.8716958278482832556, 0.8736398304566432849, 0.8746118317608234660, 0.8750978324129135011, 0.8755838330650034251, 0.9066878747987620057, 0.9222398956656412405, 0.9300159060990808024, 0.9339039113158006389, 0.9358479139241604461, 0.9368199152283405162, 0.9373059158804304403, 0.9375489162064755133, 0.9377919165325204753, 0.9533439373993892740, 0.9611199478328236179, 0.9650079530495406788, 0.9669519556578993758, 0.9679239569620786687, 0.9688959582662579617, 1.000000000000000000 ),
 .UNSPECIFIED. ) ;
#21856=CARTESIAN_POINT ( 'NONE',  ( -84.79560538139988068, -60.18951872861072161, -16.38072637616851779 ) ) ;
#21863=CARTESIAN_POINT ( 'NONE',  ( 3.301606509414619861, -4.285714285714286476, 25.22241582816893413 ) ) ;
#21866=CARTESIAN_POINT ( 'NONE',  ( 75.59946810849663734, -59.99999999999992895, -32.85428466877961284 ) ) ;
#21867=CARTESIAN_POINT ( 'NONE',  ( -78.94945067621699764, -42.96865013358673480, 142.9639642539773376 ) ) ;
#21871=CARTESIAN_POINT ( 'NONE',  ( 86.82793481660095836, -57.58489263483398446, 203.0475982403202408 ) ) ;
#21892=CARTESIAN_POINT ( 'NONE',  ( -55.44100834966593538, -14.21045842199449361, 70.81055559928208254 ) ) ;
#21893=CARTESIAN_POINT ( 'NONE',  ( 28.08999935184878893, -42.95675325573949266, 33.12999348514809839 ) ) ;
#21897=CARTESIAN_POINT ( 'NONE',  ( -15.38541618194247285, -4.285714285714295357, -20.05453516056602581 ) ) ;
#21906=CARTESIAN_POINT ( 'NONE',  ( -82.57697026063134160, -41.66718125965567054, -14.02672778557674249 ) ) ;
#21908=CARTESIAN_POINT ( 'NONE',  ( 81.17160454977077677, -29.99999999999999289, 1.346216154707244428 ) ) ;
#21928=CARTESIAN_POINT ( 'NONE',  ( 63.69280158076683307, -39.48211605329254326, 82.38451565384035291 ) ) ;
#21932=CARTESIAN_POINT ( 'NONE',  ( -45.15185372570044819, -34.39553445584278535, -36.86152318962493979 ) ) ;
#21938=CARTESIAN_POINT ( 'NONE',  ( -4.789139187686886956, -60.00000000000000711, -36.83444369039217747 ) ) ;
#21939=FACE_OUTER_BOUND ( 'NONE', #56542, .T. ) ;
#21942=CARTESIAN_POINT ( 'NONE',  ( 85.66261666857552370, -61.05915153208074742, 194.0543246977708520 ) ) ;
#21949=CARTESIAN_POINT ( 'NONE',  ( 18.57084990933715218, -18.11241891143331983, -33.93312537572241183 ) ) ;
#21953=CARTESIAN_POINT ( 'NONE',  ( -99.75299316808613526, -30.00000000000000355, 151.3284628849059459 ) ) ;
#21957=CARTESIAN_POINT ( 'NONE',  ( 43.07244424302177777, -57.68573873175960642, 61.15634709738809249 ) ) ;
#21967=CARTESIAN_POINT ( 'NONE',  ( -87.48428544808629681, -35.37239160489516365, 189.1147638953327998 ) ) ;
#21971=CARTESIAN_POINT ( 'NONE',  ( -11.36750716639379988, -42.95774986353630709, 31.07752345680997408 ) ) ;
#21973=CARTESIAN_POINT ( 'NONE',  ( -88.36736620956926913, -59.99999999999997158, 42.82440024210349350 ) ) ;
#21980=CARTESIAN_POINT ( 'NONE',  ( 71.68560605309247080, -60.00000000000000000, 151.9124196244835332 ) ) ;
#22000=CARTESIAN_POINT ( 'NONE',  ( -84.79750510667604146, -60.00000000000488853, 202.7836688792506550 ) ) ;
#22002=CARTESIAN_POINT ( 'NONE',  ( 38.24823956341693076, -60.00000000000000000, 49.79050390885200272 ) ) ;
#22005=CARTESIAN_POINT ( 'NONE',  ( -101.8002770060248139, -59.99999999999998579, 77.51242708015574578 ) ) ;
#22006=CARTESIAN_POINT ( 'NONE',  ( 11.32701196670594612, -39.47267329916473244, 30.49584611229249376 ) ) ;
#22009=CARTESIAN_POINT ( 'NONE',  ( -45.48440666609703698, -36.07416133972417782, 43.31486618243847175 ) ) ;
#22019=CARTESIAN_POINT ( 'NONE',  ( 81.72147651377501631, -29.99999999996476774, 193.8235977729058845 ) ) ;
#22022=CARTESIAN_POINT ( 'NONE',  ( 98.32443016958239923, -30.00000000000000000, 190.1219309493679646 ) ) ;
#22036=CARTESIAN_POINT ( 'NONE',  ( 101.5909309265440470, -38.45050066038580638, 199.8806868041374400 ) ) ;
#22038=CARTESIAN_POINT ( 'NONE',  ( 82.53206627490877167, -37.86144382515931994, 6.795202634608455305 ) ) ;
#22059=CARTESIAN_POINT ( 'NONE',  ( 26.53083019430453859, -22.65905336700136630, 37.38260693527033851 ) ) ;
#22063=CARTESIAN_POINT ( 'NONE',  ( 85.67953511968930513, -35.65700491136370687, 184.2338551578000363 ) ) ;
#22069=CARTESIAN_POINT ( 'NONE',  ( 93.83525582135544596, -57.67459712079030254, 11.50689781192917671 ) ) ;
#22072=CARTESIAN_POINT ( 'NONE',  ( -7.664487212094859281, -22.09574587988852556, -38.54460460203753058 ) ) ;
#22078=CARTESIAN_POINT ( 'NONE',  ( 37.73245083015999057, -25.32999417115200558, 34.64601903076129474 ) ) ;
#22084=CARTESIAN_POINT ( 'NONE',  ( -42.36837551588181583, -33.99149918245159085, -29.05969016418114492 ) ) ;
#22087=CARTESIAN_POINT ( 'NONE',  ( -102.5618070566913218, -38.00000000000000000, 164.2657687415081682 ) ) ;
#22094=CARTESIAN_POINT ( 'NONE',  ( -40.42326134380499525, -21.77016373189269416, -27.31203147464151115 ) ) ;
#22103=CARTESIAN_POINT ( 'NONE',  ( -92.65366311753854234, -60.00000000000000711, -9.671686281151320230 ) ) ;
#22111=CARTESIAN_POINT ( 'NONE',  ( -84.47875027511349799, -18.66658693311171291, 151.2515477827395500 ) ) ;
#22113=CARTESIAN_POINT ( 'NONE',  ( -12.81917055448085030, 0.000000000000000000, 11.24487389205527776 ) ) ;
#22123=CARTESIAN_POINT ( 'NONE',  ( -81.06400256271496119, -57.51341943371168952, 199.7941202169005805 ) ) ;
#22128=CARTESIAN_POINT ( 'NONE',  ( 94.69963775048552179, -60.00000000000009948, 1.032162584924374293 ) ) ;
#22129=CARTESIAN_POINT ( 'NONE',  ( -49.67087318978585841, -59.99999999999999289, 77.31351762338060496 ) ) ;
#22131=CARTESIAN_POINT ( 'NONE',  ( -56.41525400592121287, -42.96960946770816037, 64.88850874853261530 ) ) ;
#22134=CARTESIAN_POINT ( 'NONE',  ( -73.50473004590615744, -60.00000000000000000, -24.84693947030580574 ) ) ;
#22136=CARTESIAN_POINT ( 'NONE',  ( -102.6327129110277099, -60.18409667677708086, 193.3961458806942062 ) ) ;
#22142=CARTESIAN_POINT ( 'NONE',  ( 108.0899631164236609, -38.35819308738822997, 192.6723653064404402 ) ) ;
#22152=CARTESIAN_POINT ( 'NONE',  ( -29.01716069711826762, -49.91287937905969585, 34.62871294549472623 ) ) ;
#22156=CARTESIAN_POINT ( 'NONE',  ( 47.01495483615595816, -29.15207790528993570, 43.18957708107585347 ) ) ;
#22160=CARTESIAN_POINT ( 'NONE',  ( -108.0744233114761244, -38.35871118714575090, 192.8189671270986310 ) ) ;
#22163=CARTESIAN_POINT ( 'NONE',  ( 85.86996992767592474, -38.36131443074192049, -22.03495116904964135 ) ) ;
#22174=CARTESIAN_POINT ( 'NONE',  ( 94.81893203379229362, -60.00000000000002132, 202.5725863315619222 ) ) ;
#22178=CARTESIAN_POINT ( 'NONE',  ( 57.43676197718647103, -22.13903279540451052, 58.37046990149170256 ) ) ;
#22183=CARTESIAN_POINT ( 'NONE',  ( -107.3760131578118404, -38.36153571196422973, 194.1939700411200533 ) ) ;
#22196=CARTESIAN_POINT ( 'NONE',  ( 82.14827175627938516, -49.98004452256672181, 178.0753244963457291 ) ) ;
#22209=CARTESIAN_POINT ( 'NONE',  ( -81.59189379692385558, -30.00000000000000711, -7.173991459043422836 ) ) ;
#22213=CARTESIAN_POINT ( 'NONE',  ( -0.7156389501956513799, -18.04057304077605295, 35.00644575174603546 ) ) ;
#22220=EDGE_CURVE ( 'NONE', #25066, #24456, #67762, .T. ) ;
#22238=CARTESIAN_POINT ( 'NONE',  ( -111.1099793248805838, -60.00000000000001421, 153.2218623716563286 ) ) ;
#22244=CARTESIAN_POINT ( 'NONE',  ( -83.69448559273577359, -46.54495372303564693, 183.4117449980363403 ) ) ;
#22251=CARTESIAN_POINT ( 'NONE',  ( -84.90758499310180696, -52.70380024735796809, 13.63252645412560682 ) ) ;
#22259=CARTESIAN_POINT ( 'NONE',  ( 99.10782808284749024, -14.21045842199446163, 197.1815751231716263 ) ) ;
#22260=CARTESIAN_POINT ( 'NONE',  ( -104.0151861009774166, -30.00000000000006750, 120.6691871043967126 ) ) ;
#22261=CARTESIAN_POINT ( 'NONE',  ( -62.71288653495292209, -60.34586746940613011, 90.28915145330465464 ) ) ;
#22264=CARTESIAN_POINT ( 'NONE',  ( 95.99019121356252526, -60.00000000000866152, 204.9761892479625089 ) ) ;
#22276=CARTESIAN_POINT ( 'NONE',  ( -47.12223804421648055, -59.99999999999998579, -38.46817206024380909 ) ) ;
#22287=CARTESIAN_POINT ( 'NONE',  ( -39.17226668844914883, -39.51869471205692008, 38.04320566444418006 ) ) ;
#22292=CARTESIAN_POINT ( 'NONE',  ( 33.91238484704524581, -53.36470455789326905, 37.37873827427225848 ) ) ;
#22293=CARTESIAN_POINT ( 'NONE',  ( -13.60704923275580924, -1.734723475976807094E-15, -10.45706415777457465 ) ) ;
#22297=CARTESIAN_POINT ( 'NONE',  ( -75.95103116715310421, -38.37491938504500411, 177.9832065501431941 ) ) ;
#22308=CARTESIAN_POINT ( 'NONE',  ( 94.17286979174674855, -59.99999999999999289, 42.72536648720843999 ) ) ;
#22314=CARTESIAN_POINT ( 'NONE',  ( -63.87591448453517984, -30.00000000000000711, 77.01698376430015003 ) ) ;
#22321=CARTESIAN_POINT ( 'NONE',  ( 83.26081960998183717, -52.72642717100047349, -16.35834959482691175 ) ) ;
#22330=CARTESIAN_POINT ( 'NONE',  ( 78.78750774858497152, -53.37144728722491038, 153.4658605898123369 ) ) ;
#22337=CARTESIAN_POINT ( 'NONE',  ( -33.87510863592373767, -57.69360311548409470, 48.02532427896534983 ) ) ;
#22347=EDGE_CURVE ( 'NONE', #45998, #39827, #14407, .T. ) ;
#22351=CARTESIAN_POINT ( 'NONE',  ( -7.543428673995849820, -13.25821866003511751, 32.00908194862271472 ) ) ;
#22364=CARTESIAN_POINT ( 'NONE',  ( 22.34684471419683760, -26.69134893376664763, -38.45222277864926497 ) ) ;
#22365=CARTESIAN_POINT ( 'NONE',  ( -82.83519950011617539, -30.00000000000000711, 151.7030435779494439 ) ) ;
#22372=CARTESIAN_POINT ( 'NONE',  ( 107.9489589369664202, -57.65951413602503095, 199.0667566530268573 ) ) ;
#22373=CARTESIAN_POINT ( 'NONE',  ( 67.20503002699381057, -47.40899075066970170, -25.20247587780630383 ) ) ;
#22377=CARTESIAN_POINT ( 'NONE',  ( -73.55625695019807608, -60.00000000000001421, 167.7443850725575203 ) ) ;
#22382=CARTESIAN_POINT ( 'NONE',  ( -84.16960440523372711, -61.06210287833253147, 192.5424730624227436 ) ) ;
#22389=CARTESIAN_POINT ( 'NONE',  ( -81.77152546554842161, -37.79979095042777004, -14.16671787682579087 ) ) ;
#22397=CARTESIAN_POINT ( 'NONE',  ( 12.70248734011840597, -4.285714285713678073, -22.03900363279143093 ) ) ;
#22399=CARTESIAN_POINT ( 'NONE',  ( 82.45758146611665040, -29.99999999999998579, -23.17547892442675916 ) ) ;
#22400=CARTESIAN_POINT ( 'NONE',  ( -77.47082139812327739, -60.31520998343973616, 152.1232861070816114 ) ) ;
#22402=CARTESIAN_POINT ( 'NONE',  ( 8.555523463203789092, -60.00000000000005684, 41.98724916707659816 ) ) ;
#22404=CARTESIAN_POINT ( 'NONE',  ( 75.40687419154917848, -57.56243725155260904, 191.7921977673724996 ) ) ;
#22412=CARTESIAN_POINT ( 'NONE',  ( -103.7245430960311126, -45.26537689992342450, 163.3981769379987270 ) ) ;
#22422=CARTESIAN_POINT ( 'NONE',  ( -8.181074200006944963, -14.21045842199423603, 34.35486773805523342 ) ) ;
#22423=CARTESIAN_POINT ( 'NONE',  ( 25.83843143683618848, -32.52250552547243956, 30.74844871866972085 ) ) ;
#22424=CIRCLE ( 'NONE', #53421, 1.999999999999998224 ) ;
#22439=CARTESIAN_POINT ( 'NONE',  ( 1.309624450538505291, -60.00000000000000711, -42.63907992752542953 ) ) ;
#22440=CARTESIAN_POINT ( 'NONE',  ( 59.64050360443124532, -29.99999999999996447, 65.96467207391573595 ) ) ;
#22451=CARTESIAN_POINT ( 'NONE',  ( 0.000000000000000000, 30.00000000000000000, 0.000000000000000000 ) ) ;
#22464=CARTESIAN_POINT ( 'NONE',  ( 64.56574826876759232, -25.57792867474360321, 77.78118918835328088 ) ) ;
#22476=CARTESIAN_POINT ( 'NONE',  ( 70.62474104179052858, -59.99999999999999289, -26.13143283881593604 ) ) ;
#22483=CARTESIAN_POINT ( 'NONE',  ( 86.60940601525219051, -20.70715439809982783, 184.3503468479922276 ) ) ;
#22494=CARTESIAN_POINT ( 'NONE',  ( 37.98648538845074540, -60.00000000000001421, 49.46892715370867677 ) ) ;
#22495=CARTESIAN_POINT ( 'NONE',  ( -101.1095592966768208, -29.99999999999999645, 175.2763840439222633 ) ) ;
#22497=CARTESIAN_POINT ( 'NONE',  ( 45.10052333452469497, -57.68305435951591420, 65.38036528418656701 ) ) ;
#22506=CARTESIAN_POINT ( 'NONE',  ( -12.66494344392306104, -60.00000000000002132, 39.70460679373117330 ) ) ;
#22508=FACE_OUTER_BOUND ( 'NONE', #27577, .T. ) ;
#22511=CARTESIAN_POINT ( 'NONE',  ( -15.72133563019506930, -42.95781215222940830, 31.23342921828535523 ) ) ;
#22513=CARTESIAN_POINT ( 'NONE',  ( -99.12185298998538485, -59.99999999999997868, 109.9295474875607397 ) ) ;
#22521=CARTESIAN_POINT ( 'NONE',  ( 61.80701749067248585, -60.00000000000001421, 106.6076082615842040 ) ) ;
#22526=CARTESIAN_POINT ( 'NONE',  ( 29.53284356080077444, -60.00000000000004974, 45.26708560465603171 ) ) ;
#22541=CARTESIAN_POINT ( 'NONE',  ( -112.1437713539201866, -59.99999999994144417, 141.3908632541163115 ) ) ;
#22544=CARTESIAN_POINT ( 'NONE',  ( 72.76612462108283808, -59.99999999999997868, 160.3201290646432824 ) ) ;
#22547=CARTESIAN_POINT ( 'NONE',  ( -113.8519240760089133, -60.00000000000002842, 157.1483645435538108 ) ) ;
#22548=CARTESIAN_POINT ( 'NONE',  ( 9.282106017489308414, -46.43475792098434596, 31.63186067789786904 ) ) ;
#22549=CARTESIAN_POINT ( 'NONE',  ( 83.27820862095059340, -37.99999999999996447, 29.76319823405992082 ) ) ;
#22552=CARTESIAN_POINT ( 'NONE',  ( -47.02002132585242578, -39.52884493021316104, 46.23036517761990893 ) ) ;
#22560=AXIS2_PLACEMENT_3D ( 'NONE', #2867, #50879, #1797 ) ;
#22566=CARTESIAN_POINT ( 'NONE',  ( 108.0570916867202556, -29.99999999999827693, 188.3392959967954994 ) ) ;
#22570=CARTESIAN_POINT ( 'NONE',  ( 97.41453105692403369, -29.99999999999999645, 190.9275840960229118 ) ) ;
#22584=CARTESIAN_POINT ( 'NONE',  ( 96.06384290910234824, -38.48472166148474827, 201.2020660132053536 ) ) ;
#22587=CARTESIAN_POINT ( 'NONE',  ( 86.94475506094372008, -60.16925933034688967, -3.940419869023602750 ) ) ;
#22588=CARTESIAN_POINT ( 'NONE',  ( 63.28416903638269275, -38.00000000000000711, 80.42582590836656209 ) ) ;
#22607=CARTESIAN_POINT ( 'NONE',  ( 33.70467876106231131, -25.90788300163896452, 41.06987389266631538 ) ) ;
#22611=CARTESIAN_POINT ( 'NONE',  ( 84.82672610503449562, -46.56838776579275674, 187.1272610940604579 ) ) ;
#22615=CARTESIAN_POINT ( 'NONE',  ( 94.40918845809700599, -57.67101149516233249, -0.2801014365498262215 ) ) ;
#22624=CARTESIAN_POINT ( 'NONE',  ( -53.26687959709935427, -38.00000000000001421, 56.03731585654522007 ) ) ;
#22636=CARTESIAN_POINT ( 'NONE',  ( -10.05811987131503038, -16.24350643256279625, -34.80807818328759851 ) ) ;
#22638=CARTESIAN_POINT ( 'NONE',  ( -61.40929618123364264, -47.40892651706064953, -27.09027404592079336 ) ) ;
#22645=CARTESIAN_POINT ( 'NONE',  ( -92.50385710939508499, -59.99999999999999289, -1.307865944661959601 ) ) ;
#22649=CARTESIAN_POINT ( 'NONE',  ( 98.35997379234478899, -37.76608977019981239, 192.3278014986217954 ) ) ;
#22651=CARTESIAN_POINT ( 'NONE',  ( -84.67995877784876768, -22.10573975591750795, 157.8301934640955437 ) ) ;
#22652=VERTEX_POINT ( 'NONE', #724 ) ;
#22656=ADVANCED_FACE ( 'NONE', ( #33692 ), #98911, .F. ) ;
#22661=CARTESIAN_POINT ( 'NONE',  ( -74.79081370483122271, -57.58316160299655451, 190.1003635006443346 ) ) ;
#22666=CARTESIAN_POINT ( 'NONE',  ( 82.45758146611665040, -29.99999999999998579, -23.17547892442675916 ) ) ;
#22668=CARTESIAN_POINT ( 'NONE',  ( -65.47633411339396048, -60.00000000000000000, 130.5853305762684329 ) ) ;
#22669=CARTESIAN_POINT ( 'NONE',  ( -52.14842760859697535, -60.31282274427849188, 62.32353961952082955 ) ) ;
#22673=CARTESIAN_POINT ( 'NONE',  ( -99.43116831379333576, -37.79880016511722118, 191.4274298609611833 ) ) ;
#22678=CARTESIAN_POINT ( 'NONE',  ( 108.7231916027115091, -38.35574387428263066, 143.1493928306014709 ) ) ;
#22685=CARTESIAN_POINT ( 'NONE',  ( 62.37459373232455562, -30.00000000000000711, 73.01631233425933942 ) ) ;
#22686=AXIS2_PLACEMENT_3D ( 'NONE', #25251, #40869, #23653 ) ;
#22687=EDGE_CURVE ( 'NONE', #32439, #16675, #87689, .T. ) ;
#22694=CARTESIAN_POINT ( 'NONE',  ( 48.90658294110461668, -46.43936590027043820, 51.21113800430314456 ) ) ;
#22699=CARTESIAN_POINT ( 'NONE',  ( -104.3457841577212548, -38.40612335771167807, 198.1033792868130092 ) ) ;
#22701=CARTESIAN_POINT ( 'NONE',  ( 91.21127784508071557, -38.35815842224639027, -0.8486547785704385838 ) ) ;
#22705=CARTESIAN_POINT ( 'NONE',  ( 99.36430944222280459, -37.84839370588183982, 135.1400454678828567 ) ) ;
#22710=CARTESIAN_POINT ( 'NONE',  ( 83.61247817121171977, -59.99999999999999289, 199.2525199516834675 ) ) ;
#22714=CARTESIAN_POINT ( 'NONE',  ( 56.51965637257737285, -56.85211480795176442, 71.22111066778985844 ) ) ;
#22720=CARTESIAN_POINT ( 'NONE',  ( -93.80762359828875674, -38.49308346633976186, 201.2011921042621623 ) ) ;
#22730=CARTESIAN_POINT ( 'NONE',  ( 83.89975545334559115, -35.96486616408294879, 172.8035680471575972 ) ) ;
#22768=CARTESIAN_POINT ( 'NONE',  ( 2.500000000000013767, -30.00000000000000355, -31.87333685190803223 ) ) ;
#22769=CARTESIAN_POINT ( 'NONE',  ( -112.1928422005939296, -60.00000000000000000, 169.7268788603109897 ) ) ;
#22773=ADVANCED_FACE ( 'NONE', ( #19665 ), #20739, .F. ) ;
#22774=CARTESIAN_POINT ( 'NONE',  ( -85.02596717797761983, -28.87890062726760121, 172.9544161691474073 ) ) ;
#22775=EDGE_LOOP ( 'NONE', ( #42834, #30728 ) ) ;
#22781=CARTESIAN_POINT ( 'NONE',  ( -82.42609297192525730, -37.83176493496422665, 10.66243034473970397 ) ) ;
#22788=CARTESIAN_POINT ( 'NONE',  ( 77.57360435794387854, -29.99999999999995026, 180.9683789367223596 ) ) ;
#22789=CARTESIAN_POINT ( 'NONE',  ( -92.59939171350268339, -30.00000000000003908, 50.96567362325610873 ) ) ;
#22791=CARTESIAN_POINT ( 'NONE',  ( -59.99947494157906647, -60.34347021642804521, 82.29587262930701286 ) ) ;
#22794=CARTESIAN_POINT ( 'NONE',  ( 75.17919639455512026, -59.99999999999258904, 192.7260124497774996 ) ) ;
#22796=CARTESIAN_POINT ( 'NONE',  ( 3.071111545132248821, -53.39674026084604463, 32.78391494241015636 ) ) ;
#22805=CARTESIAN_POINT ( 'NONE',  ( -102.7609246503226359, -60.00000000000000000, 97.23335699513624775 ) ) ;
#22817=CARTESIAN_POINT ( 'NONE',  ( -38.10162474868671012, -39.51454026084844884, 37.25341933606826217 ) ) ;
#22821=CARTESIAN_POINT ( 'NONE',  ( 42.37181301095660757, -46.43334447366678575, 42.48581940379023081 ) ) ;
#22822=CARTESIAN_POINT ( 'NONE',  ( -19.43146043914380172, -4.830718742626120971E-12, 11.19959342723174522 ) ) ;
#22827=CARTESIAN_POINT ( 'NONE',  ( -57.19092749709510315, -38.34444523165630869, 87.83926972307914127 ) ) ;
#22837=CARTESIAN_POINT ( 'NONE',  ( 95.37157257520208020, -60.00000000000000711, 51.69444047675210641 ) ) ;
#22845=CARTESIAN_POINT ( 'NONE',  ( -88.76425966579064664, -30.00000000000024514, -15.41591536337368140 ) ) ;
#22858=CARTESIAN_POINT ( 'NONE',  ( 81.17915358008252724, -39.49775230550695682, 153.9097520608757463 ) ) ;
#22878=CARTESIAN_POINT ( 'NONE',  ( -5.863289337118752442, -12.99053128498974630, 32.07553765330735018 ) ) ;
#22888=CARTESIAN_POINT ( 'NONE',  ( -24.72970151039347186, -27.61749151431341431, -38.39745497380010164 ) ) ;
#22894=CARTESIAN_POINT ( 'NONE',  ( 101.7050805557714739, -57.63128474202212459, 203.3834090003539643 ) ) ;
#22899=CARTESIAN_POINT ( 'NONE',  ( -73.77751223451437568, -59.99999999999999289, 169.9644275812541991 ) ) ;
#22904=CARTESIAN_POINT ( 'NONE',  ( -86.39553218061814732, -17.42288545000702982, 179.1655162981548699 ) ) ;
#22919=CARTESIAN_POINT ( 'NONE',  ( 5.820808985963070725, 3.863013742957921305E-12, 21.65942590380143074 ) ) ;
#22921=CARTESIAN_POINT ( 'NONE',  ( 64.66821620130598092, -14.21045842199433373, -28.81313120037184916 ) ) ;
#22923=CARTESIAN_POINT ( 'NONE',  ( -79.28526668511025832, -36.02933522492092777, 138.0984090641172770 ) ) ;
#22925=CARTESIAN_POINT ( 'NONE',  ( 1.425929562426998531, -60.00000000000000000, 41.99999999999999289 ) ) ;
#22927=CARTESIAN_POINT ( 'NONE',  ( 91.32027366411901426, -57.61411389006468653, 204.2399109338346932 ) ) ;
#22935=CARTESIAN_POINT ( 'NONE',  ( -104.3522526634287857, -60.15517057847299043, 144.3591752484916242 ) ) ;
#22947=CARTESIAN_POINT ( 'NONE',  ( -24.48725402052853184, -14.21045842199434084, 35.52122251240935924 ) ) ;
#22948=CARTESIAN_POINT ( 'NONE',  ( 26.15828352856528127, -25.56935877229565790, 29.61310315546906224 ) ) ;
#22960=CARTESIAN_POINT ( 'NONE',  ( 49.60909704566071099, -60.00000000000000711, -37.98112837208373094 ) ) ;
#22961=CARTESIAN_POINT ( 'NONE',  ( 83.13875906005428362, -29.99999999999996447, 153.7901336831974390 ) ) ;
#22985=CARTESIAN_POINT ( 'NONE',  ( 64.70032873768002446, -39.48212153678270653, 85.31995070285097427 ) ) ;
#22999=DIRECTION ( 'NONE',  ( -0.000000000000000000, -1.000000000000000000, -0.000000000000000000 ) ) ;
#23002=CARTESIAN_POINT ( 'NONE',  ( 87.02191047559196591, -31.70738880027288431, 187.4629506568093689 ) ) ;
#23006=( NAMED_UNIT ( * ) PLANE_ANGLE_UNIT ( ) SI_UNIT ( $, .RADIAN. ) );
#23010=CARTESIAN_POINT ( 'NONE',  ( 36.54387785002509759, -60.00000000000001421, 47.89680925484002216 ) ) ;
#23012=CARTESIAN_POINT ( 'NONE',  ( -99.80602541531122540, -30.00000000000000355, 186.3886247876614846 ) ) ;
#23018=CARTESIAN_POINT ( 'NONE',  ( 35.30542147758094274, -57.69548023038977647, 49.46059037094081390 ) ) ;
#23025=CARTESIAN_POINT ( 'NONE',  ( -8.434902168003450385, -60.00000000000000711, 39.63584717613949948 ) ) ;
#23027=CARTESIAN_POINT ( 'NONE',  ( -86.53663329270624160, -57.41224747399611772, 193.5711379720445109 ) ) ;
#23031=CARTESIAN_POINT ( 'NONE',  ( -11.20631249100435589, -29.03129763674975905, 28.75315964071688413 ) ) ;
#23032=CARTESIAN_POINT ( 'NONE',  ( -106.4735328932949869, -59.99999999999999289, 175.0934596608935863 ) ) ;
#23040=CARTESIAN_POINT ( 'NONE',  ( 65.16906654191903669, -60.00000000000000000, 118.9734969953735515 ) ) ;
#23046=CARTESIAN_POINT ( 'NONE',  ( 24.85181238201470322, -30.00000000000000000, 38.32581332381749206 ) ) ;
#23059=CARTESIAN_POINT ( 'NONE',  ( -88.50868962893154901, -59.99999999999261036, 204.1120144510070702 ) ) ;
#23061=CARTESIAN_POINT ( 'NONE',  ( 83.70906304977542334, -60.00000000000002132, 199.3180261249159742 ) ) ;
#23063=CARTESIAN_POINT ( 'NONE',  ( -109.0466421874928074, -29.99999999999997513, 159.8085545269249224 ) ) ;
#23064=CARTESIAN_POINT ( 'NONE',  ( 9.379153979492304671, -56.87790722318686676, 33.37334884318637762 ) ) ;
#23066=CARTESIAN_POINT ( 'NONE',  ( 97.17332080658498228, -38.00000000000000711, 120.7792972779389373 ) ) ;
#23068=CARTESIAN_POINT ( 'NONE',  ( -46.34968830293420439, -53.35688838113154731, 49.29538158241714996 ) ) ;
#23079=CARTESIAN_POINT ( 'NONE',  ( 86.99672156470798257, -29.99999999998241051, 198.2267927734325497 ) ) ;
#23085=CARTESIAN_POINT ( 'NONE',  ( 98.90563218758491359, -30.00000000000000000, 144.2321003841678646 ) ) ;
#23101=CARTESIAN_POINT ( 'NONE',  ( 77.91253027013023313, -38.56360447836954108, 187.9343819089818339 ) ) ;
#23103=CARTESIAN_POINT ( 'NONE',  ( 84.43118809173812167, -45.28802927494923125, -4.046620873543590235 ) ) ;
#23118=SURFACE_SIDE_STYLE ('',( #73214 ) ) ;
#23123=CARTESIAN_POINT ( 'NONE',  ( 28.88851691220557072, -31.70747628257775119, 39.94846750239052824 ) ) ;
#23129=CARTESIAN_POINT ( 'NONE',  ( 86.20252288539451513, -21.32135871581905917, 177.4573265017570805 ) ) ;
#23133=CARTESIAN_POINT ( 'NONE',  ( 94.19233705074088903, -57.67257139432003044, 22.56487249148564089 ) ) ;
#23147=CARTESIAN_POINT ( 'NONE',  ( -7.665484706731373166, -22.68362488985719239, -30.52813087708529949 ) ) ;
#23158=CARTESIAN_POINT ( 'NONE',  ( -37.34263480636265342, -21.77016502673909315, -27.75688875962726243 ) ) ;
#23164=CARTESIAN_POINT ( 'NONE',  ( -90.87915574240211924, -60.00000000000000711, -17.17345031315606718 ) ) ;
#23167=CARTESIAN_POINT ( 'NONE',  ( 97.79202014402906684, -52.81045661888177278, 195.1525401136383380 ) ) ;
#23170=CARTESIAN_POINT ( 'NONE',  ( -80.23351082821501734, -56.88084892736377896, 171.5714587829481275 ) ) ;
#23177=EDGE_CURVE ( 'NONE', #6442, #74331, #34649, .T. ) ;
#23182=CARTESIAN_POINT ( 'NONE',  ( -107.9249424950986906, -57.65976581800653378, 199.0938304663491749 ) ) ;
#23187=CARTESIAN_POINT ( 'NONE',  ( -42.61015704936735915, -60.00000000000002842, -41.65925318937349431 ) ) ;
#23189=CARTESIAN_POINT ( 'NONE',  ( -21.36131896786188378, -60.00000000000002132, 42.72829597934922674 ) ) ;
#23191=CARTESIAN_POINT ( 'NONE',  ( -54.02244926336294384, -36.03399488101162973, 56.88089687501458513 ) ) ;
#23196=CARTESIAN_POINT ( 'NONE',  ( -98.75517273381713323, -60.33577106688449732, 196.3359775619156267 ) ) ;
#23203=CARTESIAN_POINT ( 'NONE',  ( 91.32721440143633629, -38.40026762824159334, -10.23153405760255197 ) ) ;
#23210=CARTESIAN_POINT ( 'NONE',  ( 82.11220676860955336, -29.99999999999999645, 146.7337359989799381 ) ) ;
#23217=CARTESIAN_POINT ( 'NONE',  ( 50.06701392515735449, -46.43829384136844141, 53.18051123607877884 ) ) ;
#23218=CARTESIAN_POINT ( 'NONE',  ( -10.00000000000000000, -15.00000000000000000, 10.00000000000000178 ) ) ;
#23220=CARTESIAN_POINT ( 'NONE',  ( -110.5050194399237000, -38.35611022050278507, 182.3353135514281007 ) ) ;
#23222=CARTESIAN_POINT ( 'NONE',  ( 108.7582993695906453, -38.35601099000350445, 143.4284137783402286 ) ) ;
#23225=CARTESIAN_POINT ( 'NONE',  ( 100.3592460791940368, -52.71701722894771081, 125.2415931128299746 ) ) ;
#23231=CARTESIAN_POINT ( 'NONE',  ( 80.14078518684225116, -60.00000000000000711, 196.1583502975230999 ) ) ;
#23235=CARTESIAN_POINT ( 'NONE',  ( 57.05946111255018849, -46.43605047800132724, 67.94431784311699118 ) ) ;
#23240=CARTESIAN_POINT ( 'NONE',  ( -94.79426203886504254, -38.48922377310545784, 201.2511363089133738 ) ) ;
#23248=CARTESIAN_POINT ( 'NONE',  ( 2.500000000000002220, -8.000000000000000000, -17.89626171146327138 ) ) ;
#23250=CARTESIAN_POINT ( 'NONE',  ( 82.69827821110598620, -46.48414492152276267, 177.5876388581721699 ) ) ;
#23288=CARTESIAN_POINT ( 'NONE',  ( -2.499999999999978684, -26.27793898787864890, 28.26590982313834743 ) ) ;
#23291=CARTESIAN_POINT ( 'NONE',  ( -112.2289492798716566, -60.00000000000000000, 172.3416561640010798 ) ) ;
#23293=CARTESIAN_POINT ( 'NONE',  ( 5.513005039581024867E-05, -56.88429987697963952, 33.37036660576565339 ) ) ;
#23299=CARTESIAN_POINT ( 'NONE',  ( -84.00855389726528699, -35.95715071644597316, 173.7904060909261830 ) ) ;
#23312=CARTESIAN_POINT ( 'NONE',  ( 105.4249980201500136, -14.21045842199437992, 149.5332359265665900 ) ) ;
#23313=CARTESIAN_POINT ( 'NONE',  ( -102.0721909215208427, -14.21045842199424314, 125.2231725879975954 ) ) ;
#23314=CARTESIAN_POINT ( 'NONE',  ( -62.57693323230586913, -46.43962359317384170, 82.71524195557942960 ) ) ;
#23317=CARTESIAN_POINT ( 'NONE',  ( 47.44420658916666156, -59.99999999998034639, 71.74659173365184017 ) ) ;
#23319=CARTESIAN_POINT ( 'NONE',  ( 4.937715695759576327E-05, -53.39687648151041799, 32.78912937318744980 ) ) ;
#23327=CARTESIAN_POINT ( 'NONE',  ( -107.9034470886846293, -59.99999999999998579, 195.8034858462665682 ) ) ;
#23340=CARTESIAN_POINT ( 'NONE',  ( -34.27342318777111529, -60.30598541217121067, 38.86820545827612960 ) ) ;
#23342=CARTESIAN_POINT ( 'NONE',  ( 37.73904784516052047, -32.59126324431009181, 35.55316273275742134 ) ) ;
#23344=CARTESIAN_POINT ( 'NONE',  ( 10.45706415777664411, -1.734723475976807094E-15, 13.60704923275374156 ) ) ;
#23348=CARTESIAN_POINT ( 'NONE',  ( -58.38338069927746687, -38.34396774324475388, 91.39933602100487064 ) ) ;
#23362=CARTESIAN_POINT ( 'NONE',  ( 98.38154907885181899, -60.00000000000002132, 71.28785646064007153 ) ) ;
#23368=CARTESIAN_POINT ( 'NONE',  ( -90.08654180215627605, -30.00000000002151879, -7.787506975155032762 ) ) ;
#23383=CARTESIAN_POINT ( 'NONE',  ( 79.16796225250830332, -56.84377630782282154, 161.1938245440812238 ) ) ;
#23391=CARTESIAN_POINT ( 'NONE',  ( -43.09316981551443604, -57.68566503113564892, 61.19926976090692960 ) ) ;
#23401=CARTESIAN_POINT ( 'NONE',  ( -22.41876583820823399, -18.13681534289955621, 31.47717130250301310 ) ) ;
#23414=CARTESIAN_POINT ( 'NONE',  ( 16.29626706464026142, -24.48722485856961484, -38.53282975460095372 ) ) ;
#23415=CARTESIAN_POINT ( 'NONE',  ( -54.73325009968991139, -30.00000000000000355, 55.16748736607294035 ) ) ;
#23421=CARTESIAN_POINT ( 'NONE',  ( 102.5075976590412807, -57.63377371069149291, 203.0662124941956108 ) ) ;
#23427=CARTESIAN_POINT ( 'NONE',  ( -73.05702173334942984, -60.00000000000000711, 162.9805030633762613 ) ) ;
#23434=CARTESIAN_POINT ( 'NONE',  ( -84.57188724812456826, -46.57292530288317067, 186.4415227103431505 ) ) ;
#23438=CIRCLE ( 'NONE', #16561, 15.00000000000000000 ) ;
#23444=CARTESIAN_POINT ( 'NONE',  ( -85.36974942761283103, -60.20515523833639548, -15.42856006348832310 ) ) ;
#23454=CARTESIAN_POINT ( 'NONE',  ( 88.18294634653494768, -59.99999999999992895, -24.85591942078231043 ) ) ;
#23455=CARTESIAN_POINT ( 'NONE',  ( -78.23156018859863536, -42.96802624942629478, 138.8422877898725858 ) ) ;
#23457=CARTESIAN_POINT ( 'NONE',  ( 34.17730524443083340, -14.21045842199440656, 38.95112099893761837 ) ) ;
#23459=CARTESIAN_POINT ( 'NONE',  ( 96.75771235523380653, -57.62241948994476104, 204.4691479018955818 ) ) ;
#23466=DIRECTION ( 'NONE',  ( 1.000000000000000000, 0.000000000000000000, -3.673940397442057649E-17 ) ) ;
#23477=CARTESIAN_POINT ( 'NONE',  ( -34.60361718403136422, -60.00000000000001421, 49.20626982406709971 ) ) ;
#23478=CARTESIAN_POINT ( 'NONE',  ( 30.28165720518637372, -49.90556239820476492, 35.08629451775517794 ) ) ;
#23491=CARTESIAN_POINT ( 'NONE',  ( 7.700048951879978176, -60.00000000000000000, -42.50223864661403184 ) ) ;
#23522=CARTESIAN_POINT ( 'NONE',  ( 69.47261160691843429, -60.32957453810588788, 112.5472032990401487 ) ) ;
#23544=CARTESIAN_POINT ( 'NONE',  ( 15.38671495384722121, -59.99999999999999289, 39.81262336454445006 ) ) ;
#23545=CARTESIAN_POINT ( 'NONE',  ( -97.65307766490704466, -30.00000000000000000, 190.8028841120875256 ) ) ;
#23548=CARTESIAN_POINT ( 'NONE',  ( 38.78005064836850124, -57.69447179130985859, 53.76168839330274807 ) ) ;
#23552=CARTESIAN_POINT ( 'NONE',  ( 15.68733860615400033, -24.30949475465576626, -38.52672339115742517 ) ) ;
#23554=CARTESIAN_POINT ( 'NONE',  ( -12.56390471583231516, -60.00000000000002132, 39.70168213610190833 ) ) ;
#23557=CARTESIAN_POINT ( 'NONE',  ( -87.19385550499211490, -31.68974481596827175, 187.9067576323665776 ) ) ;
#23562=CARTESIAN_POINT ( 'NONE',  ( -14.39691347112102093, -29.03163114769574449, 28.84164502424407672 ) ) ;
#23564=CARTESIAN_POINT ( 'NONE',  ( -102.6649796019329699, -60.00000000000002132, 193.3001960811608626 ) ) ;
#23571=DIRECTION ( 'NONE',  ( 0.000000000000000000, 0.000000000000000000, 1.000000000000000000 ) ) ;
#23573=CARTESIAN_POINT ( 'NONE',  ( 72.36529781780690485, -59.99999999999998579, 157.0781579372900580 ) ) ;
#23580=CARTESIAN_POINT ( 'NONE',  ( 24.48575568784926304, -14.21045842199439946, 35.52093559979998361 ) ) ;
#23594=CARTESIAN_POINT ( 'NONE',  ( -113.7086509678886443, -59.99999999998047429, 155.4592733101652584 ) ) ;
#23596=CARTESIAN_POINT ( 'NONE',  ( 46.21931631244920169, -60.00000000000000000, 63.08554439955615578 ) ) ;
#23599=CARTESIAN_POINT ( 'NONE',  ( -114.5103415054848170, -60.00000000000004263, 177.0886483751272351 ) ) ;
#23600=CARTESIAN_POINT ( 'NONE',  ( 15.36438022688010463, -22.06846381147260772, 27.72742713275420101 ) ) ;
#23601=CARTESIAN_POINT ( 'NONE',  ( 90.58584440353838829, -38.00000000000000000, 81.86263311294858624 ) ) ;
#23604=CARTESIAN_POINT ( 'NONE',  ( -44.99960878686916743, -56.80572573438033857, 48.30738373556244625 ) ) ;
#23616=CARTESIAN_POINT ( 'NONE',  ( 99.42104296369386418, -30.00000000004165557, 199.3229471623391476 ) ) ;
#23620=CARTESIAN_POINT ( 'NONE',  ( 90.42852211739197799, -30.00000000000000000, 90.99945873017442466 ) ) ;
#23631=CARTESIAN_POINT ( 'NONE',  ( 77.65721028447464391, -38.53209962432212876, 187.0521431165007584 ) ) ;
#23633=CARTESIAN_POINT ( 'NONE',  ( 72.13138110526622881, -38.00000000000000711, 108.4011625346426797 ) ) ;
#23653=DIRECTION ( 'NONE',  ( 0.000000000000000000, 0.000000000000000000, 1.000000000000000000 ) ) ;
#23660=CARTESIAN_POINT ( 'NONE',  ( 83.77195690154300678, -57.39043513791891371, 190.2506195938281621 ) ) ;
#23664=CARTESIAN_POINT ( 'NONE',  ( 93.84281965440075624, -57.67495174030868554, 10.52530039810905116 ) ) ;
#23671=CARTESIAN_POINT ( 'NONE',  ( -82.86493196561585250, -38.00000000000003553, 166.1273331999570928 ) ) ;
#23684=CARTESIAN_POINT ( 'NONE',  ( 65.65969153816354265, -29.79516960803964665, -22.78676046141628575 ) ) ;
#23693=CARTESIAN_POINT ( 'NONE',  ( -45.16882421246708645, -60.22825351688758388, -33.02234666222834392 ) ) ;
#23696=AXIS2_PLACEMENT_3D ( 'NONE', #50235, #84737, #99847 ) ;
#23698=CARTESIAN_POINT ( 'NONE',  ( -92.64811155113156360, -59.99999999999998579, -3.658885834359205003 ) ) ;
#23702=CARTESIAN_POINT ( 'NONE',  ( 95.34251263761402129, -37.71227104075504144, 193.0165489376654477 ) ) ;
#23705=CARTESIAN_POINT ( 'NONE',  ( -83.46189083830699929, -29.07720453051282661, 157.7181293371499464 ) ) ;
#23718=CARTESIAN_POINT ( 'NONE',  ( -101.2734545671114290, -57.63007487344309254, 203.5435050992661843 ) ) ;
#23725=CARTESIAN_POINT ( 'NONE',  ( -40.75117554026711275, -14.21045842199432663, -34.22202116092960011 ) ) ;
#23729=CARTESIAN_POINT ( 'NONE',  ( -52.52702786332168472, -49.90965349917357230, 59.15625794695527162 ) ) ;
#23735=CARTESIAN_POINT ( 'NONE',  ( -98.52404613076176076, -37.74647085490894938, 192.2268697399963742 ) ) ;
#23739=CARTESIAN_POINT ( 'NONE',  ( 91.44830385819240348, -38.39066018178733231, -8.169144241885213376 ) ) ;
#23745=CARTESIAN_POINT ( 'NONE',  ( 84.03603373241958252, -30.00000000000000000, 161.3276072815756663 ) ) ;
#23752=CIRCLE ( 'NONE', #15087, 7.500000000001509015 ) ;
#23755=CARTESIAN_POINT ( 'NONE',  ( 49.98712176156696785, -49.90156039724934800, 54.21681932135436455 ) ) ;
#23759=CARTESIAN_POINT ( 'NONE',  ( -90.85419583802016064, -38.34570451894640541, 4.396493097181871867 ) ) ;
#23763=CARTESIAN_POINT ( 'NONE',  ( 90.86170511367741653, -38.35175402733357686, 20.64558181097320144 ) ) ;
#23766=CARTESIAN_POINT ( 'NONE',  ( 100.0259651621010306, -60.15125716094357955, 115.3354766105753555 ) ) ;
#23772=CARTESIAN_POINT ( 'NONE',  ( 77.86138069022020147, -60.00000000000000000, 192.5414314693734070 ) ) ;
#23776=CARTESIAN_POINT ( 'NONE',  ( 55.22303882701753253, -49.90717449039305365, 65.08233922066710875 ) ) ;
#23778=LINE ( 'NONE', #89017, #66898 ) ;
#23781=CARTESIAN_POINT ( 'NONE',  ( -47.43396820366045574, -30.00000000002712497, 59.40601916810901173 ) ) ;
#23786=CARTESIAN_POINT ( 'NONE',  ( 89.99999999999997158, -52.00000000000000000, 194.0238439516549818 ) ) ;
#23791=ORIENTED_EDGE ( 'NONE', *, *, #51268, .F. ) ;
#23792=CARTESIAN_POINT ( 'NONE',  ( 81.66341672991298140, -57.04221095040819023, 183.2393683767488142 ) ) ;
#23810=CARTESIAN_POINT ( 'NONE',  ( -15.71980515041875393, -23.09657402895575729, 36.03920351886992535 ) ) ;
#23818=CARTESIAN_POINT ( 'NONE',  ( 89.99999999999997158, -60.00000000000000000, 198.0238439516549818 ) ) ;
#23835=CARTESIAN_POINT ( 'NONE',  ( -111.5755056577839497, -60.00000000000000000, 158.2576086698429094 ) ) ;
#23837=CARTESIAN_POINT ( 'NONE',  ( -8.046879842201352779E-06, -18.58623113382856573, 26.98735514857380480 ) ) ;
#23843=CARTESIAN_POINT ( 'NONE',  ( -81.85741221238644982, -53.50462993550565471, 180.4532786401848341 ) ) ;
#23855=CARTESIAN_POINT ( 'NONE',  ( 114.0149080866908946, -60.00000000000002132, 183.4845764411877553 ) ) ;
#23857=CARTESIAN_POINT ( 'NONE',  ( -108.5047409391136455, -30.00000000000001776, 153.5997188701533105 ) ) ;
#23858=CARTESIAN_POINT ( 'NONE',  ( -62.48275913083217858, -53.39271311663005548, 85.99345403212120686 ) ) ;
#23861=CARTESIAN_POINT ( 'NONE',  ( 108.9093010043188343, -60.00000000000492406, 198.5394929600591070 ) ) ;
#23863=CARTESIAN_POINT ( 'NONE',  ( 2.040551993176147771, -53.39679212784579931, 32.78650623838447586 ) ) ;
#23873=CARTESIAN_POINT ( 'NONE',  ( -112.0155942784085710, -59.99999999999998579, 179.5554985363227729 ) ) ;
#23883=CARTESIAN_POINT ( 'NONE',  ( 90.89309866034619745, -59.99999999999998579, 60.81559558904974239 ) ) ;
#23884=CARTESIAN_POINT ( 'NONE',  ( -32.49993360873129689, -22.15177377451222540, 30.86871524635706265 ) ) ;
#23886=CARTESIAN_POINT ( 'NONE',  ( 37.17835306669755369, -22.20693324183691075, 33.02635006318946154 ) ) ;
#23892=CARTESIAN_POINT ( 'NONE',  ( -72.86006754029503441, -38.32651382585556377, 151.4076042794326042 ) ) ;
#23904=CARTESIAN_POINT ( 'NONE',  ( 100.7769336070389983, -59.99999999999999289, 85.59131652555993242 ) ) ;
#23910=CARTESIAN_POINT ( 'NONE',  ( -87.74897877105536281, -30.00000000000501998, -17.46874925390407896 ) ) ;
#23927=CARTESIAN_POINT ( 'NONE',  ( 79.82907406774054948, -56.85525210295124054, 167.4536056965665125 ) ) ;
#23935=CARTESIAN_POINT ( 'NONE',  ( -27.27894591530610668, -57.67773572996152609, 43.94474244872281332 ) ) ;
#23948=CARTESIAN_POINT ( 'NONE',  ( -27.13328449130634112, -20.30828638014859422, 31.75027141071463888 ) ) ;
#23960=CARTESIAN_POINT ( 'NONE',  ( -33.87327693568649778, -30.97787551643977366, -37.97348367960884019 ) ) ;
#23965=LINE ( 'NONE', #81086, #89197 ) ;
#23966=CARTESIAN_POINT ( 'NONE',  ( 106.4547888626981944, -57.65150656016882635, 200.5657376461139449 ) ) ;
#23970=LINE ( 'NONE', #38671, #42447 ) ;
#23972=CARTESIAN_POINT ( 'NONE',  ( -74.34185808010607843, -60.00000000000000000, 175.6139210523332963 ) ) ;
#23973=AXIS2_PLACEMENT_3D ( 'NONE', #11701, #59219, #51093 ) ;
#23979=CARTESIAN_POINT ( 'NONE',  ( -85.84496634730722064, -28.47654455628507009, 180.7473491047089169 ) ) ;
#23985=CARTESIAN_POINT ( 'NONE',  ( -84.42827057453619943, -45.27066986597937159, -4.045256569822196724 ) ) ;
#23991=CARTESIAN_POINT ( 'NONE',  ( -17.01589776168603407, -1.734723475976807094E-15, 2.227375807157432774 ) ) ;
#23995=CARTESIAN_POINT ( 'NONE',  ( -69.60683966046387638, -29.99999999999998224, -29.88974110699236775 ) ) ;
#23996=CARTESIAN_POINT ( 'NONE',  ( -77.18609064198581393, -49.90775283772178028, 139.5545092987445059 ) ) ;
#23998=CARTESIAN_POINT ( 'NONE',  ( 20.75554216095374116, -29.99999999999998579, 37.60191050100322485 ) ) ;
#24000=CARTESIAN_POINT ( 'NONE',  ( 91.04805003644649730, -57.66417010318413361, -20.95954831595424039 ) ) ;
#24016=CARTESIAN_POINT ( 'NONE',  ( 29.80797822681026688, -53.38109471923124261, 35.51269461402811345 ) ) ;
#24020=EDGE_LOOP ( 'NONE', ( #37640, #38169, #91803, #59709 ) ) ;
#24030=CARTESIAN_POINT ( 'NONE',  ( 65.87419555395186421, -60.00000000000000711, -33.93111748855666576 ) ) ;
#24054=CARTESIAN_POINT ( 'NONE',  ( -26.99263046833200619, -59.99999999999997868, 35.69452638192248628 ) ) ;
#24055=CARTESIAN_POINT ( 'NONE',  ( 64.92191423604261047, -36.00617188022724946, 84.15699025978140924 ) ) ;
#24060=CARTESIAN_POINT ( 'NONE',  ( -89.99999999999997158, -52.00000000000000000, 196.0238439516549818 ) ) ;
#24077=CARTESIAN_POINT ( 'NONE',  ( 4.449340811590402289, -60.00000000000000000, 39.63040262224204469 ) ) ;
#24078=CARTESIAN_POINT ( 'NONE',  ( -98.54871067950367092, -30.00000000000000355, 189.7749550243679835 ) ) ;
#24082=CARTESIAN_POINT ( 'NONE',  ( 44.88275167603845262, -57.68329172827992579, 64.90723355357903301 ) ) ;
#24087=CARTESIAN_POINT ( 'NONE',  ( 10.12775410031062151, -22.65524328215749605, -38.54261129078143000 ) ) ;
#24090=CARTESIAN_POINT ( 'NONE',  ( -21.09521276825200786, -60.00000000000000000, 40.37433778268253803 ) ) ;
#24094=CARTESIAN_POINT ( 'NONE',  ( -86.75485909622595670, -46.46991862354892078, 190.6011527551186475 ) ) ;
#24098=CARTESIAN_POINT ( 'NONE',  ( -6.163436733616805441, -49.92086198580086176, 32.19980418369003417 ) ) ;
#24111=CARTESIAN_POINT ( 'NONE',  ( 59.47617687438206957, -60.00000000000000000, 98.79634657976947665 ) ) ;
#24118=CARTESIAN_POINT ( 'NONE',  ( 48.02079947780210745, -30.00000000000000711, 60.50169175835635826 ) ) ;
#24135=CARTESIAN_POINT ( 'NONE',  ( -66.01181427793642342, -59.99999999999997868, 132.9137452780753392 ) ) ;
#24138=CARTESIAN_POINT ( 'NONE',  ( 74.66296238351618797, -59.99999999999997868, 178.6152739014907525 ) ) ;
#24139=CARTESIAN_POINT ( 'NONE',  ( -106.7878682580589071, -14.21045842199432663, 165.8353880188381027 ) ) ;
#24140=CARTESIAN_POINT ( 'NONE',  ( 17.95348893241579091, -42.95395786364728963, 31.37188985704841215 ) ) ;
#24142=CARTESIAN_POINT ( 'NONE',  ( 98.86178962493093536, -37.99999999999999289, 192.0563723494719568 ) ) ;
#24144=CARTESIAN_POINT ( 'NONE',  ( -46.29616362358941473, -39.53031546193722079, 45.26312817876173966 ) ) ;
#24156=CARTESIAN_POINT ( 'NONE',  ( 102.2769841588865205, -30.00000000001111999, 197.9840571922390779 ) ) ;
#24159=CARTESIAN_POINT ( 'NONE',  ( 100.5419430498661768, -30.00000000000000000, 159.7472965000894192 ) ) ;
#24176=CARTESIAN_POINT ( 'NONE',  ( 81.61186971388572431, -38.84191813924242354, 195.4159226793195216 ) ) ;
#24192=CARTESIAN_POINT ( 'NONE',  ( 17.36848429690531859, -24.01528219279489917, 36.27201406405939821 ) ) ;
#24196=CARTESIAN_POINT ( 'NONE',  ( 85.22412109468345420, -42.93386880055312815, 186.3705244525062028 ) ) ;
#24200=CARTESIAN_POINT ( 'NONE',  ( 82.30040181591539294, -57.67111186717970384, -28.85252992913370917 ) ) ;
#24203=CARTESIAN_POINT ( 'NONE',  ( -81.42887515339373294, -30.00000000000000355, -2.436421276796028934 ) ) ;
#24216=CARTESIAN_POINT ( 'NONE',  ( -2.499999999981197707, -21.99834632368703069, -30.53960193249073640 ) ) ;
#24218=CARTESIAN_POINT ( 'NONE',  ( 70.74177944523411554, -29.99609282501852192, -20.32620075006109062 ) ) ;
#24227=CARTESIAN_POINT ( 'NONE',  ( -63.53617277140842390, -34.58942015808621306, -24.20806359249350592 ) ) ;
#24231=LINE ( 'NONE', #9062, #86217 ) ;
#24235=CARTESIAN_POINT ( 'NONE',  ( -49.94482164224617549, -59.99999999999999289, -37.91551347345771461 ) ) ;
#24239=CARTESIAN_POINT ( 'NONE',  ( 96.57334640236589962, -45.27060142599663095, 194.0782599365211922 ) ) ;
#24255=CARTESIAN_POINT ( 'NONE',  ( -27.27894591530610668, -57.67773572996152609, 43.94474244872281332 ) ) ;
#24260=CARTESIAN_POINT ( 'NONE',  ( -17.09952670627316706, -60.00000000000001421, -44.43607591113852351 ) ) ;
#24262=CARTESIAN_POINT ( 'NONE',  ( -53.08102895155478507, -18.70615072099417731, 48.69294712436818884 ) ) ;
#24266=CARTESIAN_POINT ( 'NONE',  ( -99.29599809189417670, -45.25123437682626104, 193.1448974876303168 ) ) ;
#24270=CARTESIAN_POINT ( 'NONE',  ( 90.59251118385301993, -38.35027144420563161, 14.22736211764586223 ) ) ;
#24275=CARTESIAN_POINT ( 'NONE',  ( 81.12011883507125276, -30.00000000000000711, 140.6539142541519709 ) ) ;
#24285=CARTESIAN_POINT ( 'NONE',  ( 50.52250052960007309, -25.65762928410081400, 46.96345956391975562 ) ) ;
#24290=CARTESIAN_POINT ( 'NONE',  ( -107.9473917804004941, -38.35630723407592768, 137.4504611278363768 ) ) ;
#24293=CARTESIAN_POINT ( 'NONE',  ( 90.86173999633324172, -38.35175481737118020, 20.64625151213274989 ) ) ;
#24296=CARTESIAN_POINT ( 'NONE',  ( 98.65904876352816189, -37.84861505694159689, 130.4062528344186944 ) ) ;
#24301=CARTESIAN_POINT ( 'NONE',  ( 74.37097096341283020, -59.99999999999999289, 175.8909987187326749 ) ) ;
#24308=CARTESIAN_POINT ( 'NONE',  ( 57.60575626135791083, -18.66803500383183589, 57.28382109102082609 ) ) ;
#24313=CARTESIAN_POINT ( 'NONE',  ( -77.55597287852873478, -29.99999999981872989, 179.8129485814087900 ) ) ;
#24324=CARTESIAN_POINT ( 'NONE',  ( 83.30572369024382340, -42.97726960787509398, 177.5867044128110592 ) ) ;
#24341=CARTESIAN_POINT ( 'NONE',  ( -27.09524894485997493, -30.47611868180892003, 39.10809118615605939 ) ) ;
#24347=EDGE_LOOP ( 'NONE', ( #66022, #98353 ) ) ;
#24360=CARTESIAN_POINT ( 'NONE',  ( -2.499999999999978684, -29.99999999999999645, 28.88619816519791073 ) ) ;
#24362=CARTESIAN_POINT ( 'NONE',  ( -102.3275229563159598, -60.00000000000000000, 94.65514192416549122 ) ) ;
#24364=CARTESIAN_POINT ( 'NONE',  ( 3.215662123186951678E-05, -42.95772942492470747, 31.04927153042315524 ) ) ;
#24370=CARTESIAN_POINT ( 'NONE',  ( -83.11698702663863969, -42.98028782721130625, 176.1582416638941027 ) ) ;
#24388=CARTESIAN_POINT ( 'NONE',  ( 103.8765618273974951, -14.21045842199444209, 137.3601107225250360 ) ) ;
#24391=CARTESIAN_POINT ( 'NONE',  ( -105.4253011914250067, -14.21045842199428222, 149.5333493894512458 ) ) ;
#24392=CARTESIAN_POINT ( 'NONE',  ( -63.57062938988862300, -36.00914355728743743, 80.26143161827371841 ) ) ;
#24395=CARTESIAN_POINT ( 'NONE',  ( 94.31441069461205018, -60.00000000001458744, 17.33446251183617903 ) ) ;
#24397=CARTESIAN_POINT ( 'NONE',  ( 0.9846689345368905277, -18.58625483750316576, 26.98735909918624287 ) ) ;
#24405=CARTESIAN_POINT ( 'NONE',  ( -107.3823593786986095, -60.00000000000001421, 124.9939677557050430 ) ) ;
#24416=CARTESIAN_POINT ( 'NONE',  ( 103.3323615576035195, -60.00000000000002132, 136.8515639484661790 ) ) ;
#24417=CARTESIAN_POINT ( 'NONE',  ( -33.78495839492549635, -56.84029651377081649, 37.95014195405838109 ) ) ;
#24421=CARTESIAN_POINT ( 'NONE',  ( 42.25895859003348676, -42.97903088149762851, 41.54068014075424742 ) ) ;
#24429=CARTESIAN_POINT ( 'NONE',  ( -81.13099867360766382, -38.83658557384262622, 194.7852543518826849 ) ) ;
#24441=CARTESIAN_POINT ( 'NONE',  ( 110.0499776139819659, -59.99999999999999289, 143.8492112426671667 ) ) ;
#24446=CARTESIAN_POINT ( 'NONE',  ( -93.51384743021765189, -30.00000000000006040, 191.2118971003746708 ) ) ;
#24456=VERTEX_POINT ( 'NONE', #79328 ) ;
#24458=ORIENTED_EDGE ( 'NONE', *, *, #104411, .T. ) ;
#24459=CARTESIAN_POINT ( 'NONE',  ( 82.38380642140619159, -29.09073277922306744, 149.5372663468040741 ) ) ;
#24469=CARTESIAN_POINT ( 'NONE',  ( 67.67130416077930022, -59.99999999999999289, -27.26907627581506333 ) ) ;
#24482=CARTESIAN_POINT ( 'NONE',  ( 24.10582191788833484, -28.43080354620355266, 37.96870486749567419 ) ) ;
#24495=CARTESIAN_POINT ( 'NONE',  ( 110.2197559186844131, -57.66896312012423920, 195.6918597009357370 ) ) ;
#24503=CARTESIAN_POINT ( 'NONE',  ( -74.34326984540557248, -60.00000000000000711, 175.6274979054055336 ) ) ;
#24507=CARTESIAN_POINT ( 'NONE',  ( -84.74621718593478192, -50.19506395242900254, 188.7085204688150952 ) ) ;
#24513=CARTESIAN_POINT ( 'NONE',  ( -85.72632401489656218, -52.73136465668492434, -5.089855646812738499 ) ) ;
#24519=CARTESIAN_POINT ( 'NONE',  ( 13.60704923275372202, -1.734723475976807094E-15, 10.45706415777666365 ) ) ;
#24521=CARTESIAN_POINT ( 'NONE',  ( 48.21450566731007825, -29.99999999999995381, -35.59756164575514958 ) ) ;
#24522=CARTESIAN_POINT ( 'NONE',  ( -75.09116195550693362, -60.32198986609109426, 137.4145651127319070 ) ) ;
#24524=CARTESIAN_POINT ( 'NONE',  ( 16.35858893754161869, -14.21045842199445630, 34.55986707822809478 ) ) ;
#24526=CARTESIAN_POINT ( 'NONE',  ( 93.83421280875700177, -57.67400127416684796, 13.19124553429083058 ) ) ;
#24540=CARTESIAN_POINT ( 'NONE',  ( 1.295095875561511761E-05, -30.00000000000000000, 37.00000000000000711 ) ) ;
#24541=CARTESIAN_POINT ( 'NONE',  ( 31.37193178408734795, -46.43139637310807899, 34.89162135181897639 ) ) ;
#24556=CARTESIAN_POINT ( 'NONE',  ( 33.19500532560861927, -60.00000000000002842, -40.53309893464972902 ) ) ;
#24580=CARTESIAN_POINT ( 'NONE',  ( -22.92989048780488304, -59.99999999999997158, 34.79415195187766585 ) ) ;
#24581=CARTESIAN_POINT ( 'NONE',  ( 69.47498401038441784, -25.58548699416417094, 92.27391141522187468 ) ) ;
#24584=CARTESIAN_POINT ( 'NONE',  ( -44.70137845890145911, -57.67116879762227910, -40.89012893473564958 ) ) ;
#24603=CARTESIAN_POINT ( 'NONE',  ( -95.47858839875321735, -29.99999999999999289, 191.3280271152898706 ) ) ;
#24607=CARTESIAN_POINT ( 'NONE',  ( 73.80742417545810952, -57.62089382719297959, 186.0993484855978579 ) ) ;
#24611=CARTESIAN_POINT ( 'NONE',  ( 19.40646391855202779, -25.62022252646447384, -38.49139321023872640 ) ) ;
#24614=CARTESIAN_POINT ( 'NONE',  ( -12.67931802180743972, -59.99999999999998579, 39.70502876154672123 ) ) ;
#24619=CARTESIAN_POINT ( 'NONE',  ( -85.77437932991819025, -61.06087370286046934, 194.1425874229156250 ) ) ;
#24623=CARTESIAN_POINT ( 'NONE',  ( -10.12172432390016752, -25.54964335568536171, 28.15750748029973494 ) ) ;
#24637=CARTESIAN_POINT ( 'NONE',  ( 109.2895958250431931, -30.00000000000001776, 180.5620058458624442 ) ) ;
#24654=CARTESIAN_POINT ( 'NONE',  ( -69.35185981456076831, -60.00000000005866241, 152.1736452874216639 ) ) ;
#24657=CARTESIAN_POINT ( 'NONE',  ( 91.95750203301783188, -59.99999999999998579, 17.41842218427850497 ) ) ;
#24658=CARTESIAN_POINT ( 'NONE',  ( -111.5324017304388207, -60.00000000000003553, 193.8614060841614730 ) ) ;
#24659=CARTESIAN_POINT ( 'NONE',  ( 16.83005395452520148, -42.95383171955222679, 31.29264600947682240 ) ) ;
#24662=CARTESIAN_POINT ( 'NONE',  ( -43.03151631067254357, -39.52863235512158724, 41.51148371547483151 ) ) ;
#24674=CARTESIAN_POINT ( 'NONE',  ( 73.52265062858249678, -30.00000000000002132, -18.84734495193007220 ) ) ;
#24680=CARTESIAN_POINT ( 'NONE',  ( 100.5424548002938252, -30.00000000000000355, 159.7537580344667560 ) ) ;
#24689=MECHANICAL_DESIGN_GEOMETRIC_PRESENTATION_REPRESENTATION('',(#507),#65996);
#24696=CARTESIAN_POINT ( 'NONE',  ( 79.87769542981580173, -38.77283384872364991, 192.7642698354605670 ) ) ;
#24709=( NAMED_UNIT ( * ) SI_UNIT ( $, .STERADIAN. ) SOLID_ANGLE_UNIT ( ) );
#24716=CARTESIAN_POINT ( 'NONE',  ( 35.86397158582656886, -35.96817661624932327, 45.02762458631914200 ) ) ;
#24720=CARTESIAN_POINT ( 'NONE',  ( 85.72981139660485894, -35.64577651797950608, 184.4330373048933325 ) ) ;
#24723=CARTESIAN_POINT ( 'NONE',  ( 92.77703971953890516, -57.65704708596170747, -17.75489428273840886 ) ) ;
#24727=CARTESIAN_POINT ( 'NONE',  ( -80.75022429576897309, -30.00000000000000711, 11.83902672125366706 ) ) ;
#24729=CARTESIAN_POINT ( 'NONE',  ( -66.13744702806401676, -38.00000000000000711, 88.79736889982228831 ) ) ;
#24741=CARTESIAN_POINT ( 'NONE',  ( -101.6436112212510920, -37.99999999999999289, 186.0797090425507463 ) ) ;
#24751=CARTESIAN_POINT ( 'NONE',  ( -72.23576987978789532, -60.22812697544318183, -25.48613692067792158 ) ) ;
#24758=CARTESIAN_POINT ( 'NONE',  ( -33.67313932047541414, -59.99999999999998579, -40.47465270752430655 ) ) ;
#24763=CARTESIAN_POINT ( 'NONE',  ( 94.65454574660577691, -37.70782373346656868, 193.0112514210578638 ) ) ;
#24767=VERTEX_POINT ( 'NONE', #83706 ) ;
#24774=DIRECTION ( 'NONE',  ( 0.000000000000000000, 0.000000000000000000, 1.000000000000000000 ) ) ;
#24777=CARTESIAN_POINT ( 'NONE',  ( -35.27718283856832926, -57.69548877625971528, 49.41932622563938793 ) ) ;
#24783=CARTESIAN_POINT ( 'NONE',  ( 16.60915088697842990, -29.99999999999996092, -39.45628980158949162 ) ) ;
#24784=CARTESIAN_POINT ( 'NONE',  ( -16.35964837410663364, -14.21045842199427156, 34.56001531359335388 ) ) ;
#24785=CARTESIAN_POINT ( 'NONE',  ( -52.77677503717105623, -42.97426568945239467, 57.04412880052729662 ) ) ;
#24787=CARTESIAN_POINT ( 'NONE',  ( -101.6154700970077727, -60.23106683408825290, 194.6025349640015918 ) ) ;
#24793=CARTESIAN_POINT ( 'NONE',  ( 80.29706273292998731, -38.80371450807032119, 193.5207487054061914 ) ) ;
#24798=CARTESIAN_POINT ( 'NONE',  ( 84.65172267273683815, -29.99999999999999645, 167.0116762541745743 ) ) ;
#24807=CARTESIAN_POINT ( 'NONE',  ( 49.06076903878732764, -36.05571625808668301, 48.12677125807188361 ) ) ;
#24811=ORIENTED_EDGE ( 'NONE', *, *, #80100, .T. ) ;
#24812=CARTESIAN_POINT ( 'NONE',  ( -95.62104924639133685, -38.35497854891799108, 61.91038439842863284 ) ) ;
#24815=CARTESIAN_POINT ( 'NONE',  ( 92.11484161200772292, -38.35416711761700270, 35.82767016875815358 ) ) ;
#24817=CARTESIAN_POINT ( 'NONE',  ( 100.8218116053281648, -60.15118524285145440, 120.1860783564071227 ) ) ;
#24818=PLANE ( 'NONE',  #70003 ) ;
#24822=CARTESIAN_POINT ( 'NONE',  ( 74.08415778415269415, -60.00000000000000711, 173.0691721023521552 ) ) ;
#24825=ORIENTED_EDGE ( 'NONE', *, *, #99117, .F. ) ;
#24826=CARTESIAN_POINT ( 'NONE',  ( 60.41798261738436082, -53.38619297810041076, 80.04375523387287217 ) ) ;
#24831=CARTESIAN_POINT ( 'NONE',  ( -90.03305742383118115, -38.39730272076602091, -15.91574180056000465 ) ) ;
#24841=CARTESIAN_POINT ( 'NONE',  ( 83.51337046645885209, -46.52999516907490118, 182.5729501482931028 ) ) ;
#24858=CARTESIAN_POINT ( 'NONE',  ( -12.33365875486739682, -21.28429137792180370, 35.60179995485724902 ) ) ;
#24870=CARTESIAN_POINT ( 'NONE',  ( 69.08232371648826131, -34.58963181410090471, -22.16762132562647380 ) ) ;
#24880=CARTESIAN_POINT ( 'NONE',  ( -98.09114130456060821, -59.99999999999997158, 69.48956915287729430 ) ) ;
#24889=CARTESIAN_POINT ( 'NONE',  ( -85.73826008725094994, -21.86594983941249026, 169.1353952584642286 ) ) ;
#24905=CARTESIAN_POINT ( 'NONE',  ( 109.5811936024938120, -29.99999999999993250, 174.3369879458943217 ) ) ;
#24906=CARTESIAN_POINT ( 'NONE',  ( -109.4365443207511390, -30.00000000000002487, 178.4890703142130519 ) ) ;
#24907=CARTESIAN_POINT ( 'NONE',  ( -63.94872130549475742, -18.62866409033716408, 72.61401410517680688 ) ) ;
#24910=CARTESIAN_POINT ( 'NONE',  ( 95.06272658828241617, -60.00000000001715250, -9.381997069871475858 ) ) ;
#24912=CARTESIAN_POINT ( 'NONE',  ( 5.139007685894275923, -53.39669312118982702, 32.77870000778612791 ) ) ;
#24913=CARTESIAN_POINT ( 'NONE',  ( -100.5925313966044996, -45.26526810289921343, 134.9952907213105675 ) ) ;
#24921=CARTESIAN_POINT ( 'NONE',  ( -93.31313149041179145, -59.99999999999997158, 202.5005118382522937 ) ) ;
#24933=CARTESIAN_POINT ( 'NONE',  ( 86.13399275866341043, -59.99999999999998579, -13.61178955313006256 ) ) ;
#24936=CARTESIAN_POINT ( 'NONE',  ( -31.80442458140531770, -25.61247349453389788, 31.25873360126171718 ) ) ;
#24939=CARTESIAN_POINT ( 'NONE',  ( 41.19214003654240486, -39.52178756432360274, 39.71506556026432122 ) ) ;
#24943=CARTESIAN_POINT ( 'NONE',  ( -77.17977131689143278, -38.47780548771186204, 185.1846801741239688 ) ) ;
#24954=CARTESIAN_POINT ( 'NONE',  ( 110.8877446216819465, -60.00000000000000711, 151.0616722329774007 ) ) ;
#24960=CARTESIAN_POINT ( 'NONE',  ( -90.75085121845700087, -29.99999999999981171, 190.3706885672457645 ) ) ;
#24975=CARTESIAN_POINT ( 'NONE',  ( 79.57055945170098710, -53.37446314916106616, 159.7373772712091125 ) ) ;
#24977=CARTESIAN_POINT ( 'NONE',  ( 89.99999999999997158, -52.00000000000000000, 194.0238439516549818 ) ) ;
#24983=CARTESIAN_POINT ( 'NONE',  ( 73.50474219086036953, -59.99999999999997158, -24.84696050693406022 ) ) ;
#24990=CARTESIAN_POINT ( 'NONE',  ( 86.67822773504592249, -50.11939951311777719, 191.5819010267896374 ) ) ;
#24993=CARTESIAN_POINT ( 'NONE',  ( 21.57322603007769146, -26.73334242327893406, 37.22254679213403961 ) ) ;
#25011=CARTESIAN_POINT ( 'NONE',  ( 114.2261582128081585, -57.67133197082363694, 172.3102140180382378 ) ) ;
#25017=CARTESIAN_POINT ( 'NONE',  ( -77.65926509950536172, -59.99999999999999289, 192.1015713222786871 ) ) ;
#25022=CARTESIAN_POINT ( 'NONE',  ( -84.07736508537209374, -57.42622439993449746, 190.7929976290621710 ) ) ;
#25029=CARTESIAN_POINT ( 'NONE',  ( -85.73889581639751611, -52.73376626706190251, -5.626253082883039269 ) ) ;
#25036=CARTESIAN_POINT ( 'NONE',  ( 2.083846472846741813E-15, -1.734723475976807094E-15, 17.01589776168603407 ) ) ;
#25038=CARTESIAN_POINT ( 'NONE',  ( -48.21571607899795708, -30.00000000000001066, -35.59733477200444440 ) ) ;
#25039=CARTESIAN_POINT ( 'NONE',  ( -76.07387704635563352, -39.49473305854762373, 125.2008553257723804 ) ) ;
#25042=CARTESIAN_POINT ( 'NONE',  ( 64.81979848413079992, -29.99999999999996803, 107.4021778588664375 ) ) ;
#25044=CARTESIAN_POINT ( 'NONE',  ( 111.6759504537514829, -57.67120741609547707, 140.8126062134855658 ) ) ;
#25064=CARTESIAN_POINT ( 'NONE',  ( 31.02192573903809958, -39.48738554629173336, 33.50131639203233647 ) ) ;
#25066=VERTEX_POINT ( 'NONE', #9314 ) ;
#25075=DIRECTION ( 'NONE',  ( -1.850371707710400463E-15, 0.000000000000000000, 1.000000000000000000 ) ) ;
#25078=CARTESIAN_POINT ( 'NONE',  ( 92.74028942188910207, -60.00000000000002132, -6.481442454470473180 ) ) ;
#25092=CARTESIAN_POINT ( 'NONE',  ( 83.13711729878457390, -37.83719930664555164, -3.006607161073368228 ) ) ;
#25101=CARTESIAN_POINT ( 'NONE',  ( -84.83517221518071949, -38.71298880862309488, 198.3806444392209301 ) ) ;
#25104=CARTESIAN_POINT ( 'NONE',  ( -74.60970371152679093, -59.99999999999997158, 134.6542277587269894 ) ) ;
#25106=CARTESIAN_POINT ( 'NONE',  ( 67.34244021800664370, -56.85823850909442712, 103.2051531002039155 ) ) ;
#25110=CARTESIAN_POINT ( 'NONE',  ( -94.50453298674098335, -57.65443526055588563, -11.14264577307068294 ) ) ;
#25117=CARTESIAN_POINT ( 'NONE',  ( -83.88445482477082749, -59.99999999999995737, 191.6821729358339610 ) ) ;
#25135=CARTESIAN_POINT ( 'NONE',  ( -97.30680262177158113, -30.00000000000000711, 190.9787031741742567 ) ) ;
#25138=CARTESIAN_POINT ( 'NONE',  ( 63.27202089354346271, -57.67868661202842162, 119.5670882431399491 ) ) ;
#25143=CARTESIAN_POINT ( 'NONE',  ( 5.404552530375831054, -21.70842134127357426, -38.54708377808628939 ) ) ;
#25146=CARTESIAN_POINT ( 'NONE',  ( -38.60657232694759955, -59.99999999999999289, 50.24250451447390020 ) ) ;
#25150=CARTESIAN_POINT ( 'NONE',  ( -86.94464142740093848, -28.02521910232672653, 186.6926187431337212 ) ) ;
#25154=CARTESIAN_POINT ( 'NONE',  ( -7.105946766212089649, -35.99435547297646565, 29.87904593495951389 ) ) ;
#25169=CARTESIAN_POINT ( 'NONE',  ( 104.4271199315001013, -14.21045842199428932, 141.4133776126798523 ) ) ;
#25171=VERTEX_POINT ( 'NONE', #73520 ) ;
#25178=ORIENTED_EDGE ( 'NONE', *, *, #22687, .F. ) ;
#25189=CARTESIAN_POINT ( 'NONE',  ( -62.16730077632442431, -59.99999999996094857, 116.6023417739558425 ) ) ;
#25192=CARTESIAN_POINT ( 'NONE',  ( 95.52617796645279213, -59.99999999999993605, 202.5679377223947029 ) ) ;
#25194=CARTESIAN_POINT ( 'NONE',  ( -80.26890325034752038, -59.99999999999982947, 200.1011331233653721 ) ) ;
#25195=CARTESIAN_POINT ( 'NONE',  ( 19.33195322576188246, -53.39568836721204548, 33.25297745405755734 ) ) ;
#25200=CARTESIAN_POINT ( 'NONE',  ( -41.65521368984826722, -25.70102211639285628, 36.84734771239409667 ) ) ;
#25204=VECTOR ( 'NONE', #51304, 1000.000000000000000 ) ;
#25214=CARTESIAN_POINT ( 'NONE',  ( 81.46863496367946311, -30.00000000000010303, -3.011595879706462142 ) ) ;
#25218=CARTESIAN_POINT ( 'NONE',  ( 83.32745884141306192, -29.99999999999999289, 45.50778505098266891 ) ) ;
#25234=CARTESIAN_POINT ( 'NONE',  ( 78.81833263833561887, -38.67058111308598001, 190.4994190873096898 ) ) ;
#25247=SURFACE_STYLE_USAGE ( .BOTH. , #23118 ) ;
#25251=CARTESIAN_POINT ( 'NONE',  ( 0.000000000000000000, -8.000000000000000000, 0.000000000000000000 ) ) ;
#25255=CARTESIAN_POINT ( 'NONE',  ( 85.41732212696841486, -42.91985075306342878, 186.8826177936102795 ) ) ;
#25259=CARTESIAN_POINT ( 'NONE',  ( 93.08838507352525937, -57.65565157171307931, -16.99954835227337213 ) ) ;
#25263=CARTESIAN_POINT ( 'NONE',  ( -80.77633485222713716, -30.00000000000000355, 10.02478776459890675 ) ) ;
#25280=CARTESIAN_POINT ( 'NONE',  ( -97.35930377584806195, -38.00000000000000711, 192.7749382691207813 ) ) ;
#25288=CARTESIAN_POINT ( 'NONE',  ( -63.25291691186279763, -29.60348520313671727, -23.77066348807526452 ) ) ;
#25297=CARTESIAN_POINT ( 'NONE',  ( -33.39843217748020265, -60.00000000000000711, -40.50829833586755768 ) ) ;
#25299=CARTESIAN_POINT ( 'NONE',  ( 69.78853948234211657, -37.99999999999999289, -22.51057024784411098 ) ) ;
#25301=CARTESIAN_POINT ( 'NONE',  ( 100.0744711941220828, -45.27419155593420896, 192.5344585825728245 ) ) ;
#25302=CARTESIAN_POINT ( 'NONE',  ( 28.67833651802481754, -29.89477528201764400, 30.92734934190152885 ) ) ;
#25307=ORIENTED_EDGE ( 'NONE', *, *, #45660, .F. ) ;
#25315=CARTESIAN_POINT ( 'NONE',  ( -53.52971897118871425, -57.67555505732850207, 87.03092276603273092 ) ) ;
#25320=CARTESIAN_POINT ( 'NONE',  ( -56.79577812574758156, -14.21045842199439591, -31.02744264688941556 ) ) ;
#25321=CARTESIAN_POINT ( 'NONE',  ( -24.48725402052853184, -14.21045842199434084, 35.52122251240935924 ) ) ;
#25323=CARTESIAN_POINT ( 'NONE',  ( -50.87568867342284307, -36.04944650272992845, 51.03950296323957048 ) ) ;
#25326=CARTESIAN_POINT ( 'NONE',  ( -101.3987088893176889, -60.24204779500730922, 194.8051035594306484 ) ) ;
#25332=CARTESIAN_POINT ( 'NONE',  ( 84.96569581588377673, -38.70379807337806710, 198.4584125899654339 ) ) ;
#25337=CARTESIAN_POINT ( 'NONE',  ( 84.01303099038503319, -29.99999999999999645, 161.1241072836490957 ) ) ;
#25344=ORIENTED_EDGE ( 'NONE', *, *, #2696, .T. ) ;
#25345=CARTESIAN_POINT ( 'NONE',  ( 53.50953716884873756, -22.16763606720927626, 50.70318854014821142 ) ) ;
#25350=CARTESIAN_POINT ( 'NONE',  ( -90.64414275519084185, -38.34462549197198200, 9.748502710164705931 ) ) ;
#25353=CARTESIAN_POINT ( 'NONE',  ( 94.42873002227078416, -38.35542734117505859, 53.97500541993706946 ) ) ;
#25355=CARTESIAN_POINT ( 'NONE',  ( 86.28022341275342910, -60.14323854837493855, 19.05399894497716318 ) ) ;
#25363=CARTESIAN_POINT ( 'NONE',  ( 74.88199338232608682, -60.00000000000000000, 180.3605328980037257 ) ) ;
#25369=CARTESIAN_POINT ( 'NONE',  ( 59.49458740857772909, -56.85954389590153824, 79.18117010720280291 ) ) ;
#25374=CARTESIAN_POINT ( 'NONE',  ( -76.12537862032631608, -38.35598417008159799, -28.58435412235101225 ) ) ;
#25384=CARTESIAN_POINT ( 'NONE',  ( 83.83469278148253068, -39.45372097025308022, 177.1342842458970495 ) ) ;
#25396=CARTESIAN_POINT ( 'NONE',  ( -27.77263666253245589, -28.74976145023062557, -38.27455432825868087 ) ) ;
#25399=CARTESIAN_POINT ( 'NONE',  ( 43.69737412773557850, -60.00000000000000000, 58.12383163124780339 ) ) ;
#25401=CARTESIAN_POINT ( 'NONE',  ( 26.89082867329939575, -20.19349464338415601, 31.72560904215549726 ) ) ;
#25403=CARTESIAN_POINT ( 'NONE',  ( -14.80423426860585678, -22.57669348423709721, 35.90345806391073324 ) ) ;
#25415=CARTESIAN_POINT ( 'NONE',  ( 22.10411833928789349, -34.58974732179735412, -31.65657241835295110 ) ) ;
#25426=CARTESIAN_POINT ( 'NONE',  ( -101.0097921112870836, -59.99999999999998579, 86.95724220043298658 ) ) ;
#25431=CARTESIAN_POINT ( 'NONE',  ( -89.99999999999997158, -38.00000000001091394, 188.5238439516623146 ) ) ;
#25438=CARTESIAN_POINT ( 'NONE',  ( -85.53824590343933210, -21.95572400392595469, 166.5517161537221682 ) ) ;
#25450=CARTESIAN_POINT ( 'NONE',  ( -36.37294538904226471, -57.67119865010090507, -42.13310955380372747 ) ) ;
#25451=CARTESIAN_POINT ( 'NONE',  ( 2.499999999999997780, -18.83380486180452706, 27.02532357426314036 ) ) ;
#25456=CARTESIAN_POINT ( 'NONE',  ( 106.4854190881680154, -14.21045842199434439, 182.1792229330528983 ) ) ;
#25457=CARTESIAN_POINT ( 'NONE',  ( -107.9655701563618067, -29.99999999999997158, 188.7577781645654795 ) ) ;
#25459=CARTESIAN_POINT ( 'NONE',  ( -58.04404759258189728, -56.86246254669144662, 75.20273737405429415 ) ) ;
#25463=CARTESIAN_POINT ( 'NONE',  ( 114.2077509676909557, -59.99999999999023004, 161.8867648380875153 ) ) ;
#25464=VERTEX_POINT ( 'NONE', #75529 ) ;
#25465=CARTESIAN_POINT ( 'NONE',  ( 4.074124056600999744, -46.43456338532926964, 31.62120482653921982 ) ) ;
#25466=CARTESIAN_POINT ( 'NONE',  ( -98.65422846995242878, -37.82071831846016607, 130.4055507037949155 ) ) ;
#25470=CARTESIAN_POINT ( 'NONE',  ( -64.44341639718678039, -59.99999999999998579, 116.0066787658274308 ) ) ;
#25474=CARTESIAN_POINT ( 'NONE',  ( 17.01594651245413203, -0.000000000000000000, -1.113195845613775381 ) ) ;
#25481=CARTESIAN_POINT ( 'NONE',  ( -31.71388525929565816, -18.67330243560268954, 29.92571452508646601 ) ) ;
#25483=CARTESIAN_POINT ( 'NONE',  ( 46.35797818206071241, -56.80661940937356746, 50.30410939637813073 ) ) ;
#25488=CARTESIAN_POINT ( 'NONE',  ( -78.45413196039172021, -38.62859691719035027, 189.5535229323872386 ) ) ;
#25493=CARTESIAN_POINT ( 'NONE',  ( 8.351634798667673110, -59.99999999999998579, 33.88072871824981291 ) ) ;
#25500=CARTESIAN_POINT ( 'NONE',  ( 108.9153292171738059, -59.99999999999999289, 135.3754215099987732 ) ) ;
#25506=CARTESIAN_POINT ( 'NONE',  ( -94.47165723176175334, -29.99999999999987210, 191.3277322571271100 ) ) ;
#25523=CARTESIAN_POINT ( 'NONE',  ( 82.82954590797592687, -39.48843416255702010, 168.2668317262558446 ) ) ;
#25540=CARTESIAN_POINT ( 'NONE',  ( 85.88830989802964666, -61.04876075054228579, 194.2276438132367673 ) ) ;
#25560=CARTESIAN_POINT ( 'NONE',  ( 107.6015356060339911, -57.67123274086495854, 114.0084083295923563 ) ) ;
#25567=CARTESIAN_POINT ( 'NONE',  ( -86.42863255622134488, -60.00000000000000000, 200.7652140804842134 ) ) ;
#25569=DIRECTION ( 'NONE',  ( 0.000000000000000000, 0.000000000000000000, -1.000000000000000000 ) ) ;
#25573=CARTESIAN_POINT ( 'NONE',  ( -84.96946970298199631, -35.81198127296185163, 180.8558154136740939 ) ) ;
#25580=CARTESIAN_POINT ( 'NONE',  ( -85.58543702643984830, -52.75005472265036843, -10.05567657277402382 ) ) ;
#25590=CARTESIAN_POINT ( 'NONE',  ( 49.63358250961842799, -60.00000000000001421, -40.41868810089377462 ) ) ;
#25591=CARTESIAN_POINT ( 'NONE',  ( -79.25090170193163885, -32.55892561338175284, 134.6608944345848329 ) ) ;
#25593=CARTESIAN_POINT ( 'NONE',  ( 77.10949051821226874, -30.00000000000007461, 176.8385238405566326 ) ) ;
#25595=CARTESIAN_POINT ( 'NONE',  ( 94.44279491447446162, -57.67056076577856771, -0.6735058548411319013 ) ) ;
#25615=CARTESIAN_POINT ( 'NONE',  ( 32.05687126736489745, -60.31738256606855231, 37.68480598271252546 ) ) ;
#25630=CARTESIAN_POINT ( 'NONE',  ( 84.25014938015986843, -60.00000000000002132, -25.16421652135344544 ) ) ;
#25643=CARTESIAN_POINT ( 'NONE',  ( 83.22070310856115327, -37.82803493101771153, -4.681492691623674318 ) ) ;
#25657=CARTESIAN_POINT ( 'NONE',  ( 76.83599883816330589, -18.66163333761462439, 113.2182193956237057 ) ) ;
#25664=CARTESIAN_POINT ( 'NONE',  ( -80.00483118099813851, -57.67118036264142944, -30.22182926596574148 ) ) ;
#25669=CARTESIAN_POINT ( 'NONE',  ( 103.8601077188106672, -45.28281436907764146, 165.7359996305474112 ) ) ;
#25685=CARTESIAN_POINT ( 'NONE',  ( -92.68948487369793554, -30.00000000000000355, 191.0483739415028310 ) ) ;
#25691=CARTESIAN_POINT ( 'NONE',  ( 63.69210850852088868, -57.67891201327802975, 121.2445212169528475 ) ) ;
#25692=CARTESIAN_POINT ( 'NONE',  ( 80.00000000000000000, -52.00000000000000000, -21.09707704303352926 ) ) ;
#25698=CARTESIAN_POINT ( 'NONE',  ( 20.69727557552225505, -26.09496662598620276, -38.47203802730707878 ) ) ;
#25701=CARTESIAN_POINT ( 'NONE',  ( -36.13861969606174540, -60.00000000000002132, 47.48874267815981653 ) ) ;
#25705=CARTESIAN_POINT ( 'NONE',  ( -86.86729174969509870, -24.34025208997100620, 185.9213970984535820 ) ) ;
#25708=CARTESIAN_POINT ( 'NONE',  ( -6.226963257687841313, -60.36578172299497425, 33.94043655557382522 ) ) ;
#25724=CARTESIAN_POINT ( 'NONE',  ( 114.5768552918926986, -59.99999999999997868, 170.6725192690976485 ) ) ;
#25725=CARTESIAN_POINT ( 'NONE',  ( -82.36662456894917739, -36.02719610116624693, 158.6189278519784409 ) ) ;
#25747=CARTESIAN_POINT ( 'NONE',  ( 103.9293398954433201, -60.00000000000001421, 200.0405719490170213 ) ) ;
#25748=CARTESIAN_POINT ( 'NONE',  ( -75.43392636619238090, -30.00000000000003553, 160.3050061908775206 ) ) ;
#25749=CARTESIAN_POINT ( 'NONE',  ( 15.30468211099681319, -18.58757702105601339, 27.14322304785206441 ) ) ;
#25750=CARTESIAN_POINT ( 'NONE',  ( 82.23886140992384242, -37.99999999999997868, -13.37499424629273292 ) ) ;
#25751=CARTESIAN_POINT ( 'NONE',  ( -39.23155690887019631, -18.76732848933246700, 33.52670975879949822 ) ) ;
#25754=CARTESIAN_POINT ( 'NONE',  ( -6.539732759932832096, -4.285714285714296246, 24.41571844174603001 ) ) ;
#25757=MECHANICAL_DESIGN_GEOMETRIC_PRESENTATION_REPRESENTATION('',(#1579),#49792);
#25762=CARTESIAN_POINT ( 'NONE',  ( -46.09313609967871628, -38.31867567570748179, 60.02686483055563826 ) ) ;
#25765=CARTESIAN_POINT ( 'NONE',  ( 80.80396565660879560, -29.99999999999999289, -12.40573726492647744 ) ) ;
#25767=UNCERTAINTY_MEASURE_WITH_UNIT (LENGTH_MEASURE( 1.000000000000000082E-05 ), #98562, 'distance_accuracy_value', 'NONE');
#25770=CARTESIAN_POINT ( 'NONE',  ( 82.65538836485218610, -30.00000000000001421, 40.06710242176322367 ) ) ;
#25790=CARTESIAN_POINT ( 'NONE',  ( 75.07689429088097199, -38.33936338830137203, 170.2545699534454400 ) ) ;
#25814=CARTESIAN_POINT ( 'NONE',  ( 85.02982003489246665, -46.56546437767619295, 187.6125479875748283 ) ) ;
#25818=CARTESIAN_POINT ( 'NONE',  ( 85.03610603180797511, -57.67078060003379392, -26.99171295196738285 ) ) ;
#25822=CARTESIAN_POINT ( 'NONE',  ( -80.80785939509713955, -29.99999999999999645, 8.456651002378157145 ) ) ;
#25831=FACE_OUTER_BOUND ( 'NONE', #46177, .T. ) ;
#25842=CARTESIAN_POINT ( 'NONE',  ( -68.05023500849456752, -60.22824080543345104, -27.16814012153120927 ) ) ;
#25852=CARTESIAN_POINT ( 'NONE',  ( -66.22057664901657859, -60.00000000000000000, -33.82046026944324524 ) ) ;
#25856=CARTESIAN_POINT ( 'NONE',  ( 99.66320498351910828, -45.27082587009371650, 192.8921995371364631 ) ) ;
#25871=CARTESIAN_POINT ( 'NONE',  ( -38.25590479036647906, -57.69571505705692260, 53.01769594715635492 ) ) ;
#25877=CARTESIAN_POINT ( 'NONE',  ( -76.02716361407355805, -14.21045842199433018, -24.18402117868763312 ) ) ;
#25879=CARTESIAN_POINT ( 'NONE',  ( -49.80859045805021168, -29.12840406359013556, 47.03773477635749600 ) ) ;
#25890=CARTESIAN_POINT ( 'NONE',  ( 95.01222379904187676, -38.48886571037592574, 201.2294609025024670 ) ) ;
#25895=CARTESIAN_POINT ( 'NONE',  ( 89.33714348230114410, -30.00000000000000355, 189.1719500048700979 ) ) ;
#25900=EDGE_LOOP ( 'NONE', ( #67924, #82926, #68273, #37402 ) ) ;
#25902=CARTESIAN_POINT ( 'NONE',  ( 52.74007187349189962, -56.84010683540350328, 62.26390772461709844 ) ) ;
#25907=CARTESIAN_POINT ( 'NONE',  ( -90.66182577935869347, -38.34383351580818555, 8.928474947456855659 ) ) ;
#25910=CARTESIAN_POINT ( 'NONE',  ( 106.9867655987633839, -38.36460303376994574, 194.8700637373434859 ) ) ;
#25912=CARTESIAN_POINT ( 'NONE',  ( 90.29360518614763009, -60.15064404123215525, 56.70420316085070311 ) ) ;
#25917=CARTESIAN_POINT ( 'NONE',  ( 76.40233392909763666, -60.00000000000000711, 188.5393174096115843 ) ) ;
#25922=CARTESIAN_POINT ( 'NONE',  ( 60.71647413655895065, -36.01272182586236426, 72.46326076516903925 ) ) ;
#25932=CARTESIAN_POINT ( 'NONE',  ( -50.84467228568406227, -29.86834801596571154, 47.91031235514574149 ) ) ;
#25936=CARTESIAN_POINT ( 'NONE',  ( 83.34764017132830816, -46.52104804447979092, 181.7006552018694094 ) ) ;
#25945=CARTESIAN_POINT ( 'NONE',  ( -14.11945738078545709, -23.79845479901861083, -38.53423393589877577 ) ) ;
#25949=CARTESIAN_POINT ( 'NONE',  ( 50.87433458991679203, -60.00000000000000000, 74.01426795907130440 ) ) ;
#25952=CARTESIAN_POINT ( 'NONE',  ( -8.680069730182619736, -19.69849086824678608, 35.28136294433512887 ) ) ;
#25954=EDGE_CURVE ( 'NONE', #16368, #16675, #14003, .T. ) ;
#25962=CARTESIAN_POINT ( 'NONE',  ( -30.81781730487858084, -29.88286713088693958, -38.15156302677360145 ) ) ;
#25967=CARTESIAN_POINT ( 'NONE',  ( 12.60774193670373755, -34.58958930473867355, -32.31369604931713013 ) ) ;
#25975=CARTESIAN_POINT ( 'NONE',  ( -97.59218698678627391, -60.00000000000000711, 66.40864316552561775 ) ) ;
#25983=CARTESIAN_POINT ( 'NONE',  ( -85.06961102174302880, -25.47176778552115195, 167.4802045267348092 ) ) ;
#25994=FILL_AREA_STYLE ('',( #2176 ) ) ;
#26000=CARTESIAN_POINT ( 'NONE',  ( 98.01458704197314376, -60.00000000000006395, 53.57113828723962001 ) ) ;
#26001=CARTESIAN_POINT ( 'NONE',  ( -114.0746799351349665, -60.00000000000000000, 159.9915189542998633 ) ) ;
#26002=CARTESIAN_POINT ( 'NONE',  ( -61.12306988036042554, -29.06572220310668442, 70.22504446809620049 ) ) ;
#26005=CARTESIAN_POINT ( 'NONE',  ( 11.22784523005032042, -60.00000000003856826, -44.73795172861001390 ) ) ;
#26007=CARTESIAN_POINT ( 'NONE',  ( 4.963618185166544627, -18.58607934322651190, 26.97811559224125944 ) ) ;
#26008=CARTESIAN_POINT ( 'NONE',  ( -102.1368288975054384, -37.82054834480975103, 158.6782685907600410 ) ) ;
#26015=CARTESIAN_POINT ( 'NONE',  ( -68.31247128209859909, -59.99999999999997868, 132.4338893582065566 ) ) ;
#26022=CARTESIAN_POINT ( 'NONE',  ( 2.220638482690572957, -0.000000000000000000, 16.90642566760537591 ) ) ;
#26028=CARTESIAN_POINT ( 'NONE',  ( 86.66370790318070760, -60.00000000000002842, -0.08902744567370259043 ) ) ;
#26029=CARTESIAN_POINT ( 'NONE',  ( -31.27606781357311760, -32.54866752878100300, 32.34274477842507167 ) ) ;
#26031=CARTESIAN_POINT ( 'NONE',  ( 43.92012437998704399, -39.52645832331002396, 42.42191456129378224 ) ) ;
#26037=CARTESIAN_POINT ( 'NONE',  ( -78.40755826573125375, -38.62304279762774684, 189.4248641629946803 ) ) ;
#26041=CARTESIAN_POINT ( 'NONE',  ( 33.22078196456656940, -59.99999999999998579, 38.21881171944680489 ) ) ;
#26048=CARTESIAN_POINT ( 'NONE',  ( 106.3730004120468635, -60.00000000000000000, 118.7265111617542743 ) ) ;
#26054=CARTESIAN_POINT ( 'NONE',  ( -98.04222423866050917, -30.00000000000004619, 190.4877416275006397 ) ) ;
#26067=CARTESIAN_POINT ( 'NONE',  ( 82.60475124576561257, -36.02199222531928058, 160.6691209302269669 ) ) ;
#26080=CARTESIAN_POINT ( 'NONE',  ( 87.15839251447800962, -53.73024192609155847, 193.0048309959825872 ) ) ;
#26101=CARTESIAN_POINT ( 'NONE',  ( 111.7135535141261187, -57.67100837368887767, 192.2061815498727526 ) ) ;
#26108=CARTESIAN_POINT ( 'NONE',  ( -76.72214885510777549, -60.00000000000001421, 189.6187291083674040 ) ) ;
#26113=CARTESIAN_POINT ( 'NONE',  ( -84.13144306823785712, -50.17137820680997606, 187.2782904672004634 ) ) ;
#26120=CARTESIAN_POINT ( 'NONE',  ( -87.03651754438010357, -60.20087593430655204, -7.185994694023575491 ) ) ;
#26129=CARTESIAN_POINT ( 'NONE',  ( 49.67137106584178241, -60.00000000000004263, 77.31490210218785819 ) ) ;
#26131=CARTESIAN_POINT ( 'NONE',  ( -67.59740049799954420, -60.00000000000004263, -35.88590100950167994 ) ) ;
#26132=CARTESIAN_POINT ( 'NONE',  ( -69.72170801787599714, -56.86188030024484874, 111.2991454040818695 ) ) ;
#26134=CARTESIAN_POINT ( 'NONE',  ( 77.72372478688149045, -60.00000000000015632, 197.5639835283903381 ) ) ;
#26135=CARTESIAN_POINT ( 'NONE',  ( 110.0995903249117589, -57.67119305192648682, 129.6557836479702246 ) ) ;
#26145=CARTESIAN_POINT ( 'NONE',  ( 22.67073868809948323, -4.285714285714295357, -11.17734400176825815 ) ) ;
#26154=CARTESIAN_POINT ( 'NONE',  ( 33.42066694708537256, -49.89779052485263122, 36.47770383487736012 ) ) ;
#26166=CARTESIAN_POINT ( 'NONE',  ( 92.55080760481821756, -59.99999999999997868, -10.81156607774824607 ) ) ;
#26181=CARTESIAN_POINT ( 'NONE',  ( 85.00363781311220635, -60.19116803139766603, -16.05942585105188058 ) ) ;
#26194=CARTESIAN_POINT ( 'NONE',  ( 71.71719020375222442, -29.06458548707639622, 101.3022678019235343 ) ) ;
#26198=CARTESIAN_POINT ( 'NONE',  ( -113.3548229410037465, -57.67117998536030399, 185.4730977758015911 ) ) ;
#26203=CARTESIAN_POINT ( 'NONE',  ( 102.7192639426134662, -37.84832478631605568, 177.0129730847589258 ) ) ;
#26220=CARTESIAN_POINT ( 'NONE',  ( -87.76554063038440745, -29.99999999999999645, 186.1736720200109971 ) ) ;
#26224=CARTESIAN_POINT ( 'NONE',  ( 71.71515109230394103, -57.67815897944166181, 169.1494729058397581 ) ) ;
#26227=CARTESIAN_POINT ( 'NONE',  ( 46.76197682092300312, -34.80551308950123968, -36.64518833549670518 ) ) ;
#26230=CARTESIAN_POINT ( 'NONE',  ( -33.53236062124648953, -60.00000000000000711, 45.21991715472178441 ) ) ;
#26233=CARTESIAN_POINT ( 'NONE',  ( -84.25800729984597126, -61.06716200360207125, 192.6535660339058040 ) ) ;
#26237=CARTESIAN_POINT ( 'NONE',  ( -8.282562182867314604, -53.40262204257363976, 32.78376551419927409 ) ) ;
#26251=FILL_AREA_STYLE_COLOUR ( '', #68516 ) ;
#26253=CARTESIAN_POINT ( 'NONE',  ( 109.4365241820779460, -29.99999999999997158, 178.4894931318444264 ) ) ;
#26254=CARTESIAN_POINT ( 'NONE',  ( -81.37979335976676509, -32.56286079620799967, 146.9012815414374415 ) ) ;
#26267=DIRECTION ( 'NONE',  ( 0.000000000000000000, 0.000000000000000000, 1.000000000000000000 ) ) ;
#26273=CARTESIAN_POINT ( 'NONE',  ( 112.0843263065733453, -59.99999999999998579, 166.2625348020058311 ) ) ;
#26275=CARTESIAN_POINT ( 'NONE',  ( -91.59718878904411099, -29.99999999999996803, 199.7679234505767738 ) ) ;
#26276=CARTESIAN_POINT ( 'NONE',  ( 25.24426991834572576, -49.91242165019021826, 33.57203989678414757 ) ) ;
#26280=CARTESIAN_POINT ( 'NONE',  ( -42.37195134635844340, -46.43793568724321119, 42.48696600435207671 ) ) ;
#26293=CARTESIAN_POINT ( 'NONE',  ( -47.61850715973584869, -38.32480789866512083, 63.16917730038245082 ) ) ;
#26295=CARTESIAN_POINT ( 'NONE',  ( 76.05159319993262557, -29.99999999993064037, 166.0196408361732381 ) ) ;
#26299=CARTESIAN_POINT ( 'NONE',  ( 80.81161881489168763, -30.00000000000000355, 8.164499038400824915 ) ) ;
#26305=ORIENTED_EDGE ( 'NONE', *, *, #9063, .F. ) ;
#26318=CARTESIAN_POINT ( 'NONE',  ( 71.34172708741220958, -38.32795092330694331, 142.0021045512803539 ) ) ;
#26336=AXIS2_PLACEMENT_3D ( 'NONE', #45375, #78256, #100405 ) ;
#26341=CARTESIAN_POINT ( 'NONE',  ( 86.12920843257361980, -28.31461485542720879, 182.7851167764210913 ) ) ;
#26345=CARTESIAN_POINT ( 'NONE',  ( 91.71403545851765671, -57.66150985471095680, -19.81184364356237637 ) ) ;
#26350=CARTESIAN_POINT ( 'NONE',  ( -97.22778952995973611, -30.00000000000000355, 132.2006373510576509 ) ) ;
#26363=CARTESIAN_POINT ( 'NONE',  ( 12.43157790776222704, -16.68004855619690119, -34.60072825135022612 ) ) ;
#26364=CARTESIAN_POINT ( 'NONE',  ( -25.70623218437548374, -29.04638407032486924, 30.12123181827645979 ) ) ;
#26368=CARTESIAN_POINT ( 'NONE',  ( -60.87314043734040325, -29.35674091808159147, -24.66679337420148244 ) ) ;
#26379=CARTESIAN_POINT ( 'NONE',  ( -81.74325047390442478, -60.00000000000000711, -26.86817790202253065 ) ) ;
#26382=CARTESIAN_POINT ( 'NONE',  ( 100.5709118951127152, -52.75385023292707842, 193.7746871183922792 ) ) ;
#26397=CARTESIAN_POINT ( 'NONE',  ( -73.03813016181682372, -57.65004463643786892, 181.4998991682408302 ) ) ;
#26402=CARTESIAN_POINT ( 'NONE',  ( -90.15663891815873399, -29.99999999999996447, 30.33658191415442573 ) ) ;
#26404=CARTESIAN_POINT ( 'NONE',  ( -51.23517434054790698, -42.97794402298157479, 54.10049340080158231 ) ) ;
#26412=CARTESIAN_POINT ( 'NONE',  ( 76.52617406485063611, -38.41457857166980006, 181.9190546311624814 ) ) ;
#26417=CARTESIAN_POINT ( 'NONE',  ( 93.74430992741119439, -30.00000000000001066, 191.2477460422086892 ) ) ;
#26425=CARTESIAN_POINT ( 'NONE',  ( 51.21436344590323131, -22.18943343881225871, 46.87532722179359013 ) ) ;
#26430=CARTESIAN_POINT ( 'NONE',  ( -87.92473828310710360, -38.36961232417662160, -19.67705683220690105 ) ) ;
#26433=CARTESIAN_POINT ( 'NONE',  ( 110.2521165255493969, -38.35601262087017460, 184.3169374418023665 ) ) ;
#26435=CARTESIAN_POINT ( 'NONE',  ( 90.66858095960151331, -52.71678089307656023, 67.18335908107627574 ) ) ;
#26439=DIRECTION ( 'NONE',  ( 0.000000000000000000, 0.000000000000000000, -1.000000000000000000 ) ) ;
#26442=CARTESIAN_POINT ( 'NONE',  ( 60.76565412937480204, -22.11966791577999913, 66.05797801596867203 ) ) ;
#26451=CARTESIAN_POINT ( 'NONE',  ( -43.60180431260018707, -27.81332246800423036, 38.60050550264399050 ) ) ;
#26456=CARTESIAN_POINT ( 'NONE',  ( 84.74406210802428063, -35.85138381605241875, 179.5088509989636805 ) ) ;
#26464=CARTESIAN_POINT ( 'NONE',  ( -23.31310657521862240, -27.07274008780074936, -38.41778960086845984 ) ) ;
#26467=CARTESIAN_POINT ( 'NONE',  ( 47.51011502736643166, -59.99999999999999289, 65.91768184338560843 ) ) ;
#26470=CARTESIAN_POINT ( 'NONE',  ( 19.24333786597378193, -16.79214355476590015, 31.49079971865065986 ) ) ;
#26471=CARTESIAN_POINT ( 'NONE',  ( -39.40204838967584777, -37.44295604146311263, 49.05621705154725021 ) ) ;
#26485=CARTESIAN_POINT ( 'NONE',  ( 25.58909025738432774, -47.40908607597074820, -33.48593688835422455 ) ) ;
#26496=ADVANCED_FACE ( 'NONE', ( #66661 ), #41056, .T. ) ;
#26499=CARTESIAN_POINT ( 'NONE',  ( -105.4858918486370385, -60.00000000000000711, 113.2841891985042366 ) ) ;
#26506=CARTESIAN_POINT ( 'NONE',  ( -82.51321957585668088, -46.47945556470999406, 176.1511104553312350 ) ) ;
#26514=ORIENTED_EDGE ( 'NONE', *, *, #1587, .T. ) ;
#26523=CARTESIAN_POINT ( 'NONE',  ( 86.74683449613482367, -14.21045842199431242, 20.02856677177719646 ) ) ;
#26524=CARTESIAN_POINT ( 'NONE',  ( -101.1248876217780719, -29.99999999999996803, 198.7487848662925387 ) ) ;
#26525=CARTESIAN_POINT ( 'NONE',  ( -57.05921168992595227, -46.44064480593611677, 67.94562297101694526 ) ) ;
#26528=CARTESIAN_POINT ( 'NONE',  ( 39.12642507647372270, -59.99999999997108802, -42.14755403963000191 ) ) ;
#26530=CARTESIAN_POINT ( 'NONE',  ( 6.121031749467999106, -42.95355877999562466, 31.03873517957318739 ) ) ;
#26531=CARTESIAN_POINT ( 'NONE',  ( -105.2354536759059869, -52.71042663006205231, 175.0634013992600160 ) ) ;
#26532=FILL_AREA_STYLE ('',( #68559 ) ) ;
#26537=CARTESIAN_POINT ( 'NONE',  ( -59.79892528436459997, -60.00000000000002842, 99.75862326221643173 ) ) ;
#26549=CARTESIAN_POINT ( 'NONE',  ( -30.91330409187026262, -49.90965397396043102, 35.32750583910272013 ) ) ;
#26552=CARTESIAN_POINT ( 'NONE',  ( 42.51421430475448915, -22.24489720477335908, 36.74246443512219429 ) ) ;
#26557=CARTESIAN_POINT ( 'NONE',  ( -77.93035626155285911, -38.56579719186625255, 187.9925447483828123 ) ) ;
#26560=CARTESIAN_POINT ( 'NONE',  ( 39.55075348946911618, -60.00000000000002132, 42.69056844256114402 ) ) ;
#26568=CARTESIAN_POINT ( 'NONE',  ( 109.1439378327955723, -60.00000000000000711, 136.9933165474393491 ) ) ;
#26572=CARTESIAN_POINT ( 'NONE',  ( -45.71963733757689852, -30.00000000000002842, 56.30991746768105344 ) ) ;
#26578=CARTESIAN_POINT ( 'NONE',  ( -81.51781765243289612, -30.00000000000003908, -9.022581224190874494 ) ) ;
#26590=CARTESIAN_POINT ( 'NONE',  ( 80.25229455199325912, -53.38333115846620558, 165.9811891832442825 ) ) ;
#26603=CARTESIAN_POINT ( 'NONE',  ( 87.32513032536655828, -39.06015956257186161, 189.6234660408021000 ) ) ;
#26612=VERTEX_POINT ( 'NONE', #35255 ) ;
#26626=CARTESIAN_POINT ( 'NONE',  ( -92.00444157296256265, -60.00000000000001421, 202.3484270727608134 ) ) ;
#26630=CARTESIAN_POINT ( 'NONE',  ( -83.21273294567592416, -57.32323371491776243, 189.0402996391318879 ) ) ;
#26638=CARTESIAN_POINT ( 'NONE',  ( -85.12517225352462447, -52.70214463376765934, 4.505281520561013942 ) ) ;
#26643=CARTESIAN_POINT ( 'NONE',  ( 59.93162491489189847, -30.00000000000002842, 91.51739161628221098 ) ) ;
#26644=CARTESIAN_POINT ( 'NONE',  ( -75.59778980771257295, -60.00000000000000711, -32.85486631586996253 ) ) ;
#26645=CARTESIAN_POINT ( 'NONE',  ( -72.11871523709537257, -53.38464545085997059, 118.2014658002872665 ) ) ;
#26647=CARTESIAN_POINT ( 'NONE',  ( 72.31505286502601848, -14.21045842199433373, 125.5027806063605595 ) ) ;
#26649=CARTESIAN_POINT ( 'NONE',  ( 18.22952343553518162, -60.00000000000000000, 42.38361649051553570 ) ) ;
#26670=CARTESIAN_POINT ( 'NONE',  ( 32.66538190274433617, -53.37042454289756677, 36.73435524595355162 ) ) ;
#26689=CARTESIAN_POINT ( 'NONE',  ( 81.12704008932206534, -60.00000000000000711, -27.25892719060451341 ) ) ;
#26699=ORIENTED_EDGE ( 'NONE', *, *, #82452, .F. ) ;
#26705=CARTESIAN_POINT ( 'NONE',  ( 82.73735319387645859, -37.80016373507481120, -11.88716716749071800 ) ) ;
#26716=CARTESIAN_POINT ( 'NONE',  ( 76.26163437509697474, -25.60425469984666691, 115.8635891106310680 ) ) ;
#26722=AXIS2_PLACEMENT_3D ( 'NONE', #62520, #45793, #52817 ) ;
#26723=CARTESIAN_POINT ( 'NONE',  ( -95.04855897266367037, -57.67186573470212352, 33.03592761066350647 ) ) ;
#26724=ADVANCED_FACE ( 'NONE', ( #63095 ), #14509, .F. ) ;
#26728=CARTESIAN_POINT ( 'NONE',  ( 105.0593050701437079, -52.71712251083815204, 179.5715820065424850 ) ) ;
#26733=CYLINDRICAL_SURFACE ( 'NONE', #10636, 7.499999999992679633 ) ;
#26744=CARTESIAN_POINT ( 'NONE',  ( -86.31276977314503540, -29.99999999999999645, 180.5061992413450298 ) ) ;
#26747=CARTESIAN_POINT ( 'NONE',  ( 71.49549276749331739, -57.67960528813748056, 166.9847680060588857 ) ) ;
#26751=CARTESIAN_POINT ( 'NONE',  ( 34.56201351537013267, -31.18758961746727465, -37.90746136657972443 ) ) ;
#26755=CARTESIAN_POINT ( 'NONE',  ( -40.00918711724499843, -59.99999999999998579, 52.09662703808838558 ) ) ;
#26760=CARTESIAN_POINT ( 'NONE',  ( -85.44437512040904892, -61.07326030157955188, 193.8761068449719573 ) ) ;
#26763=CARTESIAN_POINT ( 'NONE',  ( -5.033944729454126410, -32.51260769746507151, 29.29872852438901631 ) ) ;
#26777=SURFACE_SIDE_STYLE ('',( #100614 ) ) ;
#26779=CARTESIAN_POINT ( 'NONE',  ( 108.0662294780436383, -29.99999999999999645, 149.4678247624379708 ) ) ;
#26780=CARTESIAN_POINT ( 'NONE',  ( -82.46821273478651904, -25.62404814617509530, 146.0476204998806793 ) ) ;
#26784=CARTESIAN_POINT ( 'NONE',  ( 39.13906141225513835, -57.69405802890273094, 54.30799458850530215 ) ) ;
#26799=CARTESIAN_POINT ( 'NONE',  ( 109.9245725901865853, -60.00000000000000000, 191.4319832265045704 ) ) ;
#26800=CARTESIAN_POINT ( 'NONE',  ( -85.76719879059909601, -14.21045842199445630, 195.9089143291284074 ) ) ;
#26801=CARTESIAN_POINT ( 'NONE',  ( 18.86798682596964838, -32.51239220599620694, 29.71099402561047498 ) ) ;
#26803=CARTESIAN_POINT ( 'NONE',  ( -40.63004339231220996, -25.69609495895222651, 36.04365259879974559 ) ) ;
#26808=CARTESIAN_POINT ( 'NONE',  ( -1.650803255657556479, -4.285714285714296246, 25.22241582816892702 ) ) ;
#26809=DIRECTION ( 'NONE',  ( 1.871721906610600077E-16, 0.000000000000000000, -1.000000000000000000 ) ) ;
#26818=CARTESIAN_POINT ( 'NONE',  ( 57.01429441072921378, -30.00000000006595968, 82.99024849085006394 ) ) ;
#26822=CARTESIAN_POINT ( 'NONE',  ( 83.30424347533678997, -30.00000000000000711, 45.32559808931431178 ) ) ;
#26842=CARTESIAN_POINT ( 'NONE',  ( 74.51953474006475631, -38.33012379840763373, 164.9748051664451793 ) ) ;
#26866=CARTESIAN_POINT ( 'NONE',  ( 84.31560656641553919, -57.43926515212457673, 191.1735246261523855 ) ) ;
#26874=CARTESIAN_POINT ( 'NONE',  ( -93.92629083922592770, -29.99999999999999645, 111.5267929669124101 ) ) ;
#26881=CARTESIAN_POINT ( 'NONE',  ( -28.73416115563823681, -29.92329866866804977, 30.94992384361019688 ) ) ;
#26885=CARTESIAN_POINT ( 'NONE',  ( 40.90099630364926497, -25.13177883036392757, -30.10567145231062369 ) ) ;
#26887=CARTESIAN_POINT ( 'NONE',  ( -23.35130136342643326, -29.03948800314977063, 29.66951933061897151 ) ) ;
#26891=CARTESIAN_POINT ( 'NONE',  ( -19.99473970835801140, -32.51530817802121476, 29.81274010585231338 ) ) ;
#26892=CARTESIAN_POINT ( 'NONE',  ( -71.80342408229677176, -30.00000000000000000, -19.71767938363507966 ) ) ;
#26906=CARTESIAN_POINT ( 'NONE',  ( 100.8650305359696517, -52.74513607102953472, 193.5094557858945450 ) ) ;
#26908=CARTESIAN_POINT ( 'NONE',  ( 5.121377489766137714, -19.23622649283650077, 27.08678039004259830 ) ) ;
#26923=CARTESIAN_POINT ( 'NONE',  ( -92.22404989346505033, -59.99999999999755573, -19.73939852595544764 ) ) ;
#26928=CARTESIAN_POINT ( 'NONE',  ( -77.20948002450832348, -29.99999999999995737, -26.53460153345886496 ) ) ;
#26930=CARTESIAN_POINT ( 'NONE',  ( -51.29768049186471046, -18.72484688875610459, 45.83708237476789549 ) ) ;
#26939=CARTESIAN_POINT ( 'NONE',  ( 81.18586761171566479, -38.84088417715932451, 194.8800132995233412 ) ) ;
#26944=CARTESIAN_POINT ( 'NONE',  ( 87.05705487234845918, -30.00000000000000355, 183.9282422150870104 ) ) ;
#26949=CARTESIAN_POINT ( 'NONE',  ( 52.29916411013782351, -25.64426098774818286, 49.83386183445969664 ) ) ;
#26953=CARTESIAN_POINT ( 'NONE',  ( -85.51831432850400461, -38.36002604018491979, -22.36822977887920771 ) ) ;
#26955=CARTESIAN_POINT ( 'NONE',  ( 107.7883601516577698, -38.35935003634334350, 193.3568233556534324 ) ) ;
#26957=CARTESIAN_POINT ( 'NONE',  ( 85.97056482012806100, -45.28272053107379236, 43.44903282293562796 ) ) ;
#26977=CARTESIAN_POINT ( 'NONE',  ( 48.13867764410746020, -29.30200429754887992, 43.72835771138513650 ) ) ;
#26986=CARTESIAN_POINT ( 'NONE',  ( 82.60104337135625485, -57.21257082304840935, 187.3407815826748788 ) ) ;
#26988=CARTESIAN_POINT ( 'NONE',  ( -87.14767027655014431, -37.99999999998310329, 189.0874028505847662 ) ) ;
#26990=CARTESIAN_POINT ( 'NONE',  ( -97.17100149276052434, -37.82057918150324838, 120.9264675858186848 ) ) ;
#26996=CARTESIAN_POINT ( 'NONE',  ( -26.07542528179775587, -28.11225759749947883, -38.33793174107837132 ) ) ;
#26997=CARTESIAN_POINT ( 'NONE',  ( 47.40123518113406220, -60.00000000000001421, 65.67392086698521325 ) ) ;
#26998=CARTESIAN_POINT ( 'NONE',  ( 21.50348335299959857, -26.68737644460689751, 37.20438602441733167 ) ) ;
#27001=CARTESIAN_POINT ( 'NONE',  ( -30.23468791487915297, -32.60645102688423691, 40.71049962837252423 ) ) ;
#27011=UNCERTAINTY_MEASURE_WITH_UNIT (LENGTH_MEASURE( 1.000000000000000082E-05 ), #16054, 'distance_accuracy_value', 'NONE');
#27016=CARTESIAN_POINT ( 'NONE',  ( 40.42072553015707115, -21.77015276485149187, -27.31244395070953956 ) ) ;
#27027=CARTESIAN_POINT ( 'NONE',  ( -92.14138347090150205, -59.99999999999999289, 3.768088791749690802 ) ) ;
#27033=CARTESIAN_POINT ( 'NONE',  ( -82.99743053524834124, -42.97928617255369943, 175.1928188408835751 ) ) ;
#27045=DIRECTION ( 'NONE',  ( 0.000000000000000000, 0.000000000000000000, 1.000000000000000000 ) ) ;
#27050=SURFACE_STYLE_FILL_AREA ( #100357 ) ;
#27053=CARTESIAN_POINT ( 'NONE',  ( 104.6755681235317326, -59.99999999999997158, 94.38101796850538960 ) ) ;
#27055=CARTESIAN_POINT ( 'NONE',  ( -83.90898588706018302, -30.00000000000009592, 196.6629347554013520 ) ) ;
#27056=CARTESIAN_POINT ( 'NONE',  ( -60.51311341646994890, -39.49057771885277646, 73.58478999695718414 ) ) ;
#27061=CARTESIAN_POINT ( 'NONE',  ( -105.1848697628562661, -52.71040872453725967, 177.3350388984402173 ) ) ;
#27062=SURFACE_STYLE_FILL_AREA ( #26532 ) ;
#27068=CARTESIAN_POINT ( 'NONE',  ( -78.46824605727127278, -60.00000000000002132, 193.7232304666046900 ) ) ;
#27080=CARTESIAN_POINT ( 'NONE',  ( -29.45685281427571311, -32.53887230772507877, 31.71332361860625682 ) ) ;
#27082=CARTESIAN_POINT ( 'NONE',  ( 43.41165897559503861, -18.78955090332965483, 36.60811760637851364 ) ) ;
#27085=CARTESIAN_POINT ( 'NONE',  ( -85.94205773066651943, -38.64533204748195061, 199.0279254153126374 ) ) ;
#27087=CARTESIAN_POINT ( 'NONE',  ( 84.15948067047270342, -38.35796929636687480, -23.57197301947594781 ) ) ;
#27096=CARTESIAN_POINT ( 'NONE',  ( 112.1460658327969497, -60.00000000000000711, 168.0038417747363440 ) ) ;
#27102=CARTESIAN_POINT ( 'NONE',  ( -85.26005096827651641, -30.00000000000000711, 59.54443886065791247 ) ) ;
#27115=CARTESIAN_POINT ( 'NONE',  ( 83.26238809008557951, -32.54124788460179474, 161.2361585245887170 ) ) ;
#27121=DIRECTION ( 'NONE',  ( 0.000000000000000000, 0.000000000000000000, 1.000000000000000000 ) ) ;
#27158=CARTESIAN_POINT ( 'NONE',  ( -82.77836920865000536, -60.00000000000002132, 198.6656318658897078 ) ) ;
#27162=CARTESIAN_POINT ( 'NONE',  ( -83.76789176632343015, -50.14492659078340608, 186.2261076651866460 ) ) ;
#27168=CARTESIAN_POINT ( 'NONE',  ( -84.99953569365740691, -52.70058240222559931, 7.104635508431614177 ) ) ;
#27175=CARTESIAN_POINT ( 'NONE',  ( 76.24208907273079205, -14.21045842199436571, 145.5826741442930086 ) ) ;
#27176=CARTESIAN_POINT ( 'NONE',  ( -91.01451176774321539, -60.00000000000003553, -21.65129702257078392 ) ) ;
#27177=CARTESIAN_POINT ( 'NONE',  ( -73.71532386833389694, -32.54439743916745442, 110.4898480562198415 ) ) ;
#27179=CARTESIAN_POINT ( 'NONE',  ( 71.62958147348905413, -29.99999999999999645, 135.6714503744467493 ) ) ;
#27181=CARTESIAN_POINT ( 'NONE',  ( 29.86891141250063697, -59.99999999999378275, 45.62306988735215185 ) ) ;
#27192=CARTESIAN_POINT ( 'NONE',  ( -28.59280391696366053, -60.00000000000000711, 44.96178721945644696 ) ) ;
#27195=DIRECTION ( 'NONE',  ( 0.000000000000000000, -1.000000000000000000, 0.000000000000000000 ) ) ;
#27207=CARTESIAN_POINT ( 'NONE',  ( 32.06800782219411872, -36.02032094391599770, 33.29063352059957026 ) ) ;
#27208=CARTESIAN_POINT ( 'NONE',  ( -2.910977163136218682, -8.673617379884035472E-16, 22.23822744035697241 ) ) ;
#27224=CARTESIAN_POINT ( 'NONE',  ( 92.49443939637855294, -60.00000000000000711, -11.29237403364020409 ) ) ;
#27232=CARTESIAN_POINT ( 'NONE',  ( -103.3985022873205111, -30.00000000000063238, 197.1317429111190904 ) ) ;
#27239=CARTESIAN_POINT ( 'NONE',  ( 83.25497522988638366, -37.81035774849722486, -7.772203072343009111 ) ) ;
#27249=SURFACE_SIDE_STYLE ('',( #68746 ) ) ;
#27253=CARTESIAN_POINT ( 'NONE',  ( 72.38549888608767446, -49.90611211077317222, 116.9150284757207174 ) ) ;
#27261=CARTESIAN_POINT ( 'NONE',  ( -100.9355741078537676, -57.67123050614609525, 74.71304529006944506 ) ) ;
#27265=CARTESIAN_POINT ( 'NONE',  ( 104.0818543291210858, -52.71697307696259571, 186.3349087221899367 ) ) ;
#27277=CARTESIAN_POINT ( 'NONE',  ( 97.47675437802963927, -60.00000000000000000, 196.6138812136176739 ) ) ;
#27284=CARTESIAN_POINT ( 'NONE',  ( -90.30437240975373925, -30.00000000000000000, 190.0991083897584417 ) ) ;
#27288=CARTESIAN_POINT ( 'NONE',  ( 85.39600985831239655, -57.56620033426278127, 202.4570461212290695 ) ) ;
#27292=CARTESIAN_POINT ( 'NONE',  ( 72.70106880652396342, -38.32395693884171095, -30.14377858825407230 ) ) ;
#27294=CARTESIAN_POINT ( 'NONE',  ( -32.45631383308813867, -60.00000000000000711, 44.46787372447708009 ) ) ;
#27299=CARTESIAN_POINT ( 'NONE',  ( -86.71180320006325815, -28.07811669808429755, 185.8229765233257922 ) ) ;
#27302=CARTESIAN_POINT ( 'NONE',  ( -2.040435125742793954, -53.40256923005231471, 32.78745887589579411 ) ) ;
#27319=CARTESIAN_POINT ( 'NONE',  ( 102.0720237449618679, -14.21045842199434439, 125.2221798637976349 ) ) ;
#27320=CARTESIAN_POINT ( 'NONE',  ( -78.40731456737989902, -56.84664622636871201, 154.9013258714905987 ) ) ;
#27324=CARTESIAN_POINT ( 'NONE',  ( 11.32753640269611850, -57.67122862458237620, 41.63783267011080369 ) ) ;
#27345=CARTESIAN_POINT ( 'NONE',  ( -77.10962715007582347, -30.00000000000002842, 176.8398472105207020 ) ) ;
#27346=CARTESIAN_POINT ( 'NONE',  ( 21.89153770144105948, -18.59655829513583214, 27.69837461209327145 ) ) ;
#27349=CARTESIAN_POINT ( 'NONE',  ( -34.28121086557304409, -32.56895737632404320, 33.60869056487658213 ) ) ;
#27360=CARTESIAN_POINT ( 'NONE',  ( 95.05407124332270996, -30.00000000000007461, 191.3402996794985427 ) ) ;
#27364=CARTESIAN_POINT ( 'NONE',  ( 82.29247763371455449, -30.00000000000000000, 36.77940851373791276 ) ) ;
#27380=VERTEX_POINT ( 'NONE', #45614 ) ;
#27382=CARTESIAN_POINT ( 'NONE',  ( 77.51835495759516448, -38.51555964928014930, 186.5383354859341409 ) ) ;
#27406=CARTESIAN_POINT ( 'NONE',  ( 86.54311645508100526, -24.44606347078198283, 184.2149994208030535 ) ) ;
#27413=CARTESIAN_POINT ( 'NONE',  ( -81.90009874109570376, -30.00000000000000000, 32.92589465123853643 ) ) ;
#27420=CARTESIAN_POINT ( 'NONE',  ( -41.16595618007350055, -35.63923124053023628, 38.70344113984020140 ) ) ;
#27424=CARTESIAN_POINT ( 'NONE',  ( 64.15845098142789027, -29.68239269618735321, -23.41016185180100351 ) ) ;
#27427=CARTESIAN_POINT ( 'NONE',  ( -24.22841651280220887, -56.87824106493767573, 34.54384085670383797 ) ) ;
#27431=CARTESIAN_POINT ( 'NONE',  ( -20.16347608971366867, -39.47721886123265733, 30.99930452457605767 ) ) ;
#27443=CARTESIAN_POINT ( 'NONE',  ( 98.96726417907956375, -37.80060191501620181, 191.9129845458357408 ) ) ;
#27458=CARTESIAN_POINT ( 'NONE',  ( -92.79822040692241103, -60.00000000000483169, -18.69254732702162514 ) ) ;
#27463=CARTESIAN_POINT ( 'NONE',  ( -84.17958645690445962, -14.21045842199424314, -18.06708323581670328 ) ) ;
#27467=CARTESIAN_POINT ( 'NONE',  ( -49.42298433514555001, -49.90609790616115049, 53.22976286859889683 ) ) ;
#27478=CARTESIAN_POINT ( 'NONE',  ( 68.48188116143754200, -38.33341530762260163, 126.0809973183768307 ) ) ;
#27483=CARTESIAN_POINT ( 'NONE',  ( 85.96547421025208280, -30.00000000000000355, 178.3596608991437904 ) ) ;
#27491=CARTESIAN_POINT ( 'NONE',  ( 51.33239210164947508, -39.50898634762949513, 53.05425396579943254 ) ) ;
#27495=CARTESIAN_POINT ( 'NONE',  ( -90.54712574570254446, -38.40309215953966770, -14.40705472300955847 ) ) ;
#27499=CARTESIAN_POINT ( 'NONE',  ( 110.3742243073734812, -38.35605051120794684, 158.9574927243544948 ) ) ;
#27501=CARTESIAN_POINT ( 'NONE',  ( 83.05433171731620234, -37.85161955793942923, 27.04821047549421564 ) ) ;
#27516=CARTESIAN_POINT ( 'NONE',  ( -3.672464763049774796E-06, -18.02989419364509516, 35.00496915990722613 ) ) ;
#27519=CARTESIAN_POINT ( 'NONE',  ( -48.22718221699823005, -29.29832994236101484, 43.93128805990089347 ) ) ;
#27524=CARTESIAN_POINT ( 'NONE',  ( 82.99625799389046676, -60.91576764804962352, 190.5939014586151643 ) ) ;
#27526=CARTESIAN_POINT ( 'NONE',  ( -86.73809324249754127, -41.71369293968039926, 189.2643421761773936 ) ) ;
#27528=CARTESIAN_POINT ( 'NONE',  ( -94.35836587452192248, -45.26550033706196530, 96.73288487592235185 ) ) ;
#27532=CARTESIAN_POINT ( 'NONE',  ( -27.71163250425533420, -28.72695625282879561, -38.27699728131180024 ) ) ;
#27536=CARTESIAN_POINT ( 'NONE',  ( 41.13664993942406767, -60.00000000000000000, 53.77317075040697603 ) ) ;
#27537=CARTESIAN_POINT ( 'NONE',  ( 34.91252575250545931, -35.46210594863769217, 44.14912163742516071 ) ) ;
#27539=CARTESIAN_POINT ( 'NONE',  ( 17.70630566656853233, -16.17175919650291505, 31.52307540510448192 ) ) ;
#27540=CARTESIAN_POINT ( 'NONE',  ( -2.499999999999996447, -10.61161683768976083, -19.67321569086711364 ) ) ;
#27549=CARTESIAN_POINT ( 'NONE',  ( -1.758251042101240058, -60.00000000000000000, 39.63689313157515670 ) ) ;
#27557=CARTESIAN_POINT ( 'NONE',  ( -6.444268991759913412, -60.22817020191458681, -36.83317943627129409 ) ) ;
#27567=CARTESIAN_POINT ( 'NONE',  ( -92.04245549561946405, -60.00000000000000000, 19.36274040525862006 ) ) ;
#27574=CARTESIAN_POINT ( 'NONE',  ( -85.62098330289637715, -21.92300381590476732, 167.5840582116480562 ) ) ;
#27577=EDGE_LOOP ( 'NONE', ( #25178, #18606, #39054, #97855, #73856, #105474, #61317 ) ) ;
#27584=CARTESIAN_POINT ( 'NONE',  ( -88.38279035983548226, -57.66943555457145720, -24.13713039724196818 ) ) ;
#27590=CARTESIAN_POINT ( 'NONE',  ( 91.01367250360885919, -30.00000000000005684, 38.60059757395459457 ) ) ;
#27592=CARTESIAN_POINT ( 'NONE',  ( -81.10703223160209063, -14.21045842199456288, 192.6080781080067652 ) ) ;
#27593=CARTESIAN_POINT ( 'NONE',  ( -58.97854848860931298, -53.38957946420630662, 76.08090858395418365 ) ) ;
#27597=CARTESIAN_POINT ( 'NONE',  ( -106.4199118972464788, -60.15533903948110606, 177.4979064205827513 ) ) ;
#27598=( LENGTH_UNIT ( ) NAMED_UNIT ( * ) SI_UNIT ( .MILLI., .METRE. ) );
#27613=CARTESIAN_POINT ( 'NONE',  ( -31.71665931334666055, -53.38053263592674114, 36.28720432217011904 ) ) ;
#27617=CARTESIAN_POINT ( 'NONE',  ( 45.30861358563132057, -22.24403561376615812, 39.34052521140961289 ) ) ;
#27620=CARTESIAN_POINT ( 'NONE',  ( -97.97456883874956191, -38.48009392417085195, 200.9861677195517586 ) ) ;
#27624=CARTESIAN_POINT ( 'NONE',  ( 57.46228475329571239, -59.99999999999999289, 75.03564804614198636 ) ) ;
#27631=CARTESIAN_POINT ( 'NONE',  ( 111.6052588162456516, -60.00000000000000711, 183.6789224556778208 ) ) ;
#27638=CARTESIAN_POINT ( 'NONE',  ( -84.13737281345436259, -29.99999999999997158, 51.97699099161796710 ) ) ;
#27641=CARTESIAN_POINT ( 'NONE',  ( -86.79134504753260160, -38.60262278463063979, 199.4600156365133614 ) ) ;
#27655=CARTESIAN_POINT ( 'NONE',  ( 80.23453759376155858, -56.87460238040762306, 171.5698434726804464 ) ) ;
#27672=CARTESIAN_POINT ( 'NONE',  ( 86.62318117064180001, -60.99931462043210928, 194.7255943711274426 ) ) ;
#27693=CARTESIAN_POINT ( 'NONE',  ( -108.4242937615723719, -59.99999999999997868, 194.8630744897274667 ) ) ;
#27699=CARTESIAN_POINT ( 'NONE',  ( -85.41269523509512851, -32.17776350644170691, 180.5340902165694388 ) ) ;
#27707=CARTESIAN_POINT ( 'NONE',  ( -86.78765346559656280, -60.15861341457728884, -1.594545952693453339 ) ) ;
#27715=CARTESIAN_POINT ( 'NONE',  ( 76.30472591814422856, -30.00000000000007105, 168.5677193688796649 ) ) ;
#27718=CARTESIAN_POINT ( 'NONE',  ( -94.38155987036965655, -60.00000000000007105, 5.296623108471039565 ) ) ;
#27719=CARTESIAN_POINT ( 'NONE',  ( -67.30718710595479592, -39.48677006991138683, 93.17581753966889835 ) ) ;
#27721=CARTESIAN_POINT ( 'NONE',  ( 86.31905819422470927, -30.00000000000006750, 198.0863690661441296 ) ) ;
#27724=CARTESIAN_POINT ( 'NONE',  ( 29.01678287318512162, -59.99999999999877787, 45.16868993385956799 ) ) ;
#27736=CARTESIAN_POINT ( 'NONE',  ( -43.97714636534035293, -60.00000000001949019, 63.83295154858610232 ) ) ;
#27740=PLANE ( 'NONE',  #22560 ) ;
#27741=CARTESIAN_POINT ( 'NONE',  ( 1.650803255657553592, -4.285714285714296246, -25.22241582816892347 ) ) ;
#27748=CARTESIAN_POINT ( 'NONE',  ( 32.80054068545892676, -49.89943310828323320, 36.16858534763461819 ) ) ;
#27750=CARTESIAN_POINT ( 'NONE',  ( -15.50035291838204721, -4.285714285714287364, -20.16952962162827845 ) ) ;
#27762=CARTESIAN_POINT ( 'NONE',  ( 92.68349473529568172, -60.00000000000001421, -4.407455099632911377 ) ) ;
#27770=CARTESIAN_POINT ( 'NONE',  ( -92.17868644654814148, -29.99999999997585931, 199.7068435760925809 ) ) ;
#27777=CARTESIAN_POINT ( 'NONE',  ( 82.90625021741112732, -37.79796058491805866, -11.19383744670581571 ) ) ;
#27789=CARTESIAN_POINT ( 'NONE',  ( 76.14851803333424130, -56.84259894051964324, 140.2336560434112300 ) ) ;
#27796=CARTESIAN_POINT ( 'NONE',  ( -72.23603530542938245, -57.67079283669161782, 174.4370243615865661 ) ) ;
#27800=CARTESIAN_POINT ( 'NONE',  ( 105.2612990973347991, -52.71713998817723024, 170.4785330017703302 ) ) ;
#27806=CARTESIAN_POINT ( 'NONE',  ( -51.41203370401020578, -29.90211857482027114, 49.01905699928327209 ) ) ;
#27818=CARTESIAN_POINT ( 'NONE',  ( -86.35638819720911386, -30.00000000000000355, 180.7480702730107112 ) ) ;
#27821=CARTESIAN_POINT ( 'NONE',  ( 77.35975252159606441, -57.51975665479443478, 195.6400774986267095 ) ) ;
#27824=CARTESIAN_POINT ( 'NONE',  ( 46.78448780204201540, -34.81110335320523319, -36.64205672983788276 ) ) ;
#27829=CARTESIAN_POINT ( 'NONE',  ( -67.41425160460600807, -60.00000000000000711, 128.3978068706913973 ) ) ;
#27832=CARTESIAN_POINT ( 'NONE',  ( -86.49700811817415058, -46.49039750389685821, 190.2550539850416840 ) ) ;
#27835=CARTESIAN_POINT ( 'NONE',  ( -0.9911087893856018738, -25.54951634130952698, 28.14790268315395849 ) ) ;
#27852=CARTESIAN_POINT ( 'NONE',  ( 98.01458704197314376, -60.00000000000006395, 53.57113828723962001 ) ) ;
#27853=CARTESIAN_POINT ( 'NONE',  ( -79.54470974501947467, -46.43897030528811598, 150.5969177418128595 ) ) ;
#27857=CARTESIAN_POINT ( 'NONE',  ( 56.31243090753932989, -57.67579812645779924, 95.28593385378083269 ) ) ;
#27878=CARTESIAN_POINT ( 'NONE',  ( 92.74075353299672031, -60.00000000000002132, -7.839124456446247891 ) ) ;
#27880=CARTESIAN_POINT ( 'NONE',  ( -74.83603090277703984, -14.21045842199441012, 137.5224045200043577 ) ) ;
#27881=CARTESIAN_POINT ( 'NONE',  ( 20.49951756439809358, -53.39523566873690186, 33.37178152886023952 ) ) ;
#27883=CARTESIAN_POINT ( 'NONE',  ( -37.51903186869294871, -49.89542786323897161, 39.00874087383915167 ) ) ;
#27895=CARTESIAN_POINT ( 'NONE',  ( 92.20262301002225058, -29.99999999999975486, 190.9253757062230932 ) ) ;
#27898=CARTESIAN_POINT ( 'NONE',  ( 81.43962946624536414, -30.00000000000000355, -9.755616628628736464 ) ) ;
#27918=CARTESIAN_POINT ( 'NONE',  ( 74.24252310225787710, -38.32799067271444926, 162.4645122954939609 ) ) ;
#27935=CARTESIAN_POINT ( 'NONE',  ( 86.13876527465689037, -31.92079174777700956, 184.4232561367118137 ) ) ;
#27948=CARTESIAN_POINT ( 'NONE',  ( -86.44692486882411231, -29.99999999999999645, 67.03969724269380492 ) ) ;
#27952=CARTESIAN_POINT ( 'NONE',  ( 27.54371250915762914, -57.67848980524139080, 44.08961535850244218 ) ) ;
#27959=CARTESIAN_POINT ( 'NONE',  ( 39.31680540536973467, -24.66152148494653673, -30.43544166128774009 ) ) ;
#27960=CARTESIAN_POINT ( 'NONE',  ( -26.10329066505708440, -39.48148657949686680, 32.00599043094255336 ) ) ;
#27964=CARTESIAN_POINT ( 'NONE',  ( -15.89867790359543065, -53.40221630055644653, 32.98641644927912608 ) ) ;
#27976=CARTESIAN_POINT ( 'NONE',  ( 103.8597403422939180, -52.71705505079059861, 187.2922404200451183 ) ) ;
#27991=CARTESIAN_POINT ( 'NONE',  ( -94.19891500039717869, -60.00000000000972022, 13.58511310247205728 ) ) ;
#27996=CARTESIAN_POINT ( 'NONE',  ( -82.74168755217822024, -14.21045842199452203, -19.52755005266771349 ) ) ;
#27997=CARTESIAN_POINT ( 'NONE',  ( -47.91943188888855332, -53.36384233853009107, 51.78005963556529423 ) ) ;
#28007=CARTESIAN_POINT ( 'NONE',  ( 89.65068677404821074, -30.00000000002016165, 1.483486992794977866 ) ) ;
#28011=CARTESIAN_POINT ( 'NONE',  ( 90.40025181191772674, -29.99999999999999289, 190.1625712390529088 ) ) ;
#28017=CARTESIAN_POINT ( 'NONE',  ( 53.60758669369196383, -46.43620476034607236, 60.07046025485742291 ) ) ;
#28022=CARTESIAN_POINT ( 'NONE',  ( -91.40442697271741679, -38.39518381489244803, -9.089042331466192337 ) ) ;
#28026=CARTESIAN_POINT ( 'NONE',  ( 107.0273482872364923, -38.36426640808143418, 194.8006998555924270 ) ) ;
#28028=CARTESIAN_POINT ( 'NONE',  ( 83.68922614653902770, -45.28292466992145648, 14.69678876732623074 ) ) ;
#28050=CARTESIAN_POINT ( 'NONE',  ( 84.63799656866569876, -42.96597369867873795, 184.5360133087482382 ) ) ;
#28055=CARTESIAN_POINT ( 'NONE',  ( -86.61035443086036878, -45.26537160163291418, 48.35290667932413555 ) ) ;
#28059=CARTESIAN_POINT ( 'NONE',  ( -4.536700128592405790, -21.59318128966070205, -38.54827054018984711 ) ) ;
#28062=CARTESIAN_POINT ( 'NONE',  ( 31.63672064570198472, -60.00000000000000711, 43.92342796496127022 ) ) ;
#28063=CARTESIAN_POINT ( 'NONE',  ( 27.17445174878161396, -30.53057906289133072, 39.14485286163986899 ) ) ;
#28064=CARTESIAN_POINT ( 'NONE',  ( 45.13615050346792401, -28.34248706039453580, 40.22011616339790407 ) ) ;
#28081=CARTESIAN_POINT ( 'NONE',  ( -12.93448875801435172, -60.22812974450989998, -36.57614896566138896 ) ) ;
#28090=CARTESIAN_POINT ( 'NONE',  ( -91.98126730952112950, -59.99999999999999289, 6.611212861507896221 ) ) ;
#28098=CARTESIAN_POINT ( 'NONE',  ( -84.78135591110488178, -25.52853119631381418, 164.4154881268317752 ) ) ;
#28100=CARTESIAN_POINT ( 'NONE',  ( -5.483224646687553161, 0.000000000000000000, -16.14659623657211540 ) ) ;
#28108=CARTESIAN_POINT ( 'NONE',  ( -81.27538057784241232, -57.67119034933180188, -29.50368748078413361 ) ) ;
#28113=DIRECTION ( 'NONE',  ( 0.000000000000000000, 0.000000000000000000, 1.000000000000000000 ) ) ;
#28116=CARTESIAN_POINT ( 'NONE',  ( 104.6654747121523030, -30.00000000000000000, 124.7724495044359116 ) ) ;
#28117=CARTESIAN_POINT ( 'NONE',  ( -78.42690035548760363, -14.21045842199427156, 178.5095186877798028 ) ) ;
#28118=CARTESIAN_POINT ( 'NONE',  ( -55.57844914912075041, -32.55979464754466335, 58.72184905296868607 ) ) ;
#28122=CARTESIAN_POINT ( 'NONE',  ( -105.9261641753950727, -60.15502446452519081, 182.9949040398753368 ) ) ;
#28123=FACE_OUTER_BOUND ( 'NONE', #69453, .T. ) ;
#28128=CARTESIAN_POINT ( 'NONE',  ( -21.83613416818080921, -59.99999999999997868, 40.48705974210427172 ) ) ;
#28140=CARTESIAN_POINT ( 'NONE',  ( -30.44433818822805549, -53.38490099487817986, 35.76380123852791826 ) ) ;
#28142=CARTESIAN_POINT ( 'NONE',  ( 48.60192115950092528, -46.43965766730325129, 50.71851945537365935 ) ) ;
#28145=CARTESIAN_POINT ( 'NONE',  ( -101.6512650445923498, -38.44858725811527478, 199.8639472654733424 ) ) ;
#28146=ADVANCED_FACE ( 'NONE', ( #64709 ), #79820, .T. ) ;
#28157=CARTESIAN_POINT ( 'NONE',  ( 112.1206467272125451, -60.00000000000000711, 177.5187025037823219 ) ) ;
#28164=CARTESIAN_POINT ( 'NONE',  ( -100.9645298483791578, -29.99999999999999289, 165.4281941735794987 ) ) ;
#28166=CARTESIAN_POINT ( 'NONE',  ( -90.66027514559715428, -38.50790017717925195, 200.7323953230764459 ) ) ;
#28177=CARTESIAN_POINT ( 'NONE',  ( 82.60770557527793301, -42.97231573429220219, 171.7383286845875148 ) ) ;
#28191=ADVANCED_FACE ( 'NONE', ( #97065 ), #97579, .F. ) ;
#28220=CARTESIAN_POINT ( 'NONE',  ( -111.9121283550977637, -60.00000000000000000, 180.8211707975872287 ) ) ;
#28223=CARTESIAN_POINT ( 'NONE',  ( -84.56571597818337693, -39.40317381275280439, 181.6710895502921232 ) ) ;
#28231=CARTESIAN_POINT ( 'NONE',  ( -85.28888020613797494, -52.70782351190823078, 1.970730064499419676 ) ) ;
#28238=CARTESIAN_POINT ( 'NONE',  ( 64.81979848413079992, -29.99999999999996803, 107.4021778588664375 ) ) ;
#28240=CARTESIAN_POINT ( 'NONE',  ( -94.98233504546384154, -60.00000000000004263, -11.07720828487985720 ) ) ;
#28241=CARTESIAN_POINT ( 'NONE',  ( -76.26205980810522078, -25.60539408125360339, 115.8660843457751213 ) ) ;
#28243=CARTESIAN_POINT ( 'NONE',  ( 100.5651899622199039, -60.00000000000009948, 204.3456409986242477 ) ) ;
#28245=CARTESIAN_POINT ( 'NONE',  ( 27.95186532817653458, -57.67113474561467257, -43.11548192448071148 ) ) ;
#28255=CARTESIAN_POINT ( 'NONE',  ( -92.16331255555544999, -59.99999999999997158, 22.02966310501888003 ) ) ;
#28270=CARTESIAN_POINT ( 'NONE',  ( 32.30020061510025897, -18.68143019929715365, 30.13538509804329735 ) ) ;
#28271=( NAMED_UNIT ( * ) SI_UNIT ( $, .STERADIAN. ) SOLID_ANGLE_UNIT ( ) );
#28281=CARTESIAN_POINT ( 'NONE',  ( 92.68696368336701141, -60.00000000000000711, -4.489033240709536798 ) ) ;
#28289=CARTESIAN_POINT ( 'NONE',  ( -103.6855961668380388, -29.99999999989386978, 118.5309966294316126 ) ) ;
#28295=CARTESIAN_POINT ( 'NONE',  ( 84.14220056850236062, -52.73722939407674204, -14.99994838795616658 ) ) ;
#28306=CARTESIAN_POINT ( 'NONE',  ( 80.38791889184808781, -29.09062692944559458, 137.3129237731349974 ) ) ;
#28310=CARTESIAN_POINT ( 'NONE',  ( -92.76516906498835624, -57.61752273625296539, 204.4213914816233739 ) ) ;
#28311=EDGE_CURVE ( 'NONE', #50990, #80843, #23970, .T. ) ;
#28314=DIRECTION ( 'NONE',  ( 0.000000000000000000, 0.000000000000000000, 1.000000000000000000 ) ) ;
#28318=CARTESIAN_POINT ( 'NONE',  ( -49.54284130610121650, -29.59840805727827018, 45.89079715898707690 ) ) ;
#28319=CARTESIAN_POINT ( 'NONE',  ( -2.499999999999911182, -27.33278205846447406, -31.42875897075158420 ) ) ;
#28331=CARTESIAN_POINT ( 'NONE',  ( -50.11359024763238068, -27.54911214440137357, -27.96617461654303227 ) ) ;
#28332=CARTESIAN_POINT ( 'NONE',  ( -84.86247741117115595, -30.00000000000000355, 169.0207004501273786 ) ) ;
#28337=CARTESIAN_POINT ( 'NONE',  ( 75.27064724514200122, -57.56701362099152419, 191.4025409768277370 ) ) ;
#28339=CARTESIAN_POINT ( 'NONE',  ( 28.36231118427504327, -28.96865690853695341, -38.25004534194034989 ) ) ;
#28342=CARTESIAN_POINT ( 'NONE',  ( -72.02742768976531806, -59.99999999999998579, 154.4823517272751303 ) ) ;
#28345=CARTESIAN_POINT ( 'NONE',  ( -86.12932764275537068, -28.31670544872752160, 182.7863807612648941 ) ) ;
#28348=CARTESIAN_POINT ( 'NONE',  ( -2.014047270709469650, -39.47599645772569232, 30.46658341959906480 ) ) ;
#28367=CARTESIAN_POINT ( 'NONE',  ( 91.97789438503755832, -14.21045842199438880, 64.70176211216229945 ) ) ;
#28368=CARTESIAN_POINT ( 'NONE',  ( -82.38381349158181877, -29.09245844371520917, 149.5394180625729916 ) ) ;
#28373=CARTESIAN_POINT ( 'NONE',  ( 33.02302426302988181, -57.69141391618915549, 47.29285870251012369 ) ) ;
#28393=CARTESIAN_POINT ( 'NONE',  ( 92.42253650716426705, -60.00000000000000000, -12.04573449290273501 ) ) ;
#28394=CARTESIAN_POINT ( 'NONE',  ( -39.73689531673777964, -14.21045842199425735, 43.02931800076370195 ) ) ;
#28395=CARTESIAN_POINT ( 'NONE',  ( 18.79022120343070057, -29.03183620043990487, 29.12074868831081886 ) ) ;
#28398=CARTESIAN_POINT ( 'NONE',  ( -35.62035736894353732, -56.82933308392254190, 39.01374127240671896 ) ) ;
#28403=EDGE_CURVE ( 'NONE', #105826, #102392, #74123, .T. ) ;
#28406=CARTESIAN_POINT ( 'NONE',  ( -50.50675741891196679, -38.33489965697940249, 69.68679463715933764 ) ) ;
#28408=CARTESIAN_POINT ( 'NONE',  ( 100.8461010101613056, -30.00000000000000711, 163.5864315675907790 ) ) ;
#28411=CARTESIAN_POINT ( 'NONE',  ( 81.22126038271350978, -30.00000000000000000, 0.6198818140041580937 ) ) ;
#28432=CARTESIAN_POINT ( 'NONE',  ( 60.62648580738628112, -49.91109213625085772, 78.91779010420800944 ) ) ;
#28453=CARTESIAN_POINT ( 'NONE',  ( 86.38981295467488053, -17.31679843281874653, 180.1952732809204463 ) ) ;
#28465=CARTESIAN_POINT ( 'NONE',  ( -86.45353334008343893, -30.00000000000000000, 67.08143912832863975 ) ) ;
#28467=CARTESIAN_POINT ( 'NONE',  ( 24.14728948785597851, -57.67409579684246523, 42.95855127128432116 ) ) ;
#28475=CARTESIAN_POINT ( 'NONE',  ( 39.55779653878227009, -24.73393910763277503, -30.38590686191570356 ) ) ;
#28476=CARTESIAN_POINT ( 'NONE',  ( -25.24413934897445344, -49.91765848946642592, 33.57297437054807432 ) ) ;
#28480=CARTESIAN_POINT ( 'NONE',  ( -19.17790022078855827, -46.43920341883650593, 32.07300667617749923 ) ) ;
#28492=CARTESIAN_POINT ( 'NONE',  ( 103.2090184944486282, -60.16447056206801847, 192.4869700436993583 ) ) ;
#28507=CARTESIAN_POINT ( 'NONE',  ( -77.58781548604920886, -60.00000000000972733, -31.90504231437157756 ) ) ;
#28509=CARTESIAN_POINT ( 'NONE',  ( 81.75077423159443413, -59.99999999999513989, -29.65143176264461999 ) ) ;
#28513=CARTESIAN_POINT ( 'NONE',  ( -110.2447566669111154, -59.99999999999998579, 128.1452744908969521 ) ) ;
#28514=CARTESIAN_POINT ( 'NONE',  ( 3.977723760351280724, -22.06712578761976928, 27.56078887507262820 ) ) ;
#28516=CARTESIAN_POINT ( 'NONE',  ( -47.55744046191945529, -60.27975237171524014, 53.32522255953509926 ) ) ;
#28531=CARTESIAN_POINT ( 'NONE',  ( 89.50673784543010925, -30.00000000007396039, 3.352248442594707889 ) ) ;
#28537=CARTESIAN_POINT ( 'NONE',  ( 98.01492924831322284, -30.00000000000000000, 190.5156199418535152 ) ) ;
#28543=CARTESIAN_POINT ( 'NONE',  ( 55.26521301051785429, -29.08954164444167034, 56.68115046284776781 ) ) ;
#28547=CARTESIAN_POINT ( 'NONE',  ( -91.42805026571208771, -38.39309202493998185, -8.617090538173520997 ) ) ;
#28550=CARTESIAN_POINT ( 'NONE',  ( 88.56961690390389208, -38.54355387740943684, 200.1502377494141456 ) ) ;
#28552=CARTESIAN_POINT ( 'NONE',  ( 83.86163892754350968, -45.28585860511496719, 5.009633451048947528 ) ) ;
#28568=CARTESIAN_POINT ( 'NONE',  ( 11.94032942385361018, -16.68599286367008716, 34.79957533961248117 ) ) ;
#28572=CARTESIAN_POINT ( 'NONE',  ( 85.93733347156485536, -24.97102198799566253, 178.1358747736554164 ) ) ;
#28577=CARTESIAN_POINT ( 'NONE',  ( -91.04256780768773183, -60.15438401438225924, 61.63257487189168415 ) ) ;
#28586=CARTESIAN_POINT ( 'NONE',  ( 33.60718460261718121, -60.00000000000000000, 45.28735806869271840 ) ) ;
#28588=CARTESIAN_POINT ( 'NONE',  ( 6.493927703541009677, -18.97370440754745857, 35.15281767446274586 ) ) ;
#28590=CARTESIAN_POINT ( 'NONE',  ( 42.00705846777699293, -27.16471903480216454, 37.37245921768317203 ) ) ;
#28611=CARTESIAN_POINT ( 'NONE',  ( -1.564112305163676497, -34.58958035781643758, -32.65456768497247708 ) ) ;
#28620=CARTESIAN_POINT ( 'NONE',  ( -92.00833143843689754, -60.00000000000000711, 6.014465541360822343 ) ) ;
#28623=DIRECTION ( 'NONE',  ( 0.000000000000000000, 0.000000000000000000, -1.000000000000000000 ) ) ;
#28627=CARTESIAN_POINT ( 'NONE',  ( -82.28676419405165632, -42.97473223736994896, 168.7210715244461312 ) ) ;
#28639=CARTESIAN_POINT ( 'NONE',  ( -64.02773510654475331, -57.67113784069211135, -36.59462343474526591 ) ) ;
#28644=CARTESIAN_POINT ( 'NONE',  ( 72.33341283407553135, -14.21045842199439235, -25.95464913363236548 ) ) ;
#28645=CARTESIAN_POINT ( 'NONE',  ( -89.23267494088513274, -59.99999999999987921, 204.3671292578742680 ) ) ;
#28647=CARTESIAN_POINT ( 'NONE',  ( -55.86786607641659685, -36.02883296429982352, 60.77031267314215768 ) ) ;
#28648=ORIENTED_EDGE ( 'NONE', *, *, #51386, .F. ) ;
#28651=CARTESIAN_POINT ( 'NONE',  ( -100.4719902400335343, -45.25992542466413227, 192.0840524196355830 ) ) ;
#28652=CARTESIAN_POINT ( 'NONE',  ( 100.2031709646873310, -38.00000000000000000, 190.2875524083539744 ) ) ;
#28657=SURFACE_STYLE_FILL_AREA ( #102513 ) ;
#28663=CARTESIAN_POINT ( 'NONE',  ( 68.78515106805255641, -30.00000000000000000, 91.48474193797456167 ) ) ;
#28669=CARTESIAN_POINT ( 'NONE',  ( -29.17244825486319471, -39.48658745795624014, 32.84959031112921224 ) ) ;
#28670=CARTESIAN_POINT ( 'NONE',  ( 47.95189470694865719, -49.89909759463478878, 50.75627975532390224 ) ) ;
#28674=CARTESIAN_POINT ( 'NONE',  ( -86.58980629399917461, -38.61205887094109812, 199.3558248615631214 ) ) ;
#28678=CARTESIAN_POINT ( 'NONE',  ( 81.86055861641301590, -59.99999999999994316, 186.9037213880110926 ) ) ;
#28687=FACE_BOUND ( 'NONE', #94466, .T. ) ;
#28688=CARTESIAN_POINT ( 'NONE',  ( 112.1074610866378691, -60.00000000000000711, 166.9029264543243301 ) ) ;
#28696=CARTESIAN_POINT ( 'NONE',  ( -71.80342408229677176, -30.00000000000000711, -19.71767938363505834 ) ) ;
#28698=CARTESIAN_POINT ( 'NONE',  ( -58.27688207720395752, -38.34417119533264184, 91.02890418086518309 ) ) ;
#28708=CARTESIAN_POINT ( 'NONE',  ( 84.34664725709313871, -29.01649459423289557, 165.8781276598768954 ) ) ;
#28755=CARTESIAN_POINT ( 'NONE',  ( -106.6453062919850225, -60.00000000000000000, 197.5725164084929872 ) ) ;
#28764=CARTESIAN_POINT ( 'NONE',  ( -82.57751153944624889, -53.60564265856869071, 184.4179057790843217 ) ) ;
#28772=CARTESIAN_POINT ( 'NONE',  ( -84.13707156515019392, -45.27010591465764833, 0.6314432930867477367 ) ) ;
#28778=CARTESIAN_POINT ( 'NONE',  ( 62.45579587598661675, -29.99999999999998934, 99.43503315974342627 ) ) ;
#28779=CARTESIAN_POINT ( 'NONE',  ( -87.19976908022060513, -14.21045842199435860, -12.72659765151139233 ) ) ;
#28780=CARTESIAN_POINT ( 'NONE',  ( -63.81267340554329337, -53.39190204468273038, 89.97204334792978386 ) ) ;
#28782=CARTESIAN_POINT ( 'NONE',  ( 89.23375057675741573, -59.99999999999977973, 204.3679297810271862 ) ) ;
#28784=CARTESIAN_POINT ( 'NONE',  ( 9.918622661780615246, -60.00000000000981970, 42.00659582329527097 ) ) ;
#28796=CARTESIAN_POINT ( 'NONE',  ( -80.27472688732939332, -60.00000000000000000, -27.80218209016123510 ) ) ;
#28801=CARTESIAN_POINT ( 'NONE',  ( 12.64023069600375315, -4.285714285714297134, 21.88880945939638778 ) ) ;
#28811=CARTESIAN_POINT ( 'NONE',  ( 34.67182219425094303, -39.49850266814299715, 35.14395799684566413 ) ) ;
#28812=FILL_AREA_STYLE_COLOUR ( '', #12759 ) ;
#28826=CARTESIAN_POINT ( 'NONE',  ( 91.87288384113435313, -60.00000000000000000, 10.25306695411674873 ) ) ;
#28836=CARTESIAN_POINT ( 'NONE',  ( -108.9347409199276342, -29.99999999999999289, 183.7868372424095185 ) ) ;
#28852=B_SPLINE_CURVE_WITH_KNOTS ( 'NONE', 3,
 ( #68908, #12232, #3090, #86164, #76973, #45163, #20928, #36036, #53763, #37627, #11695, #3631, #78561, #79099, #36567, #4694, #78044, #62404, #94236, #101784, #44630, #95298, #69436, #69957, #54267, #21427, #4161, #86691, #77518, #87209, #37092, #102855, #70490, #44089, #52164, #5222, #28467, #103383, #13284, #29532, #27952, #61345, #46213, #60815, #12760, #102315, #71008, #94782, #20399, #53243, #38151, #29022, #93705, #103901, #60294, #61887, #45683, #93168, #19334, #85076, #19857, #11160, #52692, #85619, #23018, #104428, #65035, #6796, #6253, #97930, #88267, #72067, #104977, #31636, #7315, #23548, #89324, #5740, #14880, #47251, #30577, #56390, #62932, #48305, #30045, #80675, #80152, #63471, #95827, #21957, #31118, #14346, #96367, #24082, #71527, #7849, #38660, #88789, #54808, #22497, #15418, #55337, #56923, #89849, #15954, #39715, #81201, #97387, #40229, #64006, #96881, #55849, #46733, #39190, #47773, #72591, #87740, #105497, #64519, #79623, #73097, #106010, #32156, #48832, #81722, #40754, #73644, #13819, #74707, #16487, #8915, #90918, #25138, #32701, #41820, #25691, #49366, #787, #83874, #82275, #91455, #33759, #100588, #257, #8387, #58555, #41289, #17569, #67177, #74177, #100057, #9986, #57996, #49907, #18102, #18646, #82815, #50961, #50430, #1880, #66632, #59084, #42889, #34836, #99516, #9432, #26747, #67707, #83342, #26224, #17031, #59624, #42353, #75240, #75786, #90374, #98455, #51504, #1337, #92494, #84420, #33224, #10513, #34301, #43428, #66099, #91970, #106548, #65568, #24607, #57456, #98973, #78438, #69311, #19199, #29405, #54146, #53115, #69828, #94101, #19728, #12109, #20267, #28337, #61761, #45038, #102188, #43955, #4562, #86036, #52565, #37499, #27821, #11569, #44499, #77923, #53636, #102727, #28889, #52036, #61213, #12632, #4032, #94657, #2422, #20803, #76309, #36962, #93579, #76846, #35365, #68234, #77388, #60691, #2951, #70363, #11037, #87086, #84948, #86569, #101127, #3502, #45566, #101663, #103258, #62286, #95177, #21308, #13161, #27288, #60171, #93038, #35908, #85490, #68782, #36443, #14223, #40110, #54677, #39600, #88143, #55216, #87614, #56263, #6671, #95695, #71404, #38027, #62807, #81087, #89199, #15297, #63345, #30451, #88663, #63875, #104849, #31518, #14753, #39065, #13696, #32038, #47127, #21838, #78971, #29921, #96241, #46608, #64400, #47656, #64918, #96763, #80551, #48184, #7197, #22894, #72472, #5096, #97274, #46089, #55732, #97801, #105379, #23421, #80024, #6136, #72985, #105891, #23966, #56808, #70886, #89732, #103779, #79504, #71946, #5615, #104301, #38539, #22372, #30993, #41701, #99379, #50310, #24495, #17443, #90253, #1202, #41173, #26101, #660, #58418, #81599, #7725, #49784, #15828, #99926, #8260, #65450, #17972, #98851, #67048, #33106, #82147, #83216, #40632, #25011, #74052, #32576, #66501, #16905, #91331, #73517, #34170, #50829, #57331, #65970, #25560, #42220, #82688, #9310, #75105, #49241, #140, #57865, #58956, #74584, #91844, #8793, #48710, #98341, #90792, #33627, #106417, #16356, #39309, #38774, #79215, #55974, #72191, #56515, #88386, #55451, #87852, #71123, #15535, #46326, #71640, #14459, #97500, #48428, #89445, #96996, #6373, #104549, #5850, #80799, #47371, #23133, #81320, #62518, #64121, #95403, #104013, #88904, #30157, #63043, #13933, #95946, #7431, #80261, #31233, #47892, #38262, #15001, #22069, #31751, #46845, #70602, #105095, #6912, #29644, #39832, #103495, #23664, #54927, #13403, #21543, #30700, #64632, #79745, #5340, #96477, #87323, #22615, #72708, #63588, #105608, #54378, #98576, #90496, #58671, #51078, #40880, #82402, #33882, #83460, #58119, #99643, #9560, #42467, #16605, #50027, #34426, #75363, #91047, #905, #57573, #67298, #25259, #66214, #99097, #41938, #33345, #17156, #100176, #16069, #24723, #73768, #1464, #8505, #26345, #48952, #66758, #41408, #83999, #74824, #49496, #74299, #59206, #82932, #89964, #57046, #92083, #18224, #40347, #375, #9029, #25818, #91573, #17680, #50544, #73225, #106126, #7968, #32282, #65152, #98051, #24200, #81846, #106667, #32815, #65688, #29013, #60288, #61337, #36027, #12224, #44080, #51623, #101257, #52154, #76426, #35484, #76965, #37084, #19848, #69948, #60804, #78035, #75903, #84542, #68901, #18775 ),
 .UNSPECIFIED., .F., .F.,
 ( 4, 2, 1, 1, 1, 1, 1, 1, 2, 2, 2, 2, 2, 2, 2, 1, 2, 2, 1, 1, 1, 2, 2, 2, 2, 2, 1, 2, 2, 1, 2, 2, 2, 1, 1, 1, 2, 2, 2, 1, 2, 2, 1, 1, 1, 2, 2, 2, 2, 1, 1, 2, 2, 1, 1, 2, 2, 2, 1, 1, 1, 2, 2, 1, 1, 2, 2, 2, 1, 1, 2, 2, 1, 1, 1, 1, 2, 2, 2, 2, 2, 2, 1, 2, 2, 1, 2, 2, 2, 2, 2, 1, 2, 2, 1, 1, 1, 1, 2, 2, 2, 1, 1, 2, 2, 1, 2, 2, 2, 1, 2, 2, 1, 1, 2, 2, 2, 2, 1, 2, 2, 2, 2, 2, 1, 2, 2, 1, 1, 2, 2, 2, 2, 1, 1, 2, 2, 2, 2, 2, 2, 1, 2, 2, 1, 2, 2, 2, 1, 2, 2, 1, 2, 2, 2, 1, 1, 1, 1, 2, 2, 2, 2, 1, 2, 2, 1, 1, 1, 2, 2, 2, 2, 2, 2, 1, 1, 1, 2, 2, 2, 2, 1, 2, 2, 1, 2, 2, 2, 2, 2, 2, 1, 1, 2, 2, 2, 2, 2, 2, 2, 1, 1, 2, 2, 1, 2, 2, 2, 2, 2, 2, 2, 2, 2, 1, 1, 2, 2, 1, 1, 1, 1, 2, 2, 2, 2, 2, 2, 2, 1, 1, 1, 1, 1, 2, 2, 1, 1, 2, 2, 2, 1, 1, 1, 2, 2, 1, 1, 1, 2, 2, 2, 2, 1, 1, 2, 2, 1, 1, 1, 2, 2, 2, 2, 1, 2, 2, 1, 1, 1, 2, 2, 2, 1, 1, 2, 2, 2, 2, 2, 2, 2, 1, 1, 1, 2, 2, 2, 2, 1, 2, 2, 1, 1, 1, 1, 2, 2, 2, 2, 2, 2, 1, 1, 1, 1, 2, 2, 2, 2, 2, 2, 2, 2, 2, 2, 2, 2, 4 ),
 ( 0.000000000000000000, 1.525878906243263716E-05, 3.051757812486527433E-05, 6.103515624973057576E-05, 0.0001220703124994611515, 0.0002441406249989222488, 0.0004882812499978443892, 0.0009765624999956887785, 0.001953124999991377123, 0.003906249999982753813, 0.007812499999965508493, 0.01562499999993101872, 0.02343749999989653068, 0.03124999999986202703, 0.03515624999984477694, 0.03564453124984255650, 0.03570556640609228588, 0.03573608398421715404, 0.03576660156234201526, 0.03588867187484149485, 0.03613281249984046095, 0.03710937499983629762, 0.03906249999982795706, 0.04687499999979457405, 0.05078124999977788601, 0.05273437499976953852, 0.05322265624976742215, 0.05346679687476636744, 0.05358886718726584703, 0.05371093749976533355, 0.05468749999976125348, 0.06249999999972860598, 0.06262207031222810638, 0.06274414062472760678, 0.06298828124972663534, 0.06347656249972469245, 0.06445312499972079279, 0.06640624999971297959, 0.07031249999969736708, 0.07128906249969346742, 0.07141113281219298170, 0.07147216796844274578, 0.07153320312469249598, 0.07177734374969177433, 0.07226562499969023390, 0.07421874999968423869, 0.07812499999967219277, 0.08593749999964817032, 0.08789062499964214736, 0.08886718749963912201, 0.08911132812463838648, 0.08923339843713799791, 0.08929443359338778974, 0.08935546874963759545, 0.08984374999963599950, 0.09374999999962320418, 0.1015624999995976691, 0.1054687499995848599, 0.1064453124995816818, 0.1069335937495801275, 0.1070556640620797112, 0.1071166992183295030, 0.1071472167964543920, 0.1071777343745792810, 0.1074218749995787259, 0.1093749999995740768, 0.1249999999995368705, 0.1406249999994996780, 0.1425781249994950706, 0.1428222656244944877, 0.1428527832026193767, 0.1428833007807442934, 0.1429443359369942934, 0.1430664062494943489, 0.1435546874994940714, 0.1445312499994932387, 0.1484374999994895750, 0.1562499999994824140, 0.1718749999994681199, 0.1874999999994538258, 0.2031249999994395317, 0.2109374999994323985, 0.2128906249994305944, 0.2138671874994296784, 0.2143554687494292066, 0.2148437499994287625, 0.2187499999994252653, 0.2499999999993973154, 0.2656249999993833266, 0.2812499999993693933, 0.2851562499993659516, 0.2856445312493656741, 0.2857055664056155075, 0.2857360839837404520, 0.2857666015618653965, 0.2858886718743650635, 0.2861328124993642308, 0.2871093749993612887, 0.2890624999993551825, 0.2968749999993313682, 0.3007812499993194333, 0.3027343749993134936, 0.3032226562493120503, 0.3034667968743114397, 0.3035888671868111066, 0.3037109374993107735, 0.3046874999993075539, 0.3124999999992819633, 0.3203124999992564281, 0.3212890624992533195, 0.3214111328117529309, 0.3215332031242525423, 0.3217773437492516542, 0.3222656249992499333, 0.3242187499992429944, 0.3281249999992290611, 0.3359374999992012500, 0.3378906249991942556, 0.3388671874991907584, 0.3391113281241897037, 0.3393554687491887045, 0.3398437499991866506, 0.3437499999991696087, 0.3476562499991526223, 0.3481445312491504573, 0.3482055664054001798, 0.3482666015616499022, 0.3483886718741493471, 0.3486328124991484589, 0.3496093749991446842, 0.3515624999991371902, 0.3554687499991220911, 0.3564453124991184274, 0.3569335937491165400, 0.3570556640616160404, 0.3571166992178658739, 0.3571777343741157074, 0.3574218749991152633, 0.3593749999991109889, 0.3632812499991022737, 0.3652343749990979993, 0.3657226562490968336, 0.3659667968740962785, 0.3660888671865960009, 0.3662109374990956678, 0.3671874999990931143, 0.3691406249990881738, 0.3701171874990857313, 0.3703613281240851762, 0.3704833984365848987, 0.3705444335928347321, 0.3706054687490845656, 0.3710937499990832333, 0.3749999999990726307, 0.3750610351553224642, 0.3751220703115722976, 0.3752441406240719091, 0.3754882812490710209, 0.3759765624990693555, 0.3769531249990659139, 0.3789062499990589750, 0.3828124999990452082, 0.3837890624990417665, 0.3839111328115412669, 0.3839263916006037114, 0.3839416503896661559, 0.3839721679677911004, 0.3840332031240412114, 0.3842773437490414334, 0.3847656249990420996, 0.3867187499990447086, 0.3906249999990498156, 0.3925781249990523691, 0.3928222656240527022, 0.3928833007803027577, 0.3929443359365528132, 0.3930664062490529798, 0.3935546874990535904, 0.3945312499990548671, 0.3984374999990598076, 0.4003906249990623056, 0.4013671874990635269, 0.4016113281240637489, 0.4017333984365638044, 0.4017944335928138044, 0.4018554687490638044, 0.4023437499990634714, 0.4062499999990610844, 0.4101562499990586419, 0.4106445312490583088, 0.4107055664053083088, 0.4107666015615583643, 0.4108886718740583088, 0.4111328124990581423, 0.4121093749990578092, 0.4140624999990570876, 0.4179687499990558108, 0.4199218749990552002, 0.4218749999990546451, 0.4257812499990533128, 0.4277343749990527022, 0.4282226562490524802, 0.4284667968740524802, 0.4285278320303024802, 0.4285888671865524802, 0.4287109374990525912, 0.4296874999990539790, 0.4374999999990648036, 0.4453124999990756838, 0.4531249999990865640, 0.4687499999991082134, 0.4843749999991299182, 0.4999999999991515676, 0.5312499999991950883, 0.5624999999992387201, 0.5703124999992494892, 0.5712890624992508215, 0.5714111328117509325, 0.5714721679680011546, 0.5715332031242513766, 0.5717773437492519317, 0.5722656249992531530, 0.5742187499992581490, 0.5781249999992679189, 0.5937499999993074429, 0.6249999999993862687, 0.6562499999994652056, 0.6874999999995440314, 0.7031249999995835553, 0.7109374999996032063, 0.7128906249996082023, 0.7138671874996106448, 0.7141113281246111999, 0.7142333984371115330, 0.7142639160152366440, 0.7142791748042991440, 0.7142944335933617550, 0.7143554687496118660, 0.7148437499996128652, 0.7187499999996208588, 0.7343749999996527222, 0.7421874999996688205, 0.7426757812496697087, 0.7427978515621699307, 0.7428283691402950417, 0.7428436279293576527, 0.7428588867184201527, 0.7429199218746702638, 0.7431640624996705968, 0.7441406249996721511, 0.7460937499996752598, 0.7499999999996815880, 0.7578124999996940225, 0.7617187499997003508, 0.7636718749997034594, 0.7641601562497042366, 0.7642822265622044586, 0.7643127441403295697, 0.7643432617184546807, 0.7644042968747046807, 0.7646484374997051248, 0.7656249999997067901, 0.7734374999997198907, 0.7812499999997329914, 0.7851562499997395417, 0.7856445312497404299, 0.7857055664059904299, 0.7857666015622405409, 0.7858886718747407629, 0.7861328124997410960, 0.7871093749997426503, 0.7890624999997459810, 0.7968749999997589706, 0.8007812499997655209, 0.8027343749997687405, 0.8032226562497696287, 0.8034667968747699618, 0.8037109374997702949, 0.8046874999997718492, 0.8124999999997845057, 0.8144531249997876143, 0.8154296874997891686, 0.8154907226560392797, 0.8155517578122892797, 0.8156738281247896127, 0.8159179687497900568, 0.8164062499997909450, 0.8183593749997947198, 0.8203124999997983835, 0.8212890624998001599, 0.8214111328123003819, 0.8214263916013629929, 0.8214416503904254929, 0.8214721679685504929, 0.8215332031248006039, 0.8217773437498008260, 0.8222656249998012701, 0.8242187499998036015, 0.8281249999998080424, 0.8359374999998170352, 0.8398437499998213651, 0.8417968749998236966, 0.8418579101560736966, 0.8419189453123238076, 0.8420410156248239186, 0.8422851562498241407, 0.8427734374998246958, 0.8437499999998258060, 0.8515624999998342437, 0.8554687499998385736, 0.8564453124998395728, 0.8574218749998405720, 0.8593749999998427924, 0.8749999999998602229, 0.8906249999998777644, 0.9062499999998953060, 0.9374999999999301670, 0.9687499999999651390, 0.9843749999999825695, 1.000000000000000000 ),
 .UNSPECIFIED. ) ;
#28855=CARTESIAN_POINT ( 'NONE',  ( 78.67412638886875698, -56.84030183992913265, 157.0013697797242003 ) ) ;
#28860=CARTESIAN_POINT ( 'NONE',  ( -74.79081370483122271, -57.58316160299655451, 190.1003635006443346 ) ) ;
#28870=CARTESIAN_POINT ( 'NONE',  ( -40.04143003125063416, -26.34375225975082202, 35.98697943332009430 ) ) ;
#28883=CARTESIAN_POINT ( 'NONE',  ( 72.41334042352660560, -30.15556180264357167, -28.78532156097261563 ) ) ;
#28884=CARTESIAN_POINT ( 'NONE',  ( -73.96231721666636361, -30.00000000000000000, 108.7202594212511286 ) ) ;
#28889=CARTESIAN_POINT ( 'NONE',  ( 77.70094160008299866, -57.51527222009625007, 196.1490637833984181 ) ) ;
#28891=DIRECTION ( 'NONE',  ( 0.000000000000000000, -1.000000000000000000, 0.000000000000000000 ) ) ;
#28894=CARTESIAN_POINT ( 'NONE',  ( -58.54394063265895909, -60.00000000000000711, 95.84204639138707194 ) ) ;
#28899=CARTESIAN_POINT ( 'NONE',  ( -85.11955292133191620, -50.19866990164982212, 189.4213824591150228 ) ) ;
#28902=CARTESIAN_POINT ( 'NONE',  ( -3.020169591079187033, -35.99429810687945519, 29.88393149923355452 ) ) ;
#28914=CARTESIAN_POINT ( 'NONE',  ( -13.66642973271509831, 3.860411657743955287E-12, 17.78317311657911404 ) ) ;
#28916=CARTESIAN_POINT ( 'NONE',  ( 99.06540890750190442, -59.99999999999989342, 60.62284496578245552 ) ) ;
#28917=CARTESIAN_POINT ( 'NONE',  ( -78.59050543240782360, -42.96833819150651124, 140.9031260219249759 ) ) ;
#28922=CARTESIAN_POINT ( 'NONE',  ( 19.63101818396287257, -57.67185339817164191, 42.14267493330406467 ) ) ;
#28942=CARTESIAN_POINT ( 'NONE',  ( -66.64776185298879341, -30.00000000000000711, 114.0837597745640721 ) ) ;
#28943=CARTESIAN_POINT ( 'NONE',  ( 27.89594507718583571, -53.38588701379882906, 34.87338555987020072 ) ) ;
#28947=CARTESIAN_POINT ( 'NONE',  ( -35.43501430766470861, -53.36447985331461297, 38.23648758541151693 ) ) ;
#28957=CARTESIAN_POINT ( 'NONE',  ( -51.86356884536327527, -38.33854880839309232, 73.08413421716038272 ) ) ;
#28959=CARTESIAN_POINT ( 'NONE',  ( 98.90803512229713590, -29.99999999999997868, 189.0481524369670012 ) ) ;
#28964=CARTESIAN_POINT ( 'NONE',  ( 81.43483218857002726, -30.00000000000000355, -9.794887574534724806 ) ) ;
#28988=CARTESIAN_POINT ( 'NONE',  ( 63.03724330110081553, -49.91051537755201650, 85.83604783815560779 ) ) ;
#29009=CARTESIAN_POINT ( 'NONE',  ( 86.38779590130293684, -17.19466876150733370, 181.4510809460217615 ) ) ;
#29013=CARTESIAN_POINT ( 'NONE',  ( 76.23378044719352431, -57.67121141546430607, -32.09450996628105912 ) ) ;
#29014=CARTESIAN_POINT ( 'NONE',  ( 58.71306015749776464, -29.11378994003339216, -25.44451803556423641 ) ) ;
#29018=CARTESIAN_POINT ( 'NONE',  ( -101.1538706603591180, -30.00000000000000355, 168.9986721791281639 ) ) ;
#29022=CARTESIAN_POINT ( 'NONE',  ( 31.98563216593261416, -57.68901072815521758, 46.54681308492085634 ) ) ;
#29035=CARTESIAN_POINT ( 'NONE',  ( -18.30425709642254972, -60.36451714365048105, 34.31014664571683426 ) ) ;
#29039=VECTOR ( 'NONE', #16500, 1000.000000000000000 ) ;
#29049=CARTESIAN_POINT ( 'NONE',  ( 101.0450726704344646, -45.28112087516579010, 191.2503734327964366 ) ) ;
#29063=CARTESIAN_POINT ( 'NONE',  ( -96.34159525672876612, -59.99999999990227906, 41.34496478704701872 ) ) ;
#29065=CARTESIAN_POINT ( 'NONE',  ( 51.58253327500602126, -59.99999999998549782, -40.00153396047142706 ) ) ;
#29069=CARTESIAN_POINT ( 'NONE',  ( -97.09821068641753072, -30.00000000000001776, 79.69957433219180132 ) ) ;
#29070=CARTESIAN_POINT ( 'NONE',  ( 11.40768022813701243, -46.43473930232784141, 31.65783319488408409 ) ) ;
#29074=CARTESIAN_POINT ( 'NONE',  ( -48.45733930310002080, -56.82700549898684983, 53.79929747904154169 ) ) ;
#29084=ORIENTED_EDGE ( 'NONE', *, *, #62503, .T. ) ;
#29085=CARTESIAN_POINT ( 'NONE',  ( 108.6711098457755611, -30.00000000000668621, 155.0946490741732191 ) ) ;
#29089=CARTESIAN_POINT ( 'NONE',  ( 100.7015874939240376, -30.00000000000000000, 161.8710660039678828 ) ) ;
#29094=CARTESIAN_POINT ( 'NONE',  ( 54.36390350096709057, -49.90582396615677396, 63.10843653790805519 ) ) ;
#29104=CARTESIAN_POINT ( 'NONE',  ( 98.56158271022805195, -38.47369220965149594, 200.8892253048653629 ) ) ;
#29106=CARTESIAN_POINT ( 'NONE',  ( 85.05651546852904232, -52.70738422179273641, 5.798279539873188781 ) ) ;
#29109=DIRECTION ( 'NONE',  ( 0.000000000000000000, 1.000000000000000000, 0.000000000000000000 ) ) ;
#29124=CARTESIAN_POINT ( 'NONE',  ( 37.81320834215699733, -27.69356383356495854, 44.71441020632808971 ) ) ;
#29128=CARTESIAN_POINT ( 'NONE',  ( 86.18054470901965658, -21.36750242109700793, 176.9380357467274507 ) ) ;
#29133=CARTESIAN_POINT ( 'NONE',  ( -99.60505029529538490, -52.71012916261938130, 120.4313145599469408 ) ) ;
#29137=CARTESIAN_POINT ( 'NONE',  ( -9.186147765600862769, -22.42665461655586157, -38.54335720488538897 ) ) ;
#29139=CARTESIAN_POINT ( 'NONE',  ( 15.03942254395109046, -22.71148339282385820, 35.93912477487155854 ) ) ;
#29140=CARTESIAN_POINT ( 'NONE',  ( 46.54793763053436351, -28.81014148338916314, 41.79554432402118636 ) ) ;
#29156=CARTESIAN_POINT ( 'NONE',  ( 6.278603737950535724, -34.58964686943891564, -32.56275994427586795 ) ) ;
#29165=CARTESIAN_POINT ( 'NONE',  ( -91.93118328357623170, -60.00000000000001421, 7.837162816498209672 ) ) ;
#29174=CARTESIAN_POINT ( 'NONE',  ( -82.83002596087247582, -39.49110685017327427, 168.2621467706148906 ) ) ;
#29184=CARTESIAN_POINT ( 'NONE',  ( -98.27571109168336250, -57.67134109913899209, 58.06786128689789450 ) ) ;
#29193=CARTESIAN_POINT ( 'NONE',  ( 61.70037527280209844, -30.00000000000006040, -32.45262418874342103 ) ) ;
#29195=CARTESIAN_POINT ( 'NONE',  ( -67.93243969554674777, -60.00000000000000711, 143.1807200622937728 ) ) ;
#29196=CARTESIAN_POINT ( 'NONE',  ( -54.05961884913804738, -56.85113118587781145, 65.25060302166593829 ) ) ;
#29200=CARTESIAN_POINT ( 'NONE',  ( -101.4140262225946003, -52.72498359022472414, 192.9040562268387191 ) ) ;
#29211=CARTESIAN_POINT ( 'NONE',  ( 56.86967849623623295, -29.99999999999999645, 59.52404653438935611 ) ) ;
#29216=CARTESIAN_POINT ( 'NONE',  ( -27.49130160687422375, -29.05394088803144115, 30.53830709630566531 ) ) ;
#29218=CARTESIAN_POINT ( 'NONE',  ( 48.06845630413710069, -36.06226588698234536, 46.66767315606317368 ) ) ;
#29221=LINE ( 'NONE', #79827, #47888 ) ;
#29222=CARTESIAN_POINT ( 'NONE',  ( -89.30654270732652833, -38.52662107162988292, 200.3831435256876432 ) ) ;
#29224=CARTESIAN_POINT ( 'NONE',  ( 90.39058703242112358, -38.40011783027308212, -14.99676332985419691 ) ) ;
#29228=COLOUR_RGB ( '', 0.31764706, 0.68627451, 0.89019608) ;
#29231=CARTESIAN_POINT ( 'NONE',  ( 112.1662010274523453, -59.99999999999999289, 176.3906357321001508 ) ) ;
#29235=ORIENTED_EDGE ( 'NONE', *, *, #51268, .T. ) ;
#29236=CARTESIAN_POINT ( 'NONE',  ( -91.06811619128255586, -38.35144331576948673, 1.256099165720845345 ) ) ;
#29248=CARTESIAN_POINT ( 'NONE',  ( 85.74730987966626117, -18.52705124433025219, 162.5160542404693444 ) ) ;
#29251=ORIENTED_EDGE ( 'NONE', *, *, #54806, .F. ) ;
#29260=CARTESIAN_POINT ( 'NONE',  ( -72.75733770493380348, -30.00000000000000355, -19.25270559974459061 ) ) ;
#29278=DIRECTION ( 'NONE',  ( -3.673940397442057649E-17, 0.000000000000000000, -1.000000000000000000 ) ) ;
#29285=CARTESIAN_POINT ( 'NONE',  ( -94.64169479211049918, -60.00000000000000000, 202.5669859057673534 ) ) ;
#29290=CARTESIAN_POINT ( 'NONE',  ( -86.30021902774615228, -18.16438055758039027, 170.9070947866538575 ) ) ;
#29296=CARTESIAN_POINT ( 'NONE',  ( -86.97225581348263290, -60.15082631087481957, 29.24283001683475192 ) ) ;
#29301=CARTESIAN_POINT ( 'NONE',  ( 97.80297141475710987, -14.21045842199415432, 197.6895799465713708 ) ) ;
#29303=CARTESIAN_POINT ( 'NONE',  ( -97.09821068641753072, -30.00000000000001776, 79.69957433219180132 ) ) ;
#29304=CARTESIAN_POINT ( 'NONE',  ( -63.47421256789260724, -42.96224801778237889, 83.53665870048976672 ) ) ;
#29306=CARTESIAN_POINT ( 'NONE',  ( 107.3649583438541271, -29.99999999999998579, 190.7484263893222192 ) ) ;
#29308=CARTESIAN_POINT ( 'NONE',  ( 53.27405869684046991, -60.00000000005845635, 87.46234259303579961 ) ) ;
#29317=CARTESIAN_POINT ( 'NONE',  ( -92.06659163830985904, -60.00000000000001421, -13.68159610222980760 ) ) ;
#29322=CARTESIAN_POINT ( 'NONE',  ( 3.301565691951512616, -4.285714285714295357, 25.05982991920904013 ) ) ;
#29332=CARTESIAN_POINT ( 'NONE',  ( 32.59170211760999081, -29.08667747155562822, 32.21612061202412036 ) ) ;
#29333=CARTESIAN_POINT ( 'NONE',  ( 3.301606509414339641, -4.285714285714286476, -25.22241582816893413 ) ) ;
#29348=CARTESIAN_POINT ( 'NONE',  ( 92.56983564317958724, -60.00000000000000000, -2.305466784945364278 ) ) ;
#29353=CARTESIAN_POINT ( 'NONE',  ( -83.51106636389977211, -30.00000000000859757, 196.0047889519032935 ) ) ;
#29359=CARTESIAN_POINT ( 'NONE',  ( 84.58342993391340769, -60.18021989816856632, -16.69648072670474193 ) ) ;
#29369=CARTESIAN_POINT ( 'NONE',  ( 77.57230420934776305, -49.90228353259792726, 141.6236765526268186 ) ) ;
#29374=CARTESIAN_POINT ( 'NONE',  ( -76.05665976993959987, -57.54410268428485153, 193.2876952671887523 ) ) ;
#29386=CARTESIAN_POINT ( 'NONE',  ( -53.08935917470201815, -30.00000000000000000, 52.21147893555080799 ) ) ;
#29398=CARTESIAN_POINT ( 'NONE',  ( -26.58951646937336122, -22.83209710930301384, -37.42561714443979781 ) ) ;
#29399=CARTESIAN_POINT ( 'NONE',  ( -82.13850053252956229, -30.00000000000000000, 146.8543398922747372 ) ) ;
#29405=CARTESIAN_POINT ( 'NONE',  ( 74.07983334089789196, -57.61003258331666643, 187.3778442680205387 ) ) ;
#29413=CARTESIAN_POINT ( 'NONE',  ( -65.49076136059264286, -60.00000000000000711, 120.3024543388731047 ) ) ;
#29419=CARTESIAN_POINT ( 'NONE',  ( -86.32942810031956071, -21.03686018850741846, 180.4869550100015942 ) ) ;
#29435=CARTESIAN_POINT ( 'NONE',  ( -21.65942590380950605, 4.828984019150144164E-12, 5.820808985950977288 ) ) ;
#29437=CARTESIAN_POINT ( 'NONE',  ( 108.9225596800844897, -59.99999999999995737, 119.6931403564588123 ) ) ;
#29439=CARTESIAN_POINT ( 'NONE',  ( -77.19855406467927139, -56.84693317175008787, 146.5104320596075240 ) ) ;
#29443=CARTESIAN_POINT ( 'NONE',  ( 75.69611295408795115, -57.55331998792648562, 192.5082608592401812 ) ) ;
#29463=CARTESIAN_POINT ( 'NONE',  ( 60.59807815084354132, -59.99999999999997868, -35.49710509377640477 ) ) ;
#29464=CARTESIAN_POINT ( 'NONE',  ( -49.67087318978585841, -59.99999999999999289, 77.31351762338060496 ) ) ;
#29465=CARTESIAN_POINT ( 'NONE',  ( 26.49659615693567005, -49.91097369680763052, 33.89243893083332893 ) ) ;
#29480=CARTESIAN_POINT ( 'NONE',  ( 81.33754917041331112, -29.99999999999999645, -1.044461975028134759 ) ) ;
#29504=CARTESIAN_POINT ( 'NONE',  ( -82.14545208350013183, -60.00000000000006395, 187.9265396763507567 ) ) ;
#29505=CARTESIAN_POINT ( 'NONE',  ( 64.14738722512768732, -42.95805876620670460, 85.49931417512519261 ) ) ;
#29508=CARTESIAN_POINT ( 'NONE',  ( -46.27818643745989391, -34.68435135132106240, -36.71170783072079047 ) ) ;
#29521=CARTESIAN_POINT ( 'NONE',  ( 86.58602178717934805, -20.72065498216530699, 184.1443362589780008 ) ) ;
#29528=CARTESIAN_POINT ( 'NONE',  ( -100.7573317175203584, -29.99999999999998934, 180.7148766695847542 ) ) ;
#29532=CARTESIAN_POINT ( 'NONE',  ( 27.29310425584678157, -57.67805528695544126, 43.98917206289641513 ) ) ;
#29542=CARTESIAN_POINT ( 'NONE',  ( -86.95016803385389892, -20.65679883627421987, 186.2957625121753722 ) ) ;
#29547=CARTESIAN_POINT ( 'NONE',  ( -13.22635504380575355, -22.06836642973110330, 27.64052428449707577 ) ) ;
#29549=CARTESIAN_POINT ( 'NONE',  ( -86.67772857939944231, -60.00000000000007816, -11.42669097351372187 ) ) ;
#29553=B_SPLINE_CURVE_WITH_KNOTS ( 'NONE', 3,
 ( #4851, #53913, #86845, #5384, #28100, #101940, #60975, #62052, #52863, #95446, #13978, #20021, #38304, #95988, #71164, #104059, #4315, #11865, #77683, #20567, #63087, #12920, #30201, #85791, #22113, #86324, #29688, #102486, #69594, #44794, #45842, #37250, #70113, #37785 ),
 .UNSPECIFIED., .F., .F.,
 ( 4, 2, 2, 2, 2, 2, 2, 2, 2, 2, 2, 2, 2, 2, 2, 2, 4 ),
 ( 0.5000000000000000000, 0.5312500000000000000, 0.5625000000000000000, 0.5937500000000000000, 0.6250000000000000000, 0.6562500000000000000, 0.6875000000000000000, 0.7187500000000000000, 0.7500000000000000000, 0.7812500000000000000, 0.8125000000000000000, 0.8437500000000000000, 0.8750000000000000000, 0.9062500000000000000, 0.9375000000000000000, 0.9687500000000000000, 1.000000000000000000 ),
 .UNSPECIFIED. ) ;
#29562=CARTESIAN_POINT ( 'NONE',  ( 50.54929637512975660, -37.96391612271221305, 51.13126295237949392 ) ) ;
#29575=CARTESIAN_POINT ( 'NONE',  ( -114.2613009911679427, -59.99999999997056221, 181.1642683633762942 ) ) ;
#29577=CARTESIAN_POINT ( 'NONE',  ( 93.94581488726784357, -60.00000000000240874, -15.82352347238299650 ) ) ;
#29581=CARTESIAN_POINT ( 'NONE',  ( -104.0151861009774166, -30.00000000000006750, 120.6691871043967126 ) ) ;
#29582=CARTESIAN_POINT ( 'NONE',  ( 10.44722405557104494, -56.87790227778863539, 33.38355414254041165 ) ) ;
#29585=CARTESIAN_POINT ( 'NONE',  ( -48.11708999912524121, -29.14444454005715102, 44.62783549548100837 ) ) ;
#29595=CARTESIAN_POINT ( 'NONE',  ( 46.12602165870173820, -38.31898768030290370, 59.97271842373840656 ) ) ;
#29599=CARTESIAN_POINT ( 'NONE',  ( 95.99411590063971289, -30.00000000000000000, 191.2869372966427193 ) ) ;
#29604=ORIENTED_EDGE ( 'NONE', *, *, #9174, .F. ) ;
#29605=CARTESIAN_POINT ( 'NONE',  ( 54.56792591830877370, -22.15785971680534416, 52.62277654788229597 ) ) ;
#29609=ORIENTED_EDGE ( 'NONE', *, *, #54901, .T. ) ;
#29613=CARTESIAN_POINT ( 'NONE',  ( 88.56294407034239669, -38.54372130031631372, 200.1479997606907659 ) ) ;
#29615=CARTESIAN_POINT ( 'NONE',  ( 86.55999845485922606, -60.13929112694511048, 1.461019888335082673 ) ) ;
#29624=ORIENTED_EDGE ( 'NONE', *, *, #79527, .T. ) ;
#29634=CARTESIAN_POINT ( 'NONE',  ( 45.71963875501243280, -29.99999999999999645, 56.30994126864628413 ) ) ;
#29640=CARTESIAN_POINT ( 'NONE',  ( 83.65579274812736799, -50.12940242402542879, 185.8577423453587585 ) ) ;
#29644=CARTESIAN_POINT ( 'NONE',  ( 93.83764888837048090, -57.67474972874411066, 11.09789775104367848 ) ) ;
#29653=CARTESIAN_POINT ( 'NONE',  ( 13.00603131147514802, -21.61757453066702439, 35.67497680198176369 ) ) ;
#29655=CARTESIAN_POINT ( 'NONE',  ( 45.19148592063464065, -28.36164282789344071, 40.27822637177104070 ) ) ;
#29664=CARTESIAN_POINT ( 'NONE',  ( -83.70148025459225494, -38.00000000000000000, 34.15054458896100442 ) ) ;
#29671=CARTESIAN_POINT ( 'NONE',  ( -7.761546958154228903, -21.77037872703017385, -30.37584562454359727 ) ) ;
#29679=CARTESIAN_POINT ( 'NONE',  ( -92.74820878259032497, -59.99999999999999289, -6.808916855407564306 ) ) ;
#29686=CARTESIAN_POINT ( 'NONE',  ( -85.55402800175718880, -18.57074191616040792, 160.4554053421518915 ) ) ;
#29688=CARTESIAN_POINT ( 'NONE',  ( -10.38441970549191495, 0.000000000000000000, 13.52487676487815271 ) ) ;
#29700=CARTESIAN_POINT ( 'NONE',  ( -110.1907765348834403, -57.67120634471875462, 130.2639824976604643 ) ) ;
#29705=CARTESIAN_POINT ( 'NONE',  ( 81.17508142137076277, -14.21045842199431952, -20.85096179708197184 ) ) ;
#29707=CARTESIAN_POINT ( 'NONE',  ( -76.24265395543058332, -14.21045842199434794, 145.5858823757693301 ) ) ;
#29708=CARTESIAN_POINT ( 'NONE',  ( -54.95499996707611245, -46.44145850250006191, 63.02118750885743736 ) ) ;
#29712=CARTESIAN_POINT ( 'NONE',  ( -99.36458642854884715, -37.79545065244527535, 191.5056538517512195 ) ) ;
#29721=CARTESIAN_POINT ( 'NONE',  ( 72.17674141521742115, -29.99999999999999645, 102.2643789533765784 ) ) ;
#29727=CARTESIAN_POINT ( 'NONE',  ( -28.40130354532971779, -36.00929858293697805, 32.00103210455104374 ) ) ;
#29731=CARTESIAN_POINT ( 'NONE',  ( 47.70061809322042023, -39.52289543229544933, 47.20263342004708562 ) ) ;
#29735=CARTESIAN_POINT ( 'NONE',  ( -110.5701501222436605, -38.35612523280028796, 181.7181079214109047 ) ) ;
#29737=CARTESIAN_POINT ( 'NONE',  ( 90.64011768444591155, -38.34321871509011004, 9.780805722092965837 ) ) ;
#29746=CARTESIAN_POINT ( 'NONE',  ( 93.66759751282268098, -60.00000000000001421, 202.5255995218111877 ) ) ;
#29755=CARTESIAN_POINT ( 'NONE',  ( -110.9831532232078075, -38.35615782300705945, 171.0432724854665594 ) ) ;
#29764=CARTESIAN_POINT ( 'NONE',  ( 81.29766393407724934, -56.98409711725605575, 180.9609411103209879 ) ) ;
#29807=CARTESIAN_POINT ( 'NONE',  ( -98.84102348079841249, -59.99999999999999289, 202.1787051656507685 ) ) ;
#29813=CARTESIAN_POINT ( 'NONE',  ( -85.51529951615857783, -28.66441007062391932, 177.8911255557245283 ) ) ;
#29817=CARTESIAN_POINT ( 'NONE',  ( -82.42959359406624742, -37.82875958912266867, 13.21936520248347868 ) ) ;
#29823=CARTESIAN_POINT ( 'NONE',  ( 101.7112553140276390, -14.21045842199441367, 195.4619641463733615 ) ) ;
#29826=CARTESIAN_POINT ( 'NONE',  ( -105.9103127569300966, -29.99999999999996092, 132.9890815309780123 ) ) ;
#29827=CARTESIAN_POINT ( 'NONE',  ( -65.02951926827741147, -29.05579461752434511, 80.86596411567830955 ) ) ;
#29830=CARTESIAN_POINT ( 'NONE',  ( 50.47126045336576539, -59.99999999997075406, 79.55909678837365107 ) ) ;
#29841=CARTESIAN_POINT ( 'NONE',  ( -88.80181889419175434, -59.99999999999998579, -20.61832237384453492 ) ) ;
#29854=TOROIDAL_SURFACE ( 'NONE', #102187, 74.46152422706630603, 60.00000000000000000 ) ;
#29855=CARTESIAN_POINT ( 'NONE',  ( 34.21697539897928664, -53.36349323917029608, 37.55009111937090438 ) ) ;
#29856=CARTESIAN_POINT ( 'NONE',  ( 21.65942590380180022, -2.602085213965209853E-15, -5.820808985962528936 ) ) ;
#29862=DIRECTION ( 'NONE',  ( 0.000000000000000000, 0.000000000000000000, -1.000000000000000000 ) ) ;
#29869=CARTESIAN_POINT ( 'NONE',  ( 91.96602543791587436, -60.00000000000001421, 6.905806405724360886 ) ) ;
#29877=CARTESIAN_POINT ( 'NONE',  ( -81.70366676428112385, -30.00000000000000711, 144.0154804593513802 ) ) ;
#29888=CARTESIAN_POINT ( 'NONE',  ( 78.42944077827469584, -32.55433236142065567, 130.6023639830650325 ) ) ;
#29893=CARTESIAN_POINT ( 'NONE',  ( -99.73481241717010448, -57.62673548571369508, 203.9935789388791250 ) ) ;
#29901=CARTESIAN_POINT ( 'NONE',  ( -0.9091344387254992609, -12.57755568720529027, 32.18680658398173478 ) ) ;
#29910=PLANE ( 'NONE',  #49151 ) ;
#29914=CARTESIAN_POINT ( 'NONE',  ( 42.34475754208664000, -27.06717000920707861, -36.11866503128073447 ) ) ;
#29915=CARTESIAN_POINT ( 'NONE',  ( -81.04018713825384168, -30.00000000000000711, 140.2278789465622140 ) ) ;
#29918=ORIENTED_EDGE ( 'NONE', *, *, #75137, .T. ) ;
#29921=CARTESIAN_POINT ( 'NONE',  ( 96.61421562474644986, -57.62226520396125551, 204.4765988090299800 ) ) ;
#29922=CARTESIAN_POINT ( 'NONE',  ( 62.18148360307306888, -60.22838722633849073, -29.09035595218466952 ) ) ;
#29926=CARTESIAN_POINT ( 'NONE',  ( -60.69885249676274697, -60.00000000000000711, 102.8462125076963360 ) ) ;
#29931=CARTESIAN_POINT ( 'NONE',  ( -84.56126607524946337, -57.46072418158504291, 191.5362485997459885 ) ) ;
#29941=CARTESIAN_POINT ( 'NONE',  ( -82.62686422651856333, -45.26163198499813234, -15.10635754027111055 ) ) ;
#29948=CARTESIAN_POINT ( 'NONE',  ( -15.50035291838204721, -4.285714285714287364, -20.16952962162827845 ) ) ;
#29951=CARTESIAN_POINT ( 'NONE',  ( 80.19743504398171297, -30.00000000000002487, -24.77996380036185187 ) ) ;
#29952=CARTESIAN_POINT ( 'NONE',  ( -79.65043784881741828, -39.49985926501358335, 143.6092781588031642 ) ) ;
#29956=CARTESIAN_POINT ( 'NONE',  ( 95.97031388804177254, -57.62154756878710771, 204.5181911369658394 ) ) ;
#29973=STYLED_ITEM ( 'NONE', ( #92811 ), #61612 ) ;
#29977=CARTESIAN_POINT ( 'NONE',  ( -72.40149263128425616, -29.99999999999999289, 139.7559031367707405 ) ) ;
#29978=CARTESIAN_POINT ( 'NONE',  ( 26.84979521222222587, -42.95598080738816549, 32.78234588387326198 ) ) ;
#29991=CARTESIAN_POINT ( 'NONE',  ( 87.60795424214978766, -30.00000000000000000, 185.8138595367513233 ) ) ;
#29994=CARTESIAN_POINT ( 'NONE',  ( 4.154708322984369194E-08, -57.67120202538961138, 41.61186700422869933 ) ) ;
#29995=CARTESIAN_POINT ( 'NONE',  ( 77.19385768473838993, -30.00000000000000355, -16.50491056378216115 ) ) ;
#30000=VERTEX_POINT ( 'NONE', #17502 ) ;
#30013=CARTESIAN_POINT ( 'NONE',  ( 60.37731204512586913, -38.34250980313896662, 97.59513848696614957 ) ) ;
#30017=CARTESIAN_POINT ( 'NONE',  ( 65.00163223881457952, -18.62600959983467774, 75.47887303634519185 ) ) ;
#30020=CARTESIAN_POINT ( 'NONE',  ( -55.88663790324028469, -36.71134587742232469, -35.08381123762609377 ) ) ;
#30028=CARTESIAN_POINT ( 'NONE',  ( -2.857580275982106954, -59.99999999999997868, -36.86911833281171624 ) ) ;
#30032=CARTESIAN_POINT ( 'NONE',  ( 86.88686737857604214, -39.10008494188175376, 188.8693110577609957 ) ) ;
#30033=CARTESIAN_POINT ( 'NONE',  ( 89.99999999999997158, -60.00000000000000000, 196.0238439516549818 ) ) ;
#30036=CARTESIAN_POINT ( 'NONE',  ( 24.87981348507249990, -20.00187728542004706, -33.03831867686129442 ) ) ;
#30041=CARTESIAN_POINT ( 'NONE',  ( -100.3779187766488405, -30.00000000000000355, 157.7784893630589522 ) ) ;
#30045=CARTESIAN_POINT ( 'NONE',  ( 40.77881392998116183, -57.69042326476748883, 56.97214866716775106 ) ) ;
#30062=CARTESIAN_POINT ( 'NONE',  ( -13.56997494041515218, -46.43935299279289808, 31.71586160483574091 ) ) ;
#30064=CARTESIAN_POINT ( 'NONE',  ( -87.36849624350148247, -59.99999999999996447, 33.81939915725044443 ) ) ;
#30071=CARTESIAN_POINT ( 'NONE',  ( 73.84586213920505315, -60.00000000000001421, 170.6559303522170694 ) ) ;
#30075=CARTESIAN_POINT ( 'NONE',  ( 38.21924934408536245, -34.43263479671050220, 36.26631857391012659 ) ) ;
#30091=CARTESIAN_POINT ( 'NONE',  ( -87.01069910675980168, -60.00000000000727596, 203.6540258465300894 ) ) ;
#30093=CARTESIAN_POINT ( 'NONE',  ( 90.24307525190243950, -60.00000000000001421, 202.0291797872075676 ) ) ;
#30096=CARTESIAN_POINT ( 'NONE',  ( -108.2372990039095271, -60.00000000000000000, 115.4700740038245499 ) ) ;
#30097=CARTESIAN_POINT ( 'NONE',  ( 9.217361846978604945, -39.47265868016614121, 30.47086924679750908 ) ) ;
#30098=CARTESIAN_POINT ( 'NONE',  ( -49.54250463381430336, -25.66846576903583355, 45.52667409298107515 ) ) ;
#30107=CARTESIAN_POINT ( 'NONE',  ( 82.01977462800290652, -29.99999999997359623, 194.2710566929856952 ) ) ;
#30110=CARTESIAN_POINT ( 'NONE',  ( 97.07539879229518931, -30.00000000000000000, 191.0633822395669768 ) ) ;
#30117=DIRECTION ( 'NONE',  ( -0.000000000000000000, -1.000000000000000000, -0.000000000000000000 ) ) ;
#30126=CARTESIAN_POINT ( 'NONE',  ( 102.8743298759455911, -38.42936654585968625, 199.1928420204874044 ) ) ;
#30129=CARTESIAN_POINT ( 'NONE',  ( 86.27400346893527683, -60.13093677512101465, 5.975714098585993561 ) ) ;
#30136=VECTOR ( 'NONE', #8526, 1000.000000000000000 ) ;
#30150=CARTESIAN_POINT ( 'NONE',  ( -44.47534256803319153, -38.31161230092084224, 57.00189278798913506 ) ) ;
#30153=CARTESIAN_POINT ( 'NONE',  ( 85.23043926280386984, -39.32506677273280360, 184.5449207610389237 ) ) ;
#30157=CARTESIAN_POINT ( 'NONE',  ( 94.16631605059897936, -57.67261574475512731, 22.14266882980151507 ) ) ;
#30165=CARTESIAN_POINT ( 'NONE',  ( 43.34668154757743963, -27.69613747131105796, 38.46247136646560705 ) ) ;
#30172=CARTESIAN_POINT ( 'NONE',  ( -82.66276222626812853, -38.00000000000004974, 21.06924847054219541 ) ) ;
#30178=CARTESIAN_POINT ( 'NONE',  ( -38.30773932209359600, -47.40885879408931913, -31.93446002179309318 ) ) ;
#30188=CARTESIAN_POINT ( 'NONE',  ( -91.92679597868495023, -60.00000000000000711, -14.22741696697412017 ) ) ;
#30198=CARTESIAN_POINT ( 'NONE',  ( -83.21178524358640516, -29.08282875446304772, 155.6723645619419472 ) ) ;
#30201=CARTESIAN_POINT ( 'NONE',  ( -14.76969908562827349, 0.000000000000000000, 8.521411446768476949 ) ) ;
#30212=CARTESIAN_POINT ( 'NONE',  ( -92.76516906498835624, -57.61752273625296539, 204.4213914816233739 ) ) ;
#30217=CARTESIAN_POINT ( 'NONE',  ( 86.89874827037927218, -29.99999999999997868, -18.81865104787653920 ) ) ;
#30218=CARTESIAN_POINT ( 'NONE',  ( -72.31573431813527009, -14.21045842199431064, 125.5062215401438266 ) ) ;
#30219=CARTESIAN_POINT ( 'NONE',  ( -54.21185734353947083, -53.38106178705758964, 64.18017538421840129 ) ) ;
#30223=CARTESIAN_POINT ( 'NONE',  ( -102.8276541885064717, -60.17762386373496497, 193.1075909480691166 ) ) ;
#30227=CARTESIAN_POINT ( 'NONE',  ( 90.71044788504735834, -38.34175721622889910, 7.076824436591243384 ) ) ;
#30233=CARTESIAN_POINT ( 'NONE',  ( 53.08934989192464826, -30.00000000000000000, 52.21148837440648549 ) ) ;
#30238=CARTESIAN_POINT ( 'NONE',  ( -29.49181701981505910, -46.43697584440771919, 34.18020204610339619 ) ) ;
#30242=CARTESIAN_POINT ( 'NONE',  ( 48.55458696805421681, -49.90003314422357050, 51.74501749119150418 ) ) ;
#30247=CARTESIAN_POINT ( 'NONE',  ( -110.5250911598958226, -38.35611436153418197, 182.1522587334059722 ) ) ;
#30249=CARTESIAN_POINT ( 'NONE',  ( 91.32589455155351743, -38.36701310358807149, -2.641594532008445739 ) ) ;
#30259=CARTESIAN_POINT ( 'NONE',  ( 83.15400578599735582, -59.99999999999999289, 198.9384841273030986 ) ) ;
#30264=CARTESIAN_POINT ( 'NONE',  ( 57.26729019237954788, -25.61006374783701034, 59.45692232418873147 ) ) ;
#30270=CARTESIAN_POINT ( 'NONE',  ( -96.39762838794068500, -38.48434118611966426, 201.1825086705471506 ) ) ;
#30283=CARTESIAN_POINT ( 'NONE',  ( 85.06960557373632525, -25.47056552230032977, 167.4782931879399257 ) ) ;
#30295=CARTESIAN_POINT ( 'NONE',  ( -81.12865512346820651, -30.00000000000000355, 1.958835504223271018 ) ) ;
#30320=CARTESIAN_POINT ( 'NONE',  ( -112.1996801038472995, -59.99999999999999289, 170.0554107543789257 ) ) ;
#30326=CARTESIAN_POINT ( 'NONE',  ( -81.79652205476276094, -60.68003446516232913, 187.1438624714922980 ) ) ;
#30334=CARTESIAN_POINT ( 'NONE',  ( -83.25482506818879358, -37.82319541480158875, 29.52994787646102637 ) ) ;
#30340=CARTESIAN_POINT ( 'NONE',  ( 105.6362521817138713, -29.99999999999994671, 194.5266552104434368 ) ) ;
#30341=CARTESIAN_POINT ( 'NONE',  ( -107.5810679786090702, -30.00000000000002487, 145.3413084537935163 ) ) ;
#30342=CARTESIAN_POINT ( 'NONE',  ( -65.80800410575133697, -22.10322226003651380, 79.50655047398903719 ) ) ;
#30346=CARTESIAN_POINT ( 'NONE',  ( 94.38326820372073200, -59.99999999999746336, 204.9998441075219091 ) ) ;
#30359=CARTESIAN_POINT ( 'NONE',  ( -83.77391689997462265, -59.99999999999995737, -25.46673677812911407 ) ) ;
#30371=CARTESIAN_POINT ( 'NONE',  ( 103.9907751973010335, -59.99999999999997868, 190.8231350958398878 ) ) ;
#30375=CARTESIAN_POINT ( 'NONE',  ( 36.78615735600832437, -36.04596638446182766, 35.70108577633924085 ) ) ;
#30376=CARTESIAN_POINT ( 'NONE',  ( -2.227375807149027054, -1.734723475976807094E-15, 17.01589776168603407 ) ) ;
#30390=ADVANCED_FACE ( 'NONE', ( #21124 ), #78764, .T. ) ;
#30392=CARTESIAN_POINT ( 'NONE',  ( 97.99660889140263009, -60.00000000000000711, 68.90520065234117908 ) ) ;
#30399=CARTESIAN_POINT ( 'NONE',  ( -88.86068578946498064, -29.99999999999961275, -15.16702001146615864 ) ) ;
#30412=CARTESIAN_POINT ( 'NONE',  ( 78.97029474429139384, -42.96455894964061883, 142.9603876401418461 ) ) ;
#30432=CARTESIAN_POINT ( 'NONE',  ( -13.42771739161924494, -14.69885084449941104, 31.71672228287745909 ) ) ;
#30444=DIRECTION ( 'NONE',  ( -3.673940397442057649E-17, 0.000000000000000000, -1.000000000000000000 ) ) ;
#30446=CARTESIAN_POINT ( 'NONE',  ( -69.22537020059996848, -29.97316140627671288, -21.14164747078667972 ) ) ;
#30447=CARTESIAN_POINT ( 'NONE',  ( -63.07201610543538806, -29.99999999999999645, 74.88422784947999844 ) ) ;
#30451=CARTESIAN_POINT ( 'NONE',  ( 91.42196762672531918, -57.61411189307126790, 204.2437217276433046 ) ) ;
#30453=EDGE_CURVE ( 'NONE', #88504, #94858, #29221, .T. ) ;
#30458=CARTESIAN_POINT ( 'NONE',  ( -75.41463958967447923, -60.00000000000000711, 183.9905783904083592 ) ) ;
#30464=CARTESIAN_POINT ( 'NONE',  ( -85.99570664262481046, -35.58902874923357018, 185.3986280066468453 ) ) ;
#30475=PRESENTATION_STYLE_ASSIGNMENT (( #54171 ) ) ;
#30477=CARTESIAN_POINT ( 'NONE',  ( 68.53628924694606894, -14.21045842199431597, -27.48009014525527860 ) ) ;
#30478=CARTESIAN_POINT ( 'NONE',  ( -80.34670115289323178, -36.03127197182796237, 144.2402978679412229 ) ) ;
#30481=CARTESIAN_POINT ( 'NONE',  ( 16.61664997849939240, -30.00000000000006395, 37.21280938527437598 ) ) ;
#30483=CARTESIAN_POINT ( 'NONE',  ( 72.11178192614376314, -57.67306540792444025, 173.1801346106868493 ) ) ;
#30490=CARTESIAN_POINT ( 'NONE',  ( -2.499999999999996447, -30.00000000000000000, -13.00000000000000000 ) ) ;
#30491=CARTESIAN_POINT ( 'NONE',  ( -102.9402037365450866, -45.26537910807851972, 153.9863529572914445 ) ) ;
#30505=CARTESIAN_POINT ( 'NONE',  ( 24.39961550212768415, -25.56170002018362553, 29.25281948027246059 ) ) ;
#30521=CARTESIAN_POINT ( 'NONE',  ( 5.802656403430185961, -59.99999999999999289, -42.56106326075611435 ) ) ;
#30532=VERTEX_POINT ( 'NONE', #49583 ) ;
#30542=CARTESIAN_POINT ( 'NONE',  ( 60.38390319005696227, -38.34250386216492501, 97.61615657541973690 ) ) ;
#30545=CARTESIAN_POINT ( 'NONE',  ( -80.33450311392522281, -60.00000000000002842, 177.7302725502722751 ) ) ;
#30546=CARTESIAN_POINT ( 'NONE',  ( 62.70097925198960098, -49.91075561683145168, 84.84605103675988858 ) ) ;
#30550=CARTESIAN_POINT ( 'NONE',  ( -59.38248720328446240, -37.25844438171453987, -34.32352965270520428 ) ) ;
#30552=CARTESIAN_POINT ( 'NONE',  ( -61.29065067449151627, -57.67115771167040350, -37.35479649122906665 ) ) ;
#30553=ORIENTED_EDGE ( 'NONE', *, *, #38243, .T. ) ;
#30560=CARTESIAN_POINT ( 'NONE',  ( 86.48923150265004267, -50.13329297819660013, 191.3735317416930286 ) ) ;
#30571=CARTESIAN_POINT ( 'NONE',  ( 36.75192448471445061, -60.00000000000000000, 48.11202499009017686 ) ) ;
#30572=CARTESIAN_POINT ( 'NONE',  ( -100.4436717631274405, -30.00000000000001066, 183.3501104447698253 ) ) ;
#30573=EDGE_CURVE ( 'NONE', #98077, #85478, #32372, .T. ) ;
#30577=CARTESIAN_POINT ( 'NONE',  ( 40.69853667173202894, -57.69061545352386133, 56.83570513438750993 ) ) ;
#30584=CARTESIAN_POINT ( 'NONE',  ( -13.47129954280381625, -60.00000000000000711, 39.72841581181796045 ) ) ;
#30589=CARTESIAN_POINT ( 'NONE',  ( -87.01710432979982102, -57.37281113167114199, 193.9090236191709380 ) ) ;
#30594=CARTESIAN_POINT ( 'NONE',  ( -14.77380270916763116, -53.40237792673437411, 32.92252495082122010 ) ) ;
#30596=CARTESIAN_POINT ( 'NONE',  ( -94.52029764136869971, -60.00000000000002132, 83.13177969407045964 ) ) ;
#30603=CARTESIAN_POINT ( 'NONE',  ( 72.13637180897663370, -60.00000000000000711, 155.3038211014013257 ) ) ;
#30609=CARTESIAN_POINT ( 'NONE',  ( 20.75554216095374116, -29.99999999999998579, 37.60191050100322485 ) ) ;
#30616=CIRCLE ( 'NONE', #49517, 8.000000000000000000 ) ;
#30624=CARTESIAN_POINT ( 'NONE',  ( -114.3478711580139304, -60.00000000001953282, 163.9674887148623839 ) ) ;
#30626=CARTESIAN_POINT ( 'NONE',  ( 73.65925679185706088, -60.00000000000001421, 168.7609027532264179 ) ) ;
#30629=CARTESIAN_POINT ( 'NONE',  ( -97.22630358410161477, -59.99999999999998579, 47.92073696641181613 ) ) ;
#30630=CARTESIAN_POINT ( 'NONE',  ( 12.30984511850486740, -32.51068972755530950, 29.36027658876032120 ) ) ;
#30631=CARTESIAN_POINT ( 'NONE',  ( 99.27397055116384195, -38.00000000000000711, 191.6755426901316071 ) ) ;
#30634=CARTESIAN_POINT ( 'NONE',  ( -45.70114157808188082, -60.26445691949498951, 50.30722036196431901 ) ) ;
#30646=CARTESIAN_POINT ( 'NONE',  ( 80.13328830561965788, -29.99999999999337064, 190.7101562830954720 ) ) ;
#30651=CARTESIAN_POINT ( 'NONE',  ( 97.38464793213240966, -29.99999999999999645, 190.9410892311414614 ) ) ;
#30660=AXIS2_PLACEMENT_3D ( 'NONE', #8686, #41590, #551 ) ;
#30667=CARTESIAN_POINT ( 'NONE',  ( 101.8625646185573856, -38.44601613749367885, 199.7504753397604986 ) ) ;
#30669=CARTESIAN_POINT ( 'NONE',  ( 82.77473000103051959, -37.85543405128064620, 2.355868850680865823 ) ) ;
#30691=CARTESIAN_POINT ( 'NONE',  ( 34.45567488635992248, -26.24090404973739865, 41.62864160396504332 ) ) ;
#30695=CARTESIAN_POINT ( 'NONE',  ( 84.38907022229382449, -53.80946252041021438, 189.6612499249015400 ) ) ;
#30700=CARTESIAN_POINT ( 'NONE',  ( 94.16204370421009173, -57.67429201036151909, 3.106671879859604246 ) ) ;
#30708=CARTESIAN_POINT ( 'NONE',  ( 21.21144082669073327, -26.49527374954287495, 37.12913197614864202 ) ) ;
#30720=CARTESIAN_POINT ( 'NONE',  ( -102.6007910818582616, -38.00000000000002132, 179.5952160768334238 ) ) ;
#30724=CARTESIAN_POINT ( 'NONE',  ( -10.76224560403525032, -16.36478912462312252, -34.75025230997614756 ) ) ;
#30727=CARTESIAN_POINT ( 'NONE',  ( -46.51767665254412520, -21.77006129918473576, -26.23258419899174498 ) ) ;
#30728=ORIENTED_EDGE ( 'NONE', *, *, #38286, .T. ) ;
#30737=CARTESIAN_POINT ( 'NONE',  ( -92.38965560796522425, -59.99999999999999289, 0.2914275940444852053 ) ) ;
#30742=CARTESIAN_POINT ( 'NONE',  ( 98.26932492730686874, -37.76192426467496688, 192.3739912550726956 ) ) ;
#30744=CARTESIAN_POINT ( 'NONE',  ( -80.76959687771581287, -53.40869547565652198, 171.1175977112955877 ) ) ;
#30755=CARTESIAN_POINT ( 'NONE',  ( -75.26480569136067800, -57.56533996972894585, 191.5310976926263322 ) ) ;
#30760=CARTESIAN_POINT ( 'NONE',  ( 87.60230161701383622, -14.21045842199431064, -3.802929300262678947 ) ) ;
#30761=CARTESIAN_POINT ( 'NONE',  ( -76.85442806461188070, -14.21045842199432663, 149.6320961301125578 ) ) ;
#30762=CARTESIAN_POINT ( 'NONE',  ( -53.00585131428307761, -49.90973205979414473, 60.14564158691946716 ) ) ;
#30766=CARTESIAN_POINT ( 'NONE',  ( -99.87378953022019346, -37.81191256832239134, 190.7979464389039208 ) ) ;
#30770=ORIENTED_EDGE ( 'NONE', *, *, #100975, .F. ) ;
#30772=CARTESIAN_POINT ( 'NONE',  ( 109.6487595463947287, -38.35581244533405254, 151.0088976801097260 ) ) ;
#30777=B_SPLINE_SURFACE_WITH_KNOTS ( 'NONE', 3, 3, ( 
 ( #80569, #6688, #103797, #80041 ),
 ( #95718, #40126, #29941, #22389 ),
 ( #15315, #73003, #55749, #55233 ),
 ( #21856, #89216, #54696, #32058 ),
 ( #6153, #13181, #87629, #39615 ),
 ( #13715, #5634, #46624, #95195 ),
 ( #72488, #105395, #79521, #64421 ),
 ( #48203, #38558, #7217, #97290 ),
 ( #54165, #87107, #14241, #104322 ),
 ( #23444, #81104, #39086, #21328 ),
 ( #46110, #38047, #78992, #5115 ),
 ( #16373, #81618, #99397, #90810 ),
 ( #15846, #99947, #75668, #65468 ),
 ( #58438, #1223, #82708, #17461 ),
 ( #67066, #8279, #74601, #58977 ),
 ( #8812, #25580, #82165, #91864 ),
 ( #16926, #49802, #73535, #50327 ),
 ( #17990, #40653, #49262, #98359 ),
 ( #33123, #50850, #106437, #91349 ),
 ( #1769, #83234, #41189, #65992 ),
 ( #57885, #7743, #83756, #42776 ),
 ( #34190, #74071, #156, #682 ),
 ( #41717, #9328, #33644, #66525 ),
 ( #26120, #9865, #32596, #64935 ),
 ( #98869, #25029, #42237, #75126 ),
 ( #97823, #24513, #23985, #56828 ),
 ( #89749, #57350, #48727, #90272 ),
 ( #12519, #53531, #61103, #60058 ),
 ( #61651, #44382, #94541, #85369 ),
 ( #100477, #2299, #43839, #84303 ),
 ( #27707, #60581, #28772, #10398 ),
 ( #102614, #2841, #20692, #43314 ),
 ( #76728, #45452, #69200, #51920 ),
 ( #36854, #93471, #76197, #86459 ),
 ( #11456, #28231, #52454, #84836 ),
 ( #35248, #78327, #102071, #35793 ),
 ( #51389, #19082, #34726, #77277 ),
 ( #3387, #67599, #10919, #68113 ),
 ( #36331, #26638, #93991, #20151 ),
 ( #77809, #53002, #85923, #59508 ),
 ( #92382, #11994, #68671, #101011 ),
 ( #101551, #19621, #44926, #3922 ),
 ( #18528, #27168, #69722, #92916 ),
 ( #87501, #79914, #37913, #22781 ),
 ( #80441, #104190, #88029, #38947 ),
 ( #6023, #78855, #96646, #29817 ),
 ( #96118, #47014, #70247, #103149 ),
 ( #54033, #22251, #71824, #55099 ),
 ( #62695, #38433, #45977, #21203 ),
 ( #62182, #79390, #14108, #95068 ),
 ( #104726, #70776, #95587, #30879 ),
 ( #13047, #21723, #63757, #55618 ),
 ( #88555, #14635, #47543, #6549 ),
 ( #63227, #39484, #4443, #30334 ),
 ( #29296, #37387, #86977, #4985 ),
 ( #5508, #54565, #13582, #103670 ),
 ( #46497, #71298, #35609, #78670 ),
 ( #52816, #18899, #101375, #53354 ),
 ( #94892, #21036, #53871, #3750 ),
 ( #61464, #86274, #28055, #60928 ),
 ( #10745, #3211, #85187, #19444 ),
 ( #59869, #19970, #2660, #102435 ),
 ( #28577, #93814, #11272, #85742 ),
 ( #43660, #11813, #76548, #44744 ),
 ( #68485, #94357, #78152, #52274 ),
 ( #12348, #12875, #44206, #45274 ),
 ( #102969, #77630, #27528, #77092 ),
 ( #60405, #36151, #36681, #86802 ),
 ( #45791, #69545, #62003, #92743 ),
 ( #69021, #93285, #20520, #4272 ),
 ( #4803, #101895, #37200, #70067 ),
 ( #37742, #29133, #100823, #26990 ),
 ( #51743, #84661, #58318, #98759 ),
 ( #79545, #104342, #17351, #25466 ),
 ( #104898, #71987, #24913, #105418 ),
 ( #74491, #57767, #80595, #55256 ),
 ( #91244, #63392, #75015, #50225 ),
 ( #22935, #90695, #66406, #82596 ),
 ( #66957, #96287, #39642, #5657 ),
 ( #41608, #14266, #47167, #31037 ),
 ( #99836, #64441, #49689, #99290 ),
 ( #14801, #55773, #30491, #96804 ),
 ( #6175, #13738, #88708, #566 ),
 ( #16803, #9221, #8700, #26008 ),
 ( #34085, #83126, #47695, #39108 ),
 ( #6716, #33534, #22412, #42129 ),
 ( #63917, #72512, #1110, #87656 ),
 ( #46645, #31558, #38579, #71444 ),
 ( #88181, #80068, #18419, #84196 ),
 ( #85812, #68558, #11888, #2731 ),
 ( #17880, #26531, #68009, #1661 ),
 ( #27597, #27061, #77167, #20042 ),
 ( #67488, #58871, #59945, #52890 ),
 ( #18969, #93883, #100893, #101962 ),
 ( #28122, #101444, #10292, #50734 ),
 ( #44816, #60997, #77703, #76089 ),
 ( #60479, #76619, #10811, #44274 ),
 ( #51813, #59404, #3814, #36752 ),
 ( #69614, #102508, #92810, #84726 ),
 ( #93358, #91761, #35684, #19510 ),
 ( #83644, #52344, #85257, #9751 ),
 ( #42666, #75565, #34619, #11340 ),
 ( #43729, #3281, #69090, #36221 ),
 ( #2189, #100367, #92265, #51275 ),
 ( #43204, #35139, #96011, #78223 ),
 ( #5912, #86868, #78739, #46908 ),
 ( #4873, #79811, #54446, #30766 ),
 ( #70138, #12942, #70670, #94963 ),
 ( #95469, #55511, #38326, #88451 ),
 ( #96542, #94429, #103043, #37809 ),
 ( #30223, #21616, #87399, #22673 ),
 ( #38840, #37272, #28651, #29712 ),
 ( #22136, #103562, #39375, #63109 ),
 ( #62586, #29200, #63653, #4338 ),
 ( #6439, #5405, #54988, #46393 ),
 ( #87918, #62075, #14525, #13999 ),
 ( #71703, #45344, #45863, #47435 ),
 ( #104617, #71188, #80325, #13471 ),
 ( #72253, #61537, #20589, #79283 ),
 ( #53429, #86347, #104082, #12413 ),
 ( #21100, #53935, #49018, #15601 ),
 ( #40948, #32353, #40411, #8572 ),
 ( #24787, #9097, #97053, #98638 ),
 ( #57640, #65224, #16670, #23735 ),
 ( #25326, #99168, #8035, #90562 ),
 ( #49564, #98117, #24266, #73293 ),
 ( #17223, #73839, #82471, #64183 ),
 ( #57114, #6976, #106733, #41475 ),
 ( #47957, #32882, #90028, #16134 ),
 ( #80864, #89507, #31810, #66281 ),
 ( #58188, #39893, #74362, #106189 ),
 ( #440, #33411, #91114, #65757 ),
 ( #23196, #15072, #50097, #83002 ),
 ( #48491, #81386, #42005, #81917 ),
 ( #105155, #31297, #56039, #72767 ),
 ( #88972, #105673, #64697, #97568 ),
 ( #56584, #7496, #52218, #68426 ),
 ( #50606, #59807, #92146, #75436 ),
 ( #83522, #43081, #18842, #101839 ) ),
 .UNSPECIFIED., .F., .F., .F.,
 ( 4, 3, 3, 3, 3, 3, 3, 3, 3, 3, 3, 3, 3, 3, 3, 3, 3, 3, 3, 3, 3, 3, 3, 3, 3, 3, 3, 3, 3, 3, 3, 3, 3, 3, 3, 3, 3, 3, 3, 3, 3, 3, 3, 3, 3, 3, 4 ),
 ( 4, 4 ),
 ( 0.5869767053942211987, 0.5886709324131782495, 0.5895180459226567748, 0.5903651594321354112, 0.5937536134700496238, 0.5971420675079637252, 0.5988362945269207760, 0.6005305215458779378, 0.6022247485648350995, 0.6039189755837921503, 0.6073074296217062518, 0.6090016566406633025, 0.6106958836596204643, 0.6123901106785776260, 0.6140843376975346768, 0.6174727917354488893, 0.6208612457733631018, 0.6276381538491915268, 0.6344150619250199519, 0.6411919700008482659, 0.6547457861525050049, 0.6682996023041618550, 0.6954072346074753330, 0.7089610507591320721, 0.7225148669107888111, 0.7360686830624455501, 0.7428455911382738641, 0.7496224992141022891, 0.7563994072899307142, 0.7631763153657590282, 0.7699532234415873422, 0.7767301315174157672, 0.7801185855553299797, 0.7835070395932441922, 0.7868954936311584047, 0.7885897206501155665, 0.7902839476690726173, 0.7911310611785511426, 0.7919781746880296680, 0.7928252881975081934, 0.7936724017069868298, 0.7945195152164654662, 0.7953666287259439915, 0.7970608557449010423, 0.8004493097828151438, 0.8021435368017721945, 0.8038377638207293563 ),
 ( 0.03867574233413020868, 0.7831529818502380724 ),
 .UNSPECIFIED. ) ;
#30778=CARTESIAN_POINT ( 'NONE',  ( 89.99999999999997158, -52.00000000000000000, 196.0238439516549818 ) ) ;
#30787=CARTESIAN_POINT ( 'NONE',  ( 49.64451713816125533, -18.74260289896121634, 43.46749392098310949 ) ) ;
#30791=CARTESIAN_POINT ( 'NONE',  ( -103.7057709786833897, -38.41803280166803347, 198.6430474523727980 ) ) ;
#30793=CARTESIAN_POINT ( 'NONE',  ( 90.80408946376662982, -38.34284569562218792, 5.322705216289786989 ) ) ;
#30796=CARTESIAN_POINT ( 'NONE',  ( 100.0064967486124772, -37.84851846554567345, 139.8641161912917426 ) ) ;
#30803=CARTESIAN_POINT ( 'NONE',  ( 87.43192352441741377, -60.00000000000000711, 201.1725596287192275 ) ) ;
#30807=CARTESIAN_POINT ( 'NONE',  ( 57.09735546842818366, -29.08113214485917197, 60.54316683975517321 ) ) ;
#30812=ORIENTED_EDGE ( 'NONE', *, *, #18177, .F. ) ;
#30813=CARTESIAN_POINT ( 'NONE',  ( -101.1906192923223102, -38.45514854918585712, 200.0682938694438064 ) ) ;
#30825=CARTESIAN_POINT ( 'NONE',  ( 81.01602980331753656, -60.51226052367474040, 183.3185133159588531 ) ) ;
#30867=CARTESIAN_POINT ( 'NONE',  ( -112.1945380839098192, -60.00000000000000000, 169.8055786374723084 ) ) ;
#30872=CARTESIAN_POINT ( 'NONE',  ( -82.62937363827076354, -50.03007458202083058, 181.3268356314227390 ) ) ;
#30879=CARTESIAN_POINT ( 'NONE',  ( -82.71436517315559911, -37.82479280323671844, 22.06480504041530466 ) ) ;
#30885=CARTESIAN_POINT ( 'NONE',  ( 79.57068731991196842, -14.21045842199434794, 190.0104166006057085 ) ) ;
#30886=CARTESIAN_POINT ( 'NONE',  ( -96.14371828217340976, -60.00000000000000711, 39.43406270914149303 ) ) ;
#30887=CARTESIAN_POINT ( 'NONE',  ( -66.03000109903794623, -39.48590419423089060, 89.23932064986095725 ) ) ;
#30890=CARTESIAN_POINT ( 'NONE',  ( 85.17823266485417832, -60.00000000000981970, 202.9514142658082960 ) ) ;
#30893=CARTESIAN_POINT ( 'NONE',  ( 5.511955672705553421E-05, -56.87793864768104157, 33.36930640088255728 ) ) ;
#30902=CARTESIAN_POINT ( 'NONE',  ( -100.2951002466030417, -60.00000000000001421, 201.7966096354651029 ) ) ;
#30911=CARTESIAN_POINT ( 'NONE',  ( 97.47675437802963927, -60.00000000000000000, 196.6138812136176739 ) ) ;
#30912=CARTESIAN_POINT ( 'NONE',  ( -37.92269680623696360, -36.05438877271811293, 36.40206401741252051 ) ) ;
#30916=CARTESIAN_POINT ( 'NONE',  ( 37.55314937966022626, -29.13011038508879125, 34.70950243149740544 ) ) ;
#30917=CARTESIAN_POINT ( 'NONE',  ( 19.43146043915153953, -2.602085213965209853E-15, -11.19959342722011364 ) ) ;
#30922=CARTESIAN_POINT ( 'NONE',  ( -73.79179841926161032, -38.32627029603643365, 158.6094216522652971 ) ) ;
#30934=CARTESIAN_POINT ( 'NONE',  ( 94.31231819446564657, -59.99999999999999289, 43.83016036555673622 ) ) ;
#30939=EDGE_CURVE ( 'NONE', #88504, #93532, #16893, .T. ) ;
#30940=CARTESIAN_POINT ( 'NONE',  ( -85.06054849208743462, -29.99999999999999289, 170.9067780956840181 ) ) ;
#30957=CARTESIAN_POINT ( 'NONE',  ( 83.08172053995880901, -25.61919862906970735, 150.1175688109731823 ) ) ;
#30964=CARTESIAN_POINT ( 'NONE',  ( -11.25203090971146302, -57.67122638729478723, 41.63652355756774881 ) ) ;
#30973=CARTESIAN_POINT ( 'NONE',  ( -19.29186002098929364, -16.81175181876205471, 31.48980669193186799 ) ) ;
#30985=CARTESIAN_POINT ( 'NONE',  ( -64.27136633399638299, -37.82663551496658982, -33.04686093788494361 ) ) ;
#30986=CARTESIAN_POINT ( 'NONE',  ( -62.59165975746622479, -30.00000000000000355, 73.59412878083956855 ) ) ;
#30990=ORIENTED_EDGE ( 'NONE', *, *, #74554, .F. ) ;
#30993=CARTESIAN_POINT ( 'NONE',  ( 108.7532849881359738, -57.66361498164450694, 198.0832724003855105 ) ) ;
#30994=CARTESIAN_POINT ( 'NONE',  ( 59.17992575935892319, -34.58953265655708975, -25.51721825149453693 ) ) ;
#30999=CARTESIAN_POINT ( 'NONE',  ( -74.80069672659014657, -59.99999999999999289, 179.7118729274451425 ) ) ;
#31003=CARTESIAN_POINT ( 'NONE',  ( -86.26451976794668042, -21.18125813129296020, 178.9885725162824599 ) ) ;
#31023=CARTESIAN_POINT ( 'NONE',  ( 93.17370000506844008, -59.99999999999994316, -17.95777172718301173 ) ) ;
#31024=CARTESIAN_POINT ( 'NONE',  ( -76.84998475036370280, -60.31673342858857012, 147.9117224744258579 ) ) ;
#31026=CARTESIAN_POINT ( 'NONE',  ( 35.94918560889485093, -14.21045842199434439, 40.02951443902858841 ) ) ;
#31028=CARTESIAN_POINT ( 'NONE',  ( 109.0603063891997095, -57.66547707161688407, 197.6446080142187895 ) ) ;
#31037=CARTESIAN_POINT ( 'NONE',  ( -101.1956550818799769, -37.82070586317561833, 149.2949577844976545 ) ) ;
#31049=CARTESIAN_POINT ( 'NONE',  ( 24.27759548268132406, -22.08292253087573798, 28.63655142963175493 ) ) ;
#31059=FACE_OUTER_BOUND ( 'NONE', #87700, .T. ) ;
#31066=CARTESIAN_POINT ( 'NONE',  ( 49.46860733447498149, -59.99999999999999289, -38.00840947334077669 ) ) ;
#31067=CARTESIAN_POINT ( 'NONE',  ( 87.31629069312508307, -29.99999999999992184, 184.8944350655740720 ) ) ;
#31092=CARTESIAN_POINT ( 'NONE',  ( 63.09060442939562563, -32.53182640883167664, 77.17087058294897872 ) ) ;
#31105=CARTESIAN_POINT ( 'NONE',  ( 86.80239051670210415, -28.05175165373529822, 186.1822811582222812 ) ) ;
#31114=CARTESIAN_POINT ( 'NONE',  ( 20.63737383274147419, -60.00000000000001421, 40.30261454582264236 ) ) ;
#31115=CARTESIAN_POINT ( 'NONE',  ( -99.81090197708762446, -30.00000000000000000, 186.3697714946532358 ) ) ;
#31118=CARTESIAN_POINT ( 'NONE',  ( 44.03287093842978805, -57.68433743212944620, 63.10718159453834630 ) ) ;
#31128=CARTESIAN_POINT ( 'NONE',  ( -21.11529628636797540, -60.00000000000000000, 40.37737908323012448 ) ) ;
#31132=CARTESIAN_POINT ( 'NONE',  ( -13.42288265799313685, -35.99464357137680537, 29.96928068455888905 ) ) ;
#31134=CARTESIAN_POINT ( 'NONE',  ( -86.20182090415494258, -60.00000000000003553, 6.671171230388342366 ) ) ;
#31143=CARTESIAN_POINT ( 'NONE',  ( 73.72526574475637062, -60.00000000000001421, 169.4364817653470539 ) ) ;
#31148=CARTESIAN_POINT ( 'NONE',  ( 4.277780656302746287, -59.99999999999995737, 41.98959578111988122 ) ) ;
#31162=CARTESIAN_POINT ( 'NONE',  ( -112.6191437711416796, -60.00000000000245848, 190.6377985708280676 ) ) ;
#31165=CARTESIAN_POINT ( 'NONE',  ( 48.53038198857916541, -59.99999999999997868, 68.24634254656791654 ) ) ;
#31169=CARTESIAN_POINT ( 'NONE',  ( -114.5724197576058714, -60.00000000000000000, 174.9505165961822684 ) ) ;
#31170=CARTESIAN_POINT ( 'NONE',  ( 12.13045461104100298, -18.58664849654226359, 27.03410863527348695 ) ) ;
#31171=CARTESIAN_POINT ( 'NONE',  ( 97.88801951303621252, -38.00000000000009237, 192.5957827294996321 ) ) ;
#31174=CARTESIAN_POINT ( 'NONE',  ( -44.14030560050159835, -49.89427143720936186, 45.35222468316599986 ) ) ;
#31180=CARTESIAN_POINT ( 'NONE',  ( 2.500000000000003109, -19.94872423595276700, -28.09930031681329154 ) ) ;
#31186=CARTESIAN_POINT ( 'NONE',  ( 104.6012708058323994, -30.00000000000270362, 195.8924596499454651 ) ) ;
#31190=CARTESIAN_POINT ( 'NONE',  ( 95.54465322637203428, -30.00000000000000355, 121.3526640118945892 ) ) ;
#31205=CARTESIAN_POINT ( 'NONE',  ( 78.22497488676229693, -38.60204001542046370, 188.9231901909346618 ) ) ;
#31207=CARTESIAN_POINT ( 'NONE',  ( 84.22446622427618479, -45.28768642902152664, -0.5874579490476177224 ) ) ;
#31208=CARTESIAN_POINT ( 'NONE',  ( 85.73618404534279591, -38.00000000000005684, 185.6577708967697617 ) ) ;
#31225=CARTESIAN_POINT ( 'NONE',  ( -89.99999999999997158, 500000.0000000000582, 188.5238439516623146 ) ) ;
#31230=CARTESIAN_POINT ( 'NONE',  ( 85.48340152300438888, -35.70049165519398571, 183.4273707390578920 ) ) ;
#31233=CARTESIAN_POINT ( 'NONE',  ( 93.86032054255686319, -57.67368490835236372, 14.83889430886123151 ) ) ;
#31241=CARTESIAN_POINT ( 'NONE',  ( -56.97597412751945711, -38.00000000000000711, 64.03091273156307750 ) ) ;
#31252=CARTESIAN_POINT ( 'NONE',  ( -82.86548094586187574, -38.00000000000001421, 1.363017090156070532 ) ) ;
#31260=CARTESIAN_POINT ( 'NONE',  ( -41.46718496839501000, -47.40889074441435724, -31.47343794193032451 ) ) ;
#31267=CARTESIAN_POINT ( 'NONE',  ( -92.03488671148051026, -60.00000000000000000, -13.80638005471863572 ) ) ;
#31271=CARTESIAN_POINT ( 'NONE',  ( 98.78140442897466755, -45.26732928611253470, 193.4374649867567086 ) ) ;
#31274=CARTESIAN_POINT ( 'NONE',  ( -81.96440918278869958, -42.97365977493816303, 165.6671748287174637 ) ) ;
#31285=CARTESIAN_POINT ( 'NONE',  ( -73.23646197434321437, -57.64251361348243563, 182.9240549372742635 ) ) ;
#31290=CARTESIAN_POINT ( 'NONE',  ( -63.50642133866089978, -59.99999999999999289, -37.13819210229684842 ) ) ;
#31291=CARTESIAN_POINT ( 'NONE',  ( -39.73689531673777964, -14.21045842199425735, 43.02931800076370195 ) ) ;
#31293=CARTESIAN_POINT ( 'NONE',  ( -52.74279523840890960, -29.10740770686958712, 51.85141972818043143 ) ) ;
#31297=CARTESIAN_POINT ( 'NONE',  ( -97.15103619198865204, -52.80984743541710458, 195.3003251582881319 ) ) ;
#31301=CARTESIAN_POINT ( 'NONE',  ( 90.70342993949924448, -38.35092529657300275, 17.86702295203266999 ) ) ;
#31303=DIRECTION ( 'NONE',  ( -0.000000000000000000, -1.000000000000000000, -0.000000000000000000 ) ) ;
#31310=CARTESIAN_POINT ( 'NONE',  ( 85.86921380053233577, -29.99999999999999645, 177.6924406031379817 ) ) ;
#31311=COLOUR_RGB ( '', 0.40784314, 0.44705882, 0.49803922) ;
#31320=CARTESIAN_POINT ( 'NONE',  ( 49.55649468912712763, -42.97651784452486368, 51.16379761201464049 ) ) ;
#31324=CARTESIAN_POINT ( 'NONE',  ( -108.8742740125438075, -38.35654636151372188, 190.5310075001649466 ) ) ;
#31326=CARTESIAN_POINT ( 'NONE',  ( 91.33800103527501335, -38.39896688930978996, -9.982889340764455000 ) ) ;
#31330=CARTESIAN_POINT ( 'NONE',  ( 102.9432490270377514, -45.28273091632402725, 153.9878045269907432 ) ) ;
#31335=CARTESIAN_POINT ( 'NONE',  ( 78.36952841773975820, -60.00000000000000000, 193.5507905296401532 ) ) ;
#31340=CARTESIAN_POINT ( 'NONE',  ( 55.06123850360377503, -53.37751811208404007, 66.16048837899118951 ) ) ;
#31347=CARTESIAN_POINT ( 'NONE',  ( -102.8054511067312973, -38.43301377309627753, 199.2360175344277309 ) ) ;
#31359=CARTESIAN_POINT ( 'NONE',  ( 82.41388130231072751, -50.00333596804200909, 179.9547445588053733 ) ) ;
#31398=CARTESIAN_POINT ( 'NONE',  ( -110.9407563509171553, -60.00000000000000000, 151.5418352708265957 ) ) ;
#31404=CARTESIAN_POINT ( 'NONE',  ( -82.48518652320663591, -50.01571124582150674, 180.4131216091861063 ) ) ;
#31416=CARTESIAN_POINT ( 'NONE',  ( 85.76531507393636389, -14.21045842199426801, 195.9085670305863118 ) ) ;
#31417=CARTESIAN_POINT ( 'NONE',  ( -101.4323841882945771, -14.21045842199443499, 121.1831906623697677 ) ) ;
#31420=CARTESIAN_POINT ( 'NONE',  ( -64.22233557390354974, -25.57930763091898640, 76.82107432232744770 ) ) ;
#31423=CARTESIAN_POINT ( 'NONE',  ( 98.39731940781094011, -60.00000000000247979, 204.7396733380437581 ) ) ;
#31434=CARTESIAN_POINT ( 'NONE',  ( -99.92409395513189452, -60.00000000000000000, 80.58707614375684614 ) ) ;
#31443=CARTESIAN_POINT ( 'NONE',  ( -32.00796974007340623, -18.67729007039406497, 30.02893240338449488 ) ) ;
#31446=CARTESIAN_POINT ( 'NONE',  ( 41.77872314523253294, -29.15662253184162722, 37.78149640197655401 ) ) ;
#31447=CARTESIAN_POINT ( 'NONE',  ( 2.723397405354400211E-15, -8.673617379884035472E-16, 22.23822744035697241 ) ) ;
#31450=CARTESIAN_POINT ( 'NONE',  ( -73.25624440150409100, -38.32611741607561839, 154.3746391340933144 ) ) ;
#31460=CARTESIAN_POINT ( 'NONE',  ( 93.34302217634724741, -59.99999999999998579, 35.60011999643739244 ) ) ;
#31468=CARTESIAN_POINT ( 'NONE',  ( -89.12256709102487662, -30.00000000000086686, -14.43968776839223800 ) ) ;
#31483=CARTESIAN_POINT ( 'NONE',  ( 81.27861452902187978, -42.96768989124994675, 159.4987958060827111 ) ) ;
#31493=CARTESIAN_POINT ( 'NONE',  ( -24.14082041284044422, -57.67406494483144286, 42.97874410022470215 ) ) ;
#31501=CARTESIAN_POINT ( 'NONE',  ( -34.10647007375028039, -23.64402837878609986, 33.18254751217250487 ) ) ;
#31518=CARTESIAN_POINT ( 'NONE',  ( 93.70983742795966975, -57.61862147648758992, 204.5155149370983452 ) ) ;
#31523=CARTESIAN_POINT ( 'NONE',  ( -74.81432347301979746, -60.00000000000002132, 179.8222036999654563 ) ) ;
#31528=CARTESIAN_POINT ( 'NONE',  ( -86.09903236225166268, -24.81206519315382764, 180.1009231137148561 ) ) ;
#31535=B_SPLINE_CURVE_WITH_KNOTS ( 'NONE', 3,
 ( #55314, #56903, #89302, #88762, #88241, #14859, #89826, #40201, #90350, #24584, #5715, #15397, #73078, #7823, #105985, #30552, #97904, #48809, #81698, #40733, #74153, #25664, #90892, #50403, #17007, #34810, #67147, #42322, #9957, #18617, #76285, #50934, #42863, #66073, #84394, #49884, #67678, #17542, #83317, #2394, #1854, #10485, #75215, #43403, #25110, #98951, #82248, #35341, #75756, #1309, #9407, #68202, #93009, #101102, #41265, #83849, #92469, #18076, #51479, #58525, #26723, #19173, #100562, #59594, #57971, #27261, #236, #60145, #41795, #91944, #8364, #34270, #33203, #82790, #8891, #74682, #91431, #100029, #59057, #762, #33728, #66608, #26198, #99486, #46060, #20241, #52537, #102161, #86009, #62263, #69285, #4527, #61187, #78943, #45011, #36416, #4005, #87060, #61733, #2926, #70333, #60667, #35879, #85456, #103231, #86544, #29893, #70863, #103754, #94073, #3474, #54118, #28310, #62780, #11542, #53087, #45540, #5065, #43927, #12080, #93554, #77894, #19703, #37473, #36935, #69801, #12602, #95148, #37999, #20773, #78413, #68760, #13131, #44466, #29374, #102697, #28860, #95668, #21282, #52007, #53609, #84924, #101639, #27796, #11010, #76815, #77361, #94629, #55702, #89700, #32549, #15802, #87581, #97246, #32009, #64372, #97769, #104815, #72959, #88634, #105348, #40080, #71375, #15271, #13669, #64883, #14724, #23391, #105866, #106387, #81566, #48682, #47622, #48154, #7696, #63313, #47095, #22337, #65421, #81055, #56228, #96209, #72444, #80525, #63840, #23935, #89167, #31493, #96734, #46577, #56778, #40606, #7168, #6107, #73490, #30964, #55184, #21807, #6642, #104277 ),
 .UNSPECIFIED., .F., .F.,
 ( 4, 2, 2, 2, 2, 2, 2, 2, 2, 2, 2, 2, 2, 2, 2, 2, 2, 2, 2, 2, 2, 2, 2, 2, 2, 2, 2, 2, 2, 2, 2, 2, 2, 2, 2, 2, 2, 2, 2, 2, 2, 2, 2, 2, 2, 2, 2, 2, 2, 2, 2, 2, 2, 2, 2, 2, 2, 2, 2, 2, 2, 2, 2, 2, 2, 2, 2, 2, 2, 2, 2, 2, 2, 2, 2, 2, 2, 2, 2, 2, 2, 2, 2, 2, 2, 2, 2, 2, 2, 2, 2, 2, 2, 2, 2, 2, 2, 2, 2, 4 ),
 ( 1.408790152747874003E-05, 0.008346361953628917210, 0.01669272390725783442, 0.03338544781451566884, 0.04173180976814458432, 0.05007817172177350673, 0.05425135269858796794, 0.05842453367540242221, 0.06677089562903133768, 0.07511725758266024622, 0.07929043855947470743, 0.08346361953628916863, 0.08555021002469639924, 0.08763680051310362984, 0.09180998148991809105, 0.09389657197832532165, 0.09493986722252893695, 0.09598316246673255225, 0.09806975295513978286, 0.1001563434435470135, 0.1011996386877506288, 0.1022429339319542441, 0.1043295244203614747, 0.1085027053971759359, 0.1126758863739903971, 0.1168490673508048444, 0.1210222483276192917, 0.1251954293044337529, 0.1335417912580626754, 0.1418881532116915700, 0.1502345151653204924, 0.1669272390725783373, 0.1836199629798361821, 0.2003126868870940269, 0.2336981347016096888, 0.2503908586088675059, 0.2670835825161253507, 0.2754299444697542176, 0.2837763064233831400, 0.2921226683770120625, 0.2962958493538265237, 0.3004690303306409849, 0.3025556208190481877, 0.3046422113074554461, 0.3088153922842699073, 0.3109019827726771101, 0.3119452780168807671, 0.3129885732610843685, 0.3150751637494916269, 0.3161184589936952283, 0.3171617542378988297, 0.3192483447263060325, 0.3202916399705096895, 0.3213349352147132909, 0.3255081161915277521, 0.3265514114357313535, 0.3275947066799349550, 0.3296812971683422133, 0.3317678876567494717, 0.3338544781451566745, 0.3359410686335638774, 0.3380276591219711357, 0.3390709543661747372, 0.3401142496103783941, 0.3422008400987855969, 0.3442874305871927998, 0.3453307258313964567, 0.3463740210756000582, 0.3505472020524145194, 0.3547203830292289806, 0.3588935640060434418, 0.3630667449828579030, 0.3672399259596723642, 0.3755862879133012866, 0.3839326498669302090, 0.3922790118205591314, 0.4006253737741880538, 0.4173180976814458987, 0.4340108215887037435, 0.4507035454959615883, 0.4590499074495905107, 0.4673962694032193776, 0.4757426313568481890, 0.4799158123336627613, 0.4840889933104772225, 0.4882621742872916282, 0.4924353552641060894, 0.4945219457525132922, 0.4966085362409205506, 0.5007817172177350118, 0.5028683077061422146, 0.5039116029503458716, 0.5049548981945495285, 0.5091280791713639342, 0.5112146696597711371, 0.5133012601481783399, 0.5174744411249928566, 0.5216476221018073733, 0.5258208030786217790, 0.5341671650322507015 ),
 .UNSPECIFIED. ) ;
#31545=CARTESIAN_POINT ( 'NONE',  ( 22.23822744035697241, -8.673617379884035472E-16, 2.910977163136220014 ) ) ;
#31547=CARTESIAN_POINT ( 'NONE',  ( 87.60230161701383622, -14.21045842199431064, -3.802929300262678947 ) ) ;
#31548=CARTESIAN_POINT ( 'NONE',  ( -76.51940332190571326, -56.84804871597534515, 142.3230989425833855 ) ) ;
#31550=CARTESIAN_POINT ( 'NONE',  ( 82.31973535306708811, -57.52566952622508012, 200.7289113873300437 ) ) ;
#31558=CARTESIAN_POINT ( 'NONE',  ( -105.1817855895727263, -52.71030988280897134, 168.1451182041190293 ) ) ;
#31571=CARTESIAN_POINT ( 'NONE',  ( 28.68725023401711738, -29.05854980118881059, 30.85773263594263938 ) ) ;
#31583=CARTESIAN_POINT ( 'NONE',  ( 85.04705102683632845, -29.99999999999995026, 170.8080372376007006 ) ) ;
#31607=CARTESIAN_POINT ( 'NONE',  ( -2.087134204587958841, -60.00000000000000000, 33.88964995960240145 ) ) ;
#31608=CARTESIAN_POINT ( 'NONE',  ( 64.47874323931745266, -42.95807119333815649, 86.48291114592055351 ) ) ;
#31628=CARTESIAN_POINT ( 'NONE',  ( 21.36556348850374221, -60.00000000000001421, 40.41599463261538006 ) ) ;
#31631=CARTESIAN_POINT ( 'NONE',  ( -90.59850697782101747, -29.99999999999999289, 190.2918799463446931 ) ) ;
#31636=CARTESIAN_POINT ( 'NONE',  ( 36.78581192191307281, -57.69605431621219793, 51.12723935542062037 ) ) ;
#31638=EDGE_CURVE ( 'NONE', #59296, #60348, #15333, .T. ) ;
#31640=CARTESIAN_POINT ( 'NONE',  ( 5.199577819732106754, -21.67934222354764628, -38.54735607716909840 ) ) ;
#31645=CARTESIAN_POINT ( 'NONE',  ( -25.26314279777532690, -60.00000000000000711, 41.24176291422744356 ) ) ;
#31647=CARTESIAN_POINT ( 'NONE',  ( -85.88498695457488452, -57.45118064709335925, 193.0270043969651397 ) ) ;
#31651=CARTESIAN_POINT ( 'NONE',  ( -14.72005785463202621, -49.92084221828517343, 32.33953701706330008 ) ) ;
#31663=CARTESIAN_POINT ( 'NONE',  ( 61.48198989113487301, -60.00000000000000000, 105.4918018471999517 ) ) ;
#31668=CARTESIAN_POINT ( 'NONE',  ( 21.36200998601213641, -60.00000000000005684, 42.72826288236584702 ) ) ;
#31679=CARTESIAN_POINT ( 'NONE',  ( -114.6154627495407965, -59.99999999999028688, 172.5259999663634289 ) ) ;
#31682=CARTESIAN_POINT ( 'NONE',  ( 47.97043484894224719, -59.99999999999998579, 66.94516856292635509 ) ) ;
#31685=CARTESIAN_POINT ( 'NONE',  ( -109.5584880022855998, -59.99999999999993605, 197.6571416747650574 ) ) ;
#31686=CARTESIAN_POINT ( 'NONE',  ( 18.16438888712567490, -53.39614106568718910, 33.13417337925488226 ) ) ;
#31688=CARTESIAN_POINT ( 'NONE',  ( 100.8551254251243563, -38.00000000000002842, 188.7646223632392264 ) ) ;
#31690=CARTESIAN_POINT ( 'NONE',  ( -45.52144803689373020, -39.53055252850298018, 44.31166116903103358 ) ) ;
#31700=CARTESIAN_POINT ( 'NONE',  ( 100.1372358933510327, -30.00000000002086509, 199.1046915188701405 ) ) ;
#31702=VECTOR ( 'NONE', #1857, 1000.000000000000000 ) ;
#31705=CARTESIAN_POINT ( 'NONE',  ( 100.5523255717907745, -30.00000000000000355, 159.8787756642091153 ) ) ;
#31721=CARTESIAN_POINT ( 'NONE',  ( 80.57150957014567894, -38.81697432977912854, 193.9564742164324969 ) ) ;
#31736=( NAMED_UNIT ( * ) PLANE_ANGLE_UNIT ( ) SI_UNIT ( $, .RADIAN. ) );
#31746=CARTESIAN_POINT ( 'NONE',  ( 85.57898256585818331, -35.67946169813210133, 183.8354908636134724 ) ) ;
#31749=VERTEX_POINT ( 'NONE', #79023 ) ;
#31751=CARTESIAN_POINT ( 'NONE',  ( 93.83684923425705904, -57.67470318766702064, 11.22057503938936129 ) ) ;
#31755=CARTESIAN_POINT ( 'NONE',  ( -86.49015731118424810, -37.99999999999980105, 187.7658702032705378 ) ) ;
#31766=CARTESIAN_POINT ( 'NONE',  ( 69.44037080505408710, -29.97022514493267309, -21.01289856691821001 ) ) ;
#31771=CARTESIAN_POINT ( 'NONE',  ( -10.82100110659969516, -16.37520694100678043, -34.74528928969461106 ) ) ;
#31774=CARTESIAN_POINT ( 'NONE',  ( -31.96895277089044995, -47.40887110283673422, -32.79492523475107646 ) ) ;
#31780=CARTESIAN_POINT ( 'NONE',  ( -92.59975610422581838, -60.00000000000001421, -2.780597702228391643 ) ) ;
#31782=CARTESIAN_POINT ( 'NONE',  ( 33.90317062511168444, -31.39243716251483107, -29.86178143371859051 ) ) ;
#31783=CARTESIAN_POINT ( 'NONE',  ( -75.51516288543759003, -29.99999999999999289, -27.33247042156351725 ) ) ;
#31784=CARTESIAN_POINT ( 'NONE',  ( 101.1766009655264895, -60.24913381348638097, 194.9937302242699673 ) ) ;
#31788=CARTESIAN_POINT ( 'NONE',  ( -81.20415014607263515, -49.93051291868427199, 169.6414208886321262 ) ) ;
#31798=CARTESIAN_POINT ( 'NONE',  ( -114.2271649293462445, -57.67113267762195505, 172.5270642037310722 ) ) ;
#31803=CARTESIAN_POINT ( 'NONE',  ( 2.726837646490497757, -14.21045842199434794, -37.36840973699905533 ) ) ;
#31805=CARTESIAN_POINT ( 'NONE',  ( -54.29644833178524976, -29.09616009912803491, 54.75307643248039824 ) ) ;
#31810=CARTESIAN_POINT ( 'NONE',  ( -98.54215169052864098, -45.24992954469452400, 193.5376205676895722 ) ) ;
#31817=CARTESIAN_POINT ( 'NONE',  ( 89.38838440990150502, -38.38695707012075786, -17.36236548429767623 ) ) ;
#31823=CARTESIAN_POINT ( 'NONE',  ( 84.03426563400070393, -30.00000000000000000, 161.3119413430846407 ) ) ;
#31830=EDGE_LOOP ( 'NONE', ( #43264, #92378, #89406, #41202 ) ) ;
#31832=CARTESIAN_POINT ( 'NONE',  ( 49.20253590315749648, -46.43899358245619169, 51.70391652283478834 ) ) ;
#31837=CARTESIAN_POINT ( 'NONE',  ( -106.5422770149979357, -38.37230016228074447, 195.6026319719495064 ) ) ;
#31840=CARTESIAN_POINT ( 'NONE',  ( 110.3060959018607576, -38.35604839215716311, 158.1135554324671944 ) ) ;
#31844=CARTESIAN_POINT ( 'NONE',  ( 101.5801647266594046, -60.15125686205630018, 125.0291127044086892 ) ) ;
#31849=CARTESIAN_POINT ( 'NONE',  ( 78.07448996005189201, -60.00000000000000000, 192.9802269763975744 ) ) ;
#31853=CARTESIAN_POINT ( 'NONE',  ( 57.85089049392932026, -60.32948186521389289, 76.30787142766249076 ) ) ;
#31860=CARTESIAN_POINT ( 'NONE',  ( -81.38022930017784518, -38.35629332861885388, -25.64663872047383819 ) ) ;
#31870=CARTESIAN_POINT ( 'NONE',  ( 82.76193996168436229, -46.48728455946643834, 178.0629670417869761 ) ) ;
#31884=CARTESIAN_POINT ( 'NONE',  ( -12.53202292880966873, -21.38207867075475477, 35.62331039717147974 ) ) ;
#31909=CARTESIAN_POINT ( 'NONE',  ( -109.3749600128534354, -60.00000000000001421, 138.6821750997686422 ) ) ;
#31917=CARTESIAN_POINT ( 'NONE',  ( -83.30516160954981331, -42.98134678973099199, 177.5882959578982252 ) ) ;
#31931=CARTESIAN_POINT ( 'NONE',  ( 113.0845476695725864, -59.99999999999993605, 149.3435440849930842 ) ) ;
#31932=CARTESIAN_POINT ( 'NONE',  ( -109.2896413415886485, -29.99999999999996092, 180.5615511752786233 ) ) ;
#31933=CARTESIAN_POINT ( 'NONE',  ( -61.87588688699417361, -29.06269388545054966, 72.16211123457625831 ) ) ;
#31936=CARTESIAN_POINT ( 'NONE',  ( 107.2599453223138681, -60.00000000001746514, 200.4174002960321843 ) ) ;
#31938=CARTESIAN_POINT ( 'NONE',  ( -8.046840872620296425E-06, -18.58625481980403649, 26.98735909623638207 ) ) ;
#31948=CARTESIAN_POINT ( 'NONE',  ( -82.56557049406225701, -59.99999999999998579, 198.5083017901899893 ) ) ;
#31958=CARTESIAN_POINT ( 'NONE',  ( 104.1990965023338447, -60.00000000000000711, 190.2933881766849993 ) ) ;
#31960=CARTESIAN_POINT ( 'NONE',  ( -32.37223141510428093, -36.02462889410557523, 33.42066239552286078 ) ) ;
#31962=CARTESIAN_POINT ( 'NONE',  ( 38.79797393659272586, -53.34597881264516417, 40.67431443658261259 ) ) ;
#31966=CARTESIAN_POINT ( 'NONE',  ( -57.85136142586996755, -38.34423032919368524, 89.80014059173201701 ) ) ;
#31979=CARTESIAN_POINT ( 'NONE',  ( 99.85406479428269222, -60.00000000000002132, 80.14550826570986430 ) ) ;
#31986=CARTESIAN_POINT ( 'NONE',  ( -79.59017023080539843, -30.00000000000330402, -25.12590073989853323 ) ) ;
#32000=CARTESIAN_POINT ( 'NONE',  ( 82.11076762983330468, -36.02623207226398705, 156.5626120355436512 ) ) ;
#32009=CARTESIAN_POINT ( 'NONE',  ( -65.18805258578451856, -57.67964089302213893, 127.3758707571902846 ) ) ;
#32019=CARTESIAN_POINT ( 'NONE',  ( -27.84441264740780042, -20.64603143622934667, 31.82904849691709614 ) ) ;
#32031=CARTESIAN_POINT ( 'NONE',  ( -7.794767814137952833, -22.09678263551836253, -38.54438751446986089 ) ) ;
#32038=CARTESIAN_POINT ( 'NONE',  ( 96.42806518034892349, -57.62205372991940067, 204.4897109694943822 ) ) ;
#32043=CARTESIAN_POINT ( 'NONE',  ( -74.42952615539968519, -60.00000000000000711, 176.4565370492489933 ) ) ;
#32050=CARTESIAN_POINT ( 'NONE',  ( -85.50811847932432386, -39.29135958765198211, 185.4900395003674305 ) ) ;
#32058=CARTESIAN_POINT ( 'NONE',  ( -82.06014707987355905, -37.79109599669338593, -13.64768699179697187 ) ) ;
#32068=CARTESIAN_POINT ( 'NONE',  ( 24.50706706878033359, -14.21045842199442077, -36.19515235953155496 ) ) ;
#32069=CARTESIAN_POINT ( 'NONE',  ( -77.27742402748401673, -36.02507073553299222, 127.9111887702353840 ) ) ;
#32071=CARTESIAN_POINT ( 'NONE',  ( 48.80991865481109215, -14.21045842199436215, 55.83985330155353921 ) ) ;
#32073=CARTESIAN_POINT ( 'NONE',  ( 92.56122130409121951, -57.65783127504731453, -18.25359173818277014 ) ) ;
#32074=DIRECTION ( 'NONE',  ( 0.000000000000000000, 1.000000000000000000, 0.000000000000000000 ) ) ;
#32089=CARTESIAN_POINT ( 'NONE',  ( 30.60635347677523299, -56.85241792156345042, 36.44043152735474678 ) ) ;
#32094=FACE_BOUND ( 'NONE', #20044, .T. ) ;
#32100=CARTESIAN_POINT ( 'NONE',  ( 8.295375291309756705, -59.99999999999999289, -42.48138218885826234 ) ) ;
#32129=CARTESIAN_POINT ( 'NONE',  ( -77.37933372540865662, -59.99999999999995737, 150.9740157483943506 ) ) ;
#32130=CARTESIAN_POINT ( 'NONE',  ( 68.68987387269132228, -18.63274608647051878, 85.98930702359679401 ) ) ;
#32136=EDGE_CURVE ( 'NONE', #4466, #86580, #95553, .T. ) ;
#32152=CARTESIAN_POINT ( 'NONE',  ( 8.550030583596393896, -60.00000000000000000, 39.63663732540850759 ) ) ;
#32153=CARTESIAN_POINT ( 'NONE',  ( -98.86655644987608582, -30.00000000000000355, 189.1318155084324246 ) ) ;
#32155=CARTESIAN_POINT ( 'NONE',  ( -89.99999999999997158, -52.00000000000000000, 196.0238439516549818 ) ) ;
#32156=CARTESIAN_POINT ( 'NONE',  ( 54.56491434472576429, -57.67593140129608997, 90.07630786268572365 ) ) ;
#32162=CARTESIAN_POINT ( 'NONE',  ( -6.181622435106722158, -60.00000000000001421, 39.62780610759933353 ) ) ;
#32165=CARTESIAN_POINT ( 'NONE',  ( -86.00392355705747605, -61.04916185595598677, 194.3144374245121639 ) ) ;
#32169=CARTESIAN_POINT ( 'NONE',  ( -9.217550163516040840, -39.47610853938331843, 30.47143711703355251 ) ) ;
#32171=CARTESIAN_POINT ( 'NONE',  ( -101.1267960657979756, -59.99999999999995737, 195.0049809712846525 ) ) ;
#32182=CARTESIAN_POINT ( 'NONE',  ( 73.53860074992563511, -59.99999999999999289, 167.5715982711623440 ) ) ;
#32191=CARTESIAN_POINT ( 'NONE',  ( 12.46466094585187889, -29.99999999999991118, 37.03825901911487506 ) ) ;
#32206=CARTESIAN_POINT ( 'NONE',  ( -21.44411787121075363, -60.00000000000489564, 42.81394995815333715 ) ) ;
#32208=CARTESIAN_POINT ( 'NONE',  ( 67.29303862372746892, -60.00000000000000000, 127.0361366969463859 ) ) ;
#32210=CARTESIAN_POINT ( 'NONE',  ( -106.9310521912263710, -14.21045842199434794, 169.9232300575910131 ) ) ;
#32211=CARTESIAN_POINT ( 'NONE',  ( 15.72127475791274342, -42.95378344181465025, 31.23277305341622778 ) ) ;
#32212=CARTESIAN_POINT ( 'NONE',  ( 82.81422886519544591, -37.99999999999996447, 23.20150160915743243 ) ) ;
#32214=CARTESIAN_POINT ( 'NONE',  ( -47.78472977372928909, -18.76678906305324901, 41.09994231454981417 ) ) ;
#32227=CARTESIAN_POINT ( 'NONE',  ( 88.50590120176012476, -30.00000000000198597, 198.8119346494863464 ) ) ;
#32232=CARTESIAN_POINT ( 'NONE',  ( 92.46214547348466795, -30.00000000000000000, 102.8783225717633627 ) ) ;
#32246=CARTESIAN_POINT ( 'NONE',  ( 85.83366297925716992, -38.65129167634649576, 198.9702531129130421 ) ) ;
#32261=( NAMED_UNIT ( * ) SI_UNIT ( $, .STERADIAN. ) SOLID_ANGLE_UNIT ( ) );
#32277=CARTESIAN_POINT ( 'NONE',  ( 84.23888984516474920, -53.80018453417523716, 189.3803214424800672 ) ) ;
#32282=CARTESIAN_POINT ( 'NONE',  ( 82.96216422859413342, -57.67107778185281575, -28.42881364454757076 ) ) ;
#32288=CARTESIAN_POINT ( 'NONE',  ( -81.59242062888966984, -30.00000000000000355, -7.123010226814199264 ) ) ;
#32301=CARTESIAN_POINT ( 'NONE',  ( -97.88527447864335329, -38.00000000000000000, 192.5969185656728371 ) ) ;
#32307=CARTESIAN_POINT ( 'NONE',  ( -20.54902761521100629, -18.70952130878982089, -33.64984671759549428 ) ) ;
#32309=CARTESIAN_POINT ( 'NONE',  ( -28.41674959901979847, -34.58966139483771229, -31.03040257763374399 ) ) ;
#32319=B_SPLINE_CURVE_WITH_KNOTS ( 'NONE', 3,
 ( #7705, #51753, #19978, #33092, #74040, #65957, #60416, #57846, #93825, #84135, #3218, #27537, #93294, #101904, #90772, #10233, #43669, #68494, #36160, #44214, #76557, #77101, #59877, #2668, #101383, #19450, #98326, #2127, #57317, #52285, #85196, #122, #43148, #84668, #76031, #69031, #28063, #60935, #35082, #67951, #92750, #10753, #81579, #73500, #18909, #106399, #40616, #32560, #90235, #65432, #100833, #24482, #16340, #49226, #82128, #8245, #41157, #98836, #24993, #16890, #49770, #26998, #54387, #45281, #30708, #11821, #13409, #36690, #54931, #20526, #94900, #102443, #61472, #4279, #46853, #79221, #95953, #29139, #52823, #70610, #37207, #29653, #37748, #38781, #86283, #21042, #53876, #95410, #70076, #12882, #53363, #87333, #13942, #62525, #21552, #62008, #12355, #102977, #79749, #78160, #5856, #28588, #46334, #71647, #44754, #86809, #69553 ),
 .UNSPECIFIED., .F., .F.,
 ( 4, 2, 2, 2, 2, 1, 2, 2, 2, 1, 1, 2, 2, 1, 2, 2, 1, 1, 2, 2, 1, 1, 2, 2, 1, 2, 2, 2, 2, 2, 1, 2, 2, 2, 1, 2, 2, 1, 1, 2, 2, 2, 2, 1, 2, 2, 1, 1, 2, 2, 1, 2, 2, 1, 2, 2, 1, 2, 2, 1, 1, 2, 2, 4 ),
 ( 0.000000000000000000, 0.06202959713925935287, 0.1240591942785187057, 0.1279360440997223958, 0.1318128939209261274, 0.1395665935633337573, 0.1550739928481488783, 0.1860887914177792313, 0.1880272163283812359, 0.1899656412389832127, 0.1938424910601872775, 0.2015961907025952682, 0.2171035899874111386, 0.2180728024427120992, 0.2185574086703626628, 0.2190420148980131709, 0.2209804398086148702, 0.2248572896298183244, 0.2326109892722254824, 0.2481183885570396597, 0.2490876010123405093, 0.2495722072399910174, 0.2498145103538162159, 0.2500568134676414700, 0.2519952383782430583, 0.2558720881994462348, 0.2636257878418524769, 0.2791331871266647946, 0.2810716120372663274, 0.2820408244925671215, 0.2830100369478679156, 0.2868868867690712032, 0.2946405864114776119, 0.3101479856962904291, 0.3120864106068919619, 0.3123287137207171882, 0.3125710168345423590, 0.3130556230621926450, 0.3140248355174932171, 0.3179016853386955610, 0.3256553849811001378, 0.3411627842659093468, 0.3721775828355277094, 0.3741160077461288536, 0.3746006139737790841, 0.3750852202014293146, 0.3760544326567299422, 0.3799312824779323972, 0.3876849821203374180, 0.4031923814051473487, 0.4051308063157485484, 0.4061000187710491205, 0.4070692312263496926, 0.4109460810475520920, 0.4186997806899569463, 0.4342071799747664884, 0.4361456048853676881, 0.4371148173406683157, 0.4375994235683186018, 0.4380840297959688878, 0.4419608796171713982, 0.4497145792595763636, 0.4652219785443864053, 0.4962367771140062667 ),
 .UNSPECIFIED. ) ;
#32320=CARTESIAN_POINT ( 'NONE',  ( -50.52133408753726229, -59.99999999999999289, -37.80162784956270627 ) ) ;
#32321=VERTEX_POINT ( 'NONE', #50747 ) ;
#32322=CARTESIAN_POINT ( 'NONE',  ( 14.20401263913925760, -24.37963745956056272, -30.50600035239884633 ) ) ;
#32326=EDGE_CURVE ( 'NONE', #63501, #38791, #64018, .T. ) ;
#32327=CARTESIAN_POINT ( 'NONE',  ( -80.25168178368869576, -53.38897274610327770, 165.9826718664497776 ) ) ;
#32340=CARTESIAN_POINT ( 'NONE',  ( -104.5387911149144600, -57.64184148030879840, 201.9936694370400971 ) ) ;
#32346=CARTESIAN_POINT ( 'NONE',  ( -8.554898963428433589, -59.99999999999994316, -44.87740334038038270 ) ) ;
#32348=CARTESIAN_POINT ( 'NONE',  ( -53.46773452942882443, -49.90981900733154220, 61.13492274314185693 ) ) ;
#32353=CARTESIAN_POINT ( 'NONE',  ( -100.6707438451295218, -52.74366064756212324, 193.6868164564221786 ) ) ;
#32358=CARTESIAN_POINT ( 'NONE',  ( 83.07532134950429281, -38.35702953817527572, -24.43146694555268539 ) ) ;
#32363=CARTESIAN_POINT ( 'NONE',  ( 82.59595123229216540, -30.00000000000000000, 150.0044142168436849 ) ) ;
#32370=CARTESIAN_POINT ( 'NONE',  ( 49.68469382639499088, -36.05181846547831270, 49.09954005784402398 ) ) ;
#32372=LINE ( 'NONE', #66845, #1376 ) ;
#32375=CARTESIAN_POINT ( 'NONE',  ( -91.04146929460924298, -38.35192349718176530, 1.571303803682228439 ) ) ;
#32379=CARTESIAN_POINT ( 'NONE',  ( 90.88251751199774731, -38.35193396244151387, 21.04299878531615775 ) ) ;
#32382=CARTESIAN_POINT ( 'NONE',  ( 103.5574493089503960, -45.28273134603495720, 161.0537541144917384 ) ) ;
#32388=CARTESIAN_POINT ( 'NONE',  ( 75.01297031408984139, -59.99999999999999289, 181.3575635546025069 ) ) ;
#32391=CARTESIAN_POINT ( 'NONE',  ( 54.73609672033058615, -60.31833313769052296, 68.31609071314774440 ) ) ;
#32393=DIRECTION ( 'NONE',  ( -3.700743415420800925E-15, 0.000000000000000000, 1.000000000000000000 ) ) ;
#32395=CARTESIAN_POINT ( 'NONE',  ( -79.79561180674197374, -30.00000000001763212, 189.8119606060800209 ) ) ;
#32407=CARTESIAN_POINT ( 'NONE',  ( 84.88381472203214173, -28.91780597334601310, 171.4463788976194394 ) ) ;
#32425=CARTESIAN_POINT ( 'NONE',  ( -27.41650441252286186, -30.69644322685219606, 39.25280176715715896 ) ) ;
#32438=CARTESIAN_POINT ( 'NONE',  ( 2.500000000000013767, -30.00000000000000355, -31.87333685190803223 ) ) ;
#32439=VERTEX_POINT ( 'NONE', #53943 ) ;
#32449=CARTESIAN_POINT ( 'NONE',  ( -100.8702866454455460, -60.00000000000000000, 86.13925423138952908 ) ) ;
#32457=CARTESIAN_POINT ( 'NONE',  ( -83.83424416342712959, -39.45725404996229457, 177.1358821851452490 ) ) ;
#32472=CARTESIAN_POINT ( 'NONE',  ( 104.9451034742319706, -14.21045842199432663, 145.4709692194043669 ) ) ;
#32473=CARTESIAN_POINT ( 'NONE',  ( -114.5930292407900879, -59.99999999999997868, 172.8116974628616163 ) ) ;
#32474=CARTESIAN_POINT ( 'NONE',  ( -61.45978968603484560, -36.01376588712385995, 74.41489827584142347 ) ) ;
#32477=CARTESIAN_POINT ( 'NONE',  ( 113.8393408857289586, -60.00000000002444978, 184.8621818493575404 ) ) ;
#32479=CARTESIAN_POINT ( 'NONE',  ( 1.003931843719813255, -39.47262783694441168, 30.46842126575976906 ) ) ;
#32489=CARTESIAN_POINT ( 'NONE',  ( -96.32505468604630039, -59.99999999999997868, 58.36311956787620403 ) ) ;
#32499=CARTESIAN_POINT ( 'NONE',  ( 94.52956274838354034, -59.99999999999999289, 83.18473151235357932 ) ) ;
#32500=CARTESIAN_POINT ( 'NONE',  ( -33.05142072533534048, -42.96510174916534197, 35.01105748586546440 ) ) ;
#32502=CARTESIAN_POINT ( 'NONE',  ( 40.91608130519752962, -32.60971946095668983, 37.87311596600657992 ) ) ;
#32508=CARTESIAN_POINT ( 'NONE',  ( -78.02821241015172404, -38.57756610151510301, 188.3064634691189099 ) ) ;
#32510=CARTESIAN_POINT ( 'NONE',  ( 2.499999999999997780, -18.83380486180452706, 27.02532357426314036 ) ) ;
#32519=CARTESIAN_POINT ( 'NONE',  ( 99.00645613855532190, -60.00000000000000711, 75.09026749361882480 ) ) ;
#32526=CARTESIAN_POINT ( 'NONE',  ( -87.40951643045639230, -30.00000000000008171, 185.2141721731731820 ) ) ;
#32539=CARTESIAN_POINT ( 'NONE',  ( 80.99391690137066746, -36.02900316038034134, 148.3428981197941425 ) ) ;
#32548=CARTESIAN_POINT ( 'NONE',  ( -1.286415259407877265, -60.00000000000000711, -36.88577855157840446 ) ) ;
#32549=CARTESIAN_POINT ( 'NONE',  ( -69.31411742845799040, -57.68241165371757262, 149.3509116208381329 ) ) ;
#32560=CARTESIAN_POINT ( 'NONE',  ( 24.52173661427685758, -28.71376923063367315, 38.10928809281097784 ) ) ;
#32561=CARTESIAN_POINT ( 'NONE',  ( 80.00000000000000000, -60.00000000000000000, -21.09707704303352926 ) ) ;
#32571=CARTESIAN_POINT ( 'NONE',  ( 1.207272737710394672, -21.32703354115300698, -38.55255691456996914 ) ) ;
#32576=CARTESIAN_POINT ( 'NONE',  ( 113.9480634309076379, -57.67139826047481677, 163.7752955952890659 ) ) ;
#32581=B_SPLINE_CURVE_WITH_KNOTS ( 'NONE', 3,
 ( #30233, #96551, #29211, #14011, #20601, #13482, #46406, #103055, #62597, #6450, #12952, #22685, #12424, #5923, #88462, #14536, #79292, #94975, #61549, #86359, #47445, #71197, #70150, #80337, #102520, #78234, #28663, #53438, #37821, #45356, #62084, #45872, #78752, #4885, #29721, #7505, #40424, #83014, #39904, #65235, #8048, #97578, #64708, #39386, #15081, #80876, #24275, #8584, #23210, #66295, #56595, #106744, #32893, #49574, #57127, #32363, #64193, #65768, #16145, #90036, #106200, #49032, #25337, #40962, #91126, #31823, #23745, #98127, #58200, #72262, #81929, #56048, #105164, #81394, #98649, #73305, #73850, #88983, #24798, #47966, #82483, #97063, #6985, #72777, #57653, #48501, #105683, #99177, #89518, #15612, #90574, #50107, #16683, #41484, #74374, #451, #31310, #17237, #33421, #984, #18853, #18304, #85140, #59818, #27483, #10701, #19929, #2615, #60360, #84076, #101850, #42544, #26944, #68977, #101331, #50616, #43615, #92695, #75447, #60881, #19398, #84615, #67372, #11233, #58753, #52230, #44158, #77046, #51698, #34507, #33964, #25895, #3162, #1540, #35564, #66835, #76507, #68438, #93235, #67893, #36106, #28011, #9107, #93771, #52772, #74900, #42015, #10176, #43092, #99725, #9636, #35030, #91647, #17760, #75980, #2077, #83533, #100254, #26417, #59282, #92158, #51158, #100781, #46282, #79165, #95897, #103448, #78624, #3707, #5296, #62470, #29599, #45748, #86232, #87278, #46805, #30110, #63002, #104503, #30651, #79697, #22570, #4758, #102384, #11766, #20992, #38215, #12827, #53826, #28537, #37697, #94309, #22022, #71077, #36633, #20471, #53312, #95361, #94847, #12304, #38729, #54878, #87808, #37160, #103968, #70562, #13886, #5805, #71598, #63538, #21498, #54335, #96433, #85689, #86759, #44700, #13355, #77587, #69498, #61417, #45232, #78107, #4225, #70022, #102921, #29089, #61954, #105566, #40834, #31705, #80753, #98007, #73722, #24680, #24159, #89401, #96950, #23085, #90453, #65110, #16565, #6323, #7391, #40304, #88864, #48384, #99052, #57006, #89920, #106084, #56472, #31190, #57531, #16026, #15496, #55921, #73177, #6868, #81276, #39791, #48907, #14953, #8463, #47846, #72665, #39265, #66170, #64593, #32232, #81800, #97463, #88341, #41365, #7927, #47324, #106625, #32775, #49448, #333, #65648, #80220, #55407, #98533, #82357, #23620, #74257, #33300, #14413, #72139, #105049, #64075, #59695, #1957, #91528, #76924, #35440, #60243, #75320, #67775, #100133, #92574, #34910, #93111, #100661, #76381, #67254, #99593, #25218, #26822, #49984, #59161, #42971, #9515, #75862, #34381, #25770, #27364, #74783, #85022, #3035, #18725, #51578, #82891, #84494, #10586, #43502, #83952, #2491, #862, #33840, #68312, #1417, #58073, #58629, #101207, #66713, #35983, #10062, #19284, #90997, #52110, #92043, #18176, #8989, #11106, #44031, #68856, #26299, #17109, #17643, #41894, #51038, #50504, #83416, #42427, #86642, #45112, #11646, #62881, #45634, #70957, #103333, #95772, #46162, #79050, #13766, #46678, #21908, #28411, #62356, #20347, #60765, #93654, #102263, #29480, #94729, #52639, #95246, #61285, #12707, #77991, #54754, #78509, #103849, #4643, #87686, #21379, #79574, #94183, #86109, #20876, #5687, #38612, #53709, #44575, #27898, #37035, #54217, #28964, #69903, #77465, #87157, #102802, #36514, #37574, #53192, #61833, #12180, #13238, #101732, #19802, #70439, #5170, #29995, #4108, #38099, #85571, #3578, #69381, #106492, #56874, #7264, #63423, #81154 ),
 .UNSPECIFIED., .F., .F.,
 ( 4, 1, 1, 1, 1, 1, 1, 1, 1, 1, 2, 2, 1, 1, 1, 1, 1, 1, 2, 2, 1, 1, 1, 1, 1, 1, 2, 2, 1, 1, 1, 1, 1, 1, 1, 1, 2, 2, 1, 1, 1, 1, 1, 1, 2, 2, 1, 1, 1, 1, 1, 1, 1, 1, 2, 2, 1, 1, 1, 1, 1, 1, 1, 1, 2, 2, 1, 1, 1, 1, 1, 1, 1, 1, 1, 2, 2, 1, 1, 1, 1, 1, 1, 1, 1, 2, 2, 1, 1, 1, 1, 1, 1, 1, 2, 2, 1, 1, 1, 2, 2, 1, 1, 1, 1, 1, 1, 1, 1, 2, 2, 1, 1, 1, 2, 2, 1, 1, 1, 1, 1, 2, 2, 1, 1, 2, 2, 1, 1, 1, 1, 2, 2, 1, 1, 1, 1, 1, 2, 2, 1, 1, 1, 1, 1, 2, 2, 1, 1, 1, 2, 2, 1, 1, 1, 1, 1, 2, 2, 1, 1, 1, 1, 1, 1, 2, 2, 1, 1, 1, 1, 1, 1, 1, 1, 2, 2, 1, 1, 1, 1, 1, 1, 1, 1, 1, 1, 2, 2, 1, 1, 1, 1, 1, 1, 1, 1, 1, 1, 2, 2, 1, 1, 1, 1, 1, 1, 1, 1, 1, 1, 2, 2, 1, 1, 1, 1, 1, 1, 1, 1, 2, 2, 1, 1, 1, 1, 1, 1, 1, 1, 2, 2, 1, 1, 1, 1, 1, 1, 1, 1, 1, 1, 2, 2, 1, 1, 1, 1, 1, 1, 1, 1, 1, 2, 2, 1, 1, 1, 1, 1, 1, 1, 2, 2, 1, 1, 1, 1, 1, 1, 1, 2, 2, 1, 1, 1, 1, 1, 1, 2, 2, 1, 1, 1, 1, 1, 1, 1, 2, 2, 1, 1, 1, 1, 1, 1, 2, 2, 1, 1, 1, 1, 1, 1, 2, 2, 1, 1, 1, 1, 1, 1, 1, 1, 2, 2, 1, 1, 1, 1, 1, 1, 1, 2, 2, 1, 1, 1, 1, 1, 2, 2, 1, 1, 1, 1, 1, 1, 1, 1, 2, 2, 4 ),
 ( 0.000000000000000000, 0.03124999999957970426, 0.04687499999936961537, 0.05468749999926453276, 0.05859374999921199145, 0.06054687499918578325, 0.06152343749917271037, 0.06201171874916613230, 0.06225585937416285021, 0.06237792968666124732, 0.06243896484291044241, 0.06249999999915964444, 0.07812499999895176905, 0.08593749999884778279, 0.08984374999879572721, 0.09179687499876966472, 0.09277343749875666123, 0.09326171874875018031, 0.09350585937374693291, 0.09374999999874368550, 0.1093749999985339227, 0.1171874999984289789, 0.1210937499983765070, 0.1230468749983502086, 0.1240234374983369969, 0.1245117187483303772, 0.1247558593733270049, 0.1249999999983236187, 0.1874999999974600873, 0.2187499999970283215, 0.2343749999968123832, 0.2421874999967045528, 0.2460937499966507347, 0.2480468749966238118, 0.2490234374966104891, 0.2495117187466037167, 0.2497558593716003028, 0.2499999999965969166, 0.2656249999963781194, 0.2734374999962687069, 0.2773437499962139174, 0.2792968749961864949, 0.2802734374961726727, 0.2807617187461656783, 0.2810058593711620700, 0.2812499999961584618, 0.2968749999959144348, 0.3046874999957924213, 0.3085937499957315255, 0.3105468749957010499, 0.3115234374956858399, 0.3120117187456782348, 0.3122558593706744046, 0.3123779296831725172, 0.3124389648394215735, 0.3124999999956706298, 0.3203124999955406782, 0.3242187499954757302, 0.3261718749954432561, 0.3271484374954269914, 0.3276367187454188867, 0.3278808593704149454, 0.3280029296829130581, 0.3280639648391620034, 0.3280944824172863927, 0.3281249999954107821, 0.3359374999952490781, 0.3398437499951681984, 0.3417968749951277863, 0.3427734374951075802, 0.3432617187450975327, 0.3435058593700924812, 0.3436279296825899277, 0.3436889648388389840, 0.3437194824169632068, 0.3437347412060256513, 0.3437499999950880403, 0.3515624999950815455, 0.3554687499950783258, 0.3574218749950767715, 0.3583984374950760499, 0.3588867187450754948, 0.3591308593700751062, 0.3592529296825751062, 0.3593139648388249396, 0.3593444824169498841, 0.3593749999950747731, 0.3671874999950420770, 0.3710937499950257568, 0.3730468749950177076, 0.3740234374950136553, 0.3745117187450116569, 0.3747558593700106577, 0.3748779296825102691, 0.3749389648387601026, 0.3749999999950099361, 0.3789062499950078267, 0.3808593749950066609, 0.3811035156200064944, 0.3812255859325062723, 0.3813476562450061058, 0.3818359374950055507, 0.3828124999950045515, 0.3867187499950002216, 0.3886718749949980567, 0.3896484374949969465, 0.3901367187449965024, 0.3903808593699961693, 0.3905029296824958918, 0.3905639648387459473, 0.3906249999949959473, 0.3925781249949994445, 0.3935546874950012763, 0.3940429687450022200, 0.3942871093700026641, 0.3945312499950030527, 0.3964843749950062723, 0.3974609374950079377, 0.3979492187450087148, 0.3981933593700090479, 0.3983154296825091589, 0.3983764648387592144, 0.3984374999950092699, 0.4003906249950098251, 0.4013671874950099916, 0.4018554687450100471, 0.4023437499950101026, 0.4042968749950097695, 0.4052734374950096585, 0.4057617187450095475, 0.4060058593700094365, 0.4061279296825093255, 0.4062499999950091589, 0.4082031249950073826, 0.4091796874950064944, 0.4096679687450061058, 0.4099121093700058838, 0.4100341796825057727, 0.4100952148387557172, 0.4101562499950057172, 0.4121093749950055507, 0.4130859374950055507, 0.4135742187450055507, 0.4138183593700054397, 0.4139404296825054397, 0.4140014648387554397, 0.4140624999950054397, 0.4150390624950059393, 0.4155273437450061058, 0.4157714843700061058, 0.4158935546825060503, 0.4160156249950059393, 0.4169921874950046625, 0.4174804687450040519, 0.4177246093700036633, 0.4178466796825034413, 0.4179077148387534968, 0.4179382324168784413, 0.4179687499950034413, 0.4199218749950064944, 0.4208984374950079932, 0.4213867187450087703, 0.4216308593700091589, 0.4217529296825094365, 0.4218139648387596585, 0.4218444824168848251, 0.4218749999950099361, 0.4296874999950471286, 0.4335937499950655583, 0.4355468749950748841, 0.4365234374950796026, 0.4370117187450819896, 0.4372558593700832108, 0.4373779296825838769, 0.4374389648388341545, 0.4374694824169592100, 0.4374999999950843210, 0.4687499999954365948, 0.4843749999956128982, 0.4921874999957009944, 0.4960937499957450147, 0.4980468749957669417, 0.4990234374957779329, 0.4995117187457834840, 0.4997558593707862595, 0.4998779296832877028, 0.4999389648395383690, 0.4999694824176637575, 0.4999999999957892571, 0.5312499999960962338, 0.5468749999962496666, 0.5546874999963264941, 0.5585937499963649078, 0.5605468749963840036, 0.5615234374963936625, 0.5620117187463983255, 0.5622558593714006570, 0.5623779296839017672, 0.5624389648401522113, 0.5624694824182773223, 0.5624999999964025443, 0.5937499999967007502, 0.6093749999968498532, 0.6171874999969244602, 0.6210937499969616526, 0.6230468749969803044, 0.6240234374969896303, 0.6245117187469941822, 0.6247558593719966247, 0.6248779296844978459, 0.6249389648407485121, 0.6249694824188737341, 0.6249999999969989561, 0.6406249999970944353, 0.6484374999971422859, 0.6523437499971662668, 0.6542968749971781461, 0.6552734374971841413, 0.6557617187471871389, 0.6560058593721885822, 0.6561279296846893594, 0.6561889648409398035, 0.6562499999971902476, 0.6718749999972619680, 0.6796874999972977172, 0.6835937499973157028, 0.6855468749973245846, 0.6865234374973291365, 0.6870117187473313569, 0.6872558593723324671, 0.6873779296848331333, 0.6874389648410834663, 0.6874999999973339104, 0.7187499999975396348, 0.7343749999976424414, 0.7421874999976939558, 0.7460937499977197129, 0.7480468749977324805, 0.7490234374977389198, 0.7495117187477421394, 0.7497558593727436937, 0.7498779296852444709, 0.7499389648414949150, 0.7499694824196200260, 0.7499999999977451370, 0.7812499999980321297, 0.7968749999981755705, 0.8046874999982472909, 0.8085937499982830401, 0.8105468749983010257, 0.8115234374983099075, 0.8120117187483144594, 0.8122558593733167909, 0.8123779296858179011, 0.8124389648420684562, 0.8124999999983189003, 0.8281249999984525711, 0.8359374999985194066, 0.8398437499985528243, 0.8417968749985694776, 0.8427734374985778043, 0.8432617187485820232, 0.8435058593735840216, 0.8436279296860850208, 0.8437499999985860200, 0.8593749999987186916, 0.8671874999987848609, 0.8710937499988180566, 0.8730468749988345989, 0.8740234374988429256, 0.8745117187488470334, 0.8747558593738490318, 0.8748779296863501420, 0.8749999999988511412, 0.8906249999989839239, 0.8984374999990503152, 0.9023437499990835109, 0.9042968749991001642, 0.9052734374991083799, 0.9057617187491125987, 0.9060058593741147082, 0.9062499999991167066, 0.9140624999991834310, 0.9179687499992166266, 0.9199218749992333910, 0.9208984374992417177, 0.9213867187492458255, 0.9216308593742479349, 0.9217529296867489341, 0.9218139648429994892, 0.9218749999992499333, 0.9257812499992839061, 0.9277343749993007815, 0.9287109374993093303, 0.9291992187493135491, 0.9294433593743156585, 0.9295654296868167688, 0.9296264648430672128, 0.9296874999993177680, 0.9335937499993516298, 0.9355468749993685051, 0.9365234374993769428, 0.9370117187493811617, 0.9372558593743832711, 0.9373779296868842703, 0.9374389648431348254, 0.9374999999993852695, 0.9453124999994531041, 0.9492187499994869659, 0.9511718749995038413, 0.9521484374995123900, 0.9526367187495166089, 0.9528808593745187183, 0.9530029296870197175, 0.9530639648432702726, 0.9530944824213954947, 0.9531249999995208277, 0.9570312499995546895, 0.9589843749995717870, 0.9599609374995802247, 0.9604492187495844435, 0.9606933593745866640, 0.9608154296870876632, 0.9608764648433382183, 0.9609069824214634403, 0.9609374999995886624, 0.9648437499996247446, 0.9667968749996427302, 0.9677734374996518341, 0.9682617187496563860, 0.9685058593746586064, 0.9686279296871597166, 0.9687499999996609379, 0.9765624999997345457, 0.9804687499997714051, 0.9824218749997898348, 0.9833984374997990496, 0.9838867187498037126, 0.9841308593748060440, 0.9842529296873072653, 0.9843139648435577094, 0.9843444824216830424, 0.9843749999998082645, 1.000000000000000000 ),
 .UNSPECIFIED. ) ;
#32582=CARTESIAN_POINT ( 'NONE',  ( -73.90092748813849255, -60.00000000000000000, 171.2155407444064110 ) ) ;
#32588=CARTESIAN_POINT ( 'NONE',  ( -85.28664353795764441, -42.93378835376115887, 186.5457363852486310 ) ) ;
#32596=CARTESIAN_POINT ( 'NONE',  ( -84.46960190694564119, -45.27041167832899760, -5.142523808328494539 ) ) ;
#32603=CARTESIAN_POINT ( 'NONE',  ( 11.19959342722337681, 2.897043466792154898E-12, -19.43146043914873289 ) ) ;
#32606=CARTESIAN_POINT ( 'NONE',  ( 33.15797435408901350, -29.99999999999994671, -37.92174772678599481 ) ) ;
#32607=CARTESIAN_POINT ( 'NONE',  ( -78.84973396984698013, -32.55776669678326130, 132.6303212860630367 ) ) ;
#32609=CARTESIAN_POINT ( 'NONE',  ( 55.31236231582965956, -60.00000000000003553, 93.46951393418744658 ) ) ;
#32611=CARTESIAN_POINT ( 'NONE',  ( 94.10923974253748270, -57.67266607662146782, 21.51150559826979602 ) ) ;
#32629=CARTESIAN_POINT ( 'NONE',  ( -20.75616973061526949, -30.00000000000004263, 37.60198765588109637 ) ) ;
#32630=CARTESIAN_POINT ( 'NONE',  ( 29.54011214367963589, -22.11874979585171275, 29.86351015682103238 ) ) ;
#32646=CARTESIAN_POINT ( 'NONE',  ( 33.25680808871401695, -60.00000000000000000, -40.52559416211042276 ) ) ;
#32659=DIRECTION ( 'NONE',  ( 0.000000000000000000, 0.000000000000000000, 1.000000000000000000 ) ) ;
#32674=CARTESIAN_POINT ( 'NONE',  ( 68.29127775091039609, -42.95892816396526825, 98.34793835544786589 ) ) ;
#32698=CARTESIAN_POINT ( 'NONE',  ( -98.12681787409746903, -29.99999999999999645, 190.3891223338559655 ) ) ;
#32701=CARTESIAN_POINT ( 'NONE',  ( 63.30621635515526435, -57.67870488568929233, 119.7030265864528076 ) ) ;
#32705=CARTESIAN_POINT ( 'NONE',  ( 10.26328300195640963, -22.68956793900527913, -38.54249056527262951 ) ) ;
#32708=CARTESIAN_POINT ( 'NONE',  ( -3.925451770789095463, -60.00000000000000711, 39.63159641071881367 ) ) ;
#32712=CARTESIAN_POINT ( 'NONE',  ( -87.13321523403938329, -42.76517114182743029, 190.1424499742896330 ) ) ;
#32716=CARTESIAN_POINT ( 'NONE',  ( -8.140123003886579056, -35.99444279251709844, 29.88182697456086601 ) ) ;
#32731=CARTESIAN_POINT ( 'NONE',  ( 112.5893299866519897, -60.00000000000007105, 145.0945492492805045 ) ) ;
#32750=CARTESIAN_POINT ( 'NONE',  ( -15.38582294317437338, -60.00000000000488853, 42.16893985326622385 ) ) ;
#32752=CARTESIAN_POINT ( 'NONE',  ( 92.13933835806670913, -59.99999999999998579, 21.62654867099170275 ) ) ;
#32753=CARTESIAN_POINT ( 'NONE',  ( -112.2649012439172793, -59.99999999999995026, 191.8495178741738130 ) ) ;
#32754=CARTESIAN_POINT ( 'NONE',  ( 15.60252081763109544, -35.99201029456901324, 30.06430533318423670 ) ) ;
#32758=CARTESIAN_POINT ( 'NONE',  ( -47.76393914926944717, -25.68763306169221394, 43.13152166428435663 ) ) ;
#32765=CARTESIAN_POINT ( 'NONE',  ( 2.500000000000002220, -8.000000000000000000, -17.89626171146327138 ) ) ;
#32771=CARTESIAN_POINT ( 'NONE',  ( 73.12653570793921176, -29.99999999999997868, 143.9247086217570768 ) ) ;
#32775=CARTESIAN_POINT ( 'NONE',  ( 91.56652514123703668, -30.00000000000000355, 97.63639661058265062 ) ) ;
#32790=CARTESIAN_POINT ( 'NONE',  ( 81.63480950427671701, -38.84194040926732328, 195.4446013772895583 ) ) ;
#32806=CARTESIAN_POINT ( 'NONE',  ( 4.433434719022584680, -18.46178206518997911, 35.06931429451628901 ) ) ;
#32812=CARTESIAN_POINT ( 'NONE',  ( 85.91493313960407363, -31.99806336651779404, 183.3893818021954019 ) ) ;
#32815=CARTESIAN_POINT ( 'NONE',  ( 77.65333090421673035, -57.67122462496276825, -31.42556703637626470 ) ) ;
#32820=CARTESIAN_POINT ( 'NONE',  ( -80.86820734843506386, -30.00000000000000711, 18.00287957002532835 ) ) ;
#32822=CARTESIAN_POINT ( 'NONE',  ( -81.12287823873506909, -38.00000000000000711, 151.5567027523417778 ) ) ;
#32833=CARTESIAN_POINT ( 'NONE',  ( -98.63393505101123537, -37.99999999999995737, 192.2163830362448493 ) ) ;
#32839=CARTESIAN_POINT ( 'NONE',  ( -19.15334754509612125, -18.31105778728934297, -33.83673051268581133 ) ) ;
#32842=CARTESIAN_POINT ( 'NONE',  ( -65.77390279226092673, -47.40885602207553262, -25.69725042524944669 ) ) ;
#32852=CARTESIAN_POINT ( 'NONE',  ( -34.63102061609615845, -60.00000000000000000, -40.35545487002439558 ) ) ;
#32854=CARTESIAN_POINT ( 'NONE',  ( 52.55293351040379690, -36.28902381433119473, -27.45765431991302563 ) ) ;
#32855=LINE ( 'NONE', #65732, #60926 ) ;
#32856=CARTESIAN_POINT ( 'NONE',  ( 95.90148991104773302, -45.27101873155104528, 194.1444148739948332 ) ) ;
#32869=CARTESIAN_POINT ( 'NONE',  ( 2.500000000000003109, -8.000000000000000000, -9.184850993605154600E-17 ) ) ;
#32870=CARTESIAN_POINT ( 'NONE',  ( -36.61061158941262761, -57.69633519219438966, 50.91350493295865931 ) ) ;
#32876=CARTESIAN_POINT ( 'NONE',  ( -49.63234380517151578, -59.99999999999993605, -40.41886796471348475 ) ) ;
#32879=CARTESIAN_POINT ( 'NONE',  ( -52.19514852257324122, -29.11169795166002316, 50.88471273071843370 ) ) ;
#32882=CARTESIAN_POINT ( 'NONE',  ( -99.71322838326179294, -52.76976600324411493, 194.3808308585486770 ) ) ;
#32888=CARTESIAN_POINT ( 'NONE',  ( 73.36361653136737004, -38.32548766739345325, 155.0768100110214789 ) ) ;
#32893=CARTESIAN_POINT ( 'NONE',  ( 82.57022881561088923, -29.99999999999999645, 149.8254230277452450 ) ) ;
#32901=CARTESIAN_POINT ( 'NONE',  ( 49.21559585471668896, -60.28730590752689267, 56.32551750424051562 ) ) ;
#32905=CARTESIAN_POINT ( 'NONE',  ( -92.91729557026953046, -38.35493114579749374, 42.71798821936229729 ) ) ;
#32908=CARTESIAN_POINT ( 'NONE',  ( 92.01162595420805701, -38.35403553970205337, 34.85480957562649706 ) ) ;
#32910=CARTESIAN_POINT ( 'NONE',  ( 106.0485595022860394, -60.15138397827151806, 161.1432654068886166 ) ) ;
#32914=CARTESIAN_POINT ( 'NONE',  ( 74.30875725675150534, -60.00000000000000711, 175.2953947742391279 ) ) ;
#32917=CARTESIAN_POINT ( 'NONE',  ( 89.99999999999997158, 500000.0000000000582, 196.0238439516549818 ) ) ;
#32920=CARTESIAN_POINT ( 'NONE',  ( 62.29079176448218647, -22.11117550964195644, 69.90653633777594678 ) ) ;
#32926=CARTESIAN_POINT ( 'NONE',  ( -76.05260806692862730, -29.99999999983540633, 166.0217771130949131 ) ) ;
#32939=CARTESIAN_POINT ( 'NONE',  ( 82.34467536305523083, -49.99737630304606739, 179.4894546011980481 ) ) ;
#32954=CARTESIAN_POINT ( 'NONE',  ( -27.44437592492746703, -30.71555339929342665, 39.26539023425417696 ) ) ;
#32966=CARTESIAN_POINT ( 'NONE',  ( 70.42381680912748720, -34.58960566250176072, -21.61503493545830779 ) ) ;
#32977=CARTESIAN_POINT ( 'NONE',  ( -98.09477537189171414, -59.99999999999999289, 69.51200655767426895 ) ) ;
#32984=CARTESIAN_POINT ( 'NONE',  ( -81.99888381046133645, -53.52207800286723227, 181.3765808315105801 ) ) ;
#32997=CARTESIAN_POINT ( 'NONE',  ( -44.70137845890145911, -57.67116879762227910, -40.89012893473564958 ) ) ;
#33004=CARTESIAN_POINT ( 'NONE',  ( 109.5128197388708031, -29.99999999999998934, 168.1051457340969932 ) ) ;
#33006=CARTESIAN_POINT ( 'NONE',  ( -109.5811972119284690, -29.99999999999999289, 174.3366342583755113 ) ) ;
#33007=CARTESIAN_POINT ( 'NONE',  ( -64.30537749630316569, -18.62720888008740161, 73.57097262722605535 ) ) ;
#33010=CARTESIAN_POINT ( 'NONE',  ( 95.09347488121859726, -60.00000000001951150, -4.937967903116023294 ) ) ;
#33012=CARTESIAN_POINT ( 'NONE',  ( 3.214995758538034771E-05, -42.95368998299849750, 31.04859829010212380 ) ) ;
#33020=CARTESIAN_POINT ( 'NONE',  ( -99.26889953123149724, -60.00000000000001421, 202.0842824767352681 ) ) ;
#33031=CARTESIAN_POINT ( 'NONE',  ( -33.72753996741100480, -49.90232404750766904, 36.63834850608077431 ) ) ;
#33034=CARTESIAN_POINT ( 'NONE',  ( 40.62329115609131236, -49.88684013868402900, 41.58757686396207731 ) ) ;
#33040=CARTESIAN_POINT ( 'NONE',  ( -76.67538504582743997, -38.42797185326705289, 182.7090895004452591 ) ) ;
#33042=CARTESIAN_POINT ( 'NONE',  ( 2.499999999999998668, -12.75202509204646972, 21.42349226578282995 ) ) ;
#33051=CARTESIAN_POINT ( 'NONE',  ( 103.6141585822474411, -60.00000000000000711, 102.1783202260197925 ) ) ;
#33055=EDGE_CURVE ( 'NONE', #85958, #87422, #102587, .T. ) ;
#33056=CARTESIAN_POINT ( 'NONE',  ( -98.75918947158213257, -29.99999999999995026, 189.3635776327697897 ) ) ;
#33071=CARTESIAN_POINT ( 'NONE',  ( 80.22144217257282151, -42.96589628622726309, 151.2297849153674463 ) ) ;
#33089=CARTESIAN_POINT ( 'NONE',  ( 86.12568212521020428, -61.03451969644774522, 194.3966504858508983 ) ) ;
#33092=CARTESIAN_POINT ( 'NONE',  ( 39.40329081872960160, -37.47882864960006088, 48.99327379398392424 ) ) ;
#33106=CARTESIAN_POINT ( 'NONE',  ( 113.6035234506770024, -57.67119983476416678, 183.6741733121881737 ) ) ;
#33113=CARTESIAN_POINT ( 'NONE',  ( -76.26472227669087545, -60.00000000000000000, 188.0289714178661882 ) ) ;
#33117=CARTESIAN_POINT ( 'NONE',  ( -84.38815688596613995, -53.81528062727464601, 189.6626461044262442 ) ) ;
#33120=ORIENTED_EDGE ( 'NONE', *, *, #5854, .F. ) ;
#33123=CARTESIAN_POINT ( 'NONE',  ( -86.93649315962268531, -60.22167703688511864, -9.633606967954129630 ) ) ;
#33129=CARTESIAN_POINT ( 'NONE',  ( -10.45706415777455689, -1.734723475976807094E-15, -13.60704923275582701 ) ) ;
#33131=CARTESIAN_POINT ( 'NONE',  ( 41.39111156191358276, -30.00000000000003908, -36.78675873448672462 ) ) ;
#33132=CARTESIAN_POINT ( 'NONE',  ( -77.89137182638854995, -46.43782183837505073, 140.2357373465546004 ) ) ;
#33134=CARTESIAN_POINT ( 'NONE',  ( 66.64731328016637235, -30.00000000000005684, 114.0820693445010363 ) ) ;
#33136=CARTESIAN_POINT ( 'NONE',  ( 113.2613034959341149, -57.67119509769668184, 154.8441214569275530 ) ) ;
#33157=CARTESIAN_POINT ( 'NONE',  ( 30.57601822009955228, -42.95894917474103636, 33.95501319845223520 ) ) ;
#33169=CARTESIAN_POINT ( 'NONE',  ( 91.96166712811336197, -60.00000000000000711, -14.13641865815662868 ) ) ;
#33178=ORIENTED_EDGE ( 'NONE', *, *, #61734, .T. ) ;
#33183=CARTESIAN_POINT ( 'NONE',  ( 84.40376416015234895, -45.28787472347771370, -3.486817255051028130 ) ) ;
#33194=CARTESIAN_POINT ( 'NONE',  ( -39.59863853631028974, -59.99999999999997158, 42.73346896236057546 ) ) ;
#33196=CARTESIAN_POINT ( 'NONE',  ( 67.53797569337646678, -36.00813603609307734, 91.97696651167636617 ) ) ;
#33203=CARTESIAN_POINT ( 'NONE',  ( -112.4702214903622490, -57.67117150189849895, 147.0458187677821797 ) ) ;
#33221=CARTESIAN_POINT ( 'NONE',  ( -97.10167131913696892, -30.00000000000000000, 191.0522010627015561 ) ) ;
#33224=CARTESIAN_POINT ( 'NONE',  ( 72.60991038965168798, -57.66267021765413148, 177.9523047781559910 ) ) ;
#33228=CARTESIAN_POINT ( 'NONE',  ( 14.67184194744775461, -23.97522478767837129, -38.53186082317327532 ) ) ;
#33231=CARTESIAN_POINT ( 'NONE',  ( -46.99610915538814737, -59.99999999999999289, 64.77681108800881304 ) ) ;
#33234=CARTESIAN_POINT ( 'NONE',  ( -87.02199110510677826, -31.71018611468244686, 187.4638403878138604 ) ) ;
#33238=CARTESIAN_POINT ( 'NONE',  ( -10.04926806037129161, -18.58639629729638543, 26.99593289150223185 ) ) ;
#33252=CARTESIAN_POINT ( 'NONE',  ( 107.9653405324804680, -30.00000000000002132, 188.7583403580863717 ) ) ;
#33274=CARTESIAN_POINT ( 'NONE',  ( -70.09088371448167720, -59.99999999994136601, 157.7190277870289492 ) ) ;
#33277=CARTESIAN_POINT ( 'NONE',  ( 111.6827242965483151, -59.99999999999997868, 183.1303449405941706 ) ) ;
#33278=CARTESIAN_POINT ( 'NONE',  ( -106.8727010878311745, -14.21045842199433373, 167.8788319932906461 ) ) ;
#33279=CARTESIAN_POINT ( 'NONE',  ( 19.40890743283955899, -56.87623265366909919, 33.84337721544303434 ) ) ;
#33281=CARTESIAN_POINT ( 'NONE',  ( -43.41331196749857924, -18.78938622932218649, 36.60976053377660833 ) ) ;
#33293=CARTESIAN_POINT ( 'NONE',  ( 81.37391084052052292, -30.00000000000006040, -10.28767919861631164 ) ) ;
#33300=CARTESIAN_POINT ( 'NONE',  ( 90.42490069223487126, -30.00000000000000000, 90.97836846167180624 ) ) ;
#33306=ORIENTED_EDGE ( 'NONE', *, *, #8991, .F. ) ;
#33317=CARTESIAN_POINT ( 'NONE',  ( 77.69612501048428044, -38.53685538454406156, 187.1913476843784281 ) ) ;
#33322=CIRCLE ( 'NONE', #47298, 60.00000000000000000 ) ;
#33338=CARTESIAN_POINT ( 'NONE',  ( 39.35377274615763099, -37.46504824054412808, 48.92861146246112014 ) ) ;
#33342=CARTESIAN_POINT ( 'NONE',  ( 86.09503755511013878, -28.33328412234302718, 182.5637252326066289 ) ) ;
#33345=CARTESIAN_POINT ( 'NONE',  ( 93.06064234306185767, -57.65576527925703232, -17.06971926439956277 ) ) ;
#33348=CARTESIAN_POINT ( 'NONE',  ( -81.03088382936273604, -30.00000000000000000, 21.51870931205188953 ) ) ;
#33350=CARTESIAN_POINT ( 'NONE',  ( -83.15876612675486967, -37.99999999999995737, 169.0493242017684281 ) ) ;
#33363=CARTESIAN_POINT ( 'NONE',  ( -99.26691377649297010, -38.00000000000004974, 191.6702388746358849 ) ) ;
#33368=CARTESIAN_POINT ( 'NONE',  ( -53.90143474190011830, -28.29133745413889756, -26.90304354338606174 ) ) ;
#33377=CARTESIAN_POINT ( 'NONE',  ( -55.01636684413512768, -59.99999999999999289, -36.85708210959909792 ) ) ;
#33379=CARTESIAN_POINT ( 'NONE',  ( 2.499999999999984457, -21.99834388059804269, -30.53959902372158908 ) ) ;
#33381=CARTESIAN_POINT ( 'NONE',  ( 102.6319757891835707, -60.18047993876283641, 193.3962675965070730 ) ) ;
#33382=CARTESIAN_POINT ( 'NONE',  ( 21.93725470949543421, -26.33177549557095176, 28.96246740876147641 ) ) ;
#33399=CARTESIAN_POINT ( 'NONE',  ( -41.14701979708251400, -57.68941641447864299, 57.58229189354211286 ) ) ;
#33405=CARTESIAN_POINT ( 'NONE',  ( 2.851859124854637884, -60.00000000000000711, -45.00000000000000711 ) ) ;
#33407=CARTESIAN_POINT ( 'NONE',  ( -28.84153870763153904, -30.00000000000004619, 39.52238898731670247 ) ) ;
#33408=CARTESIAN_POINT ( 'NONE',  ( -49.86947586418430234, -25.66521200955699555, 46.00621269778669387 ) ) ;
#33411=CARTESIAN_POINT ( 'NONE',  ( -98.41647369420755354, -52.79632805706295784, 194.9882854070544340 ) ) ;
#33415=CARTESIAN_POINT ( 'NONE',  ( 86.46411780683014570, -38.61740881457028962, 199.3064231678986005 ) ) ;
#33421=CARTESIAN_POINT ( 'NONE',  ( 85.94206644272870221, -30.00000000000000711, 178.2002489271057470 ) ) ;
#33422=B_SPLINE_SURFACE_WITH_KNOTS ( 'NONE', 3, 3, ( 
 ( #40, #30893, #23319, #105799, #82047, #33012, #73959, #73420, #97699, #48084, #56158, #98242, #31938 ),
 ( #65879, #47026, #48615, #98758, #106315, #80985, #32479, #80454, #49144, #8169, #41075, #64820, #24397 ),
 ( #57236, #7101, #23863, #89630, #71836, #88045, #39499, #6565, #14125, #79928, #6037, #104742, #38962 ),
 ( #63773, #96661, #22796, #55631, #88568, #14649, #72373, #105279, #90694, #99835, #83125, #41607, #59403 ),
 ( #85671, #82594, #61397, #37139, #25465, #66956, #19906, #69481, #42665, #11746, #102366, #28514, #75014 ),
 ( #34618, #12286, #24912, #42128, #1108, #53293, #9749, #50733, #44682, #8699, #16802, #78091, #26007 ),
 ( #94286, #34084, #91760, #20453, #58870, #26530, #17350, #77569, #57766, #50224, #49688, #74490, #86214 ),
 ( #45216, #17879, #9220, #67487, #75564, #83643, #3685, #100366, #1659, #99288, #4209, #92264, #52748 ),
 ( #36616, #70005, #565, #33533, #66405, #58317, #91242, #78609, #87789, #13337, #103432, #47825, #4740 ),
 ( #46787, #23064, #80729, #14933, #22548, #38712, #30097, #38201, #6305, #13872, #55390, #6847, #94829 ),
 ( #20976, #29582, #88319, #62453, #95345, #46264, #21480, #39772, #79680, #63519, #80201, #70541, #47305 ),
 ( #12813, #5275, #87262, #54316, #29070, #71060, #22006, #45728, #103952, #39245, #37680, #5790, #54860 ),
 ( #64054, #62981, #79149, #72120, #61939, #95882, #71577, #104483, #30630, #96417, #14393, #53809, #31170 ),
 ( #105029, #96929, #55903, #88839, #102905, #86739, #8967, #74760, #16009, #82332, #8442, #58604, #72646 ),
 ( #89898, #99570, #57511, #98510, #90974, #56448, #64572, #17621, #40808, #17085, #33813, #49962, #81257 ),
 ( #73702, #66689, #7371, #56983, #7902, #32211, #97986, #32754, #91507, #82870, #49428, #23600, #25749 ),
 ( #40282, #81779, #106060, #50482, #58052, #24659, #83394, #48365, #48885, #65089, #9491, #106604, #105548 ),
 ( #66149, #65628, #31686, #313, #73159, #24140, #90434, #16538, #15471, #97439, #89381, #41343, #99031 ),
 ( #74236, #33279, #25195, #41872, #840, #10566, #68835, #59138, #26801, #28395, #43482, #92020, #75298 ),
 ( #59672, #51013, #27881, #44012, #61268, #60223, #85002, #52618, #85546, #19263, #35965, #1391, #60746 ),
 ( #93091, #92553, #10040, #34358, #67233, #76358, #18701, #42947, #36496, #83929, #20328, #75838, #101185 ),
 ( #2471, #93634, #67754, #69364, #102243, #94158, #52091, #101714, #3013, #19785, #35419, #68290, #27346 ),
 ( #51557, #84471, #100641, #100111, #11086, #76900, #18156, #11626, #44556, #1936, #77443, #3558, #53173 ),
 ( #34887, #86090, #42403, #26276, #79558, #61817, #5672, #96299, #70421, #62336, #30505, #31049, #95231 ),
 ( #38084, #14280, #46146, #29465, #12688, #96816, #95751, #38591, #22423, #86625, #63405, #78492, #80079 ),
 ( #63929, #87670, #71458, #77972, #4089, #29978, #45093, #39121, #103317, #94710, #22948, #13218, #6187 ),
 ( #20859, #70941, #28943, #103833, #104357, #53692, #55268, #88194, #21362, #54202, #47178, #55783, #87141 ),
 ( #62866, #71999, #79032, #45620, #5151, #21893, #4623, #37553, #54734, #104911, #12162, #13749, #69885 ),
 ( #37017, #46660, #102781, #15350, #8844, #74103, #7778, #82740, #64452, #73034, #48235, #49836, #56859 ),
 ( #97325, #82198, #24016, #99438, #16412, #56315, #89252, #40683, #40158, #31571, #41749, #66557, #65503 ),
 ( #106472, #32089, #49292, #23478, #74637, #8314, #89780, #41217, #105431, #105944, #715, #15884, #81139 ),
 ( #48760, #81653, #90303, #66026, #193, #33157, #7248, #73570, #64966, #97858, #33685, #32630, #98392 ),
 ( #25615, #88720, #14811, #98904, #24541, #57391, #25064, #57922, #90842, #16959, #47707, #80606, #6730 ),
 ( #39653, #72524, #76771, #83794, #75166, #100515, #35831, #1259, #43354, #10438, #68156, #19660, #67637 ),
 ( #2874, #17498, #26670, #9906, #34226, #92961, #84345, #10960, #9361, #93512, #69239, #59010, #59549 ),
 ( #101592, #76238, #43876, #27748, #60622, #1804, #101051, #27207, #44420, #58475, #75710, #34763, #85411 ),
 ( #2347, #68711, #42275, #50359, #3428, #92416, #52491, #11493, #77315, #67099, #91380, #18569, #36371 ),
 ( #51431, #102111, #19121, #26154, #91899, #35286, #42814, #99982, #83272, #18024, #60096, #51959, #84875 ),
 ( #50888, #36891, #22292, #62733, #103188, #54598, #44964, #12561, #14147, #29332, #77846, #61139, #12036 ),
 ( #69758, #13620, #29855, #47050, #46016, #70816, #38467, #71334, #5023, #21763, #94028, #46535, #28270 ),
 ( #45498, #102653, #20189, #53043, #62222, #78366, #28811, #55138, #61692, #6060, #94583, #87015, #85962 ),
 ( #79428, #53569, #88068, #79950, #38987, #37956, #87539, #95621, #5541, #95106, #21241, #54074, #3960 ),
 ( #4489, #86500, #20731, #37425, #13087, #104227, #78897, #30375, #70291, #71861, #103708, #63265, #96160 ),
 ( #65375, #90179, #31962, #64841, #72912, #14672, #7122, #89122, #23342, #30916, #40037, #23886, #47580 ),
 ( #82073, #80475, #89653, #56731, #7645, #65900, #105821, #56183, #49165, #63797, #97721, #15221, #6591 ),
 ( #15753, #57257, #55655, #33034, #8721, #105302, #48636, #98266, #41100, #81521, #16282, #73981, #63 ),
 ( #40561, #73444, #90717, #104767, #48106, #81007, #24939, #106339, #32502, #8190, #88592, #96683, #49712 ),
 ( #98783, #57790, #16827, #39522, #22821, #24421, #82619, #41629, #72397, #31446, #64327, #97198, #66978 ),
 ( #74513, #99859, #66427, #91261, #2751, #10829, #43750, #91782, #58890, #10311, #92286, #26552, #59967 ),
 ( #67508, #42152, #35703, #51297, #50756, #68581, #26031, #9774, #42689, #76112, #51834, #68026, #27082 ),
 ( #59423, #17903, #75035, #19529, #50245, #75585, #18441, #101464, #52366, #93379, #100918, #43228, #1684 ),
 ( #84216, #92828, #85277, #99311, #18991, #11364, #2210, #60497, #35160, #84748, #76642, #27617, #590 ),
 ( #33555, #25483, #58339, #17372, #83663, #1133, #83147, #9244, #34640, #100390, #34107, #38346, #85833 ),
 ( #52911, #103063, #69110, #44838, #103580, #77724, #3835, #61555, #36768, #22156, #21121, #4896, #21634 ),
 ( #95490, #69634, #5421, #94452, #63130, #12960, #29731, #3297, #36241, #62091, #77186, #71206, #102526 ),
 ( #55006, #45361, #104101, #28670, #93906, #70158, #61019, #29218, #37828, #20061, #70691, #54465, #20607 ),
 ( #62604, #96030, #53446, #87416, #94983, #46414, #78243, #11908, #86367, #12432, #4356, #37292, #53952 ),
 ( #13492, #86887, #101983, #30242, #28142, #45882, #78762, #79301, #87938, #44291, #39912, #8055, #96561 ),
 ( #47453, #81936, #88992, #40969, #22694, #7514, #56055, #24807, #48509, #88470, #14544, #72785, #72270 ),
 ( #73857, #98656, #97585, #40432, #31832, #64202, #81402, #55531, #106751, #73311, #15090, #106206, #30787 ),
 ( #32901, #47977, #63671, #46926, #104635, #31320, #80346, #32370, #97071, #65243, #6460, #65776, #98134 ),
 ( #6994, #39394, #49039, #23755, #23217, #57659, #105174, #80883, #105691, #15620, #24285, #57134, #90045 ),
 ( #64715, #56603, #89526, #14019, #16151, #79825, #5931, #38858, #71723, #2622, #10185, #26425, #17770 ),
 ( #100787, #1548, #43098, #101337, #82490, #84083, #27491, #75986, #50624, #2083, #9114, #84622, #10706 ),
 ( #67380, #51163, #67900, #58208, #35036, #50115, #51703, #33970, #35570, #59290, #26949, #49581, #8590 ),
 ( #16690, #43621, #42024, #33429, #68443, #91654, #76514, #91133, #66302, #9642, #459, #42550, #59825 ),
 ( #92701, #18860, #74907, #66843, #90582, #41493, #99733, #74380, #75453, #99183, #83541, #25345, #991 ),
 ( #83022, #25902, #34512, #17243, #58759, #100261, #92164, #18311, #19405, #68983, #44706, #101858, #78630 ),
 ( #102393, #45753, #77052, #19935, #28017, #4763, #77593, #37704, #3168, #4231, #3713, #29605, #78115 ),
 ( #36113, #61423, #52777, #44164, #70569, #103454, #20479, #37166, #94316, #61962, #11238, #53319, #86237 ),
 ( #62477, #36640, #93776, #29094, #93241, #69506, #85696, #60887, #70027, #28543, #102927, #85146, #86767 ),
 ( #94853, #12311, #12834, #45238, #11774, #20997, #53834, #60366, #52238, #106231, #40452, #56072, #72804 ),
 ( #32391, #97093, #31340, #23776, #96050, #104119, #57154, #80369, #56623, #73332, #89545, #14039, #5440 ),
 ( #65263, #88489, #72288, #98152, #14565, #7015, #104655, #64734, #38362, #30807, #30264, #22178, #24308 ),
 ( #81422, #22714, #96580, #47998, #23235, #64222, #97611, #80904, #105194, #79846, #90067, #89015, #47473 ),
 ( #63692, #6483, #39413, #39932, #15638, #105712, #48530, #87960, #15110, #55552, #5952, #16174, #46945 ),
 ( #31853, #49059, #71226, #63153, #7535, #55027, #38877, #71746, #92180, #99752, #1567, #94203, #73876 ),
 ( #20372, #34529, #9133, #100281, #479, #77488, #3602, #36537, #91674, #67402, #42574, #26442, #42045 ),
 ( #43116, #25369, #102285, #50640, #59309, #40986, #106771, #25922, #8081, #69403, #81955, #9660, #49601 ),
 ( #33995, #33448, #24826, #28432, #61315, #58779, #75473, #17790, #58226, #18330, #90602, #32920, #51185 ),
 ( #84104, #98672, #66321, #65797, #83041, #57679, #16713, #82509, #99204, #8611, #10203, #83561, #41514 ),
 ( #66864, #91154, #74399, #17261, #50133, #74927, #1011, #80120, #31092, #72042, #79597, #95798, #87180 ),
 ( #63443, #70980, #5708, #63970, #45135, #46701, #96858, #38633, #13260, #71497, #78534, #47219, #6225 ),
 ( #62902, #104397, #13788, #30546, #46181, #79073, #21399, #69928, #62379, #37597, #4664, #86133, #95270 ),
 ( #102826, #54237, #96339, #28988, #38124, #5192, #21928, #14316, #103867, #70461, #22464, #12206, #30017 ),
 ( #61855, #87708, #54778, #55308, #4129, #88236, #53213, #53734, #39161, #104951, #78014, #37059, #94751 ),
 ( #20900, #103358, #86663, #12732, #45655, #29505, #90345, #40195, #49879, #7817, #48803, #41261, #6770 ),
 ( #74674, #97899, #74148, #90887, #232, #31608, #22985, #24055, #17002, #105980, #89822, #89296, #82784 ),
 ( #41791, #98431, #82244, #88757, #14854, #40726, #55820, #8886, #81178, #72565, #756, #56895, #33723 ),
 ( #105468, #81692, #39689, #73613, #16450, #64492, #49338, #33196, #7289, #73071, #66068, #66602, #32130 ),
 ( #106517, #25106, #15926, #97362, #65009, #32674, #15391, #48277, #65542, #47747, #24581, #80646, #57424 ),
 ( #23522, #8359, #56360, #98945, #57965, #18612, #93550, #75209, #83842, #26194, #60663, #67673, #19698 ),
 ( #93004, #34805, #3468, #27253, #67142, #100023, #51473, #50928, #42317, #52532, #77356, #76280, #19166 ),
 ( #42857, #60139, #1305, #85451, #52002, #100554, #84918, #9400, #9951, #11536, #26716, #34265, #25657 ),
 ( #75751, #59053, #11004, #101095, #44461, #10477, #35334, #2918, #35874, #2388, #43921, #58520, #76809 ),
 ( #43397, #1847, #91937, #91424, #17538, #59588, #92460, #18070, #36411, #84389, #99481, #68195, #68752 ),
 ( #101634, #27789, #50398, #83311, #86537, #69796, #47089, #46052, #29888, #46571, #36930, #13661, #78937 ),
 ( #62773, #54640, #103225, #29369, #37465, #86003, #78408, #53603, #94622, #102156, #4520, #95143, #12075 ),
 ( #79465, #45004, #54112, #21275, #5058, #30412, #70328, #20767, #5577, #28306, #62257, #12597, #77890 ),
 ( #87054, #21800, #20235, #104268, #79989, #102691, #13125, #95662, #38503, #37994, #87575, #71368, #63305 ),
 ( #70855, #96202, #22330, #103746, #55177, #45533, #88103, #14185, #6100, #69281, #53082, #61181, #94068 ),
 ( #4001, #28855, #61729, #102, #7159, #33071, #47615, #32539, #81046, #49749, #73479, #6635, #39561 ),
 ( #97238, #88626, #98820, #16870, #15792, #65411, #56767, #89159, #106378, #80516, #65939, #98306, #40071 ),
 ( #55695, #23383, #24975, #72950, #14715, #71907, #22858, #56220, #72436, #24459, #40597, #57826, #89692 ),
 ( #49208, #82107, #48673, #57295, #104808, #90215, #39024, #81557, #15263, #105338, #30957, #63834, #105858 ),
 ( #7684, #16318, #82655, #96723, #8228, #31483, #41139, #32000, #74020, #64365, #90751, #48146, #64874 ),
 ( #97760, #23927, #26590, #67546, #100956, #51338, #1722, #83181, #43786, #92328, #91817, #76679, #67014 ),
 ( #50794, #10347, #92863, #2245, #68064, #91294, #100424, #26067, #9280, #60529, #17406, #83701, #59460 ),
 ( #93413, #27655, #35195, #84251, #42727, #9809, #19030, #18474, #27115, #19565, #624, #60006, #52398 ),
 ( #75619, #51868, #34140, #2789, #35737, #68619, #43262, #84782, #76144, #10866, #34674, #101500, #8757 ),
 ( #17937, #99894, #58922, #41661, #74550, #33591, #25523, #66466, #99342, #58377, #50277, #42188, #75073 ),
 ( #1165, #4392, #102016, #37331, #45920, #28177, #78799, #62641, #36800, #28708, #103616, #104138, #61590 ),
 ( #70190, #87450, #12465, #20098, #69665, #20640, #44869, #3870, #45398, #5457, #95019, #38378, #29248 ),
 ( #44326, #52942, #94486, #11942, #71241, #70723, #103099, #79336, #61051, #102562, #77758, #46448, #53480 ),
 ( #93943, #4932, #86402, #96064, #12995, #85870, #78276, #62128, #21154, #53983, #30283, #63170, #86924 ),
 ( #37864, #29764, #95527, #22196, #21672, #54505, #13531, #85316, #11401, #77222, #3334, #36278, #69149 ),
 ( #15129, #81973, #64754, #8094, #105726, #16188, #14057, #22730, #64236, #88505, #41004, #40467, #80923 ),
 ( #30825, #39432, #14581, #49075, #23250, #73891, #63710, #48549, #97108, #65809, #89560, #55568, #47491 ),
 ( #6496, #104673, #102441, #32939, #31870, #81438, #72822, #105212, #15656, #96597, #98687, #7553, #56092 ),
 ( #80387, #90084, #97626, #31359, #55047, #72306, #89029, #48013, #56641, #32407, #73349, #106247, #7034 ),
 ( #39949, #23792, #87976, #65279, #98170, #24324, #46961, #79859, #5967, #57172, #38897, #71761, #66880 ),
 ( #18896, #66336, #2654, #33462, #83570, #49617, #25384, #84121, #58241, #91172, #42058, #17276, #35605 ),
 ( #92193, #2116, #99220, #76017, #50151, #92738, #74944, #43655, #100294, #10220, #90622, #16727, #42588 ),
 ( #51739, #83058, #74418, #68480, #25936, #84656, #9149, #493, #50654, #41528, #9678, #18347, #1034 ),
 ( #35067, #34008, #82526, #51200, #24841, #43132, #58795, #67935, #99767, #10741, #76544, #57693, #34543 ),
 ( #100818, #26986, #91690, #17803, #75487, #1582, #67417, #26456, #59321, #8627, #59864, #20514, #11268 ),
 ( #78665, #44201, #86270, #53350, #4267, #62515, #3747, #19964, #45786, #60401, #69539, #52812, #77087 ),
 ( #12343, #53868, #52269, #29640, #5335, #101892, #36677, #94888, #37738, #45270, #86798, #70599, #103490 ),
 ( #37195, #95398, #21539, #78147, #61998, #11808, #54372, #70063, #102964, #12869, #85182, #93279, #46320 ),
 ( #4799, #87318, #13397, #3206, #101371, #102430, #79211, #77626, #61460, #38257, #28572, #29128, #93809 ),
 ( #27524, #85736, #19439, #36147, #69017, #28050, #60922, #44741, #94352, #21032, #88899, #23129, #56511 ),
 ( #87848, #55448, #57042, #72186, #13929, #104008, #54922, #88381, #79741, #89441, #72705, #89959, #14997 ),
 ( #14455, #71635, #16064, #46841, #39305, #47886, #98047, #48947, #81843, #97497, #6907, #105090, #6368 ),
 ( #80795, #23660, #7963, #80256, #47367, #96473, #30153, #31230, #96993, #5845, #64118, #48424, #38770 ),
 ( #55969, #39828, #32277, #105604, #22611, #15531, #63038, #31746, #64630, #104545, #81315, #7427, #40343 ),
 ( #106121, #71119, #30695, #73221, #65148, #24196, #95941, #22063, #63582, #43011, #91042, #50540, #34945 ),
 ( #91569, #1459, #58116, #67816, #25814, #66754, #59202, #24720, #32812, #92612, #9025, #92078, #1997 ),
 ( #49492, #40877, #41934, #100696, #17150, #901, #75900, #50023, #42464, #33342, #100172, #73764, #66210 ),
 ( #57567, #26866, #83994, #10099, #82928, #25255, #83455, #58668, #99639, #26341, #9556, #33876, #8501 ),
 ( #17677, #74820, #59734, #99092, #75359, #34422, #67294, #18221, #51073, #18770, #16601, #51617, #84538 ),
 ( #106662, #82396, #65684, #98572, #90492, #41404, #74295, #372, #53230, #44617, #52679, #20917, #28453 ),
 ( #95286, #19322, #69421, #35481, #11147, #69944, #44076, #76960, #27935, #3077, #21415, #94221, #78031 ),
 ( #85065, #61873, #36023, #78553, #61333, #37078, #54255, #2536, #4148, #10623, #102840, #77506, #29009 ),
 ( #4681, #37615, #70478, #20388, #94768, #53750, #86679, #3620, #36553, #85609, #27406, #19843, #101771 ),
 ( #43542, #11683, #102304, #60284, #86150, #12750, #93153, #12220, #45150, #45671, #103374, #29521, #68897 ),
 ( #76422, #62392, #60800, #52150, #68353, #101253, #93693, #38141, #16886, #99358, #87725, #22483, #80663 ),
 ( #21942, #71515, #55324, #46718, #5725, #47237, #8775, #96868, #41678, #31105, #49766, #46201, #54795 ),
 ( #13806, #74568, #72580, #6239, #82670, #62921, #104415, #79610, #641, #88251, #33608, #95815, #6783 ),
 ( #25540, #14868, #38649, #30560, #39175, #63459, #30032, #66481, #87195, #63989, #39703, #104962, #96352 ),
 ( #14331, #13273, #47759, #80137, #118, #103885, #72057, #79087, #23002, #55838, #5210, #70994, #88776 ),
 ( #33089, #65953, #98833, #24990, #57842, #90769, #101513, #35211, #51884, #91310, #76695, #58399, #2262 ),
 ( #84801, #100974, #92343, #100445, #68637, #19046, #1183, #10886, #35757, #9826, #1736, #2806, #77237 ),
 ( #27672, #84267, #60544, #18491, #99911, #42742, #26603, #17951, #83717, #51355, #85332, #68082, #11417 ),
 ( #19585, #17420, #26080, #67563, #91831, #44343, #43800, #10363, #52414, #34153, #75634, #50813, #3354 ) ),
 .UNSPECIFIED., .F., .F., .F.,
 ( 4, 3, 3, 3, 3, 3, 3, 3, 3, 3, 3, 3, 3, 3, 3, 3, 3, 3, 3, 3, 3, 3, 3, 3, 3, 3, 3, 3, 3, 3, 3, 3, 3, 3, 3, 3, 3, 3, 3, 3, 3, 3, 3, 3, 3, 3, 3, 3, 3, 3, 3, 4 ),
 ( 4, 3, 3, 3, 4 ),
 ( -1.110223024625156540E-16, 0.002843925521740953144, 0.005687851043482017310, 0.008531776565223081477, 0.01137570208696414564, 0.01421962760870520981, 0.01706355313044627398, 0.01990747865218733814, 0.02275140417392840231, 0.02417336693479893439, 0.02559532969566946647, 0.02701729245653999856, 0.02772827383697526460, 0.02843925521741053064, 0.03128318073915159481, 0.03412710626089265897, 0.03697103178263372314, 0.03981495730437478731, 0.04265888282611585147, 0.04408084558698638356, 0.04550280834785691564, 0.04834673386959797980, 0.05119065939133904397, 0.05403458491308010814, 0.05687851043482117230, 0.06256636147830330064, 0.06825421252178542897, 0.07394206356526755730, 0.07678598908700862147, 0.07962991460874968563, 0.09100561669571394230, 0.1137570208696424556, 0.1251327229566067123, 0.1365084250435709690, 0.1421962760870530973, 0.1478841271305352256, 0.1535719781740173540, 0.1592598292174994823, 0.1621037547392405465, 0.1635257175001110785, 0.1649476802609816106, 0.1677916057827226748, 0.1706355313044637390, 0.1720574940653342710, 0.1734794568262048031, 0.1749014195870753352, 0.1756124009675106012, 0.1763233823479458673, 0.1791673078696869315, 0.1798782892501221975, 0.1805892706305574635, 0.1820112333914279956 ),
 ( 0.03187303615303928306, 0.3799792527701029710, 0.7280854693871666727, 1.076191686004230430, 1.424297902621294076 ),
 .UNSPECIFIED. ) ;
#33429=CARTESIAN_POINT ( 'NONE',  ( 52.04862490863282432, -49.90435108743835002, 58.16575394986750069 ) ) ;
#33433=CARTESIAN_POINT ( 'NONE',  ( -90.63796294261014452, -38.34935958327475447, 15.74237372901285070 ) ) ;
#33436=CARTESIAN_POINT ( 'NONE',  ( 92.51741348077821669, -38.35456167585839893, 39.42312903733464680 ) ) ;
#33438=CARTESIAN_POINT ( 'NONE',  ( 87.71464298479139643, -60.14869002622434380, 36.80113247628132456 ) ) ;
#33440=FACE_BOUND ( 'NONE', #67697, .T. ) ;
#33444=CARTESIAN_POINT ( 'NONE',  ( 75.19059096504483364, -59.99999999999999289, 182.6202054854667836 ) ) ;
#33445=( GEOMETRIC_REPRESENTATION_CONTEXT ( 3 ) GLOBAL_UNCERTAINTY_ASSIGNED_CONTEXT ( ( #67095 ) ) GLOBAL_UNIT_ASSIGNED_CONTEXT ( ( #4598, #35401, #60725 ) ) REPRESENTATION_CONTEXT ( 'NONE', 'WORKASPACE' ) );
#33446=DIRECTION ( 'NONE',  ( 0.000000000000000000, -1.000000000000000000, 0.000000000000000000 ) ) ;
#33448=CARTESIAN_POINT ( 'NONE',  ( 60.20930824510026014, -56.86133611672916999, 81.16955359436684603 ) ) ;
#33452=CARTESIAN_POINT ( 'NONE',  ( -90.13693044984590585, -38.39872991106614109, -15.64445292063840576 ) ) ;
#33462=CARTESIAN_POINT ( 'NONE',  ( 82.63019022871336006, -50.02483195698248863, 181.3254256235556170 ) ) ;
#33467=CIRCLE ( 'NONE', #52444, 8.000000000000000000 ) ;
#33473=STYLED_ITEM ( 'NONE', ( #105084 ), #16991 ) ;
#33474=CARTESIAN_POINT ( 'NONE',  ( 55.93715591288651723, -60.00000000000000711, 87.98903091118835107 ) ) ;
#33476=CARTESIAN_POINT ( 'NONE',  ( 12.22201992443273966, -14.34686031290847907, 31.77896201686625943 ) ) ;
#33477=CARTESIAN_POINT ( 'NONE',  ( -12.15630314080767960, -21.19743429706114313, 35.58279596609094853 ) ) ;
#33487=CARTESIAN_POINT ( 'NONE',  ( 47.71644133373404628, -47.40887823659345202, -30.35360365216715550 ) ) ;
#33493=ORIENTED_EDGE ( 'NONE', *, *, #69525, .F. ) ;
#33498=CARTESIAN_POINT ( 'NONE',  ( -98.78051181877384579, -59.99999999999999289, 73.70903175910844141 ) ) ;
#33507=CARTESIAN_POINT ( 'NONE',  ( -81.84813229431372861, -49.96181332713019430, 175.6604539455789222 ) ) ;
#33525=CARTESIAN_POINT ( 'NONE',  ( 109.4307067020638726, -30.00000000000001066, 166.0292171922573345 ) ) ;
#33527=CARTESIAN_POINT ( 'NONE',  ( -106.9593936918335544, -14.21045842199438880, 171.9682640579732436 ) ) ;
#33528=CARTESIAN_POINT ( 'NONE',  ( -58.81820099218335685, -42.96702668141021064, 70.77761850075783912 ) ) ;
#33531=CARTESIAN_POINT ( 'NONE',  ( 94.67678376100681703, -60.00000000000000000, 24.26864735211880486 ) ) ;
#33533=CARTESIAN_POINT ( 'NONE',  ( 8.254048633541648528, -49.91580099947954352, 32.20254773541059024 ) ) ;
#33534=CARTESIAN_POINT ( 'NONE',  ( -104.9716744181120305, -52.71025089284185583, 163.4601265114661715 ) ) ;
#33540=CARTESIAN_POINT ( 'NONE',  ( -75.93880995127246081, -59.99999999999997868, 186.8032436320886518 ) ) ;
#33554=CARTESIAN_POINT ( 'NONE',  ( -33.65812250636221137, -42.96608556679607460, 35.30899569834211604 ) ) ;
#33555=CARTESIAN_POINT ( 'NONE',  ( 46.36249026935708173, -60.26199203029697316, 51.31417678178487307 ) ) ;
#33559=CARTESIAN_POINT ( 'NONE',  ( -78.45636384825381526, -38.62886288010908231, 189.5596485861315159 ) ) ;
#33570=CARTESIAN_POINT ( 'NONE',  ( 111.0056519548954128, -60.00000000000002132, 152.1919057739970924 ) ) ;
#33576=CARTESIAN_POINT ( 'NONE',  ( -99.06500401421689617, -29.99999999999995026, 188.7035041724194286 ) ) ;
#33591=CARTESIAN_POINT ( 'NONE',  ( 82.39176465435255636, -42.97103400991685618, 169.7411559209277243 ) ) ;
#33600=CARTESIAN_POINT ( 'NONE',  ( -40.85164678844374464, -60.00000000000000000, -33.69328355261731645 ) ) ;
#33608=CARTESIAN_POINT ( 'NONE',  ( 86.79046891330465030, -24.35748604248244220, 185.5599931926667523 ) ) ;
#33627=CARTESIAN_POINT ( 'NONE',  ( 99.73478044767607287, -57.67101520680783011, 67.37346591704599064 ) ) ;
#33632=CARTESIAN_POINT ( 'NONE',  ( -76.16011686981150319, -60.00000000000001421, 187.6210859576851249 ) ) ;
#33635=CARTESIAN_POINT ( 'NONE',  ( -83.65499586678340904, -50.13462276898575709, 185.8592676192767783 ) ) ;
#33644=CARTESIAN_POINT ( 'NONE',  ( -84.48354631104164980, -45.26985310514864835, -5.680659070506059116 ) ) ;
#33651=ADVANCED_FACE ( 'NONE', ( #33440, #84096 ), #43634, .F. ) ;
#33655=CARTESIAN_POINT ( 'NONE',  ( 16.60915088697842990, -29.99999999999996092, -39.45628980158949162 ) ) ;
#33656=CARTESIAN_POINT ( 'NONE',  ( -75.71675511854569152, -53.37976804700807776, 134.7001851824688856 ) ) ;
#33658=CARTESIAN_POINT ( 'NONE',  ( 71.28669324481667502, -60.00000000000002132, 168.6228882893990715 ) ) ;
#33660=CARTESIAN_POINT ( 'NONE',  ( 93.90460291926041236, -57.67583523855721950, 7.672568471264877843 ) ) ;
#33685=CARTESIAN_POINT ( 'NONE',  ( 29.71491464515361969, -25.59252497190302122, 30.54298176171112544 ) ) ;
#33692=FACE_OUTER_BOUND ( 'NONE', #1892, .T. ) ;
#33698=CARTESIAN_POINT ( 'NONE',  ( 79.32333215263945192, -60.00000000000000711, -28.32974529982569578 ) ) ;
#33712=CARTESIAN_POINT ( 'NONE',  ( 86.78697920443168812, -60.15489657647691502, -1.591601715208872836 ) ) ;
#33723=CARTESIAN_POINT ( 'NONE',  ( 67.38364752544607938, -18.62895086270174616, 82.15773094806566235 ) ) ;
#33728=CARTESIAN_POINT ( 'NONE',  ( -113.8744714263418842, -57.67115484533559311, 181.1306260539751918 ) ) ;
#33734=CARTESIAN_POINT ( 'NONE',  ( 105.9254696489590089, -60.15131266928262477, 182.9954770859043833 ) ) ;
#33754=CARTESIAN_POINT ( 'NONE',  ( 7.961919226131998428, -60.00000000000000711, 39.63277225375871637 ) ) ;
#33755=CARTESIAN_POINT ( 'NONE',  ( -95.56182489229684052, -29.99999999999999645, 191.3238752510769700 ) ) ;
#33759=CARTESIAN_POINT ( 'NONE',  ( 69.93972929822530205, -57.68247516750832915, 153.7333845119171940 ) ) ;
#33762=CARTESIAN_POINT ( 'NONE',  ( 13.62955596626466992, -23.64027760696375324, -38.53637356313394946 ) ) ;
#33765=CARTESIAN_POINT ( 'NONE',  ( -43.49728549343999617, -59.99999999999999289, 57.75799430402353352 ) ) ;
#33769=CARTESIAN_POINT ( 'NONE',  ( -86.58000157545598086, -16.99658149479392222, 184.8764613376573038 ) ) ;
#33772=CARTESIAN_POINT ( 'NONE',  ( -10.26648064962001605, -39.47613848608923348, 30.48065965013316969 ) ) ;
#33788=CARTESIAN_POINT ( 'NONE',  ( 112.8608516834554649, -60.00000000000000000, 189.7942083920301855 ) ) ;
#33810=CARTESIAN_POINT ( 'NONE',  ( 108.1941172262546331, -60.00000000000000000, 195.3107487755136162 ) ) ;
#33812=CARTESIAN_POINT ( 'NONE',  ( -86.32002947858198638, -29.99999999999988987, 198.0868106477030892 ) ) ;
#33813=CARTESIAN_POINT ( 'NONE',  ( 14.34223220226681050, -25.54896781464430688, 28.25844851971035965 ) ) ;
#33817=CARTESIAN_POINT ( 'NONE',  ( -40.18246394402392951, -39.52194550917157301, 38.87972210423134101 ) ) ;
#33822=CARTESIAN_POINT ( 'NONE',  ( 0.000000000000000000, -8.000000000000000000, 0.000000000000000000 ) ) ;
#33834=CARTESIAN_POINT ( 'NONE',  ( 47.39620038011970138, -30.00000000026522784, 59.33786523996079865 ) ) ;
#33840=CARTESIAN_POINT ( 'NONE',  ( 81.10868664982288578, -29.99999999999999645, 22.89651086349327258 ) ) ;
#33857=CARTESIAN_POINT ( 'NONE',  ( 74.25335412531610757, -38.32804716266574019, 162.5607055868849500 ) ) ;
#33876=CARTESIAN_POINT ( 'NONE',  ( 86.34082203149947077, -21.01137834141258409, 180.7326751960264630 ) ) ;
#33882=CARTESIAN_POINT ( 'NONE',  ( 94.66746555106050209, -57.65776586346519395, -9.025452738816129639 ) ) ;
#33883=FACE_OUTER_BOUND ( 'NONE', #8610, .T. ) ;
#33887=CARTESIAN_POINT ( 'NONE',  ( -80.92579118157559037, -29.99999999999999645, 5.338923669854157339 ) ) ;
#33906=CARTESIAN_POINT ( 'NONE',  ( 69.77959388908855942, -29.97820759226561194, -20.83712817169497811 ) ) ;
#33913=CARTESIAN_POINT ( 'NONE',  ( -61.99390519559347013, -29.47934043886439071, -24.25302986929749949 ) ) ;
#33922=CARTESIAN_POINT ( 'NONE',  ( -88.11432633863014985, -59.99999999999999289, -21.44888580323229377 ) ) ;
#33926=CARTESIAN_POINT ( 'NONE',  ( 102.2338188462963871, -60.19688077974823415, 193.9243752497099536 ) ) ;
#33942=CARTESIAN_POINT ( 'NONE',  ( -11.27550409577679247, -60.00000000000000000, -44.73582912082186169 ) ) ;
#33948=CARTESIAN_POINT ( 'NONE',  ( -86.99605493950913626, -14.21045842199422005, 24.11595694609475160 ) ) ;
#33951=CARTESIAN_POINT ( 'NONE',  ( -49.62087710221392456, -39.51757389364818351, 50.13317839744063065 ) ) ;
#33957=ORIENTED_EDGE ( 'NONE', *, *, #42907, .F. ) ;
#33960=CARTESIAN_POINT ( 'NONE',  ( 104.6430114620182081, -38.40051020932904180, 197.8370924372202637 ) ) ;
#33964=CARTESIAN_POINT ( 'NONE',  ( 89.31065340740984482, -30.00000000000000000, 189.1380160600958789 ) ) ;
#33970=CARTESIAN_POINT ( 'NONE',  ( 51.98390228014496728, -36.04151142941384478, 52.98091492913632550 ) ) ;
#33975=CARTESIAN_POINT ( 'NONE',  ( -92.63712589027728939, -38.35495981404815069, 40.41764578554981568 ) ) ;
#33979=CARTESIAN_POINT ( 'NONE',  ( 92.04444232229207046, -38.35407781392872550, 35.16507766400177815 ) ) ;
#33982=CARTESIAN_POINT ( 'NONE',  ( 89.89243487226349316, -52.71666739316034977, 62.30352106449856109 ) ) ;
#33989=CARTESIAN_POINT ( 'NONE',  ( 76.53976976327565751, -60.00000000000000000, 189.0222597737091803 ) ) ;
#33995=CARTESIAN_POINT ( 'NONE',  ( 60.00046932338042893, -60.33652138363083850, 82.29518702760771021 ) ) ;
#34008=CARTESIAN_POINT ( 'NONE',  ( 82.38523181566540643, -57.17260357990272723, 186.5832430736296885 ) ) ;
#34017=CARTESIAN_POINT ( 'NONE',  ( -18.64535684107481472, -25.34425824956045048, -38.50098957481070983 ) ) ;
#34021=CARTESIAN_POINT ( 'NONE',  ( 50.11026576053689752, -60.00000000000000000, 72.06894001542156047 ) ) ;
#34023=CARTESIAN_POINT ( 'NONE',  ( 19.18487022566833033, -16.76851763133264583, 31.49200998272180030 ) ) ;
#34026=CARTESIAN_POINT ( 'NONE',  ( -25.34519795292129629, -29.27581004272202136, 38.40335314319461446 ) ) ;
#34039=CARTESIAN_POINT ( 'NONE',  ( 50.18622294521377114, -34.58945973367626436, -27.70670043957319706 ) ) ;
#34048=CARTESIAN_POINT ( 'NONE',  ( -103.7179628943768535, -60.00000000000000711, 102.7867851543608140 ) ) ;
#34057=CARTESIAN_POINT ( 'NONE',  ( -83.14853206027666488, -39.48440948074397738, 171.2778937662942838 ) ) ;
#34069=( NAMED_UNIT ( * ) PLANE_ANGLE_UNIT ( ) SI_UNIT ( $, .RADIAN. ) );
#34076=CARTESIAN_POINT ( 'NONE',  ( 99.06540890750190442, -59.99999999999989342, 60.62284496578245552 ) ) ;
#34077=CARTESIAN_POINT ( 'NONE',  ( -114.4520492995273315, -60.00000000000003553, 166.3968728284598342 ) ) ;
#34078=CARTESIAN_POINT ( 'NONE',  ( -59.78161821688770061, -25.59841304440983478, 65.24320542831817704 ) ) ;
#34082=CARTESIAN_POINT ( 'NONE',  ( 109.3871879777513669, -60.00000000001244871, 197.8688627231219073 ) ) ;
#34084=CARTESIAN_POINT ( 'NONE',  ( 6.205941524835793643, -56.87779645166712328, 33.35922039782534654 ) ) ;
#34085=CARTESIAN_POINT ( 'NONE',  ( -106.0491298257543775, -60.15510293424402732, 161.1420266926477325 ) ) ;
#34092=CARTESIAN_POINT ( 'NONE',  ( -75.18318468975571989, -59.99999999999997868, 182.6337824465098834 ) ) ;
#34098=CARTESIAN_POINT ( 'NONE',  ( 16.90652009647421394, -0.000000000000000000, 2.220657265755147325 ) ) ;
#34104=CARTESIAN_POINT ( 'NONE',  ( -28.78195043134853037, -18.63874505867011777, 29.02999481432414797 ) ) ;
#34107=CARTESIAN_POINT ( 'NONE',  ( 46.21019612037324009, -25.69888004963982908, 41.24161030058627375 ) ) ;
#34112=CARTESIAN_POINT ( 'NONE',  ( -76.71984652716008668, -38.43189599304911752, 182.9491387776208171 ) ) ;
#34116=CARTESIAN_POINT ( 'NONE',  ( 55.18499737084820111, -59.99999999999997158, 69.25531299354273074 ) ) ;
#34122=CARTESIAN_POINT ( 'NONE',  ( 108.8577760144673761, -60.00000000000000711, 134.9695025774865940 ) ) ;
#34127=CARTESIAN_POINT ( 'NONE',  ( -86.67473478203353920, -30.00000000000003908, 182.4036165407476631 ) ) ;
#34140=CARTESIAN_POINT ( 'NONE',  ( 80.87394805517843110, -53.40757338515430774, 172.1382403962514331 ) ) ;
#34153=CARTESIAN_POINT ( 'NONE',  ( 87.29183096894618643, -28.00114413134319946, 187.7157000835711642 ) ) ;
#34170=CARTESIAN_POINT ( 'NONE',  ( 110.1281201688277918, -57.67139407212744118, 129.8419390022934294 ) ) ;
#34178=CARTESIAN_POINT ( 'NONE',  ( -79.65127760519116862, -60.00000000000001421, 195.5387530500997855 ) ) ;
#34184=CARTESIAN_POINT ( 'NONE',  ( -86.22339662976257557, -21.27558923800543056, 177.9722882754944067 ) ) ;
#34190=CARTESIAN_POINT ( 'NONE',  ( -87.01690208926603987, -60.20973691192937594, -8.193354508930786650 ) ) ;
#34201=CARTESIAN_POINT ( 'NONE',  ( 35.94918560889485093, -14.21045842199434439, 40.02951443902858841 ) ) ;
#34203=CARTESIAN_POINT ( 'NONE',  ( -57.68513734192992359, -30.00000000000002487, -33.51766283710919225 ) ) ;
#34204=CARTESIAN_POINT ( 'NONE',  ( -67.76884453457680024, -32.53527454055805634, 90.78174967798416617 ) ) ;
#34206=CARTESIAN_POINT ( 'NONE',  ( 70.85242353449750397, -59.99999999999999289, 164.3672743468505359 ) ) ;
#34208=CARTESIAN_POINT ( 'NONE',  ( 94.10310489044364601, -57.65276993155347895, -13.84278669819006247 ) ) ;
#34226=CARTESIAN_POINT ( 'NONE',  ( 32.30811475795603371, -46.43045952615185712, 35.30348012445732309 ) ) ;
#34243=CARTESIAN_POINT ( 'NONE',  ( 92.73630845656811061, -59.99999999999999289, -6.105622175954798614 ) ) ;
#34256=CARTESIAN_POINT ( 'NONE',  ( 87.00105230417793223, -60.21000100938282884, -8.688507030231054529 ) ) ;
#34265=CARTESIAN_POINT ( 'NONE',  ( 76.54894832708983188, -22.13291403085647602, 114.5410150515899943 ) ) ;
#34270=CARTESIAN_POINT ( 'NONE',  ( -111.7589076751911392, -57.67119524614439285, 141.4413276519820784 ) ) ;
#34275=CARTESIAN_POINT ( 'NONE',  ( 103.7274724878040928, -45.28268791833052376, 163.4000004519256208 ) ) ;
#34278=PLANE ( 'NONE',  #101232 ) ;
#34296=CARTESIAN_POINT ( 'NONE',  ( -89.78872880365601361, -30.00000000000000711, 189.6862794871168774 ) ) ;
#34301=CARTESIAN_POINT ( 'NONE',  ( 72.83774066108748002, -57.65622831221423183, 179.9088005362346792 ) ) ;
#34306=CARTESIAN_POINT ( 'NONE',  ( 24.88129734378813751, -27.66378606029807585, -38.37538378080514434 ) ) ;
#34309=CARTESIAN_POINT ( 'NONE',  ( -45.08300348252168277, -60.00000000000001421, 60.74044995775830103 ) ) ;
#34313=CARTESIAN_POINT ( 'NONE',  ( -85.89194148627102265, -42.88414227571757209, 188.0209850057943015 ) ) ;
#34316=CARTESIAN_POINT ( 'NONE',  ( -7.155724036906063290, -42.95763110478070246, 31.03959182391562521 ) ) ;
#34334=CARTESIAN_POINT ( 'NONE',  ( 108.4360931436784767, -30.00000000000001066, 186.7338794867829677 ) ) ;
#34335=CARTESIAN_POINT ( 'NONE',  ( -79.83446298086737158, -46.43891928859385843, 152.6746585543230026 ) ) ;
#34356=CARTESIAN_POINT ( 'NONE',  ( 102.7236711658890158, -59.99999999999997868, 200.7889012320235622 ) ) ;
#34357=CARTESIAN_POINT ( 'NONE',  ( -94.36268555338997999, -29.99999999999996803, 200.0833938634536935 ) ) ;
#34358=CARTESIAN_POINT ( 'NONE',  ( 21.59831149744555390, -49.91455128373721095, 32.92735310832569695 ) ) ;
#34363=CARTESIAN_POINT ( 'NONE',  ( -39.81795437584664654, -53.34937766137575466, 41.56781054599359493 ) ) ;
#34377=CARTESIAN_POINT ( 'NONE',  ( 81.05248856670681334, -30.00000000000004619, -11.71509379367667414 ) ) ;
#34381=CARTESIAN_POINT ( 'NONE',  ( 83.01728599698354572, -30.00000000000000000, 43.06514241403382215 ) ) ;
#34393=VERTEX_POINT ( 'NONE', #56391 ) ;
#34397=CARTESIAN_POINT ( 'NONE',  ( 61.83185530181933132, -38.34112017042167508, 102.3246735217670675 ) ) ;
#34422=CARTESIAN_POINT ( 'NONE',  ( 85.48307987227248361, -42.91479745304676641, 187.0500961933685744 ) ) ;
#34426=CARTESIAN_POINT ( 'NONE',  ( 94.39065875124650518, -57.65262801469535248, -12.18580112889518041 ) ) ;
#34430=ADVANCED_FACE ( 'NONE', ( #72069 ), #50963, .T. ) ;
#34432=CARTESIAN_POINT ( 'NONE',  ( -83.18484191182862730, -30.00000000000000711, 44.38092683156298079 ) ) ;
#34444=CARTESIAN_POINT ( 'NONE',  ( -61.22706150350772702, -37.51812599910320500, -25.43655289629557004 ) ) ;
#34447=CARTESIAN_POINT ( 'NONE',  ( 39.44553997851354410, -24.70023121783347264, -30.40899877233305304 ) ) ;
#34448=CARTESIAN_POINT ( 'NONE',  ( -23.00482107871162185, -56.87968423956402120, 34.33352247912110755 ) ) ;
#34453=CARTESIAN_POINT ( 'NONE',  ( -63.89019755539457179, -29.65979330600327302, -23.51777689157650642 ) ) ;
#34454=CARTESIAN_POINT ( 'NONE',  ( -67.20361504359703986, -47.40886506081861995, -25.20267518921325589 ) ) ;
#34458=VERTEX_POINT ( 'NONE', #9434 ) ;
#34463=CARTESIAN_POINT ( 'NONE',  ( -81.47805564997403849, -59.99999999999999289, -27.03802318630214430 ) ) ;
#34467=CARTESIAN_POINT ( 'NONE',  ( 98.52377646302282699, -37.77507002369925715, 192.2321652874637152 ) ) ;
#34484=CARTESIAN_POINT ( 'NONE',  ( -68.42433815231228778, -57.68192485334662933, 143.8276693603407068 ) ) ;
#34489=CARTESIAN_POINT ( 'NONE',  ( -94.85933876937251341, -60.00000000000005684, 26.66572952598730595 ) ) ;
#34490=CARTESIAN_POINT ( 'NONE',  ( -51.21545289590059724, -22.18992440698552215, 46.87729257222688517 ) ) ;
#34502=CARTESIAN_POINT ( 'NONE',  ( 106.0128498860127877, -38.37620446819514086, 196.3282179351167258 ) ) ;
#34507=CARTESIAN_POINT ( 'NONE',  ( 89.25784830564948891, -29.99999999999999645, 189.0691493792201925 ) ) ;
#34512=CARTESIAN_POINT ( 'NONE',  ( 52.87357985501328983, -53.37229541906862806, 61.20433885443490141 ) ) ;
#34517=CARTESIAN_POINT ( 'NONE',  ( -90.76089875232968041, -38.34354976312844343, 6.139603795565712119 ) ) ;
#34520=CARTESIAN_POINT ( 'NONE',  ( 110.6797206184853621, -38.35606018631307990, 162.8134989819215832 ) ) ;
#34522=CARTESIAN_POINT ( 'NONE',  ( 89.59839892097701863, -60.15026689961409545, 51.75009883440984026 ) ) ;
#34529=CARTESIAN_POINT ( 'NONE',  ( 58.77986657205519805, -56.85775167507390648, 77.19278662003875979 ) ) ;
#34533=CARTESIAN_POINT ( 'NONE',  ( -80.00000000000000000, -60.00000000000000000, -23.09707704303352926 ) ) ;
#34539=CARTESIAN_POINT ( 'NONE',  ( -31.69663852278251781, -22.50060937418604112, 32.41930772561958207 ) ) ;
#34540=VECTOR ( 'NONE', #43958, 1000.000000000000000 ) ;
#34543=CARTESIAN_POINT ( 'NONE',  ( 86.34230506928878413, -18.09223085222674143, 171.9728401114309975 ) ) ;
#34552=CARTESIAN_POINT ( 'NONE',  ( -40.34222971095775989, -33.04913957068288255, -37.41736829041874302 ) ) ;
#34557=CARTESIAN_POINT ( 'NONE',  ( 43.68292435923753914, -60.00000000000001421, 58.09727205077876278 ) ) ;
#34559=CARTESIAN_POINT ( 'NONE',  ( 14.05888324584411109, -14.89647871732337592, 31.68400523270869229 ) ) ;
#34560=CARTESIAN_POINT ( 'NONE',  ( -32.95192556782836846, -34.33711306273711727, 42.52861473283787319 ) ) ;
#34569=CARTESIAN_POINT ( 'NONE',  ( 31.39943587937961311, -30.09334884167371271, -38.12009580904052086 ) ) ;
#34575=CARTESIAN_POINT ( 'NONE',  ( 35.59138712027602480, -60.22815789036102530, -34.49238072042346914 ) ) ;
#34586=CARTESIAN_POINT ( 'NONE',  ( -103.8364008283201940, -59.99999999999998579, 103.4830970040553666 ) ) ;
#34592=CARTESIAN_POINT ( 'NONE',  ( -85.96019084596983362, -18.45086501588650307, 165.1132801238956063 ) ) ;
#34610=CARTESIAN_POINT ( 'NONE',  ( 99.88996038257948840, -14.21045842199439946, 111.7630621600675198 ) ) ;
#34611=CARTESIAN_POINT ( 'NONE',  ( -97.75001763179835734, -59.99999999999991473, 204.9118596629033675 ) ) ;
#34612=CARTESIAN_POINT ( 'NONE',  ( -57.77607850381885157, -32.55063884621782933, 63.57510918078556017 ) ) ;
#34615=CARTESIAN_POINT ( 'NONE',  ( 2.377971214860273304E-07, -59.99999999999998579, 39.63907915656436387 ) ) ;
#34618=CARTESIAN_POINT ( 'NONE',  ( 5.174065430531224585, -60.35881594324177968, 33.93881697174609258 ) ) ;
#34619=CARTESIAN_POINT ( 'NONE',  ( -101.9946220817418663, -45.26526879604974596, 189.2069091854172598 ) ) ;
#34624=CARTESIAN_POINT ( 'NONE',  ( -71.26649465934139016, -60.00000000000000000, 149.0547838307006430 ) ) ;
#34630=CARTESIAN_POINT ( 'NONE',  ( 8.521411446770892795, 0.000000000000000000, 14.76969908562504408 ) ) ;
#34637=CARTESIAN_POINT ( 'NONE',  ( 86.31767834415556706, -59.99999999999999289, 20.32226923651656847 ) ) ;
#34638=CARTESIAN_POINT ( 'NONE',  ( -31.57922577310468526, -32.55042699868089784, 32.45668791033146050 ) ) ;
#34640=CARTESIAN_POINT ( 'NONE',  ( 46.25750148850488586, -32.61358005543022642, 43.24939596980505030 ) ) ;
#34645=CARTESIAN_POINT ( 'NONE',  ( -81.44491332629058888, -38.84114197386964662, 195.2043805330731345 ) ) ;
#34648=CARTESIAN_POINT ( 'NONE',  ( 10.44019003300671500, -59.99999999999997158, 33.89246852536604848 ) ) ;
#34649=LINE ( 'NONE', #84226, #25204 ) ;
#34650=EDGE_CURVE ( 'NONE', #61487, #86629, #102189, .T. ) ;
#34656=CARTESIAN_POINT ( 'NONE',  ( 103.6205286009478215, -60.00000000000002132, 102.2157128241041590 ) ) ;
#34661=CARTESIAN_POINT ( 'NONE',  ( -97.33989514445055136, -29.99999999999995026, 190.9629009002478597 ) ) ;
#34674=CARTESIAN_POINT ( 'NONE',  ( 84.36382179597347886, -25.57599070838802646, 160.3264503554693761 ) ) ;
#34714=CARTESIAN_POINT ( 'NONE',  ( -78.47844370984229556, -60.00000000000001421, 193.7840747555254950 ) ) ;
#34718=CARTESIAN_POINT ( 'NONE',  ( -84.44772399558564757, -46.57216599554897130, 186.0917793300985750 ) ) ;
#34726=CARTESIAN_POINT ( 'NONE',  ( -83.89485214324410833, -45.26916324968230043, 4.375863353757575069 ) ) ;
#34735=CARTESIAN_POINT ( 'NONE',  ( 72.31505286502601848, -14.21045842199433373, 125.5027806063605595 ) ) ;
#34737=CARTESIAN_POINT ( 'NONE',  ( -89.80806051762600362, -30.00000000000005684, 26.19611557095339904 ) ) ;
#34738=CARTESIAN_POINT ( 'NONE',  ( -67.34159380897033031, -56.86460610103189595, 103.2059302081343901 ) ) ;
#34740=CARTESIAN_POINT ( 'NONE',  ( 62.54367487775790124, -59.99999999999994316, 118.0935059193921575 ) ) ;
#34742=CARTESIAN_POINT ( 'NONE',  ( 44.09900958218985778, -59.99999999999509726, 64.08949965347366629 ) ) ;
#34763=CARTESIAN_POINT ( 'NONE',  ( 31.31534349697233921, -22.13725448416145980, 30.43540540151346718 ) ) ;
#34775=CARTESIAN_POINT ( 'NONE',  ( 87.25490207742672055, -60.00000000000000711, -22.40272287519551853 ) ) ;
#34792=CARTESIAN_POINT ( 'NONE',  ( 83.10716226388446159, -37.79806746364081249, -10.04868559838506670 ) ) ;
#34805=CARTESIAN_POINT ( 'NONE',  ( 71.85279723664308449, -56.85193184329963856, 119.4851267806225508 ) ) ;
#34810=CARTESIAN_POINT ( 'NONE',  ( -84.95435462066053844, -57.67079294309295534, -27.04779982294425977 ) ) ;
#34816=CARTESIAN_POINT ( 'NONE',  ( 102.9736477862243191, -45.28271309083630314, 185.6071471573901874 ) ) ;
#34817=ADVANCED_FACE ( 'NONE', ( #37500 ), #104816, .F. ) ;
#34830=DIRECTION ( 'NONE',  ( 1.776356839400250465E-15, 0.000000000000000000, 1.000000000000000000 ) ) ;
#34833=CARTESIAN_POINT ( 'NONE',  ( -87.74742208423795375, -30.00000000000000355, 186.1250627137971492 ) ) ;
#34836=CARTESIAN_POINT ( 'NONE',  ( 71.48264316122191531, -57.67967896547522599, 166.8593090913044819 ) ) ;
#34838=CARTESIAN_POINT ( 'NONE',  ( 37.38852656643516070, -32.12008312474581118, -37.68358437264794958 ) ) ;
#34841=CARTESIAN_POINT ( 'NONE',  ( -41.36542036488555851, -59.99999999999999289, 54.13965941178337005 ) ) ;
#34844=CARTESIAN_POINT ( 'NONE',  ( -86.61008243043399091, -20.70827441317174333, 184.3512822565784575 ) ) ;
#34845=AXIS2_PLACEMENT_3D ( 'NONE', #41145, #55701, #14722 ) ;
#34848=CARTESIAN_POINT ( 'NONE',  ( -3.091320174682205657, -60.36579976115420720, 33.94522616076510246 ) ) ;
#34863=CARTESIAN_POINT ( 'NONE',  ( 105.8603286302927984, -14.21045842199436571, 153.6005582235227678 ) ) ;
#34864=CARTESIAN_POINT ( 'NONE',  ( -79.31517829596272406, -53.37869160261720936, 157.6496308188775117 ) ) ;
#34884=CARTESIAN_POINT ( 'NONE',  ( 108.5319597222283079, -60.00000000000001421, 194.6846619470310316 ) ) ;
#34886=CARTESIAN_POINT ( 'NONE',  ( -88.91591484687975822, -30.00000000000007105, 199.0554621605764680 ) ) ;
#34887=CARTESIAN_POINT ( 'NONE',  ( 25.60135656087680545, -60.34811172916996469, 35.42567114881672552 ) ) ;
#34891=CARTESIAN_POINT ( 'NONE',  ( -40.77353850287842363, -29.15401300376588267, 36.95902376227557085 ) ) ;
#34905=CARTESIAN_POINT ( 'NONE',  ( 81.49538808793018063, -30.00000000000000000, 29.79622834626826489 ) ) ;
#34910=CARTESIAN_POINT ( 'NONE',  ( 85.92470906003214282, -30.00000000000000355, 63.76399589821353686 ) ) ;
#34924=CARTESIAN_POINT ( 'NONE',  ( 75.45573842239058138, -38.35112759154727513, 173.8072745080378070 ) ) ;
#34945=CARTESIAN_POINT ( 'NONE',  ( 86.39650202725968597, -17.44888770226837948, 178.9044480368839629 ) ) ;
#34955=CARTESIAN_POINT ( 'NONE',  ( -83.17859549212624870, -30.00000000000000000, 44.33109224352784850 ) ) ;
#34971=CARTESIAN_POINT ( 'NONE',  ( 48.18193197797202032, -27.07217853350000780, -28.43546366937567882 ) ) ;
#34972=CARTESIAN_POINT ( 'NONE',  ( -26.71263552688614240, -39.48221859129683509, 32.14868509336800173 ) ) ;
#34976=CARTESIAN_POINT ( 'NONE',  ( -19.48547116245557476, -60.36370404294115843, 34.43491227761722939 ) ) ;
#34977=CARTESIAN_POINT ( 'NONE',  ( -67.88365031951838091, -29.91622526688993844, -21.77912222725431235 ) ) ;
#34979=CARTESIAN_POINT ( 'NONE',  ( -72.65287874387934153, -47.40885675805417065, -22.95091789652445158 ) ) ;
#34988=CARTESIAN_POINT ( 'NONE',  ( 100.4734033239317057, -45.27744650063931431, 192.0868348784580348 ) ) ;
#35005=CARTESIAN_POINT ( 'NONE',  ( -69.72050231116651275, -57.68271840123205862, 152.1212729744891590 ) ) ;
#35010=CARTESIAN_POINT ( 'NONE',  ( -95.18184656059791848, -59.99999999999997158, -7.511930356246473650 ) ) ;
#35013=CARTESIAN_POINT ( 'NONE',  ( -49.14104052736104933, -49.90578126524030722, 52.73558596523304232 ) ) ;
#35023=CARTESIAN_POINT ( 'NONE',  ( 74.64902420247312875, -38.33065913207683906, 166.1686744667666176 ) ) ;
#35030=CARTESIAN_POINT ( 'NONE',  ( 91.95784082022851180, -29.99999999999999289, 190.8526501999825200 ) ) ;
#35036=CARTESIAN_POINT ( 'NONE',  ( 51.66197549029767799, -46.43860231094777902, 56.12756693511081352 ) ) ;
#35041=CARTESIAN_POINT ( 'NONE',  ( -90.49795102847224371, -38.40269404522611296, -14.57212712810775201 ) ) ;
#35044=CARTESIAN_POINT ( 'NONE',  ( 106.9166147825914663, -38.36521485666400366, 194.9876764072000697 ) ) ;
#35046=CARTESIAN_POINT ( 'NONE',  ( 91.05926484896966144, -45.28280038615342562, 77.50342918606192200 ) ) ;
#35049=FILL_AREA_STYLE_COLOUR ( '', #5721 ) ;
#35062=CARTESIAN_POINT ( 'NONE',  ( 44.21857466350731869, -28.02261279241452385, 39.26658464693652917 ) ) ;
#35067=CARTESIAN_POINT ( 'NONE',  ( 82.00125028607160971, -60.71606377786684305, 187.9277208723676154 ) ) ;
#35077=CARTESIAN_POINT ( 'NONE',  ( -42.67177486380370510, -33.72132305402984542, -37.16294406443787324 ) ) ;
#35080=CARTESIAN_POINT ( 'NONE',  ( 43.30523961208659500, -60.00000000000001421, 57.40393935450531160 ) ) ;
#35082=CARTESIAN_POINT ( 'NONE',  ( 27.14852178964998686, -30.51280503760606777, 39.13343489206324932 ) ) ;
#35084=CARTESIAN_POINT ( 'NONE',  ( -32.35805919302102041, -33.97132168949374886, 42.09303864586733113 ) ) ;
#35100=CARTESIAN_POINT ( 'NONE',  ( 50.82574175334806910, -47.40887837029733021, -29.75606519997849730 ) ) ;
#35111=CARTESIAN_POINT ( 'NONE',  ( -91.86600403542094284, -59.99999999999998579, 10.85315903371735757 ) ) ;
#35117=CARTESIAN_POINT ( 'NONE',  ( -83.47784681200417367, -39.47383177809769705, 174.2413187030911956 ) ) ;
#35126=AXIS2_PLACEMENT_3D ( 'NONE', #77704, #60998, #60480 ) ;
#35132=CARTESIAN_POINT ( 'NONE',  ( 97.22633417984880566, -59.99999999999997158, 47.92222960719137603 ) ) ;
#35134=CARTESIAN_POINT ( 'NONE',  ( -103.2140057312332715, -60.00000000000000000, 203.2732544657875167 ) ) ;
#35135=CARTESIAN_POINT ( 'NONE',  ( -58.23786245037103981, -53.38855727373060489, 74.09665987365666240 ) ) ;
#35136=VERTEX_POINT ( 'NONE', #54828 ) ;
#35139=CARTESIAN_POINT ( 'NONE',  ( -102.5594303321801277, -52.71277882121110281, 191.0325329949383217 ) ) ;
#35144=CARTESIAN_POINT ( 'NONE',  ( -77.97286044409068495, -60.00000000000002132, 192.7800898974841175 ) ) ;
#35150=CARTESIAN_POINT ( 'NONE',  ( 5.483261958904508404, -0.000000000000000000, -16.14668631625339046 ) ) ;
#35157=CARTESIAN_POINT ( 'NONE',  ( -30.57629521487107738, -42.96300971420584602, 33.95585917984841728 ) ) ;
#35160=CARTESIAN_POINT ( 'NONE',  ( 45.44314741231004717, -32.61510095533251530, 42.31814636275050390 ) ) ;
#35163=CARTESIAN_POINT ( 'NONE',  ( -90.23139260845938736, -38.51326215213924797, 200.6299674765010366 ) ) ;
#35165=CARTESIAN_POINT ( 'NONE',  ( 83.84769081256168022, -38.35769379593097739, -23.82778957254525665 ) ) ;
#35167=CARTESIAN_POINT ( 'NONE',  ( 41.68366003721723700, -59.99999999999995026, 44.95385205308215859 ) ) ;
#35174=CARTESIAN_POINT ( 'NONE',  ( 108.5077592403022066, -60.00000000000002842, 194.7355029765727465 ) ) ;
#35182=CARTESIAN_POINT ( 'NONE',  ( -80.82737729657345938, -30.00000000000002132, 17.73016317466827729 ) ) ;
#35184=CARTESIAN_POINT ( 'NONE',  ( -76.78686838515666579, -38.43714460091105423, 183.3497871105654440 ) ) ;
#35195=CARTESIAN_POINT ( 'NONE',  ( 80.66719333992175223, -53.39832462065744068, 170.0938344876146857 ) ) ;
#35211=CARTESIAN_POINT ( 'NONE',  ( 87.09139377491906941, -35.39572006237809632, 188.3556698165368459 ) ) ;
#35220=STYLED_ITEM ( 'NONE', ( #11604 ), #85165 ) ;
#35234=CARTESIAN_POINT ( 'NONE',  ( -76.29495167748918050, -60.00000000000000000, 188.1436829353336861 ) ) ;
#35239=CARTESIAN_POINT ( 'NONE',  ( -85.97713623827759477, -24.93338126948129485, 178.6360369055118724 ) ) ;
#35240=VECTOR ( 'NONE', #91049, 1000.000000000000000 ) ;
#35248=CARTESIAN_POINT ( 'NONE',  ( -86.56086951948698527, -60.14310811859036221, 1.458335607829068126 ) ) ;
#35255=CARTESIAN_POINT ( 'NONE',  ( 71.80342808059909032, -30.00000000000000000, -19.71766482350836469 ) ) ;
#35256=CARTESIAN_POINT ( 'NONE',  ( 72.40119513776858184, -29.99999999999997868, 139.7542682952119719 ) ) ;
#35258=CARTESIAN_POINT ( 'NONE',  ( -87.78075539319912934, -14.21045842199443499, -8.620330001511526063 ) ) ;
#35259=CARTESIAN_POINT ( 'NONE',  ( -64.67222873873710398, -60.34389612767258626, 96.31452158953769072 ) ) ;
#35261=CARTESIAN_POINT ( 'NONE',  ( 75.88724551625310255, -29.99999999999989697, 164.4338130987444231 ) ) ;
#35263=CARTESIAN_POINT ( 'NONE',  ( 5.691016455591895173, -59.99999999998026823, 41.97878891002031310 ) ) ;
#35272=CARTESIAN_POINT ( 'NONE',  ( -50.35455267728183770, -59.99999999998047429, 79.24196553474639870 ) ) ;
#35286=CARTESIAN_POINT ( 'NONE',  ( 33.05110402582430851, -42.96104700131527210, 35.01015022028214929 ) ) ;
#35287=SURFACE_STYLE_USAGE ( .BOTH. , #36373 ) ;
#35303=CARTESIAN_POINT ( 'NONE',  ( 65.90086000808869926, -60.00000000000000000, -33.92264569605602276 ) ) ;
#35312=CARTESIAN_POINT ( 'NONE',  ( -85.46292727709757742, -29.99999999999107914, 197.4394013638547278 ) ) ;
#35320=CARTESIAN_POINT ( 'NONE',  ( 84.40332656976852377, -45.28403232242267507, -9.145071154980445982 ) ) ;
#35334=CARTESIAN_POINT ( 'NONE',  ( 76.07410448762261979, -39.49124980177613509, 125.1990055723632906 ) ) ;
#35341=CARTESIAN_POINT ( 'NONE',  ( -94.67953089133513345, -57.66492561105124537, -4.550087184288205577 ) ) ;
#35346=CARTESIAN_POINT ( 'NONE',  ( 105.5944179521240756, -60.15122995615571710, 185.0766847636498085 ) ) ;
#35350=CARTESIAN_POINT ( 'NONE',  ( -39.88018151434195602, -26.27442631564857578, 35.88468731287488822 ) ) ;
#35360=CARTESIAN_POINT ( 'NONE',  ( -89.04407725700431797, -30.00000000000000355, 188.7674523140026679 ) ) ;
#35365=CARTESIAN_POINT ( 'NONE',  ( 81.35062306902976559, -57.51595381549781649, 200.0166916054824071 ) ) ;
#35370=CARTESIAN_POINT ( 'NONE',  ( 31.06825638305650727, -29.95875917721051351, -38.12153552884113594 ) ) ;
#35372=CARTESIAN_POINT ( 'NONE',  ( -41.39662806798475003, -59.99999999999998579, 54.18885812487171449 ) ) ;
#35378=CARTESIAN_POINT ( 'NONE',  ( -86.46969285347701373, -17.03976896954880615, 183.6895310209484364 ) ) ;
#35381=CARTESIAN_POINT ( 'NONE',  ( -2.020640315534143028, -42.95763966138775913, 31.04680227545052773 ) ) ;
#35396=CARTESIAN_POINT ( 'NONE',  ( 93.38347165230982228, -30.00000000000000711, 56.44843285056885662 ) ) ;
#35397=CARTESIAN_POINT ( 'NONE',  ( -82.53661707010365944, -22.15634074740264126, 142.5693487567720865 ) ) ;
#35401=( NAMED_UNIT ( * ) PLANE_ANGLE_UNIT ( ) SI_UNIT ( $, .RADIAN. ) );
#35418=CARTESIAN_POINT ( 'NONE',  ( -77.57376394631657490, -29.99999999999998934, 180.9696502640093172 ) ) ;
#35419=CARTESIAN_POINT ( 'NONE',  ( 22.09608613383313980, -25.55606579312770066, 28.90373523675440381 ) ) ;
#35423=CARTESIAN_POINT ( 'NONE',  ( -35.82267405487428391, -18.72926178012174603, 31.62524112213710481 ) ) ;
#35436=AXIS2_PLACEMENT_3D ( 'NONE', #61751, #37490, #19190 ) ;
#35437=CARTESIAN_POINT ( 'NONE',  ( 98.21845683671166682, -30.00000000000000711, 190.2718979233115419 ) ) ;
#35440=CARTESIAN_POINT ( 'NONE',  ( 86.62833229249164901, -30.00000000000000355, 68.18189329567420032 ) ) ;
#35456=CARTESIAN_POINT ( 'NONE',  ( 74.24387853852118724, -38.32799764064220227, 162.4765421416901177 ) ) ;
#35481=CARTESIAN_POINT ( 'NONE',  ( 85.12024738230812204, -50.19341801944306525, 189.4198906295553400 ) ) ;
#35484=CARTESIAN_POINT ( 'NONE',  ( 55.74658202726395473, -57.67088109086454750, -38.72831865961387621 ) ) ;
#35489=CARTESIAN_POINT ( 'NONE',  ( -93.51094265731104827, -29.99999999999998934, 109.0518179395232892 ) ) ;
#35500=CARTESIAN_POINT ( 'NONE',  ( 21.83701553852647947, -19.09061506513711493, -33.46987204855414433 ) ) ;
#35502=CARTESIAN_POINT ( 'NONE',  ( -25.36348844297524963, -53.39683697002490703, 34.19068731400996342 ) ) ;
#35507=CARTESIAN_POINT ( 'NONE',  ( -19.65540319560976101, -18.59144410933823366, 27.44006592855480520 ) ) ;
#35525=CARTESIAN_POINT ( 'NONE',  ( 98.68619524362034667, -37.78306943100542270, 192.1284777729563302 ) ) ;
#35541=CARTESIAN_POINT ( 'NONE',  ( -91.59607114535849348, -60.00000000000365219, -20.75833340651075787 ) ) ;
#35545=CARTESIAN_POINT ( 'NONE',  ( -86.84190767202800032, -14.21045842199442788, 3.676479754794546473 ) ) ;
#35549=CARTESIAN_POINT ( 'NONE',  ( -52.50648933632491833, -18.71248995424286932, 47.73799938596632586 ) ) ;
#35559=CARTESIAN_POINT ( 'NONE',  ( 84.40133724763363432, -29.99999999999239364, -21.52947726462551969 ) ) ;
#35564=CARTESIAN_POINT ( 'NONE',  ( 89.35863705434196902, -29.99999999999999645, 189.1991920285174160 ) ) ;
#35570=CARTESIAN_POINT ( 'NONE',  ( 52.08973531413104041, -32.57578831394647523, 51.93190986806391862 ) ) ;
#35575=CARTESIAN_POINT ( 'NONE',  ( -89.77470481043597772, -38.39469723191136552, -16.55334520362848849 ) ) ;
#35577=CARTESIAN_POINT ( 'NONE',  ( 106.0169255512641087, -38.37657707414045660, 196.3210357038191205 ) ) ;
#35579=CARTESIAN_POINT ( 'NONE',  ( 86.03480774772026507, -52.71534935679705569, 32.67177944397322875 ) ) ;
#35582=( LENGTH_UNIT ( ) NAMED_UNIT ( * ) SI_UNIT ( .MILLI., .METRE. ) );
#35598=CARTESIAN_POINT ( 'NONE',  ( -53.08935917470198262, -30.00000000000002132, 52.21147893555088615 ) ) ;
#35603=COLOUR_RGB ( '', 0.40784314, 0.44705882, 0.49803922) ;
#35605=CARTESIAN_POINT ( 'NONE',  ( 86.20298226707136280, -18.29538666924914025, 168.7790078290781253 ) ) ;
#35609=CARTESIAN_POINT ( 'NONE',  ( -85.13303551996550311, -45.26552266227979260, 36.04504711083556856 ) ) ;
#35615=CARTESIAN_POINT ( 'NONE',  ( -14.02598654517192678, -23.76892447270615705, -38.53458435890105704 ) ) ;
#35617=CARTESIAN_POINT ( 'NONE',  ( 45.83015609643102550, -60.00000000000000000, 62.25697969437710810 ) ) ;
#35623=CARTESIAN_POINT ( 'NONE',  ( -2.499999999999996447, -19.94872641843396721, -28.09930264074299444 ) ) ;
#35634=EDGE_CURVE ( 'NONE', #32321, #38839, #47086, .T. ) ;
#35641=CARTESIAN_POINT ( 'NONE',  ( 9.564681418035569038, -47.40889936360509438, -34.57825658523572798 ) ) ;
#35648=CARTESIAN_POINT ( 'NONE',  ( -94.53821169941970481, -60.00000000000002132, 45.58263737987853403 ) ) ;
#35655=CARTESIAN_POINT ( 'NONE',  ( -83.68639855425038832, -35.98482338576268802, 170.8203333709438425 ) ) ;
#35667=CARTESIAN_POINT ( 'NONE',  ( -113.5700743903323087, -57.67116359713492812, 158.3188924881959849 ) ) ;
#35675=CARTESIAN_POINT ( 'NONE',  ( 97.09801539114592117, -30.00000000000000711, 79.69841507686976456 ) ) ;
#35677=CARTESIAN_POINT ( 'NONE',  ( -94.36268555338997999, -29.99999999999996803, 200.0833938634536935 ) ) ;
#35678=CARTESIAN_POINT ( 'NONE',  ( -60.76648917972766384, -22.12019031114792966, 66.06036334567909307 ) ) ;
#35684=CARTESIAN_POINT ( 'NONE',  ( -102.5236597725247947, -45.26536941210562759, 187.4725801446850255 ) ) ;
#35685=CYLINDRICAL_SURFACE ( 'NONE', #35126, 2.000000000000001776 ) ;
#35691=CARTESIAN_POINT ( 'NONE',  ( -42.15816230349173566, -59.99999999999998579, 55.39162115207339099 ) ) ;
#35696=CARTESIAN_POINT ( 'NONE',  ( 13.52495681778930958, -0.000000000000000000, -10.38447319517952216 ) ) ;
#35702=CARTESIAN_POINT ( 'NONE',  ( -30.83233686821828456, -18.66184128751320515, 29.63134590784697409 ) ) ;
#35703=CARTESIAN_POINT ( 'NONE',  ( 44.20965380832324598, -53.34280533345454955, 46.32928704068250880 ) ) ;
#35707=CARTESIAN_POINT ( 'NONE',  ( -97.86142940197255768, -38.48039219746727468, 201.0047720557965363 ) ) ;
#35711=CARTESIAN_POINT ( 'NONE',  ( 47.15958797797829050, -60.00000000000000711, 52.51100894563059995 ) ) ;
#35719=CARTESIAN_POINT ( 'NONE',  ( 112.1770130220217112, -60.00000000000001421, 169.0659528092184587 ) ) ;
#35724=CARTESIAN_POINT ( 'NONE',  ( -80.17022493459282373, -30.00000000000006040, -13.56932818816917496 ) ) ;
#35726=CARTESIAN_POINT ( 'NONE',  ( -71.97172513630449942, -38.32687865468555088, 145.5980316631960818 ) ) ;
#35737=CARTESIAN_POINT ( 'NONE',  ( 81.74643333074975260, -46.44958790937922544, 169.1855094761081943 ) ) ;
#35757=CARTESIAN_POINT ( 'NONE',  ( 87.19375473865754600, -31.68694345013608427, 187.9059264421138948 ) ) ;
#35775=VERTEX_POINT ( 'NONE', #21201 ) ;
#35783=CARTESIAN_POINT ( 'NONE',  ( -99.64086268788143741, -60.00000000000001421, 202.0020366782889880 ) ) ;
#35788=CARTESIAN_POINT ( 'NONE',  ( -85.30085673280602521, -35.74314973840716192, 182.5942498631214050 ) ) ;
#35793=CARTESIAN_POINT ( 'NONE',  ( -82.61673979528575273, -37.83313480826174668, 4.882814718300323875 ) ) ;
#35800=CARTESIAN_POINT ( 'NONE',  ( 77.87328754808491738, -14.21045842199420228, 157.7472683744473159 ) ) ;
#35802=CARTESIAN_POINT ( 'NONE',  ( -89.52600508066183238, -29.99999999999992539, 22.05060892610427814 ) ) ;
#35803=CARTESIAN_POINT ( 'NONE',  ( -71.71757422039344476, -29.06626939408458554, 101.3046069043710560 ) ) ;
#35805=CARTESIAN_POINT ( 'NONE',  ( 81.10520000301197285, -14.21045842199436926, 192.6066858413676925 ) ) ;
#35807=CARTESIAN_POINT ( 'NONE',  ( 27.27612554697342517, -60.00000000000986233, 44.35091487113613340 ) ) ;
#35817=CARTESIAN_POINT ( 'NONE',  ( -70.42324668238815377, -59.99999999998043876, 160.4961440857183277 ) ) ;
#35827=ORIENTED_EDGE ( 'NONE', *, *, #65444, .F. ) ;
#35831=CARTESIAN_POINT ( 'NONE',  ( 31.63731285819285688, -39.48887728662363372, 33.75230942950094715 ) ) ;
#35832=PRESENTATION_STYLE_ASSIGNMENT (( #35287 ) ) ;
#35846=CARTESIAN_POINT ( 'NONE',  ( 91.86088825387464851, -60.00000000000000711, 13.72134700691805698 ) ) ;
#35855=CARTESIAN_POINT ( 'NONE',  ( -109.5118039930968052, -30.00000000000000000, 177.2736533842592621 ) ) ;
#35861=CARTESIAN_POINT ( 'NONE',  ( 84.04211440375647157, -45.27896428354746661, -11.65066557963491967 ) ) ;
#35874=CARTESIAN_POINT ( 'NONE',  ( 76.67219034576102388, -32.54950668678723957, 122.5186054704328882 ) ) ;
#35879=CARTESIAN_POINT ( 'NONE',  ( -102.4013124767651135, -57.63331223797548120, 203.1247769353137755 ) ) ;
#35885=CARTESIAN_POINT ( 'NONE',  ( 104.2870107326527034, -52.71696054412868193, 185.3521057339551135 ) ) ;
#35890=CARTESIAN_POINT ( 'NONE',  ( -50.73617477660454966, -29.81564531741702595, 47.82844993627990249 ) ) ;
#35898=EDGE_LOOP ( 'NONE', ( #42799, #16524, #93342, #79795 ) ) ;
#35903=CARTESIAN_POINT ( 'NONE',  ( -87.46766941343894075, -30.00000000000000000, 185.3710213780722427 ) ) ;
#35908=CARTESIAN_POINT ( 'NONE',  ( 86.15165790503920107, -57.57631507345369926, 202.7687108331410286 ) ) ;
#35913=CARTESIAN_POINT ( 'NONE',  ( 67.49251172716176939, -38.07658496841629869, -32.03956923833649029 ) ) ;
#35916=CARTESIAN_POINT ( 'NONE',  ( -65.63516414262727494, -59.99999999999999289, 120.8879485127422129 ) ) ;
#35920=CARTESIAN_POINT ( 'NONE',  ( -84.61161887829497630, -61.08739850468023036, 193.0979379198380173 ) ) ;
#35923=CARTESIAN_POINT ( 'NONE',  ( -4.963955403123392784, -18.58604024885853434, 26.97813512196605856 ) ) ;
#35938=CARTESIAN_POINT ( 'NONE',  ( 94.85921371064608820, -60.00000000000004263, 26.66736809083038651 ) ) ;
#35940=CARTESIAN_POINT ( 'NONE',  ( -78.78664253753292712, -53.37736891008503903, 153.4667062920331659 ) ) ;
#35942=SURFACE_STYLE_USAGE ( .BOTH. , #86601 ) ;
#35944=CARTESIAN_POINT ( 'NONE',  ( 50.82724289091086689, -57.67763088439131280, 79.42815591981056400 ) ) ;
#35963=CARTESIAN_POINT ( 'NONE',  ( 36.03932222122800511, -60.00000000000000000, -40.18715066664060487 ) ) ;
#35964=CARTESIAN_POINT ( 'NONE',  ( -64.82027869498183748, -30.00000000000004619, 107.4038593739741430 ) ) ;
#35965=CARTESIAN_POINT ( 'NONE',  ( 19.82456495684694531, -25.55224884438233701, 28.62604876544009969 ) ) ;
#35968=CARTESIAN_POINT ( 'NONE',  ( -38.48681241573974887, -25.68051362833467977, 34.55373408003233493 ) ) ;
#35970=CARTESIAN_POINT ( 'NONE',  ( -16.66764709352488083, -4.285714285714295357, 19.00223544648543950 ) ) ;
#35980=CARTESIAN_POINT ( 'NONE',  ( 97.98091450867445928, -29.99999999999992184, 190.5507201259314627 ) ) ;
#35983=CARTESIAN_POINT ( 'NONE',  ( 80.94547152824299019, -30.00000000000000000, 20.01427389387851719 ) ) ;
#35993=AXIS2_PLACEMENT_3D ( 'NONE', #57101, #90015, #24774 ) ;
#36002=CARTESIAN_POINT ( 'NONE',  ( 72.04471834908918026, -38.32678965749821032, 146.1819033111827935 ) ) ;
#36023=CARTESIAN_POINT ( 'NONE',  ( 85.18141407811432941, -53.83922793184471800, 190.9676820986030350 ) ) ;
#36027=CARTESIAN_POINT ( 'NONE',  ( 75.60846622749433266, -57.67119937720136136, -32.37792878120276896 ) ) ;
#36028=CARTESIAN_POINT ( 'NONE',  ( 69.26914063590702142, -29.97404492864524883, -21.11895981858886984 ) ) ;
#36032=CARTESIAN_POINT ( 'NONE',  ( -92.47187049835589789, -30.00000000000000355, 102.9253929577534592 ) ) ;
#36036=CARTESIAN_POINT ( 'NONE',  ( 0.2599417667399435139, -57.67120205748143036, 41.61181906779697215 ) ) ;
#36045=CARTESIAN_POINT ( 'NONE',  ( 50.89319870900899900, -27.68869576212836847, -27.73928759546735634 ) ) ;
#36048=CARTESIAN_POINT ( 'NONE',  ( -23.10449564462755490, -60.35990861106341754, 34.93722728922637089 ) ) ;
#36052=CARTESIAN_POINT ( 'NONE',  ( -20.76759987540068053, -18.59339395674310680, 27.55335100898648548 ) ) ;
#36058=CARTESIAN_POINT ( 'NONE',  ( 1.544427540536530710E-15, -4.285714285714290916, -25.22241582816893057 ) ) ;
#36067=CARTESIAN_POINT ( 'NONE',  ( 103.7353799882583019, -52.71710819990906316, 187.7499664499858909 ) ) ;
#36069=SURFACE_STYLE_USAGE ( .BOTH. , #3124 ) ;
#36084=CARTESIAN_POINT ( 'NONE',  ( -94.39696246771445942, -59.99999999999998579, 5.332034942330889038 ) ) ;
#36088=CARTESIAN_POINT ( 'NONE',  ( -89.21407719722087393, -30.00000000000005684, 9.591031914958218607 ) ) ;
#36091=CARTESIAN_POINT ( 'NONE',  ( -49.29312953085187132, -18.74715051740997040, 42.99385802251428146 ) ) ;
#36102=CARTESIAN_POINT ( 'NONE',  ( 90.08918622825524380, -30.00000000000337153, -5.724205789237760911 ) ) ;
#36106=CARTESIAN_POINT ( 'NONE',  ( 90.37482638485310815, -29.99999999999999645, 190.1461905130674950 ) ) ;
#36113=CARTESIAN_POINT ( 'NONE',  ( 53.47773224423268346, -60.31207318078936197, 65.32173576400356296 ) ) ;
#36114=DIRECTION ( 'NONE',  ( 0.000000000000000000, -1.000000000000000000, 0.000000000000000000 ) ) ;
#36118=CARTESIAN_POINT ( 'NONE',  ( -88.03633069172695969, -38.37099167637006047, -19.52536479018785087 ) ) ;
#36122=CARTESIAN_POINT ( 'NONE',  ( 111.0097756496680006, -38.35607304391395189, 172.2120856835122709 ) ) ;
#36124=CARTESIAN_POINT ( 'NONE',  ( 86.51436465318690239, -60.13692532640241240, 2.092395710485930316 ) ) ;
#36143=CARTESIAN_POINT ( 'NONE',  ( 31.19249401299645186, -22.25766550667198374, 32.30297921700840647 ) ) ;
#36144=CIRCLE ( 'NONE', #20454, 7.499999999992679633 ) ;
#36147=CARTESIAN_POINT ( 'NONE',  ( 84.00677267882208810, -50.15819390199315819, 186.9337807051296352 ) ) ;
#36151=CARTESIAN_POINT ( 'NONE',  ( -96.37380543725086568, -52.71037193844853874, 101.1465460539529460 ) ) ;
#36154=CARTESIAN_POINT ( 'NONE',  ( -31.37180257112542847, -30.07018934284766232, -38.10741079039508605 ) ) ;
#36157=STYLED_ITEM ( 'NONE', ( #12666 ), #45875 ) ;
#36158=CARTESIAN_POINT ( 'NONE',  ( 25.47307600370571379, -59.99999999999998579, 41.30018710837394735 ) ) ;
#36160=CARTESIAN_POINT ( 'NONE',  ( 31.55798995419172570, -33.46712117103052009, 41.53811485048920105 ) ) ;
#36162=CARTESIAN_POINT ( 'NONE',  ( 51.37712067241238145, -29.89819866070208576, 48.95739146609739123 ) ) ;
#36164=CARTESIAN_POINT ( 'NONE',  ( -32.45767638303610170, -34.03325006748782044, 42.16482906108820572 ) ) ;
#36179=CARTESIAN_POINT ( 'NONE',  ( -18.69900205392447390, -21.77036642001481681, -29.76779902863794192 ) ) ;
#36189=CARTESIAN_POINT ( 'NONE',  ( -93.05166615780947836, -60.00000000000000000, 32.92217660829798831 ) ) ;
#36197=CARTESIAN_POINT ( 'NONE',  ( -84.68119024137185136, -25.54381684178671108, 163.3937236597952563 ) ) ;
#36208=CARTESIAN_POINT ( 'NONE',  ( -94.50453298674098335, -57.65443526055588563, -11.14264577307068294 ) ) ;
#36215=CARTESIAN_POINT ( 'NONE',  ( 100.4059631369621570, -60.00000000000003553, 69.07260714096372567 ) ) ;
#36216=CARTESIAN_POINT ( 'NONE',  ( -78.68906450541477682, -14.21045842199436926, 170.0145061391070271 ) ) ;
#36217=CARTESIAN_POINT ( 'NONE',  ( -55.11669765333618898, -32.56112197649012074, 57.75454668961312166 ) ) ;
#36221=CARTESIAN_POINT ( 'NONE',  ( -100.4908920805564065, -37.81811875270330603, 189.5769949498487961 ) ) ;
#36235=EDGE_CURVE ( 'NONE', #80843, #98077, #51251, .T. ) ;
#36238=CARTESIAN_POINT ( 'NONE',  ( -30.06290811726797330, -32.54186696253240996, 31.90563260260433154 ) ) ;
#36241=CARTESIAN_POINT ( 'NONE',  ( 47.73540206996886326, -32.60520857632516822, 45.16482891593580007 ) ) ;
#36246=CARTESIAN_POINT ( 'NONE',  ( -96.51435786616053747, -38.48409689973218661, 201.1738884492503132 ) ) ;
#36257=CARTESIAN_POINT ( 'NONE',  ( 106.5750692260998278, -59.99999999999999289, 197.6315772264619284 ) ) ;
#36263=CARTESIAN_POINT ( 'NONE',  ( -80.54403476602729484, -30.00000000000000000, -12.95354117423075024 ) ) ;
#36267=CARTESIAN_POINT ( 'NONE',  ( -75.25348839758508745, -38.34335650720067434, 171.9446546056112481 ) ) ;
#36278=CARTESIAN_POINT ( 'NONE',  ( 85.53813280434940225, -21.95506244895780412, 166.5497984053122593 ) ) ;
#36293=CARTESIAN_POINT ( 'NONE',  ( -80.64317183426827285, -30.00000000000000355, -12.75789385870653270 ) ) ;
#36319=CARTESIAN_POINT ( 'NONE',  ( -111.1388128507345812, -60.00000000000001421, 186.5774987372416263 ) ) ;
#36325=CARTESIAN_POINT ( 'NONE',  ( -81.59287406109901042, -60.63717241894644161, 186.3584735478276002 ) ) ;
#36331=CARTESIAN_POINT ( 'NONE',  ( -86.42542376329605247, -60.13647821371448288, 3.360464890229343915 ) ) ;
#36338=CARTESIAN_POINT ( 'NONE',  ( 68.99587917277882809, -30.00000000000005329, 123.4883035811859884 ) ) ;
#36341=CARTESIAN_POINT ( 'NONE',  ( -86.58068678654640848, -14.21045842199428932, 15.94391106889438525 ) ) ;
#36342=CARTESIAN_POINT ( 'NONE',  ( -71.85214048801175579, -56.85815330016787783, 119.4862648020721423 ) ) ;
#36344=CARTESIAN_POINT ( 'NONE',  ( 79.87681789614374850, -30.00000000000000711, 191.0754539389706395 ) ) ;
#36347=CARTESIAN_POINT ( 'NONE',  ( 38.08648362024728584, -60.00000000001480061, 53.39166904922846868 ) ) ;
#36358=CARTESIAN_POINT ( 'NONE',  ( -75.28337991137821916, -60.00000000000001421, -30.37543036780875028 ) ) ;
#36361=DIRECTION ( 'NONE',  ( 0.000000000000000000, 0.000000000000000000, -1.000000000000000000 ) ) ;
#36362=CARTESIAN_POINT ( 'NONE',  ( 16.66764709352488083, -4.285714285714297134, 19.00223544648544660 ) ) ;
#36371=CARTESIAN_POINT ( 'NONE',  ( 31.41811726210679723, -18.66951844216680811, 29.82563105361673550 ) ) ;
#36373=SURFACE_SIDE_STYLE ('',( #53570 ) ) ;
#36386=CARTESIAN_POINT ( 'NONE',  ( 91.92393271586485071, -59.99999999999997868, 7.963687493680886575 ) ) ;
#36396=CARTESIAN_POINT ( 'NONE',  ( -107.1317281283567411, -29.99999999989391242, 141.4592884034056226 ) ) ;
#36401=CARTESIAN_POINT ( 'NONE',  ( 82.97322089956890068, -37.79799621115897423, -10.81212016393223330 ) ) ;
#36411=CARTESIAN_POINT ( 'NONE',  ( 77.58893270196534786, -32.55198695177040946, 126.5507534963122254 ) ) ;
#36416=CARTESIAN_POINT ( 'NONE',  ( -107.1080015683288025, -57.65528894494657663, 199.9870551016494744 ) ) ;
#36426=CARTESIAN_POINT ( 'NONE',  ( -50.27151869105384208, -29.73838331303861082, 47.05395887657598308 ) ) ;
#36437=CARTESIAN_POINT ( 'NONE',  ( 76.12557658274100447, -38.35599704320050307, -28.58424740099938077 ) ) ;
#36438=CARTESIAN_POINT ( 'NONE',  ( -86.68002163611333799, -30.00000000000000355, 182.3895294052472309 ) ) ;
#36443=CARTESIAN_POINT ( 'NONE',  ( 86.38368744081424211, -57.57931805107565992, 202.8627517790685886 ) ) ;
#36446=CARTESIAN_POINT ( 'NONE',  ( 28.32874302589403825, -28.95622013529227345, -38.25147845281513526 ) ) ;
#36450=CARTESIAN_POINT ( 'NONE',  ( -61.21521598792825358, -60.00000000000000000, 104.5839967611049843 ) ) ;
#36454=CARTESIAN_POINT ( 'NONE',  ( -86.21391966553235875, -50.15659743610942201, 191.0482607519209921 ) ) ;
#36457=CARTESIAN_POINT ( 'NONE',  ( -3.060819570925945587, -49.92087050383263858, 32.20467130113398468 ) ) ;
#36469=CARTESIAN_POINT ( 'NONE',  ( -13.66642973270730010, -3.469446951953614189E-15, -17.78317311658304689 ) ) ;
#36471=CARTESIAN_POINT ( 'NONE',  ( 98.48959774644481513, -29.99999999999997158, 87.89110648026155559 ) ) ;
#36472=CARTESIAN_POINT ( 'NONE',  ( -78.98497190652808797, -60.32446057300273878, 164.7472437911728207 ) ) ;
#36476=CARTESIAN_POINT ( 'NONE',  ( 21.65479446793900919, -57.67253147474830399, 42.45767589424171717 ) ) ;
#36494=CARTESIAN_POINT ( 'NONE',  ( 71.14491545185333621, -59.99999999999998579, -32.14747307439793644 ) ) ;
#36495=CARTESIAN_POINT ( 'NONE',  ( -70.38749560794603610, -14.21045842199435860, 117.5518806561683078 ) ) ;
#36496=CARTESIAN_POINT ( 'NONE',  ( 21.13798171326017439, -32.51397013334567987, 29.94121226608427833 ) ) ;
#36498=CARTESIAN_POINT ( 'NONE',  ( -35.45552176936942601, -32.57855910578506808, 34.20812180394899826 ) ) ;
#36508=CARTESIAN_POINT ( 'NONE',  ( -57.77825852280871999, -38.34426397139789344, 89.58174797475106743 ) ) ;
#36510=CARTESIAN_POINT ( 'NONE',  ( 90.31977347436274783, -30.00000000000004619, 190.1102673397166996 ) ) ;
#36514=CARTESIAN_POINT ( 'NONE',  ( 80.84952124054477451, -30.00000000000000000, -12.29353673406206937 ) ) ;
#36523=FACE_OUTER_BOUND ( 'NONE', #82021, .T. ) ;
#36533=CARTESIAN_POINT ( 'NONE',  ( 60.80738147631894464, -38.34211472478318683, 98.97440318161500272 ) ) ;
#36537=CARTESIAN_POINT ( 'NONE',  ( 59.97331936630651228, -36.01454316455284754, 70.51342924789160804 ) ) ;
#36553=CARTESIAN_POINT ( 'NONE',  ( 86.52296945539703188, -31.80420732485877977, 185.9741549876141562 ) ) ;
#36558=CARTESIAN_POINT ( 'NONE',  ( 66.68220009426445927, -29.86615941953475684, -22.35219315092264836 ) ) ;
#36563=CARTESIAN_POINT ( 'NONE',  ( -83.15749301179586439, -30.00000000000000355, 44.16248718578879107 ) ) ;
#36567=CARTESIAN_POINT ( 'NONE',  ( 5.530835398441388051, -57.67122193196713908, 41.60095799607574207 ) ) ;
#36572=CARTESIAN_POINT ( 'NONE',  ( -3.821462797104940634, -18.99812766127876174, 27.04963633765945374 ) ) ;
#36576=CARTESIAN_POINT ( 'NONE',  ( 27.01940400982110546, -20.71597891303181527, -32.68677040832736225 ) ) ;
#36579=CARTESIAN_POINT ( 'NONE',  ( -23.90155539105087001, -46.43881993149235399, 32.71507686279078797 ) ) ;
#36582=CARTESIAN_POINT ( 'NONE',  ( -18.55741136884755704, -18.59012425588017692, 27.35021598045728908 ) ) ;
#36596=CARTESIAN_POINT ( 'NONE',  ( 100.0337298755554230, -37.84183079272108330, 190.5202142185493699 ) ) ;
#36610=CARTESIAN_POINT ( 'NONE',  ( -14.08095268206308504, -59.99999999999999289, -44.59230323635646442 ) ) ;
#36612=CARTESIAN_POINT ( 'NONE',  ( 30.07770292690122815, -60.00000000000002132, 43.07392525451504639 ) ) ;
#36615=CARTESIAN_POINT ( 'NONE',  ( -107.5810679786090702, -30.00000000000002487, 145.3413084537935163 ) ) ;
#36616=CARTESIAN_POINT ( 'NONE',  ( 8.339588973682309003, -60.35896782574766917, 33.94344157875258361 ) ) ;
#36618=CARTESIAN_POINT ( 'NONE',  ( -48.09415955654135644, -32.60490053195846372, 45.64808559464792381 ) ) ;
#36627=CARTESIAN_POINT ( 'NONE',  ( 90.04388030624265582, -29.99999999999673861, -4.623977600603863536 ) ) ;
#36628=CARTESIAN_POINT ( 'NONE',  ( -80.00000000000000000, -52.00000000000000000, -19.09707704303353282 ) ) ;
#36633=CARTESIAN_POINT ( 'NONE',  ( 98.42221274954739840, -29.99999999999999645, 189.9688103559335843 ) ) ;
#36640=CARTESIAN_POINT ( 'NONE',  ( 54.06037389446854036, -56.84474632814804806, 65.24979699813212619 ) ) ;
#36647=CARTESIAN_POINT ( 'NONE',  ( -91.44502381616234743, -38.39034967759808836, -8.065114872009855773 ) ) ;
#36650=CARTESIAN_POINT ( 'NONE',  ( 110.4228564477537731, -38.35603995587537440, 183.0518417510637903 ) ) ;
#36652=CARTESIAN_POINT ( 'NONE',  ( 85.16482653615426557, -52.71016913870263920, 3.865994483585396768 ) ) ;
#36671=CARTESIAN_POINT ( 'NONE',  ( -48.90696361353268884, -29.46655839692037304, 44.90436084855983268 ) ) ;
#36672=B_SPLINE_CURVE_WITH_KNOTS ( 'NONE', 3,
 ( #95313, #53776, #20941, #37645, #21445, #61902, #37109, #46750, #29549, #104991, #103396, #46228, #96384, #38166, #69969, #102871, #79640, #31134, #86706, #5756, #12778, #88805, #14357, #63485, #47269, #30064, #104444, #21973, #96899, #64022, #87223, #45696, #30596, #78577, #22513, #95842, #71024, #70508, #54282, #80165, #62946, #62419, #6269, #79116, #38676, #23032, #5239, #103915, #54827, #71542, #55866, #88282, #55353, #39208, #81743, #57473, #7865, #97402, #23564, #17047, #82833, #16501, #32171, #40772, #81218, #82295, #41837, #90399 ),
 .UNSPECIFIED., .F., .F.,
 ( 4, 2, 2, 2, 2, 2, 2, 2, 2, 2, 2, 2, 2, 2, 2, 2, 2, 2, 2, 2, 2, 2, 2, 2, 2, 2, 2, 2, 2, 2, 2, 2, 2, 4 ),
 ( 0.1506134683214106484, 0.1514461594375161591, 0.1522788505536216697, 0.1539442327858326909, 0.1556096150180437121, 0.1572749972502547333, 0.1606057617146767758, 0.1639365261790988182, 0.1705980551079429031, 0.1772595840367869879, 0.1839211129656310728, 0.1905826418944751577, 0.1972441708233192426, 0.2039056997521633274, 0.2172287576098514972, 0.2305518154675396392, 0.2571979311829159509, 0.2838440468982922349, 0.2971671047559804046, 0.3104901626136685744, 0.3238132204713566886, 0.3304747494002007180, 0.3371362783290448029, 0.3437978072578888877, 0.3471285717223109302, 0.3504593361867328616, 0.3537901006511549040, 0.3554554828833658697, 0.3571208651155768354, 0.3579535562316823460, 0.3587862473477878567, 0.3604516295799988779, 0.3621170118122099546, 0.3637823940444209758 ),
 .UNSPECIFIED. ) ;
#36677=CARTESIAN_POINT ( 'NONE',  ( 84.65060209411045378, -39.39181383550964455, 182.1002992804161806 ) ) ;
#36681=CARTESIAN_POINT ( 'NONE',  ( -95.18091335215243021, -45.26558765076902091, 101.5330899563590350 ) ) ;
#36689=CARTESIAN_POINT ( 'NONE',  ( 13.12308708762594911, -59.99999999999999289, 39.71877776328085474 ) ) ;
#36690=CARTESIAN_POINT ( 'NONE',  ( 20.28905229919182318, -25.89519513380055926, 36.90487281070432601 ) ) ;
#36692=CARTESIAN_POINT ( 'NONE',  ( 34.04917345139565299, -23.61692477459231654, 33.16394827626064057 ) ) ;
#36702=CARTESIAN_POINT ( 'NONE',  ( -0.7676806199076874337, -59.99999999999999289, 39.63870301987680733 ) ) ;
#36710=CARTESIAN_POINT ( 'NONE',  ( -1.584597276592265125, -47.40884508701223155, -34.79111164743952855 ) ) ;
#36719=CARTESIAN_POINT ( 'NONE',  ( -94.69289845178556675, -60.00000000000000711, 46.75947207219763868 ) ) ;
#36726=CARTESIAN_POINT ( 'NONE',  ( -84.88152158083789800, -25.51324555084091372, 165.4372525938682656 ) ) ;
#36739=CARTESIAN_POINT ( 'NONE',  ( -84.95435462066053844, -57.67079294309295534, -27.04779982294425977 ) ) ;
#36746=CARTESIAN_POINT ( 'NONE',  ( 84.17695284478443796, -14.21045842199441367, -18.06956050794424584 ) ) ;
#36747=CARTESIAN_POINT ( 'NONE',  ( -91.59718878904411099, -29.99999999999996803, 199.7679234505767738 ) ) ;
#36748=CARTESIAN_POINT ( 'NONE',  ( -57.43764937006150717, -22.13952449013476453, 58.37273624025862517 ) ) ;
#36752=CARTESIAN_POINT ( 'NONE',  ( -101.7629185681098676, -37.82064707025393346, 185.3707029836525351 ) ) ;
#36767=CARTESIAN_POINT ( 'NONE',  ( -27.25852268718031368, -53.39317531337917444, 34.68901558833220378 ) ) ;
#36768=CARTESIAN_POINT ( 'NONE',  ( 47.01925740490068506, -32.61024417345276305, 44.20151961235264793 ) ) ;
#36772=CARTESIAN_POINT ( 'NONE',  ( -85.74841582853835575, -38.65771171113095050, 198.9235328716311813 ) ) ;
#36782=CARTESIAN_POINT ( 'NONE',  ( 111.8879798515403365, -59.99999999999998579, 181.3037615216028371 ) ) ;
#36788=CARTESIAN_POINT ( 'NONE',  ( -78.58275268908097644, -29.99999999999997868, -15.35986885401157842 ) ) ;
#36800=CARTESIAN_POINT ( 'NONE',  ( 83.91197280327008912, -32.50557349083430125, 167.3429057765409027 ) ) ;
#36842=CARTESIAN_POINT ( 'NONE',  ( -110.8672444992828332, -59.99999999999999289, 187.9148104057422302 ) ) ;
#36848=CARTESIAN_POINT ( 'NONE',  ( -83.19761587003101511, -53.69446230421030464, 186.7557214745879151 ) ) ;
#36850=ADVANCED_FACE ( 'NONE', ( #63231 ), #5512, .T. ) ;
#36854=CARTESIAN_POINT ( 'NONE',  ( -86.65393392273510642, -60.14883673965872646, 0.2203813179658791754 ) ) ;
#36860=CARTESIAN_POINT ( 'NONE',  ( 77.40131791002600892, -14.21045842199445630, 153.6837402093314324 ) ) ;
#36861=CARTESIAN_POINT ( 'NONE',  ( -94.21198422502472170, -59.99999999999998579, 13.85022971857252649 ) ) ;
#36863=CARTESIAN_POINT ( 'NONE',  ( -62.93303494182386970, -56.86903391315339462, 89.13530110543882756 ) ) ;
#36865=CARTESIAN_POINT ( 'NONE',  ( 106.6028846201213440, -30.00000000000002487, 192.6838848496860521 ) ) ;
#36867=CARTESIAN_POINT ( 'NONE',  ( 52.88197059271687550, -57.67115856031815468, -39.33710569591229245 ) ) ;
#36878=CARTESIAN_POINT ( 'NONE',  ( -55.33337412123101728, -60.00000000000000000, -36.77909458192313252 ) ) ;
#36891=CARTESIAN_POINT ( 'NONE',  ( 34.09463002446733526, -56.83197632054391590, 38.12211492157798887 ) ) ;
#36892=CARTESIAN_POINT ( 'NONE',  ( 15.50035291838848472, -4.285714285715568117, -20.16952962162309859 ) ) ;
#36904=CARTESIAN_POINT ( 'NONE',  ( 92.51399846021976714, -60.00000000000000711, -1.448676682892423795 ) ) ;
#36912=AXIS2_PLACEMENT_3D ( 'NONE', #2190, #52891, #85258 ) ;
#36913=CARTESIAN_POINT ( 'NONE',  ( -103.5615167553033302, -29.99999999999941380, 196.9855737867926848 ) ) ;
#36918=CARTESIAN_POINT ( 'NONE',  ( 82.32180399435387130, -37.81125714862378828, -13.10781145855886898 ) ) ;
#36921=CARTESIAN_POINT ( 'NONE',  ( 72.61817852641561899, -45.32557365410384875, -22.56083099965291439 ) ) ;
#36930=CARTESIAN_POINT ( 'NONE',  ( 79.07936512157644415, -25.61524179269867219, 127.8490551884245150 ) ) ;
#36935=CARTESIAN_POINT ( 'NONE',  ( -81.06400256271496119, -57.51341943371168952, 199.7941202169005805 ) ) ;
#36942=CARTESIAN_POINT ( 'NONE',  ( -51.43727798272582419, -29.90494385022926593, 49.06446334853066560 ) ) ;
#36954=CARTESIAN_POINT ( 'NONE',  ( -41.84433561564012649, -26.95236078925062628, -36.17932813448958029 ) ) ;
#36955=CARTESIAN_POINT ( 'NONE',  ( -81.17922251170084280, -29.99999999999999289, 141.0271696047036301 ) ) ;
#36957=EDGE_CURVE ( 'NONE', #85958, #38016, #12523, .T. ) ;
#36962=CARTESIAN_POINT ( 'NONE',  ( 80.71913178869228034, -57.51110409648728705, 199.5057488713411260 ) ) ;
#36969=CARTESIAN_POINT ( 'NONE',  ( -69.88144121408996057, -59.99999999999999289, 140.7071162517904668 ) ) ;
#36973=CARTESIAN_POINT ( 'NONE',  ( -85.83393798185170454, -35.62537476688432747, 184.8253129914004376 ) ) ;
#36976=CARTESIAN_POINT ( 'NONE',  ( -1.020036429124608679, -56.88429985501548458, 33.37036660210496564 ) ) ;
#36981=( GEOMETRIC_REPRESENTATION_CONTEXT ( 3 ) GLOBAL_UNCERTAINTY_ASSIGNED_CONTEXT ( ( #88015 ) ) GLOBAL_UNIT_ASSIGNED_CONTEXT ( ( #61140, #60097, #28271 ) ) REPRESENTATION_CONTEXT ( 'NONE', 'WORKASPACE' ) );
#36989=CARTESIAN_POINT ( 'NONE',  ( 6.601913983208107517, -4.285714285714895766, -24.56594385547655790 ) ) ;
#36991=CARTESIAN_POINT ( 'NONE',  ( 110.8743008064580664, -59.99999999999998579, 132.3768192050824268 ) ) ;
#36992=CARTESIAN_POINT ( 'NONE',  ( -79.97908447249672292, -29.09054715422505666, 135.2929009280034904 ) ) ;
#36995=FILL_AREA_STYLE_COLOUR ( '', #5093 ) ;
#37014=ORIENTED_EDGE ( 'NONE', *, *, #2655, .F. ) ;
#37015=CARTESIAN_POINT ( 'NONE',  ( 2.783335637615752756, -60.00000000000000711, -42.63908079511851668 ) ) ;
#37016=CARTESIAN_POINT ( 'NONE',  ( -74.04808884210443409, -14.21045842199433018, 133.5060932470338741 ) ) ;
#37017=CARTESIAN_POINT ( 'NONE',  ( 29.47255165424405021, -60.33275022954688893, 36.60376788069852694 ) ) ;
#37021=CARTESIAN_POINT ( 'NONE',  ( -38.83480971963878403, -32.60089154014189461, 36.29250106144353083 ) ) ;
#37023=CARTESIAN_POINT ( 'NONE',  ( -25.05982991920904368, -4.285714285714296246, 3.301565691951511727 ) ) ;
#37030=CARTESIAN_POINT ( 'NONE',  ( -59.57757130603854279, -38.34325986228989791, 95.06209312383862198 ) ) ;
#37032=CARTESIAN_POINT ( 'NONE',  ( 99.71799369003751679, -30.00000000000000000, 186.7405845989215152 ) ) ;
#37035=CARTESIAN_POINT ( 'NONE',  ( 81.43683860099746141, -30.00000000000000000, -9.778545213351637955 ) ) ;
#37052=ORIENTED_EDGE ( 'NONE', *, *, #16962, .T. ) ;
#37054=CARTESIAN_POINT ( 'NONE',  ( 60.39313911039658223, -38.34249553177825476, 97.64561399884981086 ) ) ;
#37059=CARTESIAN_POINT ( 'NONE',  ( 65.12892237437687015, -22.10168432192453380, 77.58864540890802175 ) ) ;
#37078=CARTESIAN_POINT ( 'NONE',  ( 85.89238073966772902, -42.87991800006673770, 188.0195928903932270 ) ) ;
#37084=CARTESIAN_POINT ( 'NONE',  ( 44.73608156750558607, -57.67080212258656502, -40.94571872030276438 ) ) ;
#37089=CARTESIAN_POINT ( 'NONE',  ( -99.41669103005973795, -30.00000000000000355, 148.3901553398027318 ) ) ;
#37092=CARTESIAN_POINT ( 'NONE',  ( 19.37286937753119176, -57.67185718821608731, 42.13248506237696489 ) ) ;
#37100=CARTESIAN_POINT ( 'NONE',  ( 11.58986075927344750, -16.51611378721433709, -34.67831674966147659 ) ) ;
#37105=CARTESIAN_POINT ( 'NONE',  ( -18.09414824793106291, -49.92059396303074692, 32.54756357241360121 ) ) ;
#37109=CARTESIAN_POINT ( 'NONE',  ( -86.29988659680776664, -60.00000000000005684, -13.08005935856397706 ) ) ;
#37117=CARTESIAN_POINT ( 'NONE',  ( -9.581570546826366552, -59.99999999999998579, -42.43254358624957234 ) ) ;
#37121=CARTESIAN_POINT ( 'NONE',  ( 102.5598772604434146, -52.71961633189020091, 191.0344027114808512 ) ) ;
#37122=CARTESIAN_POINT ( 'NONE',  ( 40.62786202543021830, -35.40383002152289293, 38.30709763539996970 ) ) ;
#37132=CARTESIAN_POINT ( 'NONE',  ( -95.43381492254501097, -60.00000000004885692, 32.99689897427253982 ) ) ;
#37134=CARTESIAN_POINT ( 'NONE',  ( 93.55038125663071469, -60.00000000000243006, -16.95329214822379882 ) ) ;
#37138=CARTESIAN_POINT ( 'NONE',  ( -103.3502313461265771, -29.99999999999994671, 116.5677832811329893 ) ) ;
#37139=CARTESIAN_POINT ( 'NONE',  ( 4.087897576844674141, -49.91562588958777980, 32.20126423648752478 ) ) ;
#37141=CARTESIAN_POINT ( 'NONE',  ( -47.63688977005685388, -49.90354645496473296, 50.26338200732071471 ) ) ;
#37155=CARTESIAN_POINT ( 'NONE',  ( 55.69284664406904284, -38.34494919613591435, 83.45409790606751699 ) ) ;
#37160=CARTESIAN_POINT ( 'NONE',  ( 99.05156608437981447, -30.00000000000000355, 188.7076821412088918 ) ) ;
#37161=ADVANCED_FACE ( 'NONE', ( #84188 ), #76912, .F. ) ;
#37166=CARTESIAN_POINT ( 'NONE',  ( 54.49441714554848915, -36.02968114152674417, 57.85172732363746917 ) ) ;
#37170=CARTESIAN_POINT ( 'NONE',  ( -86.02727662308166146, -38.36114455327187045, -21.87132400657947429 ) ) ;
#37173=CARTESIAN_POINT ( 'NONE',  ( 101.5818437543623531, -38.45065087239409962, 199.8849258718219630 ) ) ;
#37175=CARTESIAN_POINT ( 'NONE',  ( 82.65689217004747036, -37.85983059181354804, 4.241147794711082497 ) ) ;
#37192=CARTESIAN_POINT ( 'NONE',  ( -28.95748274387464605, -23.76855312348390825, 38.32284098381386173 ) ) ;
#37195=CARTESIAN_POINT ( 'NONE',  ( 82.72527133745752792, -60.86633776179802169, 189.9846870754455210 ) ) ;
#37200=CARTESIAN_POINT ( 'NONE',  ( -97.60405816678809288, -45.26544898532436889, 115.8977766532089930 ) ) ;
#37207=CARTESIAN_POINT ( 'NONE',  ( 13.89252497407058939, -22.08393062168078202, 35.78427392513001593 ) ) ;
#37209=CARTESIAN_POINT ( 'NONE',  ( 49.49891584455601645, -29.58924679890871090, 45.82294932986923897 ) ) ;
#37227=AXIS2_PLACEMENT_3D ( 'NONE', #56237, #6112, #39037 ) ;
#37232=CARTESIAN_POINT ( 'NONE',  ( -4.768224440014436460, -47.40888642635074746, -34.73453581626768027 ) ) ;
#37241=CARTESIAN_POINT ( 'NONE',  ( -91.86040266156631162, -59.99999999999997868, 11.95720016906147798 ) ) ;
#37246=CARTESIAN_POINT ( 'NONE',  ( 9.999999999999998224, -15.00000000000000000, -9.999999999999998224 ) ) ;
#37248=CARTESIAN_POINT ( 'NONE',  ( -83.80836329334010770, -32.51672879621551715, 166.3324284733673721 ) ) ;
#37249=ORIENTED_EDGE ( 'NONE', *, *, #22687, .T. ) ;
#37250=CARTESIAN_POINT ( 'NONE',  ( -2.220412017512216618, -0.000000000000000000, 16.90656889033980192 ) ) ;
#37252=VECTOR ( 'NONE', #75019, 1000.000000000000000 ) ;
#37260=CARTESIAN_POINT ( 'NONE',  ( -95.95698421656685184, -57.67166530053860640, 41.39248336299490916 ) ) ;
#37265=CARTESIAN_POINT ( 'NONE',  ( 65.67877680238373728, -29.99999999999995026, -31.25179767064105363 ) ) ;
#37266=CARTESIAN_POINT ( 'NONE',  ( -73.77866262884730020, -30.00000000000000711, 147.9509455049667395 ) ) ;
#37268=CARTESIAN_POINT ( 'NONE',  ( -54.06122363970894895, -46.44091381175636002, 61.05526970200972414 ) ) ;
#37272=CARTESIAN_POINT ( 'NONE',  ( -101.5936365789223856, -52.72169881341778819, 192.6675009559352532 ) ) ;
#37273=CARTESIAN_POINT ( 'NONE',  ( 96.81745522565726958, -37.99999999999980815, 192.8977754549547967 ) ) ;
#37290=CARTESIAN_POINT ( 'NONE',  ( -28.24552693224729794, -32.53317030909266805, 31.34561990023201972 ) ) ;
#37292=CARTESIAN_POINT ( 'NONE',  ( 48.53168779318080084, -22.21808085982860703, 43.06350356119703804 ) ) ;
#37295=CARTESIAN_POINT ( 'NONE',  ( -89.68492724561200191, -38.52030381430500938, 200.4876829703964347 ) ) ;
#37298=CARTESIAN_POINT ( 'NONE',  ( 90.75236045938613927, -38.34260670370428414, 6.374254514712724529 ) ) ;
#37307=PLANE ( 'NONE',  #26336 ) ;
#37308=CARTESIAN_POINT ( 'NONE',  ( 111.3516866354051160, -59.99999999999999289, 185.3684648513999491 ) ) ;
#37316=CARTESIAN_POINT ( 'NONE',  ( -81.08763726869537436, -30.00000000000003908, 2.435961963529629681 ) ) ;
#37318=CARTESIAN_POINT ( 'NONE',  ( -82.24571663913680197, -38.83862773915732447, 196.1822678393787953 ) ) ;
#37331=CARTESIAN_POINT ( 'NONE',  ( 81.73802953284047135, -49.94979035245339816, 174.6693918275601618 ) ) ;
#37352=CARTESIAN_POINT ( 'NONE',  ( 89.99999999999997158, -60.00000000000000000, 188.5238439516623146 ) ) ;
#37362=CARTESIAN_POINT ( 'NONE',  ( 2.500000000000002665, -30.00000000000000000, -13.00000000000000000 ) ) ;
#37365=ORIENTED_EDGE ( 'NONE', *, *, #84813, .F. ) ;
#37372=CARTESIAN_POINT ( 'NONE',  ( -92.52372448017906947, -60.00000000000000000, 202.4166223421563018 ) ) ;
#37380=CARTESIAN_POINT ( 'NONE',  ( -85.21723363474887947, -28.80621494017632145, 174.9461519470255837 ) ) ;
#37387=CARTESIAN_POINT ( 'NONE',  ( -85.81038825978107809, -52.70812745589994108, 30.16071544517509651 ) ) ;
#37391=( NAMED_UNIT ( * ) PLANE_ANGLE_UNIT ( ) SI_UNIT ( $, .RADIAN. ) );
#37393=CARTESIAN_POINT ( 'NONE',  ( 78.25600647866326653, -14.21045842199443499, 182.3349015425907851 ) ) ;
#37395=CARTESIAN_POINT ( 'NONE',  ( -89.06819603267832974, -14.21045842199437637, 44.46121640280500031 ) ) ;
#37397=CARTESIAN_POINT ( 'NONE',  ( -63.69277339041742891, -39.48556901039047062, 82.38618134814525718 ) ) ;
#37399=CARTESIAN_POINT ( 'NONE',  ( 99.10782808284749024, -14.21045842199446163, 197.1815751231716263 ) ) ;
#37401=CARTESIAN_POINT ( 'NONE',  ( 79.10866139746512715, -59.99999999997309175, 198.8830511339313318 ) ) ;
#37402=ORIENTED_EDGE ( 'NONE', *, *, #99307, .F. ) ;
#37411=CARTESIAN_POINT ( 'NONE',  ( -90.96217874645275003, -59.99999999999998579, -17.00786546406066435 ) ) ;
#37415=CARTESIAN_POINT ( 'NONE',  ( 15.38541618194248350, -4.285714285714296246, 20.05453516056601515 ) ) ;
#37425=CARTESIAN_POINT ( 'NONE',  ( 37.51919295870404625, -49.89018639253918508, 39.00778217076621956 ) ) ;
#37426=CARTESIAN_POINT ( 'NONE',  ( -6.601913983209747983, -4.285714285713511096, 24.56594385547482418 ) ) ;
#37437=CARTESIAN_POINT ( 'NONE',  ( 92.42316227055287925, -60.00000000000002132, -0.1668662530303857139 ) ) ;
#37444=CARTESIAN_POINT ( 'NONE',  ( -88.81473527931045453, -30.00000000002773604, 198.9409494650124657 ) ) ;
#37465=CARTESIAN_POINT ( 'NONE',  ( 77.91231580246096655, -46.43304605102353122, 140.2301567752059270 ) ) ;
#37473=CARTESIAN_POINT ( 'NONE',  ( -81.37675186042847031, -57.51598868027654987, 200.0426579070166895 ) ) ;
#37481=CARTESIAN_POINT ( 'NONE',  ( -51.05793882480850243, -29.86182477906456256, 48.38375129339014791 ) ) ;
#37490=DIRECTION ( 'NONE',  ( 0.000000000000000000, -1.000000000000000000, 0.000000000000000000 ) ) ;
#37493=CARTESIAN_POINT ( 'NONE',  ( -71.80342408229671491, -29.99999999999998579, -19.71767938363507255 ) ) ;
#37494=CARTESIAN_POINT ( 'NONE',  ( -61.79326048008234551, -30.00000000000000711, 71.46593052723335404 ) ) ;
#37499=CARTESIAN_POINT ( 'NONE',  ( 76.92828183364126460, -57.52628917366442352, 194.9584416617772149 ) ) ;
#37500=FACE_OUTER_BOUND ( 'NONE', #87098, .T. ) ;
#37506=CARTESIAN_POINT ( 'NONE',  ( -63.35497338199800055, -60.00000000000000000, 112.0391477965111022 ) ) ;
#37511=CARTESIAN_POINT ( 'NONE',  ( -85.78111746350951705, -35.63734805798310390, 184.6310799642125460 ) ) ;
#37514=CARTESIAN_POINT ( 'NONE',  ( 4.938669310872844932E-05, -53.40265726396589940, 32.79009283693002175 ) ) ;
#37526=( LENGTH_UNIT ( ) NAMED_UNIT ( * ) SI_UNIT ( .MILLI., .METRE. ) );
#37528=CARTESIAN_POINT ( 'NONE',  ( 86.99610535363679276, -14.21045842199441012, 24.11248255592787615 ) ) ;
#37529=CARTESIAN_POINT ( 'NONE',  ( -77.74926328355248017, -60.31560680552357212, 154.2294776400503622 ) ) ;
#37533=FILL_AREA_STYLE ('',( #19765 ) ) ;
#37551=CARTESIAN_POINT ( 'NONE',  ( 92.72480697121025628, -60.00000000000000000, -5.027149249431430711 ) ) ;
#37552=CARTESIAN_POINT ( 'NONE',  ( -54.44990204170284898, -30.00000000000008882, 75.82925260777241760 ) ) ;
#37553=CARTESIAN_POINT ( 'NONE',  ( 27.79149109135314788, -36.00466587923170181, 31.83270667620929828 ) ) ;
#37570=CARTESIAN_POINT ( 'NONE',  ( 100.7707649814656747, -30.00000000000000355, 180.9804943645408457 ) ) ;
#37574=CARTESIAN_POINT ( 'NONE',  ( 80.77803734578861850, -30.00000000000000000, -12.46495713760978852 ) ) ;
#37593=CARTESIAN_POINT ( 'NONE',  ( 60.52345103412395844, -38.34237732095000695, 98.06192674467523318 ) ) ;
#37597=CARTESIAN_POINT ( 'NONE',  ( 64.00467378430177234, -29.05420584686936891, 77.96572560711764766 ) ) ;
#37602=CARTESIAN_POINT ( 'NONE',  ( -46.42533371640924855, -34.72140787405426465, -36.69163149917219613 ) ) ;
#37615=CARTESIAN_POINT ( 'NONE',  ( 85.27851683770271052, -57.46677582188632272, 192.4431409699905089 ) ) ;
#37623=CARTESIAN_POINT ( 'NONE',  ( -100.3777161340725712, -29.99999999999999289, 157.7761675202767151 ) ) ;
#37627=CARTESIAN_POINT ( 'NONE',  ( 1.031133051057990135, -57.67120256293672043, 41.61115920477558916 ) ) ;
#37640=ORIENTED_EDGE ( 'NONE', *, *, #50996, .F. ) ;
#37643=CARTESIAN_POINT ( 'NONE',  ( -15.54353313750226206, -32.51340815750653945, 29.48048180118074413 ) ) ;
#37645=CARTESIAN_POINT ( 'NONE',  ( -85.70835096055856184, -60.00000000000002132, -14.66632915116390734 ) ) ;
#37650=CARTESIAN_POINT ( 'NONE',  ( -89.99999999999997158, -52.00000000000000000, 194.0238439516549818 ) ) ;
#37672=CARTESIAN_POINT ( 'NONE',  ( -87.54930676208033447, -60.00000000002437872, -25.45872903247207475 ) ) ;
#37675=CARTESIAN_POINT ( 'NONE',  ( 37.31558637970096015, -60.00000000000000000, 48.70948680922666085 ) ) ;
#37678=CIRCLE ( 'NONE', #35993, 15.00000000000000000 ) ;
#37679=CARTESIAN_POINT ( 'NONE',  ( -101.2960459709432826, -29.99999999999998579, 104.2733491104911963 ) ) ;
#37680=CARTESIAN_POINT ( 'NONE',  ( 11.16551004579882189, -25.54854244899442506, 28.17187544474615635 ) ) ;
#37683=CARTESIAN_POINT ( 'NONE',  ( -47.68213074599328394, -42.98560256933807722, 48.22320990812892205 ) ) ;
#37693=CARTESIAN_POINT ( 'NONE',  ( 44.47534377888502632, -38.31160956920666649, 57.00192013341538910 ) ) ;
#37697=CARTESIAN_POINT ( 'NONE',  ( 98.09172150708243976, -29.99999999999999645, 190.4342177531940763 ) ) ;
#37704=CARTESIAN_POINT ( 'NONE',  ( 54.02217166477871757, -36.03114398899570858, 56.87927286532268312 ) ) ;
#37714=CARTESIAN_POINT ( 'NONE',  ( 102.1500853529942106, -38.44127923276875691, 199.6050571543175067 ) ) ;
#37716=CARTESIAN_POINT ( 'NONE',  ( 86.46873085151457872, -60.13455952585971431, 2.723771532636757531 ) ) ;
#37735=CARTESIAN_POINT ( 'NONE',  ( 53.08934989192470510, -29.99999999999999289, 52.21148837440654944 ) ) ;
#37738=CARTESIAN_POINT ( 'NONE',  ( 85.27564894550540942, -32.22278697073298304, 179.6136003457102106 ) ) ;
#37742=CARTESIAN_POINT ( 'NONE',  ( -100.8220720648846225, -60.15490406098927423, 120.1837212289833019 ) ) ;
#37746=CARTESIAN_POINT ( 'NONE',  ( -5.687071598576536324, -21.74269005626036844, -38.54672360651682084 ) ) ;
#37748=CARTESIAN_POINT ( 'NONE',  ( 12.43567954112019969, -21.33041175957170310, 35.61117015663748475 ) ) ;
#37750=CARTESIAN_POINT ( 'NONE',  ( 39.77890293349060613, -26.23074748553104385, 35.82129514820142191 ) ) ;
#37757=CARTESIAN_POINT ( 'NONE',  ( -83.17009416728905080, -38.00000000000003553, -3.028942620234869931 ) ) ;
#37764=CARTESIAN_POINT ( 'NONE',  ( -6.281393465144616606, -34.58963968333188888, -32.56267242852022292 ) ) ;
#37774=CARTESIAN_POINT ( 'NONE',  ( -92.24153208330554321, -59.99999999999999289, 2.317352427123469560 ) ) ;
#37783=CARTESIAN_POINT ( 'NONE',  ( -83.70341740888480331, -32.52351292720956621, 165.3169881577036620 ) ) ;
#37785=CARTESIAN_POINT ( 'NONE',  ( 2.083846472846741813E-15, -8.673617379884035472E-16, 17.01589776168603407 ) ) ;
#37794=CARTESIAN_POINT ( 'NONE',  ( -109.3314759607053759, -57.67120315069445269, 124.6891463060778165 ) ) ;
#37802=CARTESIAN_POINT ( 'NONE',  ( 88.18294634653494768, -59.99999999999992895, -24.85591942078231043 ) ) ;
#37804=CARTESIAN_POINT ( 'NONE',  ( -70.80424915565322408, -29.99999999999997513, 131.6008933728038528 ) ) ;
#37805=CARTESIAN_POINT ( 'NONE',  ( -54.32531917774948482, -60.32353084016035893, 67.31808107234573413 ) ) ;
#37809=CARTESIAN_POINT ( 'NONE',  ( -99.49925588239455010, -37.80182837650123417, 191.3413508579977531 ) ) ;
#37821=CARTESIAN_POINT ( 'NONE',  ( 69.53704851309812796, -30.00000000000000000, 93.84895101583573762 ) ) ;
#37825=CARTESIAN_POINT ( 'NONE',  ( -26.74884781052236704, -25.57352610173401430, 29.74563790467716728 ) ) ;
#37828=CARTESIAN_POINT ( 'NONE',  ( 48.09347440250294881, -32.60269077776137436, 45.64648356772737259 ) ) ;
#37831=CARTESIAN_POINT ( 'NONE',  ( -108.6452951072574820, -38.35698101357876055, 191.2191590237300147 ) ) ;
#37833=CARTESIAN_POINT ( 'NONE',  ( 91.19386398214668077, -38.35691295928401701, -0.5933418896404458742 ) ) ;
#37841=CARTESIAN_POINT ( 'NONE',  ( 103.3672439911610468, -59.99999999999999289, 200.3982682180039490 ) ) ;
#37851=CARTESIAN_POINT ( 'NONE',  ( -103.7550299252929591, -38.41758574445464802, 198.5926835292501949 ) ) ;
#37864=CARTESIAN_POINT ( 'NONE',  ( 80.87169800746870862, -60.48560008594591153, 182.4047845298172206 ) ) ;
#37867=VERTEX_POINT ( 'NONE', #104481 ) ;
#37875=CARTESIAN_POINT ( 'NONE',  ( -76.72470682087703153, -30.00000000000000355, -16.84832387072587778 ) ) ;
#37901=CARTESIAN_POINT ( 'NONE',  ( -102.7322205242310247, -60.00000000000000000, 200.7630764697867960 ) ) ;
#37904=CARTESIAN_POINT ( 'NONE',  ( -10.00000000000000178, -15.00000000000000000, -9.999999999999998224 ) ) ;
#37907=CARTESIAN_POINT ( 'NONE',  ( -85.12052891753060635, -28.84667419981521874, 173.9529900625116454 ) ) ;
#37913=CARTESIAN_POINT ( 'NONE',  ( -83.68684263103561705, -45.26603780466695071, 9.535851223383053465 ) ) ;
#37921=CARTESIAN_POINT ( 'NONE',  ( 86.51021125171571668, -60.00000000000013500, 203.5141634203183685 ) ) ;
#37924=CARTESIAN_POINT ( 'NONE',  ( -98.48977711285814962, -30.00000000000000355, 87.89215492326917456 ) ) ;
#37925=CARTESIAN_POINT ( 'NONE',  ( -64.36786927653166401, -39.48549010098479073, 84.34220923411332649 ) ) ;
#37928=CARTESIAN_POINT ( 'NONE',  ( 77.52758066070661869, -59.99999999999010214, 196.9906909439896765 ) ) ;
#37940=CARTESIAN_POINT ( 'NONE',  ( -76.56013186602308451, -60.00000000000000000, -29.77863996211247510 ) ) ;
#37956=CARTESIAN_POINT ( 'NONE',  ( 36.03585763630033512, -42.96736410595855915, 36.59562221089151990 ) ) ;
#37957=CARTESIAN_POINT ( 'NONE',  ( -4.453875240779026079, -1.734723475976807094E-15, 16.57301948836938621 ) ) ;
#37970=CARTESIAN_POINT ( 'NONE',  ( 92.44495282290664306, -59.99999999999999289, -0.4686678803088884515 ) ) ;
#37978=CARTESIAN_POINT ( 'NONE',  ( -84.32296871598593668, -29.99999999998828670, -21.60099904174990115 ) ) ;
#37994=CARTESIAN_POINT ( 'NONE',  ( 81.08675078009645176, -29.09168970534348020, 141.3822325320448101 ) ) ;
#37999=CARTESIAN_POINT ( 'NONE',  ( -78.78539465073522763, -57.50642106797575082, 197.5849804933186817 ) ) ;
#38010=CARTESIAN_POINT ( 'NONE',  ( -5.638837409264774614, -12.95953527002633976, 32.08345554597801197 ) ) ;
#38016=VERTEX_POINT ( 'NONE', #62724 ) ;
#38021=CARTESIAN_POINT ( 'NONE',  ( -1.445468217397182231, -17.74378107465255283, -37.96072284730425395 ) ) ;
#38022=CARTESIAN_POINT ( 'NONE',  ( -83.04267475782658892, -30.00000000000000711, 153.2271410443097182 ) ) ;
#38027=CARTESIAN_POINT ( 'NONE',  ( 91.21504626101743440, -57.61349245510880479, 204.2098318074243366 ) ) ;
#38033=CARTESIAN_POINT ( 'NONE',  ( -53.97748731286613832, -60.00000000000002842, 82.35806573917696483 ) ) ;
#38038=CARTESIAN_POINT ( 'NONE',  ( -84.08473047087470320, -61.05543080211507601, 192.4300456549544833 ) ) ;
#38045=EDGE_CURVE ( 'NONE', #91737, #16098, #51241, .T. ) ;
#38047=CARTESIAN_POINT ( 'NONE',  ( -84.67955570590166303, -52.73943624728606494, -13.91631340859395571 ) ) ;
#38055=CARTESIAN_POINT ( 'NONE',  ( -22.23822744035697241, -8.673617379884035472E-16, -2.910977163147234759 ) ) ;
#38057=CARTESIAN_POINT ( 'NONE',  ( 94.38107034336813683, -59.99999999999990763, 5.298252861571447703 ) ) ;
#38059=CARTESIAN_POINT ( 'NONE',  ( -78.23876340934074847, -49.90743072093854948, 145.7851689650335061 ) ) ;
#38063=CARTESIAN_POINT ( 'NONE',  ( 87.55754732123112660, -57.59262797547410173, 203.3067698811781838 ) ) ;
#38083=CARTESIAN_POINT ( 'NONE',  ( -75.56794833712217496, -14.21045842199431597, 141.5492349273399952 ) ) ;
#38084=CARTESIAN_POINT ( 'NONE',  ( 26.88634610105399858, -60.34360723818206651, 35.78200920591456935 ) ) ;
#38095=CARTESIAN_POINT ( 'NONE',  ( 64.99863289610547668, -29.99999999999999289, 80.18763367229007599 ) ) ;
#38099=CARTESIAN_POINT ( 'NONE',  ( 76.87505874220391888, -29.99999999999999645, -16.73993432065925546 ) ) ;
#38101=DIRECTION ( 'NONE',  ( -0.000000000000000000, -1.000000000000000000, -0.000000000000000000 ) ) ;
#38123=CARTESIAN_POINT ( 'NONE',  ( -83.88445482477082749, -59.99999999999995737, 191.6821729358339610 ) ) ;
#38124=CARTESIAN_POINT ( 'NONE',  ( 63.25588472527466877, -46.43434427221221483, 84.68567794870051557 ) ) ;
#38127=CARTESIAN_POINT ( 'NONE',  ( -46.13793940742458233, -34.64890882579388887, -36.73075005924651748 ) ) ;
#38141=CARTESIAN_POINT ( 'NONE',  ( 86.76698164667543267, -35.43929735535429870, 187.6249619233078363 ) ) ;
#38148=CARTESIAN_POINT ( 'NONE',  ( -99.88944901110127716, -30.00000000000000355, 186.0585768036329739 ) ) ;
#38151=CARTESIAN_POINT ( 'NONE',  ( 30.90980334511036176, -57.68590788500401345, 45.77300714667035919 ) ) ;
#38158=CARTESIAN_POINT ( 'NONE',  ( 9.452785795943286828, -16.11909601877263754, -34.86652532129186710 ) ) ;
#38160=CARTESIAN_POINT ( 'NONE',  ( -86.93315611284394606, -53.75507749461908702, 192.8295728004336240 ) ) ;
#38164=CARTESIAN_POINT ( 'NONE',  ( -12.13119334609016065, -18.58662857061450069, 27.03411493363265450 ) ) ;
#38166=CARTESIAN_POINT ( 'NONE',  ( -86.95270011918000819, -60.00000000000005684, -4.645723306006363629 ) ) ;
#38169=ORIENTED_EDGE ( 'NONE', *, *, #89227, .T. ) ;
#38181=CARTESIAN_POINT ( 'NONE',  ( 6.243930039575695118E-05, -60.00000000000000000, 42.00000000000000711 ) ) ;
#38194=AXIS2_PLACEMENT_3D ( 'NONE', #45313, #52857, #55360 ) ;
#38195=CARTESIAN_POINT ( 'NONE',  ( -109.2418094552294718, -60.00000000000121503, 198.0553673896860687 ) ) ;
#38196=CARTESIAN_POINT ( 'NONE',  ( 30.78144837821654889, -60.00000000000000000, -43.20504364394649599 ) ) ;
#38200=CARTESIAN_POINT ( 'NONE',  ( -88.56648999577124926, -14.21045842199433018, 40.40162738224969274 ) ) ;
#38201=CARTESIAN_POINT ( 'NONE',  ( 9.184983414718331574, -35.99160910021836202, 29.89037362904370099 ) ) ;
#38202=CARTESIAN_POINT ( 'NONE',  ( -49.20447750785626084, -25.67215719499521143, 45.04643150312214317 ) ) ;
#38212=CARTESIAN_POINT ( 'NONE',  ( 93.19143838610155228, -29.99999999999330669, 199.8529442901022151 ) ) ;
#38215=CARTESIAN_POINT ( 'NONE',  ( 97.95297396224403030, -30.00000000000000711, 190.5773321744065925 ) ) ;
#38230=CARTESIAN_POINT ( 'NONE',  ( 101.5753516748054750, -38.45075819519839655, 199.8879498216157344 ) ) ;
#38232=CARTESIAN_POINT ( 'NONE',  ( 82.47009247757118544, -37.85521738824169091, 15.76104204749702653 ) ) ;
#38240=( GEOMETRIC_REPRESENTATION_CONTEXT ( 3 ) GLOBAL_UNCERTAINTY_ASSIGNED_CONTEXT ( ( #17141 ) ) GLOBAL_UNIT_ASSIGNED_CONTEXT ( ( #9670, #69012, #2651 ) ) REPRESENTATION_CONTEXT ( 'NONE', 'WORKASPACE' ) );
#38243=EDGE_CURVE ( 'NONE', #37867, #69966, #74941, .T. ) ;
#38252=CARTESIAN_POINT ( 'NONE',  ( 2.680339019791157629, -14.91472760605375036, 34.48196116050767301 ) ) ;
#38257=CARTESIAN_POINT ( 'NONE',  ( 85.67508185048706082, -28.57312383954360868, 179.3342417396961253 ) ) ;
#38262=CARTESIAN_POINT ( 'NONE',  ( 93.83510257185203329, -57.67426556498583778, 12.53502779676051304 ) ) ;
#38272=CARTESIAN_POINT ( 'NONE',  ( 39.96643535430156646, -26.31157452080049808, 35.93915362622938403 ) ) ;
#38285=CARTESIAN_POINT ( 'NONE',  ( 6.197033621690949623, -21.77038157703285037, -30.42749805555791198 ) ) ;
#38286=EDGE_CURVE ( 'NONE', #105826, #26612, #32581, .T. ) ;
#38294=CARTESIAN_POINT ( 'NONE',  ( -92.53755267726359079, -60.00000000000000711, -1.808094159106042653 ) ) ;
#38302=CARTESIAN_POINT ( 'NONE',  ( -80.00123558984591909, -60.37367201449674070, 175.0854090040365065 ) ) ;
#38304=CARTESIAN_POINT ( 'NONE',  ( -15.29459302239368235, 0.000000000000000000, -7.540142361543696659 ) ) ;
#38313=CARTESIAN_POINT ( 'NONE',  ( -84.33710589588049800, -57.55216090540037044, 201.9444809301270141 ) ) ;
#38319=CARTESIAN_POINT ( 'NONE',  ( 87.78053949331578565, -14.21045842199421294, -8.623972743651103556 ) ) ;
#38321=CARTESIAN_POINT ( 'NONE',  ( -67.17213121490354411, -60.00000000000000000, 138.9710117141604826 ) ) ;
#38322=CARTESIAN_POINT ( 'NONE',  ( -54.89818758952581845, -56.85426884866628683, 67.23925021769613863 ) ) ;
#38326=CARTESIAN_POINT ( 'NONE',  ( -100.7112993965425147, -45.26202956731061278, 191.7609640039119370 ) ) ;
#38331=CARTESIAN_POINT ( 'NONE',  ( -15.51619600599612525, -60.00000000000000000, 39.81136932477215140 ) ) ;
#38342=CARTESIAN_POINT ( 'NONE',  ( -27.79213640563233767, -36.00755841895716003, 31.83339595010198408 ) ) ;
#38343=MECHANICAL_DESIGN_GEOMETRIC_PRESENTATION_REPRESENTATION('',(#84814),#65862);
#38344=EDGE_LOOP ( 'NONE', ( #64597, #48670, #80215, #45234, #33120, #69664 ) ) ;
#38346=CARTESIAN_POINT ( 'NONE',  ( 46.18361529899789275, -22.24103619873750404, 40.23939593157469119 ) ) ;
#38350=CARTESIAN_POINT ( 'NONE',  ( -110.8441515072943986, -38.35618291059805074, 166.5699242065477677 ) ) ;
#38352=CARTESIAN_POINT ( 'NONE',  ( 90.05187521117480287, -38.39608854082356970, -15.95136963641786920 ) ) ;
#38359=CARTESIAN_POINT ( 'NONE',  ( 93.12889346891942921, -59.99999999999998579, 202.4813445689636922 ) ) ;
#38362=CARTESIAN_POINT ( 'NONE',  ( 56.92742074447681233, -32.55220054188133361, 61.62941135532160786 ) ) ;
#38367=CARTESIAN_POINT ( 'NONE',  ( -99.91270067421781675, -38.46799138967286780, 200.5326549990056151 ) ) ;
#38378=CARTESIAN_POINT ( 'NONE',  ( 85.31446539190037015, -22.01966134143505371, 163.9754572180653440 ) ) ;
#38395=CARTESIAN_POINT ( 'NONE',  ( -0.1795511817381551245, -18.03052986994432061, 35.00506736773241556 ) ) ;
#38412=EDGE_LOOP ( 'NONE', ( #44222, #90043, #51472, #5886 ) ) ;
#38420=CARTESIAN_POINT ( 'NONE',  ( -111.0763646976983381, -60.00000000000000000, 152.8868246609566484 ) ) ;
#38425=CARTESIAN_POINT ( 'NONE',  ( -86.13551971958956699, -21.45869068250014067, 175.8984454080961370 ) ) ;
#38433=CARTESIAN_POINT ( 'NONE',  ( -84.93247734541225213, -52.70439048363899559, 14.92132537576424589 ) ) ;
#38438=CARTESIAN_POINT ( 'NONE',  ( 97.75109942996037660, -59.99999999999985789, 204.9114775063931120 ) ) ;
#38439=CARTESIAN_POINT ( 'NONE',  ( -110.2447566669111154, -59.99999999999998579, 128.1452744908969521 ) ) ;
#38440=CARTESIAN_POINT ( 'NONE',  ( -63.15306896468232623, -53.39223773315245580, 87.98131365993890540 ) ) ;
#38443=CARTESIAN_POINT ( 'NONE',  ( 76.19937483932648092, -59.99999999999009503, 194.9015389639207285 ) ) ;
#38454=CARTESIAN_POINT ( 'NONE',  ( -52.60051048173597366, -60.00000000000000000, -37.38023807311972746 ) ) ;
#38458=CARTESIAN_POINT ( 'NONE',  ( 23.93420880016849139, -4.285714285714295357, 8.127057321558249114 ) ) ;
#38467=CARTESIAN_POINT ( 'NONE',  ( 33.46736520451723607, -39.49419924740560361, 34.56458480083048102 ) ) ;
#38468=CARTESIAN_POINT ( 'NONE',  ( -17.01589776168603407, -1.734723475976807094E-15, 2.227375807157432774 ) ) ;
#38481=CARTESIAN_POINT ( 'NONE',  ( 95.46109593427335938, -60.00000000000002132, 52.32479805523267657 ) ) ;
#38491=CARTESIAN_POINT ( 'NONE',  ( -89.95007437634640723, -30.00000000001658762, -2.808103800467800948 ) ) ;
#38503=CARTESIAN_POINT ( 'NONE',  ( 80.71697465536873040, -32.56001387452523943, 142.8104254745445871 ) ) ;
#38511=B_SPLINE_SURFACE_WITH_KNOTS ( 'NONE', 3, 1, ( 
 ( #77951, #5646, #48215 ),
 ( #22925, #40137, #80055 ),
 ( #64432, #14789, #73014 ),
 ( #22402, #47159, #6165 ),
 ( #55762, #55246, #104332 ),
 ( #71977, #30481, #24524 ),
 ( #80582, #23998, #7227 ),
 ( #39097, #15860, #96276 ),
 ( #57364, #79533, #88170 ),
 ( #73547, #16387, #14254 ),
 ( #105919, #97302, #23457 ),
 ( #65482, #104887, #31026 ),
 ( #90283, #6704, #98371 ),
 ( #106451, #39631, #71431 ),
 ( #63907, #96793, #64945 ),
 ( #88694, #56293, #48738 ),
 ( #47684, #105407, #32071 ),
 ( #89231, #38570, #97837 ),
 ( #89763, #81631, #7755 ),
 ( #32609, #74613, #91360 ),
 ( #83247, #68129, #90822 ),
 ( #92393, #18541, #17475 ),
 ( #34740, #25042, #16938 ),
 ( #51406, #33134, #76210 ),
 ( #9880, #42791, #59523 ),
 ( #42250, #50338, #9340 ),
 ( #693, #75141, #49816 ),
 ( #10414, #100491, #26647 ),
 ( #101025, #27179, #41729 ),
 ( #75684, #1236, #1783 ),
 ( #67611, #84317, #43329 ),
 ( #58988, #49273, #60069 ),
 ( #34206, #82721, #8825 ),
 ( #33658, #92932, #67078 ),
 ( #57898, #66537, #82177 ),
 ( #2315, #35261, #8293 ),
 ( #41199, #74085, #171 ),
 ( #66004, #50864, #98881 ),
 ( #99411, #25593, #91876 ),
 ( #99961, #58451, #18003 ),
 ( #26134, #83769, #60595 ),
 ( #70260, #93483, #20162 ),
 ( #44394, #36344, #76741 ),
 ( #20705, #102624, #69215 ),
 ( #3402, #68683, #77290 ),
 ( #28782, #101564, #35805 ),
 ( #43851, #27721, #12007 ),
 ( #77824, #53543, #86474 ),
 ( #102081, #62196, #45465 ),
 ( #28243, #21214, #12530 ),
 ( #19632, #52465, #54044 ),
 ( #94553, #84847, #78338 ),
 ( #61113, #19094, #94000 ),
 ( #95082, #4456, #37399 ),
 ( #85384, #51935, #61664 ),
 ( #2851, #10930, #11467 ),
 ( #44940, #53012, #85936 ),
 ( #3934, #36865, #69733 ),
 ( #103161, #29306, #59116 ),
 ( #33788, #33252, #58024 ),
 ( #7876, #34334, #83370 ),
 ( #8417, #73677, #67732 ),
 ( #17059, #67209, #91483 ),
 ( #106579, #24637, #66663 ),
 ( #100616, #26253, #75270 ),
 ( #83902, #59648, #57484 ),
 ( #58582, #818, #99548 ),
 ( #81754, #48861, #40783 ),
 ( #25724, #286, #50988 ),
 ( #91996, #42923, #18132 ),
 ( #90952, #65598, #90409 ),
 ( #16512, #17598, #10016 ),
 ( #75815, #66125, #9467 ),
 ( #1910, #50460, #8946 ),
 ( #49938, #42379, #74207 ),
 ( #49398, #1368, #34863 ),
 ( #100083, #26779, #15984 ),
 ( #32731, #98484, #99004 ),
 ( #82307, #41317, #25169 ),
 ( #82843, #41849, #74735 ),
 ( #36991, #61792, #68810 ),
 ( #92524, #103292, #69340 ),
 ( #19234, #93068, #27319 ),
 ( #29437, #19759, #18679 ),
 ( #68264, #51535, #84449 ),
 ( #53664, #86066, #77417 ),
 ( #10542, #94686, #20833 ),
 ( #3532, #12137, #86598 ),
 ( #43460, #36471, #2449 ),
 ( #102755, #84979, #53148 ),
 ( #76336, #77948, #76872 ),
 ( #28916, #102219, #28367 ),
 ( #27852, #35396, #101157 ),
 ( #45066, #93608, #12662 ),
 ( #60199, #101691, #44529 ),
 ( #52064, #11061, #43985 ),
 ( #2984, #61245, #94129 ),
 ( #45593, #4063, #78470 ),
 ( #35938, #60721, #52593 ),
 ( #20297, #69861, #4594 ),
 ( #85520, #11598, #37528 ),
 ( #70393, #81116, #103806 ),
 ( #63376, #54173, #47156 ),
 ( #38057, #47681, #70914 ),
 ( #105404, #38567, #21336 ),
 ( #96790, #55242, #13189 ),
 ( #62834, #80051, #64429 ),
 ( #46120, #7224, #31547 ),
 ( #48212, #63903, #40134 ),
 ( #46633, #88167, #14251 ),
 ( #31023, #73011, #79530 ),
 ( #104884, #80579, #6700 ),
 ( #71427, #105915, #97299 ),
 ( #104329, #62311, #39628 ),
 ( #23454, #87115, #96273 ),
 ( #95725, #72498, #79005 ),
 ( #56290, #22399, #95204 ),
 ( #5125, #29951, #14786 ),
 ( #89228, #15326, #6162 ),
 ( #21866, #54706, #87643 ),
 ( #13726, #5643, #30477 ),
 ( #39094, #71974, #22921 ),
 ( #55759, #88690, #16935 ),
 ( #99957, #81628, #106448 ),
 ( #40661, #8290, #7751 ),
 ( #25590, #24521, #89759 ),
 ( #16383, #33131, #83244 ),
 ( #91357, #32606, #75138 ),
 ( #42247, #9877, #32068 ),
 ( #15857, #33655, #49813 ),
 ( #50860, #82718, #57895 ),
 ( #90819, #18000, #73544 ),
 ( #74082, #42788, #66001 ),
 ( #65479, #58985, #98878 ),
 ( #8821, #49270, #98367 ),
 ( #57361, #90280, #41726 ),
 ( #48735, #91873, #82174 ),
 ( #99408, #1233, #74610 ),
 ( #167, #25038, #690 ),
 ( #66534, #41196, #58448 ),
 ( #9337, #34203, #83766 ),
 ( #17471, #50335, #67075 ),
 ( #26131, #75681, #64942 ),
 ( #97834, #23995, #56836 ),
 ( #26644, #102078, #101022 ),
 ( #84844, #60591, #69211 ),
 ( #51403, #76207, #59519 ),
 ( #52462, #93480, #86470 ),
 ( #61110, #44937, #69730 ),
 ( #43325, #19091, #44391 ),
 ( #19629, #77820, #67608 ),
 ( #27176, #43848, #12527 ),
 ( #20702, #2311, #28779 ),
 ( #100487, #85380, #92929 ),
 ( #93997, #84314, #35258 ),
 ( #3931, #92390, #61661 ),
 ( #28240, #20159, #12004 ),
 ( #101561, #76738, #2848 ),
 ( #60066, #68680, #68125 ),
 ( #3399, #53540, #51931 ),
 ( #27718, #53009, #77287 ),
 ( #11464, #85933, #36341 ),
 ( #36861, #102620, #10927 ),
 ( #94550, #35802, #45462 ),
 ( #1780, #34737, #18538 ),
 ( #10411, #88039, #4993 ),
 ( #70257, #88562, #80448 ),
 ( #4452, #21731, #78335 ),
 ( #30886, #96654, #37395 ),
 ( #64294, #79922, #63766 ),
 ( #56149, #22789, #14118 ),
 ( #14643, #70786, #38953 ),
 ( #62703, #47020, #104736 ),
 ( #55625, #103158, #71830 ),
 ( #6031, #29303, #89093 ),
 ( #63235, #37924, #78865 ),
 ( #103680, #15188, #5515 ),
 ( #54040, #86986, #62193 ),
 ( #47552, #39492, #6559 ),
 ( #96127, #95078, #72367 ),
 ( #105273, #22260, #31417 ),
 ( #21211, #97166, #23313 ),
 ( #38439, #13054, #45986 ),
 ( #54571, #29826, #95594 ),
 ( #87510, #55108, #13589 ),
 ( #46504, #79400, #71305 ),
 ( #104198, #30341, #49137 ),
 ( #57230, #56701, #24391 ),
 ( #8693, #23857, #97692 ),
 ( #105793, #89624, #98752 ),
 ( #26001, #58311, #558 ),
 ( #65873, #15724, #66949 ),
 ( #73953, #66399, #91236 ),
 ( #34077, #48608, #73411 ),
 ( #58864, #82038, #99829 ),
 ( #75008, #8162, #40010 ),
 ( #32473, #81494, #33527 ),
 ( #7613, #33006, #17343 ),
 ( #1103, #65344, #41601 ),
 ( #50218, #24906, #41069 ),
 ( #34, #31932, #91754 ),
 ( #49681, #9214, #99280 ),
 ( #48077, #80979, #7095 ),
 ( #72881, #74484, #57760 ),
 ( #83119, #25457, #42122 ),
 ( #64810, #40532, #98235 ),
 ( #90685, #16795, #106308 ),
 ( #90148, #16253, #82588 ),
 ( #2184, #52883, #68004 ),
 ( #44811, #60991, #93878 ),
 ( #67482, #26524, #76084 ),
 ( #2726, #20037, #1652 ),
 ( #35134, #85252, #11336 ),
 ( #18412, #35677, #85808 ),
 ( #34611, #36747, #11883 ),
 ( #3810, #19504, #69609 ),
 ( #100889, #43723, #69084 ),
 ( #28645, #27055, #27592 ),
 ( #59397, #101957, #9742 ),
 ( #68553, #60474, #17874 ),
 ( #101439, #93353, #51269 ),
 ( #83637, #51808, #52339 ),
 ( #3276, #42658, #28117 ),
 ( #18964, #50727, #59939 ),
 ( #102502, #77160, #36216 ),
 ( #92258, #61530, #44268 ),
 ( #75558, #100361, #77698 ),
 ( #84191, #10287, #43198 ),
 ( #92805, #84720, #10806 ),
 ( #76614, #4333, #30761 ),
 ( #5399, #4867, #29707 ),
 ( #70665, #37266, #12408 ),
 ( #86862, #45339, #39370 ),
 ( #95464, #38835, #63104 ),
 ( #94958, #63647, #78217 ),
 ( #29195, #37804, #30218 ),
 ( #38321, #96536, #53424 ),
 ( #86342, #87391, #71182 ),
 ( #22668, #103557, #55505 ),
 ( #88445, #14517, #62581 ),
 ( #103037, #45858, #47429 ),
 ( #21611, #70131, #21096 ),
 ( #13465, #62070, #96005 ),
 ( #79277, #80320, #46387 ),
 ( #6432, #72247, #104076 ),
 ( #22129, #105149, #12937 ),
 ( #54981, #71698, #87912 ),
 ( #78731, #13994, #46902 ),
 ( #104610, #53930, #79806 ),
 ( #5904, #94423, #31291 ),
 ( #20585, #54441, #64693 ),
 ( #98112, #73833, #97564 ),
 ( #56035, #74358, #66276 ),
 ( #97048, #7491, #64178 ),
 ( #968, #33407, #99164 ),
 ( #81913, #57633, #25321 ),
 ( #23189, #8029, #80859 ),
 ( #436, #56579, #24784 ),
 ( #88967, #49557, #48487 ),
 ( #6971, #58182, #40941 ),
 ( #81382, #106184, #39889 ),
 ( #72762, #15065, #90557 ),
 ( #47951, #9092, #40406 ) ),
 .UNSPECIFIED., .T., .F., .F.,
 ( 4, 1, 1, 1, 1, 1, 1, 1, 1, 1, 1, 1, 1, 1, 1, 1, 1, 1, 1, 1, 1, 1, 1, 1, 1, 1, 1, 1, 1, 1, 1, 1, 1, 1, 1, 1, 1, 1, 1, 1, 1, 1, 1, 1, 1, 1, 1, 1, 1, 1, 1, 1, 1, 1, 1, 1, 1, 1, 1, 1, 1, 1, 1, 1, 1, 1, 1, 1, 1, 1, 1, 1, 1, 1, 1, 1, 1, 1, 1, 1, 1, 1, 1, 1, 1, 1, 1, 1, 1, 1, 1, 1, 1, 1, 1, 1, 1, 1, 1, 1, 1, 1, 1, 1, 1, 1, 1, 1, 1, 1, 1, 1, 1, 1, 1, 1, 1, 1, 1, 1, 1, 1, 1, 1, 1, 1, 1, 1, 1, 1, 2, 1, 1, 1, 1, 1, 1, 1, 1, 1, 1, 1, 1, 1, 1, 1, 1, 1, 1, 1, 1, 1, 1, 1, 1, 1, 1, 1, 1, 1, 1, 1, 1, 1, 1, 1, 1, 1, 1, 1, 1, 1, 1, 1, 1, 1, 1, 1, 1, 1, 1, 1, 1, 1, 1, 1, 1, 1, 1, 1, 1, 1, 1, 1, 1, 1, 1, 1, 1, 1, 1, 1, 1, 1, 1, 1, 1, 1, 1, 1, 1, 1, 1, 1, 1, 1, 1, 1, 1, 1, 1, 1, 1, 1, 1, 1, 1, 1, 1, 1, 1, 1, 1, 1, 1, 1, 1, 1, 1, 1, 1, 1, 1, 1, 1, 1, 1, 1, 1, 1, 1, 1, 1, 1, 1, 1, 1, 1, 1, 4 ),
 ( 2, 1, 2 ),
 ( 0.000000000000000000, 0.003906146814772826562, 0.007812293629545653123, 0.01171844044431847968, 0.01562458725909130625, 0.01953073407386413107, 0.02343688088863695937, 0.02734302770340978420, 0.03124917451818261249, 0.03320224792556902144, 0.03515532133295543732, 0.03710839474034185320, 0.03906146814772826215, 0.04296761496250108697, 0.04687376177727391874, 0.05468605540681956839, 0.06249834903636522498, 0.07031064266591087464, 0.07812293629545652429, 0.08593522992500217395, 0.09374752355454783748, 0.1015598171840934594, 0.1093721108136391368, 0.1132782576284119685, 0.1171844044431848003, 0.1210905512579576043, 0.1249966980727304500, 0.1289028448875032540, 0.1328089917022760857, 0.1367151385170488620, 0.1406212853318217493, 0.1445274321465945810, 0.1484335789613673851, 0.1523397257761402168, 0.1562458725909130486, 0.1601520194056858248, 0.1640581662204587121, 0.1679643130352315439, 0.1718704598500043479, 0.1757766066647771797, 0.1796827534795499559, 0.1816358268869364412, 0.1835889002943228432, 0.1855419737017092452, 0.1874950471090956750, 0.1914011939238684790, 0.1933542673312549365, 0.1953073407386413107, 0.1992134875534140870, 0.2011665609608005445, 0.2031196343681869187, 0.2050727077755734040, 0.2060492444792665356, 0.2070257811829598060, 0.2089788545903461525, 0.2109319279977326378, 0.2128850014051190120, 0.2148380748125054418, 0.2167911482198918716, 0.2187442216272782736, 0.2206972950346647311, 0.2226503684420510498, 0.2246034418494375351, 0.2265565152568239371, 0.2285095886642103391, 0.2304626620715967689, 0.2324157354789831431, 0.2343688088863696006, 0.2363218822937560304, 0.2382749557011424046, 0.2402280291085288344, 0.2421811025159151809, 0.2441341759233016939, 0.2460872493306880127, 0.2499933961454608999, 0.2538995429602335929, 0.2578056897750065080, 0.2617118365897793675, 0.2656179834045521715, 0.2695241302193249755, 0.2734302770340977240, 0.2773364238488707501, 0.2812425706636434986, 0.2851487174784163581, 0.2890548642931891621, 0.2968671579227347701, 0.3046794515522804336, 0.3124917451818260972, 0.3203040388113716497, 0.3281163324409174242, 0.3359286260704630878, 0.3437409197000086958, 0.3476470665147816108, 0.3515532133295543593, 0.3554593601443271633, 0.3593655069590999118, 0.3632716537738728824, 0.3671778005886456864, 0.3710839474034184904, 0.3749900942181913499, 0.3788962410329640984, 0.3828023878477369579, 0.3867085346625097619, 0.3906146814772826215, 0.3945208282920554810, 0.3984269751068281740, 0.4023331219216010890, 0.4042861953289875743, 0.4062392687363738375, 0.4081923421437603228, 0.4101454155511468080, 0.4120984889585330713, 0.4140515623659196121, 0.4160046357733060973, 0.4179577091806923050, 0.4199107825880789013, 0.4218638559954652756, 0.4257700028102379686, 0.4296761496250108836, 0.4335822964397836876, 0.4374884432545565471, 0.4413945900693294067, 0.4453007368841020996, 0.4492068836988750702, 0.4531130305136478742, 0.4609253241431935377, 0.4687376177727392013, 0.4765499114022848093, 0.4843622050318303618, 0.4921744986613760253, 0.4999867922909217999, 0.5077994986613761919, 0.5156122050318305838, 0.5234249114022848648, 0.5312376177727392568, 0.5390503241431936488, 0.5468630305136479297, 0.5507693836988751812, 0.5546757368841022107, 0.5585820900693294622, 0.5624884432545566026, 0.5663947964397838541, 0.5703011496250109946, 0.5742075028102381351, 0.5781138559954652756, 0.5800670325880789013, 0.5820202091806925271, 0.5839733857733060418, 0.5859265623659195565, 0.5878797389585332933, 0.5898329155511468080, 0.5917860921437604338, 0.5937392687363740595, 0.5956924453289873522, 0.5976456219216012000, 0.6015519751068284515, 0.6054583282920554810, 0.6093646814772826215, 0.6132710346625098730, 0.6171773878477370134, 0.6210837410329641539, 0.6249900942181914054, 0.6288964474034186569, 0.6328028005886456864, 0.6367091537738729379, 0.6406155069591000784, 0.6445218601443273299, 0.6484282133295544703, 0.6523345665147814998, 0.6562409197000087513, 0.6640536260704632543, 0.6718663324409175353, 0.6796790388113718162, 0.6874917451818260972, 0.6953044515522806002, 0.7031171579227348811, 0.7109298642931891621, 0.7148362174784161915, 0.7187425706636435541, 0.7226489238488706945, 0.7265552770340979460, 0.7304616302193250865, 0.7343679834045522270, 0.7382743365897792565, 0.7421806897750065080, 0.7460870429602337595, 0.7499933961454610110, 0.7538997493306882625, 0.7558529259233015551, 0.7578061025159152919, 0.7597592791085288066, 0.7617124557011423214, 0.7636656322937560581, 0.7656188088863695729, 0.7675719854789833096, 0.7695251620715968244, 0.7714783386642103391, 0.7734315152568238538, 0.7753846918494375906, 0.7773378684420511053, 0.7792910450346646201, 0.7812442216272783568, 0.7831973982198916495, 0.7851505748125056083, 0.7871037514051189010, 0.7890569279977326378, 0.7910101045903461525, 0.7929632811829598893, 0.7949164577755734040, 0.7968696343681870298, 0.7988228109608006555, 0.8007759875534141703, 0.8046823407386413107, 0.8066355173312547144, 0.8085886939238684512, 0.8124950471090957027, 0.8144482237017094395, 0.8164014002943229542, 0.8183545768869363579, 0.8203077534795502057, 0.8242141066647772352, 0.8281204598500044867, 0.8320268130352314051, 0.8359331662204587676, 0.8398395194056857971, 0.8437458725909130486, 0.8476522257761403001, 0.8515585789613675516, 0.8554649321465945810, 0.8593712853318218325, 0.8632776385170490840, 0.8671839917022761135, 0.8710903448875033650, 0.8749966980727305055, 0.8789030512579574239, 0.8828094044431848975, 0.8867157576284119269, 0.8906221108136391784, 0.8984348171840934594, 0.9062475235545479624, 0.9140602299250022433, 0.9218729362954565243, 0.9296856426659108052, 0.9374983490363653083, 0.9453110554068195892, 0.9531237617772740922, 0.9570301149625010106, 0.9609364681477282621, 0.9628896447403418879, 0.9648428213329554026, 0.9667959979255691394, 0.9687491745181826541, 0.9726555277034099056, 0.9765618808886369351, 0.9804682340738641866, 0.9843745872590914381, 0.9882809404443185786, 0.9921872936295457190, 0.9960936468147727485, 1.000000000000000000 ),
 ( 0.000000000000000000, 1.000000000000000000, 1.526318052600188269 ),
 .UNSPECIFIED. ) ;
#38520=CARTESIAN_POINT ( 'NONE',  ( -19.84524846389541963, -17.03792638373621671, 31.48019177038823102 ) ) ;
#38534=CARTESIAN_POINT ( 'NONE',  ( 9.416339274345753907, -18.52858867495709561, -37.89033340655316806 ) ) ;
#38535=CARTESIAN_POINT ( 'NONE',  ( -83.25245042638346149, -30.00000000000000000, 154.8156864715076892 ) ) ;
#38539=CARTESIAN_POINT ( 'NONE',  ( 107.6567483471291524, -57.65797727960799079, 199.3974509801145416 ) ) ;
#38540=CARTESIAN_POINT ( 'NONE',  ( 70.85504447565058683, -60.22828372538490527, -26.05905046828224769 ) ) ;
#38544=CARTESIAN_POINT ( 'NONE',  ( -74.81545634040968196, -60.00000000000000000, 179.8313476602450862 ) ) ;
#38548=CARTESIAN_POINT ( 'NONE',  ( -85.95813120774067784, -31.98553129542242601, 183.6009373032548524 ) ) ;
#38558=CARTESIAN_POINT ( 'NONE',  ( -84.22227036138077949, -52.73149474305196094, -14.85135597291962029 ) ) ;
#38567=CARTESIAN_POINT ( 'NONE',  ( 89.36652584573501201, -30.00000000000001421, 5.436425775551051665 ) ) ;
#38568=CARTESIAN_POINT ( 'NONE',  ( -78.92481610133761194, -46.43807971556969960, 146.4481032322226497 ) ) ;
#38570=CARTESIAN_POINT ( 'NONE',  ( 51.40679407232553899, -29.99999999999998934, 68.09281640667435909 ) ) ;
#38572=CARTESIAN_POINT ( 'NONE',  ( 101.8003409713441840, -57.63152670329829874, 203.3526965820661587 ) ) ;
#38579=CARTESIAN_POINT ( 'NONE',  ( -103.9369005074886729, -45.26540285949483433, 168.0494633293456559 ) ) ;
#38591=CARTESIAN_POINT ( 'NONE',  ( 25.97097906841934289, -36.00028574033248674, 31.37664239582928261 ) ) ;
#38608=CARTESIAN_POINT ( 'NONE',  ( 89.51307813876950092, -29.99999999999982947, 189.3934310507934242 ) ) ;
#38612=CARTESIAN_POINT ( 'NONE',  ( 81.47646419641506554, -30.00000000000000355, -9.428529028395711720 ) ) ;
#38633=CARTESIAN_POINT ( 'NONE',  ( 63.22564189622978148, -36.00690027551169692, 79.28506037756856983 ) ) ;
#38649=CARTESIAN_POINT ( 'NONE',  ( 86.30952536086155646, -53.79458929396566447, 192.2603334925355512 ) ) ;
#38657=CARTESIAN_POINT ( 'NONE',  ( 21.29363090902129230, -60.00000000000000711, 40.40473236666584711 ) ) ;
#38658=CARTESIAN_POINT ( 'NONE',  ( -99.43898474115941610, -30.00000000000000355, 187.6907289620029076 ) ) ;
#38660=CARTESIAN_POINT ( 'NONE',  ( 45.08640801759163708, -57.68306945118310125, 65.34958374638743805 ) ) ;
#38671=CARTESIAN_POINT ( 'NONE',  ( -10.00000000000000000, -15.00000000000000000, 10.00000000000000178 ) ) ;
#38675=CARTESIAN_POINT ( 'NONE',  ( -13.27553105007237733, -25.54993549698307476, 28.22271134896314848 ) ) ;
#38676=CARTESIAN_POINT ( 'NONE',  ( -106.4794109352461788, -59.99999999999998579, 170.5660833250976793 ) ) ;
#38685=CARTESIAN_POINT ( 'NONE',  ( 65.83830346953287460, -59.99999999999999289, 121.7195788828446297 ) ) ;
#38690=CARTESIAN_POINT ( 'NONE',  ( 34.60434289261801410, -60.00000000000002842, 49.20687062438629056 ) ) ;
#38706=CARTESIAN_POINT ( 'NONE',  ( -106.7905710028713457, -60.00000000000244427, 200.8526573591231283 ) ) ;
#38708=CARTESIAN_POINT ( 'NONE',  ( 93.74589095632293834, -59.99999999999995737, 202.5411262228464295 ) ) ;
#38711=CARTESIAN_POINT ( 'NONE',  ( -103.2977232915219048, -14.21045842199428577, 133.3115090881459253 ) ) ;
#38712=CARTESIAN_POINT ( 'NONE',  ( 9.249740279238880092, -42.95370826011391330, 31.05136486455132072 ) ) ;
#38714=CARTESIAN_POINT ( 'NONE',  ( -46.32777947467088353, -46.44406913752303723, 47.27782089263724430 ) ) ;
#38725=CARTESIAN_POINT ( 'NONE',  ( 106.2411241248946254, -29.99999999999826628, 193.3566646931754462 ) ) ;
#38729=CARTESIAN_POINT ( 'NONE',  ( 98.72935129347025907, -30.00000000000000355, 189.4299880434703880 ) ) ;
#38732=VECTOR ( 'NONE', #36114, 1000.000000000000000 ) ;
#38740=ORIENTED_EDGE ( 'NONE', *, *, #23177, .F. ) ;
#38742=CARTESIAN_POINT ( 'NONE',  ( 94.05478402017182304, -38.49234810551472918, 201.1946758962800459 ) ) ;
#38745=CARTESIAN_POINT ( 'NONE',  ( 86.93632132420292180, -60.21781714147697784, -9.632118793199575535 ) ) ;
#38767=CARTESIAN_POINT ( 'NONE',  ( -8.532132811034937703, -15.83874480131545326, 34.63122062129517076 ) ) ;
#38770=CARTESIAN_POINT ( 'NONE',  ( 86.40302239653674121, -17.55444326215376094, 177.8619036970834486 ) ) ;
#38774=CARTESIAN_POINT ( 'NONE',  ( 96.28659315884510761, -57.67146175308503331, 43.74667604778345265 ) ) ;
#38781=CARTESIAN_POINT ( 'NONE',  ( 11.81719646716459948, -21.03406259286755642, 35.54759019141032894 ) ) ;
#38789=CARTESIAN_POINT ( 'NONE',  ( -85.24003831912723683, -38.00000000000003553, 47.20936526245474596 ) ) ;
#38791=VERTEX_POINT ( 'NONE', #61857 ) ;
#38796=CARTESIAN_POINT ( 'NONE',  ( -28.77979384944077523, -47.40897086083281664, -33.14033794634894292 ) ) ;
#38806=CARTESIAN_POINT ( 'NONE',  ( -90.49378535418108527, -60.00000000000000711, -17.94840510955679136 ) ) ;
#38811=CARTESIAN_POINT ( 'NONE',  ( 98.54373379153146573, -45.26741342605672713, 193.5399338678095376 ) ) ;
#38815=CARTESIAN_POINT ( 'NONE',  ( -82.78929023607005888, -32.55497806570344466, 157.1457539419261309 ) ) ;
#38828=CARTESIAN_POINT ( 'NONE',  ( -76.58308308725453628, -57.53248158402972479, 194.3307878365576187 ) ) ;
#38833=CARTESIAN_POINT ( 'NONE',  ( 89.53125762993630588, -30.00000000000007461, -13.19907884436577561 ) ) ;
#38835=CARTESIAN_POINT ( 'NONE',  ( -72.40149263128425616, -29.99999999999999289, 139.7559031367707405 ) ) ;
#38836=CARTESIAN_POINT ( 'NONE',  ( -55.20763222134070247, -18.68546736084697102, 52.51444300613069771 ) ) ;
#38839=VERTEX_POINT ( 'NONE', #62904 ) ;
#38840=CARTESIAN_POINT ( 'NONE',  ( -102.7301835497670908, -60.18086027025601936, 193.2518684143816472 ) ) ;
#38844=CARTESIAN_POINT ( 'NONE',  ( 90.14312592591035411, -38.39823370583771833, -15.62996679376882270 ) ) ;
#38858=CARTESIAN_POINT ( 'NONE',  ( 50.87530857847808363, -36.04660271324092946, 51.03790572413701199 ) ) ;
#38861=CARTESIAN_POINT ( 'NONE',  ( -110.5687679044198291, -38.35612487468937104, 181.7317928493044974 ) ) ;
#38863=CARTESIAN_POINT ( 'NONE',  ( 91.45439809862598679, -38.39047740764758032, -7.874681939750319160 ) ) ;
#38867=CARTESIAN_POINT ( 'NONE',  ( 94.80615415396439971, -37.84849680385329407, 106.6770409997166382 ) ) ;
#38873=CARTESIAN_POINT ( 'NONE',  ( 91.28860837299599496, -60.00000000000002132, 202.2318051499666467 ) ) ;
#38877=CARTESIAN_POINT ( 'NONE',  ( 59.01113678252345807, -39.48982602246088192, 69.66931651419592697 ) ) ;
#38883=CARTESIAN_POINT ( 'NONE',  ( -109.9283950457840433, -38.35593267714713761, 186.3516114292234818 ) ) ;
#38893=COLOUR_RGB ( '', 0.09019608, 0.27058824, 0.51372549) ;
#38897=CARTESIAN_POINT ( 'NONE',  ( 85.33552361055200208, -25.38509375986750882, 170.5403938721447616 ) ) ;
#38910=CARTESIAN_POINT ( 'NONE',  ( -81.58738582554423147, -30.00000000000000000, 29.51690375706957425 ) ) ;
#38934=CARTESIAN_POINT ( 'NONE',  ( -112.0891722639055814, -59.99999999999999289, 178.1611067759957336 ) ) ;
#38939=CARTESIAN_POINT ( 'NONE',  ( -82.07449229012887315, -53.53251292769294167, 181.8262338053436906 ) ) ;
#38947=CARTESIAN_POINT ( 'NONE',  ( -82.41975597616887228, -37.82984823159566190, 11.94393511651135142 ) ) ;
#38950=FILL_AREA_STYLE ('',( #14640 ) ) ;
#38952=CARTESIAN_POINT ( 'NONE',  ( 84.52829458723479661, -59.99999999999986500, 202.7046071135156069 ) ) ;
#38953=CARTESIAN_POINT ( 'NONE',  ( -90.94649322911389788, -14.21045842199428222, 57.96573475225447680 ) ) ;
#38954=CARTESIAN_POINT ( 'NONE',  ( -63.81269489221281788, -42.96200065895143894, 84.51879323443225189 ) ) ;
#38958=CARTESIAN_POINT ( 'NONE',  ( 70.43415898748341419, -60.00000000002942357, 160.5900936467152746 ) ) ;
#38962=CARTESIAN_POINT ( 'NONE',  ( 1.974351198080348091, -18.58616468225248397, 26.98526860823282547 ) ) ;
#38972=CARTESIAN_POINT ( 'NONE',  ( -89.85221766084636386, -60.00000000000002132, 201.9352697163374160 ) ) ;
#38983=CARTESIAN_POINT ( 'NONE',  ( -39.12603572575172706, -60.26799234672426309, 42.39855392131921974 ) ) ;
#38987=CARTESIAN_POINT ( 'NONE',  ( 36.22549068229315594, -46.43024825669357369, 37.39601728665412850 ) ) ;
#38988=CARTESIAN_POINT ( 'NONE',  ( 13.66642973270348627, -9.677049996499534265E-13, 17.78317311657527000 ) ) ;
#38991=CARTESIAN_POINT ( 'NONE',  ( -57.78802091145840336, -38.34425951725483372, 89.61089764502102639 ) ) ;
#39002=CARTESIAN_POINT ( 'NONE',  ( 100.7505531824810987, -60.00000000000000711, 85.43635729793463440 ) ) ;
#39008=CARTESIAN_POINT ( 'NONE',  ( -89.26149008746590141, -29.99999999999675993, -13.97880863715630184 ) ) ;
#39009=ORIENTED_EDGE ( 'NONE', *, *, #41419, .F. ) ;
#39014=CARTESIAN_POINT ( 'NONE',  ( 83.87732489606810304, -52.73295681655777400, -15.45569567703784131 ) ) ;
#39024=CARTESIAN_POINT ( 'NONE',  ( 81.44529849088311835, -39.49779538557150005, 155.9713579814424520 ) ) ;
#39037=DIRECTION ( 'NONE',  ( 0.000000000000000000, 0.000000000000000000, -1.000000000000000000 ) ) ;
#39043=CARTESIAN_POINT ( 'NONE',  ( -25.64088414607024546, -19.60199216900910102, 31.60029921600921554 ) ) ;
#39047=MECHANICAL_DESIGN_GEOMETRIC_PRESENTATION_REPRESENTATION('',(#104463),#59685);
#39054=ORIENTED_EDGE ( 'NONE', *, *, #95943, .F. ) ;
#39061=CARTESIAN_POINT ( 'NONE',  ( -64.74643051176546749, -30.00000000000000711, 79.49596584610381456 ) ) ;
#39065=CARTESIAN_POINT ( 'NONE',  ( 95.70874240590093507, -57.62122494225103253, 204.5320780021935150 ) ) ;
#39066=CARTESIAN_POINT ( 'NONE',  ( 62.88617926675873804, -47.40891080665988255, -26.65499022469952806 ) ) ;
#39071=CARTESIAN_POINT ( 'NONE',  ( -73.43589654061896965, -59.99999999999999289, 166.5613341509786096 ) ) ;
#39077=CARTESIAN_POINT ( 'NONE',  ( -85.31064313351537010, -46.56325337622924820, 188.2330627234076417 ) ) ;
#39081=ORIENTED_EDGE ( 'NONE', *, *, #60320, .F. ) ;
#39086=CARTESIAN_POINT ( 'NONE',  ( -83.39454600545269614, -45.25859893168446035, -13.67588221705811158 ) ) ;
#39092=CARTESIAN_POINT ( 'NONE',  ( 13.66642973271503081, -8.673617379884035472E-16, -17.78317311657917088 ) ) ;
#39094=CARTESIAN_POINT ( 'NONE',  ( 67.59883368830136874, -59.99999999999988631, -35.88524404060949990 ) ) ;
#39095=CARTESIAN_POINT ( 'NONE',  ( -77.17139058806502305, -60.31594504996868977, 150.0157547586008775 ) ) ;
#39097=CARTESIAN_POINT ( 'NONE',  ( 25.54731711030018815, -59.99999999999990763, 43.65505808401614019 ) ) ;
#39098=CARTESIAN_POINT ( 'NONE',  ( 108.5906273926863861, -57.66325265620239549, 198.2982773438044148 ) ) ;
#39108=CARTESIAN_POINT ( 'NONE',  ( -102.3071268033655059, -37.82052401323348079, 161.0073083074867952 ) ) ;
#39121=CARTESIAN_POINT ( 'NONE',  ( 26.57462979862440022, -36.00149129685673444, 31.51357150688723863 ) ) ;
#39136=CARTESIAN_POINT ( 'NONE',  ( 33.23733598311309123, -59.99999999999999289, -40.52796009714472802 ) ) ;
#39161=CARTESIAN_POINT ( 'NONE',  ( 64.47128789977597307, -32.52970818110316031, 81.05340315809206686 ) ) ;
#39175=CARTESIAN_POINT ( 'NONE',  ( 86.66893764443852888, -46.47199666242754290, 190.4867299908505061 ) ) ;
#39184=CARTESIAN_POINT ( 'NONE',  ( 19.62218219363544236, -60.00000000000000000, 40.16747987769195305 ) ) ;
#39186=CARTESIAN_POINT ( 'NONE',  ( -99.66052428874382940, -30.00000000000000355, 186.9484570685918357 ) ) ;
#39188=DIRECTION ( 'NONE',  ( 0.000000000000000000, -1.000000000000000000, 0.000000000000000000 ) ) ;
#39190=CARTESIAN_POINT ( 'NONE',  ( 52.17905232536506333, -57.67658488488999069, 83.19886591059480452 ) ) ;
#39197=CARTESIAN_POINT ( 'NONE',  ( -20.56724024172385512, -59.99999999999999289, 40.29721615606709406 ) ) ;
#39202=CARTESIAN_POINT ( 'NONE',  ( -86.62987691488393693, -16.99726452457568726, 185.2254060544966023 ) ) ;
#39206=CARTESIAN_POINT ( 'NONE',  ( -13.32466295366451448, -29.03150478239603416, 28.80490044896601276 ) ) ;
#39208=CARTESIAN_POINT ( 'NONE',  ( -104.2214876769391054, -60.00000000000002132, 190.2337882128940407 ) ) ;
#39218=CARTESIAN_POINT ( 'NONE',  ( 73.07493821064443296, -59.99999999999999289, 163.1432788538008367 ) ) ;
#39224=CARTESIAN_POINT ( 'NONE',  ( 32.49824730387988581, -59.99999999999999289, 47.28149596916139075 ) ) ;
#39239=CARTESIAN_POINT ( 'NONE',  ( -113.9444010383659105, -60.00000000002935252, 184.0739081374410659 ) ) ;
#39241=CARTESIAN_POINT ( 'NONE',  ( 82.53305096376368510, -59.99999999999992895, 198.4978234872852738 ) ) ;
#39244=CARTESIAN_POINT ( 'NONE',  ( -106.6793529335496515, -14.21045842199435860, 163.7930604915816559 ) ) ;
#39245=CARTESIAN_POINT ( 'NONE',  ( 11.20590345621723039, -29.02957503740841361, 28.75286772522219536 ) ) ;
#39247=CARTESIAN_POINT ( 'NONE',  ( 82.46348125551625685, -37.99999999999998579, 10.05151166824885500 ) ) ;
#39249=CARTESIAN_POINT ( 'NONE',  ( -47.77545754411675460, -22.22741228947390013, 42.11508245023937747 ) ) ;
#39261=CARTESIAN_POINT ( 'NONE',  ( 101.2363978237404751, -29.99999999999453948, 198.5817383530316818 ) ) ;
#39265=CARTESIAN_POINT ( 'NONE',  ( 93.01436231026998769, -30.00000000000000000, 106.1217855030838280 ) ) ;
#39279=CARTESIAN_POINT ( 'NONE',  ( 79.84666553715925374, -38.77034851676472726, 192.7062979745145981 ) ) ;
#39281=CARTESIAN_POINT ( 'NONE',  ( 85.46358041537231998, -52.72117977435281944, -0.4810073681625586794 ) ) ;
#39282=CARTESIAN_POINT ( 'NONE',  ( 76.42237582680409957, -38.00000000000002132, 125.4842420748356346 ) ) ;
#39284=DIRECTION ( 'NONE',  ( 0.000000000000000000, 0.000000000000000000, 1.000000000000000000 ) ) ;
#39300=CARTESIAN_POINT ( 'NONE',  ( -3.883979799181499715, -15.02869017758564141, 34.49744884119316879 ) ) ;
#39305=CARTESIAN_POINT ( 'NONE',  ( 84.57259215197804281, -46.56816764461522951, 186.4401838890023555 ) ) ;
#39309=CARTESIAN_POINT ( 'NONE',  ( 96.55249329909841549, -57.67139621948945205, 45.80016927409987204 ) ) ;
#39322=EDGE_CURVE ( 'NONE', #71278, #94858, #13443, .T. ) ;
#39333=CARTESIAN_POINT ( 'NONE',  ( -14.50943445205030002, -17.10998225175372411, -34.39758505370421204 ) ) ;
#39335=CARTESIAN_POINT ( 'NONE',  ( -57.70311871300574325, -34.58944410828412686, -25.91705731457850703 ) ) ;
#39345=CARTESIAN_POINT ( 'NONE',  ( -92.73296030468360129, -59.99999999999999289, -5.965765328958698710 ) ) ;
#39349=CARTESIAN_POINT ( 'NONE',  ( 100.2677560643444394, -52.76192752009863085, 194.0135600122352741 ) ) ;
#39353=CARTESIAN_POINT ( 'NONE',  ( -82.94221917796012633, -36.01794431359551396, 163.7362876441995923 ) ) ;
#39363=CARTESIAN_POINT ( 'NONE',  ( -114.1029252960232725, -57.67113437255621022, 166.8310794691209367 ) ) ;
#39368=CARTESIAN_POINT ( 'NONE',  ( 48.21450566731007825, -29.99999999999995381, -35.59756164575514958 ) ) ;
#39370=CARTESIAN_POINT ( 'NONE',  ( -74.83603090277703984, -14.21045842199441012, 137.5224045200043577 ) ) ;
#39371=CARTESIAN_POINT ( 'NONE',  ( -53.53337026754450534, -36.03630593442233021, 55.90610740931312961 ) ) ;
#39375=CARTESIAN_POINT ( 'NONE',  ( -100.3932303477031809, -45.25917866372384424, 192.1829530928476117 ) ) ;
#39380=CARTESIAN_POINT ( 'NONE',  ( 95.15023610446269231, -38.35584284022535684, 58.97509959524118273 ) ) ;
#39381=LINE ( 'NONE', #15078, #57081 ) ;
#39386=CARTESIAN_POINT ( 'NONE',  ( 80.76653117601198062, -30.00000000000000000, 138.6873283208337568 ) ) ;
#39394=CARTESIAN_POINT ( 'NONE',  ( 49.82584992942429380, -56.82805176776372491, 56.28939656403482417 ) ) ;
#39397=CARTESIAN_POINT ( 'NONE',  ( -108.9893057958549605, -38.35643123286386924, 190.1635235720441131 ) ) ;
#39399=CARTESIAN_POINT ( 'NONE',  ( 90.74781813830772137, -38.34261101312728215, 6.475050893663723883 ) ) ;
#39403=CARTESIAN_POINT ( 'NONE',  ( 98.00862599427638600, -52.71700389358836247, 110.7962579094794933 ) ) ;
#39409=CARTESIAN_POINT ( 'NONE',  ( 91.11537606070176309, -60.00000000000000711, 202.2000497971606592 ) ) ;
#39413=CARTESIAN_POINT ( 'NONE',  ( 57.46915197135655262, -53.38142663087884188, 72.11230974744191258 ) ) ;
#39419=CARTESIAN_POINT ( 'NONE',  ( -110.7961550858539255, -38.35618406817627601, 179.4776150961166081 ) ) ;
#39432=CARTESIAN_POINT ( 'NONE',  ( 81.43749204890434612, -57.00584086149340379, 181.8846221577169047 ) ) ;
#39436=ORIENTED_EDGE ( 'NONE', *, *, #74483, .T. ) ;
#39470=CARTESIAN_POINT ( 'NONE',  ( -111.3399326272597989, -60.00000000000000711, 155.6059937888795730 ) ) ;
#39476=CARTESIAN_POINT ( 'NONE',  ( -81.82008106255986490, -57.07570580673551319, 184.1260291814842844 ) ) ;
#39484=CARTESIAN_POINT ( 'NONE',  ( -85.58732770572241577, -52.70779370753110982, 27.65126831969156029 ) ) ;
#39490=CARTESIAN_POINT ( 'NONE',  ( 80.26999927900735088, -59.99999999999982947, 200.1019127161866606 ) ) ;
#39492=CARTESIAN_POINT ( 'NONE',  ( -102.4477130004285499, -30.00000000000004974, 111.1018478433771151 ) ) ;
#39493=CARTESIAN_POINT ( 'NONE',  ( -61.58610401018594160, -56.86967154772055721, 85.14694393301525110 ) ) ;
#39496=CARTESIAN_POINT ( 'NONE',  ( 97.19628318239716691, -59.99999999999878497, 204.8875827899316846 ) ) ;
#39499=CARTESIAN_POINT ( 'NONE',  ( 2.014047737277413042, -39.47254121402686877, 30.46601114062715610 ) ) ;
#39507=CARTESIAN_POINT ( 'NONE',  ( -89.17390004647626256, -59.99999999999994316, 201.7553460497344417 ) ) ;
#39518=CARTESIAN_POINT ( 'NONE',  ( -31.88243720866665143, -32.55223407456951179, 32.57539379951157343 ) ) ;
#39522=CARTESIAN_POINT ( 'NONE',  ( 42.47999858120645200, -49.88713018564629920, 43.43313861898666772 ) ) ;
#39523=CARTESIAN_POINT ( 'NONE',  ( 14.86825985028009001, 0.000000000000000000, 8.569529079650957115 ) ) ;
#39527=CARTESIAN_POINT ( 'NONE',  ( -73.92819207610308752, -38.32663662495320978, 159.7473140453433302 ) ) ;
#39538=CARTESIAN_POINT ( 'NONE',  ( 98.00938096300853886, -59.99999999999998579, 68.98427090110736515 ) ) ;
#39544=CARTESIAN_POINT ( 'NONE',  ( -53.08935917470196131, -30.00000000000000711, 52.21147893555082220 ) ) ;
#39560=ORIENTED_EDGE ( 'NONE', *, *, #12261, .F. ) ;
#39561=CARTESIAN_POINT ( 'NONE',  ( 82.92136997883486060, -18.68766406158728088, 141.1224335365927232 ) ) ;
#39580=CARTESIAN_POINT ( 'NONE',  ( -11.78651013471115050, -14.22498507149665414, 31.80223059555903475 ) ) ;
#39593=CARTESIAN_POINT ( 'NONE',  ( -1.313803945217351110, -21.30231999290575118, -38.55323443611015932 ) ) ;
#39600=CARTESIAN_POINT ( 'NONE',  ( 87.75520861027411001, -57.59389832414498755, 203.3620971134121760 ) ) ;
#39605=CARTESIAN_POINT ( 'NONE',  ( -74.34427579237575401, -59.99999999999999289, 175.6371688333348970 ) ) ;
#39608=CARTESIAN_POINT ( 'NONE',  ( -83.77086022884309102, -57.39681495382750853, 190.2519600005473421 ) ) ;
#39615=CARTESIAN_POINT ( 'NONE',  ( -82.12931037298532999, -37.78909381349949115, -13.51468982751548964 ) ) ;
#39628=CARTESIAN_POINT ( 'NONE',  ( 85.44123078815633221, -14.21045842199435505, -16.45204874176463150 ) ) ;
#39629=CARTESIAN_POINT ( 'NONE',  ( -77.86666928232057217, -18.66659128473655471, 117.1585483000689010 ) ) ;
#39631=CARTESIAN_POINT ( 'NONE',  ( 39.49823726628140719, -30.00000000000007461, 47.07845324830893929 ) ) ;
#39633=CARTESIAN_POINT ( 'NONE',  ( 74.89313546090642149, -57.57953941245633445, 190.3487796247399615 ) ) ;
#39639=CARTESIAN_POINT ( 'NONE',  ( -71.17284327374473207, -38.00000000000000711, -21.88481141223168436 ) ) ;
#39642=CARTESIAN_POINT ( 'NONE',  ( -102.1546786399030680, -45.26555502571823553, 146.8815317979925226 ) ) ;
#39652=CARTESIAN_POINT ( 'NONE',  ( -4.155049527179308200, -30.00000000000002842, 36.99135516471767460 ) ) ;
#39653=CARTESIAN_POINT ( 'NONE',  ( 32.69658716609513505, -60.31220508583461992, 38.00824357461662828 ) ) ;
#39688=CARTESIAN_POINT ( 'NONE',  ( -79.51359773737226533, -59.99999999999994316, 169.4842920155362265 ) ) ;
#39689=CARTESIAN_POINT ( 'NONE',  ( 66.38356152105049546, -53.38427602353998225, 97.96190166083606243 ) ) ;
#39703=CARTESIAN_POINT ( 'NONE',  ( 86.82806741021897778, -24.34697663169452397, 185.7438550995267406 ) ) ;
#39712=CARTESIAN_POINT ( 'NONE',  ( 28.81571653886122419, -59.99999999999999289, 42.47396466590021191 ) ) ;
#39713=CARTESIAN_POINT ( 'NONE',  ( -98.73540789171605070, -29.99999999999999645, 189.4149580153970760 ) ) ;
#39715=CARTESIAN_POINT ( 'NONE',  ( 49.43476175332632039, -57.67888354579591947, 75.71380488283527654 ) ) ;
#39723=CARTESIAN_POINT ( 'NONE',  ( -7.930648640465597587, -60.00000000000000711, 39.63302098071156365 ) ) ;
#39725=CARTESIAN_POINT ( 'NONE',  ( -86.66245912624070513, -20.68510438609584767, 184.7494804068583392 ) ) ;
#39729=CARTESIAN_POINT ( 'NONE',  ( -12.66716468281169483, -60.36572609861780592, 34.01381952931010488 ) ) ;
#39740=CARTESIAN_POINT ( 'NONE',  ( 62.15290319597050939, -60.00000000000000711, 107.8068670736100785 ) ) ;
#39745=CARTESIAN_POINT ( 'NONE',  ( 41.69321614992608716, -29.99999999999995737, 49.76314934024226488 ) ) ;
#39754=DIRECTION ( 'NONE',  ( -0.000000000000000000, -1.000000000000000000, -0.000000000000000000 ) ) ;
#39764=CARTESIAN_POINT ( 'NONE',  ( -113.1713605750742602, -60.00000000000491696, 188.4473907172926204 ) ) ;
#39767=CARTESIAN_POINT ( 'NONE',  ( 58.19072685764542996, -60.00000000000000000, 94.67969609638358008 ) ) ;
#39771=CARTESIAN_POINT ( 'NONE',  ( -110.6385074381434066, -60.00000000000007816, 195.8055798097608147 ) ) ;
#39772=CARTESIAN_POINT ( 'NONE',  ( 10.23004908500708687, -35.99163919401772205, 29.89939049008435390 ) ) ;
#39773=CARTESIAN_POINT ( 'NONE',  ( 83.10241079684797683, -38.00000000000000711, -1.999425119195920919 ) ) ;
#39775=CARTESIAN_POINT ( 'NONE',  ( -46.18499865988201947, -22.24145118935602383, 40.24121074957823652 ) ) ;
#39788=CARTESIAN_POINT ( 'NONE',  ( 106.0132497538753142, -30.00000000000378719, 193.7988435085632091 ) ) ;
#39791=CARTESIAN_POINT ( 'NONE',  ( 94.31600719128907429, -30.00000000000000000, 113.8625557724812722 ) ) ;
#39805=CARTESIAN_POINT ( 'NONE',  ( 85.15204736842385103, -38.69186732370133086, 198.5736475422584704 ) ) ;
#39807=CARTESIAN_POINT ( 'NONE',  ( 85.37734265273529388, -52.71760933736054966, 0.7316266844141512404 ) ) ;
#39808=CARTESIAN_POINT ( 'NONE',  ( 79.77431866835297569, -37.99999999999995026, 142.7581769456982954 ) ) ;
#39825=CARTESIAN_POINT ( 'NONE',  ( 28.03182135562585486, -31.11828738288172502, 39.52190999426944273 ) ) ;
#39827=VERTEX_POINT ( 'NONE', #77111 ) ;
#39828=CARTESIAN_POINT ( 'NONE',  ( 83.92266184464492085, -57.40603453690408031, 190.5289941760056251 ) ) ;
#39832=CARTESIAN_POINT ( 'NONE',  ( 93.83812592755332105, -57.67477530323803592, 11.02985781185799397 ) ) ;
#39840=CARTESIAN_POINT ( 'NONE',  ( -64.25898179071923266, -38.00000000000000711, 83.23079767160567144 ) ) ;
#39852=CARTESIAN_POINT ( 'NONE',  ( 68.05201484286467917, -29.92325765820791261, -21.69912042315977985 ) ) ;
#39858=CARTESIAN_POINT ( 'NONE',  ( -59.86887900601052337, -21.77002156294910051, -23.08918318703028660 ) ) ;
#39864=CARTESIAN_POINT ( 'NONE',  ( -92.38893592253350562, -60.00000000000000711, 0.3012529127975949739 ) ) ;
#39866=CARTESIAN_POINT ( 'NONE',  ( 64.13695837427279400, -37.76356166761983246, -24.56640574812671574 ) ) ;
#39871=CARTESIAN_POINT ( 'NONE',  ( -82.07322838537869814, -42.97417978104021330, 166.6889830305388784 ) ) ;
#39882=CARTESIAN_POINT ( 'NONE',  ( -112.2456557016906942, -57.67113047748567567, 190.5314477545807392 ) ) ;
#39888=CARTESIAN_POINT ( 'NONE',  ( -55.21321105934377726, -60.00000000000002842, -39.23988760269474341 ) ) ;
#39889=CARTESIAN_POINT ( 'NONE',  ( -4.090533018665307274, -14.21045842199441722, 34.36071901318091903 ) ) ;
#39890=CARTESIAN_POINT ( 'NONE',  ( -53.74619955778950242, -42.97187427616553634, 59.00820073232069518 ) ) ;
#39893=CARTESIAN_POINT ( 'NONE',  ( -98.97495582109610268, -52.78644234849187455, 194.7710799945916165 ) ) ;
#39898=CARTESIAN_POINT ( 'NONE',  ( 91.38085702308197256, -38.39709809381331240, -9.519024297102184562 ) ) ;
#39904=CARTESIAN_POINT ( 'NONE',  ( 80.21334409234347618, -30.00000000000000000, 135.6879503079539688 ) ) ;
#39912=CARTESIAN_POINT ( 'NONE',  ( 48.85299720893686981, -25.67496275475526346, 44.56502496020352311 ) ) ;
#39918=CARTESIAN_POINT ( 'NONE',  ( -110.1014534723386191, -38.35607734749763864, 185.3304993136136432 ) ) ;
#39921=CARTESIAN_POINT ( 'NONE',  ( 110.1708031426684187, -38.35604441332869641, 156.5327596993846839 ) ) ;
#39925=CARTESIAN_POINT ( 'NONE',  ( 104.9571888707694427, -60.15142560926327064, 149.1774971079043723 ) ) ;
#39929=CARTESIAN_POINT ( 'NONE',  ( 80.08440833438228879, -60.00000000000001421, 196.0901278236156600 ) ) ;
#39932=CARTESIAN_POINT ( 'NONE',  ( 57.65574661060767880, -49.90878574621957142, 71.01292799359110575 ) ) ;
#39939=CARTESIAN_POINT ( 'NONE',  ( -90.72701990683636097, -38.34112183637917326, 6.693821972579170776 ) ) ;
#39949=CARTESIAN_POINT ( 'NONE',  ( 81.25017303853442741, -60.55690295631904263, 184.6554220054742075 ) ) ;
#39950=ADVANCED_FACE ( 'NONE', ( #25831 ), #68373, .T. ) ;
#39988=CARTESIAN_POINT ( 'NONE',  ( -109.0276826879899943, -60.00000000000000711, 136.1730525503504907 ) ) ;
#39995=CARTESIAN_POINT ( 'NONE',  ( -84.93114117115241868, -28.90604097065245881, 171.9502745002261292 ) ) ;
#40009=CARTESIAN_POINT ( 'NONE',  ( 114.2222497212829495, -60.00000000000000000, 162.1251737369585726 ) ) ;
#40010=CARTESIAN_POINT ( 'NONE',  ( -106.9310521912263710, -14.21045842199434794, 169.9232300575910131 ) ) ;
#40011=CARTESIAN_POINT ( 'NONE',  ( -61.75299678764660882, -42.96448552206198457, 78.62763974756443019 ) ) ;
#40014=CARTESIAN_POINT ( 'NONE',  ( 104.9308453125034646, -60.00000000000243006, 202.2520219887860549 ) ) ;
#40025=CARTESIAN_POINT ( 'NONE',  ( -84.00882247759808763, -60.00000000000006395, 199.5195877717709152 ) ) ;
#40033=CARTESIAN_POINT ( 'NONE',  ( 102.6429790572119458, -59.99999999999993605, 193.3319502104955916 ) ) ;
#40034=CARTESIAN_POINT ( 'NONE',  ( -32.74448902475613465, -42.96476387111531636, 34.86933629716781269 ) ) ;
#40037=CARTESIAN_POINT ( 'NONE',  ( 37.36725091415993205, -25.66895752586749069, 33.86584213023738243 ) ) ;
#40038=CARTESIAN_POINT ( 'NONE',  ( -4.453875240773214728, -1.734723475976807094E-15, -16.57301948837565675 ) ) ;
#40041=CARTESIAN_POINT ( 'NONE',  ( -66.95983133501314910, -38.33558760111643693, 121.1209903420379703 ) ) ;
#40051=CARTESIAN_POINT ( 'NONE',  ( 93.30919872547751481, -59.99999999999999289, 35.28464305277864810 ) ) ;
#40057=CARTESIAN_POINT ( 'NONE',  ( -61.17075129193928973, -30.00000000000000711, 69.80672871272592772 ) ) ;
#40071=CARTESIAN_POINT ( 'NONE',  ( 83.25407933603389665, -18.68591088087092089, 143.1428255547100150 ) ) ;
#40080=CARTESIAN_POINT ( 'NONE',  ( -50.71028374685950268, -57.67771315371629726, 79.11066721451838646 ) ) ;
#40086=STYLED_ITEM ( 'NONE', ( #3859 ), #94617 ) ;
#40093=CARTESIAN_POINT ( 'NONE',  ( -20.83805790964204263, -17.45317829300839207, 31.47035416265072527 ) ) ;
#40106=CARTESIAN_POINT ( 'NONE',  ( -52.71312636462211287, -36.17903179718669548, -35.74065954623077346 ) ) ;
#40110=CARTESIAN_POINT ( 'NONE',  ( 86.90535743190535811, -57.58543819784419782, 203.0634495632118899 ) ) ;
#40114=CARTESIAN_POINT ( 'NONE',  ( -74.33902240994966348, -59.99999999999999289, 175.5866348027616937 ) ) ;
#40119=CARTESIAN_POINT ( 'NONE',  ( -85.57874514396658583, -35.68260388560343443, 183.8368203787026118 ) ) ;
#40123=EDGE_LOOP ( 'NONE', ( #71090, #35827, #25344, #95711, #98803 ) ) ;
#40125=ADVANCED_FACE ( 'NONE', ( #54270 ), #13290, .F. ) ;
#40126=CARTESIAN_POINT ( 'NONE',  ( -83.48784346132804046, -52.72151958306880459, -16.05522805912662676 ) ) ;
#40132=CARTESIAN_POINT ( 'NONE',  ( -17.01589776168603407, -1.734723475976807094E-15, -2.227375807157456755 ) ) ;
#40134=CARTESIAN_POINT ( 'NONE',  ( 87.76937946118395928, -14.21045842199442433, -6.551255600857777139 ) ) ;
#40135=CARTESIAN_POINT ( 'NONE',  ( -74.57516802433143255, -56.85267850989483662, 131.8985892516079446 ) ) ;
#40137=CARTESIAN_POINT ( 'NONE',  ( 1.384974311275041225, -30.00000000000000000, 37.00000000000000711 ) ) ;
#40139=CARTESIAN_POINT ( 'NONE',  ( 113.5159275335152671, -57.67115463665075481, 157.6643028401185518 ) ) ;
#40158=CARTESIAN_POINT ( 'NONE',  ( 28.84991513505058691, -32.53357776115905864, 31.52034378082766608 ) ) ;
#40172=CARTESIAN_POINT ( 'NONE',  ( 64.85336408992664303, -60.00000000000001421, -34.25061881763944172 ) ) ;
#40173=CARTESIAN_POINT ( 'NONE',  ( 74.34313532025329607, -30.00000000000000000, 109.1728309539285817 ) ) ;
#40194=CARTESIAN_POINT ( 'NONE',  ( -4.174453427199569688, -59.99999999999997868, 33.87834425268652438 ) ) ;
#40195=CARTESIAN_POINT ( 'NONE',  ( 64.58841386258137618, -36.00601803332205719, 83.18175225845169507 ) ) ;
#40201=CARTESIAN_POINT ( 'NONE',  ( -36.37294538904226471, -57.67119865010090507, -42.13310955380372747 ) ) ;
#40223=CARTESIAN_POINT ( 'NONE',  ( 2.841782347625613436, -59.99999999999999289, 39.63376178591555998 ) ) ;
#40225=CARTESIAN_POINT ( 'NONE',  ( -92.63040736140382592, -29.99999999999999645, 191.0343855628001393 ) ) ;
#40229=CARTESIAN_POINT ( 'NONE',  ( 51.98618296257861715, -57.67674160844479303, 82.65666769069098052 ) ) ;
#40232=CARTESIAN_POINT ( 'NONE',  ( 3.308827153974509994, -21.42733763530625168, -38.54996605793198938 ) ) ;
#40234=CARTESIAN_POINT ( 'NONE',  ( -12.68889540457527154, -60.00000000000001421, 39.70531046957451338 ) ) ;
#40238=CARTESIAN_POINT ( 'NONE',  ( -86.31431195955053681, -57.42698322520472232, 193.3924140938322864 ) ) ;
#40242=CARTESIAN_POINT ( 'NONE',  ( -6.015098659326455710, -25.54938308050677520, 28.13832966994452534 ) ) ;
#40256=CARTESIAN_POINT ( 'NONE',  ( 69.49330227205123833, -59.99999999999997868, 138.6641764573228102 ) ) ;
#40262=CARTESIAN_POINT ( 'NONE',  ( 20.43634719630433594, -14.21045842199429998, 34.90381869870211062 ) ) ;
#40277=CARTESIAN_POINT ( 'NONE',  ( -23.40723339434643435, -60.00000000000986233, 43.19923654131418544 ) ) ;
#40279=CARTESIAN_POINT ( 'NONE',  ( 42.28582005287888279, -60.00000000000002132, 55.60554140212523322 ) ) ;
#40281=CARTESIAN_POINT ( 'NONE',  ( -114.3490076612200568, -60.00000000000000000, 164.2604626692111367 ) ) ;
#40282=CARTESIAN_POINT ( 'NONE',  ( 17.15269105894165236, -60.35792664080034342, 34.22063819385883221 ) ) ;
#40285=DIRECTION ( 'NONE',  ( 0.000000000000000000, -0.000000000000000000, 1.000000000000000000 ) ) ;
#40286=EDGE_CURVE ( 'NONE', #30532, #59127, #4424, .T. ) ;
#40287=CARTESIAN_POINT ( 'NONE',  ( -44.33452073850874342, -60.25607191441693544, 48.29083679502918613 ) ) ;
#40300=CARTESIAN_POINT ( 'NONE',  ( 97.56484421644714189, -30.00000000002681944, 199.7415702076955597 ) ) ;
#40304=CARTESIAN_POINT ( 'NONE',  ( 97.90508973058878439, -30.00000000000000711, 136.8651816328178086 ) ) ;
#40319=CARTESIAN_POINT ( 'NONE',  ( 85.17744768472425676, -38.69024637654926835, 198.5893117286057361 ) ) ;
#40321=CARTESIAN_POINT ( 'NONE',  ( 82.21598800793653083, -38.00000000000003553, 160.2028133164328381 ) ) ;
#40336=FILL_AREA_STYLE ('',( #57559 ) ) ;
#40338=CARTESIAN_POINT ( 'NONE',  ( -20.04862318086297890, -25.72039272919216657, 36.80507196085346067 ) ) ;
#40343=CARTESIAN_POINT ( 'NONE',  ( 86.39964040925956112, -17.50171996465882174, 178.3850458645602828 ) ) ;
#40347=CARTESIAN_POINT ( 'NONE',  ( 88.75764767935135069, -57.66845035223018101, -23.73888392983841555 ) ) ;
#40363=CARTESIAN_POINT ( 'NONE',  ( -100.6662216249829243, -38.00000000000002132, 189.2678359082001123 ) ) ;
#40371=CARTESIAN_POINT ( 'NONE',  ( -44.60760376941820482, -47.40887594010209938, -30.95105337255921185 ) ) ;
#40380=CARTESIAN_POINT ( 'NONE',  ( -79.45792651602657486, -60.00000000000000711, -28.32091169615220494 ) ) ;
#40384=CARTESIAN_POINT ( 'NONE',  ( 95.67817354102299987, -37.71398327266919637, 193.0022183632935082 ) ) ;
#40387=CARTESIAN_POINT ( 'NONE',  ( -82.60449197779891506, -36.02481693259124995, 160.6711189363873302 ) ) ;
#40400=CARTESIAN_POINT ( 'NONE',  ( -97.80441453946778552, -57.62343821539597855, 204.4198989768915453 ) ) ;
#40405=CARTESIAN_POINT ( 'NONE',  ( 55.21462903151665813, -59.99999999999998579, -39.23961370773703550 ) ) ;
#40406=CARTESIAN_POINT ( 'NONE',  ( -1.309564884278361513E-05, -14.21045842199434972, 34.36840973699906243 ) ) ;
#40407=CARTESIAN_POINT ( 'NONE',  ( -54.43306722364180672, -25.62724657511986237, 53.68909144041590054 ) ) ;
#40411=CARTESIAN_POINT ( 'NONE',  ( -99.66131679920104602, -45.25319430717961211, 192.8901977128174963 ) ) ;
#40418=CARTESIAN_POINT ( 'NONE',  ( 90.50996382122711736, -38.40237687013089385, -14.56173365871752168 ) ) ;
#40424=CARTESIAN_POINT ( 'NONE',  ( 78.31067388355049275, -30.00000000000000000, 126.2693683704580394 ) ) ;
#40432=CARTESIAN_POINT ( 'NONE',  ( 49.14122930290414359, -49.90062465560988159, 52.73429724734012325 ) ) ;
#40436=CARTESIAN_POINT ( 'NONE',  ( -90.91152594127831321, -38.34737926575705558, 3.482876280662382307 ) ) ;
#40439=CARTESIAN_POINT ( 'NONE',  ( 102.8148430110912699, -38.35590780206664618, 104.8312485263550116 ) ) ;
#40442=CARTESIAN_POINT ( 'NONE',  ( 102.4777983945700299, -52.71700600495957190, 139.6461353976963835 ) ) ;
#40447=CARTESIAN_POINT ( 'NONE',  ( 77.79618479429522893, -60.00000000000002132, 192.4023258609882703 ) ) ;
#40452=CARTESIAN_POINT ( 'NONE',  ( 55.88705846244756259, -25.61800759129437566, 56.56929643049215173 ) ) ;
#40458=CARTESIAN_POINT ( 'NONE',  ( -73.94868650964912149, -29.99999999967765874, 149.0933909881836996 ) ) ;
#40467=CARTESIAN_POINT ( 'NONE',  ( 85.58024585952806262, -21.93954400496754076, 167.0656778985148208 ) ) ;
#40485=CARTESIAN_POINT ( 'NONE',  ( -25.75788261965884018, -29.55814103031516638, 38.55856135386892447 ) ) ;
#40509=CARTESIAN_POINT ( 'NONE',  ( -110.1309406653868734, -59.99999999999999289, 144.5015686475491066 ) ) ;
#40517=CARTESIAN_POINT ( 'NONE',  ( -84.23375024055349058, -35.93203514404092402, 175.7405516498321560 ) ) ;
#40531=CARTESIAN_POINT ( 'NONE',  ( 106.4003153237399459, -14.21045842199437281, 159.7124754531589019 ) ) ;
#40532=CARTESIAN_POINT ( 'NONE',  ( -107.3650189024811681, -30.00000000000002842, 190.7478110277085648 ) ) ;
#40533=CARTESIAN_POINT ( 'NONE',  ( -63.44189309749444305, -32.53320303695706173, 78.14391273869415500 ) ) ;
#40536=CARTESIAN_POINT ( 'NONE',  ( 96.28976944069333399, -59.99999999998052402, 40.92003399396909202 ) ) ;
#40541=ORIENTED_EDGE ( 'NONE', *, *, #52675, .T. ) ;
#40547=CARTESIAN_POINT ( 'NONE',  ( -109.2164123534708580, -60.00000000000000000, 193.3227612444920851 ) ) ;
#40555=EDGE_CURVE ( 'NONE', #89315, #67219, #76578, .T. ) ;
#40558=CARTESIAN_POINT ( 'NONE',  ( 105.7220129672738693, -60.00000000000001421, 184.2428138410215581 ) ) ;
#40559=CARTESIAN_POINT ( 'NONE',  ( -32.48662781215343642, -49.90568005501813786, 36.01986044320511837 ) ) ;
#40561=CARTESIAN_POINT ( 'NONE',  ( 41.95256787860516567, -60.24835236458953602, 45.28280848969064465 ) ) ;
#40566=CARTESIAN_POINT ( 'NONE',  ( -82.29585130749137534, -38.83734455563418919, 196.2398665998169918 ) ) ;
#40579=CARTESIAN_POINT ( 'NONE',  ( 92.01709497311385633, -60.00000000000000711, 18.79751796720415769 ) ) ;
#40584=CARTESIAN_POINT ( 'NONE',  ( -89.76477315035992888, -29.99999999999963407, 189.6654235243697144 ) ) ;
#40597=CARTESIAN_POINT ( 'NONE',  ( 82.78508296686045753, -25.62180102098898260, 148.0795101033245942 ) ) ;
#40606=CARTESIAN_POINT ( 'NONE',  ( -19.49904798085934843, -57.67182591607114261, 42.12704350231687300 ) ) ;
#40616=CARTESIAN_POINT ( 'NONE',  ( 24.60495542872522989, -28.77046205659021183, 38.13801889905689535 ) ) ;
#40625=CARTESIAN_POINT ( 'NONE',  ( 3.718545543012941490, -21.49349533113791821, -38.54945152629040450 ) ) ;
#40632=CARTESIAN_POINT ( 'NONE',  ( 114.2143086744109866, -57.67130378733651241, 175.1586867808284467 ) ) ;
#40638=CARTESIAN_POINT ( 'NONE',  ( -74.81582692897852382, -59.99999999999998579, 179.8343382549642229 ) ) ;
#40645=CARTESIAN_POINT ( 'NONE',  ( -85.12695384070762827, -39.34156027617945739, 184.1518049699909625 ) ) ;
#40653=CARTESIAN_POINT ( 'NONE',  ( -85.67493770007969545, -52.74798379930503245, -9.150851446102391762 ) ) ;
#40659=CARTESIAN_POINT ( 'NONE',  ( -16.57301948837645256, -1.734723475976807094E-15, 4.453875240771298039 ) ) ;
#40661=CARTESIAN_POINT ( 'NONE',  ( 55.21462903151665813, -59.99999999999998579, -39.23961370773703550 ) ) ;
#40662=CARTESIAN_POINT ( 'NONE',  ( -76.65370120091482420, -42.96681426229719136, 130.6272736503597969 ) ) ;
#40665=CARTESIAN_POINT ( 'NONE',  ( 114.1124408062617448, -57.67112371907345647, 167.6041526721556636 ) ) ;
#40682=CARTESIAN_POINT ( 'NONE',  ( -12.27152016684560820, -14.21045842199446874, 34.40193250091021326 ) ) ;
#40683=CARTESIAN_POINT ( 'NONE',  ( 29.01152024031640408, -36.00842521231714954, 32.18407090136901871 ) ) ;
#40725=CARTESIAN_POINT ( 'NONE',  ( -66.69712465749149999, -59.99999999999995026, 102.5519887578948044 ) ) ;
#40726=CARTESIAN_POINT ( 'NONE',  ( 65.80416729607647142, -42.95812090186399246, 90.41729902910192607 ) ) ;
#40733=CARTESIAN_POINT ( 'NONE',  ( -76.10153353667877241, -57.67120126903460431, -32.17100317442078961 ) ) ;
#40752=CARTESIAN_POINT ( 'NONE',  ( -92.98499943475361817, -29.99999999999999645, 191.1145340721902244 ) ) ;
#40754=CARTESIAN_POINT ( 'NONE',  ( 58.88557130045238353, -57.67677570217782801, 103.6297432740264099 ) ) ;
#40758=CARTESIAN_POINT ( 'NONE',  ( 18.16042551299854324, -25.16802437573015894, -38.50727583685194588 ) ) ;
#40762=CARTESIAN_POINT ( 'NONE',  ( -2.999195618040080280, -60.00000000000000711, 39.63393146347493712 ) ) ;
#40766=CARTESIAN_POINT ( 'NONE',  ( -86.09502989984670762, -57.44075046393530215, 193.2120879883706266 ) ) ;
#40770=CARTESIAN_POINT ( 'NONE',  ( -9.088156012238943759, -25.54958950038574272, 28.14908607299276255 ) ) ;
#40772=CARTESIAN_POINT ( 'NONE',  ( -100.1817682225040755, -59.99999999999998579, 195.6478515624593513 ) ) ;
#40783=CARTESIAN_POINT ( 'NONE',  ( 106.9596233951320698, -14.21045842199439591, 171.9689152078629775 ) ) ;
#40804=CARTESIAN_POINT ( 'NONE',  ( -75.53587094680203506, -59.99999999999879208, 193.5314785434904934 ) ) ;
#40806=CARTESIAN_POINT ( 'NONE',  ( 39.99284958193202755, -59.99999999999998579, 52.04651499647973623 ) ) ;
#40807=CARTESIAN_POINT ( 'NONE',  ( -106.5495191435086468, -14.21045842199437992, 161.7519935124221604 ) ) ;
#40808=CARTESIAN_POINT ( 'NONE',  ( 14.45045434211625413, -32.51087426405054970, 29.42422261037161846 ) ) ;
#40809=CARTESIAN_POINT ( 'NONE',  ( 102.0588018568102342, -38.00000000000000711, 183.9494848540979319 ) ) ;
#40812=CARTESIAN_POINT ( 'NONE',  ( -46.23481718400766027, -29.15784190260456654, 42.24713126758013004 ) ) ;
#40814=VERTEX_POINT ( 'NONE', #46353 ) ;
#40827=CARTESIAN_POINT ( 'NONE',  ( 82.30761750810208355, -30.00000000000000711, 37.47418852386814336 ) ) ;
#40834=CARTESIAN_POINT ( 'NONE',  ( 100.5628734160808193, -30.00000000000000000, 160.0131903483690792 ) ) ;
#40837=VERTEX_POINT ( 'NONE', #99546 ) ;
#40847=CARTESIAN_POINT ( 'NONE',  ( 85.20711124866321029, -38.68836316264033570, 198.6075243859919510 ) ) ;
#40860=ORIENTED_EDGE ( 'NONE', *, *, #31638, .F. ) ;
#40869=DIRECTION ( 'NONE',  ( 0.000000000000000000, 1.000000000000000000, 0.000000000000000000 ) ) ;
#40877=CARTESIAN_POINT ( 'NONE',  ( 84.23537949901131583, -57.43327086003616699, 191.0502212991270596 ) ) ;
#40880=CARTESIAN_POINT ( 'NONE',  ( 94.71819068412230536, -57.66088136610299841, -7.212791323503675578 ) ) ;
#40886=CARTESIAN_POINT ( 'NONE',  ( -81.00479812864165297, -30.00000000000000355, 3.928959509420340002 ) ) ;
#40901=CARTESIAN_POINT ( 'NONE',  ( -99.92473045491273353, -37.99999999999996447, 190.7707991670974934 ) ) ;
#40908=CARTESIAN_POINT ( 'NONE',  ( -35.14829367579218200, -47.40882684376428102, -32.39548210165584408 ) ) ;
#40915=CARTESIAN_POINT ( 'NONE',  ( -87.93412205286334427, -60.00000000000001421, -21.65732652878994102 ) ) ;
#40919=CARTESIAN_POINT ( 'NONE',  ( 97.07153444841249268, -60.35596137945897510, 196.7631902911030295 ) ) ;
#40923=ORIENTED_EDGE ( 'NONE', *, *, #76351, .T. ) ;
#40933=CARTESIAN_POINT ( 'NONE',  ( -46.61116709543701120, -57.68144024183414587, 68.72738526911024337 ) ) ;
#40939=CARTESIAN_POINT ( 'NONE',  ( -24.89493309229959195, -29.99999999999998934, -38.80368402536839056 ) ) ;
#40941=CARTESIAN_POINT ( 'NONE',  ( -8.181074200006944963, -14.21045842199423603, 34.35486773805523342 ) ) ;
#40943=CARTESIAN_POINT ( 'NONE',  ( -52.90029590074614418, -39.50658224128886786, 55.98782116498496464 ) ) ;
#40948=CARTESIAN_POINT ( 'NONE',  ( -101.7223263897890035, -60.22553723381597734, 194.4964868810712630 ) ) ;
#40954=CARTESIAN_POINT ( 'NONE',  ( 108.8142615268778002, -38.35658623041307180, 190.7462066422830276 ) ) ;
#40962=CARTESIAN_POINT ( 'NONE',  ( 84.02542197617383124, -29.99999999999999289, 161.2336401493205642 ) ) ;
#40969=CARTESIAN_POINT ( 'NONE',  ( 48.85197278088530481, -49.90039430658988096, 52.23959260655022518 ) ) ;
#40973=CARTESIAN_POINT ( 'NONE',  ( -108.0292185885723200, -38.35629187912161342, 138.0457264600484280 ) ) ;
#40975=ORIENTED_EDGE ( 'NONE', *, *, #39322, .T. ) ;
#40977=CARTESIAN_POINT ( 'NONE',  ( 92.04294571132990654, -38.35407588941761503, 35.15094813657322703 ) ) ;
#40979=CARTESIAN_POINT ( 'NONE',  ( 97.91740595962181715, -37.84853790336257617, 125.6665356466635188 ) ) ;
#40984=CARTESIAN_POINT ( 'NONE',  ( 74.43575368222239774, -60.00000000000000000, 176.5049923845488706 ) ) ;
#40986=CARTESIAN_POINT ( 'NONE',  ( 60.30973395284412675, -42.96154581061870203, 74.70304224304538820 ) ) ;
#40991=CARTESIAN_POINT ( 'NONE',  ( -85.26481701026371240, -38.35926911274526674, -22.62496792076730401 ) ) ;
#41004=CARTESIAN_POINT ( 'NONE',  ( 85.16083850732167093, -25.44627968698079101, 168.4994044799329629 ) ) ;
#41008=ORIENTED_EDGE ( 'NONE', *, *, #84634, .F. ) ;
#41022=CARTESIAN_POINT ( 'NONE',  ( -12.38234718253561617, -21.30825843599406255, 35.60706586959262410 ) ) ;
#41035=CARTESIAN_POINT ( 'NONE',  ( 63.53569133900827381, -34.58942215426228728, -24.20822403974327486 ) ) ;
#41044=CARTESIAN_POINT ( 'NONE',  ( -98.11006555757215608, -60.00000000000000000, 69.60638578265736953 ) ) ;
#41046=CARTESIAN_POINT ( 'NONE',  ( 1.492654932474820107E-05, -32.51280158588350133, 29.30845022391629229 ) ) ;
#41051=CARTESIAN_POINT ( 'NONE',  ( -85.24946139480805130, -25.41916126808991194, 169.5220700656399231 ) ) ;
#41056=( BOUNDED_SURFACE ( )  B_SPLINE_SURFACE ( 2, 3, ( 
 ( #95723, #3530, #4592, #102753, #86063, #5641, #45064, #96269, #79528, #71424, #78469, #94683, #95202, #29948, #62832, #4060, #21335, #46118, #36989, #22397, #102217, #55240, #12660, #61243, #46631, #20831, #45591, #13187, #70389, #103289, #13723, #79001, #21863, #5122 ),
 ( #88165, #94126, #69859, #54704, #28914, #61789, #87639, #29435, #14249, #38055, #70912, #47154, #86596, #36469, #20295, #53144, #97833, #15854, #48733, #32603, #39092, #71972, #56288, #98875, #89757, #31545, #7749, #7222, #97297, #64940, #80577, #22919, #105913, #96788 ),
 ( #15322, #89225, #74079, #48209, #73542, #81113, #90816, #40659, #23991, #40132, #47678, #82171, #55757, #33129, #57893, #56833, #81626, #14784, #8288, #65475, #88688, #164, #106446, #73009, #98365, #90278, #6697, #41194, #24519, #57358, #16381, #65999, #49268, #25036 ) ),
 .UNSPECIFIED., .F., .T., .F. ) 
 B_SPLINE_SURFACE_WITH_KNOTS ( ( 3, 3 ),
 ( 4, 2, 2, 2, 2, 2, 2, 2, 2, 2, 2, 2, 2, 2, 2, 2, 4 ),
 ( 0.000000000000000000, 1.000000000000000000 ),
 ( -3.141592653589793116, -2.748893571891068976, -2.356194490192344837, -1.963495408493620697, -1.570796326794896558, -1.178097245096172418, -0.7853981633974482790, -0.3926990816987241395, 0.000000000000000000, 0.3926990816987241395, 0.7853981633974482790, 1.178097245096172418, 1.570796326794896558, 1.963495408493620697, 2.356194490192344837, 2.748893571891068976, 3.141592653589793116 ),
 .UNSPECIFIED. ) 
 GEOMETRIC_REPRESENTATION_ITEM ( )  RATIONAL_B_SPLINE_SURFACE ( (
 ( 1.000000000000000000, 1.000000000000000000, 1.000000000000000000, 1.000000000000000000, 1.000000000000000000, 1.000000000000000000, 1.000000000000000000, 1.000000000000000000, 1.000000000000000000, 1.000000000000000000, 1.000000000000000000, 1.000000000000000000, 1.000000000000000000, 1.000000000000000000, 1.000000000000000000, 1.000000000000000000, 1.000000000000000000, 1.000000000000000000, 1.000000000000000000, 1.000000000000000000, 1.000000000000000000, 1.000000000000000000, 1.000000000000000000, 1.000000000000000000, 1.000000000000000000, 1.000000000000000000, 1.000000000000000000, 1.000000000000000000, 1.000000000000000000, 1.000000000000000000, 1.000000000000000000, 1.000000000000000000, 1.000000000000000000, 1.000000000000000000),
 ( 1.857142857142858317, 1.857142857142858317, 1.857142857142858317, 1.857142857142858317, 1.857142857142858317, 1.857142857142858317, 1.857142857142858317, 1.857142857142858317, 1.857142857142858317, 1.857142857142858317, 1.857142857142858317, 1.857142857142858317, 1.857142857142858317, 1.857142857142858317, 1.857142857142858317, 1.857142857142858317, 1.857142857142858317, 1.857142857142858317, 1.857142857142858317, 1.857142857142858317, 1.857142857142858317, 1.857142857142858317, 1.857142857142858317, 1.857142857142858317, 1.857142857142858317, 1.857142857142858317, 1.857142857142858317, 1.857142857142858317, 1.857142857142858317, 1.857142857142858317, 1.857142857142858317, 1.857142857142858317, 1.857142857142858317, 1.857142857142858317),
 ( 1.000000000000000000, 1.000000000000000000, 1.000000000000000000, 1.000000000000000000, 1.000000000000000000, 1.000000000000000000, 1.000000000000000000, 1.000000000000000000, 1.000000000000000000, 1.000000000000000000, 1.000000000000000000, 1.000000000000000000, 1.000000000000000000, 1.000000000000000000, 1.000000000000000000, 1.000000000000000000, 1.000000000000000000, 1.000000000000000000, 1.000000000000000000, 1.000000000000000000, 1.000000000000000000, 1.000000000000000000, 1.000000000000000000, 1.000000000000000000, 1.000000000000000000, 1.000000000000000000, 1.000000000000000000, 1.000000000000000000, 1.000000000000000000, 1.000000000000000000, 1.000000000000000000, 1.000000000000000000, 1.000000000000000000, 1.000000000000000000) ) ) 
 REPRESENTATION_ITEM ( '' )  SURFACE ( )  );
#41060=CARTESIAN_POINT ( 'NONE',  ( -28.02803974396783815, -57.67115643259209889, -43.15031372974605972 ) ) ;
#41068=CARTESIAN_POINT ( 'NONE',  ( 106.9596233951320698, -14.21045842199439591, 171.9689152078629775 ) ) ;
#41069=CARTESIAN_POINT ( 'NONE',  ( -106.8236106313706699, -14.21045842199435150, 178.1018237235793151 ) ) ;
#41070=CARTESIAN_POINT ( 'NONE',  ( -63.52003477808261778, -25.58132851056570090, 74.89366634491645414 ) ) ;
#41073=CARTESIAN_POINT ( 'NONE',  ( 114.6122575509365760, -60.00000000000000000, 171.8902597099684613 ) ) ;
#41075=CARTESIAN_POINT ( 'NONE',  ( 0.9910821173258683725, -25.54837917066274144, 28.14771315471283586 ) ) ;
#41080=CARTESIAN_POINT ( 'NONE',  ( -80.00000000000000000, -52.00000000000000000, -21.09707704303352926 ) ) ;
#41083=CARTESIAN_POINT ( 'NONE',  ( -103.4937426735914272, -59.99999999999997158, 200.3256067693197906 ) ) ;
#41095=CARTESIAN_POINT ( 'NONE',  ( 85.71523080318266352, -59.99999999999998579, -14.67970160156688131 ) ) ;
#41097=CARTESIAN_POINT ( 'NONE',  ( -32.59290073874363713, -29.08836541010333221, 32.21693739891244235 ) ) ;
#41100=CARTESIAN_POINT ( 'NONE',  ( 39.87495318460441496, -32.60419010241520255, 37.08222683619865734 ) ) ;
#41105=CARTESIAN_POINT ( 'NONE',  ( -76.84105350964979664, -38.44307565171133945, 183.5766925144648667 ) ) ;
#41116=CARTESIAN_POINT ( 'NONE',  ( 103.5527963412081078, -59.99999999999997868, 101.8182540185962495 ) ) ;
#41121=CARTESIAN_POINT ( 'NONE',  ( -97.91052317031356722, -29.99999999999989342, 190.6167072790179020 ) ) ;
#41139=CARTESIAN_POINT ( 'NONE',  ( 81.69469107942758512, -39.49696098175696335, 158.0307039208131812 ) ) ;
#41145=CARTESIAN_POINT ( 'NONE',  ( 0.000000000000000000, -38.00000000000000711, 0.000000000000000000 ) ) ;
#41146=CARTESIAN_POINT ( 'NONE',  ( -54.50637188337720573, -60.00000000000000000, -31.07177919240839259 ) ) ;
#41157=CARTESIAN_POINT ( 'NONE',  ( 22.06473419488195375, -27.05810140444713241, 37.35228815185911344 ) ) ;
#41173=CARTESIAN_POINT ( 'NONE',  ( 111.5704048199732199, -57.67092548021626186, 192.6104883897414197 ) ) ;
#41179=CARTESIAN_POINT ( 'NONE',  ( -75.41869077044756864, -60.00000000000000711, 184.0143711039829384 ) ) ;
#41184=CARTESIAN_POINT ( 'NONE',  ( -86.20901956646225983, -24.70671085932096389, 181.2931684475793190 ) ) ;
#41189=CARTESIAN_POINT ( 'NONE',  ( -84.49020180651892531, -45.26885603981717310, -7.230634734441095723 ) ) ;
#41194=CARTESIAN_POINT ( 'NONE',  ( 14.86825985028009001, 0.000000000000000000, 8.569529079650957115 ) ) ;
#41196=CARTESIAN_POINT ( 'NONE',  ( -53.63968661800659277, -29.99999999999997158, -34.46705067659466692 ) ) ;
#41197=CARTESIAN_POINT ( 'NONE',  ( -75.47494900001981932, -46.43776707097643452, 127.8804621272367257 ) ) ;
#41199=CARTESIAN_POINT ( 'NONE',  ( 72.58683006904378487, -60.00000000000011369, 181.3898877100950244 ) ) ;
#41201=CARTESIAN_POINT ( 'NONE',  ( 114.2218302459193353, -57.67112208883745694, 174.7537043705229109 ) ) ;
#41202=ORIENTED_EDGE ( 'NONE', *, *, #9058, .T. ) ;
#41217=CARTESIAN_POINT ( 'NONE',  ( 29.62289515650491722, -36.01063597977103825, 32.38572331401633875 ) ) ;
#41233=CARTESIAN_POINT ( 'NONE',  ( 89.49579725498631433, -60.00000000000002132, -19.63851451753554045 ) ) ;
#41255=CARTESIAN_POINT ( 'NONE',  ( 0.000000000000000000, -38.00000000000000711, 0.000000000000000000 ) ) ;
#41259=CARTESIAN_POINT ( 'NONE',  ( -51.99581617557301172, -60.00000000000000000, 61.82981693614253516 ) ) ;
#41261=CARTESIAN_POINT ( 'NONE',  ( 65.46944084899945437, -22.10224947482613445, 78.54547059327050818 ) ) ;
#41265=CARTESIAN_POINT ( 'NONE',  ( -93.85239982658497127, -57.67543968518839392, 9.450824874790988872 ) ) ;
#41285=CARTESIAN_POINT ( 'NONE',  ( -97.46380090642580285, -30.00000000000000000, 190.9071124952730827 ) ) ;
#41289=CARTESIAN_POINT ( 'NONE',  ( 70.40533769610152603, -57.68249443943340538, 157.3263788805991794 ) ) ;
#41291=DIRECTION ( 'NONE',  ( 1.000000000000000000, 0.000000000000000000, 1.871721906610600077E-16 ) ) ;
#41294=CARTESIAN_POINT ( 'NONE',  ( 10.19526563809554887, -22.67231299545676038, -38.54255160387786106 ) ) ;
#41297=CARTESIAN_POINT ( 'NONE',  ( -11.58643080058957331, -60.00000000000000000, 39.67679234348616291 ) ) ;
#41301=CARTESIAN_POINT ( 'NONE',  ( -86.81445332370094548, -39.11233341703805877, 188.7329318314524471 ) ) ;
#41306=CARTESIAN_POINT ( 'NONE',  ( -10.19412816461805349, -32.51289075256729433, 29.31908308346052650 ) ) ;
#41317=CARTESIAN_POINT ( 'NONE',  ( 107.0562500300223974, -29.99999999999996803, 141.2193814890308374 ) ) ;
#41338=CARTESIAN_POINT ( 'NONE',  ( -22.10471256930616946, -59.99999999999009503, 42.93026933855558269 ) ) ;
#41340=EDGE_LOOP ( 'NONE', ( #105763, #14194 ) ) ;
#41341=CARTESIAN_POINT ( 'NONE',  ( 96.59781651622874676, -60.00000000000002842, 202.5112741595065131 ) ) ;
#41342=CARTESIAN_POINT ( 'NONE',  ( -103.0033221043092482, -14.21045842199434084, 193.8525198385365798 ) ) ;
#41343=CARTESIAN_POINT ( 'NONE',  ( 17.52946471254341532, -22.06958086768002403, 27.84760488160436509 ) ) ;
#41345=FACE_OUTER_BOUND ( 'NONE', #101055, .T. ) ;
#41348=CARTESIAN_POINT ( 'NONE',  ( -43.59263858471909003, -25.70516687255675237, 38.53872847185795791 ) ) ;
#41360=CARTESIAN_POINT ( 'NONE',  ( 77.04941373716538067, -29.99999999997682920, 175.5720900168622052 ) ) ;
#41365=CARTESIAN_POINT ( 'NONE',  ( 92.38617115133855862, -30.00000000000000355, 102.4331776802988259 ) ) ;
#41384=CARTESIAN_POINT ( 'NONE',  ( 78.95220114007015866, -38.68516239071802687, 190.8228697010661676 ) ) ;
#41397=SURFACE_STYLE_USAGE ( .BOTH. , #14987 ) ;
#41399=CARTESIAN_POINT ( 'NONE',  ( 38.00103629177208120, -36.97174142536137254, 47.25231011079808496 ) ) ;
#41404=CARTESIAN_POINT ( 'NONE',  ( 85.55019892396339287, -42.90932130096805253, 187.2143489094230233 ) ) ;
#41408=CARTESIAN_POINT ( 'NONE',  ( 91.48635331273750637, -57.66236828961498873, -20.18083513732546663 ) ) ;
#41410=CARTESIAN_POINT ( 'NONE',  ( -80.77853634343884437, -30.00000000000000000, 9.880813862764185274 ) ) ;
#41413=CARTESIAN_POINT ( 'NONE',  ( -80.70597897318361902, -37.99999999999994316, 148.6524463937931841 ) ) ;
#41419=EDGE_CURVE ( 'NONE', #38016, #30532, #37678, .T. ) ;
#41433=CARTESIAN_POINT ( 'NONE',  ( -44.52380092682520285, -26.14798797473085656, -29.30983052058080673 ) ) ;
#41444=CARTESIAN_POINT ( 'NONE',  ( -35.89949308352697699, -60.00000000000000000, -40.19304179322571713 ) ) ;
#41448=CARTESIAN_POINT ( 'NONE',  ( 100.4700211219143284, -52.75663466979855798, 193.8560308224012374 ) ) ;
#41462=CARTESIAN_POINT ( 'NONE',  ( -62.53353137064869571, -57.67819947725070051, 116.5065130283015975 ) ) ;
#41467=CARTESIAN_POINT ( 'NONE',  ( 52.80879785486305167, -14.21045842199441722, -31.95559855168728092 ) ) ;
#41471=CARTESIAN_POINT ( 'NONE',  ( -51.80964144195790055, -22.18443608985152338, 47.83208226989306411 ) ) ;
#41475=CARTESIAN_POINT ( 'NONE',  ( -98.08353087601894060, -37.72577662167667256, 192.4636628619757630 ) ) ;
#41480=CARTESIAN_POINT ( 'NONE',  ( 104.7235773805048780, -38.39894542868824345, 197.7612429682840229 ) ) ;
#41484=CARTESIAN_POINT ( 'NONE',  ( 85.38339423818332818, -30.00000000000000355, 173.8457401421241002 ) ) ;
#41493=CARTESIAN_POINT ( 'NONE',  ( 52.77684154638642156, -42.97022567233157275, 57.04277442930182929 ) ) ;
#41498=CARTESIAN_POINT ( 'NONE',  ( -98.66193420133994607, -38.35555159526315805, 80.57390941483606639 ) ) ;
#41501=CARTESIAN_POINT ( 'NONE',  ( 98.48976283628422834, -38.35583645532683050, 79.54628558377670799 ) ) ;
#41503=CARTESIAN_POINT ( 'NONE',  ( 88.74246461038792688, -45.28266603850529037, 62.97167601515477031 ) ) ;
#41509=CARTESIAN_POINT ( 'NONE',  ( 74.50857564272573086, -60.00000000000000000, 177.1830442982434306 ) ) ;
#41514=CARTESIAN_POINT ( 'NONE',  ( 63.23442538735326934, -18.63162660745866006, 70.69744974475220545 ) ) ;
#41519=CARTESIAN_POINT ( 'NONE',  ( -51.92511257527466029, -30.00000000004022027, 69.42736369518064521 ) ) ;
#41528=CARTESIAN_POINT ( 'NONE',  ( 85.21729610370397268, -28.80435702628989603, 174.9444428549488180 ) ) ;
#41542=CARTESIAN_POINT ( 'NONE',  ( 39.21813245877796561, -60.00000000000002842, 51.03055488639744652 ) ) ;
#41547=CARTESIAN_POINT ( 'NONE',  ( -4.718689085033623165, -18.53111709059378143, 35.08043246123458658 ) ) ;
#41562=CARTESIAN_POINT ( 'NONE',  ( 24.94155541167982904, -21.77049003089739188, -29.25405592835566537 ) ) ;
#41567=EDGE_LOOP ( 'NONE', ( #75541, #78279, #104421, #8705, #39436, #47175, #70851 ) ) ;
#41571=CARTESIAN_POINT ( 'NONE',  ( -95.53324824102833190, -59.99999999999999289, 52.82992578362362934 ) ) ;
#41578=CARTESIAN_POINT ( 'NONE',  ( -85.83737659453286994, -18.50073294457022044, 163.5530722848842231 ) ) ;
#41588=B_SPLINE_CURVE_WITH_KNOTS ( 'NONE', 3,
 ( #100126, #66704, #25762, #26293, #92036, #28406, #28957, #94724, #72404, #22827, #15227, #48640, #64332, #36508, #38991, #97202, #89126, #31966, #64845, #23348, #89660, #37030, #97725, #55659, #94175, #77986, #88596, #40041, #88073, #71868, #48113, #55143, #56188, #47055, #4102, #6066, #81012, #69899, #102797, #6598, #61280, #23892, #31450, #104773, #30922, #105825, #81525, #56735, #102257, #39527, #7130, #80480, #72916, #14151, #15759, #63802, #14678, #79955, #105307, #61828, #96689, #47584, #86104, #69375, #22297, #20341, #53187, #12174, #45106, #16833, #74517, #1138, #66434, #51300, #99315, #33040, #34112, #58896, #82624, #75589, #41105, #82076, #106346, #66983, #73987, #24943, #49171, #58346, #26557, #32508, #83152, #100394, #65906, #26037, #57796, #83669, #91266, #25488, #49716, #33559, #59428, #90720, #1689, #69, #17377, #99864, #9248, #65380, #8195, #50760, #42158, #92291, #7649, #42695, #75039, #91787, #17908, #24429, #9778, #34645, #41634, #50251, #16286, #98271, #98786, #67514, #18445, #40566, #8726, #595, #57261, #73448, #90184, #78247, #11913, #44842, #21126, #61022, #36772, #43233, #61558, #27085, #3301, #84752, #20065, #11367, #76117, #28674, #4359, #2213, #51838, #86372, #62096, #45364, #52369, #68030, #77730, #103066, #93909, #69115, #93385, #29222, #94455, #101468, #37295, #43753, #52914, #69637, #85838, #35163, #10833, #20612, #3841, #94988, #84221, #12438, #102530, #53452, #70162, #100923, #10315, #59972, #92832, #36246, #18996, #76645, #2755, #35707, #68585, #27620, #60501, #19532, #85280, #44295, #77190, #101988, #28145, #88473, #97593, #30791, #6464, #22699, #96564, #103586, #79829, #54470, #55536, #87942, #45886, #105178, #80888, #78765, #21637, #56059, #31837, #15093, #22160, #37831, #47457, #72790, #14548, #55010, #31324, #95494, #87419, #80350, #4900, #70695, #6999, #39397, #14024, #46930, #47981, #64719, #39918, #12964, #72275, #64206, #97076, #23220, #30247, #5934, #53955, #88999, #13495, #38861, #46418, #29735, #71727, #62608, #104638, #79304, #63675, #105695, #86891, #5426, #63134, #38350, #71210, #104104, #96034, #16696, #50628, #16155, #9119, #65248, #996, #56608, #98138, #15624, #50120, #57139, #40973, #24290, #74386, #42556, #48516, #99187, #9646, #49043, #42029, #83029, #74911, #8596, #90052, #73316, #41498, #106212, #98661, #81940, #24812, #57663, #58763, #8062, #32905, #90587, #17248, #82495, #67386, #465, #73862, #106757, #33975, #65782, #66847, #89533, #49586, #81407, #99737, #33433, #66307, #25350, #58212, #75457, #7518, #91138, #1552, #25907, #91661, #17775, #83546, #34517, #23759, #40436, #32375, #3717, #10712, #94322, #59833, #3172, #85704, #68987, #18316, #100792, #36647, #101863, #78121, #100267, #28547, #28022, #77599, #10189, #19940, #69511, #27495, #35041, #102397, #43627, #75990, #51708, #45241, #101342, #44710, #51168, #61428, #60371, #84089, #35575, #59295, #11779, #20486, #77057, #52781, #92168, #53324, #36118, #86242, #12316, #2089, #26430, #76518, #4235, #93245, #67905, #37170, #43103, #68448, #26953, #60892, #2628, #93780, #92705, #18865, #84626, #19410, #52243, #85151, #11242, #44170, #53841, #63011, #12839, #104512, #45757, #95909 ),
 .UNSPECIFIED., .F., .F.,
 ( 4, 2, 2, 2, 2, 1, 1, 1, 2, 2, 1, 1, 2, 2, 2, 2, 2, 1, 1, 2, 2, 1, 2, 2, 2, 2, 2, 1, 1, 1, 2, 2, 1, 1, 2, 2, 2, 2, 2, 1, 1, 2, 2, 1, 2, 2, 2, 2, 2, 1, 2, 2, 2, 2, 1, 1, 1, 1, 1, 1, 1, 2, 2, 2, 2, 1, 2, 2, 1, 1, 2, 2, 2, 1, 1, 2, 2, 1, 2, 2, 2, 2, 2, 2, 1, 2, 2, 1, 1, 2, 2, 2, 1, 1, 1, 1, 2, 2, 2, 1, 1, 2, 2, 1, 2, 2, 2, 2, 2, 2, 1, 1, 2, 2, 1, 2, 2, 2, 2, 2, 2, 2, 2, 2, 2, 1, 1, 1, 2, 2, 2, 2, 2, 1, 1, 2, 2, 1, 1, 2, 2, 2, 2, 2, 2, 1, 1, 1, 1, 1, 2, 2, 2, 2, 2, 2, 2, 1, 1, 2, 2, 2, 2, 1, 2, 2, 2, 2, 2, 2, 1, 2, 2, 2, 2, 2, 2, 1, 1, 1, 1, 2, 2, 1, 2, 2, 2, 2, 1, 1, 1, 2, 2, 2, 2, 2, 2, 2, 2, 1, 1, 1, 2, 2, 1, 2, 2, 2, 2, 1, 1, 2, 2, 1, 1, 2, 2, 2, 2, 1, 2, 2, 1, 2, 2, 2, 1, 1, 1, 1, 2, 2, 1, 1, 2, 2, 2, 2, 4 ),
 ( 0.000000000000000000, 0.01562500000017991511, 0.03125000000035977471, 0.06250000000071946615, 0.09375000000107916454, 0.09765625000112419796, 0.09960937500114669385, 0.09985351562614952492, 0.09997558593865092658, 0.1000976562511523282, 0.1005859375011582263, 0.1015625000011698836, 0.1093750000012639056, 0.1250000000014519219, 0.1562500000018279822, 0.1875000000022040703, 0.1953125000022981617, 0.1992187500023451519, 0.1997070312523510360, 0.1999511718773539504, 0.2001953125023568647, 0.2011718750023685776, 0.2031250000023920033, 0.2187500000025786595, 0.2500000000029521385, 0.2812500000033256176, 0.2968750000035121350, 0.2988281250035352832, 0.2998046875035465519, 0.2999267578160477732, 0.2999877929722987169, 0.3000488281285496606, 0.3002929687535534908, 0.3007812500035613734, 0.3046875000036236014, 0.3125000000037479464, 0.3281250000039964698, 0.3437500000042449932, 0.3476562500043071657, 0.3496093750043382520, 0.3498535156293420822, 0.3499755859418440807, 0.3500976562543460235, 0.3505859375043537396, 0.3515625000043693382, 0.3593750000044939052, 0.3613281250045251025, 0.3623046875045407567, 0.3625488281295446424, 0.3627929687545484727, 0.3632812500045560777, 0.3671875000046159743, 0.3710937500046758708, 0.3730468750047058468, 0.3740234375047207793, 0.3745117187547281068, 0.3747558593797318816, 0.3748779296922336579, 0.3749389648484845461, 0.3749694824266098792, 0.3749847412156725457, 0.3749923706102039067, 0.3750000000047352677, 0.3789062500047620241, 0.3808593750047754023, 0.3811035156297769011, 0.3812255859422775672, 0.3812561035204025672, 0.3812866210985276227, 0.3813476562547776227, 0.3818359375047775672, 0.3828125000047774007, 0.3837890625047772342, 0.3842773437547771231, 0.3843383789110271231, 0.3843688964891520676, 0.3843994140672770121, 0.3845214843797769011, 0.3847656250047766235, 0.3867187500047745141, 0.3872070312547740145, 0.3874511718797736815, 0.3876953125047734039, 0.3886718750047721271, 0.3889160156297718496, 0.3890380859422716275, 0.3890686035203966275, 0.3890991210985215720, 0.3891601562547715165, 0.3896484375047711834, 0.3901367187547708504, 0.3903808593797707394, 0.3905029296922706283, 0.3905639648485206283, 0.3905944824266456283, 0.3906097412157081283, 0.3906173706102394338, 0.3906250000047707394, 0.3925781250047735149, 0.3935546875047748472, 0.3936767578172750692, 0.3937377929735251247, 0.3937988281297752358, 0.3940429687547757354, 0.3945312500047768456, 0.3964843750047810644, 0.3984375000047852833, 0.3994140625047873927, 0.3999023437547884474, 0.4000244140672886695, 0.4001464843797889470, 0.4003906250047893911, 0.4023437500047932769, 0.4042968750047971627, 0.4045410156297976623, 0.4046630859422979398, 0.4047851562547982729, 0.4052734375047992721, 0.4062500000048012705, 0.4072265625048032134, 0.4082031250048052118, 0.4091796875048071547, 0.4093017578173074322, 0.4093627929735575433, 0.4093780517626200433, 0.4093933105516825988, 0.4094238281298077653, 0.4096679687548091531, 0.4101562500048119841, 0.4121093750048231419, 0.4140625000048342996, 0.4179687500048566151, 0.4184570312548593907, 0.4187011718798607229, 0.4187316894579859450, 0.4187469482470485560, 0.4187622070361111670, 0.4188232421923611115, 0.4189453125048605564, 0.4199218750048568927, 0.4218750000048491211, 0.4296875000048183679, 0.4335937500048029358, 0.4355468750047952198, 0.4365234375047912785, 0.4370117187547892801, 0.4372558593797882809, 0.4373779296922877258, 0.4374389648485373927, 0.4374694824266622262, 0.4374847412157246707, 0.4375000000047870596, 0.4531250000046511683, 0.4687500000045152770, 0.4726562500044813042, 0.4746093750044643178, 0.4750976562544601545, 0.4755859375044559356, 0.4765625000044472759, 0.4843750000043788861, 0.5000000000042420512, 0.5312500000039681591, 0.5468750000038312686, 0.5488281250038139492, 0.5498046875038054004, 0.5507812500037969627, 0.5546875000037631009, 0.5625000000036955994, 0.6250000000031556979, 0.6875000000026157965, 0.6953125000025484059, 0.6992187500025146552, 0.7031250000024809044, 0.7187500000023461233, 0.7500000000020765611, 0.7812500000018071100, 0.8125000000015376589, 0.8164062500015040191, 0.8183593750014871437, 0.8193359375014788171, 0.8198242187514745982, 0.8199462890639735990, 0.8200683593764725998, 0.8203125000014704904, 0.8281250000014037660, 0.8437500000012704282, 0.8750000000010035306, 0.9062500000007366330, 0.9082031250007198686, 0.9091796875007116530, 0.9096679687507074341, 0.9099121093757054357, 0.9101562500007033263, 0.9140625000006702416, 0.9218750000006040723, 0.9296875000005380141, 0.9375000000004718448, 0.9453125000004056755, 0.9531250000003395062, 0.9541015625003312906, 0.9545898437503270717, 0.9548339843753250733, 0.9549560546878239631, 0.9550170898440735190, 0.9550781250003229639, 0.9570312500003061995, 0.9609375000002724487, 0.9648437500002386980, 0.9658203125002302603, 0.9660644531252281508, 0.9661865234377271516, 0.9662475585939765965, 0.9662628173830389855, 0.9662780761721013745, 0.9663085937502260414, 0.9667968750002211564, 0.9687500000002018385, 0.9707031250001825207, 0.9716796875001727507, 0.9718017578126714184, 0.9718627929689208633, 0.9719238281251701972, 0.9721679687501676437, 0.9726562500001626477, 0.9746093750001423306, 0.9765625000001219025, 0.9770507812501169065, 0.9772949218751143530, 0.9774169921876131317, 0.9774780273438624656, 0.9774932861329248546, 0.9775009155274559935, 0.9775085449219870215, 0.9775390625001119105, 0.9785156250001071365, 0.9804687500000973666, 0.9843750000000778266, 0.9921875000000389688, 1.000000000000000000 ),
 .UNSPECIFIED. ) ;
#41590=DIRECTION ( 'NONE',  ( 0.000000000000000000, 1.000000000000000000, 0.000000000000000000 ) ) ;
#41598=CARTESIAN_POINT ( 'NONE',  ( 109.0466504562702141, -30.00000000000000355, 159.8086616330221830 ) ) ;
#41601=CARTESIAN_POINT ( 'NONE',  ( -106.9108898249343156, -14.21045842199431242, 176.0583478801969193 ) ) ;
#41602=CARTESIAN_POINT ( 'NONE',  ( -62.44653457475159541, -42.96348183423683054, 80.59091618468615081 ) ) ;
#41605=CARTESIAN_POINT ( 'NONE',  ( 106.2951369877889221, -59.99999999999133848, 201.2543869268758101 ) ) ;
#41607=CARTESIAN_POINT ( 'NONE',  ( 2.979342351834940228, -22.06717662120162871, 27.56309061281193706 ) ) ;
#41608=CARTESIAN_POINT ( 'NONE',  ( -104.9289101731156961, -60.15511913292260004, 149.1721339770082295 ) ) ;
#41615=CARTESIAN_POINT ( 'NONE',  ( -35.19798225690215787, -60.00000000000001421, 46.55359730984257283 ) ) ;
#41618=CARTESIAN_POINT ( 'NONE',  ( 89.99999999999997158, -38.00000000001091394, 196.0238439516549818 ) ) ;
#41620=CARTESIAN_POINT ( 'NONE',  ( 12.81923949848201971, -0.000000000000000000, 11.24494283604525080 ) ) ;
#41625=CARTESIAN_POINT ( 'NONE',  ( 86.19989974210415085, -60.00000000000000711, 6.707520835489996003 ) ) ;
#41626=CARTESIAN_POINT ( 'NONE',  ( -32.55836021993020779, -39.49469638261044935, 34.14499934634533673 ) ) ;
#41629=CARTESIAN_POINT ( 'NONE',  ( 42.02483648120990978, -36.06897935197377336, 39.65630586122958334 ) ) ;
#41633=( GEOMETRIC_REPRESENTATION_CONTEXT ( 3 ) GLOBAL_UNCERTAINTY_ASSIGNED_CONTEXT ( ( #15960 ) ) GLOBAL_UNIT_ASSIGNED_CONTEXT ( ( #96358, #23006, #97921 ) ) REPRESENTATION_CONTEXT ( 'NONE', 'WORKASPACE' ) );
#41634=CARTESIAN_POINT ( 'NONE',  ( -81.53445610154220446, -38.84159544557321908, 195.3185924584556687 ) ) ;
#41638=CARTESIAN_POINT ( 'NONE',  ( 78.44240119052240345, -60.00000000000003553, 159.1745854876873238 ) ) ;
#41646=CARTESIAN_POINT ( 'NONE',  ( 109.4407305757422222, -60.00000000000002132, 139.1494640894100030 ) ) ;
#41650=CARTESIAN_POINT ( 'NONE',  ( -94.96020567939359580, -29.99999999999991473, 191.3500368583484885 ) ) ;
#41661=CARTESIAN_POINT ( 'NONE',  ( 81.51636251900598040, -49.93621807469046558, 172.6898897633368222 ) ) ;
#41671=CARTESIAN_POINT ( 'NONE',  ( 33.77031889322872615, -60.00000000000001421, -34.68851707423049646 ) ) ;
#41678=CARTESIAN_POINT ( 'NONE',  ( 86.85191061701388548, -31.73550785420024312, 186.9884310306377699 ) ) ;
#41697=ORIENTED_EDGE ( 'NONE', *, *, #38243, .F. ) ;
#41701=CARTESIAN_POINT ( 'NONE',  ( 109.1940635787650251, -57.66566924721494303, 197.4402562130856609 ) ) ;
#41705=CARTESIAN_POINT ( 'NONE',  ( 9.999999999999998224, -15.00000000000000000, -9.999999999999998224 ) ) ;
#41708=CARTESIAN_POINT ( 'NONE',  ( -82.81552959430850080, -60.00000000000000000, 198.6933800083513404 ) ) ;
#41712=CARTESIAN_POINT ( 'NONE',  ( -84.97692457071781291, -42.95386403672870301, 185.6637990199461115 ) ) ;
#41717=CARTESIAN_POINT ( 'NONE',  ( -87.03223608452462656, -60.20541530288490861, -7.697531398653797652 ) ) ;
#41726=CARTESIAN_POINT ( 'NONE',  ( -24.50860473033056053, -14.21045842199433018, -36.19504829128915446 ) ) ;
#41727=CARTESIAN_POINT ( 'NONE',  ( -76.85289103080442885, -53.37786451256174303, 140.9389337355551106 ) ) ;
#41729=CARTESIAN_POINT ( 'NONE',  ( 73.20681906048392307, -14.21045842199435150, 129.4971587772804185 ) ) ;
#41731=CARTESIAN_POINT ( 'NONE',  ( 96.62604160751135396, -57.67146650215429560, 46.51347612679317223 ) ) ;
#41749=CARTESIAN_POINT ( 'NONE',  ( 28.52458533298364429, -25.58352184121855899, 30.19512149105761978 ) ) ;
#41763=CARTESIAN_POINT ( 'NONE',  ( 77.39690536252481934, -60.00000000000001421, -29.37461049562547544 ) ) ;
#41778=CARTESIAN_POINT ( 'NONE',  ( 85.75250664619655083, -52.74283471586529259, -6.162475269740077088 ) ) ;
#41787=CARTESIAN_POINT ( 'NONE',  ( -77.01522031534267398, -38.45872817139124322, 184.5006283049931994 ) ) ;
#41789=CARTESIAN_POINT ( 'NONE',  ( -52.84572055339269525, -60.00000000000001421, 63.71983262547996674 ) ) ;
#41791=CARTESIAN_POINT ( 'NONE',  ( 64.67324255147873657, -60.33694573152096297, 96.31390942180495074 ) ) ;
#41795=CARTESIAN_POINT ( 'NONE',  ( -106.6432006776756083, -57.67119647726944009, 107.9924613694791589 ) ) ;
#41813=CARTESIAN_POINT ( 'NONE',  ( 11.17393077666423373, -60.00000000000000711, 39.66661916941054500 ) ) ;
#41814=CARTESIAN_POINT ( 'NONE',  ( -95.45231390711828112, -29.99999999999999645, 191.3292026307100286 ) ) ;
#41820=CARTESIAN_POINT ( 'NONE',  ( 63.37667947266371726, -57.67874266049060594, 119.9838882821124173 ) ) ;
#41824=CARTESIAN_POINT ( 'NONE',  ( 20.17806256124487874, -25.90288594722162330, -38.48045932952570070 ) ) ;
#41827=CARTESIAN_POINT ( 'NONE',  ( -36.09010194260303450, -60.00000000000000000, 47.44087383398635893 ) ) ;
#41830=CARTESIAN_POINT ( 'NONE',  ( -87.02599616935226834, -35.40601924051522076, 188.2192322684356895 ) ) ;
#41833=CARTESIAN_POINT ( 'NONE',  ( -7.056147190753457643, -29.03107994581888107, 28.71850030171957258 ) ) ;
#41837=CARTESIAN_POINT ( 'NONE',  ( -98.04235954153416799, -59.99999999999997868, 196.5000328139588532 ) ) ;
#41849=CARTESIAN_POINT ( 'NONE',  ( 106.4976671120242173, -30.00000000000003553, 137.1020467228335349 ) ) ;
#41870=CARTESIAN_POINT ( 'NONE',  ( 92.06880798540581168, -60.00000000000002842, 4.793930753321646421 ) ) ;
#41871=CARTESIAN_POINT ( 'NONE',  ( -82.63253876390992048, -60.00000000000011369, 201.7050754921980911 ) ) ;
#41872=CARTESIAN_POINT ( 'NONE',  ( 19.25484014596467830, -49.91514199782810124, 32.66260667748945679 ) ) ;
#41875=CARTESIAN_POINT ( 'NONE',  ( -40.48074807841378231, -46.43598188464789445, 40.68275167793495228 ) ) ;
#41878=CARTESIAN_POINT ( 'NONE',  ( -20.05453516056602581, -4.285714285714295357, 15.38541618194246929 ) ) ;
#41889=CARTESIAN_POINT ( 'NONE',  ( 75.22651015812265030, -30.00000000013189805, 158.5714180975027432 ) ) ;
#41894=CARTESIAN_POINT ( 'NONE',  ( 80.93729537171422805, -29.99999999999999645, 5.168379641639776700 ) ) ;
#41900=VERTEX_POINT ( 'NONE', #14274 ) ;
#41912=CARTESIAN_POINT ( 'NONE',  ( 67.25431336777386093, -38.33468234247306583, 122.2200866910623489 ) ) ;
#41928=DIRECTION ( 'NONE',  ( 1.224646799147353207E-16, 0.000000000000000000, -1.000000000000000000 ) ) ;
#41934=CARTESIAN_POINT ( 'NONE',  ( 84.54053991961795589, -53.81834405645398789, 189.9383315222177373 ) ) ;
#41938=CARTESIAN_POINT ( 'NONE',  ( 93.07376397780032562, -57.65571088614280626, -17.03660586601905180 ) ) ;
#41942=CARTESIAN_POINT ( 'NONE',  ( -81.57252369435565242, -30.00000000000000711, -8.038432599570381143 ) ) ;
#41963=CARTESIAN_POINT ( 'NONE',  ( -67.76098042632558816, -29.91089683381006026, -21.83674399635897956 ) ) ;
#41965=CARTESIAN_POINT ( 'NONE',  ( -64.12014087452101307, -21.77003452523452154, -21.74776922628243980 ) ) ;
#41972=CARTESIAN_POINT ( 'NONE',  ( -89.46289319159794218, -59.99999999999998579, -19.71868189584859721 ) ) ;
#41975=CARTESIAN_POINT ( 'NONE',  ( 101.6143094094037167, -60.22772872295755064, 194.6033318209078402 ) ) ;
#41994=CARTESIAN_POINT ( 'NONE',  ( 4.154708322984343386E-08, -57.67120202538960427, 41.61186700422869933 ) ) ;
#42000=CARTESIAN_POINT ( 'NONE',  ( -89.90470572912276737, -30.00000000000002842, -11.15078749779565825 ) ) ;
#42002=CARTESIAN_POINT ( 'NONE',  ( -51.62104046282875203, -29.11573342958205757, 49.92149681681622297 ) ) ;
#42005=CARTESIAN_POINT ( 'NONE',  ( -96.57186187874448535, -45.25305379375232206, 194.0755569586996216 ) ) ;
#42010=CARTESIAN_POINT ( 'NONE',  ( 103.6076551382766979, -38.41969712729913766, 198.6980867907736297 ) ) ;
#42015=CARTESIAN_POINT ( 'NONE',  ( 91.62648505185801184, -30.00000000000000711, 190.7393155417504715 ) ) ;
#42016=B_SPLINE_SURFACE_WITH_KNOTS ( 'NONE', 3, 3, ( 
 ( #55483, #73265, #64668, #98089 ),
 ( #40919, #7467, #15039, #48468 ),
 ( #71677, #90536, #97540, #24763 ),
 ( #89481, #98612, #32856, #73811 ),
 ( #106163, #56010, #57610, #23702 ),
 ( #15576, #47406, #24239, #40384 ),
 ( #14493, #23167, #72228, #72740 ),
 ( #16645, #8009, #65196, #6950 ),
 ( #57088, #81356, #47930, #6411 ),
 ( #88421, #49534, #38811, #90002 ),
 ( #16107, #64155, #31271, #80300 ),
 ( #48990, #104585, #105644, #97026 ),
 ( #31784, #88943, #106705, #30742 ),
 ( #63627, #39349, #96516, #22649 ),
 ( #105129, #10663, #84039, #91613 ),
 ( #100216, #41448, #60323, #34467 ),
 ( #41975, #26382, #68400, #2577 ),
 ( #59245, #75945, #25856, #35525 ),
 ( #67338, #92121, #17194, #100742 ),
 ( #83497, #26906, #76465, #59781 ),
 ( #52190, #101294, #51659, #2043 ),
 ( #17719, #84582, #43577, #27443 ),
 ( #33926, #414, #25301, #93196 ),
 ( #75406, #99140, #18266, #51121 ),
 ( #10142, #92656, #8543, #9597 ),
 ( #91087, #19362, #50068, #74340 ),
 ( #33381, #42509, #99686, #43056 ),
 ( #67856, #82976, #34988, #58712 ),
 ( #66256, #9070, #1503, #18817 ),
 ( #58159, #74859, #947, #66798 ),
 ( #50580, #69982, #61375, #78069 ),
 ( #28492, #102884, #3122, #60842 ),
 ( #93731, #19886, #29049, #77546 ),
 ( #45196, #12266, #4185, #36596 ),
 ( #52726, #37121, #3664, #85650 ),
 ( #85102, #69460, #61918, #11723 ),
 ( #94809, #86192, #78590, #94266 ),
 ( #20957, #53790, #53272, #86717 ),
 ( #12789, #45706, #11188, #44121 ),
 ( #77005, #36067, #68937, #101812 ),
 ( #44662, #27976, #102346, #20429 ),
 ( #101106, #10492, #1859, #9963 ),
 ( #92473, #27265, #43409, #84928 ),
 ( #1314, #60149, #34816, #93014 ),
 ( #50938, #35885, #75218, #74685 ),
 ( #35346, #19178, #67683, #18622 ),
 ( #52014, #42866, #59063, #100035 ),
 ( #33734, #83852, #93558, #84398 ),
 ( #2400, #100566, #91948, #59599 ),
 ( #17549, #26728, #91435, #51482 ),
 ( #50407, #68208, #11014, #26203 ),
 ( #76821, #76290, #75764, #43933 ),
 ( #767, #19706, #2930, #60671 ),
 ( #68763, #27800, #101643, #52542 ),
 ( #85462, #18079, #11547, #66611 ),
 ( #99491, #83320, #25669, #58532 ),
 ( #9412, #42328, #34275, #67151 ),
 ( #32910, #80894, #32382, #7005 ),
 ( #73322, #56614, #47987, #6471 ),
 ( #88479, #98665, #16701, #15629 ),
 ( #81413, #64212, #31330, #47463 ),
 ( #39925, #48522, #49049, #72281 ),
 ( #7524, #73867, #72797, #81946 ),
 ( #8069, #40442, #97082, #30796 ),
 ( #106762, #106219, #105701, #22705 ),
 ( #65254, #89538, #97600, #24296 ),
 ( #31844, #23225, #14554, #40979 ),
 ( #24817, #65787, #57669, #64726 ),
 ( #23766, #98144, #57145, #80356 ),
 ( #56065, #39403, #90592, #105184 ),
 ( #90058, #49592, #82500, #38867 ),
 ( #71734, #16162, #89006, #15100 ),
 ( #104644, #63682, #96570, #55542 ),
 ( #9124, #67910, #42034, #74916 ),
 ( #1000, #8601, #35046, #75995 ),
 ( #42562, #26435, #66853, #100797 ),
 ( #99742, #33982, #41503, #17780 ),
 ( #25912, #83033, #84630, #51173 ),
 ( #34522, #60376, #76522, #50633 ),
 ( #59838, #74391, #83551, #58768 ),
 ( #43107, #67391, #26957, #66312 ),
 ( #33438, #100273, #91666, #9651 ),
 ( #75464, #1557, #10717, #59300 ),
 ( #470, #35579, #18322, #68453 ),
 ( #2633, #99194, #92172, #84095 ),
 ( #10195, #2093, #92711, #101347 ),
 ( #18871, #51715, #43633, #27501 ),
 ( #93251, #19414, #52248, #58218 ),
 ( #25355, #91143, #17253, #50124 ),
 ( #93786, #11246, #95914, #95378 ),
 ( #45246, #13371, #94328, #21515 ),
 ( #52786, #87292, #28028, #38232 ),
 ( #61974, #12321, #21006, #3722 ),
 ( #19946, #79187, #12845, #53330 ),
 ( #54350, #11785, #46299, #94865 ),
 ( #53846, #5312, #86777, #71096 ),
 ( #30129, #103986, #102941, #45763 ),
 ( #63016, #78639, #4775, #44175 ),
 ( #85158, #29106, #102403, #85709 ),
 ( #77063, #86249, #69517, #44715 ),
 ( #77604, #3178, #70036, #22038 ),
 ( #37716, #36652, #28552, #62487 ),
 ( #36124, #70579, #103466, #68993 ),
 ( #29615, #101868, #61433, #60897 ),
 ( #20492, #78125, #4242, #37175 ),
 ( #75193, #66055, #6339, #90873 ),
 ( #72159, #39807, #55424, #104517 ),
 ( #71615, #80771, #16987, #30669 ),
 ( #33712, #39281, #105067, #74661 ),
 ( #79716, #6886, #31207, #47342 ),
 ( #22587, #64092, #58506, #96968 ),
 ( #50386, #91411, #219, #49865 ),
 ( #83299, #74135, #33183, #98932 ),
 ( #82771, #88879, #23103, #25092 ),
 ( #63557, #57949, #96450, #8874 ),
 ( #88357, #41778, #746, #66588 ),
 ( #17524, #99469, #55939, #25643 ),
 ( #87826, #1290, #9388, #42306 ),
 ( #34256, #67127, #100012, #54895 ),
 ( #13905, #14968, #46819, #5824 ),
 ( #38745, #14433, #80235, #47864 ),
 ( #1835, #10466, #59578, #68184 ),
 ( #20219, #101080, #19683, #27239 ),
 ( #60650, #43908, #35320, #100541 ),
 ( #75739, #85991, #3990, #2901 ),
 ( #68737, #51460, #18600, #34792 ),
 ( #93537, #60126, #35861, #36401 ),
 ( #61170, #101621, #44450, #27777 ),
 ( #52522, #94056, #85438, #77878 ),
 ( #67661, #10991, #43384, #26705 ),
 ( #92443, #92989, #76796, #53070 ),
 ( #84375, #59040, #91927, #19152 ),
 ( #76267, #12063, #2374, #18058 ),
 ( #69268, #9937, #51988, #11521 ),
 ( #84905, #3456, #77345, #36918 ),
 ( #102141, #28295, #44993, #69786 ),
 ( #26181, #42844, #50916, #83827 ),
 ( #61719, #94610, #78926, #14707 ),
 ( #87566, #39014, #86526, #103214 ),
 ( #29359, #62249, #79978, #70845 ),
 ( #104258, #63292, #6094, #70319 ),
 ( #54103, #22321, #103737, #87046 ) ),
 .UNSPECIFIED., .F., .F., .F.,
 ( 4, 3, 3, 3, 3, 3, 3, 3, 3, 3, 3, 3, 3, 3, 3, 3, 3, 3, 3, 3, 3, 3, 3, 3, 3, 3, 3, 3, 3, 3, 3, 3, 3, 3, 3, 3, 3, 3, 3, 3, 3, 3, 3, 3, 3, 3, 3, 4 ),
 ( 4, 4 ),
 ( 0.1961500227600059265, 0.1978441673325853079, 0.1995383119051646892, 0.2029266010503234796, 0.2046207456229028887, 0.2054678179091925794, 0.2063148901954822700, 0.2071619624817719607, 0.2080090347680616514, 0.2088561070543513420, 0.2097031793406410327, 0.2113973239132204140, 0.2130914684857998231, 0.2164797576309586136, 0.2181739022035379949, 0.2198680467761173762, 0.2232563359212761667, 0.2300329142115937198, 0.2368094925019113006, 0.2435860707922288537, 0.2503626490825464068, 0.2639158056631815130, 0.2774689622438166747, 0.2910221188244517809, 0.3045752754050868871, 0.3316815885663570995, 0.3452347451469922057, 0.3587879017276273119, 0.3655644800179448373, 0.3723410583082624181, 0.3791176365985799990, 0.3825059257437387616, 0.3858942148888975243, 0.3875883594614769057, 0.3892825040340562870, 0.3909766486066357238, 0.3926707931792151052, 0.3960590823243739234, 0.3977532268969533047, 0.3994473714695326860, 0.4011415160421120674, 0.4028356606146914487, 0.4062239497598502114, 0.4079180943324295927, 0.4096122389050089740, 0.4104593111912986925, 0.4113063834775884109, 0.4130005280501677922 ),
 ( 0.03879960281305409181, 0.7822234871750797236 ),
 .UNSPECIFIED. ) ;
#42024=CARTESIAN_POINT ( 'NONE',  ( 51.93105796537405894, -53.37078366791337913, 59.21816737527645813 ) ) ;
#42029=CARTESIAN_POINT ( 'NONE',  ( -101.2361249591687482, -38.35621429768038837, 95.68744428954927628 ) ) ;
#42032=CARTESIAN_POINT ( 'NONE',  ( 91.93880928415951814, -38.35394051711806895, 34.15909317860170091 ) ) ;
#42034=CARTESIAN_POINT ( 'NONE',  ( 92.71638314794412850, -45.28274863744896095, 87.13263043128905849 ) ) ;
#42035=CARTESIAN_POINT ( 'NONE',  ( 109.3513501059324255, -38.00000000000000000, 179.6549720493207190 ) ) ;
#42040=CARTESIAN_POINT ( 'NONE',  ( 76.36008957498899008, -59.99999999999998579, 188.3857483048130916 ) ) ;
#42045=CARTESIAN_POINT ( 'NONE',  ( 60.96321612378304877, -18.64603658371650852, 64.94373476075919882 ) ) ;
#42049=CARTESIAN_POINT ( 'NONE',  ( -60.77962921676822816, -30.00000000004004974, 94.17698026533876998 ) ) ;
#42058=CARTESIAN_POINT ( 'NONE',  ( 85.42082578164037443, -25.35066044882315950, 171.5601627925657340 ) ) ;
#42066=CARTESIAN_POINT ( 'NONE',  ( -14.96496930756238619, -24.06842715425924339, -38.53085418151248831 ) ) ;
#42071=CARTESIAN_POINT ( 'NONE',  ( 53.63744806657462760, -60.00000000000000000, 81.41419112139796255 ) ) ;
#42073=CARTESIAN_POINT ( 'NONE',  ( 11.01895070290840017, -14.02256158417551468, 31.84177124770781120 ) ) ;
#42076=CARTESIAN_POINT ( 'NONE',  ( -22.02381810701088227, -27.03152908169614577, 37.34294290578310438 ) ) ;
#42086=CARTESIAN_POINT ( 'NONE',  ( 28.41466101814540579, -34.58967673365405204, -31.03063672134422291 ) ) ;
#42097=CARTESIAN_POINT ( 'NONE',  ( -100.8778939643891022, -59.99999999999999289, 86.18389089348301013 ) ) ;
#42105=CARTESIAN_POINT ( 'NONE',  ( -86.03581629327824487, -18.41222013102441224, 166.1572250011447238 ) ) ;
#42120=CARTESIAN_POINT ( 'NONE',  ( 108.8020855619825653, -30.00000000000001066, 184.6883589252716433 ) ) ;
#42122=CARTESIAN_POINT ( 'NONE',  ( -105.3891558216856339, -14.21045842199431064, 188.2119682431835486 ) ) ;
#42123=CARTESIAN_POINT ( 'NONE',  ( -59.28942817012108435, -60.34107446338563108, 80.30105261389887517 ) ) ;
#42126=CARTESIAN_POINT ( 'NONE',  ( 99.44641300720719812, -60.00000000003898748, 63.07692230255130283 ) ) ;
#42128=CARTESIAN_POINT ( 'NONE',  ( 5.121475308325913467, -49.91563172172032381, 32.19864153987534650 ) ) ;
#42129=CARTESIAN_POINT ( 'NONE',  ( -102.4774247092255735, -37.82049968165720344, 163.3363480242135211 ) ) ;
#42135=CARTESIAN_POINT ( 'NONE',  ( -27.99608589347343823, -60.00000000000002132, 42.10196603562540218 ) ) ;
#42147=CARTESIAN_POINT ( 'NONE',  ( 105.0341561612351455, -60.00000000000000000, 150.3407643626507024 ) ) ;
#42149=CARTESIAN_POINT ( 'NONE',  ( -32.17252970384051736, -49.90654965793798681, 35.87652722567293040 ) ) ;
#42152=CARTESIAN_POINT ( 'NONE',  ( 44.27463941397954272, -56.79608921835394142, 47.30910395297117077 ) ) ;
#42158=CARTESIAN_POINT ( 'NONE',  ( -80.09466378707983836, -38.78899114093880485, 193.1579810679791365 ) ) ;
#42162=CARTESIAN_POINT ( 'NONE',  ( 31.81267353152397703, -59.99999999999999289, 37.51807302839154801 ) ) ;
#42168=CARTESIAN_POINT ( 'NONE',  ( 106.3905019650464396, -60.00000000000000711, 118.8348382975589885 ) ) ;
#42174=CARTESIAN_POINT ( 'NONE',  ( -97.88751494666014707, -30.00000000000000711, 190.6366788456940924 ) ) ;
#42188=CARTESIAN_POINT ( 'NONE',  ( 85.01890593301797594, -22.07538763286781602, 160.8954594108710126 ) ) ;
#42220=CARTESIAN_POINT ( 'NONE',  ( 107.5689571876914385, -57.67123018601353834, 113.8109351001579341 ) ) ;
#42226=CARTESIAN_POINT ( 'NONE',  ( -79.72788990572331613, -60.00000000000000711, 195.6396468098284345 ) ) ;
#42231=CARTESIAN_POINT ( 'NONE',  ( -83.99837553685419778, -46.55898069261829164, 184.5992319689315195 ) ) ;
#42237=CARTESIAN_POINT ( 'NONE',  ( -84.44893624074092031, -45.27054077215418459, -4.593890189075327868 ) ) ;
#42245=CARTESIAN_POINT ( 'NONE',  ( 1.425929562426998531, -60.00000000000000000, 41.99999999999999289 ) ) ;
#42247=CARTESIAN_POINT ( 'NONE',  ( 25.62974135805828979, -60.00000000000002132, -43.76006462505735328 ) ) ;
#42248=CARTESIAN_POINT ( 'NONE',  ( -68.29106402824945121, -42.96295712507508568, 98.34947639744338233 ) ) ;
#42250=CARTESIAN_POINT ( 'NONE',  ( 66.35352848486118660, -59.99999999999995737, 134.7740243497364645 ) ) ;
#42252=CARTESIAN_POINT ( 'NONE',  ( 114.0552712960643618, -57.67113080223169419, 166.1762645039309803 ) ) ;
#42265=CARTESIAN_POINT ( 'NONE',  ( 24.41571844174603356, -4.285714285714295357, -6.539732759932822326 ) ) ;
#42275=CARTESIAN_POINT ( 'NONE',  ( 33.29269151129017956, -53.36740787830309074, 37.05142291644975217 ) ) ;
#42290=CARTESIAN_POINT ( 'NONE',  ( 87.44554515300957576, -60.00000000000001421, -22.19960419083119874 ) ) ;
#42306=CARTESIAN_POINT ( 'NONE',  ( 83.23779423147905732, -37.82500537476536806, -5.216929617203576619 ) ) ;
#42317=CARTESIAN_POINT ( 'NONE',  ( 73.71512049594772975, -32.54216154817675033, 110.4876667498937479 ) ) ;
#42322=CARTESIAN_POINT ( 'NONE',  ( -87.28812347660355897, -57.67005709194983609, -25.16891244813248818 ) ) ;
#42328=CARTESIAN_POINT ( 'NONE',  ( 104.9727926896761545, -52.71702872129058903, 163.4617720493101274 ) ) ;
#42348=CARTESIAN_POINT ( 'NONE',  ( -84.86054889550955238, -30.00000000000000000, 169.0023419988235105 ) ) ;
#42353=CARTESIAN_POINT ( 'NONE',  ( 72.27211704050357355, -57.67031449669786269, 174.7872370686350223 ) ) ;
#42359=CARTESIAN_POINT ( 'NONE',  ( -38.95621058113182045, -60.00000000000000711, 50.68831809153677170 ) ) ;
#42363=CARTESIAN_POINT ( 'NONE',  ( -85.67725297654990868, -46.54890279682108911, 188.9755717729104845 ) ) ;
#42366=CARTESIAN_POINT ( 'NONE',  ( -8.026063634138786540, -22.06789999752070486, 27.56027737331870497 ) ) ;
#42379=CARTESIAN_POINT ( 'NONE',  ( 108.8241408383580193, -29.99999999999998224, 157.0475695436092565 ) ) ;
#42380=CARTESIAN_POINT ( 'NONE',  ( -80.88873720124335875, -49.92061108326104346, 166.5754553910332447 ) ) ;
#42400=CARTESIAN_POINT ( 'NONE',  ( 112.2509120385887655, -59.99999999999998579, 171.9075463260369361 ) ) ;
#42402=CARTESIAN_POINT ( 'NONE',  ( -76.85442806461188070, -14.21045842199432663, 149.6320961301125578 ) ) ;
#42403=CARTESIAN_POINT ( 'NONE',  ( 25.36379536694408543, -53.39101624669748958, 34.18967480269854065 ) ) ;
#42405=CARTESIAN_POINT ( 'NONE',  ( 83.30842096339651448, -37.99999999999997868, -6.385845932050894902 ) ) ;
#42407=CARTESIAN_POINT ( 'NONE',  ( -41.32835128475512221, -42.98145676455503406, 40.63877246576411295 ) ) ;
#42422=CARTESIAN_POINT ( 'NONE',  ( 80.93574383532660477, -30.00000000000004619, -12.06234416543689392 ) ) ;
#42427=CARTESIAN_POINT ( 'NONE',  ( 80.95826188147296421, -29.99999999999999645, 4.765542408442753342 ) ) ;
#42444=CARTESIAN_POINT ( 'NONE',  ( 64.38843716681957119, -38.33834301559899416, 111.1500240642540263 ) ) ;
#42447=VECTOR ( 'NONE', #20934, 1000.000000000000000 ) ;
#42464=CARTESIAN_POINT ( 'NONE',  ( 85.95818388483708361, -31.98290817333131031, 183.5996520270772976 ) ) ;
#42467=CARTESIAN_POINT ( 'NONE',  ( 94.58506785723692190, -57.65556415943643032, -10.24388704223456692 ) ) ;
#42471=CARTESIAN_POINT ( 'NONE',  ( -81.59120001829518287, -29.99999999999999645, -7.233253355891588576 ) ) ;
#42485=CARTESIAN_POINT ( 'NONE',  ( -71.17284327374473207, -38.00000000000000711, -21.88481141223168436 ) ) ;
#42488=CARTESIAN_POINT ( 'NONE',  ( 47.65524110203897123, -26.94530822553867822, -28.56564397192451565 ) ) ;
#42490=CARTESIAN_POINT ( 'NONE',  ( -22.80451126749514401, -49.91919812353112462, 33.12644376951882208 ) ) ;
#42496=CARTESIAN_POINT ( 'NONE',  ( -63.77693750556839802, -29.65005726330078062, -23.56308934115906339 ) ) ;
#42505=CARTESIAN_POINT ( 'NONE',  ( -81.52927428744742144, -59.99999999999999289, -27.00541479453063332 ) ) ;
#42509=CARTESIAN_POINT ( 'NONE',  ( 101.5045788610895130, -52.73011406855718519, 192.7905639140061567 ) ) ;
#42523=DIRECTION ( 'NONE',  ( -3.673940397442057649E-17, 0.000000000000000000, -1.000000000000000000 ) ) ;
#42524=CARTESIAN_POINT ( 'NONE',  ( -43.09316981551443604, -57.68566503113564892, 61.19926976090692960 ) ) ;
#42528=CARTESIAN_POINT ( 'NONE',  ( -89.80806051762600362, -30.00000000000005684, 26.19611557095339904 ) ) ;
#42530=CARTESIAN_POINT ( 'NONE',  ( -49.74770505191611392, -32.59159611762328268, 48.06925685492829814 ) ) ;
#42539=CARTESIAN_POINT ( 'NONE',  ( 104.4676181534481856, -38.40404783520960308, 197.9968809589744296 ) ) ;
#42544=CARTESIAN_POINT ( 'NONE',  ( 87.04597188044493805, -29.99999999999999645, 183.8866158033205522 ) ) ;
#42550=CARTESIAN_POINT ( 'NONE',  ( 52.96824733631504500, -22.17278515511078041, 49.74370119324648698 ) ) ;
#42556=CARTESIAN_POINT ( 'NONE',  ( -107.6814678764850015, -38.35635315369628984, 135.5461783006386725 ) ) ;
#42559=CARTESIAN_POINT ( 'NONE',  ( 108.2524867605244339, -38.35773384716500090, 192.2673139560903053 ) ) ;
#42562=CARTESIAN_POINT ( 'NONE',  ( 91.82244223932920590, -60.15085423987636659, 66.55118452451621636 ) ) ;
#42574=CARTESIAN_POINT ( 'NONE',  ( 60.56782644199743260, -25.59334256455847623, 67.17203146199634034 ) ) ;
#42583=CARTESIAN_POINT ( 'NONE',  ( -2.457247124321397802, -12.61078973057452224, 32.17714155548836175 ) ) ;
#42588=CARTESIAN_POINT ( 'NONE',  ( 86.25750675377733501, -18.23617246516705137, 169.8376886073401124 ) ) ;
#42599=CARTESIAN_POINT ( 'NONE',  ( -37.09836459488442273, -32.02632169008326457, -37.70790170121769336 ) ) ;
#42602=CARTESIAN_POINT ( 'NONE',  ( 44.74468937180378703, -60.00000000000000000, 60.10084534102561804 ) ) ;
#42604=CARTESIAN_POINT ( 'NONE',  ( 5.384078575322348570, -12.92596998821031029, 32.09213580060114879 ) ) ;
#42606=CARTESIAN_POINT ( 'NONE',  ( -13.36855599018907625, -21.80728118859962805, 35.71938858332402589 ) ) ;
#42620=CARTESIAN_POINT ( 'NONE',  ( 46.51529756520770320, -21.77006784196455413, -26.23302849808148807 ) ) ;
#42631=CARTESIAN_POINT ( 'NONE',  ( -104.1877734966528379, -60.00000000000001421, 105.5540295569807654 ) ) ;
#42640=CARTESIAN_POINT ( 'NONE',  ( -80.80365086073496173, -60.48046949481216217, 181.9398151766872616 ) ) ;
#42650=CARTESIAN_POINT ( 'NONE',  ( -72.95843482080444176, -52.66112468364584487, -23.75230364563115515 ) ) ;
#42655=( LENGTH_UNIT ( ) NAMED_UNIT ( * ) SI_UNIT ( .MILLI., .METRE. ) );
#42657=CARTESIAN_POINT ( 'NONE',  ( 101.8005042720997864, -59.99999999999995026, 77.51357286062189189 ) ) ;
#42658=CARTESIAN_POINT ( 'NONE',  ( -78.18420296597048491, -29.99999999999999645, 185.0796872551976548 ) ) ;
#42659=CARTESIAN_POINT ( 'NONE',  ( -60.17200676404426929, -32.54305267341962349, 69.40168963351582931 ) ) ;
#42663=CARTESIAN_POINT ( 'NONE',  ( 79.18410244169839984, -60.00000000000243006, -31.08583709693218822 ) ) ;
#42665=CARTESIAN_POINT ( 'NONE',  ( 4.019035380416646319, -32.51031334268923700, 29.30096715606009283 ) ) ;
#42666=CARTESIAN_POINT ( 'NONE',  ( -104.4037492068304260, -60.15596781628350698, 189.8437866221127024 ) ) ;
#42673=CARTESIAN_POINT ( 'NONE',  ( -32.39506591613324815, -60.00000000000001421, 44.41584490438672361 ) ) ;
#42679=CARTESIAN_POINT ( 'NONE',  ( 0.000000000000000000, -8.673617379884035472E-16, -17.01589776168603407 ) ) ;
#42685=CARTESIAN_POINT ( 'NONE',  ( 106.0683871028796688, -60.00000000000002132, 161.6282514473857077 ) ) ;
#42687=CARTESIAN_POINT ( 'NONE',  ( -30.31278797052050678, -25.59859917315953481, 30.73255412779541373 ) ) ;
#42689=CARTESIAN_POINT ( 'NONE',  ( 43.76121681010938858, -32.61635124531981234, 40.47551691563658238 ) ) ;
#42695=CARTESIAN_POINT ( 'NONE',  ( -80.28562564763434750, -38.80141483586817230, 193.4884166117294910 ) ) ;
#42697=CARTESIAN_POINT ( 'NONE',  ( 76.12557658274099026, -38.35599704320051018, -28.58424740099938077 ) ) ;
#42698=CARTESIAN_POINT ( 'NONE',  ( 16.69491137615832699, -59.99999999999998579, 34.10659378815499565 ) ) ;
#42705=CARTESIAN_POINT ( 'NONE',  ( 108.9327471971628540, -60.00000000000001421, 135.4986037201063596 ) ) ;
#42712=CARTESIAN_POINT ( 'NONE',  ( -100.2311398323353018, -29.99999999999999289, 184.5300451475501688 ) ) ;
#42727=CARTESIAN_POINT ( 'NONE',  ( 81.53240055878744386, -46.44585284538660375, 167.1415864390550041 ) ) ;
#42742=CARTESIAN_POINT ( 'NONE',  ( 87.29696987635691130, -42.74777952954144666, 190.3637657847306457 ) ) ;
#42758=ORIENTED_EDGE ( 'NONE', *, *, #75137, .F. ) ;
#42764=CARTESIAN_POINT ( 'NONE',  ( -76.02354287597104587, -59.99999999999999289, 187.0617520462423329 ) ) ;
#42770=CARTESIAN_POINT ( 'NONE',  ( -83.13823174912079139, -60.94556865090731179, 190.8875103384814054 ) ) ;
#42771=ORIENTED_EDGE ( 'NONE', *, *, #16415, .T. ) ;
#42776=CARTESIAN_POINT ( 'NONE',  ( -83.25012535261359403, -37.79396785790730462, -5.748279069099496041 ) ) ;
#42786=CARTESIAN_POINT ( 'NONE',  ( 77.10949051821226874, -30.00000000000007461, 176.8385238405566326 ) ) ;
#42788=CARTESIAN_POINT ( 'NONE',  ( -2.770043159915164477, -30.00000000000000355, -40.00000000000000000 ) ) ;
#42789=CARTESIAN_POINT ( 'NONE',  ( -69.71213741151544241, -22.11141246496202939, 91.06144798064602242 ) ) ;
#42791=CARTESIAN_POINT ( 'NONE',  ( 68.01663869669266660, -29.99999999999994316, 119.4502877181080862 ) ) ;
#42793=CARTESIAN_POINT ( 'NONE',  ( 36.87124630340465359, -59.99999999999258193, 51.79591773974985358 ) ) ;
#42799=ORIENTED_EDGE ( 'NONE', *, *, #16962, .F. ) ;
#42814=CARTESIAN_POINT ( 'NONE',  ( 32.86303424572704301, -39.49211861081180786, 34.27957772689813254 ) ) ;
#42830=CARTESIAN_POINT ( 'NONE',  ( 91.68327619457986088, -59.99999999999998579, -15.06735680088440965 ) ) ;
#42834=ORIENTED_EDGE ( 'NONE', *, *, #18821, .T. ) ;
#42844=CARTESIAN_POINT ( 'NONE',  ( 84.05867435070005911, -52.73583259645541688, -15.15229210315370167 ) ) ;
#42857=CARTESIAN_POINT ( 'NONE',  ( 73.37940478702553548, -60.31994814604785660, 129.0810991085878925 ) ) ;
#42863=CARTESIAN_POINT ( 'NONE',  ( -91.26204144827082132, -57.66323380191850845, -20.53964676755072105 ) ) ;
#42865=LINE ( 'NONE', #90895, #31702 ) ;
#42866=CARTESIAN_POINT ( 'NONE',  ( 104.5564995939975574, -52.71703362910472634, 183.8354400015944918 ) ) ;
#42881=DIRECTION ( 'NONE',  ( -0.000000000000000000, -1.000000000000000000, -0.000000000000000000 ) ) ;
#42884=CARTESIAN_POINT ( 'NONE',  ( -90.11912501425099720, -29.99999999999998934, 189.9661090405622019 ) ) ;
#42889=CARTESIAN_POINT ( 'NONE',  ( 71.47040382032911054, -57.67974827251811831, 166.7399757312242912 ) ) ;
#42896=CARTESIAN_POINT ( 'NONE',  ( 56.46206238374516317, -36.80706823966558972, -34.96395283256453723 ) ) ;
#42899=CARTESIAN_POINT ( 'NONE',  ( -47.26640296552387355, -60.00000000000000711, 65.37368657561523833 ) ) ;
#42903=CARTESIAN_POINT ( 'NONE',  ( -86.32370589824974161, -31.86242971515645905, 185.2303844998847637 ) ) ;
#42904=ORIENTED_EDGE ( 'NONE', *, *, #91324, .T. ) ;
#42906=CARTESIAN_POINT ( 'NONE',  ( -4.981455796065745290, -22.06768210089109772, 27.55828346185036892 ) ) ;
#42907=EDGE_CURVE ( 'NONE', #102908, #94469, #100154, .T. ) ;
#42923=CARTESIAN_POINT ( 'NONE',  ( 109.5128197388708031, -29.99999999999998934, 168.1051457340969932 ) ) ;
#42924=CARTESIAN_POINT ( 'NONE',  ( -78.52498540956069917, -60.31789553525856462, 160.5482536355575860 ) ) ;
#42945=CARTESIAN_POINT ( 'NONE',  ( 107.2890547746881822, -60.00000000000001421, 124.3984078847621788 ) ) ;
#42946=CARTESIAN_POINT ( 'NONE',  ( -78.68906450541477682, -14.21045842199436926, 170.0145061391070271 ) ) ;
#42947=CARTESIAN_POINT ( 'NONE',  ( 21.23040246788248808, -35.99409632868995601, 30.53834131912143945 ) ) ;
#42952=CARTESIAN_POINT ( 'NONE',  ( -42.93444061617797303, -36.07314741104291045, 40.55327348855406910 ) ) ;
#42956=CARTESIAN_POINT ( 'NONE',  ( -1.544427540536530316E-15, -4.285714285714290916, 25.22241582816893057 ) ) ;
#42966=CARTESIAN_POINT ( 'NONE',  ( 80.79101083364855640, -30.00000000000003553, 8.603092420626881065 ) ) ;
#42971=CARTESIAN_POINT ( 'NONE',  ( 83.28443596042880870, -29.99999999999998934, 45.16978209542076428 ) ) ;
#42989=CARTESIAN_POINT ( 'NONE',  ( 75.60688728915584988, -38.35697057576400937, 175.1550484948807593 ) ) ;
#43011=CARTESIAN_POINT ( 'NONE',  ( 86.02951077547139391, -28.36966621159877278, 182.1157798530540504 ) ) ;
#43019=CARTESIAN_POINT ( 'NONE',  ( -90.04170925992697505, -29.99999999999999645, 88.73563477756640339 ) ) ;
#43028=CARTESIAN_POINT ( 'NONE',  ( -7.716871247394699651, -19.87863916820204224, 27.19415443154595025 ) ) ;
#43031=CARTESIAN_POINT ( 'NONE',  ( -59.77583462350965959, -37.36469198411606385, -25.82931845235342294 ) ) ;
#43033=CARTESIAN_POINT ( 'NONE',  ( 62.51601690671169820, -29.54383159792558189, -24.06554947217484752 ) ) ;
#43035=CARTESIAN_POINT ( 'NONE',  ( -23.24060281120672755, -25.55958343567869306, 29.06070736075156447 ) ) ;
#43039=CARTESIAN_POINT ( 'NONE',  ( -10.00000000000000178, -15.00000000000000000, -9.999999999999998224 ) ) ;
#43041=CARTESIAN_POINT ( 'NONE',  ( -67.84377369674911051, -29.91451005171677124, -21.79787842944304188 ) ) ;
#43044=CARTESIAN_POINT ( 'NONE',  ( -70.85373708857285635, -60.22816841820291245, -26.05913268935715621 ) ) ;
#43056=CARTESIAN_POINT ( 'NONE',  ( 99.29975701822439760, -37.82025374434009279, 191.5887330688091197 ) ) ;
#43058=CARTESIAN_POINT ( 'NONE',  ( 3.156890235121763588, -18.90203136034843823, 27.03526591455209882 ) ) ;
#43070=CARTESIAN_POINT ( 'NONE',  ( -71.40526007946631637, -57.68007955256489083, 166.0300312729133623 ) ) ;
#43074=DIRECTION ( 'NONE',  ( 0.000000000000000000, -1.000000000000000000, 0.000000000000000000 ) ) ;
#43075=CARTESIAN_POINT ( 'NONE',  ( -94.21206122632280255, -59.99999999999995737, 9.571777650087724965 ) ) ;
#43078=CARTESIAN_POINT ( 'NONE',  ( -49.98687195071457978, -49.90673118800283703, 54.21811667533064139 ) ) ;
#43081=CARTESIAN_POINT ( 'NONE',  ( -95.75100734234322886, -52.81753470501251257, 195.4603346401156045 ) ) ;
#43087=CARTESIAN_POINT ( 'NONE',  ( 75.23893846245226769, -38.34369258312232631, 171.8379571195157496 ) ) ;
#43092=CARTESIAN_POINT ( 'NONE',  ( 91.70700314268253805, -30.00000000000000355, 190.7673246573001506 ) ) ;
#43098=CARTESIAN_POINT ( 'NONE',  ( 50.93739997076023229, -53.36856766373855265, 57.23326497631002496 ) ) ;
#43103=CARTESIAN_POINT ( 'NONE',  ( -85.85159476380036381, -38.36072881479658747, -22.04725531320800869 ) ) ;
#43105=CARTESIAN_POINT ( 'NONE',  ( 110.3745291010071128, -38.35605052085741562, 158.9613384561761222 ) ) ;
#43107=CARTESIAN_POINT ( 'NONE',  ( 88.26228835492393898, -60.14943515912076322, 41.81636722779243343 ) ) ;
#43116=CARTESIAN_POINT ( 'NONE',  ( 59.29040008912359383, -60.33413133801057171, 80.30034514049579286 ) ) ;
#43127=CARTESIAN_POINT ( 'NONE',  ( 37.66449544891585788, -25.29918219771590415, 34.61108901143979466 ) ) ;
#43132=CARTESIAN_POINT ( 'NONE',  ( 83.88228782411839290, -42.97938930064833585, 181.2417429171390211 ) ) ;
#43144=CARTESIAN_POINT ( 'NONE',  ( -17.45596745549606510, -24.91941539423173069, -38.51372130895111212 ) ) ;
#43147=CARTESIAN_POINT ( 'NONE',  ( 42.77053763280976284, -60.00000000000001421, 56.45409730004357840 ) ) ;
#43148=CARTESIAN_POINT ( 'NONE',  ( 27.84859843015495073, -30.99258014239854830, 39.44613863972335821 ) ) ;
#43150=CARTESIAN_POINT ( 'NONE',  ( 22.35000867505471334, -18.10629870634155125, 31.47582638679958933 ) ) ;
#43151=CARTESIAN_POINT ( 'NONE',  ( -30.59712220650429870, -32.84545843662240827, 40.92599255917917844 ) ) ;
#43165=CARTESIAN_POINT ( 'NONE',  ( 52.54835918530902461, -21.76994055301013375, -25.01027266287611539 ) ) ;
#43175=CARTESIAN_POINT ( 'NONE',  ( -100.8861591709492984, -59.99999999999999289, 86.23238314539901239 ) ) ;
#43181=CARTESIAN_POINT ( 'NONE',  ( -83.79266685549821148, -35.97651932943645647, 171.8138913702506443 ) ) ;
#43197=CARTESIAN_POINT ( 'NONE',  ( 98.75715858346298148, -14.21045842199428222, 105.0403869495405331 ) ) ;
#43198=CARTESIAN_POINT ( 'NONE',  ( -77.87378252178784521, -14.21045842199420228, 157.7502635463301317 ) ) ;
#43200=CARTESIAN_POINT ( 'NONE',  ( -60.71664721387831776, -36.01558240415723589, 72.46505467556380609 ) ) ;
#43204=CARTESIAN_POINT ( 'NONE',  ( -103.7500182398446924, -60.16060988300274914, 191.4285943361837781 ) ) ;
#43205=( NAMED_UNIT ( * ) SI_UNIT ( $, .STERADIAN. ) SOLID_ANGLE_UNIT ( ) );
#43211=CARTESIAN_POINT ( 'NONE',  ( -73.36908011962465537, -59.99999999999998579, 165.8270234517137567 ) ) ;
#43218=CARTESIAN_POINT ( 'NONE',  ( 1.113195845631288261, -0.000000000000000000, -17.01584901092319058 ) ) ;
#43219=CARTESIAN_POINT ( 'NONE',  ( 84.20870358801302302, -52.67313341312099340, -14.85892719433468123 ) ) ;
#43225=CARTESIAN_POINT ( 'NONE',  ( -31.24728166932320050, -56.85591377269362567, 36.70157539563093962 ) ) ;
#43228=CARTESIAN_POINT ( 'NONE',  ( 44.43361187226474129, -22.24703502879481221, 38.44165449124453460 ) ) ;
#43233=CARTESIAN_POINT ( 'NONE',  ( -85.87617615289288153, -38.64955979039224587, 198.9927000956684537 ) ) ;
#43236=CARTESIAN_POINT ( 'NONE',  ( 31.33832728500611609, -60.00000000000000711, 37.30313604653941439 ) ) ;
#43243=CARTESIAN_POINT ( 'NONE',  ( 101.9353215183635939, -60.00000000000000000, 92.36758675646822780 ) ) ;
#43262=CARTESIAN_POINT ( 'NONE',  ( 82.61890608584070606, -39.49166873427294178, 166.2326186401752466 ) ) ;
#43264=ORIENTED_EDGE ( 'NONE', *, *, #22220, .F. ) ;
#43302=CARTESIAN_POINT ( 'NONE',  ( -77.02578345189107267, -59.99999999999998579, 190.5239158944286828 ) ) ;
#43308=CARTESIAN_POINT ( 'NONE',  ( -86.40597577314841260, -17.76547941803659114, 175.7363829004051468 ) ) ;
#43314=CARTESIAN_POINT ( 'NONE',  ( -82.76973596104315334, -37.82754287118251568, 2.360074632004959927 ) ) ;
#43323=CARTESIAN_POINT ( 'NONE',  ( 73.20681906048392307, -14.21045842199435150, 129.4971587772804185 ) ) ;
#43325=CARTESIAN_POINT ( 'NONE',  ( -88.18129031808710749, -59.99999999999997158, -24.85705915495453411 ) ) ;
#43327=CARTESIAN_POINT ( 'NONE',  ( -64.89877610984821388, -56.86748303091376044, 95.13561503513990658 ) ) ;
#43329=CARTESIAN_POINT ( 'NONE',  ( 74.83543306973328413, -14.21045842199438347, 137.5190812362815791 ) ) ;
#43331=CARTESIAN_POINT ( 'NONE',  ( 69.18913803857314804, -57.67117611319257975, -34.94735017757600559 ) ) ;
#43341=CARTESIAN_POINT ( 'NONE',  ( -19.45294693897874794, -59.99999999999013767, 42.51175855280396831 ) ) ;
#43354=CARTESIAN_POINT ( 'NONE',  ( 31.27512390054598157, -32.54638041113430802, 32.34197377954890840 ) ) ;
#43355=CARTESIAN_POINT ( 'NONE',  ( 22.03900363279368690, -4.285714285714963268, -12.70248734011530622 ) ) ;
#43367=CARTESIAN_POINT ( 'NONE',  ( 90.09714635153191864, -59.99999999999999289, -18.66843320900434122 ) ) ;
#43377=CARTESIAN_POINT ( 'NONE',  ( -107.1906752169646353, -29.99999999999498357, 191.1798405353558792 ) ) ;
#43384=CARTESIAN_POINT ( 'NONE',  ( 83.75530807959195556, -45.27724494717428172, -12.71844083205649056 ) ) ;
#43393=FILL_AREA_STYLE_COLOUR ( '', #58814 ) ;
#43397=CARTESIAN_POINT ( 'NONE',  ( 75.09227317690647396, -60.31491160002002516, 137.4141434509855628 ) ) ;
#43403=CARTESIAN_POINT ( 'NONE',  ( -94.41147650277389403, -57.65372982601817853, -11.88746169270405773 ) ) ;
#43409=CARTESIAN_POINT ( 'NONE',  ( 102.8682207463923532, -45.28272216667533456, 186.0846881397096695 ) ) ;
#43424=CARTESIAN_POINT ( 'NONE',  ( -86.31772595132530057, -30.00000000000000355, 180.5339520493327825 ) ) ;
#43428=CARTESIAN_POINT ( 'NONE',  ( 73.12522785550909532, -57.64690656528826906, 182.1381851100867664 ) ) ;
#43433=CARTESIAN_POINT ( 'NONE',  ( 66.27523070486898860, -37.98760907505894124, -32.42822486897702561 ) ) ;
#43436=CARTESIAN_POINT ( 'NONE',  ( -35.28971009319081986, -60.00000000000002132, 46.67999809849258952 ) ) ;
#43439=CARTESIAN_POINT ( 'NONE',  ( -86.67077660397114869, -39.12965989546195544, 188.4535426357679455 ) ) ;
#43443=CARTESIAN_POINT ( 'NONE',  ( -5.103907831117815874, -46.43917523267403169, 31.61932201913767670 ) ) ;
#43460=CARTESIAN_POINT ( 'NONE',  ( 103.2299700508879567, -60.00000000000004974, 85.94867762990566007 ) ) ;
#43461=CARTESIAN_POINT ( 'NONE',  ( -80.77687318190224630, -42.97080845458604870, 155.3688440231170489 ) ) ;
#43465=CARTESIAN_POINT ( 'NONE',  ( 29.18545435546700162, -57.68205234359119515, 44.83568442682894784 ) ) ;
#43474=ADVANCED_BREP_SHAPE_REPRESENTATION ( '', ( #16991, #10728 ), #103758 ) ;
#43479=CARTESIAN_POINT ( 'NONE',  ( 74.96611493089018552, -59.99999999999998579, -30.51875920910361728 ) ) ;
#43481=CARTESIAN_POINT ( 'NONE',  ( -105.0772696006729632, -59.99999999999994316, 202.2127603465211223 ) ) ;
#43482=CARTESIAN_POINT ( 'NONE',  ( 18.71245558089175276, -25.55128019488360636, 28.53050335101116275 ) ) ;
#43486=CARTESIAN_POINT ( 'NONE',  ( -43.31012496879380080, -49.89329425690212361, 44.39323085342611819 ) ) ;
#43490=CARTESIAN_POINT ( 'NONE',  ( -89.99999999999997158, -60.00000000000000000, 196.0238439516549818 ) ) ;
#43499=CARTESIAN_POINT ( 'NONE',  ( 96.26263212673806891, -30.00000000000000711, 191.2551900954179587 ) ) ;
#43502=CARTESIAN_POINT ( 'NONE',  ( 81.76910224116089410, -30.00000000000000000, 31.60432335422153116 ) ) ;
#43521=CARTESIAN_POINT ( 'NONE',  ( 75.64534851151876182, -38.35868239334193674, 175.4885248428145701 ) ) ;
#43542=CARTESIAN_POINT ( 'NONE',  ( 85.44540022114718170, -61.06638023725951570, 193.8744620643309418 ) ) ;
#43550=CARTESIAN_POINT ( 'NONE',  ( -83.18161732247874340, -29.99999999999999645, 44.35520410614308418 ) ) ;
#43557=CARTESIAN_POINT ( 'NONE',  ( -45.06251741407306355, -36.90970505544751035, 43.04236430708314742 ) ) ;
#43559=CARTESIAN_POINT ( 'NONE',  ( 35.98291722399694237, -23.65727476560045872, -31.11900096256992398 ) ) ;
#43560=CARTESIAN_POINT ( 'NONE',  ( -24.64341543703087467, -32.52149348492427094, 30.48647817142265737 ) ) ;
#43564=CARTESIAN_POINT ( 'NONE',  ( -16.89468671705794023, -46.43925381171047917, 31.87895912059618553 ) ) ;
#43565=CARTESIAN_POINT ( 'NONE',  ( -55.56355992248217035, -28.58787366841717414, -26.41023078683522129 ) ) ;
#43574=CARTESIAN_POINT ( 'NONE',  ( -8.421684505501604079, -59.99999999999999289, -42.47678725903364949 ) ) ;
#43577=CARTESIAN_POINT ( 'NONE',  ( 99.99568154413580601, -45.27326971109869902, 192.6082355761231213 ) ) ;
#43579=CARTESIAN_POINT ( 'NONE',  ( 12.58304801162219810, -21.69704017138143115, 27.55869761091397763 ) ) ;
#43594=CARTESIAN_POINT ( 'NONE',  ( -105.0872854236518208, -59.99999999972659737, 96.83056509434175041 ) ) ;
#43598=CARTESIAN_POINT ( 'NONE',  ( -87.24749885984873288, -14.21045842199425024, -0.3946065656837255964 ) ) ;
#43600=CARTESIAN_POINT ( 'NONE',  ( -50.06693045002293019, -46.44288008262338963, 53.18188324199074657 ) ) ;
#43609=CARTESIAN_POINT ( 'NONE',  ( 89.24963295654325179, -29.99999999997994138, 8.815628760632554517 ) ) ;
#43615=CARTESIAN_POINT ( 'NONE',  ( 87.20282465662560867, -29.99999999999999645, 184.4716329640986885 ) ) ;
#43621=CARTESIAN_POINT ( 'NONE',  ( 51.81251031740741553, -56.83722578688029614, 60.27040154863821897 ) ) ;
#43627=CARTESIAN_POINT ( 'NONE',  ( -90.41562289390209628, -38.40191935066286533, -14.83428885377948347 ) ) ;
#43631=CARTESIAN_POINT ( 'NONE',  ( 106.6780022803428380, -38.36736985975626624, 195.3823964213139561 ) ) ;
#43633=CARTESIAN_POINT ( 'NONE',  ( 84.22497889915220526, -45.28298033193925676, 26.08978801077915932 ) ) ;
#43634=PLANE ( 'NONE',  #104959 ) ;
#43636=PRESENTATION_STYLE_ASSIGNMENT (( #51718 ) ) ;
#43651=FILL_AREA_STYLE_COLOUR ( '', #31311 ) ;
#43655=CARTESIAN_POINT ( 'NONE',  ( 84.35218974313944784, -35.91427077666032375, 176.6979861380962404 ) ) ;
#43660=CARTESIAN_POINT ( 'NONE',  ( -91.82262176611270377, -60.15457395765744053, 66.54832966913770065 ) ) ;
#43664=CARTESIAN_POINT ( 'NONE',  ( -14.20331398951563173, -23.82509769195230476, -38.53390941360537170 ) ) ;
#43667=CARTESIAN_POINT ( 'NONE',  ( 41.54751723293285437, -60.00000000000000711, 54.42831949363168320 ) ) ;
#43669=CARTESIAN_POINT ( 'NONE',  ( 32.03079550275963783, -33.76634389418148174, 41.86185369695325420 ) ) ;
#43671=CARTESIAN_POINT ( 'NONE',  ( 26.78471285382464018, -20.14333726486478682, 31.71525114976481063 ) ) ;
#43672=CARTESIAN_POINT ( 'NONE',  ( -38.38809213244076801, -37.07590732314030646, 47.79844471891385638 ) ) ;
#43687=CARTESIAN_POINT ( 'NONE',  ( 12.44550202702694364, -21.77031843812234868, -30.18240907129194994 ) ) ;
#43697=CARTESIAN_POINT ( 'NONE',  ( -91.86617004484983795, -60.00000000000000000, 10.83445478909512261 ) ) ;
#43705=CARTESIAN_POINT ( 'NONE',  ( -84.69258335735655407, -28.96439599382944508, 169.4305326073071853 ) ) ;
#43716=CARTESIAN_POINT ( 'NONE',  ( -113.3221076330293471, -57.67118219814813784, 155.4948299128208191 ) ) ;
#43722=CARTESIAN_POINT ( 'NONE',  ( 103.2299700508879567, -60.00000000000004974, 85.94867762990566007 ) ) ;
#43723=CARTESIAN_POINT ( 'NONE',  ( -86.32002947858198638, -29.99999999999988987, 198.0868106477030892 ) ) ;
#43724=CARTESIAN_POINT ( 'NONE',  ( -57.41802865368278930, -39.49559850351909773, 65.76057902791269782 ) ) ;
#43729=CARTESIAN_POINT ( 'NONE',  ( -104.0809943399287505, -60.15808651304565302, 190.6463388486238557 ) ) ;
#43735=AXIS2_PLACEMENT_3D ( 'NONE', #93855, #4844, #28623 ) ;
#43737=CARTESIAN_POINT ( 'NONE',  ( -81.74462499157380080, -60.00000000000002132, 197.8260547546231010 ) ) ;
#43743=CARTESIAN_POINT ( 'NONE',  ( 15.29468310206912740, -0.000000000000000000, -7.540179673762702706 ) ) ;
#43748=CARTESIAN_POINT ( 'NONE',  ( -30.40563286230810647, -39.48936947416332544, 33.27199808670961545 ) ) ;
#43750=CARTESIAN_POINT ( 'NONE',  ( 43.03101095780436935, -39.52523172002285889, 41.51020378114284881 ) ) ;
#43753=CARTESIAN_POINT ( 'NONE',  ( -89.68772280753135817, -38.52026044421657502, 200.4884354424789308 ) ) ;
#43755=CARTESIAN_POINT ( 'NONE',  ( 84.57469743677759766, -38.35847120622327822, -23.21952487094015538 ) ) ;
#43757=CARTESIAN_POINT ( 'NONE',  ( 75.38526191690708345, -59.99999999999995737, 138.7226225906020431 ) ) ;
#43764=CARTESIAN_POINT ( 'NONE',  ( 111.3354282251981573, -60.00000000000002132, 155.4017638814755173 ) ) ;
#43776=CARTESIAN_POINT ( 'NONE',  ( -68.45687734878008257, -38.33354253709327963, 127.1540152885862796 ) ) ;
#43782=EDGE_CURVE ( 'NONE', #91474, #74273, #23752, .T. ) ;
#43786=CARTESIAN_POINT ( 'NONE',  ( 82.78941698165385787, -32.55276419480425432, 157.1437384287463317 ) ) ;
#43798=PLANE ( 'NONE',  #44059 ) ;
#43800=CARTESIAN_POINT ( 'NONE',  ( 87.47287999732215269, -39.05335706277111285, 189.8424516346250073 ) ) ;
#43824=CARTESIAN_POINT ( 'NONE',  ( -107.2784424374574570, -59.99999999999998579, 196.7685047584830045 ) ) ;
#43830=CARTESIAN_POINT ( 'NONE',  ( -85.62023293286473802, -28.60697929939942696, 178.8582336157557791 ) ) ;
#43839=CARTESIAN_POINT ( 'NONE',  ( -84.22133707121940915, -45.27027536912773797, -0.5858364418087087522 ) ) ;
#43846=CARTESIAN_POINT ( 'NONE',  ( 74.93436731647082638, -29.99999999999996803, 156.1785850212263824 ) ) ;
#43848=CARTESIAN_POINT ( 'NONE',  ( -88.04114847129865495, -29.99999999999995026, -17.07571352811936194 ) ) ;
#43849=CARTESIAN_POINT ( 'NONE',  ( -66.61405105253464853, -49.91421082191510550, 96.76620431498515984 ) ) ;
#43851=CARTESIAN_POINT ( 'NONE',  ( 92.04793376076307254, -60.00000000000014211, 204.8851669578057795 ) ) ;
#43853=CARTESIAN_POINT ( 'NONE',  ( 79.00424233902616322, -57.67119432125786460, -30.74184640794639023 ) ) ;
#43864=CARTESIAN_POINT ( 'NONE',  ( -72.62418736021129462, -60.00000000002444978, 181.5552947579788849 ) ) ;
#43876=CARTESIAN_POINT ( 'NONE',  ( 32.98111995772554650, -53.36881808543628836, 36.89039439871834247 ) ) ;
#43891=CARTESIAN_POINT ( 'NONE',  ( 92.57516331644632146, -60.00000000000002132, -2.390279356456004756 ) ) ;
#43902=CARTESIAN_POINT ( 'NONE',  ( -109.0742547107064269, -29.99999999999665334, 182.6719831179964331 ) ) ;
#43908=CARTESIAN_POINT ( 'NONE',  ( 85.58715377439223460, -52.75714875827612360, -10.05349147758953698 ) ) ;
#43921=CARTESIAN_POINT ( 'NONE',  ( 77.26947396445019933, -25.60795510370099137, 119.8375088053420257 ) ) ;
#43927=CARTESIAN_POINT ( 'NONE',  ( -86.45135651325685444, -57.58031178088597812, 202.9040356603995008 ) ) ;
#43933=CARTESIAN_POINT ( 'NONE',  ( 102.7636524767473674, -37.84830847812925469, 174.7740013299970485 ) ) ;
#43938=CARTESIAN_POINT ( 'NONE',  ( -51.38767806049178688, -29.89936270055883938, 48.97532232888291759 ) ) ;
#43946=CARTESIAN_POINT ( 'NONE',  ( 0.000000000000000000, -30.00000000000000000, 0.000000000000000000 ) ) ;
#43949=CARTESIAN_POINT ( 'NONE',  ( -84.88742408119121308, -30.00000000000000000, 169.2579586347718532 ) ) ;
#43955=CARTESIAN_POINT ( 'NONE',  ( 75.55219586201926063, -57.55829115879463131, 192.1307904649139005 ) ) ;
#43958=DIRECTION ( 'NONE',  ( -0.000000000000000000, -1.000000000000000000, -0.000000000000000000 ) ) ;
#43959=CARTESIAN_POINT ( 'NONE',  ( 48.67663294687506692, -35.26610979276345148, -36.36738862548124729 ) ) ;
#43961=CARTESIAN_POINT ( 'NONE',  ( -43.45804985508113560, -60.00000000000002132, 57.68673898691244517 ) ) ;
#43967=CARTESIAN_POINT ( 'NONE',  ( -86.85197155073301190, -31.73829086694582458, 186.9893845558580381 ) ) ;
#43970=CARTESIAN_POINT ( 'NONE',  ( -2.000864354225422748, -32.51271004180395607, 29.30614571473786256 ) ) ;
#43985=CARTESIAN_POINT ( 'NONE',  ( 89.06755727843562909, -14.21045842199420939, 44.45805076957166335 ) ) ;
#43986=CARTESIAN_POINT ( 'NONE',  ( -83.77364050599970824, -22.14433376563224343, 150.6908921694812591 ) ) ;
#43990=CARTESIAN_POINT ( 'NONE',  ( 28.89319199617951739, -57.68130367911507506, 44.69050114560476317 ) ) ;
#44007=B_SPLINE_CURVE_WITH_KNOTS ( 'NONE', 3,
 ( #16552, #31180, #64065, #106615, #6857, #32765 ),
 .UNSPECIFIED., .F., .F.,
 ( 4, 2, 4 ),
 ( 0.4253311071485821881, 0.4347571321485946827, 0.4441831571486071217 ),
 .UNSPECIFIED. ) ;
#44010=CARTESIAN_POINT ( 'NONE',  ( 79.93009750732559837, -59.99999999999998579, -27.98265100805786787 ) ) ;
#44011=CARTESIAN_POINT ( 'NONE',  ( -100.0713701506240767, -14.21045842199444209, 196.7486061734171585 ) ) ;
#44012=CARTESIAN_POINT ( 'NONE',  ( 20.41555138587536788, -49.91487051538342001, 32.77847263903716879 ) ) ;
#44014=CARTESIAN_POINT ( 'NONE',  ( -34.21665458544683247, -53.36932329917436846, 37.55107279959798205 ) ) ;
#44017=DIRECTION ( 'NONE',  ( 0.000000000000000000, 1.000000000000000000, 0.000000000000000000 ) ) ;
#44027=CARTESIAN_POINT ( 'NONE',  ( 93.61383638276589636, -29.99999999999993960, 191.2346839720568710 ) ) ;
#44031=CARTESIAN_POINT ( 'NONE',  ( 80.76937127641447489, -30.00000000000000000, 10.56350537290334657 ) ) ;
#44049=CARTESIAN_POINT ( 'NONE',  ( 71.09600594220485448, -38.32840958359373218, 140.6164948842156548 ) ) ;
#44059=AXIS2_PLACEMENT_3D ( 'NONE', #76693, #90767, #82667 ) ;
#44076=CARTESIAN_POINT ( 'NONE',  ( 85.80726315722955633, -39.24464598724059528, 186.3863758982486729 ) ) ;
#44080=CARTESIAN_POINT ( 'NONE',  ( 74.80548469941292922, -57.67118132480599968, -32.73163803306931641 ) ) ;
#44081=CARTESIAN_POINT ( 'NONE',  ( 42.20625837426413085, -25.53023488050030210, -29.84183546610569593 ) ) ;
#44086=CARTESIAN_POINT ( 'NONE',  ( -86.45485542442474980, -30.00000000000000000, 67.08978895544929344 ) ) ;
#44089=CARTESIAN_POINT ( 'NONE',  ( 20.50185113829394012, -57.67216918497611999, 42.27920450415231102 ) ) ;
#44093=CARTESIAN_POINT ( 'NONE',  ( -33.08593021725691585, -32.09165124679379488, 32.96944937447516111 ) ) ;
#44097=CARTESIAN_POINT ( 'NONE',  ( 21.54459453844334149, -19.00312104139907277, -33.51129274704846495 ) ) ;
#44099=CARTESIAN_POINT ( 'NONE',  ( -23.79206963583671097, -42.95898574611043585, 32.10571046793408811 ) ) ;
#44103=CARTESIAN_POINT ( 'NONE',  ( -17.88331992309682761, -39.47666801934411041, 30.78506762338722069 ) ) ;
#44121=CARTESIAN_POINT ( 'NONE',  ( 101.0742260107603698, -37.84808717716843063, 188.0777966372289995 ) ) ;
#44137=CARTESIAN_POINT ( 'NONE',  ( -94.99329613063325439, -60.00000000000000000, -3.093086405557472496 ) ) ;
#44141=CARTESIAN_POINT ( 'NONE',  ( -80.19882167783929106, -30.00000000000005684, -24.77908391697505053 ) ) ;
#44142=CARTESIAN_POINT ( 'NONE',  ( -48.40568706220404493, -60.28780075344402434, 54.82589591225594461 ) ) ;
#44152=CARTESIAN_POINT ( 'NONE',  ( 64.82975887493691403, -38.33849854337827878, 111.7912813277601032 ) ) ;
#44158=CARTESIAN_POINT ( 'NONE',  ( 88.54308360411496892, -30.00000000000001066, 187.9651850611236341 ) ) ;
#44164=CARTESIAN_POINT ( 'NONE',  ( 53.91603561383729470, -49.90521162105653730, 62.12114408794506204 ) ) ;
#44170=CARTESIAN_POINT ( 'NONE',  ( -84.49786633764185240, -38.35845268396171548, -23.28952271651921890 ) ) ;
#44173=CARTESIAN_POINT ( 'NONE',  ( 110.3737722850151073, -38.35605049689843327, 158.9517897806462656 ) ) ;
#44175=CARTESIAN_POINT ( 'NONE',  ( 82.46918239245667337, -37.86090144012435843, 8.727031703878875391 ) ) ;
#44196=SURFACE_STYLE_USAGE ( .BOTH. , #10737 ) ;
#44201=CARTESIAN_POINT ( 'NONE',  ( 82.83931105584079546, -57.25424869743982725, 188.0379144665223521 ) ) ;
#44203=DIRECTION ( 'NONE',  ( 8.673617379884035472E-17, 0.000000000000000000, 1.000000000000000000 ) ) ;
#44206=CARTESIAN_POINT ( 'NONE',  ( -92.71327091926096386, -45.26532570964787539, 87.13247471504898556 ) ) ;
#44211=CARTESIAN_POINT ( 'NONE',  ( -35.95030584110901373, -31.65002092866515326, -37.80030597103479550 ) ) ;
#44213=CARTESIAN_POINT ( 'NONE',  ( 36.43960955224464016, -60.00000000000000000, 47.79037295421704812 ) ) ;
#44214=CARTESIAN_POINT ( 'NONE',  ( 31.26640680753876111, -33.27990713294830272, 41.34742143513260970 ) ) ;
#44215=CARTESIAN_POINT ( 'NONE',  ( 29.62811787866498037, -21.49980114393428821, 32.08485897227100736 ) ) ;
#44222=ORIENTED_EDGE ( 'NONE', *, *, #102203, .F. ) ;
#44232=CARTESIAN_POINT ( 'NONE',  ( -15.57536127888151078, -21.77027137267931778, -29.99990132288678879 ) ) ;
#44243=CARTESIAN_POINT ( 'NONE',  ( -91.97819797305179179, -59.99999999999999289, 6.679364944045982355 ) ) ;
#44247=CARTESIAN_POINT ( 'NONE',  ( -84.01518071232440832, -32.49904627238863952, 168.3571053931298707 ) ) ;
#44260=CARTESIAN_POINT ( 'NONE',  ( -92.43439519788523739, -57.65869811958181401, -18.51275992931142156 ) ) ;
#44267=CARTESIAN_POINT ( 'NONE',  ( 101.4322121444104852, -14.21045842199439235, 121.1820579999150738 ) ) ;
#44268=CARTESIAN_POINT ( 'NONE',  ( -78.54456454054628978, -14.21045842199430709, 165.9065210845421348 ) ) ;
#44269=CARTESIAN_POINT ( 'NONE',  ( -59.69793324311933702, -53.39077738384364125, 78.06283456996561654 ) ) ;
#44274=CARTESIAN_POINT ( 'NONE',  ( -101.9374456322503306, -37.82064644935130104, 184.3837810757028421 ) ) ;
#44279=CARTESIAN_POINT ( 'NONE',  ( 77.17560814547307757, -38.35599394049779676, -28.07239321058808912 ) ) ;
#44289=CARTESIAN_POINT ( 'NONE',  ( -31.63782486760322143, -39.49234467425171857, 33.75314959485503152 ) ) ;
#44291=CARTESIAN_POINT ( 'NONE',  ( 48.81385752790940558, -29.13600490472190074, 45.58993858115186271 ) ) ;
#44295=CARTESIAN_POINT ( 'NONE',  ( -99.34640669332435436, -38.47270126492327336, 200.6976403403067479 ) ) ;
#44297=CARTESIAN_POINT ( 'NONE',  ( 84.58503749160358609, -38.35848514516985119, -23.21063429474329354 ) ) ;
#44306=CARTESIAN_POINT ( 'NONE',  ( 107.9765012271092246, -60.00000000000000711, 195.7039070726993941 ) ) ;
#44312=CARTESIAN_POINT ( 'NONE',  ( -80.89051708270336860, -30.00000000000003197, -12.18533877698737911 ) ) ;
#44314=CARTESIAN_POINT ( 'NONE',  ( -50.62117180075144063, -38.33334720786235295, 69.96112571796641078 ) ) ;
#44326=CARTESIAN_POINT ( 'NONE',  ( 80.67054414735359558, -60.44982962067441434, 181.0052678533708956 ) ) ;
#44335=DIRECTION ( 'NONE',  ( 0.000000000000000000, 0.000000000000000000, -1.000000000000000000 ) ) ;
#44341=CARTESIAN_POINT ( 'NONE',  ( -80.83118878706208932, -29.99999999999999645, -12.37157226799604004 ) ) ;
#44343=CARTESIAN_POINT ( 'NONE',  ( 87.46133420739155895, -42.73768625780829211, 190.5708321053066925 ) ) ;
#44368=CARTESIAN_POINT ( 'NONE',  ( -105.3254793209803779, -60.00000000000000000, 198.9436637240303298 ) ) ;
#44374=CARTESIAN_POINT ( 'NONE',  ( -82.83829789210793137, -57.26054315054904009, 188.0394631155682532 ) ) ;
#44382=CARTESIAN_POINT ( 'NONE',  ( -85.62477652849005949, -52.72148863023463150, -2.858541068345675118 ) ) ;
#44389=CARTESIAN_POINT ( 'NONE',  ( 54.44934741818074286, -29.99999999999998224, 75.82777139632159447 ) ) ;
#44391=CARTESIAN_POINT ( 'NONE',  ( -84.17958645690445962, -14.21045842199424314, -18.06708323581670328 ) ) ;
#44392=CARTESIAN_POINT ( 'NONE',  ( -76.83671821405472713, -18.66161896678824661, 113.2210307655415704 ) ) ;
#44394=CARTESIAN_POINT ( 'NONE',  ( 82.63356161194110427, -60.00000000000014921, 201.7055385233423976 ) ) ;
#44396=CARTESIAN_POINT ( 'NONE',  ( 36.45031898219243516, -60.00000000000000000, 51.27440833837025735 ) ) ;
#44407=CARTESIAN_POINT ( 'NONE',  ( -68.79622679644177197, -60.00000000000000000, -32.99527447484252463 ) ) ;
#44411=CARTESIAN_POINT ( 'NONE',  ( 21.88880945939638778, -4.285714285714295357, -12.64023069600374427 ) ) ;
#44420=CARTESIAN_POINT ( 'NONE',  ( 31.88147913428488067, -32.54995012556515377, 32.57459458299680222 ) ) ;
#44421=CARTESIAN_POINT ( 'NONE',  ( -15.50035291838927876, -4.285714285714916194, 20.16952962162167395 ) ) ;
#44435=CARTESIAN_POINT ( 'NONE',  ( 92.00410706449807208, -59.99999999999998579, 18.49124520143980632 ) ) ;
#44444=CARTESIAN_POINT ( 'NONE',  ( -103.9606405686747053, -29.99999999999802824, 196.6005958887341194 ) ) ;
#44450=CARTESIAN_POINT ( 'NONE',  ( 83.95844515931129592, -45.27844744688253087, -12.02577428134897808 ) ) ;
#44460=VERTEX_POINT ( 'NONE', #77529 ) ;
#44461=CARTESIAN_POINT ( 'NONE',  ( 75.47549834169566907, -46.43312234463159882, 127.8789400697300493 ) ) ;
#44466=CARTESIAN_POINT ( 'NONE',  ( -76.22482491972903063, -57.54008153533397518, 193.6369246664269781 ) ) ;
#44476=B_SPLINE_CURVE_WITH_KNOTS ( 'NONE', 3,
 ( #50179, #90113, #106275, #32438 ),
 .UNSPECIFIED., .F., .F.,
 ( 4, 4 ),
 ( 0.0009107969653496763478, 0.009022847091396625149 ),
 .UNSPECIFIED. ) ;
#44494=CARTESIAN_POINT ( 'NONE',  ( -69.26106847545361234, -30.21325109223555927, -30.03938730321735306 ) ) ;
#44495=CARTESIAN_POINT ( 'NONE',  ( -87.75043898228696548, -30.00000000000000355, 186.1331779216796747 ) ) ;
#44499=CARTESIAN_POINT ( 'NONE',  ( 77.56900591926921607, -57.51690387631008861, 195.9563615345031451 ) ) ;
#44502=CARTESIAN_POINT ( 'NONE',  ( 38.72114142554678295, -32.54403767304167161, -37.56696858966843422 ) ) ;
#44504=CARTESIAN_POINT ( 'NONE',  ( -69.23101163046497675, -60.00000000000000711, 137.2813101166285605 ) ) ;
#44508=CARTESIAN_POINT ( 'NONE',  ( -85.27764252179795790, -57.47308612990543253, 192.4447815377685913 ) ) ;
#44511=CARTESIAN_POINT ( 'NONE',  ( -4.074072711644582512, -46.43917196787263890, 31.62195155993591200 ) ) ;
#44529=CARTESIAN_POINT ( 'NONE',  ( 89.60175727050132366, -14.21045842199443143, 48.51353285324994147 ) ) ;
#44530=CARTESIAN_POINT ( 'NONE',  ( -82.52651961324420427, -32.55781991263304320, 155.0962975578067642 ) ) ;
#44534=CARTESIAN_POINT ( 'NONE',  ( 4.154708322984330151E-08, -57.67120202538961138, 41.61186700422870643 ) ) ;
#44554=CARTESIAN_POINT ( 'NONE',  ( 82.32205428790078372, -60.00000000000002132, -26.51557028033280616 ) ) ;
#44555=CARTESIAN_POINT ( 'NONE',  ( -71.62990520600911282, -30.00000000000002842, 135.6731032779996156 ) ) ;
#44556=CARTESIAN_POINT ( 'NONE',  ( 23.46127647898429913, -32.51707366590390080, 30.27781536837194665 ) ) ;
#44559=CARTESIAN_POINT ( 'NONE',  ( -36.21398753213680521, -25.65888403626743752, 33.24715464751751171 ) ) ;
#44572=CARTESIAN_POINT ( 'NONE',  ( 90.84406139033485772, -29.99999999999999289, 190.4162226198302790 ) ) ;
#44575=CARTESIAN_POINT ( 'NONE',  ( 81.44514727150406941, -30.00000000000000711, -9.709585533065395069 ) ) ;
#44594=CARTESIAN_POINT ( 'NONE',  ( 53.84901272430960972, -38.34088802725808875, 78.30668236027604223 ) ) ;
#44617=CARTESIAN_POINT ( 'NONE',  ( 86.19842101853855354, -28.27713569860727816, 183.2257041085184710 ) ) ;
#44627=CARTESIAN_POINT ( 'NONE',  ( -90.20890582660780410, -29.99999999999999289, 89.71514907472229083 ) ) ;
#44630=CARTESIAN_POINT ( 'NONE',  ( 17.63980495134517668, -57.67160087258927348, 41.95025224030491984 ) ) ;
#44635=CARTESIAN_POINT ( 'NONE',  ( -43.80704950897089844, -36.52919196705796168, 41.55287977338722527 ) ) ;
#44639=CARTESIAN_POINT ( 'NONE',  ( 21.65227882671612747, -19.03527767991882058, -33.49607776825432381 ) ) ;
#44640=ADVANCED_FACE ( 'NONE', ( #87491 ), #104713, .F. ) ;
#44643=CARTESIAN_POINT ( 'NONE',  ( -25.57323824984261762, -25.56794925674672925, 29.49343980220939088 ) ) ;
#44647=CARTESIAN_POINT ( 'NONE',  ( -19.82538544910368117, -25.55338363043042804, 28.62632469270730695 ) ) ;
#44658=CARTESIAN_POINT ( 'NONE',  ( -8.528914935573171263, -60.00000000000000711, -42.47286814751166872 ) ) ;
#44662=CARTESIAN_POINT ( 'NONE',  ( 105.0707565437703579, -60.15135272885378015, 187.5576145010796836 ) ) ;
#44676=CARTESIAN_POINT ( 'NONE',  ( -94.55323015762245120, -59.99999999999268852, -13.46500496322361151 ) ) ;
#44678=CARTESIAN_POINT ( 'NONE',  ( 24.08356453790285201, -60.00000000000000000, 40.93464879651766353 ) ) ;
#44681=CARTESIAN_POINT ( 'NONE',  ( -112.5893510171550105, -59.99999999999995026, 145.0943965991558002 ) ) ;
#44682=CARTESIAN_POINT ( 'NONE',  ( 5.033794246690010965, -32.51032478759464794, 29.29834927723706883 ) ) ;
#44684=CARTESIAN_POINT ( 'NONE',  ( -48.64733360570842535, -42.98315368061135189, 49.69360454995861431 ) ) ;
#44696=CARTESIAN_POINT ( 'NONE',  ( 106.8254625047631521, -30.00000000010051693, 139.4333767052048074 ) ) ;
#44700=CARTESIAN_POINT ( 'NONE',  ( 100.4699977146906491, -30.00000000000000000, 183.0391429837226553 ) ) ;
#44706=CARTESIAN_POINT ( 'NONE',  ( 53.92222671074195972, -25.63022886178348614, 52.72325914952270409 ) ) ;
#44710=CARTESIAN_POINT ( 'NONE',  ( -90.37459492297462305, -38.40150067238776188, -14.96073006302789032 ) ) ;
#44713=CARTESIAN_POINT ( 'NONE',  ( 107.1641568268869236, -38.36318885066040707, 194.5620192865105480 ) ) ;
#44715=CARTESIAN_POINT ( 'NONE',  ( 82.50951266294359243, -37.86122216130837614, 7.438025769970757040 ) ) ;
#44718=CIRCLE ( 'NONE', #17153, 7.499999999992679633 ) ;
#44727=LINE ( 'NONE', #92183, #96988 ) ;
#44735=CARTESIAN_POINT ( 'NONE',  ( 35.58102909488143695, -24.34075600965972086, 33.68644870080316167 ) ) ;
#44741=CARTESIAN_POINT ( 'NONE',  ( 85.21443187028769728, -35.75854868015726140, 182.1664523584917106 ) ) ;
#44744=CARTESIAN_POINT ( 'NONE',  ( -88.35647174428689254, -37.82076271483501984, 68.44965775589997747 ) ) ;
#44753=CARTESIAN_POINT ( 'NONE',  ( 24.81410138265733423, -59.99999999999998579, 41.11425977102789631 ) ) ;
#44754=CARTESIAN_POINT ( 'NONE',  ( 2.701267476147420687, -18.15621507579777827, 35.02215398985747186 ) ) ;
#44755=CARTESIAN_POINT ( 'NONE',  ( 48.01188717829646180, -29.24194067517573004, 43.63834193384174398 ) ) ;
#44765=CARTESIAN_POINT ( 'NONE',  ( 0.000000000000000000, 30.00000000000000000, 0.000000000000000000 ) ) ;
#44773=CARTESIAN_POINT ( 'NONE',  ( -22.10641630101648047, -34.58974403249237639, -31.65637301226508526 ) ) ;
#44783=CARTESIAN_POINT ( 'NONE',  ( -91.86228806005425440, -60.00000000000000711, 11.38199961291973139 ) ) ;
#44786=CARTESIAN_POINT ( 'NONE',  ( -89.99999999999997158, -60.00000000000000000, 198.0238439516549818 ) ) ;
#44792=CARTESIAN_POINT ( 'NONE',  ( -85.01355329713241815, -22.07199797865288815, 160.8995575460550924 ) ) ;
#44794=CARTESIAN_POINT ( 'NONE',  ( -5.483261958908374645, -0.000000000000000000, 16.14668631624861916 ) ) ;
#44802=CARTESIAN_POINT ( 'NONE',  ( -93.88160267686131988, -57.67344353738141649, 16.36278552810739839 ) ) ;
#44809=CARTESIAN_POINT ( 'NONE',  ( 109.5930103617047422, -60.00000000000001421, 123.9179654958789456 ) ) ;
#44811=CARTESIAN_POINT ( 'NONE',  ( -108.2763249159406769, -59.99999999999986500, 199.3718883026843116 ) ) ;
#44812=CARTESIAN_POINT ( 'NONE',  ( -57.26801628779367093, -25.61114176797853048, 59.45904782552288026 ) ) ;
#44816=CARTESIAN_POINT ( 'NONE',  ( -105.7774229000524713, -60.15503266313929487, 184.0530045780120645 ) ) ;
#44817=SURFACE_SIDE_STYLE ('',( #27062 ) ) ;
#44822=( NAMED_UNIT ( * ) PLANE_ANGLE_UNIT ( ) SI_UNIT ( $, .RADIAN. ) );
#44835=CARTESIAN_POINT ( 'NONE',  ( -26.89381846417044031, -29.05099145694870799, 30.38545181110030313 ) ) ;
#44838=CARTESIAN_POINT ( 'NONE',  ( 47.00746256722314342, -49.89691352968622340, 49.27416738806363128 ) ) ;
#44842=CARTESIAN_POINT ( 'NONE',  ( -84.83356168783870999, -38.71398380538228423, 198.3796149434837730 ) ) ;
#44850=CARTESIAN_POINT ( 'NONE',  ( 111.7255001473898091, -60.00000000000002132, 159.8843962759177373 ) ) ;
#44857=CARTESIAN_POINT ( 'NONE',  ( -100.7109739928592660, -29.99999999999998224, 161.5959690901798069 ) ) ;
#44869=CARTESIAN_POINT ( 'NONE',  ( 83.14894204440837200, -39.48093398824585165, 171.2762584616673394 ) ) ;
#44876=DIRECTION ( 'NONE',  ( 0.000000000000000000, -1.000000000000000000, 0.000000000000000000 ) ) ;
#44900=CARTESIAN_POINT ( 'NONE',  ( -80.00000000000000000, -38.00000000001091394, -21.09707704303352926 ) ) ;
#44914=CARTESIAN_POINT ( 'NONE',  ( -92.43873093052026491, -59.99999999999999289, 202.4061414662364484 ) ) ;
#44919=CARTESIAN_POINT ( 'NONE',  ( -83.89707888881473252, -46.55430503609073867, 184.2034029786331359 ) ) ;
#44926=CARTESIAN_POINT ( 'NONE',  ( -83.74416109486040227, -45.26689415792657911, 7.590503140103296964 ) ) ;
#44934=CARTESIAN_POINT ( 'NONE',  ( 52.56736687853028656, -59.99999999999993605, 85.36620364727897936 ) ) ;
#44937=CARTESIAN_POINT ( 'NONE',  ( -84.06615883987635129, -30.00000000000009592, -21.85610764691116259 ) ) ;
#44938=CARTESIAN_POINT ( 'NONE',  ( -64.14719193146001430, -42.96209425739802157, 85.50081336499792428 ) ) ;
#44940=CARTESIAN_POINT ( 'NONE',  ( 110.6388055374740276, -59.99999999999995026, 195.8051704144367591 ) ) ;
#44942=CARTESIAN_POINT ( 'NONE',  ( 14.10670912403736210, -60.00000000000986233, 42.10997246407520578 ) ) ;
#44952=CARTESIAN_POINT ( 'NONE',  ( -60.77971423025187647, -59.99999999999997868, -35.44896578423877287 ) ) ;
#44964=CARTESIAN_POINT ( 'NONE',  ( 33.16625095708381110, -39.49312339222125701, 34.41974150182668524 ) ) ;
#44966=CARTESIAN_POINT ( 'NONE',  ( -20.16952962162825358, -4.285714285714285587, -15.50035291838207741 ) ) ;
#44979=CARTESIAN_POINT ( 'NONE',  ( 92.42593725262484838, -60.00000000000000000, -0.2051320214708048373 ) ) ;
#44986=CARTESIAN_POINT ( 'NONE',  ( -102.1093457436780625, -30.00000000000017764, 198.0925856303319108 ) ) ;
#44987=ORIENTED_EDGE ( 'NONE', *, *, #63940, .T. ) ;
#44993=CARTESIAN_POINT ( 'NONE',  ( 83.19409135691178392, -45.27699134791323843, -14.11599572094245936 ) ) ;
#45003=ORIENTED_EDGE ( 'NONE', *, *, #5143, .F. ) ;
#45004=CARTESIAN_POINT ( 'NONE',  ( 77.54917875449221754, -56.83930884621564417, 148.6048652908098404 ) ) ;
#45011=CARTESIAN_POINT ( 'NONE',  ( -107.9249424950986906, -57.65976581800653378, 199.0938304663491749 ) ) ;
#45022=CARTESIAN_POINT ( 'NONE',  ( -43.37936553595135791, -27.70851877802382290, 38.49181127301306304 ) ) ;
#45025=CARTESIAN_POINT ( 'NONE',  ( 97.05545962818543160, -41.67787136694374084, 193.4168249765711778 ) ) ;
#45032=CARTESIAN_POINT ( 'NONE',  ( -8.577179510621105507, -18.39515840085658382, -37.90072206629012896 ) ) ;
#45033=CARTESIAN_POINT ( 'NONE',  ( -60.71702475842560176, -30.00000000000000000, 68.69174167666419351 ) ) ;
#45038=CARTESIAN_POINT ( 'NONE',  ( 75.31978416560909295, -57.56542590815787719, 191.5343058687835764 ) ) ;
#45042=CARTESIAN_POINT ( 'NONE',  ( 27.87892343117143668, -28.78925693790030849, -38.27049670904933265 ) ) ;
#45046=CARTESIAN_POINT ( 'NONE',  ( -49.57512317434233040, -60.00000000000000711, 70.75543162407628017 ) ) ;
#45049=CARTESIAN_POINT ( 'NONE',  ( -86.36540683355931947, -20.96352888107788104, 181.2261683823607825 ) ) ;
#45051=CARTESIAN_POINT ( 'NONE',  ( -4.060342910471293365, -42.95752896766379081, 31.04180052082970676 ) ) ;
#45064=CARTESIAN_POINT ( 'NONE',  ( -22.03900363278799190, -4.285714285715346072, 12.70248734012972669 ) ) ;
#45066=CARTESIAN_POINT ( 'NONE',  ( 97.22633417984880566, -59.99999999999997158, 47.92222960719137603 ) ) ;
#45067=CARTESIAN_POINT ( 'NONE',  ( -82.86146759555738583, -22.15494292095191753, 144.5965692535937421 ) ) ;
#45071=SURFACE_STYLE_USAGE ( .BOTH. , #69345 ) ;
#45090=CARTESIAN_POINT ( 'NONE',  ( 13.89483002323571093, -60.00000000000000000, -42.23792084422591842 ) ) ;
#45092=CARTESIAN_POINT ( 'NONE',  ( -35.95074892501450847, -14.21045842199431242, 40.03088108345822604 ) ) ;
#45093=CARTESIAN_POINT ( 'NONE',  ( 26.71221250542331305, -39.47873605212244996, 32.14795869538025386 ) ) ;
#45095=CARTESIAN_POINT ( 'NONE',  ( -35.25737817069384050, -29.11316072765389151, 33.41771700477326590 ) ) ;
#45106=CARTESIAN_POINT ( 'NONE',  ( -76.00296169842491167, -38.37803246168048332, 178.3767332364141680 ) ) ;
#45108=CARTESIAN_POINT ( 'NONE',  ( 100.2372838592740720, -30.00000000000000711, 155.9018345844573901 ) ) ;
#45112=CARTESIAN_POINT ( 'NONE',  ( 80.95957609789309117, -30.00000000000000355, 4.740870403401825861 ) ) ;
#45135=CARTESIAN_POINT ( 'NONE',  ( 62.57728911496235469, -46.43500176870801965, 82.71392919577269254 ) ) ;
#45141=EDGE_CURVE ( 'NONE', #39827, #41900, #81876, .T. ) ;
#45150=CARTESIAN_POINT ( 'NONE',  ( 86.74131503813627830, -31.75820404643615902, 186.6526303525701564 ) ) ;
#45159=CARTESIAN_POINT ( 'NONE',  ( -90.20126103059185141, -30.00000000000000000, 89.67039343529408768 ) ) ;
#45163=CARTESIAN_POINT ( 'NONE',  ( 0.06508481715640716814, -57.67120202701944720, 41.61186395748749334 ) ) ;
#45175=CARTESIAN_POINT ( 'NONE',  ( -87.32469796123234573, -39.06411114470611778, 189.6241748795063700 ) ) ;
#45179=CARTESIAN_POINT ( 'NONE',  ( -16.76553171890364879, -39.47645239752473856, 30.70764041000546740 ) ) ;
#45192=CARTESIAN_POINT ( 'NONE',  ( -8.464573819226677287, -59.99999999999997868, -42.47522266335410990 ) ) ;
#45196=CARTESIAN_POINT ( 'NONE',  ( 103.5716558477763130, -60.15916816527329303, 191.7890153051873483 ) ) ;
#45197=CARTESIAN_POINT ( 'NONE',  ( 42.01828575296529777, -35.92164807018873773, 39.63900877982145232 ) ) ;
#45210=CARTESIAN_POINT ( 'NONE',  ( -94.51847600260155957, -59.99999999997076117, 21.88820220593430577 ) ) ;
#45212=CARTESIAN_POINT ( 'NONE',  ( 22.69281982466505809, -60.00000000000000000, 40.64002152815756830 ) ) ;
#45215=CARTESIAN_POINT ( 'NONE',  ( -89.60210353745294753, -14.21045842199431597, 48.51666376363581890 ) ) ;
#45216=CARTESIAN_POINT ( 'NONE',  ( 7.280253809880594673, -60.35889587898908104, 33.93986660363172092 ) ) ;
#45218=CARTESIAN_POINT ( 'NONE',  ( -48.85179756045110366, -49.90554923932949549, 52.24086561123009176 ) ) ;
#45227=CARTESIAN_POINT ( 'NONE',  ( 82.77319705486205237, -29.99999999998750866, -22.91096955354018050 ) ) ;
#45232=CARTESIAN_POINT ( 'NONE',  ( 100.4882595953770021, -29.99999999999999289, 182.9151894254146953 ) ) ;
#45234=ORIENTED_EDGE ( 'NONE', *, *, #28403, .F. ) ;
#45238=CARTESIAN_POINT ( 'NONE',  ( 54.79840299013832094, -49.90675031112721882, 64.09447975165772959 ) ) ;
#45241=CARTESIAN_POINT ( 'NONE',  ( -90.37937951170148665, -38.40155043091493781, -14.94611653123792649 ) ) ;
#45244=CARTESIAN_POINT ( 'NONE',  ( 94.02768479641977706, -38.49244630022761271, 201.1932099879993530 ) ) ;
#45246=CARTESIAN_POINT ( 'NONE',  ( 86.14658077292135374, -60.13954629211933423, 13.87186910527404748 ) ) ;
#45248=( NAMED_UNIT ( * ) SI_UNIT ( $, .STERADIAN. ) SOLID_ANGLE_UNIT ( ) );
#45266=CARTESIAN_POINT ( 'NONE',  ( -33.96155455825784486, -26.02205035446894854, 41.25632646196086029 ) ) ;
#45270=CARTESIAN_POINT ( 'NONE',  ( 85.56702050224303946, -28.63500417004610554, 178.3742600491905534 ) ) ;
#45272=CARTESIAN_POINT ( 'NONE',  ( -83.88445482477082749, -59.99999999999995737, 191.6821729358339610 ) ) ;
#45274=CARTESIAN_POINT ( 'NONE',  ( -91.53872723970857805, -37.82056087769771580, 87.62393259169999737 ) ) ;
#45281=CARTESIAN_POINT ( 'NONE',  ( 21.41851261898789005, -26.63141905998440961, 37.18235420823341286 ) ) ;
#45282=CARTESIAN_POINT ( 'NONE',  ( 31.33511474313509382, -22.32021645782860730, 32.40417205478716767 ) ) ;
#45300=CARTESIAN_POINT ( 'NONE',  ( 8.063737759921492554, -60.22818524261399631, -36.77936988234735338 ) ) ;
#45309=CARTESIAN_POINT ( 'NONE',  ( -92.03711610564900525, -60.00000000000000000, 19.24587899639053390 ) ) ;
#45313=CARTESIAN_POINT ( 'NONE',  ( 89.99999999999997158, -52.00000000000000000, 196.0238439516549818 ) ) ;
#45316=CARTESIAN_POINT ( 'NONE',  ( -80.86724053673806623, -56.93357778657505719, 177.6017799944823992 ) ) ;
#45320=ORIENTED_EDGE ( 'NONE', *, *, #49369, .F. ) ;
#45330=CARTESIAN_POINT ( 'NONE',  ( -94.77678295284667342, -57.67204358354969429, 30.25255809810320429 ) ) ;
#45337=CARTESIAN_POINT ( 'NONE',  ( 80.19743504398171297, -30.00000000000002487, -24.77996380036185187 ) ) ;
#45339=CARTESIAN_POINT ( 'NONE',  ( -73.11793949506163415, -30.00000000000001776, 143.8487384131749423 ) ) ;
#45340=CARTESIAN_POINT ( 'NONE',  ( -53.62371817297555054, -56.84947591570442427, 64.25590909039557630 ) ) ;
#45344=CARTESIAN_POINT ( 'NONE',  ( -101.1402928026442538, -52.73124438991371932, 193.2249404277670237 ) ) ;
#45345=CARTESIAN_POINT ( 'NONE',  ( 99.18548223479925241, -38.00000000000000711, 133.7811713353216874 ) ) ;
#45349=FILL_AREA_STYLE_COLOUR ( '', #29228 ) ;
#45356=CARTESIAN_POINT ( 'NONE',  ( 69.66098783280243367, -30.00000000000000000, 94.24250346725962402 ) ) ;
#45360=CARTESIAN_POINT ( 'NONE',  ( -29.16980113487907289, -53.38861740668193079, 35.28666285170401551 ) ) ;
#45361=CARTESIAN_POINT ( 'NONE',  ( 47.88527768379917404, -56.81691787927777426, 52.80198151643631377 ) ) ;
#45364=CARTESIAN_POINT ( 'NONE',  ( -87.28184510988498346, -38.58415483285815384, 199.6650293345611544 ) ) ;
#45366=CARTESIAN_POINT ( 'NONE',  ( 89.55318350885924872, -38.38936930854548990, -17.00445670180018354 ) ) ;
#45375=CARTESIAN_POINT ( 'NONE',  ( 0.000000000000000000, -15.00000000000000000, 0.000000000000000000 ) ) ;
#45376=CARTESIAN_POINT ( 'NONE',  ( 111.3059636549010065, -59.99999999999999289, 185.6424028919510363 ) ) ;
#45381=EDGE_CURVE ( 'NONE', #86580, #22652, #94578, .T. ) ;
#45383=CARTESIAN_POINT ( 'NONE',  ( -77.11398825348869934, -30.00000000000000000, -16.56961864290801500 ) ) ;
#45385=CARTESIAN_POINT ( 'NONE',  ( -77.95742533360386517, -38.56940929884702740, 188.1909952854809092 ) ) ;
#45398=CARTESIAN_POINT ( 'NONE',  ( 84.01537763452704155, -32.49674573478225170, 168.3552522700273073 ) ) ;
#45414=B_SPLINE_CURVE_WITH_KNOTS ( 'NONE', 3,
 ( #97740, #6615, #75470, #56747, #81540, #74923, #83555, #9130 ),
 .UNSPECIFIED., .F., .F.,
 ( 4, 2, 2, 4 ),
 ( 0.4104551234109616309, 0.4139675962486015215, 0.4174800690862414121, 0.4245050147615211378 ),
 .UNSPECIFIED. ) ;
#45416=CARTESIAN_POINT ( 'NONE',  ( -80.33428810687757959, -29.99999999999999645, -13.32063309743382895 ) ) ;
#45438=CARTESIAN_POINT ( 'NONE',  ( -98.77838488027474284, -60.00000000000001421, 202.1921766562477103 ) ) ;
#45444=CARTESIAN_POINT ( 'NONE',  ( -83.72764112179662277, -42.98392764094067786, 180.3475611446869777 ) ) ;
#45452=CARTESIAN_POINT ( 'NONE',  ( -85.37616942211955973, -52.71083131077448058, 0.7312150782069049004 ) ) ;
#45459=CARTESIAN_POINT ( 'NONE',  ( 100.5651899622199039, -60.00000000000009948, 204.3456409986242477 ) ) ;
#45462=CARTESIAN_POINT ( 'NONE',  ( -86.99605493950913626, -14.21045842199422005, 24.11595694609475160 ) ) ;
#45463=CARTESIAN_POINT ( 'NONE',  ( -63.59289893964069051, -46.43872110597177993, 85.67305972463248054 ) ) ;
#45465=CARTESIAN_POINT ( 'NONE',  ( 88.35660587733796945, -14.21045842199459486, 197.0604887900697122 ) ) ;
#45467=CARTESIAN_POINT ( 'NONE',  ( 80.96048728771400249, -60.00000000000738254, 200.5225259978467136 ) ) ;
#45479=CARTESIAN_POINT ( 'NONE',  ( -92.28351384443637073, -60.00000000000002842, -12.64941138170132540 ) ) ;
#45486=CARTESIAN_POINT ( 'NONE',  ( 6.539732759932823214, -4.285714285714295357, 24.41571844174603356 ) ) ;
#45498=CARTESIAN_POINT ( 'NONE',  ( 35.80305322736619189, -60.28683605755409758, 39.79195959564579255 ) ) ;
#45507=CARTESIAN_POINT ( 'NONE',  ( 2.500000000000025757, -22.55587004235349369, 27.64561374872702260 ) ) ;
#45511=CARTESIAN_POINT ( 'NONE',  ( 92.00241997389161952, -59.99999999999999289, 6.158180974754545289 ) ) ;
#45517=CARTESIAN_POINT ( 'NONE',  ( -101.8367267568395391, -29.99999999999178968, 198.2562598845839545 ) ) ;
#45533=CARTESIAN_POINT ( 'NONE',  ( 79.92391610595905149, -42.96574981224191703, 149.1602879951772138 ) ) ;
#45540=CARTESIAN_POINT ( 'NONE',  ( -88.64096389254642361, -57.60155557764662149, 203.6424623121221487 ) ) ;
#45547=CARTESIAN_POINT ( 'NONE',  ( -48.78551423464154624, -29.44057650021229477, 44.71846274219842599 ) ) ;
#45561=CARTESIAN_POINT ( 'NONE',  ( -6.831292435471142177, -18.15074247170165833, -37.92091795732829951 ) ) ;
#45562=CARTESIAN_POINT ( 'NONE',  ( -63.62542678175617539, -29.99999999999999645, 76.38903665440084012 ) ) ;
#45566=CARTESIAN_POINT ( 'NONE',  ( 83.65515381790297056, -57.54282162997657224, 201.5564494504526181 ) ) ;
#45567=CARTESIAN_POINT ( 'NONE',  ( 59.17222854736898796, -60.22833427386899530, -29.94836549083426291 ) ) ;
#45571=CARTESIAN_POINT ( 'NONE',  ( -53.40412661496910829, -59.99999999999999289, 80.76610350128422056 ) ) ;
#45574=CARTESIAN_POINT ( 'NONE',  ( -86.32981076077537352, -24.59913943680475867, 182.4586318646072414 ) ) ;
#45591=CARTESIAN_POINT ( 'NONE',  ( 24.56594385547636605, -4.285714285715934047, 6.601913983210457637 ) ) ;
#45593=CARTESIAN_POINT ( 'NONE',  ( 95.23263947746859515, -60.00000000000000000, 30.92889862699057701 ) ) ;
#45594=CARTESIAN_POINT ( 'NONE',  ( -78.59425758961695863, -46.43800249855129181, 144.3747020998414996 ) ) ;
#45598=CARTESIAN_POINT ( 'NONE',  ( 44.43430165216474137, -57.68372671355613335, 63.93072606185115347 ) ) ;
#45614=CARTESIAN_POINT ( 'NONE',  ( -2.500000000000011990, -30.00000000000000000, -31.87333704504306908 ) ) ;
#45618=CARTESIAN_POINT ( 'NONE',  ( 78.70688208539898767, -59.99999999999998579, -28.66616797828253027 ) ) ;
#45619=CARTESIAN_POINT ( 'NONE',  ( -69.27297328317253289, -60.00000000000002132, 151.6304908672517513 ) ) ;
#45620=CARTESIAN_POINT ( 'NONE',  ( 28.38568808205318916, -49.90851060535624839, 34.42946133055457381 ) ) ;
#45624=CARTESIAN_POINT ( 'NONE',  ( -3.301565691951511727, -4.285714285714296246, -25.05982991920904368 ) ) ;
#45631=CARTESIAN_POINT ( 'NONE',  ( 97.94761177215855241, -29.99999999999992184, 190.5827337369310897 ) ) ;
#45634=CARTESIAN_POINT ( 'NONE',  ( 81.07608397363662789, -29.99999999999999645, 2.777871215026683771 ) ) ;
#45651=CARTESIAN_POINT ( 'NONE',  ( 59.06997099859516709, -38.34368760562352918, 93.42682326698202644 ) ) ;
#45655=CARTESIAN_POINT ( 'NONE',  ( 63.92674818503888901, -46.43411801997230270, 86.65795160353560789 ) ) ;
#45658=CARTESIAN_POINT ( 'NONE',  ( -55.98517882506007481, -36.72792837143562394, -35.06346615357033869 ) ) ;
#45660=EDGE_CURVE ( 'NONE', #8148, #86629, #51581, .T. ) ;
#45671=CARTESIAN_POINT ( 'NONE',  ( 86.71155056234793790, -28.07589402024821723, 185.8220023598428270 ) ) ;
#45677=CARTESIAN_POINT ( 'NONE',  ( 1.406919699518766720, -15.40373694258998682, -35.22331805215249290 ) ) ;
#45681=CARTESIAN_POINT ( 'NONE',  ( -100.2369334069439617, -30.00000000000000000, 156.2071045385363846 ) ) ;
#45683=CARTESIAN_POINT ( 'NONE',  ( 32.39832671728185431, -57.69015538478544158, 46.85044192637200666 ) ) ;
#45694=CARTESIAN_POINT ( 'NONE',  ( -20.66668522848859624, -60.36289094223184293, 34.55967790951763163 ) ) ;
#45696=CARTESIAN_POINT ( 'NONE',  ( -92.99974329923009009, -60.00000000000000000, 74.19676606278758868 ) ) ;
#45706=CARTESIAN_POINT ( 'NONE',  ( 103.4866592801870553, -52.71721449814598515, 188.6654185098675214 ) ) ;
#45717=ORIENTED_EDGE ( 'NONE', *, *, #30453, .F. ) ;
#45721=CARTESIAN_POINT ( 'NONE',  ( -72.27154473826411163, -59.99999999998056666, -34.24698835184248225 ) ) ;
#45723=CARTESIAN_POINT ( 'NONE',  ( 5.625240605873267796, -59.99999999996141753, -44.94030595675567241 ) ) ;
#45727=CARTESIAN_POINT ( 'NONE',  ( -96.66672766003948425, -59.99999999999999289, 43.67975107286704883 ) ) ;
#45728=CARTESIAN_POINT ( 'NONE',  ( 11.28666612630582833, -35.99164038003812038, 29.91485281499912219 ) ) ;
#45730=CARTESIAN_POINT ( 'NONE',  ( -48.77537313921662587, -32.59926516119964646, 46.61647805872783579 ) ) ;
#45743=CARTESIAN_POINT ( 'NONE',  ( 87.88634981426525883, -29.99999999999498002, -17.24999379162776592 ) ) ;
#45748=CARTESIAN_POINT ( 'NONE',  ( 96.00844566870836161, -30.00000000000000000, 191.2852847503578460 ) ) ;
#45753=CARTESIAN_POINT ( 'NONE',  ( 53.18860290234052712, -56.84141687534781795, 63.26041922679137741 ) ) ;
#45757=CARTESIAN_POINT ( 'NONE',  ( -77.86225395006566430, -38.35593842581449309, -27.73772653773013630 ) ) ;
#45761=CARTESIAN_POINT ( 'NONE',  ( 88.88549997972674532, -38.53645272322479087, 200.2533030273275472 ) ) ;
#45763=CARTESIAN_POINT ( 'NONE',  ( 82.45637196367515287, -37.86046039678901565, 9.370868085246026880 ) ) ;
#45780=CARTESIAN_POINT ( 'NONE',  ( 4.154708322984369194E-08, -57.67120202538961138, 41.61186700422869933 ) ) ;
#45783=CARTESIAN_POINT ( 'NONE',  ( 1.046656298439633925, -14.82702095649888641, 34.47215281706392886 ) ) ;
#45786=CARTESIAN_POINT ( 'NONE',  ( 85.21129371257987373, -32.24359312048367343, 179.1469130256770086 ) ) ;
#45791=CARTESIAN_POINT ( 'NONE',  ( -98.39902859776117339, -60.15518905392604410, 105.6211524846448526 ) ) ;
#45793=DIRECTION ( 'NONE',  ( 0.000000000000000000, -1.000000000000000000, 0.000000000000000000 ) ) ;
#45804=CARTESIAN_POINT ( 'NONE',  ( 33.82190865419818948, -23.50910416088391841, 33.09154993403522838 ) ) ;
#45817=CARTESIAN_POINT ( 'NONE',  ( -89.12526225705758520, -38.00000000000000000, 73.22758371480502149 ) ) ;
#45825=CARTESIAN_POINT ( 'NONE',  ( 6.360191607006829173, -47.40891213495661560, -34.69802138687305160 ) ) ;
#45833=CARTESIAN_POINT ( 'NONE',  ( -94.40663350262447295, -60.00000000000000711, 44.56717037654195224 ) ) ;
#45840=CARTESIAN_POINT ( 'NONE',  ( -81.62634306135213080, -49.94837975070949909, 173.6806837566333286 ) ) ;
#45842=CARTESIAN_POINT ( 'NONE',  ( -4.418451808487692922, 0.000000000000000000, 16.46925340495486267 ) ) ;
#45850=CARTESIAN_POINT ( 'NONE',  ( -101.8692865417259696, -57.67122770170253432, 80.25822756173465677 ) ) ;
#45857=CARTESIAN_POINT ( 'NONE',  ( 56.79302105626919683, -14.21045842199427867, -31.02814365720875500 ) ) ;
#45858=CARTESIAN_POINT ( 'NONE',  ( -64.82027869498183748, -30.00000000000004619, 107.4038593739741430 ) ) ;
#45859=CARTESIAN_POINT ( 'NONE',  ( -55.06067097896985274, -53.38329654548371650, 66.16146764719466944 ) ) ;
#45863=CARTESIAN_POINT ( 'NONE',  ( -100.0726282877276958, -45.25679602138151125, 192.5320261463655811 ) ) ;
#45872=CARTESIAN_POINT ( 'NONE',  ( 69.74927355208504309, -30.00000000000000355, 94.52352744978905719 ) ) ;
#45875=ADVANCED_FACE ( 'NONE', ( #53151 ), #38511, .T. ) ;
#45879=CARTESIAN_POINT ( 'NONE',  ( -29.64972134613275045, -49.91194892834956676, 34.84693478522385846 ) ) ;
#45882=CARTESIAN_POINT ( 'NONE',  ( 48.64717611995057212, -42.97917151878713327, 49.69220790373555730 ) ) ;
#45886=CARTESIAN_POINT ( 'NONE',  ( -104.5817897493230788, -38.40156824060414209, 197.8926955786276949 ) ) ;
#45890=CARTESIAN_POINT ( 'NONE',  ( 91.31362265674661671, -38.40000453515457224, -10.25727057701513623 ) ) ;
#45900=CARTESIAN_POINT ( 'NONE',  ( 108.8408623652823337, -60.00000000000000711, 194.0362837791606978 ) ) ;
#45904=VERTEX_POINT ( 'NONE', #17217 ) ;
#45910=CARTESIAN_POINT ( 'NONE',  ( -91.43450980527380523, -38.37461378256361400, -4.864083082636263100 ) ) ;
#45920=CARTESIAN_POINT ( 'NONE',  ( 82.17288844096735545, -46.46110024266576488, 173.2037556483296896 ) ) ;
#45951=DIRECTION ( 'NONE',  ( 0.000000000000000000, -0.000000000000000000, -1.000000000000000000 ) ) ;
#45962=CARTESIAN_POINT ( 'NONE',  ( -108.5389370269662805, -59.99999999999999289, 194.6443121377485852 ) ) ;
#45970=CARTESIAN_POINT ( 'NONE',  ( -82.78613966356304843, -50.04786190543876501, 182.2101918582118572 ) ) ;
#45977=CARTESIAN_POINT ( 'NONE',  ( -83.71838643811501868, -45.26559428471287561, 15.97475021176123278 ) ) ;
#45981=PRESENTATION_STYLE_ASSIGNMENT (( #55104 ) ) ;
#45984=CARTESIAN_POINT ( 'NONE',  ( 104.0082629745172653, -14.21045842199441012, 192.0643512960946282 ) ) ;
#45986=CARTESIAN_POINT ( 'NONE',  ( -102.6949714452557885, -14.21045842199446518, 129.2658233771313974 ) ) ;
#45987=CARTESIAN_POINT ( 'NONE',  ( -63.59055291699712598, -56.86855241622866686, 91.13439659791259828 ) ) ;
#45990=CARTESIAN_POINT ( 'NONE',  ( 55.94905262869426110, -59.99999999988309440, 95.40321447124708243 ) ) ;
#45995=ORIENTED_EDGE ( 'NONE', *, *, #69819, .T. ) ;
#45998=VERTEX_POINT ( 'NONE', #85125 ) ;
#46001=CARTESIAN_POINT ( 'NONE',  ( -85.96599883021772825, -60.00000000000000000, -23.70204626803236891 ) ) ;
#46016=CARTESIAN_POINT ( 'NONE',  ( 33.84593435154630470, -46.42942808596986026, 36.05400579749584011 ) ) ;
#46017=CARTESIAN_POINT ( 'NONE',  ( -21.65942590379792776, -9.659702761776270386E-13, -5.820808985972203864 ) ) ;
#46022=CARTESIAN_POINT ( 'NONE',  ( -80.00000000000000000, -52.00000000000000000, -21.09707704303352926 ) ) ;
#46030=CARTESIAN_POINT ( 'NONE',  ( 92.26607695852590041, -60.00000000000001421, 1.976148175831901721 ) ) ;
#46037=CARTESIAN_POINT ( 'NONE',  ( -82.71132764841163976, -30.00000000000251532, -22.95911469658347315 ) ) ;
#46052=CARTESIAN_POINT ( 'NONE',  ( 78.10417343428038350, -36.02394493292788979, 131.9787684300717387 ) ) ;
#46060=CARTESIAN_POINT ( 'NONE',  ( -112.7923893646043183, -57.67119337860199124, 188.3631819635289446 ) ) ;
#46062=ORIENTED_EDGE ( 'NONE', *, *, #6606, .T. ) ;
#46070=CARTESIAN_POINT ( 'NONE',  ( -40.60913831900013804, -26.58592182782365398, 36.35858900883707889 ) ) ;
#46081=( GEOMETRIC_REPRESENTATION_CONTEXT ( 3 ) GLOBAL_UNCERTAINTY_ASSIGNED_CONTEXT ( ( #13196 ) ) GLOBAL_UNIT_ASSIGNED_CONTEXT ( ( #58303, #34069, #76075 ) ) REPRESENTATION_CONTEXT ( 'NONE', 'WORKASPACE' ) );
#46083=CARTESIAN_POINT ( 'NONE',  ( -50.89201122668178101, -28.75060113657595906, -34.85379606938838037 ) ) ;
#46084=CARTESIAN_POINT ( 'NONE',  ( -67.48283298184769308, -30.00000000000000000, 87.50264991667094705 ) ) ;
#46089=CARTESIAN_POINT ( 'NONE',  ( 101.8486387914506253, -57.63170129011940901, 203.3287309220910970 ) ) ;
#46090=CARTESIAN_POINT ( 'NONE',  ( 62.72655763203226087, -21.76998695923418481, -22.22484975073092883 ) ) ;
#46094=CARTESIAN_POINT ( 'NONE',  ( -53.50820603565255595, -59.99999999999999289, 81.05475964807466482 ) ) ;
#46100=CARTESIAN_POINT ( 'NONE',  ( -86.39008134157819541, -17.29286641282893555, 180.4476020658233892 ) ) ;
#46110=CARTESIAN_POINT ( 'NONE',  ( -85.71891674152472262, -60.21565766106578366, -14.78162960339309251 ) ) ;
#46118=CARTESIAN_POINT ( 'NONE',  ( 3.301606509414339641, -4.285714285714286476, -25.22241582816893413 ) ) ;
#46120=CARTESIAN_POINT ( 'NONE',  ( 94.98342851799053221, -59.99999999999993605, -11.07591208537989580 ) ) ;
#46121=CARTESIAN_POINT ( 'NONE',  ( -76.52857891266238255, -60.31752180720845047, 145.8076901902507814 ) ) ;
#46124=CARTESIAN_POINT ( 'NONE',  ( 72.70482823910218428, -57.66012140098748517, 178.8402823191526636 ) ) ;
#46145=CARTESIAN_POINT ( 'NONE',  ( -68.01705929348101165, -29.99999999999997158, 119.4519777144086703 ) ) ;
#46146=CARTESIAN_POINT ( 'NONE',  ( 26.62717767826400816, -53.38857218945616978, 34.52190694528636783 ) ) ;
#46159=CARTESIAN_POINT ( 'NONE',  ( 83.61123812565043067, -29.99999999999987566, 157.5619696514056614 ) ) ;
#46162=CARTESIAN_POINT ( 'NONE',  ( 81.13473597870090259, -30.00000000000000355, 1.891638132046062015 ) ) ;
#46177=EDGE_LOOP ( 'NONE', ( #77859, #50252, #47802, #55474 ) ) ;
#46180=CARTESIAN_POINT ( 'NONE',  ( -83.34567396899497282, -60.00000000000000711, 190.8012197679059057 ) ) ;
#46181=CARTESIAN_POINT ( 'NONE',  ( 62.91851151839247791, -46.43458783406691026, 83.69961423548066648 ) ) ;
#46185=CARTESIAN_POINT ( 'NONE',  ( -69.28496039471292534, -38.19304130032977440, -31.44853639721581473 ) ) ;
#46191=CARTESIAN_POINT ( 'NONE',  ( -73.50473004590615744, -60.00000000000000000, -24.84693947030580574 ) ) ;
#46201=CARTESIAN_POINT ( 'NONE',  ( 86.63474249928231075, -20.69447793298352423, 184.5529616228748750 ) ) ;
#46211=CARTESIAN_POINT ( 'NONE',  ( -100.3611959579476292, -30.00000000000000000, 157.5875141194946707 ) ) ;
#46213=CARTESIAN_POINT ( 'NONE',  ( 27.93397395458839938, -57.67923204457687802, 44.25413198997598840 ) ) ;
#46218=CARTESIAN_POINT ( 'NONE',  ( 80.00000000000000000, -52.00000000000000000, -21.09707704303352926 ) ) ;
#46221=CARTESIAN_POINT ( 'NONE',  ( 4.750478166817060810, -15.57755379964487297, -35.13231593693921440 ) ) ;
#46224=CARTESIAN_POINT ( 'NONE',  ( -87.35314139720050264, -35.37591848484672141, 188.8839025493173267 ) ) ;
#46227=CARTESIAN_POINT ( 'NONE',  ( -14.45088570581510190, -32.51316581980542963, 29.42462076004476756 ) ) ;
#46228=CARTESIAN_POINT ( 'NONE',  ( -87.00764824667378150, -60.00000000000000711, -8.040170719849857761 ) ) ;
#46256=CARTESIAN_POINT ( 'NONE',  ( -102.5752670435136054, -60.00000000001715250, 203.5310177018276363 ) ) ;
#46259=CARTESIAN_POINT ( 'NONE',  ( 93.40270045618473205, -59.99999999999997868, -17.32733600390682227 ) ) ;
#46263=CARTESIAN_POINT ( 'NONE',  ( -92.59939171350268339, -30.00000000000003908, 50.96567362325610873 ) ) ;
#46264=CARTESIAN_POINT ( 'NONE',  ( 10.30248428635618296, -42.95372659178649144, 31.06077762009211440 ) ) ;
#46267=CARTESIAN_POINT ( 'NONE',  ( -49.64579935860110282, -18.74248632113715374, 43.46943838681040972 ) ) ;
#46278=CARTESIAN_POINT ( 'NONE',  ( 86.44521950301134439, -30.00000000000693490, 197.9828864136313484 ) ) ;
#46282=CARTESIAN_POINT ( 'NONE',  ( 94.54221292022157286, -30.00000000000000000, 191.3208119123549409 ) ) ;
#46296=CARTESIAN_POINT ( 'NONE',  ( 88.56009130522666339, -38.54379311642402683, 200.1470422519182648 ) ) ;
#46299=CARTESIAN_POINT ( 'NONE',  ( 83.67125305368273303, -45.28243862851755352, 10.83020272535897277 ) ) ;
#46315=CARTESIAN_POINT ( 'NONE',  ( -27.02137051350053198, -22.88282787297301368, 37.55591774060851407 ) ) ;
#46320=CARTESIAN_POINT ( 'NONE',  ( 86.40316107272373358, -17.81776296206304977, 175.1963145870509209 ) ) ;
#46326=CARTESIAN_POINT ( 'NONE',  ( 95.57097302797416205, -57.67170133996449977, 37.79358618412610582 ) ) ;
#46334=CARTESIAN_POINT ( 'NONE',  ( 5.451874645059660018, -18.69079845380849747, 35.10559483537603143 ) ) ;
#46335=CARTESIAN_POINT ( 'NONE',  ( 51.87563516386928342, -29.94825904151492324, 49.86669112565530781 ) ) ;
#46344=CARTESIAN_POINT ( 'NONE',  ( -99.18585800602104996, -38.00000000000002132, 133.7838027881280425 ) ) ;
#46350=CARTESIAN_POINT ( 'NONE',  ( -3.173625681713546420, -47.40886789814266677, -34.77114549613931871 ) ) ;
#46353=CARTESIAN_POINT ( 'NONE',  ( 2.499999999999999556, -8.000000000000000000, 17.89626171146327138 ) ) ;
#46360=CARTESIAN_POINT ( 'NONE',  ( -92.40188694392391255, -60.00000000000001421, -12.05163403178383241 ) ) ;
#46368=CARTESIAN_POINT ( 'NONE',  ( -81.18994567851672173, -53.43462853400483681, 175.1505282733661204 ) ) ;
#46379=CARTESIAN_POINT ( 'NONE',  ( -86.45135651325685444, -57.58031178088597812, 202.9040356603995008 ) ) ;
#46386=CARTESIAN_POINT ( 'NONE',  ( 86.84200744108139247, -14.21045842199445630, 3.673032677714961558 ) ) ;
#46387=CARTESIAN_POINT ( 'NONE',  ( -58.28906562901213562, -14.21045842199421294, 78.48115787639689245 ) ) ;
#46388=CARTESIAN_POINT ( 'NONE',  ( -55.72770594965891178, -56.85688678655485262, 69.22944270131350208 ) ) ;
#46393=CARTESIAN_POINT ( 'NONE',  ( -99.16296381929923598, -37.78500836856461831, 191.7250047312669210 ) ) ;
#46395=ADVANCED_FACE ( 'NONE', ( #41345 ), #105550, .F. ) ;
#46406=CARTESIAN_POINT ( 'NONE',  ( 62.03678553237772775, -30.00000000000000000, 72.12393787702889369 ) ) ;
#46411=CARTESIAN_POINT ( 'NONE',  ( -28.67889886441531289, -56.86647899729697997, 35.73133030458858173 ) ) ;
#46414=CARTESIAN_POINT ( 'NONE',  ( 48.33509361711793417, -42.98009849617663036, 49.20160666384766301 ) ) ;
#46418=CARTESIAN_POINT ( 'NONE',  ( -110.5695627141435011, -38.35612508034719781, 181.7239276426034280 ) ) ;
#46420=CARTESIAN_POINT ( 'NONE',  ( 88.64318705069558746, -38.37819253202206227, -18.64980564892555748 ) ) ;
#46429=CARTESIAN_POINT ( 'NONE',  ( 99.55086857495790298, -59.99999999999998579, 202.0088339642364019 ) ) ;
#46436=CARTESIAN_POINT ( 'NONE',  ( -91.36008717904577736, -38.39848663321568267, -9.799652820967615696 ) ) ;
#46448=CARTESIAN_POINT ( 'NONE',  ( 85.40742040225673293, -21.99728074668004396, 165.0038221370978988 ) ) ;
#46487=CARTESIAN_POINT ( 'NONE',  ( -109.0225424287328480, -59.99999999999999289, 136.1364017776934077 ) ) ;
#46492=CARTESIAN_POINT ( 'NONE',  ( -84.60744667541021613, -35.87728133031075828, 178.5872408570687924 ) ) ;
#46497=CARTESIAN_POINT ( 'NONE',  ( -87.44129366413766036, -60.15208811969213087, 34.29055148929769814 ) ) ;
#46503=CARTESIAN_POINT ( 'NONE',  ( 75.52921836606891759, -59.99999999999984368, 193.8580410961210134 ) ) ;
#46504=CARTESIAN_POINT ( 'NONE',  ( -112.0516705497441876, -59.99999999999997868, 140.8505598867089645 ) ) ;
#46505=CARTESIAN_POINT ( 'NONE',  ( -63.26349711878434334, -56.86881976255739346, 90.13409198860577476 ) ) ;
#46508=CARTESIAN_POINT ( 'NONE',  ( 83.38104608230275971, -59.99999999998523492, 202.0684823824225589 ) ) ;
#46519=CARTESIAN_POINT ( 'NONE',  ( -91.91800064235249579, -60.00000000000000000, 8.006063584207543826 ) ) ;
#46535=CARTESIAN_POINT ( 'NONE',  ( 32.49827954884306536, -22.15127066472643591, 30.86793192670277719 ) ) ;
#46536=CARTESIAN_POINT ( 'NONE',  ( 19.43146043914768129, -2.896176105056903703E-12, 11.19959342721819695 ) ) ;
#46551=CARTESIAN_POINT ( 'NONE',  ( 95.81779620297204758, -60.00000000000000711, 54.82891626782047467 ) ) ;
#46557=CARTESIAN_POINT ( 'NONE',  ( -88.16932760057679275, -29.99999999999833022, -16.71407748645461666 ) ) ;
#46571=CARTESIAN_POINT ( 'NONE',  ( 78.75440294992556289, -29.08478707705966215, 129.2257095857447666 ) ) ;
#46577=CARTESIAN_POINT ( 'NONE',  ( -22.17556693859086536, -57.67274538812966256, 42.55074624272938877 ) ) ;
#46588=CARTESIAN_POINT ( 'NONE',  ( -6.501439726548199793, -13.08475520213678678, 32.05172811864072457 ) ) ;
#46601=CARTESIAN_POINT ( 'NONE',  ( -66.59044967886386246, -29.86133635736485559, -22.39369228100312981 ) ) ;
#46602=CARTESIAN_POINT ( 'NONE',  ( -66.46769023514099217, -30.00000000000000711, 84.48792742084529550 ) ) ;
#46605=ORIENTED_EDGE ( 'NONE', *, *, #65444, .T. ) ;
#46608=CARTESIAN_POINT ( 'NONE',  ( 97.17653136007717762, -57.62292585091598340, 204.4293388724284171 ) ) ;
#46614=CARTESIAN_POINT ( 'NONE',  ( -73.91699298931344231, -60.00000000000000000, 171.3787799675980352 ) ) ;
#46618=CARTESIAN_POINT ( 'NONE',  ( -85.16857999255211098, -46.56716161443675617, 187.9269890765743583 ) ) ;
#46622=EDGE_CURVE ( 'NONE', #6703, #37867, #21384, .T. ) ;
#46624=CARTESIAN_POINT ( 'NONE',  ( -83.11894961437765517, -45.25969856680515591, -14.26080704251342368 ) ) ;
#46631=CARTESIAN_POINT ( 'NONE',  ( 25.22241582816893413, -4.285714285714286476, -3.301606509414618973 ) ) ;
#46633=CARTESIAN_POINT ( 'NONE',  ( 93.93995408072316877, -60.00000000000007816, -15.95669063232190155 ) ) ;
#46634=CARTESIAN_POINT ( 'NONE',  ( -81.45673704895914113, -25.62446345033223238, 139.9564592401801804 ) ) ;
#46638=CARTESIAN_POINT ( 'NONE',  ( 100.2630844185923564, -57.62774964585633342, 203.8563738720838785 ) ) ;
#46645=CARTESIAN_POINT ( 'NONE',  ( -106.4266840043012081, -60.15521262700561778, 168.2409215529943083 ) ) ;
#46659=CARTESIAN_POINT ( 'NONE',  ( -57.89926771889555113, -60.00000000000002132, 101.6232698676003139 ) ) ;
#46660=CARTESIAN_POINT ( 'NONE',  ( 29.32191389812840754, -56.85782188410217231, 35.94437315274679889 ) ) ;
#46672=CARTESIAN_POINT ( 'NONE',  ( 68.64488335302139888, -30.00000000000000000, 91.00168987598435422 ) ) ;
#46678=CARTESIAN_POINT ( 'NONE',  ( 81.13835518361752008, -30.00000000000000711, 1.838030729709124733 ) ) ;
#46687=DIRECTION ( 'NONE',  ( 0.000000000000000000, -1.000000000000000000, 0.000000000000000000 ) ) ;
#46697=CARTESIAN_POINT ( 'NONE',  ( 60.37595104056737938, -38.34251102957333757, 97.59079878387926499 ) ) ;
#46701=CARTESIAN_POINT ( 'NONE',  ( 62.79349362354685837, -42.95894226352011458, 81.57106949543961605 ) ) ;
#46711=CARTESIAN_POINT ( 'NONE',  ( -34.74708594651274751, -60.00000000000001421, -34.56281374097226688 ) ) ;
#46715=CARTESIAN_POINT ( 'NONE',  ( 80.00000000000000000, -52.00000000000000000, -21.09707704303352926 ) ) ;
#46718=CARTESIAN_POINT ( 'NONE',  ( 86.30515197242765169, -50.14563283907419589, 191.1575415172119961 ) ) ;
#46727=CARTESIAN_POINT ( 'NONE',  ( 22.57305893494933002, -60.00000000000001421, 40.62150767137644891 ) ) ;
#46729=CARTESIAN_POINT ( 'NONE',  ( -99.80168451951495001, -29.99999999999999645, 186.4053763999687874 ) ) ;
#46733=CARTESIAN_POINT ( 'NONE',  ( 52.17701213820809159, -57.67658653755371745, 83.19312597704137602 ) ) ;
#46743=CARTESIAN_POINT ( 'NONE',  ( -87.30982930919684293, -31.68247253314202538, 188.1765524996390013 ) ) ;
#46748=CARTESIAN_POINT ( 'NONE',  ( -11.16598387641317203, -25.54968478433329437, 28.17206934784134731 ) ) ;
#46750=CARTESIAN_POINT ( 'NONE',  ( -86.57246707375212225, -60.00000000000007105, -11.98479218909116462 ) ) ;
#46758=CARTESIAN_POINT ( 'NONE',  ( 65.85939646271809522, -59.99999999999997158, 121.8062760347599465 ) ) ;
#46763=CARTESIAN_POINT ( 'NONE',  ( 42.10926113833883022, -14.21045842199418452, 45.52176705710515847 ) ) ;
#46779=CARTESIAN_POINT ( 'NONE',  ( -111.9445188126430111, -59.99999999999511147, 192.8163573256921381 ) ) ;
#46782=CARTESIAN_POINT ( 'NONE',  ( 70.42375229793672986, -60.00000000000000000, 143.5773913645265054 ) ) ;
#46786=CARTESIAN_POINT ( 'NONE',  ( -95.73631051900581213, -30.00000000000000000, 71.50198832723137343 ) ) ;
#46787=CARTESIAN_POINT ( 'NONE',  ( 9.411483143886608005, -60.35895712271108948, 33.95384518708878829 ) ) ;
#46790=CARTESIAN_POINT ( 'NONE',  ( -47.02141968940689765, -36.07080552638146997, 45.21624500582201023 ) ) ;
#46800=CARTESIAN_POINT ( 'NONE',  ( 104.9189220841502106, -29.99999999999720046, 195.4889521351916528 ) ) ;
#46805=CARTESIAN_POINT ( 'NONE',  ( 96.68547135186049957, -29.99999999999999289, 191.1807546223255940 ) ) ;
#46817=CARTESIAN_POINT ( 'NONE',  ( 101.1066808782305060, -38.45692254263880727, 200.1018791781253015 ) ) ;
#46819=CARTESIAN_POINT ( 'NONE',  ( 84.49332496811159388, -45.28622975171930420, -7.233042096027321399 ) ) ;
#46820=CARTESIAN_POINT ( 'NONE',  ( 81.87243278912710309, -37.99999999999996447, 157.2857030484634606 ) ) ;
#46836=CARTESIAN_POINT ( 'NONE',  ( -29.18624803973531456, -31.90962671462940747, 40.10543586240345348 ) ) ;
#46841=CARTESIAN_POINT ( 'NONE',  ( 84.26380273736219806, -50.17260406813100104, 187.6069518689174345 ) ) ;
#46845=CARTESIAN_POINT ( 'NONE',  ( 93.83727737954620807, -57.67472858147435488, 11.15358949908543984 ) ) ;
#46853=CARTESIAN_POINT ( 'NONE',  ( 15.13815838105152167, -22.76677273537127988, 35.95324695099370871 ) ) ;
#46861=CARTESIAN_POINT ( 'NONE',  ( -48.11205635439868900, -35.42149170368610811, -28.26377718570788744 ) ) ;
#46869=CARTESIAN_POINT ( 'NONE',  ( -25.59063492799110762, -47.40907061882889195, -33.48575065794680938 ) ) ;
#46875=CARTESIAN_POINT ( 'NONE',  ( -92.66121602952624414, -59.99999999999999289, -3.920577165534929964 ) ) ;
#46881=CARTESIAN_POINT ( 'NONE',  ( -80.86179060450608347, -46.44313512650642650, 160.9680050460582663 ) ) ;
#46894=CARTESIAN_POINT ( 'NONE',  ( -79.30961931381874308, -57.50609382800362823, 198.1725500959836666 ) ) ;
#46900=CARTESIAN_POINT ( 'NONE',  ( 94.98342851799053221, -59.99999999999993605, -11.07591208537989580 ) ) ;
#46902=CARTESIAN_POINT ( 'NONE',  ( -45.38252603333997826, -14.21045842199430354, 49.92404905378138125 ) ) ;
#46904=CARTESIAN_POINT ( 'NONE',  ( -55.54604552563809250, -42.97054307439768905, 62.92721107680804238 ) ) ;
#46908=CARTESIAN_POINT ( 'NONE',  ( -100.0299451350468161, -37.81394507940942162, 190.5172735492119216 ) ) ;
#46913=CARTESIAN_POINT ( 'NONE',  ( 110.5955579697139939, -38.35611409724038623, 181.9650721577582715 ) ) ;
#46926=CARTESIAN_POINT ( 'NONE',  ( 49.42319345579174694, -49.90093656948970846, 53.22847127201153938 ) ) ;
#46930=CARTESIAN_POINT ( 'NONE',  ( -109.2921535902703596, -38.35623054118988762, 189.1334433219931270 ) ) ;
#46932=CARTESIAN_POINT ( 'NONE',  ( 89.49617078063555198, -38.38859236215838422, -17.12117333382422402 ) ) ;
#46942=CARTESIAN_POINT ( 'NONE',  ( 99.41552838720369323, -60.00000000000000711, 202.0437798234699471 ) ) ;
#46945=CARTESIAN_POINT ( 'NONE',  ( 59.32604057062135183, -18.65621327707388488, 61.11290863963116493 ) ) ;
#46950=CARTESIAN_POINT ( 'NONE',  ( -92.04013207032886612, -38.35472338211468468, 35.72301976503869270 ) ) ;
#46961=CARTESIAN_POINT ( 'NONE',  ( 83.71331492665446206, -39.45954491553350607, 176.1762179413915703 ) ) ;
#46977=CARTESIAN_POINT ( 'NONE',  ( -80.94296027622181100, -29.99999999999999289, 19.76001105705952909 ) ) ;
#46980=CARTESIAN_POINT ( 'NONE',  ( -3.672464763049774796E-06, -18.02989419364509516, 35.00496915990722613 ) ) ;
#47002=CARTESIAN_POINT ( 'NONE',  ( -112.1929976763688188, -60.00000000000002132, 169.7340247815773182 ) ) ;
#47007=CARTESIAN_POINT ( 'NONE',  ( -83.95400002616862878, -35.96245533400819738, 173.2978818052737893 ) ) ;
#47014=CARTESIAN_POINT ( 'NONE',  ( -84.89766952350503004, -52.70258195973874393, 12.33435398003158667 ) ) ;
#47019=CARTESIAN_POINT ( 'NONE',  ( 99.17368802223589341, -30.00000000000007816, 199.4946398670649046 ) ) ;
#47020=CARTESIAN_POINT ( 'NONE',  ( -94.42208465491292202, -30.00000000000002132, 63.29659460224121403 ) ) ;
#47021=CARTESIAN_POINT ( 'NONE',  ( -63.03672031330412295, -49.91572035676450980, 85.83718877777337752 ) ) ;
#47024=CARTESIAN_POINT ( 'NONE',  ( 84.45168914632041890, -60.00000000002949463, 202.6255676462649831 ) ) ;
#47026=CARTESIAN_POINT ( 'NONE',  ( 1.020029634130620755, -56.87793866973930079, 33.36930640455891961 ) ) ;
#47037=CARTESIAN_POINT ( 'NONE',  ( -112.2540373697807325, -60.00000000000002842, 172.5324719884098101 ) ) ;
#47048=CARTESIAN_POINT ( 'NONE',  ( -35.24657627339123422, -49.89919647416704862, 37.46166166223662941 ) ) ;
#47050=CARTESIAN_POINT ( 'NONE',  ( 34.03145487526279567, -49.89646066257007817, 36.80204845843336869 ) ) ;
#47051=CARTESIAN_POINT ( 'NONE',  ( 2.910977163136224011, -8.673617379884035472E-16, 22.23822744035697241 ) ) ;
#47053=ORIENTED_EDGE ( 'NONE', *, *, #71644, .F. ) ;
#47055=CARTESIAN_POINT ( 'NONE',  ( -67.72166853775303252, -38.33445515793012248, 124.3162426451314957 ) ) ;
#47064=CARTESIAN_POINT ( 'NONE',  ( 98.00817729099017583, -60.00000000000000000, 68.97682032673503727 ) ) ;
#47073=CARTESIAN_POINT ( 'NONE',  ( -89.74886674459079927, -29.99999999998750866, -11.85434269913620220 ) ) ;
#47086=B_SPLINE_CURVE_WITH_KNOTS ( 'NONE', 1,
 ( #78851, #6020, #70774 ),
 .UNSPECIFIED., .F., .F.,
 ( 2, 1, 2 ),
 ( 0.07762659913847776150, 1.000000000000000000, 1.289432564806017645 ),
 .UNSPECIFIED. ) ;
#47089=CARTESIAN_POINT ( 'NONE',  ( 77.77861324456983994, -39.49362688318783654, 133.3549205718891812 ) ) ;
#47095=CARTESIAN_POINT ( 'NONE',  ( -35.27718283856832926, -57.69548877625971528, 49.41932622563938793 ) ) ;
#47101=CYLINDRICAL_SURFACE ( 'NONE', #37227, 2.000000000000001776 ) ;
#47106=CARTESIAN_POINT ( 'NONE',  ( -19.64607334565684837, -16.95621533664098735, 31.48343634207214592 ) ) ;
#47121=CARTESIAN_POINT ( 'NONE',  ( -21.69933433976674308, -26.44462722771605101, -38.46517870091099667 ) ) ;
#47122=CARTESIAN_POINT ( 'NONE',  ( -81.10745130575307371, -30.00000000000000355, 140.6132671042336142 ) ) ;
#47127=CARTESIAN_POINT ( 'NONE',  ( 96.51954077749346084, -57.62215758448405722, 204.4834013014043137 ) ) ;
#47134=CARTESIAN_POINT ( 'NONE',  ( -73.02673009549289418, -60.00000000000000000, 162.7051491287812723 ) ) ;
#47139=CARTESIAN_POINT ( 'NONE',  ( -86.19855657701549490, -28.27924645610051613, 183.2269261606164434 ) ) ;
#47154=CARTESIAN_POINT ( 'NONE',  ( -19.43146043915540488, 9.659702761776270386E-13, -11.19959342721046980 ) ) ;
#47156=CARTESIAN_POINT ( 'NONE',  ( 86.58060678326373250, -14.21045842199439235, 15.94037124058900901 ) ) ;
#47157=CARTESIAN_POINT ( 'NONE',  ( -81.07615537427551544, -22.15355340867505518, 134.4957932511888714 ) ) ;
#47159=CARTESIAN_POINT ( 'NONE',  ( 8.309829428344436053, -30.00000000000008527, 36.98670151680749996 ) ) ;
#47160=CARTESIAN_POINT ( 'NONE',  ( 69.36244709154269117, -57.68278289274119430, 149.4242506819062442 ) ) ;
#47167=CARTESIAN_POINT ( 'NONE',  ( -102.4400663919250292, -45.26551116408855790, 149.2539637247840858 ) ) ;
#47175=ORIENTED_EDGE ( 'NONE', *, *, #81707, .F. ) ;
#47177=CARTESIAN_POINT ( 'NONE',  ( -4.090533018665307274, -14.21045842199441722, 34.36071901318091903 ) ) ;
#47178=CARTESIAN_POINT ( 'NONE',  ( 26.74761531504731238, -25.57238952923795594, 29.74515757345933054 ) ) ;
#47193=CARTESIAN_POINT ( 'NONE',  ( 3.334507628320575900, -60.00000000000000711, -42.61916129529188879 ) ) ;
#47219=CARTESIAN_POINT ( 'NONE',  ( 64.08887429804100577, -22.10312605409954756, 74.71187393261132570 ) ) ;
#47221=ORIENTED_EDGE ( 'NONE', *, *, #85837, .F. ) ;
#47232=CARTESIAN_POINT ( 'NONE',  ( -7.105115778984035124, -60.00000000000002842, -36.77403448916896167 ) ) ;
#47234=B_SPLINE_CURVE_WITH_KNOTS ( 'NONE', 3,
 ( #67829, #19339, #20404, #86169, #53249, #18788, #19863, #43557, #11165, #44635, #93171, #27420, #51092, #101788, #51636, #44093, #84554, #26881, #76979, #59754, #60299, #84012, #85081, #60819, #68913, #93709, #10638, #76438, #43028, #75917, #3636, #36572, #69439, #2550 ),
 .UNSPECIFIED., .F., .F.,
 ( 4, 2, 2, 2, 2, 2, 2, 2, 2, 2, 2, 2, 2, 2, 2, 2, 4 ),
 ( 0.000000000000000000, 0.003935531903598469411, 0.007871063807196938822, 0.01180659571079540997, 0.01377436166259464988, 0.01574212761439389152, 0.02361319142159084422, 0.02754872332518931363, 0.03148425522878778998, 0.03935531903598470799, 0.04329085093958316699, 0.04722638284318161905, 0.05116191474678007112, 0.05509744665037853012, 0.05903297855397698218, 0.06100074450577621515, 0.06296851045757544119 ),
 .UNSPECIFIED. ) ;
#47237=CARTESIAN_POINT ( 'NONE',  ( 86.65396412451504204, -42.80459859885080220, 189.4102807469302832 ) ) ;
#47246=CARTESIAN_POINT ( 'NONE',  ( 26.67261969005227940, -60.00000000000000000, 41.66386289415872568 ) ) ;
#47247=CARTESIAN_POINT ( 'NONE',  ( -97.63767121502735336, -29.99999999999999645, 134.9972035148113605 ) ) ;
#47251=CARTESIAN_POINT ( 'NONE',  ( 40.54584476168707852, -57.69097569962055161, 56.57753608882419627 ) ) ;
#47258=CARTESIAN_POINT ( 'NONE',  ( -16.91076490362186036, -59.99999999999998579, 39.91562613777458068 ) ) ;
#47268=CARTESIAN_POINT ( 'NONE',  ( -13.17713355742532322, -18.58679757000995281, 27.05833942353407551 ) ) ;
#47269=CARTESIAN_POINT ( 'NONE',  ( -86.94432264429229917, -59.99999999999998579, 29.30728585821892551 ) ) ;
#47277=CARTESIAN_POINT ( 'NONE',  ( 60.68637083643779562, -60.00000000000002132, 102.7753246229686113 ) ) ;
#47283=( NAMED_UNIT ( * ) SI_UNIT ( $, .STERADIAN. ) SOLID_ANGLE_UNIT ( ) );
#47298=AXIS2_PLACEMENT_3D ( 'NONE', #100689, #17669, #41928 ) ;
#47299=CARTESIAN_POINT ( 'NONE',  ( -103.3252443258257216, -59.99999999999994316, 203.1850994544522564 ) ) ;
#47301=CARTESIAN_POINT ( 'NONE',  ( 79.80566310147598585, -59.99999999999998579, 195.7472193146226402 ) ) ;
#47304=CARTESIAN_POINT ( 'NONE',  ( -114.4520492995273315, -60.00000000000003553, 166.3968728284598342 ) ) ;
#47305=CARTESIAN_POINT ( 'NONE',  ( 10.04875798505854512, -18.58642205010649562, 26.99592638574074144 ) ) ;
#47306=CARTESIAN_POINT ( 'NONE',  ( 82.68768327601632961, -37.99999999999995026, 21.01035113837339097 ) ) ;
#47309=CARTESIAN_POINT ( 'NONE',  ( -45.35675342690321088, -25.70246126498986428, 40.33334816179175419 ) ) ;
#47320=CARTESIAN_POINT ( 'NONE',  ( 109.2084914459248495, -29.99999999998984634, 181.8260726147819071 ) ) ;
#47324=CARTESIAN_POINT ( 'NONE',  ( 92.38157122146077427, -30.00000000000000355, 102.4062337837748800 ) ) ;
#47331=DIRECTION ( 'NONE',  ( 0.000000000000000000, 0.000000000000000000, 1.000000000000000000 ) ) ;
#47339=CARTESIAN_POINT ( 'NONE',  ( 96.52417567451942659, -38.48283943534769946, 201.1700310018051994 ) ) ;
#47342=CARTESIAN_POINT ( 'NONE',  ( 82.90087968821347886, -37.85046927419193707, 0.5094595297241235610 ) ) ;
#47343=CARTESIAN_POINT ( 'NONE',  ( 83.62068454613667257, -38.00000000000004263, 173.3489829705700060 ) ) ;
#47365=CARTESIAN_POINT ( 'NONE',  ( 28.52923163747771440, -23.57397691714684385, 38.13648777926081834 ) ) ;
#47367=CARTESIAN_POINT ( 'NONE',  ( 84.69674785225238622, -46.56892218208203360, 186.7899396118458810 ) ) ;
#47371=CARTESIAN_POINT ( 'NONE',  ( 94.19505752079862759, -57.67256688133579701, 22.60860429288029749 ) ) ;
#47377=B_SPLINE_CURVE_WITH_KNOTS ( 'NONE', 3,
 ( #99319, #10837, #50764, #25493, #34648, #101472, #42698, #58350, #2217, #84225, #100398, #59432, #83156, #43236, #42162, #68589, #26041, #67518, #8730, #84756, #26560, #91270, #35167, #90724, #9252, #2760, #17381, #58900, #35711, #92295, #50255, #68034, #75043, #1141, #34116, #27624, #100928, #59975, #92836, #91790, #16838, #1693, #49720, #19000, #43757, #10320, #66987, #41638, #51843, #75594, #99868, #18449, #74521, #51303, #76649, #85284, #103589, #28678, #5429, #4903, #12441, #11372 ),
 .UNSPECIFIED., .F., .F.,
 ( 4, 2, 2, 2, 2, 2, 2, 2, 2, 2, 2, 2, 2, 2, 2, 2, 2, 2, 2, 2, 2, 2, 2, 2, 2, 2, 2, 2, 2, 2, 4 ),
 ( 0.5710235574187877416, 0.5770410422503359227, 0.5830585270818841037, 0.5890760119134322848, 0.5920847543292063753, 0.5950934967449803548, 0.6011109815765285358, 0.6026153527844155811, 0.6041197239923026263, 0.6071284664080768279, 0.6131459512396248979, 0.6146503224475119431, 0.6161546936553989884, 0.6191634360711730789, 0.6251809209027212599, 0.6311984057342694410, 0.6372158905658175110, 0.6432333753973656920, 0.6552683450604619431, 0.6673033147235581941, 0.6913732540497506962, 0.7034082237128469473, 0.7154431933759433093, 0.7274781630390395604, 0.7395131327021358114, 0.7455306175336839924, 0.7515481023652321735, 0.7545568447810062640, 0.7575655871967803545, 0.7605743296125544450, 0.7635830720283285356 ),
 .UNSPECIFIED. ) ;
#47387=CARTESIAN_POINT ( 'NONE',  ( -83.28021094808033808, -38.00000000000000000, -7.973042742588115850 ) ) ;
#47394=CARTESIAN_POINT ( 'NONE',  ( -51.46469236758235155, -60.22827249275542272, -31.80550166486139574 ) ) ;
#47401=CARTESIAN_POINT ( 'NONE',  ( -92.74294554908810539, -60.00000000000001421, -7.911394269966801396 ) ) ;
#47403=CARTESIAN_POINT ( 'NONE',  ( 39.57197012660297730, -33.18875763605801410, -29.36643390136424969 ) ) ;
#47406=CARTESIAN_POINT ( 'NONE',  ( 97.47947159951426954, -52.81402158103271205, 195.2340248519632553 ) ) ;
#47410=CARTESIAN_POINT ( 'NONE',  ( -83.81111989978313659, -29.06180828734868626, 160.7833297484586126 ) ) ;
#47422=CARTESIAN_POINT ( 'NONE',  ( -85.03051761340829273, -57.56200303720294897, 202.2882931814572487 ) ) ;
#47427=CARTESIAN_POINT ( 'NONE',  ( 75.59946810849663734, -59.99999999999992895, -32.85428466877961284 ) ) ;
#47429=CARTESIAN_POINT ( 'NONE',  ( -66.01875947964627755, -14.21045842199442077, 101.7785962432973292 ) ) ;
#47430=EDGE_CURVE ( 'NONE', #53605, #71336, #98319, .T. ) ;
#47431=CARTESIAN_POINT ( 'NONE',  ( -53.63040634117179906, -18.70038625127083165, 49.64862236185882693 ) ) ;
#47435=CARTESIAN_POINT ( 'NONE',  ( -99.02822291621761508, -37.77734143312120807, 191.8549729512566273 ) ) ;
#47439=CARTESIAN_POINT ( 'NONE',  ( 89.92042692463260778, -38.39514772492996286, -16.19348958354982670 ) ) ;
#47445=CARTESIAN_POINT ( 'NONE',  ( 66.15617483897442241, -29.99999999999999645, 83.57477076473479372 ) ) ;
#47453=CARTESIAN_POINT ( 'NONE',  ( 48.68234789899833714, -60.28324891123607898, 55.32515784904787637 ) ) ;
#47457=CARTESIAN_POINT ( 'NONE',  ( -108.7075558750168227, -38.35682683513768865, 191.0385089548209976 ) ) ;
#47459=CARTESIAN_POINT ( 'NONE',  ( 84.99785917221272769, -38.35913927195756656, -22.84962175036736909 ) ) ;
#47463=CARTESIAN_POINT ( 'NONE',  ( 101.6986830034126683, -37.84844073324973834, 153.9942977854028072 ) ) ;
#47469=CARTESIAN_POINT ( 'NONE',  ( 95.19103829490188673, -60.00000000000000000, 202.5701353115400991 ) ) ;
#47470=AXIS2_PLACEMENT_3D ( 'NONE', #90783, #17962, #18502 ) ;
#47473=CARTESIAN_POINT ( 'NONE',  ( 58.48759157769109862, -18.66117102831294261, 59.19987231648309489 ) ) ;
#47478=CARTESIAN_POINT ( 'NONE',  ( -102.4962415325779546, -38.43804299320050433, 199.4167516955215547 ) ) ;
#47491=CARTESIAN_POINT ( 'NONE',  ( 86.03557063178290321, -18.41209965610634214, 166.1552846382974451 ) ) ;
#47494=ORIENTED_EDGE ( 'NONE', *, *, #87986, .F. ) ;
#47509=CARTESIAN_POINT ( 'NONE',  ( -4.358015154622025378, -18.45760210153450487, 35.06886539972598626 ) ) ;
#47533=CARTESIAN_POINT ( 'NONE',  ( -107.3255816732216203, -60.00000000000000000, 124.7109082821343691 ) ) ;
#47538=CARTESIAN_POINT ( 'NONE',  ( -84.88372816773981810, -28.91961114234488761, 171.4482036657654760 ) ) ;
#47543=CARTESIAN_POINT ( 'NONE',  ( -84.22203528576365272, -45.26556005254958848, 26.09078575504823405 ) ) ;
#47550=CARTESIAN_POINT ( 'NONE',  ( 107.3649583438541271, -29.99999999999998579, 190.7484263893222192 ) ) ;
#47552=CARTESIAN_POINT ( 'NONE',  ( -107.3073691194147443, -59.99999999999994316, 109.8427349246714613 ) ) ;
#47553=CARTESIAN_POINT ( 'NONE',  ( -63.78795251116700626, -32.53250583283151798, 79.11474259739455306 ) ) ;
#47556=CARTESIAN_POINT ( 'NONE',  ( 71.86476928594946401, -59.99999999997545075, 174.6312134016923778 ) ) ;
#47567=CARTESIAN_POINT ( 'NONE',  ( -103.1916873065907652, -59.99999999999998579, 200.5090983659188169 ) ) ;
#47577=CARTESIAN_POINT ( 'NONE',  ( 100.1590866098448629, -60.00000000000002842, 195.6606663522350118 ) ) ;
#47578=CARTESIAN_POINT ( 'NONE',  ( -37.18009251321940667, -22.20738402244377951, 33.02752658207509739 ) ) ;
#47580=CARTESIAN_POINT ( 'NONE',  ( 36.98729712581772588, -18.74392476602471547, 32.19149500795003860 ) ) ;
#47581=CARTESIAN_POINT ( 'NONE',  ( -2.227375807148842313, -1.734723475976807094E-15, -17.01589776168603407 ) ) ;
#47584=CARTESIAN_POINT ( 'NONE',  ( -75.63917042766036047, -38.35856568444517478, 175.4764248205101467 ) ) ;
#47596=CARTESIAN_POINT ( 'NONE',  ( 94.76699447141982091, -60.00000000000000711, 47.33153769421498680 ) ) ;
#47602=CARTESIAN_POINT ( 'NONE',  ( -76.52889981649941831, -29.99999999999171152, -26.83830997453001288 ) ) ;
#47615=CARTESIAN_POINT ( 'NONE',  ( 80.60767953697174448, -39.49744972330380222, 149.7863415175808086 ) ) ;
#47622=CARTESIAN_POINT ( 'NONE',  ( -38.25590479036647906, -57.69571505705692260, 53.01769594715635492 ) ) ;
#47637=AXIS2_PLACEMENT_3D ( 'NONE', #69726, #70781, #103676 ) ;
#47656=CARTESIAN_POINT ( 'NONE',  ( 98.66545750752896993, -57.62490083480406611, 204.2383384864311040 ) ) ;
#47657=CARTESIAN_POINT ( 'NONE',  ( 72.65333306677447922, -47.40884695679693550, -22.95069231350860406 ) ) ;
#47661=CARTESIAN_POINT ( 'NONE',  ( -74.33330251140726830, -59.99999999999999289, 175.5315321299100901 ) ) ;
#47667=CARTESIAN_POINT ( 'NONE',  ( -84.67480933483595607, -50.19323684364298543, 188.5573917989278243 ) ) ;
#47678=CARTESIAN_POINT ( 'NONE',  ( -16.57301948836873251, -1.734723475976807094E-15, -4.453875240786733691 ) ) ;
#47681=CARTESIAN_POINT ( 'NONE',  ( 89.21410497458975897, -29.99999999999997513, 9.589292377912048693 ) ) ;
#47682=CARTESIAN_POINT ( 'NONE',  ( -79.72895134235473336, -18.67626752654355116, 125.0978594537113793 ) ) ;
#47684=CARTESIAN_POINT ( 'NONE',  ( 46.52147948847155590, -60.00000000000000000, 69.35914673975356948 ) ) ;
#47686=CARTESIAN_POINT ( 'NONE',  ( 74.66765723773309560, -57.58775781631299395, 189.6186382585397894 ) ) ;
#47695=CARTESIAN_POINT ( 'NONE',  ( -103.5544495963808913, -45.26538628390532892, 161.0521102863736473 ) ) ;
#47707=CARTESIAN_POINT ( 'NONE',  ( 30.31142205078400309, -25.59748758447105743, 30.73189178319717740 ) ) ;
#47719=ORIENTED_EDGE ( 'NONE', *, *, #5587, .F. ) ;
#47720=EDGE_CURVE ( 'NONE', #81108, #18895, #95249, .T. ) ;
#47722=CARTESIAN_POINT ( 'NONE',  ( 89.93595484110375082, -30.00000000000008882, 189.8158637124989525 ) ) ;
#47747=CARTESIAN_POINT ( 'NONE',  ( 69.23840392680455125, -29.06012857090818002, 93.48888568600646920 ) ) ;
#47759=CARTESIAN_POINT ( 'NONE',  ( 86.41025636765816387, -53.78809460387265773, 192.3578921812466831 ) ) ;
#47767=CARTESIAN_POINT ( 'NONE',  ( 33.15869397692891596, -60.00000000000001421, 44.95690229595550136 ) ) ;
#47768=CARTESIAN_POINT ( 'NONE',  ( -91.37582729904079315, -29.99999999999999645, 190.6461204354261270 ) ) ;
#47773=CARTESIAN_POINT ( 'NONE',  ( 52.18313839522158304, -57.67658158394408474, 83.21036237335373187 ) ) ;
#47779=CARTESIAN_POINT ( 'NONE',  ( -8.335663544843971096, -60.00000000000001421, 39.63523635428892788 ) ) ;
#47784=CARTESIAN_POINT ( 'NONE',  ( -85.99000842721079607, -57.44596555551432715, 193.1195461926678831 ) ) ;
#47787=CARTESIAN_POINT ( 'NONE',  ( -14.61251300444708789, -42.95777107779967707, 31.17356395705397532 ) ) ;
#47798=CARTESIAN_POINT ( 'NONE',  ( 64.13793778944149437, -60.00000000000001421, 114.9505950962200984 ) ) ;
#47802=ORIENTED_EDGE ( 'NONE', *, *, #43782, .T. ) ;
#47805=CARTESIAN_POINT ( 'NONE',  ( 35.98705420554111356, -30.00000000000000355, 43.73599804831894033 ) ) ;
#47809=STYLED_ITEM ( 'NONE', ( #82580 ), #102368 ) ;
#47819=CARTESIAN_POINT ( 'NONE',  ( -92.71863003665913538, -60.00000000000486722, 204.8833018290717405 ) ) ;
#47821=CARTESIAN_POINT ( 'NONE',  ( 87.50920607001037865, -60.00000000000000000, 201.2124321505406783 ) ) ;
#47824=CARTESIAN_POINT ( 'NONE',  ( -106.2142031390243488, -14.21045842199427867, 184.2056779555663582 ) ) ;
#47825=CARTESIAN_POINT ( 'NONE',  ( 8.025689105212569174, -22.06735756619769262, 27.56016688982502316 ) ) ;
#47827=CARTESIAN_POINT ( 'NONE',  ( 101.4591949053181850, -38.00000000000000711, 151.1652513569568441 ) ) ;
#47830=CARTESIAN_POINT ( 'NONE',  ( -46.27878468182461091, -36.07324587582905195, 44.25640521768517743 ) ) ;
#47842=CARTESIAN_POINT ( 'NONE',  ( 103.4783626894312363, -29.99999999999954170, 197.0598667280581253 ) ) ;
#47846=CARTESIAN_POINT ( 'NONE',  ( 94.04323099157159049, -30.00000000000000000, 112.2223748969013002 ) ) ;
#47862=CARTESIAN_POINT ( 'NONE',  ( 86.25238321531877261, -38.62902508625902698, 199.1927999813084398 ) ) ;
#47864=CARTESIAN_POINT ( 'NONE',  ( 83.26452227477953727, -37.81628373900264961, -6.777217245169891768 ) ) ;
#47865=CARTESIAN_POINT ( 'NONE',  ( 86.35483434040011730, -38.00000000000002842, 187.4088181658582357 ) ) ;
#47878=DIRECTION ( 'NONE',  ( 1.000000000000000000, 0.000000000000000000, 0.000000000000000000 ) ) ;
#47881=CARTESIAN_POINT ( 'NONE',  ( 87.14793098496349444, -38.00000000001091394, 189.0872956505646414 ) ) ;
#47883=CARTESIAN_POINT ( 'NONE',  ( 23.50650070960475091, -28.00707568674144810, 37.72505729721246581 ) ) ;
#47886=CARTESIAN_POINT ( 'NONE',  ( 84.86246358733825446, -42.95551756591085990, 185.2907791911740105 ) ) ;
#47888=VECTOR ( 'NONE', #71725, 1000.000000000000000 ) ;
#47892=CARTESIAN_POINT ( 'NONE',  ( 93.83829941600403401, -57.67411610650783871, 13.07459177711520937 ) ) ;
#47898=CARTESIAN_POINT ( 'NONE',  ( -58.10800684958269358, -37.99999999999999289, 66.73714291064102611 ) ) ;
#47910=CARTESIAN_POINT ( 'NONE',  ( -83.30746707032521670, -37.99999999999999289, -6.324111559126246895 ) ) ;
#47916=CARTESIAN_POINT ( 'NONE',  ( -31.16334379427010859, -21.77022426646608366, -28.58710611576712068 ) ) ;
#47921=EDGE_LOOP ( 'NONE', ( #96345, #52838, #60458, #99056, #61463, #24458 ) ) ;
#47925=CARTESIAN_POINT ( 'NONE',  ( -92.37071800302067004, -60.00000000000000000, 0.5499908112625699896 ) ) ;
#47930=CARTESIAN_POINT ( 'NONE',  ( 98.06839251664504786, -45.26758170594511199, 193.7448716299151954 ) ) ;
#47933=CARTESIAN_POINT ( 'NONE',  ( -80.45966997233487916, -53.39463783365103922, 168.0513147114344861 ) ) ;
#47945=CARTESIAN_POINT ( 'NONE',  ( -76.22482491972903063, -57.54008153533397518, 193.6369246664269781 ) ) ;
#47950=CARTESIAN_POINT ( 'NONE',  ( -2.727034095388735757, -14.21045842199435860, -37.36840973699904822 ) ) ;
#47951=CARTESIAN_POINT ( 'NONE',  ( 6.243930039575695118E-05, -60.00000000000000000, 42.00000000000000711 ) ) ;
#47953=CARTESIAN_POINT ( 'NONE',  ( -51.44312181940702544, -53.37577997994360146, 58.22593905968521000 ) ) ;
#47957=CARTESIAN_POINT ( 'NONE',  ( -100.7084081391693076, -60.27494346565931238, 195.3574602886342007 ) ) ;
#47962=CARTESIAN_POINT ( 'NONE',  ( 106.5345532972019953, -38.36891180064773721, 195.6038345425867817 ) ) ;
#47966=CARTESIAN_POINT ( 'NONE',  ( 84.65202442565809804, -30.00000000000000000, 167.0145454972611390 ) ) ;
#47977=CARTESIAN_POINT ( 'NONE',  ( 49.28648764494346324, -56.82522282173033545, 55.29322352173170430 ) ) ;
#47981=CARTESIAN_POINT ( 'NONE',  ( -109.5635314813388845, -38.35614484551107495, 188.1144259547864692 ) ) ;
#47983=CARTESIAN_POINT ( 'NONE',  ( 92.04832879187223682, -38.35408280619313359, 35.20174921906648535 ) ) ;
#47987=CARTESIAN_POINT ( 'NONE',  ( 103.3874261300967135, -45.28277477373939064, 158.7075077770578559 ) ) ;
#47993=CARTESIAN_POINT ( 'NONE',  ( 100.0145631082506128, -60.00000000000001421, 201.8807573114297895 ) ) ;
#47998=CARTESIAN_POINT ( 'NONE',  ( 56.87964969553961225, -49.90805661006463367, 69.03665511646475750 ) ) ;
#48003=CARTESIAN_POINT ( 'NONE',  ( -98.56958724828976415, -38.35590500345170994, 80.52781705630614795 ) ) ;
#48013=CARTESIAN_POINT ( 'NONE',  ( 84.06432143690391001, -35.94819419959944895, 174.2791522909043351 ) ) ;
#48055=CARTESIAN_POINT ( 'NONE',  ( -106.5960259156999541, -59.99999999999999289, 120.1111938281909914 ) ) ;
#48065=CARTESIAN_POINT ( 'NONE',  ( -82.34390938163903684, -50.00253640360821095, 179.4910488424855828 ) ) ;
#48076=CARTESIAN_POINT ( 'NONE',  ( 105.8555784348092885, -14.21045842199437637, 186.2209013957143782 ) ) ;
#48077=CARTESIAN_POINT ( 'NONE',  ( -113.7193438732989961, -60.00000000000000000, 185.6039524652145474 ) ) ;
#48078=CARTESIAN_POINT ( 'NONE',  ( -62.38895926707620987, -32.53592809500086247, 75.23077026582143390 ) ) ;
#48081=CARTESIAN_POINT ( 'NONE',  ( 94.83079671683508138, -59.99999999999024425, -0.6452062745601389038 ) ) ;
#48084=CARTESIAN_POINT ( 'NONE',  ( 9.180358464578489104E-06, -29.02944131831594632, 28.72789017932170097 ) ) ;
#48093=CARTESIAN_POINT ( 'NONE',  ( -97.54655262679582961, -60.00000000000001421, 202.4652287849740446 ) ) ;
#48103=CARTESIAN_POINT ( 'NONE',  ( 98.85644268318139893, -60.00000000000000000, 196.2379177705476252 ) ) ;
#48104=CARTESIAN_POINT ( 'NONE',  ( -31.90879697719113750, -22.14461511112060066, 30.64637690011016247 ) ) ;
#48106=CARTESIAN_POINT ( 'NONE',  ( 41.45969462480130829, -46.43236721762693975, 41.56346318067672030 ) ) ;
#48107=CARTESIAN_POINT ( 'NONE',  ( 4.453875240780039491, -1.734723475976807094E-15, 16.57301948837323380 ) ) ;
#48113=CARTESIAN_POINT ( 'NONE',  ( -67.66808814965415309, -38.33453704423400410, 124.0875110596533375 ) ) ;
#48125=CARTESIAN_POINT ( 'NONE',  ( 94.01771362528924669, -60.00000000000000711, 41.47442360232466285 ) ) ;
#48132=CARTESIAN_POINT ( 'NONE',  ( -89.18872655255631798, -29.99999999994696864, 13.78793652477736842 ) ) ;
#48142=ORIENTED_EDGE ( 'NONE', *, *, #96705, .F. ) ;
#48146=CARTESIAN_POINT ( 'NONE',  ( 83.77344519934696621, -22.14388846856150650, 150.6883876448328010 ) ) ;
#48154=CARTESIAN_POINT ( 'NONE',  ( -37.03244656124025624, -57.69633701093174949, 51.43040253561569131 ) ) ;
#48166=CARTESIAN_POINT ( 'NONE',  ( -19.51791082181538783, -16.90378180463951452, 31.48562786591203988 ) ) ;
#48177=CARTESIAN_POINT ( 'NONE',  ( -69.28690090100495524, -38.19429424212712121, -31.44801709845743787 ) ) ;
#48184=CARTESIAN_POINT ( 'NONE',  ( 101.3723521623251145, -57.63037166266066436, 203.5050614878415729 ) ) ;
#48190=CARTESIAN_POINT ( 'NONE',  ( -73.04440972101423313, -60.00000000000000711, 162.8656828868589912 ) ) ;
#48196=CARTESIAN_POINT ( 'NONE',  ( -85.23003832000186719, -39.32874488855976125, 184.5462598398625005 ) ) ;
#48203=CARTESIAN_POINT ( 'NONE',  ( -85.19250957274734048, -60.20006492606454174, -15.74789945096170207 ) ) ;
#48209=CARTESIAN_POINT ( 'NONE',  ( -8.569529079651847070, -1.734723475976807094E-15, 14.86825985028331942 ) ) ;
#48212=CARTESIAN_POINT ( 'NONE',  ( 94.49477393579812201, -60.00000000000003553, -13.88944369105108301 ) ) ;
#48213=CARTESIAN_POINT ( 'NONE',  ( -78.42949214982630224, -32.55659982916139228, 130.6045153880263854 ) ) ;
#48215=CARTESIAN_POINT ( 'NONE',  ( -1.309564884278361513E-05, -14.21045842199434972, 34.36840973699906243 ) ) ;
#48217=CARTESIAN_POINT ( 'NONE',  ( 89.04854951302100119, -57.60430045889667383, 203.7548466016606596 ) ) ;
#48235=CARTESIAN_POINT ( 'NONE',  ( 27.93076071969897001, -25.57948163322986801, 30.03616920575478133 ) ) ;
#48249=CARTESIAN_POINT ( 'NONE',  ( 45.18230306424334941, -60.00000000000002132, -38.79808340435986480 ) ) ;
#48250=CARTESIAN_POINT ( 'NONE',  ( 89.21430567429679570, -29.99999999999982947, 189.0176709876100745 ) ) ;
#48271=EDGE_LOOP ( 'NONE', ( #1193, #80184 ) ) ;
#48276=CARTESIAN_POINT ( 'NONE',  ( -44.36055083073691918, -59.99999999999993605, 48.27248335138339286 ) ) ;
#48277=CARTESIAN_POINT ( 'NONE',  ( 68.76507998961908186, -36.00945847659178867, 95.91866453639596557 ) ) ;
#48301=CARTESIAN_POINT ( 'NONE',  ( 9.890468211898383544, -60.00000000000000000, 39.64862895235242490 ) ) ;
#48302=CARTESIAN_POINT ( 'NONE',  ( -98.04267884131168387, -30.00000000000000355, 190.4907426802132591 ) ) ;
#48305=CARTESIAN_POINT ( 'NONE',  ( 40.76935397657385352, -57.69044601521297011, 56.95604026165146649 ) ) ;
#48308=CARTESIAN_POINT ( 'NONE',  ( 19.31349756789174066, -25.58635144299420006, -38.49263360045101479 ) ) ;
#48313=CARTESIAN_POINT ( 'NONE',  ( -16.90281938967774877, -59.99999999999997868, 39.91503433071412132 ) ) ;
#48317=CARTESIAN_POINT ( 'NONE',  ( -86.88653354982636756, -39.10394614662991586, 188.8703255679024267 ) ) ;
#48321=CARTESIAN_POINT ( 'NONE',  ( -15.42473530526779868, -25.55047207056445302, 28.31187399038664054 ) ) ;
#48331=DIRECTION ( 'NONE',  ( 0.000000000000000000, 0.000000000000000000, 1.000000000000000000 ) ) ;
#48335=CARTESIAN_POINT ( 'NONE',  ( 73.52189759326324747, -59.99999999999997868, 167.4063777988524464 ) ) ;
#48340=CARTESIAN_POINT ( 'NONE',  ( 31.71028148999514329, -14.21045842199427156, 37.70122135646843731 ) ) ;
#48357=CARTESIAN_POINT ( 'NONE',  ( -82.67652743962570128, -60.00000000002928857, 201.6796312862459786 ) ) ;
#48360=CARTESIAN_POINT ( 'NONE',  ( 71.31537837103485344, -59.99999999999998579, 149.1299768214489063 ) ) ;
#48364=CARTESIAN_POINT ( 'NONE',  ( -113.7193438732989961, -60.00000000000000000, 185.6039524652145474 ) ) ;
#48365=CARTESIAN_POINT ( 'NONE',  ( 16.70053533077139818, -35.99219286291273789, 30.12149763659517632 ) ) ;
#48366=CARTESIAN_POINT ( 'NONE',  ( 98.63481415922996121, -37.99999999999972289, 192.2156350310174275 ) ) ;
#48368=CARTESIAN_POINT ( 'NONE',  ( -44.50213627361837609, -25.70502922763081699, 39.42336395404723959 ) ) ;
#48379=CARTESIAN_POINT ( 'NONE',  ( 108.7023100198421446, -30.00000000000508393, 185.2916543307226789 ) ) ;
#48384=CARTESIAN_POINT ( 'NONE',  ( 97.89223034704271242, -30.00000000000000355, 136.7744468160770737 ) ) ;
#48400=CARTESIAN_POINT ( 'NONE',  ( 79.85080175595479091, -38.77068210228555500, 192.7140471300223510 ) ) ;
#48402=CARTESIAN_POINT ( 'NONE',  ( 83.78310723525129333, -37.99999999999999289, 174.8088074860800418 ) ) ;
#48418=CARTESIAN_POINT ( 'NONE',  ( 12.80902418639212748, -21.46289778021456129, 35.62032504730713356 ) ) ;
#48424=CARTESIAN_POINT ( 'NONE',  ( 86.26413129325493401, -21.18033766835324272, 178.9871004810926252 ) ) ;
#48428=CARTESIAN_POINT ( 'NONE',  ( 95.40603510496622164, -57.67176892321496240, 36.33773616593676081 ) ) ;
#48434=CARTESIAN_POINT ( 'NONE',  ( -60.27117132039084169, -38.00000000000001421, 72.18992984672541979 ) ) ;
#48452=CARTESIAN_POINT ( 'NONE',  ( -62.09692702121698460, -34.58946200273062743, -24.66260175802744570 ) ) ;
#48463=CARTESIAN_POINT ( 'NONE',  ( -81.46144558510007982, -60.00000000000000000, -27.04857943224691041 ) ) ;
#48466=CARTESIAN_POINT ( 'NONE',  ( 12.77564109741936704, -23.94125442111781510, -30.51326413066097487 ) ) ;
#48468=CARTESIAN_POINT ( 'NONE',  ( 94.30024162164785650, -37.70548019052495192, 192.9918295364696235 ) ) ;
#48470=CARTESIAN_POINT ( 'NONE',  ( -79.40492842379534011, -60.33402592105881013, 168.9271176041871740 ) ) ;
#48481=CARTESIAN_POINT ( 'NONE',  ( -112.7923893646043183, -57.67119337860199124, 188.3631819635289446 ) ) ;
#48486=CARTESIAN_POINT ( 'NONE',  ( -16.60966916665065085, -29.99999999999998934, -39.45625820571179787 ) ) ;
#48487=CARTESIAN_POINT ( 'NONE',  ( -12.27152016684560820, -14.21045842199446874, 34.40193250091021326 ) ) ;
#48488=CARTESIAN_POINT ( 'NONE',  ( -51.93045568178391846, -53.37659915090458895, 59.21916723660311277 ) ) ;
#48491=CARTESIAN_POINT ( 'NONE',  ( -98.44231968215002837, -60.34206883299947322, 196.4449518206358789 ) ) ;
#48495=CARTESIAN_POINT ( 'NONE',  ( 89.08324256299194133, -38.38303541736249969, -17.92597912426925433 ) ) ;
#48501=CARTESIAN_POINT ( 'NONE',  ( 85.24653099856575977, -30.00000000000000000, 172.6093818142646796 ) ) ;
#48504=EDGE_CURVE ( 'NONE', #25066, #102350, #45414, .T. ) ;
#48509=CARTESIAN_POINT ( 'NONE',  ( 49.10960368247432228, -32.59430926536067830, 47.09906247322906125 ) ) ;
#48516=CARTESIAN_POINT ( 'NONE',  ( -107.5459679601182472, -38.35637404592787902, 134.5943931340658821 ) ) ;
#48519=CARTESIAN_POINT ( 'NONE',  ( 98.50113857120987859, -38.35583664951423799, 79.61398634377471240 ) ) ;
#48522=CARTESIAN_POINT ( 'NONE',  ( 103.7141658930947017, -52.71714772886510758, 149.2188361930400049 ) ) ;
#48527=CARTESIAN_POINT ( 'NONE',  ( 79.59876633705728466, -60.00000000000001421, 195.4925107952827545 ) ) ;
#48530=CARTESIAN_POINT ( 'NONE',  ( 58.21454800639202887, -39.49099975802815976, 67.71415432429243708 ) ) ;
#48533=DIRECTION ( 'NONE',  ( -0.000000000000000000, -1.000000000000000000, -0.000000000000000000 ) ) ;
#48537=CARTESIAN_POINT ( 'NONE',  ( -55.91766210057292597, -29.99999999994657074, 79.88469606658499345 ) ) ;
#48546=EDGE_CURVE ( 'NONE', #67219, #25066, #82237, .T. ) ;
#48549=CARTESIAN_POINT ( 'NONE',  ( 83.95431419311037757, -35.95954853935870688, 173.2961117203365404 ) ) ;
#48563=CARTESIAN_POINT ( 'NONE',  ( -25.20238367481141140, -29.17817727520965931, 38.35064085007479662 ) ) ;
#48585=CARTESIAN_POINT ( 'NONE',  ( -111.0840224819099973, -60.00000000000000711, 152.9628786121542703 ) ) ;
#48592=CARTESIAN_POINT ( 'NONE',  ( -82.89588075628438446, -46.49890956395007180, 179.0000094130285220 ) ) ;
#48607=CARTESIAN_POINT ( 'NONE',  ( 112.5893299866519897, -60.00000000000007105, 145.0945492492805045 ) ) ;
#48608=CARTESIAN_POINT ( 'NONE',  ( -109.4306967521916221, -29.99999999999999645, 166.0290040158848797 ) ) ;
#48610=CARTESIAN_POINT ( 'NONE',  ( -62.26494006864544417, -56.86950266710078949, 87.13957684240361345 ) ) ;
#48613=CARTESIAN_POINT ( 'NONE',  ( 104.9932229724631867, -59.99999999999998579, 96.28837625296324632 ) ) ;
#48615=CARTESIAN_POINT ( 'NONE',  ( 1.016806655238071233, -53.39687650318582257, 32.78912937680000539 ) ) ;
#48622=CARTESIAN_POINT ( 'NONE',  ( -110.5108575042119412, -60.00000000000002132, 147.2781094354880338 ) ) ;
#48633=CARTESIAN_POINT ( 'NONE',  ( 106.2155570736864547, -59.99999999999999289, 163.8884563533469247 ) ) ;
#48634=CARTESIAN_POINT ( 'NONE',  ( -33.01570200386896659, -60.31662611196244228, 38.17099334662022159 ) ) ;
#48636=CARTESIAN_POINT ( 'NONE',  ( 40.18194788804924400, -39.51852554140211282, 38.87859757349198020 ) ) ;
#48640=CARTESIAN_POINT ( 'NONE',  ( -57.67084418237976706, -38.34431147036926291, 89.26121482714037825 ) ) ;
#48651=CARTESIAN_POINT ( 'NONE',  ( 100.9404511582781083, -59.99999999999999289, 86.55166955914968696 ) ) ;
#48659=CARTESIAN_POINT ( 'NONE',  ( -96.64935847557207182, -29.99999999999981171, 191.1839691282570186 ) ) ;
#48670=ORIENTED_EDGE ( 'NONE', *, *, #78441, .F. ) ;
#48673=CARTESIAN_POINT ( 'NONE',  ( 79.80652143352665462, -53.37714176188983117, 161.8226454331678212 ) ) ;
#48682=CARTESIAN_POINT ( 'NONE',  ( -39.01690548088378563, -57.69424739071683916, 54.12508632231112671 ) ) ;
#48693=CARTESIAN_POINT ( 'NONE',  ( -6.292450455944076815, -13.05272214707127354, 32.05976969049422820 ) ) ;
#48700=ORIENTED_EDGE ( 'NONE', *, *, #52675, .F. ) ;
#48704=CARTESIAN_POINT ( 'NONE',  ( 25.35164555241593476, -27.85376369652950146, -38.37886305012078481 ) ) ;
#48709=DIRECTION ( 'NONE',  ( -0.000000000000000000, -1.000000000000000000, -0.000000000000000000 ) ) ;
#48710=CARTESIAN_POINT ( 'NONE',  ( 103.7853185863665857, -57.67100931241723316, 91.47519850164491118 ) ) ;
#48716=CARTESIAN_POINT ( 'NONE',  ( -74.24642577967240697, -59.99999999999999289, 174.6858703907944914 ) ) ;
#48720=CARTESIAN_POINT ( 'NONE',  ( -85.70838396571514295, -32.07329945039565189, 182.3208811495701980 ) ) ;
#48727=CARTESIAN_POINT ( 'NONE',  ( -84.40081900408691240, -45.27047985170548827, -3.485582449796192250 ) ) ;
#48733=CARTESIAN_POINT ( 'NONE',  ( 5.820808985959283532, -2.898778190268130493E-12, -21.65942590380460686 ) ) ;
#48735=CARTESIAN_POINT ( 'NONE',  ( -34.13564290404001156, -60.00000000000002132, -42.84076297484070039 ) ) ;
#48736=CARTESIAN_POINT ( 'NONE',  ( -77.77839600099601114, -39.49706976687358662, 133.3567172694711473 ) ) ;
#48738=CARTESIAN_POINT ( 'NONE',  ( 45.38117173420300787, -14.21045842199442077, 49.92181071548740334 ) ) ;
#48740=CARTESIAN_POINT ( 'NONE',  ( 111.7962455800622479, -57.67099614711071354, 192.0613627441538540 ) ) ;
#48759=CARTESIAN_POINT ( 'NONE',  ( -16.35964837410663364, -14.21045842199427156, 34.56001531359335388 ) ) ;
#48760=CARTESIAN_POINT ( 'NONE',  ( 31.41265888251252392, -60.32177928414881052, 37.38922941594847060 ) ) ;
#48762=( BOUNDED_SURFACE ( )  B_SPLINE_SURFACE ( 2, 3, ( 
 ( #69949, #21419, #36028, #36558, #102309, #54259, #29014, #87202, #54799, #13278, #44081, #102847, #5214, #103890, #30036, #21949, #87732, #3083, #68902, #53236, #60805, #69427, #45677, #19849, #52684, #11687, #86158, #61879, #94774, #61725, #95688, #94651, #52559, #79498, #20797, #28331, #53107, #3498, #70880, #4556, #61207, #12624, #46601, #30446, #63340, #37493 ),
 ( #87080, #86030, #28883, #69822, #21303, #5609, #96234, #70356, #94097, #11563, #29914, #95170, #21832, #54671, #20261, #85483, #61753, #38534, #86564, #12102, #5088, #103774, #53629, #38021, #13154, #45561, #45032, #103252, #77917, #102182, #29398, #4026, #78430, #36954, #102720, #46083, #62281, #71396, #54140, #78964, #62801, #87608, #44494, #13689, #104295, #77382 ),
 ( #36437, #69307, #81081, #65442, #56258, #7717, #14217, #14748, #80547, #56800, #7190, #106410, #34569, #48704, #22364, #23414, #81594, #73511, #17830, #50681, #40625, #75513, #32571, #39593, #83598, #88656, #32031, #99791, #97795, #47121, #22888, #25962, #23960, #1607, #63869, #58821, #40106, #96756, #89193, #105886, #30985, #15293, #48177, #55726, #91712, #72465 ) ),
 .UNSPECIFIED., .F., .F., .F. ) 
 B_SPLINE_SURFACE_WITH_KNOTS ( ( 3, 3 ),
 ( 4, 2, 2, 2, 2, 2, 2, 2, 2, 2, 2, 2, 2, 2, 2, 2, 2, 2, 2, 2, 2, 2, 4 ),
 ( 0.000000000000000000, 1.000000000000000000 ),
 ( 0.000000000000000000, 0.004671298967716180570, 0.009342597935432361139, 0.01868519587086472228, 0.02802779380629708342, 0.03737039174172944456, 0.04671298967716180917, 0.05605558761259416684, 0.06539818554802652451, 0.07006948451574271375, 0.07240513399960080143, 0.07474078348345888911, 0.07941208245117506448, 0.08408338141889125372, 0.09342597935432361833, 0.1027685772897559691, 0.1121111752251883337, 0.1214537731606206983, 0.1307963710960530490, 0.1354676700637692521, 0.1401389690314854275, 0.1448102679992016029, 0.1494815669669177782 ),
 .UNSPECIFIED. ) 
 GEOMETRIC_REPRESENTATION_ITEM ( )  RATIONAL_B_SPLINE_SURFACE ( (
 ( 1.000000000000000000, 1.000000000000000000, 1.000000000000000000, 1.000000000000000000, 1.000000000000000000, 1.000000000000000000, 1.000000000000000000, 1.000000000000000000, 1.000000000000000000, 1.000000000000000000, 1.000000000000000000, 1.000000000000000000, 1.000000000000000000, 1.000000000000000000, 1.000000000000000000, 1.000000000000000000, 1.000000000000000000, 1.000000000000000000, 1.000000000000000000, 1.000000000000000000, 1.000000000000000000, 1.000000000000000000, 1.000000000000000000, 1.000000000000000000, 1.000000000000000000, 1.000000000000000000, 1.000000000000000000, 1.000000000000000000, 1.000000000000000000, 1.000000000000000000, 1.000000000000000000, 1.000000000000000000, 1.000000000000000000, 1.000000000000000000, 1.000000000000000000, 1.000000000000000000, 1.000000000000000000, 1.000000000000000000, 1.000000000000000000, 1.000000000000000000, 1.000000000000000000, 1.000000000000000000, 1.000000000000000000, 1.000000000000000000, 1.000000000000000000, 1.000000000000000000),
 ( 1.857142857142858317, 1.857142857142858317, 1.857142857142858317, 1.857142857142858317, 1.857142857142858317, 1.857142857142858317, 1.857142857142858317, 1.857142857142858317, 1.857142857142858317, 1.857142857142858317, 1.857142857142858317, 1.857142857142858317, 1.857142857142858317, 1.857142857142858317, 1.857142857142858317, 1.857142857142858317, 1.857142857142858317, 1.857142857142858317, 1.857142857142858317, 1.857142857142858317, 1.857142857142858317, 1.857142857142858317, 1.857142857142858317, 1.857142857142858317, 1.857142857142858317, 1.857142857142858317, 1.857142857142858317, 1.857142857142858317, 1.857142857142858317, 1.857142857142858317, 1.857142857142858317, 1.857142857142858317, 1.857142857142858317, 1.857142857142858317, 1.857142857142858317, 1.857142857142858317, 1.857142857142858317, 1.857142857142858317, 1.857142857142860093, 1.857142857142860093, 1.857142857142858317, 1.857142857142858317, 1.857142857142858317, 1.857142857142858317, 1.857142857142858317, 1.857142857142858317),
 ( 1.000000000000000000, 1.000000000000000000, 1.000000000000000000, 1.000000000000000000, 1.000000000000000000, 1.000000000000000000, 1.000000000000000000, 1.000000000000000000, 1.000000000000000000, 1.000000000000000000, 1.000000000000000000, 1.000000000000000000, 1.000000000000000000, 1.000000000000000000, 1.000000000000000000, 1.000000000000000000, 1.000000000000000000, 1.000000000000000000, 1.000000000000000000, 1.000000000000000000, 1.000000000000000000, 1.000000000000000000, 1.000000000000000000, 1.000000000000000000, 1.000000000000000000, 1.000000000000000000, 1.000000000000000000, 1.000000000000000000, 1.000000000000000000, 1.000000000000000000, 1.000000000000000000, 1.000000000000000000, 1.000000000000000000, 1.000000000000000000, 1.000000000000000000, 1.000000000000000000, 1.000000000000000000, 1.000000000000000000, 1.000000000000000000, 1.000000000000000000, 1.000000000000000000, 1.000000000000000000, 1.000000000000000000, 1.000000000000000000, 1.000000000000000000, 1.000000000000000000) ) ) 
 REPRESENTATION_ITEM ( '' )  SURFACE ( )  );
#48776=CARTESIAN_POINT ( 'NONE',  ( 8.319959379298547120, -59.99999999999998579, -42.48049722093006864 ) ) ;
#48793=EDGE_LOOP ( 'NONE', ( #30990, #98819, #45320, #5176, #69978, #18774, #26699 ) ) ;
#48802=CARTESIAN_POINT ( 'NONE',  ( -8.348350756690260610, -59.99999999999997158, 33.88065270824813524 ) ) ;
#48803=CARTESIAN_POINT ( 'NONE',  ( 65.24931495339168919, -25.57815227503792244, 79.70468693739232435 ) ) ;
#48809=CARTESIAN_POINT ( 'NONE',  ( -69.44743540119901581, -57.67117814800237596, -34.85819734733303221 ) ) ;
#48827=CARTESIAN_POINT ( 'NONE',  ( -94.02161711668794908, -30.00000000000000000, 191.2771078561046352 ) ) ;
#48832=CARTESIAN_POINT ( 'NONE',  ( 56.10950871050302879, -57.67607768850538719, 94.75155346926845823 ) ) ;
#48837=CARTESIAN_POINT ( 'NONE',  ( 8.958840525176039904, -22.36732914119846072, -38.54358237171171453 ) ) ;
#48840=CARTESIAN_POINT ( 'NONE',  ( -28.18018267510046826, -60.00000000000001421, 42.21498033703696962 ) ) ;
#48843=CARTESIAN_POINT ( 'NONE',  ( -86.67732985869325546, -50.12485329941275580, 191.5830762183649938 ) ) ;
#48847=CARTESIAN_POINT ( 'NONE',  ( -9.346815707592632805, -53.40262838734317796, 32.79379019251283012 ) ) ;
#48860=CARTESIAN_POINT ( 'NONE',  ( 73.51724252604583398, -60.00000000000000711, 167.3604022711870982 ) ) ;
#48861=CARTESIAN_POINT ( 'NONE',  ( 109.5916899561874942, -30.00000000000003197, 172.2594225519244446 ) ) ;
#48868=CARTESIAN_POINT ( 'NONE',  ( 28.84074934710125859, -30.00000000000002842, 39.52209614246421410 ) ) ;
#48881=CARTESIAN_POINT ( 'NONE',  ( -60.70436703292030245, -60.00000000001957545, 111.1961515286286613 ) ) ;
#48883=CARTESIAN_POINT ( 'NONE',  ( 81.98299855092518840, -60.00000000000000000, 198.0498435237767012 ) ) ;
#48884=CARTESIAN_POINT ( 'NONE',  ( -107.9655701563618067, -29.99999999999997158, 188.7577781645654795 ) ) ;
#48885=CARTESIAN_POINT ( 'NONE',  ( 16.63567752523875853, -32.51137318948865129, 29.53593408679408228 ) ) ;
#48887=CARTESIAN_POINT ( 'NONE',  ( 97.36093972260707119, -38.00000000000009237, 192.7743595253038791 ) ) ;
#48890=CARTESIAN_POINT ( 'NONE',  ( -44.43505828091571175, -22.24746064786846134, 38.44332992766335622 ) ) ;
#48902=CARTESIAN_POINT ( 'NONE',  ( 80.85658148696911951, -30.00000000000000000, 6.669769987989186966 ) ) ;
#48907=CARTESIAN_POINT ( 'NONE',  ( 94.31383618571270233, -29.99999999999999645, 113.8495007026067611 ) ) ;
#48921=CARTESIAN_POINT ( 'NONE',  ( 82.14726820479680214, -38.83665063316719568, 196.0510034214655946 ) ) ;
#48936=PRESENTATION_STYLE_ASSIGNMENT (( #25247 ) ) ;
#48939=LINE ( 'NONE', #31225, #19806 ) ;
#48941=CARTESIAN_POINT ( 'NONE',  ( 31.34101644064316616, -33.33332329661044469, 41.37796191375046817 ) ) ;
#48947=CARTESIAN_POINT ( 'NONE',  ( 85.39226384298076766, -35.72026385061843712, 183.0101103138053986 ) ) ;
#48952=CARTESIAN_POINT ( 'NONE',  ( 91.53261005776035120, -57.66219477115423331, -20.10647474121806155 ) ) ;
#48955=CARTESIAN_POINT ( 'NONE',  ( -81.48731548190207263, -30.00000000000001066, -3.427914186170737398 ) ) ;
#48964=CARTESIAN_POINT ( 'NONE',  ( -8.400251092734315250, -22.83500361551703861, -30.52644813539184199 ) ) ;
#48966=CARTESIAN_POINT ( 'NONE',  ( -99.53543709402866568, -38.00000000000000000, 191.3481644649123155 ) ) ;
#48974=CARTESIAN_POINT ( 'NONE',  ( -31.20322697673447720, -22.08705006449989838, -31.98265270787211634 ) ) ;
#48978=CARTESIAN_POINT ( 'NONE',  ( -52.55046997570821787, -21.76995662024391365, -25.00977836231365004 ) ) ;
#48986=CARTESIAN_POINT ( 'NONE',  ( -87.06860877932031428, -60.00000000000000000, -22.64416279712467528 ) ) ;
#48990=CARTESIAN_POINT ( 'NONE',  ( 100.9499868790999813, -60.25997814283888943, 195.1806730477072165 ) ) ;
#49006=CARTESIAN_POINT ( 'NONE',  ( -50.71028374685950268, -57.67771315371629726, 79.11066721451838646 ) ) ;
#49011=CARTESIAN_POINT ( 'NONE',  ( 47.46761990717632784, -14.21045842199427511, -33.06011575854734730 ) ) ;
#49014=CARTESIAN_POINT ( 'NONE',  ( -52.27550221499717509, -56.84507427995361439, 61.26800082247714130 ) ) ;
#49018=CARTESIAN_POINT ( 'NONE',  ( -99.74672076233166251, -45.25374114503119216, 192.8211023940378936 ) ) ;
#49026=CARTESIAN_POINT ( 'NONE',  ( 110.6919933160486664, -38.35613597905214789, 162.9682471850780132 ) ) ;
#49032=CARTESIAN_POINT ( 'NONE',  ( 83.98821470635078867, -29.99999999999999645, 160.9053504413435860 ) ) ;
#49039=CARTESIAN_POINT ( 'NONE',  ( 49.90722959797657410, -53.36482695313026170, 55.25312740662995026 ) ) ;
#49043=CARTESIAN_POINT ( 'NONE',  ( -102.5472473342257587, -38.35641472935498086, 103.2659507031501960 ) ) ;
#49046=CARTESIAN_POINT ( 'NONE',  ( 98.48880034582394671, -38.35583643892559991, 79.54055716815213373 ) ) ;
#49049=CARTESIAN_POINT ( 'NONE',  ( 102.4711514760015518, -45.28286875496431207, 149.2602369284549866 ) ) ;
#49054=CARTESIAN_POINT ( 'NONE',  ( 75.69597243072205117, -60.00000000000000000, 185.5364934770681486 ) ) ;
#49057=DIRECTION ( 'NONE',  ( 0.000000000000000000, 0.000000000000000000, -1.000000000000000000 ) ) ;
#49059=CARTESIAN_POINT ( 'NONE',  ( 58.04481121138562116, -56.85611253634766626, 75.20185096419942283 ) ) ;
#49065=CARTESIAN_POINT ( 'NONE',  ( -59.60688997945907630, -30.00000000000668976, 90.58845735111052022 ) ) ;
#49071=FACE_OUTER_BOUND ( 'NONE', #38344, .T. ) ;
#49075=CARTESIAN_POINT ( 'NONE',  ( 82.27827146869219632, -49.99153877646314470, 179.0196594568768091 ) ) ;
#49088=CARTESIAN_POINT ( 'NONE',  ( -9.802581847862906983, -20.13751096416813624, 35.36442285224644166 ) ) ;
#49112=CARTESIAN_POINT ( 'NONE',  ( -98.17166580661555031, -59.99999999999999289, 69.98620740965910159 ) ) ;
#49119=CARTESIAN_POINT ( 'NONE',  ( -85.29290479114395396, -25.40355077146805129, 170.0323860005369454 ) ) ;
#49124=ORIENTED_EDGE ( 'NONE', *, *, #98646, .T. ) ;
#49136=CARTESIAN_POINT ( 'NONE',  ( 103.2975989548790494, -14.21045842199431064, 133.3107955441116985 ) ) ;
#49137=CARTESIAN_POINT ( 'NONE',  ( -104.9451182028910239, -14.21045842199441367, 145.4712626202903323 ) ) ;
#49139=CARTESIAN_POINT ( 'NONE',  ( -62.36043780488878241, -49.91630522361305111, 83.85778711176541833 ) ) ;
#49142=CARTESIAN_POINT ( 'NONE',  ( 101.2350610320152526, -59.99999999996104094, 74.14752333521899175 ) ) ;
#49144=CARTESIAN_POINT ( 'NONE',  ( 0.9975031403653140671, -32.51050350380973697, 29.30806721023733630 ) ) ;
#49151=AXIS2_PLACEMENT_3D ( 'NONE', #62797, #54668, #30444 ) ;
#49152=CARTESIAN_POINT ( 'NONE',  ( -106.4349217454702341, -60.00000000000002132, 197.8028031639909159 ) ) ;
#49164=CARTESIAN_POINT ( 'NONE',  ( -32.20452792638825912, -22.14816194189014453, 30.75548861735132178 ) ) ;
#49165=CARTESIAN_POINT ( 'NONE',  ( 38.83382506401130030, -32.59866074387370816, 36.29133770639072765 ) ) ;
#49171=CARTESIAN_POINT ( 'NONE',  ( -77.48386536772069633, -38.51251665548984704, 186.4267636295656700 ) ) ;
#49185=CARTESIAN_POINT ( 'NONE',  ( 103.6214353051173021, -60.00000000000001421, 102.2210354960218126 ) ) ;
#49193=CARTESIAN_POINT ( 'NONE',  ( -98.46708292002269047, -30.00000000000004619, 189.8972334866360541 ) ) ;
#49208=CARTESIAN_POINT ( 'NONE',  ( 78.98612558784607529, -60.31715732648605410, 164.7471663665724861 ) ) ;
#49218=CARTESIAN_POINT ( 'NONE',  ( 58.62000344007604014, -60.00000000000000000, -30.08217214727655886 ) ) ;
#49226=CARTESIAN_POINT ( 'NONE',  ( 23.51672044067690948, -28.03177904939224518, 37.77843793023890839 ) ) ;
#49241=CARTESIAN_POINT ( 'NONE',  ( 107.5440841644286536, -57.67122823495125061, 113.6602115610031944 ) ) ;
#49246=MECHANICAL_DESIGN_GEOMETRIC_PRESENTATION_REPRESENTATION('',(#64749),#16467);
#49248=CARTESIAN_POINT ( 'NONE',  ( -77.64205621890488374, -60.00000000000002132, 192.0628139380899881 ) ) ;
#49255=CARTESIAN_POINT ( 'NONE',  ( -84.96146178370577218, -46.57119306001131775, 187.4521374934294329 ) ) ;
#49262=CARTESIAN_POINT ( 'NONE',  ( -84.46166934361085055, -45.26796119114888484, -8.211886439601322252 ) ) ;
#49268=CARTESIAN_POINT ( 'NONE',  ( 2.227375807149031495, -1.734723475976807094E-15, 17.01589776168603407 ) ) ;
#49270=CARTESIAN_POINT ( 'NONE',  ( -16.60966916665065085, -29.99999999999998934, -39.45625820571179787 ) ) ;
#49271=CARTESIAN_POINT ( 'NONE',  ( -78.21160035621433337, -25.61278769304882985, 123.8358509973067498 ) ) ;
#49273=CARTESIAN_POINT ( 'NONE',  ( 73.77841798646971938, -29.99999999999998934, 147.9493570314868123 ) ) ;
#49275=CARTESIAN_POINT ( 'NONE',  ( 109.9110342544350516, -57.66832763311409593, 196.2850603310193094 ) ) ;
#49292=CARTESIAN_POINT ( 'NONE',  ( 30.44468774519250331, -53.37907340497660869, 35.76283041829702114 ) ) ;
#49306=CARTESIAN_POINT ( 'NONE',  ( 89.96949554733780019, -59.99999999999997868, -18.88444619536232594 ) ) ;
#49336=CARTESIAN_POINT ( 'NONE',  ( -75.38507137031108130, -60.00000000000003553, 138.7214457628266473 ) ) ;
#49338=CARTESIAN_POINT ( 'NONE',  ( 67.30723638396268882, -39.48332017755057421, 93.17411211822772543 ) ) ;
#49363=CARTESIAN_POINT ( 'NONE',  ( -93.39911556732610620, -30.00000000000000711, 191.1953737942166924 ) ) ;
#49366=CARTESIAN_POINT ( 'NONE',  ( 63.99273081836761889, -57.67907566170010369, 122.4759172911383303 ) ) ;
#49368=CARTESIAN_POINT ( 'NONE',  ( 2.499999999999997335, -30.00000000000000000, 30.00000000000000000 ) ) ;
#49369=EDGE_CURVE ( 'NONE', #34458, #84319, #81000, .T. ) ;
#49371=CARTESIAN_POINT ( 'NONE',  ( 5.476207722142115486, -21.71875361764507062, -38.54698999943882853 ) ) ;
#49374=CARTESIAN_POINT ( 'NONE',  ( -4.190096357442898878, -60.00000000000000711, 39.63091782826867160 ) ) ;
#49379=CARTESIAN_POINT ( 'NONE',  ( -86.99319857952023938, -28.01872268044905923, 186.8509686606727200 ) ) ;
#49383=CARTESIAN_POINT ( 'NONE',  ( -8.225604079535896673, -46.43935024322556160, 31.62298990380002550 ) ) ;
#49394=CARTESIAN_POINT ( 'NONE',  ( 0.000000000000000000, -15.00000000000000000, 0.000000000000000000 ) ) ;
#49398=CARTESIAN_POINT ( 'NONE',  ( 113.5291039388664700, -60.00000000000007105, 153.5981272189337403 ) ) ;
#49423=CARTESIAN_POINT ( 'NONE',  ( -71.03131189882361696, -60.00000000001953282, 166.0686979362143347 ) ) ;
#49426=CARTESIAN_POINT ( 'NONE',  ( 106.1038126249908231, -60.00000000000002132, 198.1916009746322231 ) ) ;
#49427=CARTESIAN_POINT ( 'NONE',  ( -114.4010969832937121, -60.00000000000006395, 179.2248356726699399 ) ) ;
#49428=CARTESIAN_POINT ( 'NONE',  ( 15.42399563816537622, -25.54935048520918528, 28.31163924845273883 ) ) ;
#49430=CARTESIAN_POINT ( 'NONE',  ( -43.84331470278493725, -36.07451146886668880, 41.44895103270090431 ) ) ;
#49433=CARTESIAN_POINT ( 'NONE',  ( 89.99999999999997158, -38.00000000001091394, 196.0238439516549818 ) ) ;
#49443=CARTESIAN_POINT ( 'NONE',  ( 53.17600322138483904, -30.00000000000000000, 72.57813921009470448 ) ) ;
#49448=CARTESIAN_POINT ( 'NONE',  ( 90.99536718434406168, -29.99999999999998934, 94.30297898937882906 ) ) ;
#49465=CARTESIAN_POINT ( 'NONE',  ( 79.84856180006062232, -38.77050156954319959, 192.7098517259555308 ) ) ;
#49492=CARTESIAN_POINT ( 'NONE',  ( 83.91935083234469062, -61.03361821168092405, 192.1967390494019696 ) ) ;
#49496=CARTESIAN_POINT ( 'NONE',  ( 91.47756376649307697, -57.66240114371687042, -20.19489575921430102 ) ) ;
#49501=CARTESIAN_POINT ( 'NONE',  ( -81.58524466189544455, -30.00000000000001421, -7.583927274541655272 ) ) ;
#49502=CARTESIAN_POINT ( 'NONE',  ( -82.22606752459770973, -38.00000000000003553, 160.2907289571271860 ) ) ;
#49517=AXIS2_PLACEMENT_3D ( 'NONE', #98744, #1644, #27045 ) ;
#49521=CARTESIAN_POINT ( 'NONE',  ( -67.74125374443480041, -34.58950197393470916, -22.71994573540199625 ) ) ;
#49529=CARTESIAN_POINT ( 'NONE',  ( -0.8333261453522353701, -30.00000000000001421, 28.88964995960238369 ) ) ;
#49530=CARTESIAN_POINT ( 'NONE',  ( -82.02569044098642337, -60.00000000000000000, -26.68448968580177905 ) ) ;
#49532=CARTESIAN_POINT ( 'NONE',  ( 48.18879443871838930, -35.41177168222470328, -28.23099784303214577 ) ) ;
#49534=CARTESIAN_POINT ( 'NONE',  ( 99.46726541099765484, -52.78227579418069837, 194.5120875942841394 ) ) ;
#49550=CARTESIAN_POINT ( 'NONE',  ( -2.832004189415751050, -57.67120204282113605, 41.61186672541032294 ) ) ;
#49556=CARTESIAN_POINT ( 'NONE',  ( 41.39111156191358276, -30.00000000000003908, -36.78675873448672462 ) ) ;
#49557=CARTESIAN_POINT ( 'NONE',  ( -12.46506237085073110, -30.00000000000006395, 37.03826559298295251 ) ) ;
#49558=CARTESIAN_POINT ( 'NONE',  ( -50.37523485278211410, -32.58700810942853110, 49.03711277103302280 ) ) ;
#49564=CARTESIAN_POINT ( 'NONE',  ( -101.2893714159135925, -60.24741957559085392, 194.9011525870544972 ) ) ;
#49569=CARTESIAN_POINT ( 'NONE',  ( 99.79593632746312437, -38.46925667693373185, 200.5817790329920456 ) ) ;
#49574=CARTESIAN_POINT ( 'NONE',  ( 82.58295863708946172, -30.00000000000000711, 149.9139447893771262 ) ) ;
#49575=CIRCLE ( 'NONE', #59924, 15.00000000000000000 ) ;
#49581=CARTESIAN_POINT ( 'NONE',  ( 52.40275982922914011, -22.17845676421043422, 48.78481890060238868 ) ) ;
#49583=CARTESIAN_POINT ( 'NONE',  ( 2.500000000000002665, -30.00000000000000000, -14.79019945774903810 ) ) ;
#49586=CARTESIAN_POINT ( 'NONE',  ( -91.77192237904225181, -38.35461803959927352, 32.56391333383364639 ) ) ;
#49590=CARTESIAN_POINT ( 'NONE',  ( 91.15118748837623741, -38.35268490642818762, 25.35169414273645216 ) ) ;
#49592=CARTESIAN_POINT ( 'NONE',  ( 97.20070980819903639, -52.71699338941720470, 105.9753043912546673 ) ) ;
#49597=CARTESIAN_POINT ( 'NONE',  ( 74.84184181931864543, -59.99999999999998579, 180.0432328657729784 ) ) ;
#49601=CARTESIAN_POINT ( 'NONE',  ( 61.73071043583632900, -18.64118289587166899, 66.86164523920359670 ) ) ;
#49606=CARTESIAN_POINT ( 'NONE',  ( -80.31910585633404764, -38.35622671115012139, -26.31299467937850523 ) ) ;
#49617=CARTESIAN_POINT ( 'NONE',  ( 83.43530994757759345, -42.97836967012928966, 178.5296786636865534 ) ) ;
#49633=CARTESIAN_POINT ( 'NONE',  ( -21.81185593177036353, -26.89099996095279366, 37.28562843958906114 ) ) ;
#49646=CARTESIAN_POINT ( 'NONE',  ( 56.96794851135737048, -21.77000581858095174, -23.90161939876400865 ) ) ;
#49656=CARTESIAN_POINT ( 'NONE',  ( -95.56678818837158929, -59.99999999999998579, 53.06396543177949354 ) ) ;
#49664=CARTESIAN_POINT ( 'NONE',  ( -84.54716333029104192, -28.99156628927957158, 167.9126512817154264 ) ) ;
#49680=CARTESIAN_POINT ( 'NONE',  ( 114.4011996162234510, -59.99999999999997158, 179.2244502532067827 ) ) ;
#49681=CARTESIAN_POINT ( 'NONE',  ( -114.0148073962512854, -59.99999999999994316, 183.4850465800912218 ) ) ;
#49683=CARTESIAN_POINT ( 'NONE',  ( -62.14394237747171701, -53.39298685405226053, 85.00033226795140706 ) ) ;
#49686=CARTESIAN_POINT ( 'NONE',  ( 94.78037765028581418, -59.99999999999025846, -12.41180976829698857 ) ) ;
#49688=CARTESIAN_POINT ( 'NONE',  ( 6.014821585911270141, -25.54826201030574495, 28.13812934727146953 ) ) ;
#49689=CARTESIAN_POINT ( 'NONE',  ( -102.7041175444934709, -45.26540032460502516, 151.6231392685371020 ) ) ;
#49699=CARTESIAN_POINT ( 'NONE',  ( -58.09773888555076837, -59.99999999999998579, 94.39131198705021575 ) ) ;
#49710=CARTESIAN_POINT ( 'NONE',  ( -32.48576253217986931, -32.55615044963190030, 32.82149560294217139 ) ) ;
#49712=CARTESIAN_POINT ( 'NONE',  ( 40.33137201940245831, -18.77755698846380028, 34.22384520775455030 ) ) ;
#49716=CARTESIAN_POINT ( 'NONE',  ( -78.45547098499037020, -38.62875648362158643, 189.5571983322416827 ) ) ;
#49720=CARTESIAN_POINT ( 'NONE',  ( 72.90321207859628316, -60.00000000000000711, 126.5507789543278108 ) ) ;
#49728=CARTESIAN_POINT ( 'NONE',  ( 103.4784459831494559, -59.99999999999999289, 101.3822661864015231 ) ) ;
#49734=CARTESIAN_POINT ( 'NONE',  ( -92.10385064345778972, -29.99999999999979039, 190.9054133797868928 ) ) ;
#49749=CARTESIAN_POINT ( 'NONE',  ( 81.76547146975626390, -29.09233618002616950, 145.4551964297468487 ) ) ;
#49757=CARTESIAN_POINT ( 'NONE',  ( -59.00131487267276498, -60.00000000000000711, -29.97991402113869697 ) ) ;
#49766=CARTESIAN_POINT ( 'NONE',  ( 86.75287041639032282, -24.36799545327036043, 185.3761312858067640 ) ) ;
#49770=CARTESIAN_POINT ( 'NONE',  ( 21.50886870662808903, -26.69092517108576956, 37.20578707323234369 ) ) ;
#49784=CARTESIAN_POINT ( 'NONE',  ( 112.0245006668171186, -57.67108255664081184, 191.2454414640604625 ) ) ;
#49789=CARTESIAN_POINT ( 'NONE',  ( -89.99999999999997158, -60.00000000000000000, 188.5238439516623146 ) ) ;
#49790=CARTESIAN_POINT ( 'NONE',  ( -80.97052878467144410, -60.00000000000000711, 197.1200735740363257 ) ) ;
#49792=( GEOMETRIC_REPRESENTATION_CONTEXT ( 3 ) GLOBAL_UNCERTAINTY_ASSIGNED_CONTEXT ( ( #95211 ) ) GLOBAL_UNIT_ASSIGNED_CONTEXT ( ( #21106, #44822, #3819 ) ) REPRESENTATION_CONTEXT ( 'NONE', 'WORKASPACE' ) );
#49795=CARTESIAN_POINT ( 'NONE',  ( -85.48315206928592147, -35.70362574039081238, 183.4287206597788895 ) ) ;
#49798=VERTEX_POINT ( 'NONE', #52921 ) ;
#49802=CARTESIAN_POINT ( 'NONE',  ( -85.63635423108523526, -52.74933567132664791, -9.611642272926120611 ) ) ;
#49813=CARTESIAN_POINT ( 'NONE',  ( 16.35077622672217146, -14.21045842199431064, -36.83539407110947650 ) ) ;
#49814=CARTESIAN_POINT ( 'NONE',  ( -78.75458884624195832, -29.08646686470842369, 129.2280381913504357 ) ) ;
#49816=CARTESIAN_POINT ( 'NONE',  ( 71.37437158690347871, -14.21045842199427156, 121.5198118854055451 ) ) ;
#49818=CARTESIAN_POINT ( 'NONE',  ( 114.2239807911121829, -57.67113939738325712, 171.8931019229777064 ) ) ;
#49836=CARTESIAN_POINT ( 'NONE',  ( 27.77284297229067178, -22.10363696659563360, 29.38272422889403401 ) ) ;
#49844=CARTESIAN_POINT ( 'NONE',  ( -2.500000000000001776, -30.00000000000000000, 30.00000000000000000 ) ) ;
#49851=CARTESIAN_POINT ( 'NONE',  ( 92.40875900179753444, -60.00000000000000711, -11.92294509418752213 ) ) ;
#49865=CARTESIAN_POINT ( 'NONE',  ( 83.06461413968138174, -37.84181084904789572, -1.854778334287288999 ) ) ;
#49873=DIRECTION ( 'NONE',  ( 1.776356839400250465E-15, 0.000000000000000000, 1.000000000000000000 ) ) ;
#49874=CARTESIAN_POINT ( 'NONE',  ( -91.97836648421129269, -38.50002395389604715, 200.9810570860146299 ) ) ;
#49877=CARTESIAN_POINT ( 'NONE',  ( -78.44352337963121613, -59.99999999999999289, 159.1831049015135875 ) ) ;
#49879=CARTESIAN_POINT ( 'NONE',  ( 64.80880146042169088, -32.53003655438431707, 82.02282776973038381 ) ) ;
#49884=CARTESIAN_POINT ( 'NONE',  ( -92.43439519788523739, -57.65869811958181401, -18.51275992931142156 ) ) ;
#49902=CARTESIAN_POINT ( 'NONE',  ( 4.356282367766563191, -60.00000000000000711, 39.63058553034037601 ) ) ;
#49903=CARTESIAN_POINT ( 'NONE',  ( -90.94143197032809667, -30.00000000000000355, 190.4644691013067472 ) ) ;
#49907=CARTESIAN_POINT ( 'NONE',  ( 70.45866099340145183, -57.68246761816307355, 157.7518986473937161 ) ) ;
#49911=CARTESIAN_POINT ( 'NONE',  ( 23.84453580884438395, -27.27310615191336396, -38.40431109410636168 ) ) ;
#49914=CARTESIAN_POINT ( 'NONE',  ( -38.97755016977858844, -60.00000000000000000, 50.71592569719196320 ) ) ;
#49918=CARTESIAN_POINT ( 'NONE',  ( -86.89680602446821922, -28.03361883784057795, 186.5272980465382489 ) ) ;
#49922=CARTESIAN_POINT ( 'NONE',  ( -7.997530052830874148, -18.58626440210924002, 26.97989019616458961 ) ) ;
#49938=CARTESIAN_POINT ( 'NONE',  ( 113.8520663817495233, -59.99999999999995026, 157.1483003829898450 ) ) ;
#49956=CARTESIAN_POINT ( 'NONE',  ( -67.57337042125921300, -59.99999999999997868, 141.1407361875824051 ) ) ;
#49960=CARTESIAN_POINT ( 'NONE',  ( 101.0978150197463492, -59.99999999999998579, 201.5160938181417407 ) ) ;
#49961=CARTESIAN_POINT ( 'NONE',  ( -77.87378252178784521, -14.21045842199420228, 157.7502635463301317 ) ) ;
#49962=CARTESIAN_POINT ( 'NONE',  ( 14.28806202503381684, -22.06801482742367071, 27.67556484836572039 ) ) ;
#49967=CARTESIAN_POINT ( 'NONE',  ( -42.62392613728367508, -25.70309449447480432, 37.69303809212602374 ) ) ;
#49979=CARTESIAN_POINT ( 'NONE',  ( 78.63367630571566735, -29.99999999999999289, -15.31311550526425691 ) ) ;
#49984=CARTESIAN_POINT ( 'NONE',  ( 83.29267879008702380, -30.00000000000001421, 45.23466661269899447 ) ) ;
#50004=CARTESIAN_POINT ( 'NONE',  ( 81.77512476957420517, -38.84160798149201810, 195.6174134348494533 ) ) ;
#50018=CARTESIAN_POINT ( 'NONE',  ( 33.64224579327841980, -34.75806849055473435, 43.05022256185317531 ) ) ;
#50023=CARTESIAN_POINT ( 'NONE',  ( 85.78132872117437557, -35.63418972109697336, 184.6297816553372400 ) ) ;
#50027=CARTESIAN_POINT ( 'NONE',  ( 94.55070737517196733, -57.65490497192584485, -10.62783235369682799 ) ) ;
#50031=CARTESIAN_POINT ( 'NONE',  ( -81.02929317658217201, -29.99999999999999645, 3.510823643410445172 ) ) ;
#50050=CARTESIAN_POINT ( 'NONE',  ( -45.60865816377937421, -26.43209940392021906, -29.05745762912890484 ) ) ;
#50064=CARTESIAN_POINT ( 'NONE',  ( -59.89870783239705077, -60.00000000000000000, -35.70476153864051838 ) ) ;
#50068=CARTESIAN_POINT ( 'NONE',  ( 100.3141319396906823, -45.27614848971162331, 192.2799094378773361 ) ) ;
#50074=ORIENTED_EDGE ( 'NONE', *, *, #89227, .F. ) ;
#50084=CARTESIAN_POINT ( 'NONE',  ( -35.73279548032036956, -57.69589661319782437, 49.90756511973714282 ) ) ;
#50090=CARTESIAN_POINT ( 'NONE',  ( -94.21198422502472170, -59.99999999999998579, 13.85022971857252649 ) ) ;
#50092=CARTESIAN_POINT ( 'NONE',  ( -50.33888081872743214, -56.83758401715910225, 57.28329760184606556 ) ) ;
#50097=CARTESIAN_POINT ( 'NONE',  ( -96.88649155114819678, -45.25226034781319839, 194.0198334961624482 ) ) ;
#50102=CARTESIAN_POINT ( 'NONE',  ( 105.6520087378447528, -38.38240529042644766, 196.7784137681985612 ) ) ;
#50107=CARTESIAN_POINT ( 'NONE',  ( 85.25636826630055509, -30.00000000000000000, 172.6984853744677082 ) ) ;
#50115=CARTESIAN_POINT ( 'NONE',  ( 51.77002234501873090, -42.97291842264748141, 55.07874347774893664 ) ) ;
#50120=CARTESIAN_POINT ( 'NONE',  ( -108.0788720051916414, -38.35628241340692313, 138.4083630056905747 ) ) ;
#50122=CARTESIAN_POINT ( 'NONE',  ( 106.6080917448352778, -38.35597051698264437, 127.9552692107341301 ) ) ;
#50124=CARTESIAN_POINT ( 'NONE',  ( 82.71878536663017201, -37.85263159083670104, 22.06153483090329104 ) ) ;
#50125=FACE_OUTER_BOUND ( 'NONE', #48793, .T. ) ;
#50128=CARTESIAN_POINT ( 'NONE',  ( 74.36184181517107561, -60.00000000000000711, 175.8036861163617743 ) ) ;
#50133=CARTESIAN_POINT ( 'NONE',  ( 62.23191167537439838, -46.43536929189312445, 81.72875552745274774 ) ) ;
#50138=CARTESIAN_POINT ( 'NONE',  ( -76.84754332433912793, -29.99999999997301359, 173.7522665578053704 ) ) ;
#50151=CARTESIAN_POINT ( 'NONE',  ( 83.18190987619777843, -46.51210091988467354, 180.8283602554456877 ) ) ;
#50160=CARTESIAN_POINT ( 'NONE',  ( -27.36171982050201024, -28.59563504858160599, -38.29070100074284966 ) ) ;
#50165=CARTESIAN_POINT ( 'NONE',  ( 54.03418529048751395, -60.00000000000000000, 82.52390411942170090 ) ) ;
#50167=CARTESIAN_POINT ( 'NONE',  ( 6.808966170647585692, -13.13057375426282825, 32.04009476704212034 ) ) ;
#50168=CARTESIAN_POINT ( 'NONE',  ( -24.00273426019377965, -28.36012771311524361, 37.92953909826832870 ) ) ;
#50179=CARTESIAN_POINT ( 'NONE',  ( 2.499999999999984457, -21.99834388059804269, -30.53959902372158908 ) ) ;
#50180=CARTESIAN_POINT ( 'NONE',  ( 28.77839882463454657, -47.40898664704774035, -33.14052421978329477 ) ) ;
#50192=CARTESIAN_POINT ( 'NONE',  ( -98.09066009260625663, -60.00000000000000711, 69.48659794401923762 ) ) ;
#50198=CARTESIAN_POINT ( 'NONE',  ( -82.28169001980204200, -46.46948612797371680, 174.1992972938939772 ) ) ;
#50204=ORIENTED_EDGE ( 'NONE', *, *, #38286, .F. ) ;
#50209=CARTESIAN_POINT ( 'NONE',  ( -47.47329288218261922, -57.67116814553164517, -40.40967777935767202 ) ) ;
#50216=CARTESIAN_POINT ( 'NONE',  ( 108.0662294780436383, -29.99999999999999645, 149.4678247624379708 ) ) ;
#50218=CARTESIAN_POINT ( 'NONE',  ( -114.4010969832937121, -60.00000000000006395, 179.2248356726699399 ) ) ;
#50219=CARTESIAN_POINT ( 'NONE',  ( -57.65532094949794839, -49.91396688608944743, 71.01409991697076407 ) ) ;
#50222=CARTESIAN_POINT ( 'NONE',  ( 113.4579317004694445, -59.99999999998775024, 187.0486580085058961 ) ) ;
#50224=CARTESIAN_POINT ( 'NONE',  ( 6.036068601854779558, -29.02932134256533203, 28.71825046550461380 ) ) ;
#50225=CARTESIAN_POINT ( 'NONE',  ( -100.3227765610642734, -37.82072275983777843, 142.2249858778365876 ) ) ;
#50231=CARTESIAN_POINT ( 'NONE',  ( -29.92534626571542944, -60.00000000000000000, 42.99766300317948975 ) ) ;
#50235=CARTESIAN_POINT ( 'NONE',  ( -89.99999999999997158, -60.00000000000000000, 196.0238439516549818 ) ) ;
#50241=CARTESIAN_POINT ( 'NONE',  ( 103.9527125734255861, -59.99999999999999289, 141.3402690312935874 ) ) ;
#50242=CARTESIAN_POINT ( 'NONE',  ( -32.67571524685207862, -36.02606224958812930, 33.54986086304085546 ) ) ;
#50245=CARTESIAN_POINT ( 'NONE',  ( 44.85640785158575738, -46.43708517621621468, 45.33465009235806065 ) ) ;
#50251=CARTESIAN_POINT ( 'NONE',  ( -81.54857902955093607, -38.84165332927102554, 195.3365240599568153 ) ) ;
#50252=ORIENTED_EDGE ( 'NONE', *, *, #60320, .T. ) ;
#50255=CARTESIAN_POINT ( 'NONE',  ( 50.11938532533323354, -59.99999999999997868, 57.93673938823967973 ) ) ;
#50262=CARTESIAN_POINT ( 'NONE',  ( 103.3162346027592804, -59.99999999999999289, 100.4319430175666810 ) ) ;
#50267=CARTESIAN_POINT ( 'NONE',  ( -101.1327230100927181, -30.00000000000000355, 173.0889935382795954 ) ) ;
#50277=CARTESIAN_POINT ( 'NONE',  ( 84.58095252641739137, -25.55800566126467999, 162.3696887303881056 ) ) ;
#50290=B_SPLINE_CURVE_WITH_KNOTS ( 'NONE', 3,
 ( #24983, #96348, #22476, #24469, #74030, #90222, #49218, #70991, #81565, #5720, #95809, #41671, #103879, #55319, #73488, #16877, #74559, #8765, #16327, #32548, #88245, #71507, #62913, #90761, #30028, #632, #21938, #47232, #13269, #54788, #82115, #87718, #13802, #104409, #46711, #33600, #65420, #8235, #109, #7695, #41146, #49757, #5204, #82663, #95282, #21410, #54247, #46191 ),
 .UNSPECIFIED., .F., .F.,
 ( 4, 2, 2, 2, 2, 2, 2, 2, 2, 2, 1, 2, 2, 1, 2, 2, 2, 2, 2, 2, 2, 2, 2, 2, 4 ),
 ( 1.003362932294564080, 1.007956983089783654, 1.012551033885003005, 1.021739135475442151, 1.030927237065881075, 1.040115338656319999, 1.049303440246759145, 1.058491541837198069, 1.067679643427636993, 1.076867745018076139, 1.078016257716881032, 1.078303385891582256, 1.078590514066283479, 1.079164770415685926, 1.081461795813295490, 1.086055846608515063, 1.095243948198953987, 1.104432049789393133, 1.113620151379832057, 1.122808252970271203, 1.127402303765490554, 1.131996354560710127, 1.141184456151149273, 1.145778506946368624, 1.150372557741588198 ),
 .UNSPECIFIED. ) ;
#50310=CARTESIAN_POINT ( 'NONE',  ( 109.9183362485910749, -57.66822971772113959, 196.2431448240839700 ) ) ;
#50317=CARTESIAN_POINT ( 'NONE',  ( -76.86091367493919790, -60.00000000000000000, 190.0407920036354597 ) ) ;
#50320=CARTESIAN_POINT ( 'NONE',  ( -84.73889666017791455, -39.38651883830629430, 182.5246982632422714 ) ) ;
#50327=CARTESIAN_POINT ( 'NONE',  ( -83.25032691496221560, -37.78210659561245421, -7.769091474988147894 ) ) ;
#50335=CARTESIAN_POINT ( 'NONE',  ( -61.70175965769652748, -30.00000000000001066, -32.45223383460360367 ) ) ;
#50336=CARTESIAN_POINT ( 'NONE',  ( -66.15153670451748269, -56.86596900142542665, 99.15932261016065752 ) ) ;
#50337=ORIENTED_EDGE ( 'NONE', *, *, #8991, .T. ) ;
#50338=CARTESIAN_POINT ( 'NONE',  ( 68.99587917277882809, -30.00000000000005329, 123.4883035811859884 ) ) ;
#50339=CARTESIAN_POINT ( 'NONE',  ( 94.71841002673514254, -57.66036132024994743, -7.141312747736634492 ) ) ;
#50350=CARTESIAN_POINT ( 'NONE',  ( 12.64023069600374960, -4.285714285714294469, -21.88880945939638067 ) ) ;
#50359=CARTESIAN_POINT ( 'NONE',  ( 33.11060381627214610, -49.89861181656793576, 36.32314459125598916 ) ) ;
#50373=CARTESIAN_POINT ( 'NONE',  ( 92.73990332427236183, -59.99999999999999289, -6.443125037031961710 ) ) ;
#50386=CARTESIAN_POINT ( 'NONE',  ( 86.98871639540843148, -60.17830634995334549, -5.043400601815899442 ) ) ;
#50398=CARTESIAN_POINT ( 'NONE',  ( 76.47493250985364455, -53.37270521551824487, 138.8582642167188794 ) ) ;
#50403=CARTESIAN_POINT ( 'NONE',  ( -83.13494729127086202, -57.67105474064026538, -28.32277909022158724 ) ) ;
#50407=CARTESIAN_POINT ( 'NONE',  ( 106.4188425553138302, -60.15150696938596298, 177.5013719461561266 ) ) ;
#50418=CARTESIAN_POINT ( 'NONE',  ( 9.999999999999998224, -15.00000000000000000, -9.999999999999998224 ) ) ;
#50425=CARTESIAN_POINT ( 'NONE',  ( 4.268270791835775846, -59.99999999999998579, 39.63076618222462599 ) ) ;
#50426=CARTESIAN_POINT ( 'NONE',  ( -84.52869890352867799, -29.99999999999999289, 165.8509777010769426 ) ) ;
#50430=CARTESIAN_POINT ( 'NONE',  ( 71.20881682316100125, -57.68098021455711688, 164.2442580483489962 ) ) ;
#50434=CARTESIAN_POINT ( 'NONE',  ( 12.43520736934317483, -23.27680199471840439, -38.53969105432245357 ) ) ;
#50437=CARTESIAN_POINT ( 'NONE',  ( -47.25096821319525731, -60.00000000000000711, 65.33942938962390201 ) ) ;
#50440=CARTESIAN_POINT ( 'NONE',  ( -85.55236343420649803, -61.06994240337794366, 193.9676891635616585 ) ) ;
#50443=CARTESIAN_POINT ( 'NONE',  ( -6.142256572465674580, -46.43922209401467427, 31.61959343549931845 ) ) ;
#50460=CARTESIAN_POINT ( 'NONE',  ( 109.0466504562702141, -30.00000000000000355, 159.8086616330221830 ) ) ;
#50461=CARTESIAN_POINT ( 'NONE',  ( -81.74677077760871668, -42.97261976273406958, 163.6235584250746058 ) ) ;
#50479=ORIENTED_EDGE ( 'NONE', *, *, #106183, .F. ) ;
#50480=CARTESIAN_POINT ( 'NONE',  ( 111.0015139017943540, -60.00000000000001421, 187.3024812079267463 ) ) ;
#50481=CARTESIAN_POINT ( 'NONE',  ( -71.28683113122063730, -60.00000000000007816, 168.6212938583825292 ) ) ;
#50482=CARTESIAN_POINT ( 'NONE',  ( 16.95927991814305003, -49.91546993179999703, 32.46382548788433553 ) ) ;
#50483=CARTESIAN_POINT ( 'NONE',  ( 83.17034439044972771, -37.99999999999994316, -9.670047016417147034 ) ) ;
#50485=CARTESIAN_POINT ( 'NONE',  ( -40.48299353324593852, -22.23726300500976194, 35.13222277374845248 ) ) ;
#50499=CARTESIAN_POINT ( 'NONE',  ( 81.49414201415379466, -30.00000000000006040, -9.315152446787697826 ) ) ;
#50504=CARTESIAN_POINT ( 'NONE',  ( 80.95415150621239775, -30.00000000000000000, 4.843109486027489474 ) ) ;
#50508=ORIENTED_EDGE ( 'NONE', *, *, #90266, .T. ) ;
#50519=CARTESIAN_POINT ( 'NONE',  ( 74.67842920201081824, -38.33200830287892558, 166.4539110603844279 ) ) ;
#50540=CARTESIAN_POINT ( 'NONE',  ( 86.30666900314933798, -21.08433947227320360, 179.9884049068863305 ) ) ;
#50544=CARTESIAN_POINT ( 'NONE',  ( 83.09486208724929668, -57.67107040063709888, -28.34176565233813250 ) ) ;
#50549=CARTESIAN_POINT ( 'NONE',  ( -81.40926587446145390, -30.00000000000000000, -9.992568410953589719 ) ) ;
#50561=CARTESIAN_POINT ( 'NONE',  ( -98.86074489839170099, -37.99999999999991473, 192.0568120749455829 ) ) ;
#50566=CARTESIAN_POINT ( 'NONE',  ( -38.67654687014966441, -24.46767789941978677, -30.56595494665695512 ) ) ;
#50576=CARTESIAN_POINT ( 'NONE',  ( -51.17622358944377936, -60.00000000000000000, -37.67033473011792211 ) ) ;
#50580=CARTESIAN_POINT ( 'NONE',  ( 103.0186286448298745, -60.16906176935165007, 192.8004402776240340 ) ) ;
#50597=CARTESIAN_POINT ( 'NONE',  ( -69.31411742845799040, -57.68241165371757262, 149.3509116208381329 ) ) ;
#50602=CARTESIAN_POINT ( 'NONE',  ( -89.36642547188127139, -29.99999999999995381, 5.438168021589780743 ) ) ;
#50603=CARTESIAN_POINT ( 'NONE',  ( -49.32002684479864740, -39.51885134585224080, 49.64505812268525631 ) ) ;
#50606=CARTESIAN_POINT ( 'NONE',  ( -97.07210653995934990, -60.35970870470556093, 196.7639714328392415 ) ) ;
#50611=CARTESIAN_POINT ( 'NONE',  ( 100.5869678965343610, -38.46297986693701887, 200.3470908674215707 ) ) ;
#50616=CARTESIAN_POINT ( 'NONE',  ( 87.06605025660013553, -30.00000000000000000, 183.9618747148463740 ) ) ;
#50624=CARTESIAN_POINT ( 'NONE',  ( 51.52558495347906131, -32.57909100336876662, 50.96452728205734672 ) ) ;
#50628=CARTESIAN_POINT ( 'NONE',  ( -110.5377068114738108, -38.35610058096415287, 161.0159699682552343 ) ) ;
#50631=CARTESIAN_POINT ( 'NONE',  ( 110.2494631951638127, -38.35601185217798559, 184.3351315308087806 ) ) ;
#50633=CARTESIAN_POINT ( 'NONE',  ( 86.15997024733299270, -37.84900569248561908, 53.97426573764452229 ) ) ;
#50634=CARTESIAN_POINT ( 'NONE',  ( 0.000000000000000000, -30.00000000000000000, 0.000000000000000000 ) ) ;
#50636=CARTESIAN_POINT ( 'NONE',  ( 76.19063985184907040, -60.00000000000000000, 187.7640617696651191 ) ) ;
#50640=CARTESIAN_POINT ( 'NONE',  ( 59.90236492691475689, -49.91050096998650076, 76.94228515587644779 ) ) ;
#50650=CARTESIAN_POINT ( 'NONE',  ( -22.24914325797420389, -18.02156853467999653, 31.43918858065762478 ) ) ;
#50654=CARTESIAN_POINT ( 'NONE',  ( 84.85119566129066015, -32.34994737913991258, 176.2922552301222936 ) ) ;
#50664=CARTESIAN_POINT ( 'NONE',  ( -21.95063819072343492, -26.56093263958899087, -38.44887722113407591 ) ) ;
#50670=CARTESIAN_POINT ( 'NONE',  ( 50.71755735396195774, -60.00000000000000711, 73.61387294642976542 ) ) ;
#50672=CARTESIAN_POINT ( 'NONE',  ( 1.787493240145907603, -12.60618723787961315, 32.17814028491976330 ) ) ;
#50673=CARTESIAN_POINT ( 'NONE',  ( -20.54080512885244048, -26.05094486570658319, 36.94806580626582360 ) ) ;
#50675=FACE_OUTER_BOUND ( 'NONE', #31830, .T. ) ;
#50681=CARTESIAN_POINT ( 'NONE',  ( 4.540089413576434474, -21.58519901417236042, -38.54822756895638491 ) ) ;
#50686=CARTESIAN_POINT ( 'NONE',  ( 35.14719567999821948, -47.40883101621029994, -32.39563694789472237 ) ) ;
#50699=CARTESIAN_POINT ( 'NONE',  ( -95.01606930152259167, -59.99999999999999289, 49.16530457434027568 ) ) ;
#50708=CARTESIAN_POINT ( 'NONE',  ( -80.87069194252994464, -60.49237983335919466, 182.4063684378278651 ) ) ;
#50719=SURFACE_STYLE_USAGE ( .BOTH. , #16787 ) ;
#50724=CARTESIAN_POINT ( 'NONE',  ( -97.47674776263787066, -60.00000000000000000, 196.6139650356533934 ) ) ;
#50725=CARTESIAN_POINT ( 'NONE',  ( 88.56622727954015772, -14.21045842199445630, 40.39835639566682346 ) ) ;
#50727=CARTESIAN_POINT ( 'NONE',  ( -77.57376394631657490, -29.99999999999998934, 180.9696502640093172 ) ) ;
#50728=CARTESIAN_POINT ( 'NONE',  ( -56.87924109845976517, -49.91323546493563157, 69.03781967801916153 ) ) ;
#50731=CARTESIAN_POINT ( 'NONE',  ( 19.87093931444394102, -60.00000000000000000, 40.18337028875610883 ) ) ;
#50733=CARTESIAN_POINT ( 'NONE',  ( 5.051333850944835113, -35.99138616323499207, 29.87840771616124869 ) ) ;
#50734=CARTESIAN_POINT ( 'NONE',  ( -102.2537717332236440, -37.82053749917956509, 182.3686263342081588 ) ) ;
#50741=CARTESIAN_POINT ( 'NONE',  ( -49.50947049896235086, -59.99999999999998579, 70.55260509993409812 ) ) ;
#50747=CARTESIAN_POINT ( 'NONE',  ( -0.01431428620034891179, -57.67120202577072519, -44.61186648040676772 ) ) ;
#50754=CARTESIAN_POINT ( 'NONE',  ( -31.39360692306285117, -29.07856664448081219, 31.74873827322397091 ) ) ;
#50756=CARTESIAN_POINT ( 'NONE',  ( 44.07113633205571546, -46.43536708221260056, 44.37285927327917534 ) ) ;
#50760=CARTESIAN_POINT ( 'NONE',  ( -80.08513989354706553, -38.78833375829605501, 193.1411605214941005 ) ) ;
#50764=CARTESIAN_POINT ( 'NONE',  ( 4.175852187281085648, -59.99999999999998579, 33.87838816770964456 ) ) ;
#50771=CARTESIAN_POINT ( 'NONE',  ( 103.5882826872034457, -60.00000000000000711, 102.0264544966379106 ) ) ;
#50777=CARTESIAN_POINT ( 'NONE',  ( -90.96836049887622266, -29.99999999999996447, 190.4758564127751583 ) ) ;
#50794=CARTESIAN_POINT ( 'NONE',  ( 79.60221368316047119, -60.33621870816789823, 171.0006651665154607 ) ) ;
#50813=CARTESIAN_POINT ( 'NONE',  ( 86.94938139748957440, -20.65577565933631732, 186.2948166322831867 ) ) ;
#50829=CARTESIAN_POINT ( 'NONE',  ( 109.2576472045765428, -57.67135000464508465, 124.2156221577730975 ) ) ;
#50837=CARTESIAN_POINT ( 'NONE',  ( -82.60176852780435297, -60.00000000000000711, 198.5318555412940214 ) ) ;
#50842=CARTESIAN_POINT ( 'NONE',  ( -84.63742604999939090, -42.97016984000447337, 184.5374066289867585 ) ) ;
#50850=CARTESIAN_POINT ( 'NONE',  ( -85.70201354400094829, -52.74627078913300693, -8.673989746495539777 ) ) ;
#50858=CARTESIAN_POINT ( 'NONE',  ( 76.70261674817732001, -29.99999999999993250, 172.7038044719299990 ) ) ;
#50860=CARTESIAN_POINT ( 'NONE',  ( 8.555192725956649369, -60.00000000000006395, -44.87746236044966253 ) ) ;
#50861=CARTESIAN_POINT ( 'NONE',  ( -74.51172177323695678, -22.12478468806351017, 106.6322136500146627 ) ) ;
#50864=CARTESIAN_POINT ( 'NONE',  ( 76.70261674817732001, -29.99999999999993250, 172.7038044719299990 ) ) ;
#50866=CARTESIAN_POINT ( 'NONE',  ( 111.2848894786437342, -57.67078734050053868, 193.4929494032239745 ) ) ;
#50879=DIRECTION ( 'NONE',  ( -1.000000000000000000, 0.000000000000000000, 8.673617379884035472E-17 ) ) ;
#50888=CARTESIAN_POINT ( 'NONE',  ( 34.27415957760879195, -60.29897218423202077, 38.86718388344454667 ) ) ;
#50902=CARTESIAN_POINT ( 'NONE',  ( 68.98189563180189054, -60.00000000000000711, -32.94317599190360113 ) ) ;
#50916=CARTESIAN_POINT ( 'NONE',  ( 83.12214618901758456, -45.27717091314015363, -14.26087837487842869 ) ) ;
#50928=CARTESIAN_POINT ( 'NONE',  ( 73.44948613080914868, -36.01487196046611672, 111.7734220330967361 ) ) ;
#50934=CARTESIAN_POINT ( 'NONE',  ( -91.04381008827128596, -57.66401771476134996, -20.86613467659797649 ) ) ;
#50938=CARTESIAN_POINT ( 'NONE',  ( 105.5033247266267438, -60.15119772182732305, 185.5882202471690618 ) ) ;
#50948=CARTESIAN_POINT ( 'NONE',  ( 97.47675437802963927, -60.00000000000000000, 196.6138812136176739 ) ) ;
#50956=CARTESIAN_POINT ( 'NONE',  ( -84.25785865898413363, -30.00000000000000000, 163.3270934916272097 ) ) ;
#50961=CARTESIAN_POINT ( 'NONE',  ( 70.98554509634433884, -57.68173086340836164, 162.1951512261919675 ) ) ;
#50963=PLANE ( 'NONE',  #75842 ) ;
#50965=CARTESIAN_POINT ( 'NONE',  ( 40.50854106486515605, -33.09212884851145731, -37.39549675235985404 ) ) ;
#50968=CARTESIAN_POINT ( 'NONE',  ( -43.22294892181861314, -59.99999999999999289, 57.26282192755943612 ) ) ;
#50970=CARTESIAN_POINT ( 'NONE',  ( -86.74237309757550918, -39.12072068744619457, 188.5955380950024960 ) ) ;
#50973=CARTESIAN_POINT ( 'NONE',  ( -4.005429499995301512, -29.03095694028940343, 28.72119633659973204 ) ) ;
#50988=CARTESIAN_POINT ( 'NONE',  ( 106.9311160729171917, -14.21045842199435860, 169.9238089813113390 ) ) ;
#50989=CARTESIAN_POINT ( 'NONE',  ( -79.39540201253396390, -56.85378631388855553, 163.2853465063474232 ) ) ;
#50990=VERTEX_POINT ( 'NONE', #64868 ) ;
#50996=EDGE_CURVE ( 'NONE', #93158, #61487, #62325, .T. ) ;
#51010=CARTESIAN_POINT ( 'NONE',  ( 100.0806260828529162, -60.00000000000001421, 201.8633356714223339 ) ) ;
#51012=CARTESIAN_POINT ( 'NONE',  ( -97.75001763179835734, -59.99999999999991473, 204.9118596629033675 ) ) ;
#51013=CARTESIAN_POINT ( 'NONE',  ( 20.58328600930757801, -56.87559710208555686, 33.96513392023969402 ) ) ;
#51018=CARTESIAN_POINT ( 'NONE',  ( -43.67735976744434367, -29.16186524003355274, 39.50783654124030164 ) ) ;
#51033=CARTESIAN_POINT ( 'NONE',  ( 81.29237555794308889, -30.00000000000015987, -10.77076475157867463 ) ) ;
#51038=CARTESIAN_POINT ( 'NONE',  ( 80.94845987451680003, -30.00000000000001066, 4.951624427427304909 ) ) ;
#51052=CARTESIAN_POINT ( 'NONE',  ( 66.27348762673410931, -38.33599680880077187, 118.2887617752395784 ) ) ;
#51064=ORIENTED_EDGE ( 'NONE', *, *, #11707, .F. ) ;
#51069=DIRECTION ( 'NONE',  ( 0.000000000000000000, 0.000000000000000000, -1.000000000000000000 ) ) ;
#51073=CARTESIAN_POINT ( 'NONE',  ( 86.04703566227567535, -31.95183572172941666, 184.0160242643544279 ) ) ;
#51078=CARTESIAN_POINT ( 'NONE',  ( 94.69864826002789471, -57.66440398302673032, -5.036685645262155120 ) ) ;
#51082=CARTESIAN_POINT ( 'NONE',  ( -81.89555708626969022, -30.00000000000000355, 32.87881983670175856 ) ) ;
#51092=CARTESIAN_POINT ( 'NONE',  ( -39.28066024253707411, -34.89573333781912368, 37.03216938462795582 ) ) ;
#51093=DIRECTION ( 'NONE',  ( 0.000000000000000000, 0.000000000000000000, -1.000000000000000000 ) ) ;
#51100=CARTESIAN_POINT ( 'NONE',  ( 47.72628330118641315, -26.96252987353755159, -28.54815866115082912 ) ) ;
#51101=CARTESIAN_POINT ( 'NONE',  ( -22.90482800453732537, -53.39944789579089246, 33.72992494732504554 ) ) ;
#51108=CARTESIAN_POINT ( 'NONE',  ( -40.31725178085623185, -24.96478901505654591, -30.23181082201408998 ) ) ;
#51121=CARTESIAN_POINT ( 'NONE',  ( 99.09806703519338100, -37.80934666507823749, 191.7968710950989646 ) ) ;
#51138=CARTESIAN_POINT ( 'NONE',  ( -29.91071955673133687, -57.68399870184025247, 45.22199076326395328 ) ) ;
#51142=CARTESIAN_POINT ( 'NONE',  ( -90.08857655234534434, -29.99999999999997158, -9.079940112750868764 ) ) ;
#51145=CARTESIAN_POINT ( 'NONE',  ( -50.70036326620968481, -42.97893239173847491, 53.12086675882575548 ) ) ;
#51153=CARTESIAN_POINT ( 'NONE',  ( 90.40984625334591840, -38.51012991717329470, 200.6755570011027885 ) ) ;
#51156=ADVANCED_FACE ( 'NONE', ( #49071 ), #103419, .T. ) ;
#51158=CARTESIAN_POINT ( 'NONE',  ( 94.46887059736158676, -30.00000000000000355, 191.3163273378258964 ) ) ;
#51163=CARTESIAN_POINT ( 'NONE',  ( 51.33347871815171004, -56.83565511434251505, 59.27340484389767283 ) ) ;
#51168=CARTESIAN_POINT ( 'NONE',  ( -90.37015026637372728, -38.40145438430572966, -14.97427795305133458 ) ) ;
#51170=CARTESIAN_POINT ( 'NONE',  ( 108.3039360038514332, -38.35759540363747533, 192.1380689804155111 ) ) ;
#51173=CARTESIAN_POINT ( 'NONE',  ( 86.85184780015545414, -37.84892900490719825, 58.81766505457247973 ) ) ;
#51185=CARTESIAN_POINT ( 'NONE',  ( 62.49820474788960922, -18.63632920802682946, 68.77955571764800879 ) ) ;
#51195=CARTESIAN_POINT ( 'NONE',  ( -39.00146644722711642, -25.89668121096503128, 35.32705130283117256 ) ) ;
#51200=CARTESIAN_POINT ( 'NONE',  ( 83.13910501099707062, -50.07829878328394102, 183.9083247637312013 ) ) ;
#51201=CARTESIAN_POINT ( 'NONE',  ( -85.08119784002818164, -52.74728882239156036, 190.3170911141409363 ) ) ;
#51209=CARTESIAN_POINT ( 'NONE',  ( -33.64427641176231276, -30.86707006437501377, -37.96572353344528494 ) ) ;
#51211=CARTESIAN_POINT ( 'NONE',  ( 43.66925938860883605, -60.00000000000000711, 58.07216833024137514 ) ) ;
#51213=CARTESIAN_POINT ( 'NONE',  ( 0.8955584045642486224, -12.57757061814721311, 32.18682162422354054 ) ) ;
#51214=CARTESIAN_POINT ( 'NONE',  ( -30.07121567580392352, -32.49802967840809487, 40.61539330391480718 ) ) ;
#51216=DIRECTION ( 'NONE',  ( 0.000000000000000000, 1.000000000000000000, 0.000000000000000000 ) ) ;
#51227=CARTESIAN_POINT ( 'NONE',  ( 56.20992259933385782, -34.58943827994583131, -26.29397140020956058 ) ) ;
#51237=CARTESIAN_POINT ( 'NONE',  ( -103.7318945818505682, -60.00000000000000000, 102.8686475082603948 ) ) ;
#51241=CIRCLE ( 'NONE', #4780, 2.000000000000001776 ) ;
#51246=CARTESIAN_POINT ( 'NONE',  ( -85.58036756573783066, -21.94021760482315742, 167.0675817319834664 ) ) ;
#51251=LINE ( 'NONE', #67992, #71659 ) ;
#51265=CARTESIAN_POINT ( 'NONE',  ( -97.05546387255228069, -41.67764191913797589, 193.4168471130767841 ) ) ;
#51267=CARTESIAN_POINT ( 'NONE',  ( 106.1195120942077494, -59.99999999999999289, 102.8136370513695397 ) ) ;
#51268=EDGE_CURVE ( 'NONE', #70795, #57621, #53680, .T. ) ;
#51269=CARTESIAN_POINT ( 'NONE',  ( -78.42710814205257464, -14.21045842199423070, 185.4825180806740548 ) ) ;
#51270=CARTESIAN_POINT ( 'NONE',  ( -59.97371036787195209, -22.12477874294765812, 64.13592450898646291 ) ) ;
#51275=CARTESIAN_POINT ( 'NONE',  ( -100.3409567365024770, -37.81725092391206289, 189.9219167037537375 ) ) ;
#51281=CARTESIAN_POINT ( 'NONE',  ( -72.75504568474596567, -59.99999999999998579, 160.2259072040645265 ) ) ;
#51287=CARTESIAN_POINT ( 'NONE',  ( 4.418225343310108855, -0.000000000000000000, 16.46939662769216994 ) ) ;
#51294=CARTESIAN_POINT ( 'NONE',  ( -29.36599388881087691, -18.64463543894338926, 29.18619376988382541 ) ) ;
#51297=CARTESIAN_POINT ( 'NONE',  ( 44.14039507018947717, -49.88908620783357861, 45.35107315698084562 ) ) ;
#51300=CARTESIAN_POINT ( 'NONE',  ( -76.27725968842102588, -38.39574923406762252, 180.3589007190480231 ) ) ;
#51303=CARTESIAN_POINT ( 'NONE',  ( 80.72320425233836261, -59.99999999999997868, 180.7930442462130998 ) ) ;
#51304=DIRECTION ( 'NONE',  ( -1.000000000000000000, -0.000000000000000000, -0.000000000000000000 ) ) ;
#51311=CARTESIAN_POINT ( 'NONE',  ( 106.3919580027218359, -60.00000000000000000, 118.8438529489762772 ) ) ;
#51332=UNCERTAINTY_MEASURE_WITH_UNIT (LENGTH_MEASURE( 1.000000000000000082E-05 ), #68050, 'distance_accuracy_value', 'NONE');
#51338=CARTESIAN_POINT ( 'NONE',  ( 81.52133577384425678, -42.96784206407738083, 161.5630992417780192 ) ) ;
#51355=CARTESIAN_POINT ( 'NONE',  ( 87.18997347856540614, -27.99825934505209446, 187.4553388889137864 ) ) ;
#51376=CARTESIAN_POINT ( 'NONE',  ( -92.26493084220614094, -60.00000000000000711, 202.3836785854439029 ) ) ;
#51382=CARTESIAN_POINT ( 'NONE',  ( -85.55559475948190595, -32.12731255185389756, 181.4392504528566690 ) ) ;
#51386=EDGE_CURVE ( 'NONE', #24767, #95473, #10702, .T. ) ;
#51389=CARTESIAN_POINT ( 'NONE',  ( -86.51528361792135513, -60.14074312227410246, 2.089646723163113062 ) ) ;
#51400=CARTESIAN_POINT ( 'NONE',  ( 69.92546618954501980, -29.99999999999995026, 127.5380661880360975 ) ) ;
#51403=CARTESIAN_POINT ( 'NONE',  ( -82.54102867968215662, -60.00000000000007105, -29.20875881225653004 ) ) ;
#51404=CARTESIAN_POINT ( 'NONE',  ( -72.38508955459566607, -49.91119473924621985, 116.9164654461183659 ) ) ;
#51406=CARTESIAN_POINT ( 'NONE',  ( 64.23331706704713895, -60.00000000000004263, 125.0204823638418361 ) ) ;
#51408=CARTESIAN_POINT ( 'NONE',  ( 47.37111856022713141, -57.67116701030797543, -40.42796442818178093 ) ) ;
#51422=CARTESIAN_POINT ( 'NONE',  ( 15.38541618194247995, -4.285714285714296246, -20.05453516056602226 ) ) ;
#51431=CARTESIAN_POINT ( 'NONE',  ( 33.96413472286053548, -60.30148985827285202, 38.68745865078301449 ) ) ;
#51432=CARTESIAN_POINT ( 'NONE',  ( 12.70248734011840597, -4.285714285713678073, -22.03900363279143093 ) ) ;
#51447=CARTESIAN_POINT ( 'NONE',  ( 90.03398063620191749, -59.99999999999999289, -18.77590310472173130 ) ) ;
#51460=CARTESIAN_POINT ( 'NONE',  ( 85.33315027561728527, -52.75744043830332686, -11.76120068538829422 ) ) ;
#51468=ORIENTED_EDGE ( 'NONE', *, *, #9174, .T. ) ;
#51472=ORIENTED_EDGE ( 'NONE', *, *, #18492, .T. ) ;
#51473=CARTESIAN_POINT ( 'NONE',  ( 73.18364344897008777, -39.48763927256371886, 113.0589750438585241 ) ) ;
#51479=CARTESIAN_POINT ( 'NONE',  ( -94.31942352638992588, -57.67240272246704791, 24.69011299903190704 ) ) ;
#51482=CARTESIAN_POINT ( 'NONE',  ( 102.6007214329574140, -37.84836329290174461, 179.2133943646480532 ) ) ;
#51500=CARTESIAN_POINT ( 'NONE',  ( -85.08044947619957554, -30.00000000000000355, 171.0774529994631905 ) ) ;
#51504=CARTESIAN_POINT ( 'NONE',  ( 72.46853216154282507, -57.66608118650142245, 176.6536213893129741 ) ) ;
#51510=CARTESIAN_POINT ( 'NONE',  ( 25.63403565826709141, -27.94712950634049164, -38.35231772936518979 ) ) ;
#51513=CARTESIAN_POINT ( 'NONE',  ( -34.35683892909391801, -60.00000000000000711, 45.85838480689532304 ) ) ;
#51515=CARTESIAN_POINT ( 'NONE',  ( -86.44470553919718725, -17.06574261455647701, 183.2584459546009157 ) ) ;
#51518=CARTESIAN_POINT ( 'NONE',  ( -5.138880198032813595, -53.40245903056734278, 32.77961879907969234 ) ) ;
#51520=CARTESIAN_POINT ( 'NONE',  ( 85.95779223056094054, -47.24568047936485726, 189.6962305527513593 ) ) ;
#51535=CARTESIAN_POINT ( 'NONE',  ( 103.3501304845727873, -29.99999999999998579, 116.5671668536019610 ) ) ;
#51536=CARTESIAN_POINT ( 'NONE',  ( -82.78520545488002824, -25.62296466129009431, 148.0817344972886360 ) ) ;
#51540=CARTESIAN_POINT ( 'NONE',  ( 48.31638044378208718, -57.67957409234934119, 72.90164476747999345 ) ) ;
#51555=CARTESIAN_POINT ( 'NONE',  ( 111.8517878722345529, -60.00000000000001421, 162.0410978359878698 ) ) ;
#51556=CARTESIAN_POINT ( 'NONE',  ( -83.30586888084981467, -14.21045842199414011, 194.5088339777059332 ) ) ;
#51557=CARTESIAN_POINT ( 'NONE',  ( 24.33727547018983017, -60.35103628449270019, 35.15249607386650155 ) ) ;
#51559=CARTESIAN_POINT ( 'NONE',  ( 82.80078431826154883, -37.99999999999994316, -11.83170434587093744 ) ) ;
#51561=CARTESIAN_POINT ( 'NONE',  ( -40.76554704193952716, -53.34813757967989289, 42.49434450145254516 ) ) ;
#51575=CARTESIAN_POINT ( 'NONE',  ( 96.50054790619491030, -30.00000000000008882, 191.2148438178596450 ) ) ;
#51578=CARTESIAN_POINT ( 'NONE',  ( 81.97860939186369933, -30.00000000000000355, 33.72797324346839076 ) ) ;
#51581=CIRCLE ( 'NONE', #63696, 1.999999999999998224 ) ;
#51595=CARTESIAN_POINT ( 'NONE',  ( 74.26595512671680410, -38.32811518277526375, 162.6728022224276913 ) ) ;
#51617=CARTESIAN_POINT ( 'NONE',  ( 86.35266085468832387, -20.98688359306337148, 180.9796971926948004 ) ) ;
#51623=CARTESIAN_POINT ( 'NONE',  ( 71.90002237152832265, -57.67111777412542040, -33.97088182244272758 ) ) ;
#51628=CARTESIAN_POINT ( 'NONE',  ( -86.45155040232437216, -29.99999999999999645, 67.06891508925755829 ) ) ;
#51636=CARTESIAN_POINT ( 'NONE',  ( -35.22237514543125059, -33.10240969494732610, 34.19389076937522276 ) ) ;
#51640=CARTESIAN_POINT ( 'NONE',  ( 39.38097750404882902, -24.68082471414068380, -30.42226529891207676 ) ) ;
#51642=CARTESIAN_POINT ( 'NONE',  ( -26.23499765767613212, -42.95978904109873042, 32.63469194111196714 ) ) ;
#51645=CARTESIAN_POINT ( 'NONE',  ( -20.07920920781616658, -35.99626565146032675, 30.40599871804820609 ) ) ;
#51646=CARTESIAN_POINT ( 'NONE',  ( -55.42315763572941023, -28.56386927801018061, -26.45277240378572259 ) ) ;
#51648=CARTESIAN_POINT ( 'NONE',  ( -66.60144316463728842, -60.22825214799080129, -27.67180546727933788 ) ) ;
#51655=CARTESIAN_POINT ( 'NONE',  ( -15.31761884737777990, -60.00000000000000711, -42.14637892441209033 ) ) ;
#51656=ORIENTED_EDGE ( 'NONE', *, *, #3409, .F. ) ;
#51659=CARTESIAN_POINT ( 'NONE',  ( 99.91689189414954342, -45.27234786626318908, 192.6820125696734181 ) ) ;
#51674=CARTESIAN_POINT ( 'NONE',  ( -94.70492387035963588, -59.99999999995124256, 24.66237146002972835 ) ) ;
#51680=CARTESIAN_POINT ( 'NONE',  ( -84.06615883987635129, -30.00000000000009592, -21.85610764691116259 ) ) ;
#51682=CARTESIAN_POINT ( 'NONE',  ( -50.43059932419966884, -53.37294702884624087, 56.24277649152521263 ) ) ;
#51693=CARTESIAN_POINT ( 'NONE',  ( 83.38327456107505498, -38.79623963373321516, 197.2790430537241946 ) ) ;
#51698=CARTESIAN_POINT ( 'NONE',  ( 89.15293829421764826, -30.00000000000000711, 188.9274208521591731 ) ) ;
#51703=CARTESIAN_POINT ( 'NONE',  ( 51.87696231258184554, -39.50721492603066309, 54.02982920344263107 ) ) ;
#51708=CARTESIAN_POINT ( 'NONE',  ( -90.38342445295627670, -38.40159242213010771, -14.93373897757729374 ) ) ;
#51713=CARTESIAN_POINT ( 'NONE',  ( 110.2498375325866107, -38.35601196224923370, 184.3325669443497645 ) ) ;
#51715=CARTESIAN_POINT ( 'NONE',  ( 85.39580779865164573, -52.71438213946019857, 25.13192279552427877 ) ) ;
#51718=SURFACE_STYLE_USAGE ( .BOTH. , #92714 ) ;
#51735=SURFACE_STYLE_FILL_AREA ( #68475 ) ;
#51739=CARTESIAN_POINT ( 'NONE',  ( 81.79764319078026347, -60.67315069769534830, 187.1424671695783104 ) ) ;
#51743=CARTESIAN_POINT ( 'NONE',  ( -101.5804274888581205, -60.15496831279061496, 125.0268949860137155 ) ) ;
#51747=CARTESIAN_POINT ( 'NONE',  ( -36.78552755379869410, -31.92457971927218452, -37.73363741030753005 ) ) ;
#51752=CARTESIAN_POINT ( 'NONE',  ( 41.61328347345722989, -59.99999999999999289, 54.53347641298491766 ) ) ;
#51753=CARTESIAN_POINT ( 'NONE',  ( 43.25463156771495221, -38.30615329582972350, 54.80495015273535131 ) ) ;
#51755=CARTESIAN_POINT ( 'NONE',  ( 5.516412180249635533, -12.94324287202192991, 32.08767009249079649 ) ) ;
#51757=CARTESIAN_POINT ( 'NONE',  ( -32.60673480809711577, -34.12558338660269186, 42.27298281508674904 ) ) ;
#51767=CARTESIAN_POINT ( 'NONE',  ( -1.935861021877891552, -59.99999999999999289, 39.63649550858829684 ) ) ;
#51770=CARTESIAN_POINT ( 'NONE',  ( 12.93241622180732442, -60.22813012449146441, -36.57626181383834307 ) ) ;
#51781=CARTESIAN_POINT ( 'NONE',  ( -94.39104688558903433, -59.99999999999999289, 44.44594898355327928 ) ) ;
#51788=CARTESIAN_POINT ( 'NONE',  ( -83.84580100612211595, -35.97236730127333715, 172.3106703699040168 ) ) ;
#51800=CARTESIAN_POINT ( 'NONE',  ( -5.642946032546647395, -57.67118448875083203, -44.55159700680318480 ) ) ;
#51807=CARTESIAN_POINT ( 'NONE',  ( 86.99610535363679276, -14.21045842199441012, 24.11248255592787615 ) ) ;
#51808=CARTESIAN_POINT ( 'NONE',  ( -78.95080019145578376, -30.00000000000002842, 188.4626203831212479 ) ) ;
#51809=CARTESIAN_POINT ( 'NONE',  ( -60.30957961906158005, -42.96557303354831703, 74.70452531835056220 ) ) ;
#51813=CARTESIAN_POINT ( 'NONE',  ( -105.4132686368380689, -60.15493453134271817, 186.0986387432675713 ) ) ;
#51817=CARTESIAN_POINT ( 'NONE',  ( -81.48333467678395436, -59.99999999999998579, 197.5873724345494509 ) ) ;
#51823=CARTESIAN_POINT ( 'NONE',  ( 17.01584901091794322, 0.000000000000000000, 1.113195845613775825 ) ) ;
#51831=CARTESIAN_POINT ( 'NONE',  ( -29.12107580442651056, -25.58914361729731368, 30.36964868577932819 ) ) ;
#51834=CARTESIAN_POINT ( 'NONE',  ( 43.59138291442800295, -25.70414336249979570, 38.53719198648085609 ) ) ;
#51838=CARTESIAN_POINT ( 'NONE',  ( -87.07432190745933553, -38.59215479556766581, 199.5759947477305616 ) ) ;
#51841=CARTESIAN_POINT ( 'NONE',  ( 81.78041284440412539, -38.35659437205359978, -25.37965657400610553 ) ) ;
#51843=CARTESIAN_POINT ( 'NONE',  ( 78.89378607809999266, -60.00000000000006395, 163.2895204445849799 ) ) ;
#51851=CARTESIAN_POINT ( 'NONE',  ( 106.7471793853078168, -60.00000000000000000, 197.4229364724118057 ) ) ;
#51857=CARTESIAN_POINT ( 'NONE',  ( -75.15565943195267096, -30.00000000000000711, -17.90412972589801655 ) ) ;
#51859=CARTESIAN_POINT ( 'NONE',  ( -92.42649569189924819, -38.49805319420887173, 201.0465977874510770 ) ) ;
#51868=CARTESIAN_POINT ( 'NONE',  ( 80.43770127149109328, -56.88658794661572671, 173.6145532136999634 ) ) ;
#51884=CARTESIAN_POINT ( 'NONE',  ( 87.07919189661382120, -31.70057368356062000, 187.6106092519108870 ) ) ;
#51911=CARTESIAN_POINT ( 'NONE',  ( -111.0770631305250902, -59.99999999999998579, 186.8983870106532379 ) ) ;
#51915=CARTESIAN_POINT ( 'NONE',  ( -84.21710172597578037, -46.56676066005127268, 185.3566345002555806 ) ) ;
#51920=CARTESIAN_POINT ( 'NONE',  ( -82.72858650987951989, -37.82906654770548016, 2.983319424909649076 ) ) ;
#51929=CARTESIAN_POINT ( 'NONE',  ( 76.85420403038403947, -14.21045842199429288, 149.6289235591555666 ) ) ;
#51931=CARTESIAN_POINT ( 'NONE',  ( -86.55941870227799484, -14.21045842199434439, 7.758091717749037386 ) ) ;
#51933=CARTESIAN_POINT ( 'NONE',  ( -68.76518295970697636, -36.01231797821088776, 95.92058326348774244 ) ) ;
#51935=CARTESIAN_POINT ( 'NONE',  ( 103.1541778469752160, -29.99999999999992184, 197.4146557462016176 ) ) ;
#51936=CARTESIAN_POINT ( 'NONE',  ( 26.06643700053798796, -59.99999999999019451, 43.91432386791814935 ) ) ;
#51946=CARTESIAN_POINT ( 'NONE',  ( -71.84928664377656560, -60.00000000002933831, 174.4758671435405404 ) ) ;
#51959=CARTESIAN_POINT ( 'NONE',  ( 31.90715827978913310, -22.14410705931457457, 30.64563635488976701 ) ) ;
#51960=CARTESIAN_POINT ( 'NONE',  ( -11.19959342721765694, -8.673617379884035472E-16, 19.43146043914803300 ) ) ;
#51964=VERTEX_POINT ( 'NONE', #94253 ) ;
#51972=CARTESIAN_POINT ( 'NONE',  ( 92.39395720610478691, -60.00000000000000000, 0.2350603988867105976 ) ) ;
#51981=CARTESIAN_POINT ( 'NONE',  ( -104.3020865355773736, -30.00000000000412825, 196.2433964757412639 ) ) ;
#51982=ORIENTED_EDGE ( 'NONE', *, *, #91312, .F. ) ;
#51988=CARTESIAN_POINT ( 'NONE',  ( 83.33347542712400013, -45.27651489616857106, -13.82556416722983528 ) ) ;
#51998=FACE_OUTER_BOUND ( 'NONE', #57092, .T. ) ;
#52002=CARTESIAN_POINT ( 'NONE',  ( 74.53424881736971486, -46.43315849507841619, 123.7959196446912387 ) ) ;
#52007=CARTESIAN_POINT ( 'NONE',  ( -73.23646197434321437, -57.64251361348243563, 182.9240549372742635 ) ) ;
#52014=CARTESIAN_POINT ( 'NONE',  ( 105.7766044031187107, -60.15129442481250521, 184.0536137966112733 ) ) ;
#52020=CARTESIAN_POINT ( 'NONE',  ( -51.59293570839133736, -29.92165899869593559, 49.34611889700588705 ) ) ;
#52032=CARTESIAN_POINT ( 'NONE',  ( -86.40106122215911455, -30.00000000000000355, 180.9903452954047509 ) ) ;
#52036=CARTESIAN_POINT ( 'NONE',  ( 77.70728701152813755, -57.51519683822058226, 196.1582150947566845 ) ) ;
#52037=FACE_OUTER_BOUND ( 'NONE', #92162, .T. ) ;
#52039=CARTESIAN_POINT ( 'NONE',  ( 28.37604781422512090, -28.97374409063350598, -38.24945775106650103 ) ) ;
#52042=CARTESIAN_POINT ( 'NONE',  ( -42.28790913546334451, -59.99999999999999289, 55.62912243266985257 ) ) ;
#52044=CARTESIAN_POINT ( 'NONE',  ( -86.53326020941184993, -28.12733637824134547, 185.0956260656611505 ) ) ;
#52047=CARTESIAN_POINT ( 'NONE',  ( -0.9943172959230506258, -29.03115895393441193, 28.72817645192477798 ) ) ;
#52050=CARTESIAN_POINT ( 'NONE',  ( 86.96164706429843250, -39.85521162617677504, 189.1638891629380623 ) ) ;
#52064=CARTESIAN_POINT ( 'NONE',  ( 96.14436826854903018, -60.00000000000009237, 39.43554979140174765 ) ) ;
#52065=CARTESIAN_POINT ( 'NONE',  ( -80.60743116781320339, -39.50081370003077552, 149.7882430904484181 ) ) ;
#52069=CARTESIAN_POINT ( 'NONE',  ( 29.76422793413452439, -57.68363811005358599, 45.14079408021506623 ) ) ;
#52088=CARTESIAN_POINT ( 'NONE',  ( 91.32602593890536014, -59.99999999999998579, -16.10466224646018674 ) ) ;
#52090=CARTESIAN_POINT ( 'NONE',  ( -73.20331151331558317, -59.99999999999998579, 185.6225630369678470 ) ) ;
#52091=CARTESIAN_POINT ( 'NONE',  ( 22.50217560053253507, -39.47492995735613164, 31.31568985205594657 ) ) ;
#52095=CARTESIAN_POINT ( 'NONE',  ( -34.57919986246837141, -60.30355936026654717, 39.05315648927861361 ) ) ;
#52107=CARTESIAN_POINT ( 'NONE',  ( 97.93634479608400056, -29.99999999999999289, 190.5932743339873809 ) ) ;
#52110=CARTESIAN_POINT ( 'NONE',  ( 80.76301881924163695, -29.99999999999999645, 11.31298429570228059 ) ) ;
#52126=CARTESIAN_POINT ( 'NONE',  ( 71.26571211989046617, -38.32808976662677480, 141.5686193886610624 ) ) ;
#52150=CARTESIAN_POINT ( 'NONE',  ( 86.21467851622986700, -50.15124133650150640, 191.0468867715541990 ) ) ;
#52153=ORIENTED_EDGE ( 'NONE', *, *, #60706, .T. ) ;
#52154=CARTESIAN_POINT ( 'NONE',  ( 63.90509369011976304, -57.67098025992571309, -36.62925744095688430 ) ) ;
#52161=CARTESIAN_POINT ( 'NONE',  ( -84.31746037670764338, -29.99999999999999645, 52.99187934968279023 ) ) ;
#52164=CARTESIAN_POINT ( 'NONE',  ( 20.89024399768744189, -57.67230926853248718, 42.33697424510430807 ) ) ;
#52172=CARTESIAN_POINT ( 'NONE',  ( 64.59048453740965101, -29.71741133510901278, -23.23533048826496383 ) ) ;
#52173=CARTESIAN_POINT ( 'NONE',  ( -25.30535910738106509, -18.61086395607065569, 28.23931188293136785 ) ) ;
#52177=CARTESIAN_POINT ( 'NONE',  ( -16.50652937410865562, -25.55084766554285736, 28.36507869232989520 ) ) ;
#52183=CARTESIAN_POINT ( 'NONE',  ( 0.000000000000000000, -8.673617379884035472E-16, -17.01589776168603407 ) ) ;
#52190=CARTESIAN_POINT ( 'NONE',  ( 102.0322780741121846, -60.20636929944893012, 194.1630386048543926 ) ) ;
#52203=ORIENTED_EDGE ( 'NONE', *, *, #102203, .T. ) ;
#52206=CARTESIAN_POINT ( 'NONE',  ( -2.499999999981197707, -21.99834632368703069, -30.53960193249073640 ) ) ;
#52207=CARTESIAN_POINT ( 'NONE',  ( -94.38618793271719198, -60.00000000000733991, -14.22879310620676740 ) ) ;
#52212=CARTESIAN_POINT ( 'NONE',  ( -88.92180072262880230, -30.00000000000001421, -15.18793788064705197 ) ) ;
#52214=CARTESIAN_POINT ( 'NONE',  ( -48.50349631401147121, -25.67985106503867598, 44.08718021024470346 ) ) ;
#52218=CARTESIAN_POINT ( 'NONE',  ( -95.55881383635450277, -45.25346914612557470, 194.1665852426087326 ) ) ;
#52224=CARTESIAN_POINT ( 'NONE',  ( 51.86593418231710473, -38.33572705716591145, 73.09143234397147637 ) ) ;
#52230=CARTESIAN_POINT ( 'NONE',  ( 88.16265431536430697, -29.99999999999999289, 187.1745416955410235 ) ) ;
#52238=CARTESIAN_POINT ( 'NONE',  ( 55.57801962097006765, -32.55754387728045174, 58.72004439221983318 ) ) ;
#52243=CARTESIAN_POINT ( 'NONE',  ( -85.30392625238515336, -38.35961253370006574, -22.56936445887191311 ) ) ;
#52246=CARTESIAN_POINT ( 'NONE',  ( 110.3209537404446223, -38.35602685585281080, 183.8300678904132610 ) ) ;
#52248=CARTESIAN_POINT ( 'NONE',  ( 84.06531897659476726, -45.28288193063320222, 23.57404419494545067 ) ) ;
#52265=CARTESIAN_POINT ( 'NONE',  ( -4.285641891732125508, -12.76267229504570011, 32.13335911023925462 ) ) ;
#52269=CARTESIAN_POINT ( 'NONE',  ( 83.31253321705135306, -53.70450120492168367, 187.1177796283798216 ) ) ;
#52274=CARTESIAN_POINT ( 'NONE',  ( -89.89320630590951566, -37.82073183721878706, 78.06522437777182688 ) ) ;
#52279=CARTESIAN_POINT ( 'NONE',  ( -37.04799130315296196, -32.00998463668386051, -37.71207847285617731 ) ) ;
#52283=CARTESIAN_POINT ( 'NONE',  ( 39.48197415042214686, -60.00000000000000000, 51.38249238638569238 ) ) ;
#52285=CARTESIAN_POINT ( 'NONE',  ( 29.22136840097360633, -31.92850515648737542, 40.14001151005216173 ) ) ;
#52287=CARTESIAN_POINT ( 'NONE',  ( 10.69334538532959122, -13.94028717871298539, 31.85850709728139307 ) ) ;
#52304=CARTESIAN_POINT ( 'NONE',  ( -16.18453578148346139, -60.22808678499453805, -36.38447698959835463 ) ) ;
#52314=CARTESIAN_POINT ( 'NONE',  ( -91.86321863162261536, -59.99999999999999289, 13.12527847739685249 ) ) ;
#52319=CARTESIAN_POINT ( 'NONE',  ( -81.30862360253455279, -49.93417848018496130, 170.6586799718517398 ) ) ;
#52332=CARTESIAN_POINT ( 'NONE',  ( -94.67953089133513345, -57.66492561105124537, -4.550087184288205577 ) ) ;
#52333=CARTESIAN_POINT ( 'NONE',  ( 2.500000000000000444, -30.00000000000000000, 28.88619651857252535 ) ) ;
#52338=CARTESIAN_POINT ( 'NONE',  ( 95.99465422657044655, -14.21045842199428222, 88.91344185009528189 ) ) ;
#52339=CARTESIAN_POINT ( 'NONE',  ( -78.25705875637353870, -14.21045842199447939, 182.3370610225134953 ) ) ;
#52340=CARTESIAN_POINT ( 'NONE',  ( -59.32705706084635722, -18.65613686416636696, 61.11537755004999894 ) ) ;
#52344=CARTESIAN_POINT ( 'NONE',  ( -103.4860089683291022, -52.71038146289320991, 188.6634783447426003 ) ) ;
#52363=CARTESIAN_POINT ( 'NONE',  ( -31.54433348721467922, -49.90828886377769891, 35.58986079060855445 ) ) ;
#52366=CARTESIAN_POINT ( 'NONE',  ( 44.62879333611520849, -32.61662185523480417, 41.38689675569595749 ) ) ;
#52369=CARTESIAN_POINT ( 'NONE',  ( -87.30475775079190726, -38.58328791312629846, 199.6746598993676116 ) ) ;
#52380=CARTESIAN_POINT ( 'NONE',  ( 109.0644082823126695, -60.00000000000001421, 193.5531632337274175 ) ) ;
#52388=CARTESIAN_POINT ( 'NONE',  ( -80.72051579742614535, -30.00000000000003197, 13.90560478027946445 ) ) ;
#52390=CARTESIAN_POINT ( 'NONE',  ( -73.58054804561130879, -38.32516351570817648, 156.7495410978815755 ) ) ;
#52398=CARTESIAN_POINT ( 'NONE',  ( 84.99175437857353188, -18.63712082014315286, 155.3294098635141438 ) ) ;
#52411=CARTESIAN_POINT ( 'NONE',  ( -80.61739365636806554, -30.00000000000000355, -12.80982504787266940 ) ) ;
#52414=CARTESIAN_POINT ( 'NONE',  ( 87.42597901065016686, -31.67953177600239201, 188.4201908730174750 ) ) ;
#52438=CARTESIAN_POINT ( 'NONE',  ( -92.96881148959433006, -60.00000000000001421, 202.4687464090484355 ) ) ;
#52443=CARTESIAN_POINT ( 'NONE',  ( -84.92579027340632081, -39.36590996067631920, 183.3526443039159233 ) ) ;
#52444=AXIS2_PLACEMENT_3D ( 'NONE', #69428, #78558, #4156 ) ;
#52454=CARTESIAN_POINT ( 'NONE',  ( -83.97025560380723164, -45.26987198569664628, 3.107597088425433807 ) ) ;
#52460=CARTESIAN_POINT ( 'NONE',  ( 61.00101809772601769, -14.21045842199439591, 86.19763211990357377 ) ) ;
#52462=CARTESIAN_POINT ( 'NONE',  ( -84.89308075164642275, -60.00000000000002842, -27.59301604020478038 ) ) ;
#52463=CARTESIAN_POINT ( 'NONE',  ( -69.23882386195900551, -29.06181850512027864, 93.49118526020582465 ) ) ;
#52465=CARTESIAN_POINT ( 'NONE',  ( 97.13532076618713518, -30.00000000000002842, 199.9107784265496264 ) ) ;
#52467=CARTESIAN_POINT ( 'NONE',  ( 19.58684304517602470, -57.67119434593145400, -43.84739835614993808 ) ) ;
#52478=CARTESIAN_POINT ( 'NONE',  ( -27.14100146121103307, -60.00000000000000711, 44.29861369568705953 ) ) ;
#52491=CARTESIAN_POINT ( 'NONE',  ( 32.55783135264621109, -39.49123201241251024, 34.14412841509428631 ) ) ;
#52507=CARTESIAN_POINT ( 'NONE',  ( 91.96543020101078980, -60.00000000000000000, 17.51050721529170318 ) ) ;
#52516=CARTESIAN_POINT ( 'NONE',  ( -108.3254638997414077, -29.99999999997997335, 187.2860949193978684 ) ) ;
#52522=CARTESIAN_POINT ( 'NONE',  ( 85.99566667790004715, -60.22088695362039346, -14.08581190481345402 ) ) ;
#52532=CARTESIAN_POINT ( 'NONE',  ( 73.98053784616911344, -29.06950772015738238, 109.2017082355514503 ) ) ;
#52537=CARTESIAN_POINT ( 'NONE',  ( -112.2456557016906942, -57.67113047748567567, 190.5314477545807392 ) ) ;
#52542=CARTESIAN_POINT ( 'NONE',  ( 102.7781224394537816, -37.84834821706366625, 170.2548301641596140 ) ) ;
#52547=CARTESIAN_POINT ( 'NONE',  ( -45.23652315699401072, -28.37715625667643948, 40.32569774422481856 ) ) ;
#52559=CARTESIAN_POINT ( 'NONE',  ( -36.06522973182497793, -23.67578041333969452, -31.09724018593250960 ) ) ;
#52560=CARTESIAN_POINT ( 'NONE',  ( -89.55025994633662378, -30.00000000000000355, 189.4425988133392025 ) ) ;
#52565=CARTESIAN_POINT ( 'NONE',  ( 76.55898268265609374, -57.53316911256309396, 194.3133562938762680 ) ) ;
#52568=CARTESIAN_POINT ( 'NONE',  ( 37.71804776410431259, -32.22589162183228240, -37.65546176092030350 ) ) ;
#52572=CARTESIAN_POINT ( 'NONE',  ( -71.88192843937767407, -59.99999999999999289, 153.4067312503538005 ) ) ;
#52575=CARTESIAN_POINT ( 'NONE',  ( -86.80266053460367459, -28.05398439696902457, 186.1832171119652628 ) ) ;
#52578=CARTESIAN_POINT ( 'NONE',  ( -5.068928611176632515, -39.47589145737825334, 30.45902526352114847 ) ) ;
#52593=CARTESIAN_POINT ( 'NONE',  ( 87.68135845022958108, -14.21045842199445275, 32.26523303912966156 ) ) ;
#52594=CARTESIAN_POINT ( 'NONE',  ( -79.80561878445170976, -53.38318872916766367, 161.8232012627484551 ) ) ;
#52607=DIRECTION ( 'NONE',  ( 0.000000000000000000, -1.000000000000000000, 0.000000000000000000 ) ) ;
#52616=CARTESIAN_POINT ( 'NONE',  ( 92.17363683422854592, -59.99999999999997868, -13.42148695742234921 ) ) ;
#52617=CARTESIAN_POINT ( 'NONE',  ( -62.54317499552948334, -60.00000000000000711, 118.0918133646953976 ) ) ;
#52618=CARTESIAN_POINT ( 'NONE',  ( 20.07868812831179284, -35.99339030059921640, 30.40546157090997070 ) ) ;
#52621=CARTESIAN_POINT ( 'NONE',  ( -38.62665293114096698, -49.89296806199684653, 39.81745112272700737 ) ) ;
#52634=CARTESIAN_POINT ( 'NONE',  ( 91.96900705543794174, -29.99999999999987921, 190.8564251733103276 ) ) ;
#52639=CARTESIAN_POINT ( 'NONE',  ( 81.33900641567250034, -30.00000000000000355, -1.065096365412631529 ) ) ;
#52656=CARTESIAN_POINT ( 'NONE',  ( 74.38267031189917589, -38.32888619803856756, 163.7218043044017293 ) ) ;
#52674=CARTESIAN_POINT ( 'NONE',  ( 89.99999999999997158, -52.00000000000000000, 196.0238439516549818 ) ) ;
#52675=EDGE_CURVE ( 'NONE', #38791, #63501, #29553, .T. ) ;
#52679=CARTESIAN_POINT ( 'NONE',  ( 86.30431136706036455, -24.61821740116755208, 182.2296409677384759 ) ) ;
#52684=CARTESIAN_POINT ( 'NONE',  ( -3.462711550064783150, -15.46674754799754226, -35.18986906109944357 ) ) ;
#52689=CARTESIAN_POINT ( 'NONE',  ( -94.06284170466219052, -29.99999999999999289, 112.3432347928509074 ) ) ;
#52692=CARTESIAN_POINT ( 'NONE',  ( 35.03266159394272705, -57.69518171884941893, 49.17802768995313301 ) ) ;
#52702=CARTESIAN_POINT ( 'NONE',  ( 23.19675064131305930, -19.50463141275981016, -33.27316171080115481 ) ) ;
#52704=CARTESIAN_POINT ( 'NONE',  ( -22.09705705695840550, -25.55721621211691286, 28.90405252608048414 ) ) ;
#52708=CARTESIAN_POINT ( 'NONE',  ( -16.57135497164903981, -29.03224908037524798, 28.95071076732330795 ) ) ;
#52726=CARTESIAN_POINT ( 'NONE',  ( 103.7490062218180356, -60.15690558421150058, 191.4294801856832180 ) ) ;
#52728=CARTESIAN_POINT ( 'NONE',  ( 35.17791155467128306, -33.08171577008500464, 34.16701531372348200 ) ) ;
#52742=CARTESIAN_POINT ( 'NONE',  ( -88.66004994158249986, -60.00000000000486011, -24.41333391927541641 ) ) ;
#52744=CARTESIAN_POINT ( 'NONE',  ( 2.816747937689971781, -59.99999999995171862, -45.00000176639943561 ) ) ;
#52747=CARTESIAN_POINT ( 'NONE',  ( -112.0516705497441876, -59.99999999999997868, 140.8505598867089645 ) ) ;
#52748=CARTESIAN_POINT ( 'NONE',  ( 6.981006337927150973, -18.58620748038632442, 26.97765893144556770 ) ) ;
#52752=CARTESIAN_POINT ( 'NONE',  ( -48.01388463784094540, -42.98496168698468267, 48.71257218748448281 ) ) ;
#52763=CARTESIAN_POINT ( 'NONE',  ( 9.797174393178825657E-16, 0.000000000000000000, 8.000000000000000000 ) ) ;
#52765=CARTESIAN_POINT ( 'NONE',  ( 90.72652982786716791, -30.00000000012070345, 36.53626809240827811 ) ) ;
#52772=CARTESIAN_POINT ( 'NONE',  ( 91.30097760447456778, -30.00000000000000000, 190.6181298806798736 ) ) ;
#52777=CARTESIAN_POINT ( 'NONE',  ( 53.77059603358078022, -53.37413041404379754, 63.18823621241026700 ) ) ;
#52781=CARTESIAN_POINT ( 'NONE',  ( -88.12222426954021159, -38.37225613763864374, -19.40653620767198007 ) ) ;
#52784=CARTESIAN_POINT ( 'NONE',  ( 108.2513347943879722, -38.35773709419970601, 192.2701858252870295 ) ) ;
#52786=CARTESIAN_POINT ( 'NONE',  ( 86.12903045990179862, -60.13851843310877854, 12.57144976733284025 ) ) ;
#52805=CARTESIAN_POINT ( 'NONE',  ( 2.957810341175842961, -12.64483219941317138, 32.16612171018341826 ) ) ;
#52812=CARTESIAN_POINT ( 'NONE',  ( 86.11061767232767750, -21.49857324288878502, 175.3763454229637659 ) ) ;
#52816=CARTESIAN_POINT ( 'NONE',  ( -87.71484843151664279, -60.15235330828886617, 36.79746090376434609 ) ) ;
#52817=DIRECTION ( 'NONE',  ( 0.000000000000000000, 0.000000000000000000, -1.000000000000000000 ) ) ;
#52821=CARTESIAN_POINT ( 'NONE',  ( -4.823443502104696634, -21.62908485124496138, -38.54787723814094846 ) ) ;
#52822=CARTESIAN_POINT ( 'NONE',  ( 29.71588918770380161, -60.00000000000002132, 42.89755770512662991 ) ) ;
#52823=CARTESIAN_POINT ( 'NONE',  ( 14.84465811918519584, -22.60273344730966727, 35.91147243655147037 ) ) ;
#52825=CARTESIAN_POINT ( 'NONE',  ( 39.86870225387427524, -26.26949144110688650, 35.87748434985530821 ) ) ;
#52826=CARTESIAN_POINT ( 'NONE',  ( -33.24326047732412093, -34.51171323919459155, 42.75321002329071973 ) ) ;
#52834=ADVANCED_FACE ( 'NONE', ( #17063 ), #82846, .F. ) ;
#52835=FACE_OUTER_BOUND ( 'NONE', #11588, .T. ) ;
#52837=CARTESIAN_POINT ( 'NONE',  ( -2.064928172609607149, -60.00000000000000711, 39.63619459862159289 ) ) ;
#52838=ORIENTED_EDGE ( 'NONE', *, *, #32136, .T. ) ;
#52844=CARTESIAN_POINT ( 'NONE',  ( -19.42937613716337353, -60.22819676930696886, -36.14109189875915717 ) ) ;
#52853=CARTESIAN_POINT ( 'NONE',  ( -92.22380160643884039, -59.99999999999999289, 2.566636606020737954 ) ) ;
#52857=DIRECTION ( 'NONE',  ( -0.000000000000000000, -1.000000000000000000, -0.000000000000000000 ) ) ;
#52861=CARTESIAN_POINT ( 'NONE',  ( -82.18019381229618148, -42.97457168899456548, 167.7073896577822154 ) ) ;
#52863=CARTESIAN_POINT ( 'NONE',  ( -11.24487389204439580, 0.000000000000000000, -12.81917055449304854 ) ) ;
#52871=CARTESIAN_POINT ( 'NONE',  ( -94.30414684669057124, -57.67279326051714605, 1.132156541063573441 ) ) ;
#52880=CARTESIAN_POINT ( 'NONE',  ( 93.27827242126578255, -14.21045842199433729, 72.77868743038563082 ) ) ;
#52883=CARTESIAN_POINT ( 'NONE',  ( -104.4188068117427264, -29.99999999999997868, 196.2181340123987923 ) ) ;
#52884=CARTESIAN_POINT ( 'NONE',  ( -55.55496807634862932, -60.32879899568890636, 70.31421429908731113 ) ) ;
#52890=CARTESIAN_POINT ( 'NONE',  ( -102.5962067017768220, -37.82042529878841464, 179.2107196536337597 ) ) ;
#52891=DIRECTION ( 'NONE',  ( 0.000000000000000000, 1.000000000000000000, 0.000000000000000000 ) ) ;
#52895=CARTESIAN_POINT ( 'NONE',  ( -9.878668896128520061, -59.99999999999998579, 39.64507338328628094 ) ) ;
#52908=CARTESIAN_POINT ( 'NONE',  ( -28.08878474957800719, -29.05689031911417430, 30.69116238151102749 ) ) ;
#52911=CARTESIAN_POINT ( 'NONE',  ( 46.97773782595957925, -60.26704657434898138, 52.32291326186037850 ) ) ;
#52914=CARTESIAN_POINT ( 'NONE',  ( -89.72076565952676219, -38.51974297931068492, 200.4973812629772851 ) ) ;
#52921=CARTESIAN_POINT ( 'NONE',  ( -53.08935917470201815, -30.00000000000000000, 52.21147893555080799 ) ) ;
#52924=CARTESIAN_POINT ( 'NONE',  ( 112.1626836976212189, -59.99999999999999289, 168.5469237518007901 ) ) ;
#52929=CARTESIAN_POINT ( 'NONE',  ( -81.07966025770872420, -30.00000000000007816, -11.61909237075606782 ) ) ;
#52931=CARTESIAN_POINT ( 'NONE',  ( -78.99534078293335426, -38.69139673457585360, 190.9623183980413046 ) ) ;
#52942=CARTESIAN_POINT ( 'NONE',  ( 81.10180942102270762, -56.95487215000356684, 179.5490733622490325 ) ) ;
#52957=CARTESIAN_POINT ( 'NONE',  ( -75.46669749351579526, -30.00000000000000355, -17.70126405444623430 ) ) ;
#52973=CARTESIAN_POINT ( 'NONE',  ( 1.405425595346621037E-06, -60.00000000000000000, -42.63907915653317104 ) ) ;
#52990=CARTESIAN_POINT ( 'NONE',  ( -95.46090277292731230, -60.00000000000000711, 202.5799021258702055 ) ) ;
#52996=CARTESIAN_POINT ( 'NONE',  ( -85.41187482593770142, -28.71929674247896358, 176.9217622319580130 ) ) ;
#52999=ORIENTED_EDGE ( 'NONE', *, *, #30573, .T. ) ;
#53002=CARTESIAN_POINT ( 'NONE',  ( -85.09040274407558968, -52.70139051021373433, 5.151369049883602891 ) ) ;
#53008=CARTESIAN_POINT ( 'NONE',  ( 73.77841798646971938, -29.99999999999998934, 147.9493570314868123 ) ) ;
#53009=CARTESIAN_POINT ( 'NONE',  ( -89.21407719722087393, -30.00000000000005684, 9.591031914958218607 ) ) ;
#53010=CARTESIAN_POINT ( 'NONE',  ( -65.24994020922159166, -25.57926860193576601, 79.70707070267074812 ) ) ;
#53012=CARTESIAN_POINT ( 'NONE',  ( 105.6362521817138713, -29.99999999999994671, 194.5266552104434368 ) ) ;
#53014=CARTESIAN_POINT ( 'NONE',  ( 63.81996746097805584, -57.67113359436530118, -36.65424566499065406 ) ) ;
#53026=CARTESIAN_POINT ( 'NONE',  ( -9.852487725491519299, -60.00000000001466560, 42.00587080741184565 ) ) ;
#53043=CARTESIAN_POINT ( 'NONE',  ( 35.24668317487790148, -49.89395819369836715, 37.46068582077064235 ) ) ;
#53044=CARTESIAN_POINT ( 'NONE',  ( -24.56594385547200687, -4.285714285715344296, -6.601913983219908744 ) ) ;
#53058=CARTESIAN_POINT ( 'NONE',  ( 92.68096304076409808, -60.00000000000000711, -4.348986201877333535 ) ) ;
#53066=CARTESIAN_POINT ( 'NONE',  ( -94.81618536359641780, -30.00000000002265210, 199.9516214458937782 ) ) ;
#53070=CARTESIAN_POINT ( 'NONE',  ( 82.64754189831576525, -37.80179898866133215, -12.22144125512486390 ) ) ;
#53082=CARTESIAN_POINT ( 'NONE',  ( 81.81383369307825149, -25.62393137265173237, 141.9806983117227048 ) ) ;
#53087=CARTESIAN_POINT ( 'NONE',  ( -89.37884834614470719, -57.60609784898206698, 203.8391154356046115 ) ) ;
#53096=CARTESIAN_POINT ( 'NONE',  ( -46.94109106579729485, -28.93092366380357205, 42.27278928388007984 ) ) ;
#53107=CARTESIAN_POINT ( 'NONE',  ( -52.88890906521714186, -28.13393072479325951, -27.22359359308505589 ) ) ;
#53108=CARTESIAN_POINT ( 'NONE',  ( -62.53308941777711993, -30.00000000000000000, 73.43786462750344413 ) ) ;
#53115=CARTESIAN_POINT ( 'NONE',  ( 74.64417150186339711, -57.58847707714879505, 189.5392262892293616 ) ) ;
#53120=CARTESIAN_POINT ( 'NONE',  ( 28.87846294582190509, -29.15946654300748975, -38.22760178079393967 ) ) ;
#53123=CARTESIAN_POINT ( 'NONE',  ( -57.21714066519500363, -60.00000000000000711, 91.78310137730963447 ) ) ;
#53127=CARTESIAN_POINT ( 'NONE',  ( -86.23427538531471725, -28.26129243476134079, 183.4415589754995892 ) ) ;
#53130=CARTESIAN_POINT ( 'NONE',  ( -2.989696676026662558, -25.54936876401580292, 28.14337665864941229 ) ) ;
#53144=CARTESIAN_POINT ( 'NONE',  ( -5.820808985953483727, -9.668376379147026354E-13, -21.65942590380073085 ) ) ;
#53148=CARTESIAN_POINT ( 'NONE',  ( 94.62301060094824834, -14.21045842199438525, 80.84833697736402769 ) ) ;
#53149=CARTESIAN_POINT ( 'NONE',  ( -80.10456516755152734, -46.43972398824795533, 154.7502001011243351 ) ) ;
#53151=FACE_OUTER_BOUND ( 'NONE', #41567, .T. ) ;
#53153=CARTESIAN_POINT ( 'NONE',  ( 36.72327209579803764, -57.69637131458309653, 51.04913384944509147 ) ) ;
#53171=CARTESIAN_POINT ( 'NONE',  ( 80.53725183873906701, -60.00000000000002132, -27.62580428353563633 ) ) ;
#53172=CARTESIAN_POINT ( 'NONE',  ( -35.98784834194372451, -29.99999999999998934, 43.73664282352994803 ) ) ;
#53173=CARTESIAN_POINT ( 'NONE',  ( 23.01660328067156769, -18.59970856359895564, 27.84350729933087365 ) ) ;
#53177=CARTESIAN_POINT ( 'NONE',  ( -38.28055269113645664, -42.97469174897878474, 38.10477465472399672 ) ) ;
#53186=ORIENTED_EDGE ( 'NONE', *, *, #100644, .T. ) ;
#53187=CARTESIAN_POINT ( 'NONE',  ( -75.99682948615210876, -38.37765750765254325, 178.3306665773977500 ) ) ;
#53189=CARTESIAN_POINT ( 'NONE',  ( 97.53565773566364783, -30.00000000000016698, 190.8694968829258301 ) ) ;
#53192=CARTESIAN_POINT ( 'NONE',  ( 80.74124341164603891, -30.00000000000000355, -12.54865364685866247 ) ) ;
#53213=CARTESIAN_POINT ( 'NONE',  ( 64.03239688625770043, -39.48186605976993491, 83.36271444441133838 ) ) ;
#53230=CARTESIAN_POINT ( 'NONE',  ( 86.09253067001675674, -31.93605399604700068, 184.2217672492984377 ) ) ;
#53236=CARTESIAN_POINT ( 'NONE',  ( 5.296018678377662603, -15.62506502678866127, -35.11036406914151797 ) ) ;
#53239=CARTESIAN_POINT ( 'NONE',  ( -83.59878907863057407, -30.00000000000000355, 47.68203053101536426 ) ) ;
#53243=CARTESIAN_POINT ( 'NONE',  ( 29.78108665591588888, -57.68312184062244086, 45.10668838524471624 ) ) ;
#53249=CARTESIAN_POINT ( 'NONE',  ( -48.49798649753537916, -37.71222160853894678, 47.78134261254622572 ) ) ;
#53253=CARTESIAN_POINT ( 'NONE',  ( 49.23114114914121586, -27.31787067993425211, -28.17124660505862010 ) ) ;
#53255=CARTESIAN_POINT ( 'NONE',  ( -23.01798323853113004, -18.59969654692860530, 27.84368168669262644 ) ) ;
#53259=CARTESIAN_POINT ( 'NONE',  ( -19.25491102509279528, -49.92033008237394398, 32.66346180105560393 ) ) ;
#53272=CARTESIAN_POINT ( 'NONE',  ( 101.9973258343542426, -45.28264241616768970, 189.2080144842875598 ) ) ;
#53287=CARTESIAN_POINT ( 'NONE',  ( -94.27213507841179307, -59.99999999999998579, 8.085468415347424553 ) ) ;
#53289=CARTESIAN_POINT ( 'NONE',  ( 28.14493782455200943, -59.99999999999997868, 42.15984703162648373 ) ) ;
#53292=CARTESIAN_POINT ( 'NONE',  ( -95.99503958615204624, -14.21045842199434794, 88.91558689677049188 ) ) ;
#53293=CARTESIAN_POINT ( 'NONE',  ( 5.086408192983678411, -42.95350893056307484, 31.03852461352498793 ) ) ;
#53297=CARTESIAN_POINT ( 'NONE',  ( -48.89129092203405946, -22.21415037853287089, 43.54257904152331804 ) ) ;
#53308=CARTESIAN_POINT ( 'NONE',  ( 107.3415078906099041, -30.00000000001339728, 143.3259930713776384 ) ) ;
#53312=CARTESIAN_POINT ( 'NONE',  ( 98.44576339691531075, -30.00000000000000000, 189.9304428966003684 ) ) ;
#53319=CARTESIAN_POINT ( 'NONE',  ( 55.06520104054218478, -22.15438351385262550, 53.58026775065899727 ) ) ;
#53324=CARTESIAN_POINT ( 'NONE',  ( -88.05788157026037766, -38.37130978355936151, -19.49573130021213174 ) ) ;
#53328=CARTESIAN_POINT ( 'NONE',  ( 105.4234212887860593, -38.38633086054609578, 197.0379193257338386 ) ) ;
#53330=CARTESIAN_POINT ( 'NONE',  ( 82.43424158715217231, -37.85663943339775273, 13.21557699368458749 ) ) ;
#53336=EDGE_LOOP ( 'NONE', ( #50337, #29084, #98046, #19300 ) ) ;
#53345=CARTESIAN_POINT ( 'NONE',  ( -31.57410453687917240, -24.95193506975139996, 39.69783569089302944 ) ) ;
#53350=CARTESIAN_POINT ( 'NONE',  ( 83.54813190880366847, -50.11917785585441010, 185.4780095451953628 ) ) ;
#53352=CARTESIAN_POINT ( 'NONE',  ( -85.95674408092972385, -47.25038601905195179, 189.6969179814721542 ) ) ;
#53354=CARTESIAN_POINT ( 'NONE',  ( -84.25945711018864870, -37.82198024268028291, 39.37117510918165664 ) ) ;
#53361=CARTESIAN_POINT ( 'NONE',  ( 17.70487366776518456, -59.99999999999999289, 39.97903104620380788 ) ) ;
#53363=CARTESIAN_POINT ( 'NONE',  ( 10.34872164634795944, -20.36626283564415374, 35.40946532406196923 ) ) ;
#53365=CARTESIAN_POINT ( 'NONE',  ( 33.70824286937537551, -23.45512021558194959, 33.05602448900377510 ) ) ;
#53367=CARTESIAN_POINT ( 'NONE',  ( -30.90129479073731034, -33.04371094065780312, 41.11476907690651217 ) ) ;
#53385=CARTESIAN_POINT ( 'NONE',  ( 7.860286775113991098, -34.58965292698938754, -32.51041876009787757 ) ) ;
#53391=VERTEX_POINT ( 'NONE', #58867 ) ;
#53395=CARTESIAN_POINT ( 'NONE',  ( -93.39800921275812584, -60.00000000000001421, 36.10795237943069225 ) ) ;
#53404=CARTESIAN_POINT ( 'NONE',  ( -80.75355258942967396, -56.92082733154106933, 176.6204916418753328 ) ) ;
#53415=CARTESIAN_POINT ( 'NONE',  ( -76.10153353667877241, -57.67120126903460431, -32.17100317442078961 ) ) ;
#53421=AXIS2_PLACEMENT_3D ( 'NONE', #32561, #98328, #71930 ) ;
#53422=CARTESIAN_POINT ( 'NONE',  ( 89.36652584573501201, -30.00000000000001421, 5.436425775551051665 ) ) ;
#53424=CARTESIAN_POINT ( 'NONE',  ( -71.37516729659446924, -14.21045842199439946, 121.5232625957608974 ) ) ;
#53425=CARTESIAN_POINT ( 'NONE',  ( -56.02824104333507904, -32.55801343818508542, 59.69165126840069036 ) ) ;
#53429=CARTESIAN_POINT ( 'NONE',  ( -101.9318200314704654, -60.21492788965887399, 194.2758051580982510 ) ) ;
#53430=CARTESIAN_POINT ( 'NONE',  ( 101.3518415701702509, -38.00000000000003553, 187.1895103287365600 ) ) ;
#53438=CARTESIAN_POINT ( 'NONE',  ( 69.28798965557233203, -30.00000000000000000, 93.06143263165685653 ) ) ;
#53444=CARTESIAN_POINT ( 'NONE',  ( -27.03878911781851713, -32.52845681216340523, 31.02526571752343543 ) ) ;
#53446=CARTESIAN_POINT ( 'NONE',  ( 48.21714293254901662, -53.35939452937847705, 52.27498384522137798 ) ) ;
#53452=CARTESIAN_POINT ( 'NONE',  ( -93.96311375434591184, -38.49251773605704585, 201.1897569393096603 ) ) ;
#53454=CARTESIAN_POINT ( 'NONE',  ( 90.72286138954092394, -38.34264739770473085, 7.039974769606621940 ) ) ;
#53462=CARTESIAN_POINT ( 'NONE',  ( 108.8942926950823562, -60.00000000000000000, 193.9232647688770896 ) ) ;
#53480=CARTESIAN_POINT ( 'NONE',  ( 85.83717647578178855, -18.50068724157089761, 163.5510133277480520 ) ) ;
#53492=CARTESIAN_POINT ( 'NONE',  ( -71.80342408229677176, -30.00000000000000000, -19.71767938363507966 ) ) ;
#53507=DIRECTION ( 'NONE',  ( -0.000000000000000000, -1.000000000000000000, -0.000000000000000000 ) ) ;
#53519=CARTESIAN_POINT ( 'NONE',  ( -111.1270554948388138, -59.99999999999997868, 186.6394392527870423 ) ) ;
#53524=CARTESIAN_POINT ( 'NONE',  ( -84.85100970293773059, -32.35236433163615288, 176.2939257893381182 ) ) ;
#53531=CARTESIAN_POINT ( 'NONE',  ( -85.67862191555909135, -52.72633685597455155, -3.980294966729134742 ) ) ;
#53538=CARTESIAN_POINT ( 'NONE',  ( 92.04793376076307254, -60.00000000000014211, 204.8851669578057795 ) ) ;
#53540=CARTESIAN_POINT ( 'NONE',  ( -89.36642547188127139, -29.99999999999995381, 5.438168021589780743 ) ) ;
#53541=CARTESIAN_POINT ( 'NONE',  ( -65.34887224726313093, -18.62568967254298258, 76.43621171049910856 ) ) ;
#53543=CARTESIAN_POINT ( 'NONE',  ( 88.91505260351625850, -29.99999999999995381, 199.0551756924508879 ) ) ;
#53545=CARTESIAN_POINT ( 'NONE',  ( 24.18667721825848105, -60.00000000000492406, 43.38656107002559281 ) ) ;
#53555=CARTESIAN_POINT ( 'NONE',  ( -91.70308476423518584, -60.00000000000001421, -15.04706914105544335 ) ) ;
#53569=CARTESIAN_POINT ( 'NONE',  ( 36.78006001946765480, -56.81696112801252951, 39.80776084952203320 ) ) ;
#53570=SURFACE_STYLE_FILL_AREA ( #3429 ) ;
#53576=DIRECTION ( 'NONE',  ( -0.000000000000000000, -1.000000000000000000, -0.000000000000000000 ) ) ;
#53584=CARTESIAN_POINT ( 'NONE',  ( 91.99065738214881094, -59.99999999999998579, 18.16284596454354272 ) ) ;
#53591=CARTESIAN_POINT ( 'NONE',  ( -99.52556328755157722, -30.00000000001300293, 199.2777381299856359 ) ) ;
#53603=CARTESIAN_POINT ( 'NONE',  ( 78.93084866786456644, -36.02569822567065216, 136.0482817868801533 ) ) ;
#53605=VERTEX_POINT ( 'NONE', #22134 ) ;
#53609=CARTESIAN_POINT ( 'NONE',  ( -73.03813016181682372, -57.65004463643786892, 181.4998991682408302 ) ) ;
#53618=CARTESIAN_POINT ( 'NONE',  ( -38.83689927739595049, -25.82488296874500477, 35.22879776301019206 ) ) ;
#53629=CARTESIAN_POINT ( 'NONE',  ( 1.328130235833654194, -17.76412090456761206, -37.95834240885186972 ) ) ;
#53630=CARTESIAN_POINT ( 'NONE',  ( -65.73160349868967955, -30.00000000000001066, 82.32586786504053578 ) ) ;
#53636=CARTESIAN_POINT ( 'NONE',  ( 77.67582994109527306, -57.51557269059810551, 196.1127657593792435 ) ) ;
#53639=CARTESIAN_POINT ( 'NONE',  ( 76.12557658274099026, -38.35599704320051018, -28.58424740099938077 ) ) ;
#53643=CARTESIAN_POINT ( 'NONE',  ( -61.37266631565433528, -59.99999999999999289, 105.1188813016446488 ) ) ;
#53648=CARTESIAN_POINT ( 'NONE',  ( -85.23892774877984380, -46.56544201171040953, 188.0817372555855229 ) ) ;
#53664=CARTESIAN_POINT ( 'NONE',  ( 107.3070812967312833, -60.00000000000004263, 109.8435067956896063 ) ) ;
#53665=CARTESIAN_POINT ( 'NONE',  ( -80.68031237769524466, -36.03175770690578616, 146.2908660090107560 ) ) ;
#53669=CARTESIAN_POINT ( 'NONE',  ( 45.02094980754542775, -57.68314110126151206, 65.19008676313157480 ) ) ;
#53680=CIRCLE ( 'NONE', #22686, 15.00000000000000000 ) ;
#53691=CARTESIAN_POINT ( 'NONE',  ( -65.47633411339396048, -60.00000000000000000, 130.5853305762684329 ) ) ;
#53692=CARTESIAN_POINT ( 'NONE',  ( 27.46944893902966811, -42.95628726384470042, 32.94719848304510634 ) ) ;
#53699=CARTESIAN_POINT ( 'NONE',  ( 72.50181414422412729, -37.99999999999997868, -21.26202816386757277 ) ) ;
#53706=CARTESIAN_POINT ( 'NONE',  ( 84.25466803195676846, -30.00000000000000711, 52.81349775392430956 ) ) ;
#53709=CARTESIAN_POINT ( 'NONE',  ( 81.45592718107263863, -29.99999999999999289, -9.616827637468841061 ) ) ;
#53730=CARTESIAN_POINT ( 'NONE',  ( 47.25211357378231014, -38.32332363358291616, 62.33327775702132811 ) ) ;
#53734=CARTESIAN_POINT ( 'NONE',  ( 64.25190437804278076, -36.00576792741288301, 82.20812981856342105 ) ) ;
#53738=CARTESIAN_POINT ( 'NONE',  ( -48.09573466820452836, -35.14038410512238642, -36.46244952396737915 ) ) ;
#53746=CYLINDRICAL_SURFACE ( 'NONE', #84043, 1.999999999999998224 ) ;
#53750=CARTESIAN_POINT ( 'NONE',  ( 86.18704556189692312, -42.85049290463535243, 188.6112712611597999 ) ) ;
#53759=CARTESIAN_POINT ( 'NONE',  ( -97.61462959795420602, -29.99999999999999289, 134.8380256732861824 ) ) ;
#53763=CARTESIAN_POINT ( 'NONE',  ( 0.5184698344275693316, -57.67120215776962056, 41.61168020182621063 ) ) ;
#53775=CARTESIAN_POINT ( 'NONE',  ( -20.95351130271008699, -25.55484898855512910, 28.74739769140940382 ) ) ;
#53776=CARTESIAN_POINT ( 'NONE',  ( -85.33010815977807795, -59.99999999999997868, -15.43476000316156060 ) ) ;
#53779=AXIS2_PLACEMENT_3D ( 'NONE', #60341, #43074, #16664 ) ;
#53790=CARTESIAN_POINT ( 'NONE',  ( 103.1999130473613917, -52.71749418885885774, 189.5266586246194720 ) ) ;
#53792=CARTESIAN_POINT ( 'NONE',  ( 33.59409845015440510, -32.33189051068966791, 33.26142729798142739 ) ) ;
#53803=CARTESIAN_POINT ( 'NONE',  ( -94.26650740058524036, -60.00000000002918199, 16.35100827053066652 ) ) ;
#53805=CARTESIAN_POINT ( 'NONE',  ( 9.945383863341344721, -59.99999999999997868, 39.64580126611800637 ) ) ;
#53808=CARTESIAN_POINT ( 'NONE',  ( -104.6757555735165113, -59.99999999999997158, 94.38003174760403624 ) ) ;
#53809=CARTESIAN_POINT ( 'NONE',  ( 12.17534591919128673, -22.06765856734515197, 27.61564892469329990 ) ) ;
#53811=CARTESIAN_POINT ( 'NONE',  ( -48.85398691093387669, -25.67600413001694548, 44.56680585668343753 ) ) ;
#53821=CARTESIAN_POINT ( 'NONE',  ( 105.1748584867626448, -29.99999999979880272, 127.7968817635670149 ) ) ;
#53826=CARTESIAN_POINT ( 'NONE',  ( 98.00383005827913507, -30.00000000000000711, 190.5271024077575248 ) ) ;
#53834=CARTESIAN_POINT ( 'NONE',  ( 55.26720936171336973, -39.49716498785167573, 60.87020311775951598 ) ) ;
#53841=CARTESIAN_POINT ( 'NONE',  ( -84.13976397268963581, -38.35808942511454234, -23.59170179902847053 ) ) ;
#53844=CARTESIAN_POINT ( 'NONE',  ( 91.09535448090358045, -38.50834339303245457, 200.8244615020851711 ) ) ;
#53846=CARTESIAN_POINT ( 'NONE',  ( 86.21060625849945325, -60.13110528944792321, 7.291613586972188088 ) ) ;
#53865=CARTESIAN_POINT ( 'NONE',  ( 40.21925173228400752, -28.65855273295322903, 47.52501080937051370 ) ) ;
#53868=CARTESIAN_POINT ( 'NONE',  ( 82.95844489808305866, -57.27508763463553976, 188.3864809084460603 ) ) ;
#53871=CARTESIAN_POINT ( 'NONE',  ( -85.96746068820245057, -45.26520172839578748, 43.44881241068694067 ) ) ;
#53876=CARTESIAN_POINT ( 'NONE',  ( 11.54496644200874833, -20.90541225272014714, 35.52027033150145741 ) ) ;
#53878=CARTESIAN_POINT ( 'NONE',  ( 51.38629157293619443, -29.89924560112501695, 48.97383748303278139 ) ) ;
#53889=CARTESIAN_POINT ( 'NONE',  ( -82.65439507748990877, -38.00000000000004263, 4.655876099402581403 ) ) ;
#53897=CARTESIAN_POINT ( 'NONE',  ( -4.645929030050260700, -21.77035645984657108, -30.46299186750976062 ) ) ;
#53905=CARTESIAN_POINT ( 'NONE',  ( -93.45431775348167491, -59.99999999999999289, 36.62235110546294692 ) ) ;
#53911=CARTESIAN_POINT ( 'NONE',  ( -83.59546275602320975, -32.52938965378904612, 164.2985913065920727 ) ) ;
#53913=CARTESIAN_POINT ( 'NONE',  ( -1.113195845631288261, 0.000000000000000000, -17.01594651244888468 ) ) ;
#53923=CARTESIAN_POINT ( 'NONE',  ( -93.89173215636174064, -57.65323629495627245, -14.51111636511549996 ) ) ;
#53929=CARTESIAN_POINT ( 'NONE',  ( 85.55833380596646975, -30.00000000000001776, -20.40969086358413520 ) ) ;
#53930=CARTESIAN_POINT ( 'NONE',  ( -41.69391581180516937, -30.00000000000004974, 49.76410629065788527 ) ) ;
#53931=CARTESIAN_POINT ( 'NONE',  ( -56.75726646438702261, -36.02614299241896845, 62.71715199122408535 ) ) ;
#53935=CARTESIAN_POINT ( 'NONE',  ( -100.7672544247349720, -52.74092989697082601, 193.5979465487865241 ) ) ;
#53943=CARTESIAN_POINT ( 'NONE',  ( 6.026974479199131350E-05, -59.99999999999998579, 33.88964995960238014 ) ) ;
#53949=CARTESIAN_POINT ( 'NONE',  ( -27.34044518871554175, -25.57706821543484565, 29.89117138373360660 ) ) ;
#53952=CARTESIAN_POINT ( 'NONE',  ( 48.55886448841192049, -18.75703111879850127, 42.04255479722105804 ) ) ;
#53954=DIRECTION ( 'NONE',  ( 0.000000000000000000, 0.000000000000000000, -1.000000000000000000 ) ) ;
#53955=CARTESIAN_POINT ( 'NONE',  ( -110.5591912841294686, -38.35612243691561218, 181.8259589841011632 ) ) ;
#53957=CARTESIAN_POINT ( 'NONE',  ( 91.08098746901168852, -38.40443225276378314, -12.15589167778872692 ) ) ;
#53963=CARTESIAN_POINT ( 'NONE',  ( 110.4675968189470012, -59.99999999999997868, 189.7332865883540478 ) ) ;
#53973=CARTESIAN_POINT ( 'NONE',  ( -110.8177222418062655, -38.35606902373660887, 164.8957494206476611 ) ) ;
#53983=CARTESIAN_POINT ( 'NONE',  ( 84.64420705326479322, -28.97169219033941445, 168.9226975528648040 ) ) ;
#54023=CARTESIAN_POINT ( 'NONE',  ( -111.6689541673699750, -60.00000000000000000, 183.3448424905921286 ) ) ;
#54028=CARTESIAN_POINT ( 'NONE',  ( -85.31393835196715258, -28.76575568053742415, 175.9393138315395504 ) ) ;
#54033=CARTESIAN_POINT ( 'NONE',  ( -86.12938452815190260, -60.14213912132001383, 12.56794793439099500 ) ) ;
#54038=CARTESIAN_POINT ( 'NONE',  ( 103.1541778469752160, -29.99999999999992184, 197.4146557462016176 ) ) ;
#54040=CARTESIAN_POINT ( 'NONE',  ( -106.1205840060921730, -60.00000000000004263, 102.8126256328862667 ) ) ;
#54041=CARTESIAN_POINT ( 'NONE',  ( -64.56638066497201578, -25.57904519531993870, 77.78355544515780196 ) ) ;
#54044=CARTESIAN_POINT ( 'NONE',  ( 93.93534938131868728, -14.21045842199442433, 198.1410878059230072 ) ) ;
#54046=CARTESIAN_POINT ( 'NONE',  ( 77.77493926578759442, -60.00000000000120792, 197.3217668548883239 ) ) ;
#54057=CARTESIAN_POINT ( 'NONE',  ( -92.45990064392792362, -60.00000000000002842, -11.61392837640961595 ) ) ;
#54061=CARTESIAN_POINT ( 'NONE',  ( 21.88880945939638067, -4.285714285714295357, 12.64023069600375493 ) ) ;
#54074=CARTESIAN_POINT ( 'NONE',  ( 34.85686279961707612, -22.18117105793543331, 31.83958341934053848 ) ) ;
#54075=CARTESIAN_POINT ( 'NONE',  ( -19.43146043915540488, 9.659702761776270386E-13, -11.19959342721046980 ) ) ;
#54090=CARTESIAN_POINT ( 'NONE',  ( 92.27083909279834018, -59.99999999999999289, 1.911750569454251814 ) ) ;
#54097=STYLED_ITEM ( 'NONE', ( #35832 ), #61965 ) ;
#54098=CARTESIAN_POINT ( 'NONE',  ( -106.3631125035437464, -30.00000000000582290, 193.1115520981887812 ) ) ;
#54103=CARTESIAN_POINT ( 'NONE',  ( 84.09852957777411575, -60.17183186639107362, -17.33093850757677146 ) ) ;
#54106=CARTESIAN_POINT ( 'NONE',  ( 73.50474219086036953, -59.99999999999997158, -24.84696050693406022 ) ) ;
#54112=CARTESIAN_POINT ( 'NONE',  ( 77.90476537984217487, -53.37054513156353863, 147.1940195355752792 ) ) ;
#54118=CARTESIAN_POINT ( 'NONE',  ( -93.14832842661381562, -57.61817439972283239, 204.4570750068989469 ) ) ;
#54140=CARTESIAN_POINT ( 'NONE',  ( -60.05068428883747345, -29.84980960968719188, -32.87300430704357268 ) ) ;
#54141=CARTESIAN_POINT ( 'NONE',  ( -82.83898444641884851, -29.99999999999999645, 151.7304382314388249 ) ) ;
#54146=CARTESIAN_POINT ( 'NONE',  ( 74.24793750212994325, -57.60337406675898819, 188.0840138985208512 ) ) ;
#54151=CARTESIAN_POINT ( 'NONE',  ( -68.42323370297573604, -60.00000000000000711, 133.1930357778236385 ) ) ;
#54155=CARTESIAN_POINT ( 'NONE',  ( -84.77375970704859753, -53.83494961134933021, 190.3341756863800356 ) ) ;
#54165=CARTESIAN_POINT ( 'NONE',  ( -85.28245759913484392, -60.20252963265404844, -15.59029267851214584 ) ) ;
#54171=SURFACE_STYLE_USAGE ( .BOTH. , #26777 ) ;
#54173=CARTESIAN_POINT ( 'NONE',  ( 89.21217950020245269, -30.00000000000004974, 13.74488734703711934 ) ) ;
#54174=CARTESIAN_POINT ( 'NONE',  ( -78.19826841161986408, -53.37652838430405922, 149.2861074551972536 ) ) ;
#54179=CARTESIAN_POINT ( 'NONE',  ( 82.65254975104842572, -57.52971634350765839, 200.9502613691210229 ) ) ;
#54200=CARTESIAN_POINT ( 'NONE',  ( 91.56522374861557978, -59.99999999999998579, -15.43920004744107644 ) ) ;
#54201=CARTESIAN_POINT ( 'NONE',  ( -76.24265395543058332, -14.21045842199434794, 145.5858823757693301 ) ) ;
#54202=CARTESIAN_POINT ( 'NONE',  ( 26.89278686401765484, -29.04926881985026554, 30.38490685316056883 ) ) ;
#54213=CARTESIAN_POINT ( 'NONE',  ( 85.68806591786149340, -29.99999999999991473, 176.4821778899267599 ) ) ;
#54217=CARTESIAN_POINT ( 'NONE',  ( 81.43563566675868515, -30.00000000000000711, -9.788353114720324655 ) ) ;
#54222=PRODUCT_DEFINITION_FORMATION_WITH_SPECIFIED_SOURCE ( 'ANY', '', #19103, .NOT_KNOWN. ) ;
#54237=CARTESIAN_POINT ( 'NONE',  ( 62.59984008646965492, -56.86289542963405808, 88.13664758048848569 ) ) ;
#54240=CARTESIAN_POINT ( 'NONE',  ( -76.12537862032631608, -38.35598417008158378, -28.58435412235099804 ) ) ;
#54247=CARTESIAN_POINT ( 'NONE',  ( -72.10178200369317381, -60.00000000000000711, -25.50777580964439650 ) ) ;
#54255=CARTESIAN_POINT ( 'NONE',  ( 86.05395271266333168, -39.20869856352000937, 187.0836467292549514 ) ) ;
#54259=CARTESIAN_POINT ( 'NONE',  ( 61.40732561923240951, -29.45172577994906860, -24.51876011215350104 ) ) ;
#54264=CARTESIAN_POINT ( 'NONE',  ( -100.8172700586428618, -29.99999999999999645, 180.0901824726140035 ) ) ;
#54267=CARTESIAN_POINT ( 'NONE',  ( 19.20286887953066923, -57.67181979952086124, 42.11251578178057287 ) ) ;
#54270=FACE_OUTER_BOUND ( 'NONE', #24020, .T. ) ;
#54275=CARTESIAN_POINT ( 'NONE',  ( -86.77107750842486666, -57.39365593820878075, 193.7434059132478978 ) ) ;
#54279=CARTESIAN_POINT ( 'NONE',  ( -12.35491406422132776, -35.99458353833710333, 29.94231072834120155 ) ) ;
#54282=CARTESIAN_POINT ( 'NONE',  ( -103.9455512838813718, -60.00000000000002842, 141.2845372866246123 ) ) ;
#54309=CARTESIAN_POINT ( 'NONE',  ( -76.85716460373025427, -60.00000000000000711, 196.0240674832539582 ) ) ;
#54311=CARTESIAN_POINT ( 'NONE',  ( 24.77227526506132094, -60.00000000000001421, 41.10247213741922678 ) ) ;
#54315=CARTESIAN_POINT ( 'NONE',  ( -109.5929118004772818, -60.00000000000001421, 123.9174817212569621 ) ) ;
#54316=CARTESIAN_POINT ( 'NONE',  ( 11.44797993206735853, -49.91577255025450199, 32.23882742997456319 ) ) ;
#54318=CARTESIAN_POINT ( 'NONE',  ( -48.17436038642846796, -56.82532612053482524, 53.30083711335295504 ) ) ;
#54330=CARTESIAN_POINT ( 'NONE',  ( 89.79167478614425590, -30.00000000002385647, -11.58638050850938761 ) ) ;
#54335=CARTESIAN_POINT ( 'NONE',  ( 100.1645178837010377, -30.00000000000000355, 184.8515023625643323 ) ) ;
#54348=CARTESIAN_POINT ( 'NONE',  ( 101.7179331410454637, -38.44840262328585112, 199.8206546545780498 ) ) ;
#54350=CARTESIAN_POINT ( 'NONE',  ( 86.16765823093783183, -60.13206058599219261, 8.614730465306884355 ) ) ;
#54368=CARTESIAN_POINT ( 'NONE',  ( -37.98285244702580599, -27.77434865196162406, 44.84875665863523153 ) ) ;
#54372=CARTESIAN_POINT ( 'NONE',  ( 84.73931994313983296, -39.38290620261815889, 182.5232074107245239 ) ) ;
#54378=CARTESIAN_POINT ( 'NONE',  ( 94.43512559729094846, -57.67054883863127657, -0.6433801497298585748 ) ) ;
#54387=CARTESIAN_POINT ( 'NONE',  ( 21.47514250170511474, -26.66870654467904345, 37.19702469120311150 ) ) ;
#54389=CARTESIAN_POINT ( 'NONE',  ( 49.62245147187759642, -29.61487503896438156, 46.01461058099387458 ) ) ;
#54398=CARTESIAN_POINT ( 'NONE',  ( -84.68040789762383724, -38.00000000000000711, 42.85769669637753765 ) ) ;
#54407=CARTESIAN_POINT ( 'NONE',  ( -9.323832755003198969, -21.77035872086719337, -30.31131560807224901 ) ) ;
#54416=CARTESIAN_POINT ( 'NONE',  ( -92.61211680020106485, -60.00000000000000000, -10.18716978393410599 ) ) ;
#54422=CARTESIAN_POINT ( 'NONE',  ( -84.44835114658116026, -29.00614591161477662, 166.8971789934990682 ) ) ;
#54434=CARTESIAN_POINT ( 'NONE',  ( -113.8744714263418842, -57.67115484533559311, 181.1306260539751918 ) ) ;
#54440=CARTESIAN_POINT ( 'NONE',  ( 86.58060678326373250, -14.21045842199439235, 15.94037124058900901 ) ) ;
#54441=CARTESIAN_POINT ( 'NONE',  ( -37.55014638933011639, -30.00000000000003553, 45.10809268468624111 ) ) ;
#54442=CARTESIAN_POINT ( 'NONE',  ( -54.63826354663243734, -32.56309779981316410, 56.78580405707901235 ) ) ;
#54446=CARTESIAN_POINT ( 'NONE',  ( -101.0425723163289007, -45.26379046336233358, 191.2487722153988727 ) ) ;
#54451=CARTESIAN_POINT ( 'NONE',  ( -11.28908492393962959, -60.00000000000002132, 39.66396576309020361 ) ) ;
#54462=CARTESIAN_POINT ( 'NONE',  ( -26.45657344687305113, -18.61827304227935898, 28.46810496584365779 ) ) ;
#54465=CARTESIAN_POINT ( 'NONE',  ( 48.15947195856908536, -22.22280960889669998, 42.58632823541661594 ) ) ;
#54470=CARTESIAN_POINT ( 'NONE',  ( -104.5228042232798060, -38.40271399333908420, 197.9462138014538652 ) ) ;
#54474=CARTESIAN_POINT ( 'NONE',  ( 89.02348576509739075, -38.38241123853795500, -18.01053637648232097 ) ) ;
#54482=( GEOMETRIC_REPRESENTATION_CONTEXT ( 3 ) GLOBAL_UNCERTAINTY_ASSIGNED_CONTEXT ( ( #54740 ) ) GLOBAL_UNIT_ASSIGNED_CONTEXT ( ( #42655, #59935, #67478 ) ) REPRESENTATION_CONTEXT ( 'NONE', 'WORKASPACE' ) );
#54485=CARTESIAN_POINT ( 'NONE',  ( 87.14226255876803862, -60.00000000000000000, 201.0601579501399385 ) ) ;
#54486=VECTOR ( 'NONE', #79877, 1000.000000000000000 ) ;
#54494=CARTESIAN_POINT ( 'NONE',  ( -91.47160050282491284, -38.38034665535289491, -5.985717668559722426 ) ) ;
#54505=CARTESIAN_POINT ( 'NONE',  ( 82.99793886178632363, -42.97529097282338739, 175.1910793254024838 ) ) ;
#54519=ORIENTED_EDGE ( 'NONE', *, *, #76351, .F. ) ;
#54547=CARTESIAN_POINT ( 'NONE',  ( -111.0778047984082804, -60.00000000000001421, 152.9011151817173015 ) ) ;
#54554=DIRECTION ( 'NONE',  ( 0.000000000000000000, 0.000000000000000000, -1.000000000000000000 ) ) ;
#54557=CARTESIAN_POINT ( 'NONE',  ( -82.22483725259803578, -60.77147558768366054, 188.6628005082894788 ) ) ;
#54565=CARTESIAN_POINT ( 'NONE',  ( -86.03344881383972620, -52.70846120426877235, 32.67016257065858298 ) ) ;
#54570=CARTESIAN_POINT ( 'NONE',  ( 103.0033180414816343, -14.21045842199429643, 193.8537495780579150 ) ) ;
#54571=CARTESIAN_POINT ( 'NONE',  ( -110.8742113967375928, -60.00000000000001421, 132.3764718065442594 ) ) ;
#54572=CARTESIAN_POINT ( 'NONE',  ( -62.04700422542156701, -60.34632947214632992, 88.28556169221526773 ) ) ;
#54575=CARTESIAN_POINT ( 'NONE',  ( 100.7783224761645045, -60.00000000000495959, 204.1744434044741467 ) ) ;
#54580=ORIENTED_EDGE ( 'NONE', *, *, #93204, .F. ) ;
#54585=CARTESIAN_POINT ( 'NONE',  ( -92.04536671911790791, -60.00000000000000000, 5.198000682803741945 ) ) ;
#54598=CARTESIAN_POINT ( 'NONE',  ( 33.35568202832040896, -42.96150302412274868, 35.15671921136284084 ) ) ;
#54599=CARTESIAN_POINT ( 'NONE',  ( -17.78317311657527000, -3.867350551647862515E-12, 13.66642973271121342 ) ) ;
#54612=CARTESIAN_POINT ( 'NONE',  ( 100.7803950627615279, -60.00000000000000711, 85.61164634517442096 ) ) ;
#54619=CARTESIAN_POINT ( 'NONE',  ( -90.65468487766462147, -30.00000000010611956, 35.87486351368138315 ) ) ;
#54640=CARTESIAN_POINT ( 'NONE',  ( 76.89198577027414672, -56.84083229141209159, 144.4104520508552696 ) ) ;
#54657=CARTESIAN_POINT ( 'NONE',  ( -33.81503581996810226, -23.50581328268117076, 33.08946069656037992 ) ) ;
#54668=DIRECTION ( 'NONE',  ( 1.000000000000000000, 0.000000000000000000, -3.673940397442057649E-17 ) ) ;
#54671=CARTESIAN_POINT ( 'NONE',  ( 27.22613109232188933, -23.01811225391248072, -37.39308776158987513 ) ) ;
#54672=CARTESIAN_POINT ( 'NONE',  ( -66.94430381114793249, -30.00000000000000000, 85.89596885270491100 ) ) ;
#54677=CARTESIAN_POINT ( 'NONE',  ( 87.40653855078360834, -57.59069015034623362, 203.2446439553187076 ) ) ;
#54678=CARTESIAN_POINT ( 'NONE',  ( 63.67661289323277174, -60.22834765982614869, -28.64704440831590659 ) ) ;
#54685=CARTESIAN_POINT ( 'NONE',  ( -68.90087116575429604, -60.00000000000000711, 135.5803340585387389 ) ) ;
#54690=CARTESIAN_POINT ( 'NONE',  ( -85.61816920359592586, -42.90765739005369994, 187.3767756352330309 ) ) ;
#54696=CARTESIAN_POINT ( 'NONE',  ( -82.96269021345402450, -45.26010578133133322, -14.54628423973963613 ) ) ;
#54704=CARTESIAN_POINT ( 'NONE',  ( -11.19959342721765694, -8.673617379884035472E-16, 19.43146043914803300 ) ) ;
#54706=CARTESIAN_POINT ( 'NONE',  ( 73.45964196357411424, -30.00000000000000355, -28.33384050355910588 ) ) ;
#54707=CARTESIAN_POINT ( 'NONE',  ( -78.24281470800275429, -46.43791216846317127, 142.3052197231980642 ) ) ;
#54711=CARTESIAN_POINT ( 'NONE',  ( 97.15025092940463480, -57.62288696014798006, 204.4334119669128143 ) ) ;
#54724=CIRCLE ( 'NONE', #63397, 2.000000000000001776 ) ;
#54733=CARTESIAN_POINT ( 'NONE',  ( -52.32131825073019371, -14.21045842199420584, 63.24190059944674402 ) ) ;
#54734=CARTESIAN_POINT ( 'NONE',  ( 27.64130989961823914, -32.52850770992262852, 31.18481338930833857 ) ) ;
#54740=UNCERTAINTY_MEASURE_WITH_UNIT (LENGTH_MEASURE( 1.000000000000000082E-05 ), #42655, 'distance_accuracy_value', 'NONE');
#54742=CARTESIAN_POINT ( 'NONE',  ( -16.66764709352487372, -4.285714285714296246, -19.00223544648545015 ) ) ;
#54754=CARTESIAN_POINT ( 'NONE',  ( 81.59386212306293373, -29.99999999999999289, -6.572264366181854278 ) ) ;
#54778=CARTESIAN_POINT ( 'NONE',  ( 63.15375676826720763, -53.38644956618764326, 87.98034761718228935 ) ) ;
#54788=CARTESIAN_POINT ( 'NONE',  ( -13.27149476923476712, -60.00000000000002842, -36.51807098106452543 ) ) ;
#54795=CARTESIAN_POINT ( 'NONE',  ( 86.46880582727897036, -17.03922905361648077, 183.6885730758262412 ) ) ;
#54799=CARTESIAN_POINT ( 'NONE',  ( 50.48997130883752504, -27.63153651148716250, -27.86727969785274084 ) ) ;
#54804=CARTESIAN_POINT ( 'NONE',  ( -99.16400268747783286, -30.00000000000000355, 146.3272739617164859 ) ) ;
#54806=EDGE_CURVE ( 'NONE', #38839, #51964, #1018, .T. ) ;
#54808=CARTESIAN_POINT ( 'NONE',  ( 45.09708299774578677, -57.68305803399005072, 65.37286121897045632 ) ) ;
#54825=CARTESIAN_POINT ( 'NONE',  ( -11.32722631842166017, -39.47613668441685064, 30.49643211446674584 ) ) ;
#54827=CARTESIAN_POINT ( 'NONE',  ( -106.0333887696626078, -59.99999999999998579, 181.9111336990339680 ) ) ;
#54828=CARTESIAN_POINT ( 'NONE',  ( 4.154708322984369194E-08, -57.67120202538961138, 41.61186700422869933 ) ) ;
#54835=CARTESIAN_POINT ( 'NONE',  ( 69.44492854271774718, -60.00000000000000711, 138.4067570271645025 ) ) ;
#54841=FILL_AREA_STYLE ('',( #93732 ) ) ;
#54853=CARTESIAN_POINT ( 'NONE',  ( -110.5746535952040972, -60.00000000005854872, 130.2065959066731011 ) ) ;
#54855=CARTESIAN_POINT ( 'NONE',  ( 92.33617079703029162, -59.99999999999995737, 202.4045417339447397 ) ) ;
#54859=CARTESIAN_POINT ( 'NONE',  ( -100.4058209406884856, -60.00000000000003553, 69.07134566225379047 ) ) ;
#54860=CARTESIAN_POINT ( 'NONE',  ( 11.08465001081330925, -18.58647777032097181, 27.00989251387364476 ) ) ;
#54864=CARTESIAN_POINT ( 'NONE',  ( -44.62962198081419984, -32.61883708493877521, 41.38836346102954167 ) ) ;
#54874=CARTESIAN_POINT ( 'NONE',  ( 81.20698152405282144, -30.00000000003515055, 192.9746070141664234 ) ) ;
#54878=CARTESIAN_POINT ( 'NONE',  ( 98.91475564777206841, -30.00000000000000000, 189.0293257016073483 ) ) ;
#54893=CARTESIAN_POINT ( 'NONE',  ( 95.07921971528816130, -38.48855209000599586, 201.2237972424360635 ) ) ;
#54895=CARTESIAN_POINT ( 'NONE',  ( 83.25488535439697557, -37.82197581851302459, -5.752366542783479808 ) ) ;
#54896=CARTESIAN_POINT ( 'NONE',  ( 73.65690706782872610, -38.00000000000002842, 114.0709836083384658 ) ) ;
#54901=EDGE_CURVE ( 'NONE', #94858, #71278, #97086, .T. ) ;
#54917=CARTESIAN_POINT ( 'NONE',  ( -12.85249586701553071, -16.98649936182289721, 34.86928669122507074 ) ) ;
#54922=CARTESIAN_POINT ( 'NONE',  ( 85.02428816751515228, -39.35071464379650052, 183.7559687439404854 ) ) ;
#54927=CARTESIAN_POINT ( 'NONE',  ( 93.86644721295161276, -57.67548266447655436, 8.769766783338946325 ) ) ;
#54930=CARTESIAN_POINT ( 'NONE',  ( -3.503743025706806513, -21.47813235944761345, -38.54973997311672207 ) ) ;
#54931=CARTESIAN_POINT ( 'NONE',  ( 19.42789538572690233, -25.34295863529625592, 36.70993147433372883 ) ) ;
#54933=CARTESIAN_POINT ( 'NONE',  ( 49.52626439931135138, -29.59496896688949619, 45.86522708161003692 ) ) ;
#54939=CARTESIAN_POINT ( 'NONE',  ( -14.17377942356327125, -24.37016208792438121, -30.50618185950635564 ) ) ;
#54942=CARTESIAN_POINT ( 'NONE',  ( -102.6774475846397650, -37.99999999999999289, 166.4555440054269013 ) ) ;
#54949=CARTESIAN_POINT ( 'NONE',  ( -43.48600344072682589, -21.77010246326202036, -26.80835130359935192 ) ) ;
#54958=CARTESIAN_POINT ( 'NONE',  ( -91.91080975627225769, -59.99999999999999289, -14.28697677751371842 ) ) ;
#54965=CARTESIAN_POINT ( 'NONE',  ( -79.19495016516171404, -60.32924324703077446, 166.8371806976799974 ) ) ;
#54975=CARTESIAN_POINT ( 'NONE',  ( -106.5151323516585649, -57.65184864013982491, 200.5412705504392079 ) ) ;
#54980=CARTESIAN_POINT ( 'NONE',  ( 91.01458086108723933, -60.00000000000020606, -21.64996939806972520 ) ) ;
#54981=CARTESIAN_POINT ( 'NONE',  ( -46.52099778141491271, -60.00000000000009948, 69.35786614446448084 ) ) ;
#54983=CARTESIAN_POINT ( 'NONE',  ( -54.73520214394920202, -60.32528689200320571, 68.31679214792625032 ) ) ;
#54988=CARTESIAN_POINT ( 'NONE',  ( -100.2331735737419507, -45.25801489425005997, 192.3635796437690146 ) ) ;
#54993=CARTESIAN_POINT ( 'NONE',  ( 84.77039385422880002, -38.35861834270041015, -23.06278009602441514 ) ) ;
#54998=DIRECTION ( 'NONE',  ( 0.000000000000000000, -1.000000000000000000, 0.000000000000000000 ) ) ;
#55003=CARTESIAN_POINT ( 'NONE',  ( -28.09024253349489086, -42.96081926787068994, 33.13080107984512068 ) ) ;
#55006=CARTESIAN_POINT ( 'NONE',  ( 47.84836796458573360, -60.27567004627039893, 53.82506687556728764 ) ) ;
#55010=CARTESIAN_POINT ( 'NONE',  ( -108.8686793369359691, -38.35655312135317985, 190.5485178590994337 ) ) ;
#55012=CARTESIAN_POINT ( 'NONE',  ( 89.32126971945325522, -38.38618640067141285, -17.46414196423140908 ) ) ;
#55023=CARTESIAN_POINT ( 'NONE',  ( 94.29025393882723449, -60.00000000000000711, 202.5621357744927025 ) ) ;
#55027=CARTESIAN_POINT ( 'NONE',  ( 58.81832265629508782, -42.96300998799636517, 70.77614602442089620 ) ) ;
#55034=CARTESIAN_POINT ( 'NONE',  ( -110.9034503428022589, -38.35606005712202204, 177.3331091593476287 ) ) ;
#55047=CARTESIAN_POINT ( 'NONE',  ( 82.82797534076844670, -46.49035231702586657, 178.5343783493842693 ) ) ;
#55060=CARTESIAN_POINT ( 'NONE',  ( -81.59233676157388970, -29.99999999999999289, -7.131517857166998375 ) ) ;
#55063=CARTESIAN_POINT ( 'NONE',  ( -1.778128680800643568, -18.09823649448113159, 35.01458484713825925 ) ) ;
#55087=CARTESIAN_POINT ( 'NONE',  ( -111.0802930874671404, -59.99999999999999289, 152.9258238175857514 ) ) ;
#55091=CARTESIAN_POINT ( 'NONE',  ( -85.58345756656004255, -25.26006554871649357, 173.5983781047130776 ) ) ;
#55099=CARTESIAN_POINT ( 'NONE',  ( -82.46547003015899691, -37.82730713131258682, 15.76482451545277819 ) ) ;
#55100=CARTESIAN_POINT ( 'NONE',  ( -80.00000000000000000, -52.00000000000000000, -21.09707704303352926 ) ) ;
#55104=SURFACE_STYLE_USAGE ( .BOTH. , #86465 ) ;
#55106=CARTESIAN_POINT ( 'NONE',  ( 111.5326445490954228, -59.99999999999995737, 193.8609935400126005 ) ) ;
#55108=CARTESIAN_POINT ( 'NONE',  ( -106.4977058212534189, -30.00000000000001776, 137.1023255444873428 ) ) ;
#55110=CARTESIAN_POINT ( 'NONE',  ( -64.25203903599586397, -36.00863644870968727, 82.20997637332776264 ) ) ;
#55113=CARTESIAN_POINT ( 'NONE',  ( 72.30394896831228380, -59.99999999998524203, 178.8862666714183831 ) ) ;
#55123=CARTESIAN_POINT ( 'NONE',  ( -91.48089212003628745, -59.99999999999998579, -15.71179409066253108 ) ) ;
#55134=CARTESIAN_POINT ( 'NONE',  ( 104.5753504995763166, -60.00000000000000711, 189.2153576413880387 ) ) ;
#55135=CARTESIAN_POINT ( 'NONE',  ( -37.15836322851141915, -42.97305262937527459, 37.35069024152737427 ) ) ;
#55138=CARTESIAN_POINT ( 'NONE',  ( 34.47736779890171732, -36.03285718270048932, 34.37443323975536913 ) ) ;
#55139=CARTESIAN_POINT ( 'NONE',  ( 17.01589776168603407, -1.734723475976807094E-15, 2.227375807149028386 ) ) ;
#55143=CARTESIAN_POINT ( 'NONE',  ( -67.69295672967986377, -38.33449906752677094, 124.1936149075851006 ) ) ;
#55154=CARTESIAN_POINT ( 'NONE',  ( 94.32990217694337787, -60.00000000000000711, 43.96823495280933969 ) ) ;
#55160=CARTESIAN_POINT ( 'NONE',  ( -89.26045497392905759, -30.00000000002656364, 8.412000526470205131 ) ) ;
#55177=CARTESIAN_POINT ( 'NONE',  ( 79.54531020092385063, -46.43426362482939851, 150.5956621145262488 ) ) ;
#55184=CARTESIAN_POINT ( 'NONE',  ( -9.856791769558052252, -57.67120557387264768, 41.61776228975389813 ) ) ;
#55203=ORIENTED_EDGE ( 'NONE', *, *, #17173, .T. ) ;
#55211=CARTESIAN_POINT ( 'NONE',  ( -83.66754629239434848, -30.00000000000000000, 158.1039837908334391 ) ) ;
#55213=EDGE_CURVE ( 'NONE', #16368, #102350, #91052, .T. ) ;
#55216=CARTESIAN_POINT ( 'NONE',  ( 89.63106980978587046, -57.60730104231549831, 203.9042347144641951 ) ) ;
#55217=CARTESIAN_POINT ( 'NONE',  ( 61.40955143832069751, -47.40894800045192881, -27.09024030718980924 ) ) ;
#55222=CARTESIAN_POINT ( 'NONE',  ( -75.24012889104587032, -60.00000000000000000, 182.9205892844746870 ) ) ;
#55227=CARTESIAN_POINT ( 'NONE',  ( -84.00149967252067995, -61.04795672767421877, 192.3141443173471998 ) ) ;
#55233=CARTESIAN_POINT ( 'NONE',  ( -81.92182049364998875, -37.79510036308117549, -13.91368132035993455 ) ) ;
#55240=CARTESIAN_POINT ( 'NONE',  ( 20.16952962162183738, -4.285714285713005722, -15.50035291838722884 ) ) ;
#55242=CARTESIAN_POINT ( 'NONE',  ( 89.66268371970539874, -30.00000000000002487, 1.291492552605954858 ) ) ;
#55244=CARTESIAN_POINT ( 'NONE',  ( -79.28778576954361768, -42.96893229327703523, 145.0288265907346386 ) ) ;
#55246=CARTESIAN_POINT ( 'NONE',  ( 12.46466094585187889, -29.99999999999991118, 37.03825901911487506 ) ) ;
#55248=CARTESIAN_POINT ( 'NONE',  ( 74.06814223428997934, -57.60986418767995332, 187.4363434323835804 ) ) ;
#55256=CARTESIAN_POINT ( 'NONE',  ( -100.0016765554683928, -37.82064696691352879, 139.8630582154185049 ) ) ;
#55268=CARTESIAN_POINT ( 'NONE',  ( 27.32589341038793052, -39.47960534280331046, 32.30614241192893132 ) ) ;
#55278=CARTESIAN_POINT ( 'NONE',  ( 1.405425595346621037E-06, -60.00000000000000000, -42.63907915653317104 ) ) ;
#55280=CARTESIAN_POINT ( 'NONE',  ( 88.15283761886021807, -30.00000000000000000, 187.1385865483707960 ) ) ;
#55296=DIRECTION ( 'NONE',  ( 0.000000000000000000, 1.000000000000000000, 0.000000000000000000 ) ) ;
#55307=CARTESIAN_POINT ( 'NONE',  ( -79.71008617727251533, -60.00000000000007816, 171.5468452086663262 ) ) ;
#55308=CARTESIAN_POINT ( 'NONE',  ( 63.37350735021203718, -49.91027513827258133, 86.82604463955132701 ) ) ;
#55314=CARTESIAN_POINT ( 'NONE',  ( -0.01431428620034891179, -57.67120202577072519, -44.61186648040676772 ) ) ;
#55316=AXIS2_PLACEMENT_3D ( 'NONE', #49394, #17594, #23571 ) ;
#55319=CARTESIAN_POINT ( 'NONE',  ( 24.34055539606506002, -60.00000000000002842, -35.71097672886680385 ) ) ;
#55324=CARTESIAN_POINT ( 'NONE',  ( 86.11264096538754131, -53.80573175718830470, 192.0612798401426176 ) ) ;
#55332=CARTESIAN_POINT ( 'NONE',  ( 25.60766401561201278, -60.00000000000000000, 41.33855483581840673 ) ) ;
#55333=CARTESIAN_POINT ( 'NONE',  ( -99.97669482139977504, -30.00000000000000000, 185.6954798495859222 ) ) ;
#55337=CARTESIAN_POINT ( 'NONE',  ( 45.24179637743248605, -57.68290370260588418, 65.68885952698795450 ) ) ;
#55345=CARTESIAN_POINT ( 'NONE',  ( -16.35932222714940920, -60.00000000000000000, 39.87631610020545736 ) ) ;
#55346=CARTESIAN_POINT ( 'NONE',  ( -87.47245207465813621, -39.05729538259036104, 189.8431066894454773 ) ) ;
#55351=CARTESIAN_POINT ( 'NONE',  ( -15.30569569889779302, -18.58753576952222630, 27.14328885328878016 ) ) ;
#55353=CARTESIAN_POINT ( 'NONE',  ( -104.7817843546067564, -60.00000000000002842, 188.6132346340173740 ) ) ;
#55360=DIRECTION ( 'NONE',  ( 0.000000000000000000, 0.000000000000000000, -1.000000000000000000 ) ) ;
#55364=CARTESIAN_POINT ( 'NONE',  ( 73.43745472883394143, -60.00000000000001421, 166.5727501461540214 ) ) ;
#55369=CARTESIAN_POINT ( 'NONE',  ( 4.154910845142357978, -29.99999999999994316, 36.99135396797706932 ) ) ;
#55370=CARTESIAN_POINT ( 'NONE',  ( 1.544427540536530710E-15, -4.285714285714290916, -25.22241582816893057 ) ) ;
#55384=CARTESIAN_POINT ( 'NONE',  ( -107.3965502307806901, -59.99999999998781419, 200.2794665723340586 ) ) ;
#55385=CARTESIAN_POINT ( 'NONE',  ( 75.69572031415813740, -60.00000000000000000, 185.6113820405912236 ) ) ;
#55389=CARTESIAN_POINT ( 'NONE',  ( -105.3891558216856339, -14.21045842199431064, 188.2119682431835486 ) ) ;
#55390=CARTESIAN_POINT ( 'NONE',  ( 9.087783854787057081, -25.54846076700239976, 28.14888778420710835 ) ) ;
#55391=CARTESIAN_POINT ( 'NONE',  ( 102.8126250176293013, -38.00000000000001421, 170.8513491865694505 ) ) ;
#55393=CARTESIAN_POINT ( 'NONE',  ( -47.00499629171626026, -22.23575002398623113, 41.16886872908139594 ) ) ;
#55404=CARTESIAN_POINT ( 'NONE',  ( 89.85535138209283446, -29.99999999996537525, 199.2189362433487076 ) ) ;
#55407=CARTESIAN_POINT ( 'NONE',  ( 90.45918241757048861, -30.00000000000000000, 91.17802396393395270 ) ) ;
#55422=CARTESIAN_POINT ( 'NONE',  ( 104.1038336098137478, -38.40903114083004510, 198.3374114307139280 ) ) ;
#55424=CARTESIAN_POINT ( 'NONE',  ( 84.05541200475410335, -45.28723854143181882, 1.855072029239146936 ) ) ;
#55425=CARTESIAN_POINT ( 'NONE',  ( 68.83552688692435595, -38.00000000000000000, 97.13860410137628776 ) ) ;
#55442=CARTESIAN_POINT ( 'NONE',  ( 35.86766554461611634, -26.86117697613646627, 42.80318219311200068 ) ) ;
#55448=CARTESIAN_POINT ( 'NONE',  ( 83.48300417591265443, -57.35605306953866744, 189.6652105889277777 ) ) ;
#55451=CARTESIAN_POINT ( 'NONE',  ( 95.57936171141837178, -57.67169793798020550, 37.86718902071597626 ) ) ;
#55457=CARTESIAN_POINT ( 'NONE',  ( -85.96552653199317717, -37.99999999999979394, 186.3819002138399412 ) ) ;
#55468=CARTESIAN_POINT ( 'NONE',  ( -82.11800378195846406, -37.99999999999997868, -13.62076433111584883 ) ) ;
#55471=CARTESIAN_POINT ( 'NONE',  ( -21.03575760287767693, -18.85229723311598349, -33.58254685689154684 ) ) ;
#55473=CARTESIAN_POINT ( 'NONE',  ( -60.63884085839525540, -34.58948043286759599, -25.08978428314187781 ) ) ;
#55474=ORIENTED_EDGE ( 'NONE', *, *, #2655, .T. ) ;
#55480=CARTESIAN_POINT ( 'NONE',  ( -92.53051596449445526, -59.99999999999998579, -1.702129118078903547 ) ) ;
#55483=CARTESIAN_POINT ( 'NONE',  ( 96.70244981892803082, -60.35942960495466991, 196.8117809302864316 ) ) ;
#55487=CARTESIAN_POINT ( 'NONE',  ( -81.09797583371168628, -46.44412491365037710, 163.0375973178554432 ) ) ;
#55491=ORIENTED_EDGE ( 'NONE', *, *, #22347, .T. ) ;
#55498=CARTESIAN_POINT ( 'NONE',  ( -113.5594301016874539, -57.67117831481159840, 184.0234983118591856 ) ) ;
#55504=CARTESIAN_POINT ( 'NONE',  ( 89.66801957890137942, -59.99999999999992895, -23.31517609469964469 ) ) ;
#55505=CARTESIAN_POINT ( 'NONE',  ( -69.35428882245668092, -14.21045842199431064, 113.5922931172439263 ) ) ;
#55507=CARTESIAN_POINT ( 'NONE',  ( -52.65234607686913648, -46.44195135248897799, 58.10028993942689368 ) ) ;
#55511=CARTESIAN_POINT ( 'NONE',  ( -101.8606233574472526, -52.71812712487817976, 192.2808579428766507 ) ) ;
#55513=ORIENTED_EDGE ( 'NONE', *, *, #63940, .F. ) ;
#55515=CARTESIAN_POINT ( 'NONE',  ( 107.9104760785782560, -38.35877191852540591, 193.0889224582925294 ) ) ;
#55529=ORIENTED_EDGE ( 'NONE', *, *, #38045, .T. ) ;
#55531=CARTESIAN_POINT ( 'NONE',  ( 49.37742207085376123, -36.05361790536632327, 48.61349652102713748 ) ) ;
#55536=CARTESIAN_POINT ( 'NONE',  ( -104.5277147594802756, -38.40261826923566701, 197.9417711179345645 ) ) ;
#55538=CARTESIAN_POINT ( 'NONE',  ( 91.07270688230414635, -38.34878623222908089, 1.164067527244401656 ) ) ;
#55542=CARTESIAN_POINT ( 'NONE',  ( 93.17606065420541483, -37.84849057407753037, 97.15365511994282599 ) ) ;
#55548=CARTESIAN_POINT ( 'NONE',  ( 80.84005111079980566, -60.00000000000000000, 196.9542464304632290 ) ) ;
#55552=CARTESIAN_POINT ( 'NONE',  ( 58.77133666112784027, -29.07347965779057120, 64.41413915537998491 ) ) ;
#55558=CARTESIAN_POINT ( 'NONE',  ( -98.14959585606926851, -38.47957152706085537, 200.9671316718450385 ) ) ;
#55568=CARTESIAN_POINT ( 'NONE',  ( 85.62085174182965375, -21.92232634333130292, 167.5821520937073785 ) ) ;
#55605=CARTESIAN_POINT ( 'NONE',  ( -106.9148777809588893, -60.00000000000000000, 122.1078712977356275 ) ) ;
#55611=CARTESIAN_POINT ( 'NONE',  ( -81.58353690299945526, -57.03497744733997621, 182.7981024581307850 ) ) ;
#55618=CARTESIAN_POINT ( 'NONE',  ( -82.88211207980042161, -37.82423770264409058, 24.55814771371032634 ) ) ;
#55624=CARTESIAN_POINT ( 'NONE',  ( 110.6388055374740276, -59.99999999999995026, 195.8051704144367591 ) ) ;
#55625=CARTESIAN_POINT ( 'NONE',  ( -100.4058209406884856, -60.00000000000003553, 69.07134566225379047 ) ) ;
#55626=CARTESIAN_POINT ( 'NONE',  ( -60.69105336276258100, -60.34595984108710098, 84.28698886197565798 ) ) ;
#55629=CARTESIAN_POINT ( 'NONE',  ( 73.60417151696405824, -59.99999999999506173, 187.5411878019601204 ) ) ;
#55631=CARTESIAN_POINT ( 'NONE',  ( 3.060910634449126366, -49.91567764747507141, 32.20382334822807024 ) ) ;
#55641=CARTESIAN_POINT ( 'NONE',  ( -109.7211485432284803, -60.00000000000001421, 192.0136906049105505 ) ) ;
#55650=CARTESIAN_POINT ( 'NONE',  ( 101.7378945492313562, -60.00000000000000000, 194.4303705058995604 ) ) ;
#55651=CARTESIAN_POINT ( 'NONE',  ( -37.69739591874598972, -53.35635198386449929, 39.83913967554838109 ) ) ;
#55655=CARTESIAN_POINT ( 'NONE',  ( 40.76590610560279515, -53.34231791925814292, 42.49342577743990290 ) ) ;
#55656=CARTESIAN_POINT ( 'NONE',  ( 13.66642973271503081, -8.673617379884035472E-16, -17.78317311657917088 ) ) ;
#55659=CARTESIAN_POINT ( 'NONE',  ( -62.11818655019798996, -38.34127833389678841, 103.2225466343185047 ) ) ;
#55669=CARTESIAN_POINT ( 'NONE',  ( 97.95620506833432728, -59.99999999999999289, 68.65487923523417635 ) ) ;
#55678=CARTESIAN_POINT ( 'NONE',  ( -80.61473454522898408, -29.99999999998848565, -24.48213655620298113 ) ) ;
#55695=CARTESIAN_POINT ( 'NONE',  ( 78.76512178856368962, -60.31316846768228856, 162.6500093631206312 ) ) ;
#55701=DIRECTION ( 'NONE',  ( -0.000000000000000000, -1.000000000000000000, -0.000000000000000000 ) ) ;
#55702=CARTESIAN_POINT ( 'NONE',  ( -70.46077158043857480, -57.68242143155622159, 157.6729293506350018 ) ) ;
#55713=CARTESIAN_POINT ( 'NONE',  ( -4.871453668401689791E-08, -12.57758911513053413, 32.18678843846154081 ) ) ;
#55726=CARTESIAN_POINT ( 'NONE',  ( -72.67357598896492732, -38.32474216590297544, -30.15551316088291856 ) ) ;
#55732=CARTESIAN_POINT ( 'NONE',  ( 101.8619292074444616, -57.63174066258962824, 203.3235957780899525 ) ) ;
#55733=CARTESIAN_POINT ( 'NONE',  ( 70.79744548977303964, -21.77034749440733563, -19.10173070115413552 ) ) ;
#55737=CARTESIAN_POINT ( 'NONE',  ( -73.06098663455794906, -60.00000000000000000, 163.0166479149870042 ) ) ;
#55741=CARTESIAN_POINT ( 'NONE',  ( -83.62637298746453496, -57.37962585073366739, 189.9592516013256613 ) ) ;
#55749=CARTESIAN_POINT ( 'NONE',  ( -82.80220596410995881, -45.26056562500249925, -14.83041380441539481 ) ) ;
#55757=CARTESIAN_POINT ( 'NONE',  ( -13.60704923275580924, -1.734723475976807094E-15, -10.45706415777457465 ) ) ;
#55759=CARTESIAN_POINT ( 'NONE',  ( 63.50796903478703115, -60.00000000000007816, -37.13796669901890368 ) ) ;
#55760=CARTESIAN_POINT ( 'NONE',  ( -79.97615926384021634, -39.50033131370128814, 145.6677927735757976 ) ) ;
#55762=CARTESIAN_POINT ( 'NONE',  ( 12.83322425571993186, -59.99999999999995737, 42.04720346242444151 ) ) ;
#55763=CARTESIAN_POINT ( 'NONE',  ( 84.69632291683485903, -57.55696416148584404, 202.1270370136284953 ) ) ;
#55773=CARTESIAN_POINT ( 'NONE',  ( -104.1865559966542634, -52.71019955170553573, 153.9800267041457005 ) ) ;
#55782=CARTESIAN_POINT ( 'NONE',  ( -28.84153870763153904, -30.00000000000004619, 39.52238898731670247 ) ) ;
#55783=CARTESIAN_POINT ( 'NONE',  ( 26.60165167295768640, -22.09540625163044325, 29.10608926666087726 ) ) ;
#55785=ORIENTED_EDGE ( 'NONE', *, *, #100644, .F. ) ;
#55796=CARTESIAN_POINT ( 'NONE',  ( 52.74623303553200060, -60.00000000000001421, -37.36890884799756662 ) ) ;
#55819=CARTESIAN_POINT ( 'NONE',  ( -16.68757544607984755, -59.99999999999999289, 34.10598086550765373 ) ) ;
#55820=CARTESIAN_POINT ( 'NONE',  ( 66.03004151298199531, -39.48245408485600194, 89.23762064710109598 ) ) ;
#55838=CARTESIAN_POINT ( 'NONE',  ( 86.94434408382100798, -28.02298374760003341, 186.6917276570115121 ) ) ;
#55845=CARTESIAN_POINT ( 'NONE',  ( 33.36523397932889878, -60.00000000000000000, 45.10737781336894159 ) ) ;
#55846=CARTESIAN_POINT ( 'NONE',  ( -100.3771068072541652, -30.00000000000000000, 157.7691867327778539 ) ) ;
#55849=CARTESIAN_POINT ( 'NONE',  ( 52.17722917352445222, -57.67658636093570834, 83.19373642209534125 ) ) ;
#55855=CARTESIAN_POINT ( 'NONE',  ( -9.265796308445876761, -59.99999999999999289, 39.64115480165225591 ) ) ;
#55865=CARTESIAN_POINT ( 'NONE',  ( -12.31021798142609747, -32.51299227848760864, 29.36066974128064544 ) ) ;
#55866=CARTESIAN_POINT ( 'NONE',  ( -105.5472279711990069, -60.00000000000000711, 185.2932126898874969 ) ) ;
#55877=CARTESIAN_POINT ( 'NONE',  ( 73.07796749574373507, -60.00000000000000711, 163.1709902845379077 ) ) ;
#55882=CARTESIAN_POINT ( 'NONE',  ( 28.47648766833107103, -14.21045842199436926, 36.49840447651481412 ) ) ;
#55890=CYLINDRICAL_SURFACE ( 'NONE', #3511, 8.000000000000000000 ) ;
#55895=CARTESIAN_POINT ( 'NONE',  ( -15.74020471409081168, -23.10826456785950356, 36.04230649636249950 ) ) ;
#55898=CARTESIAN_POINT ( 'NONE',  ( -93.89671634583459081, -60.00000000000852651, 204.9703477895711217 ) ) ;
#55900=CARTESIAN_POINT ( 'NONE',  ( 54.58065226052892882, -60.00000000000002842, 84.04142156818011244 ) ) ;
#55902=CARTESIAN_POINT ( 'NONE',  ( -106.9108898249343156, -14.21045842199431242, 176.0583478801969193 ) ) ;
#55903=CARTESIAN_POINT ( 'NONE',  ( 13.66819726461015705, -53.39670533342206227, 32.87928641480030478 ) ) ;
#55904=CARTESIAN_POINT ( 'NONE',  ( 82.87101461148294845, -37.99999999999997868, 1.285415469843371294 ) ) ;
#55906=CARTESIAN_POINT ( 'NONE',  ( -47.75002082045136831, -29.14752499694496990, 44.14896982249094037 ) ) ;
#55917=CARTESIAN_POINT ( 'NONE',  ( 85.05745714698613824, -29.99999999998833644, 197.1808723821329465 ) ) ;
#55921=CARTESIAN_POINT ( 'NONE',  ( 94.39176720276513777, -30.00000000000000000, 114.3184923802386521 ) ) ;
#55937=CARTESIAN_POINT ( 'NONE',  ( 78.83138536026389431, -38.67202492304706141, 190.5315074774399307 ) ) ;
#55939=CARTESIAN_POINT ( 'NONE',  ( 84.48650984408737941, -45.28710619378168900, -5.682957750312108480 ) ) ;
#55959=( NAMED_UNIT ( * ) PLANE_ANGLE_UNIT ( ) SI_UNIT ( $, .RADIAN. ) );
#55968=ORIENTED_EDGE ( 'NONE', *, *, #99117, .T. ) ;
#55969=CARTESIAN_POINT ( 'NONE',  ( 83.59514486132030697, -60.99987548644057966, 191.7053679419932735 ) ) ;
#55974=CARTESIAN_POINT ( 'NONE',  ( 95.81300639422605059, -57.67160901947544005, 39.88044211767749658 ) ) ;
#55978=CARTESIAN_POINT ( 'NONE',  ( -69.67520780818028925, -37.99999999999996447, 100.0064218607845277 ) ) ;
#55988=CARTESIAN_POINT ( 'NONE',  ( -81.98196232622828461, -37.99999999999996447, -13.86369433938586582 ) ) ;
#55994=CARTESIAN_POINT ( 'NONE',  ( -56.92527863508112063, -47.40887414813248313, -28.31673470188760788 ) ) ;
#56004=CARTESIAN_POINT ( 'NONE',  ( -90.41325670661385061, -60.00000000000002132, -18.10141139825902101 ) ) ;
#56010=CARTESIAN_POINT ( 'NONE',  ( 97.15172723662661269, -52.81671128251268499, 195.3014279785832343 ) ) ;
#56014=CARTESIAN_POINT ( 'NONE',  ( -82.39702631368088248, -39.49694748076612427, 164.1908697851564796 ) ) ;
#56029=CARTESIAN_POINT ( 'NONE',  ( -105.2191501062491881, -57.64508961356604999, 201.5420537206667291 ) ) ;
#56034=CARTESIAN_POINT ( 'NONE',  ( -65.68019474265784652, -30.00000000000001776, -31.25134080541240422 ) ) ;
#56035=CARTESIAN_POINT ( 'NONE',  ( -34.60361718403136422, -60.00000000000001421, 49.20626982406709971 ) ) ;
#56036=CARTESIAN_POINT ( 'NONE',  ( -52.62903541624970671, -32.57446218424134798, 52.90420147508846327 ) ) ;
#56039=CARTESIAN_POINT ( 'NONE',  ( -96.24129786307111090, -45.25353125910449847, 194.1168147664394610 ) ) ;
#56043=CARTESIAN_POINT ( 'NONE',  ( 81.42364061245054074, -38.35622654735483650, -25.61884919812055372 ) ) ;
#56048=CARTESIAN_POINT ( 'NONE',  ( 84.55162599420341962, -29.99999999999999645, 166.0629177430633092 ) ) ;
#56055=CARTESIAN_POINT ( 'NONE',  ( 49.01001383078526175, -39.51698039974216670, 49.15479020084767114 ) ) ;
#56059=CARTESIAN_POINT ( 'NONE',  ( -106.2167736919956837, -38.37611417361867439, 196.0685381891890700 ) ) ;
#56061=CARTESIAN_POINT ( 'NONE',  ( 96.41480450689181225, -38.35574263741993661, 66.97822750028046812 ) ) ;
#56065=CARTESIAN_POINT ( 'NONE',  ( 99.21197506481942696, -60.15124926635865421, 110.4799484367256923 ) ) ;
#56070=CARTESIAN_POINT ( 'NONE',  ( 101.7954163560313816, -60.00000000000000711, 201.2573263482775303 ) ) ;
#56072=CARTESIAN_POINT ( 'NONE',  ( 56.04098195827219797, -22.14826547861250461, 55.49373265869978411 ) ) ;
#56074=CARTESIAN_POINT ( 'NONE',  ( -89.99999999999997158, -38.00000000001091394, 196.0238439516549818 ) ) ;
#56078=CARTESIAN_POINT ( 'NONE',  ( -106.3530780054166343, -38.37121618136543333, 195.8661688634274469 ) ) ;
#56092=CARTESIAN_POINT ( 'NONE',  ( 86.07226235559976146, -18.39178924599106324, 166.6779042990540063 ) ) ;
#56128=CARTESIAN_POINT ( 'NONE',  ( -109.0665197127778754, -60.00000000000001421, 136.4503932063792320 ) ) ;
#56134=CARTESIAN_POINT ( 'NONE',  ( -84.42293876102274908, -32.44484160355589353, 172.3670057701875749 ) ) ;
#56143=DIRECTION ( 'NONE',  ( 0.000000000000000000, 0.000000000000000000, -1.000000000000000000 ) ) ;
#56148=CARTESIAN_POINT ( 'NONE',  ( 110.8743008064580664, -59.99999999999998579, 132.3768192050824268 ) ) ;
#56149=CARTESIAN_POINT ( 'NONE',  ( -97.22630358410161477, -59.99999999999998579, 47.92073696641181613 ) ) ;
#56150=CARTESIAN_POINT ( 'NONE',  ( -61.96503433816666728, -39.48828635186461611, 77.49540155723640567 ) ) ;
#56152=ORIENTED_EDGE ( 'NONE', *, *, #28311, .T. ) ;
#56154=CARTESIAN_POINT ( 'NONE',  ( 95.39352241366582064, -60.00000000000974865, 32.59770702840283718 ) ) ;
#56156=CIRCLE ( 'NONE', #95794, 1.999999999999998224 ) ;
#56158=CARTESIAN_POINT ( 'NONE',  ( 3.437958683066990667E-06, -25.54837915214530852, 28.14771315162659349 ) ) ;
#56163=DIRECTION ( 'NONE',  ( 0.000000000000000000, -1.000000000000000000, 0.000000000000000000 ) ) ;
#56167=CARTESIAN_POINT ( 'NONE',  ( -104.0851100789305690, -59.99999999999997158, 199.9324485923847021 ) ) ;
#56178=CARTESIAN_POINT ( 'NONE',  ( 98.03244328573691746, -59.99999999999997868, 196.4906452546746038 ) ) ;
#56179=CARTESIAN_POINT ( 'NONE',  ( -33.35600173507818056, -42.96555714314101948, 35.15763485665254962 ) ) ;
#56183=CARTESIAN_POINT ( 'NONE',  ( 39.00479706145522840, -36.05733951926574576, 37.16496500682296755 ) ) ;
#56184=CARTESIAN_POINT ( 'NONE',  ( -22.23822744035697241, -8.673617379884035472E-16, -2.910977163147234759 ) ) ;
#56188=CARTESIAN_POINT ( 'NONE',  ( -67.70953212967587831, -38.33447372670084263, 124.2643868202984976 ) ) ;
#56199=CARTESIAN_POINT ( 'NONE',  ( 94.32674073916098223, -60.00000000000001421, 43.94342970808462923 ) ) ;
#56206=CARTESIAN_POINT ( 'NONE',  ( -78.07839977982523294, -30.00000000000002132, 124.9873134342141867 ) ) ;
#56220=CARTESIAN_POINT ( 'NONE',  ( 81.58097494048502085, -36.02867041663544256, 152.4525182214984511 ) ) ;
#56228=CARTESIAN_POINT ( 'NONE',  ( -30.75663703201544408, -57.68613454458090217, 45.71164565728040685 ) ) ;
#56237=CARTESIAN_POINT ( 'NONE',  ( 89.99999999999997158, -52.00000000000000000, 196.0238439516549818 ) ) ;
#56243=CARTESIAN_POINT ( 'NONE',  ( -27.41612642967203328, -20.44246825615584839, 31.78064786534578445 ) ) ;
#56258=CARTESIAN_POINT ( 'NONE',  ( 67.75539237747796051, -38.10441934046211543, -31.96820234319118370 ) ) ;
#56263=CARTESIAN_POINT ( 'NONE',  ( 90.90101844823369959, -57.61245536370559961, 204.1559653898591193 ) ) ;
#56267=CARTESIAN_POINT ( 'NONE',  ( -73.05954267193276053, -60.00000000000000000, 163.0034808650574405 ) ) ;
#56272=CARTESIAN_POINT ( 'NONE',  ( -83.92159281446114960, -57.41240253432310681, 190.5303650487262814 ) ) ;
#56288=CARTESIAN_POINT ( 'NONE',  ( 19.43146043915153953, -2.602085213965209853E-15, -11.19959342722011364 ) ) ;
#56290=CARTESIAN_POINT ( 'NONE',  ( 84.89432107329884047, -60.00000000000002132, -27.59204247542200505 ) ) ;
#56291=CARTESIAN_POINT ( 'NONE',  ( -78.18481269439429582, -39.49763340085283403, 135.4004602990579258 ) ) ;
#56293=CARTESIAN_POINT ( 'NONE',  ( 44.75958163560274272, -30.00000000000001776, 54.38364795613178870 ) ) ;
#56294=CARTESIAN_POINT ( 'NONE',  ( 105.0394626471009758, -57.64423819974435759, 201.6665972083923748 ) ) ;
#56295=DIRECTION ( 'NONE',  ( -0.000000000000000000, -1.000000000000000000, -0.000000000000000000 ) ) ;
#56315=CARTESIAN_POINT ( 'NONE',  ( 29.33244438116370389, -42.95779854847726398, 33.51356301004039295 ) ) ;
#56335=CARTESIAN_POINT ( 'NONE',  ( 16.31486644108454342, -60.00000000000000711, -42.08170890485629201 ) ) ;
#56336=CARTESIAN_POINT ( 'NONE',  ( 86.10514064236191700, -29.99999999999991473, 179.3049154362485353 ) ) ;
#56359=CARTESIAN_POINT ( 'NONE',  ( -46.13314991754092631, -59.99999999999993605, 50.82605641278608033 ) ) ;
#56360=CARTESIAN_POINT ( 'NONE',  ( 69.97227875550414922, -53.38154203728925751, 110.0492415815727014 ) ) ;
#56385=CARTESIAN_POINT ( 'NONE',  ( 8.529325899348924267, -60.00000000000000000, 39.63650018205241565 ) ) ;
#56386=CARTESIAN_POINT ( 'NONE',  ( -97.57213534682868783, -30.00000000000000711, 190.8491232417298988 ) ) ;
#56390=CARTESIAN_POINT ( 'NONE',  ( 40.74024583315892301, -57.69051585465551568, 56.90653008474016161 ) ) ;
#56391=CARTESIAN_POINT ( 'NONE',  ( 89.99999999999997158, -38.00000000001091394, 188.5238439516623146 ) ) ;
#56392=CARTESIAN_POINT ( 'NONE',  ( 19.25210312709571880, -25.56399626811505854, -38.49344732436618699 ) ) ;
#56396=CARTESIAN_POINT ( 'NONE',  ( -19.98591378148901399, -59.99999999999998579, 40.21844962042136729 ) ) ;
#56402=CARTESIAN_POINT ( 'NONE',  ( -86.98677026252562428, -24.32171485741916683, 186.4285793591348579 ) ) ;
#56406=CARTESIAN_POINT ( 'NONE',  ( -12.17599302799778549, -22.06821926268190381, 27.61575194255241428 ) ) ;
#56420=CARTESIAN_POINT ( 'NONE',  ( 69.41260820018891309, -60.00000000000000711, 138.2351751275483878 ) ) ;
#56424=DIRECTION ( 'NONE',  ( 0.000000000000000000, 0.000000000000000000, 1.000000000000000000 ) ) ;
#56426=CARTESIAN_POINT ( 'NONE',  ( 16.35858893754161869, -14.21045842199445630, 34.55986707822809478 ) ) ;
#56434=DIRECTION ( 'NONE',  ( 0.000000000000000000, 0.000000000000000000, -1.000000000000000000 ) ) ;
#56442=CARTESIAN_POINT ( 'NONE',  ( -101.0269275500464659, -60.00000000001482903, 204.0963534135034934 ) ) ;
#56444=CARTESIAN_POINT ( 'NONE',  ( 78.98376820745889404, -60.00000000000002842, 194.5816734064725892 ) ) ;
#56447=CARTESIAN_POINT ( 'NONE',  ( -106.9593936918335544, -14.21045842199438880, 171.9682640579732436 ) ) ;
#56448=CARTESIAN_POINT ( 'NONE',  ( 14.61249556130028004, -42.95373516407707370, 31.17290009735563316 ) ) ;
#56450=CARTESIAN_POINT ( 'NONE',  ( 83.17395798262967332, -38.00000000000000000, -3.094716530419567402 ) ) ;
#56453=CARTESIAN_POINT ( 'NONE',  ( -46.97696546697627440, -60.27403396181129835, 52.32368530384916738 ) ) ;
#56468=CARTESIAN_POINT ( 'NONE',  ( 104.4225999297474203, -29.99999999999820233, 196.1060340301228564 ) ) ;
#56472=CARTESIAN_POINT ( 'NONE',  ( 96.65141799564703717, -30.00000000000001066, 128.3146508404916801 ) ) ;
#56488=CARTESIAN_POINT ( 'NONE',  ( 77.54571322305440617, -38.51875396053564060, 186.6416166875725935 ) ) ;
#56490=CARTESIAN_POINT ( 'NONE',  ( 81.10970025696315133, -37.99999999999997158, 151.4617437746981068 ) ) ;
#56505=CARTESIAN_POINT ( 'NONE',  ( -23.96426571639764092, -28.31959789768340130, 37.87134685329586148 ) ) ;
#56511=CARTESIAN_POINT ( 'NONE',  ( 86.40784132907582205, -17.71253999786838307, 176.2732639067367586 ) ) ;
#56515=CARTESIAN_POINT ( 'NONE',  ( 95.63906378175919087, -57.67167413368508022, 38.38847120207383767 ) ) ;
#56520=CARTESIAN_POINT ( 'NONE',  ( -79.29266753505190479, -38.00000000000007105, 139.9631112146612395 ) ) ;
#56532=CARTESIAN_POINT ( 'NONE',  ( 68.90372024251841765, -29.95430108788154300, -21.28323659810347834 ) ) ;
#56538=CARTESIAN_POINT ( 'NONE',  ( -28.05387351602792023, -21.77034952975806803, -28.92045250891730390 ) ) ;
#56542=EDGE_LOOP ( 'NONE', ( #50074, #94538, #92448, #97055 ) ) ;
#56550=CARTESIAN_POINT ( 'NONE',  ( -92.65848319411558975, -59.99999999999999289, -3.864875569882980866 ) ) ;
#56555=FACE_OUTER_BOUND ( 'NONE', #84704, .T. ) ;
#56558=CARTESIAN_POINT ( 'NONE',  ( -83.89053484538156624, -25.60343038821535799, 156.2415415813698871 ) ) ;
#56571=CARTESIAN_POINT ( 'NONE',  ( -100.8911947370258844, -57.62911827813870502, 203.6698938757279223 ) ) ;
#56577=CARTESIAN_POINT ( 'NONE',  ( 40.74889026577078965, -14.21045842199439591, -34.22240887780809260 ) ) ;
#56579=CARTESIAN_POINT ( 'NONE',  ( -16.61716630718971643, -29.99999999999995026, 37.21284229651715947 ) ) ;
#56580=CARTESIAN_POINT ( 'NONE',  ( -54.05184654259630150, -22.16297058472909498, 51.66483102732016874 ) ) ;
#56584=CARTESIAN_POINT ( 'NONE',  ( -97.42952934929957109, -60.35587105709884526, 196.6991795949842299 ) ) ;
#56590=CARTESIAN_POINT ( 'NONE',  ( 92.11181465698672355, -38.35455481329138649, 36.38192987799886424 ) ) ;
#56595=CARTESIAN_POINT ( 'NONE',  ( 82.48055652934633031, -30.00000000000000711, 149.2060676150218796 ) ) ;
#56603=CARTESIAN_POINT ( 'NONE',  ( 50.33955204055388322, -56.83121431495037967, 57.28224304148754698 ) ) ;
#56608=CARTESIAN_POINT ( 'NONE',  ( -108.4759618192267538, -38.35621021443558476, 141.3483429577475761 ) ) ;
#56611=CARTESIAN_POINT ( 'NONE',  ( 92.05394513303022563, -38.35408998850439133, 35.25469512580827569 ) ) ;
#56614=CARTESIAN_POINT ( 'NONE',  ( 104.6332049901833301, -52.71708914408988278, 158.7351461483158062 ) ) ;
#56619=CARTESIAN_POINT ( 'NONE',  ( 85.18286175503386914, -59.99999999999999289, 200.1974052157080735 ) ) ;
#56623=CARTESIAN_POINT ( 'NONE',  ( 56.02781999547231351, -32.55576276548075043, 59.68983337992042948 ) ) ;
#56629=CARTESIAN_POINT ( 'NONE',  ( -90.41875325581872858, -38.40214660397878532, -14.85380760910452125 ) ) ;
#56633=LINE ( 'NONE', #23786, #76480 ) ;
#56641=CARTESIAN_POINT ( 'NONE',  ( 84.47475691905646045, -32.43330153130234095, 172.8622483833046033 ) ) ;
#56652=B_SPLINE_CURVE_WITH_KNOTS ( 'NONE', 3,
 ( #74841, #98069, #24218, #33906, #31766, #56532, #58690, #91591, #83478, #39852, #72724, #105626, #64648, #97522, #23684, #57068, #52172, #85630, #27424, #76986, #92635, #19867, #43033, #101274, #75922, #59225, #60302, #92100, #84559, #10123, #59759, #3100, #10642, #69443, #18793, #76444, #36045, #68380, #53253, #93175, #34971, #2023, #101791, #51100, #93713, #42488, #84017, #1482, #68917, #67834, #26885, #100723, #19343, #28475, #34447, #85086, #102325, #51640, #27959, #43559, #11704, #3640, #36576, #60822, #61353, #52702, #2554, #94248, #35500, #11171, #44639, #44097, #67316, #77526, #20408, #9577, #75383, #100198, #26363, #18242, #20933, #21436, #61894, #86699, #37100, #104436, #38158, #94790, #46221, #80160, #64014, #96892, #71017, #104985, #95306 ),
 .UNSPECIFIED., .F., .F.,
 ( 4, 2, 2, 1, 1, 1, 2, 2, 2, 1, 1, 1, 1, 2, 2, 2, 2, 1, 1, 1, 2, 2, 1, 2, 2, 1, 1, 1, 2, 2, 1, 2, 2, 1, 1, 1, 1, 2, 2, 1, 2, 2, 2, 1, 1, 2, 2, 1, 2, 2, 2, 1, 1, 2, 2, 2, 2, 2, 2, 4 ),
 ( 0.000000000000000000, 0.01569797913311701126, 0.02354696869967563139, 0.02747146348295482002, 0.02943371087459440219, 0.03041483457041407878, 0.03090539641832402984, 0.03139595826623398089, 0.04709393739935408690, 0.05494292696591414338, 0.05886742174919416121, 0.06082966914083415971, 0.06181079283665415897, 0.06230135468456415859, 0.06279191653247415128, 0.09418787479871693069, 0.1098858539318383204, 0.1177348434983990361, 0.1216593382816793245, 0.1236215856733193647, 0.1246027093691394749, 0.1250932712170494676, 0.1255838330649594325, 0.1569797913311997695, 0.1726777704643198963, 0.1805267600308799736, 0.1844512548141599984, 0.1864135022058000801, 0.1873946259016200655, 0.1878851877495300027, 0.1883757495974398843, 0.2197717078636771959, 0.2354696869967959350, 0.2433186765633552073, 0.2472431713466348435, 0.2492054187382747588, 0.2496959805861847237, 0.2499412615101397617, 0.2501865424340947719, 0.2511676661299149793, 0.3139595826624118069, 0.3453555409286603317, 0.3610535200617845941, 0.3689025096283466421, 0.3728270044116277493, 0.3747892518032683307, 0.3757703754990885936, 0.3767514991949088565, 0.4081474574611569928, 0.4238454365942810331, 0.4316944261608430811, 0.4356189209441241328, 0.4366000446399443957, 0.4370906064878545272, 0.4375811683357646587, 0.4395434157274052400, 0.4709393739936550416, 0.4866373531267799146, 0.4944863426933423511, 0.5023353322599047877 ),
 .UNSPECIFIED. ) ;
#56655=CARTESIAN_POINT ( 'NONE',  ( -22.17399802466769287, -27.13132360212460981, 37.38406957163105915 ) ) ;
#56680=CARTESIAN_POINT ( 'NONE',  ( -112.0851447084041439, -60.00000000000000000, 178.2367466408115888 ) ) ;
#56688=CARTESIAN_POINT ( 'NONE',  ( -85.50314036829099962, -25.31086881602239913, 172.5804574615907541 ) ) ;
#56689=ORIENTED_EDGE ( 'NONE', *, *, #99839, .T. ) ;
#56700=CARTESIAN_POINT ( 'NONE',  ( 114.5100518737696689, -60.00000000000002132, 177.0882855716755557 ) ) ;
#56701=CARTESIAN_POINT ( 'NONE',  ( -108.0662369917864680, -29.99999999999997513, 149.4678941581608740 ) ) ;
#56702=CARTESIAN_POINT ( 'NONE',  ( -61.92732175817126716, -56.86970651190488724, 86.14273502844355335 ) ) ;
#56705=CARTESIAN_POINT ( 'NONE',  ( 103.1163125918749870, -59.99999999997518785, 203.2865156566705025 ) ) ;
#56707=ORIENTED_EDGE ( 'NONE', *, *, #88264, .F. ) ;
#56717=CARTESIAN_POINT ( 'NONE',  ( -101.6271150938965633, -59.99999999999997868, 201.3150328502970581 ) ) ;
#56726=CARTESIAN_POINT ( 'NONE',  ( 90.21675587111627692, -60.00000000000002132, 56.33244548193629697 ) ) ;
#56727=CARTESIAN_POINT ( 'NONE',  ( -31.50654607522282546, -25.60952003222888251, 31.14771393841350644 ) ) ;
#56731=CARTESIAN_POINT ( 'NONE',  ( 39.66000813785471735, -49.88695016216475864, 40.68345913021443039 ) ) ;
#56735=CARTESIAN_POINT ( 'NONE',  ( -73.92149184568339138, -38.32661406644628244, 159.6910106498240225 ) ) ;
#56737=CARTESIAN_POINT ( 'NONE',  ( 2.499999999999999556, -8.980730705452300455, 18.56355459479395620 ) ) ;
#56744=CARTESIAN_POINT ( 'NONE',  ( 100.6605546286570529, -60.00000000000000711, 84.90741128258979131 ) ) ;
#56747=CARTESIAN_POINT ( 'NONE',  ( -2.499999999999999556, -11.82939293535852343, 20.68570066208713243 ) ) ;
#56750=CARTESIAN_POINT ( 'NONE',  ( -99.54366155252257897, -30.00000000000000711, 187.3415679194916947 ) ) ;
#56767=CARTESIAN_POINT ( 'NONE',  ( 80.89341655852713586, -39.49760101440538307, 151.8480467892282775 ) ) ;
#56778=CARTESIAN_POINT ( 'NONE',  ( -21.50832034731008591, -57.67247026516260178, 42.43288772392129715 ) ) ;
#56782=FACE_OUTER_BOUND ( 'NONE', #103559, .T. ) ;
#56783=CIRCLE ( 'NONE', #10284, 2.000000000000001776 ) ;
#56788=CARTESIAN_POINT ( 'NONE',  ( -10.93314270704077629, -14.00130306865723817, 31.84631742024726009 ) ) ;
#56800=CARTESIAN_POINT ( 'NONE',  ( 43.65977048856617415, -34.03584407960176605, -37.07728933806833993 ) ) ;
#56808=CARTESIAN_POINT ( 'NONE',  ( 106.5779991752715148, -57.65217259572543895, 200.4557265301127984 ) ) ;
#56814=CARTESIAN_POINT ( 'NONE',  ( -75.32987886060202243, -60.00000000000000711, 183.4819721636450254 ) ) ;
#56816=DIRECTION ( 'NONE',  ( 0.000000000000000000, -1.000000000000000000, 0.000000000000000000 ) ) ;
#56820=CARTESIAN_POINT ( 'NONE',  ( -86.31808703902099467, -21.06115829967098918, 180.2389313303544895 ) ) ;
#56828=CARTESIAN_POINT ( 'NONE',  ( -83.13229060262131043, -37.80927313738316542, -3.002860636706784270 ) ) ;
#56833=CARTESIAN_POINT ( 'NONE',  ( -4.453875240773214728, -1.734723475976807094E-15, -16.57301948837565675 ) ) ;
#56836=CARTESIAN_POINT ( 'NONE',  ( -68.53940498225642841, -14.21045842199433729, -27.47940008941059276 ) ) ;
#56837=CARTESIAN_POINT ( 'NONE',  ( -80.17676966763509938, -18.67864944542718675, 127.0877505495672466 ) ) ;
#56840=CARTESIAN_POINT ( 'NONE',  ( 90.12561416859028895, -57.66693923673333444, -22.18623277742999989 ) ) ;
#56858=CARTESIAN_POINT ( 'NONE',  ( -8.310099524471651122, -29.99999999999994316, 36.98670313214555705 ) ) ;
#56859=CARTESIAN_POINT ( 'NONE',  ( 27.61403203557017250, -18.62762456134801070, 28.73031301232119716 ) ) ;
#56871=CARTESIAN_POINT ( 'NONE',  ( 65.88819888065104635, -59.99999999999998579, -33.92666894943724287 ) ) ;
#56874=CARTESIAN_POINT ( 'NONE',  ( 76.76915258873057724, -30.00000000000000711, -16.81647129862127699 ) ) ;
#56894=CARTESIAN_POINT ( 'NONE',  ( -71.97080448170594025, -59.99999999999997158, 122.5097884546718490 ) ) ;
#56895=CARTESIAN_POINT ( 'NONE',  ( 67.15832716194654495, -22.10445124349199020, 83.33801890902627463 ) ) ;
#56903=CARTESIAN_POINT ( 'NONE',  ( -2.836400373815510800, -57.67120205560058110, -44.61166178099613688 ) ) ;
#56920=CARTESIAN_POINT ( 'NONE',  ( 2.377971153322278042E-07, -60.00000000000000000, 39.63907915656436387 ) ) ;
#56921=CARTESIAN_POINT ( 'NONE',  ( -98.87062525871608898, -29.99999999999999289, 189.1229995020886179 ) ) ;
#56923=CARTESIAN_POINT ( 'NONE',  ( 45.36739251505076709, -57.68277139381120122, 65.96562024646243572 ) ) ;
#56933=CARTESIAN_POINT ( 'NONE',  ( -8.458412064297640143, -60.00000000000000000, 39.63599595626720884 ) ) ;
#56936=CARTESIAN_POINT ( 'NONE',  ( -87.09125453590827703, -35.39906969241756229, 188.3565598345231251 ) ) ;
#56940=CARTESIAN_POINT ( 'NONE',  ( -5.993894117748983952, -22.06774329507786447, 27.55811915394870226 ) ) ;
#56955=CARTESIAN_POINT ( 'NONE',  ( 72.91237123256428276, -60.00000000000000000, 161.6570857422749157 ) ) ;
#56978=CARTESIAN_POINT ( 'NONE',  ( -57.54921171551777093, -59.99999999998048139, 100.4542084673178408 ) ) ;
#56981=CARTESIAN_POINT ( 'NONE',  ( 78.09062726087394424, -59.99999999999997158, 193.0367330576344784 ) ) ;
#56982=CARTESIAN_POINT ( 'NONE',  ( -114.0148073962512854, -59.99999999999994316, 183.4850465800912218 ) ) ;
#56983=CARTESIAN_POINT ( 'NONE',  ( 15.83979721888547409, -49.91555666069991304, 32.40126087659623977 ) ) ;
#56984=CARTESIAN_POINT ( 'NONE',  ( 101.2009270926939450, -38.00000000000001421, 187.7194746866334185 ) ) ;
#56986=CARTESIAN_POINT ( 'NONE',  ( -46.21137058018805277, -25.69989330234890801, 41.24333236953626169 ) ) ;
#57001=CARTESIAN_POINT ( 'NONE',  ( 106.8088085084784780, -30.00000000000934719, 192.1296079279642584 ) ) ;
#57006=CARTESIAN_POINT ( 'NONE',  ( 97.88916531341952521, -30.00000000000000000, 136.7528328087380203 ) ) ;
#57020=CARTESIAN_POINT ( 'NONE',  ( 81.85842773695857488, -38.84088539656383432, 195.7169493522233950 ) ) ;
#57033=DIRECTION ( 'NONE',  ( 0.000000000000000000, 0.000000000000000000, 1.000000000000000000 ) ) ;
#57038=CARTESIAN_POINT ( 'NONE',  ( 32.89005191666632300, -34.30586786915193187, 42.46426960025681296 ) ) ;
#57042=CARTESIAN_POINT ( 'NONE',  ( 83.81614971311275042, -53.76474988997830451, 188.4634654509657707 ) ) ;
#57046=CARTESIAN_POINT ( 'NONE',  ( 90.98197251250333295, -57.66404948542993480, -20.95280514685850193 ) ) ;
#57052=CARTESIAN_POINT ( 'NONE',  ( -81.36109053512349476, -30.00000000000000711, -1.390147020584881155 ) ) ;
#57066=CARTESIAN_POINT ( 'NONE',  ( -10.58321096220334034, -23.34997317828527841, -30.52089866259334272 ) ) ;
#57068=CARTESIAN_POINT ( 'NONE',  ( 65.16637633022084231, -29.76141079654699695, -22.99752254794697137 ) ) ;
#57073=CARTESIAN_POINT ( 'NONE',  ( -35.05577973701957717, -23.33692852230415582, -31.27659717426585573 ) ) ;
#57075=CARTESIAN_POINT ( 'NONE',  ( -25.26744833228682197, -34.58977355993737746, -31.36978027168452954 ) ) ;
#57081=VECTOR ( 'NONE', #31303, 1000.000000000000000 ) ;
#57084=CARTESIAN_POINT ( 'NONE',  ( -85.63645619683279619, -59.99999999999998579, -24.02817151352510194 ) ) ;
#57088=CARTESIAN_POINT ( 'NONE',  ( 99.94366276826657725, -60.30227360360919420, 195.8446303873824945 ) ) ;
#57092=EDGE_LOOP ( 'NONE', ( #78170, #29251, #55513, #2349, #17537, #73550 ) ) ;
#57101=CARTESIAN_POINT ( 'NONE',  ( 0.000000000000000000, -30.00000000000000000, 0.000000000000000000 ) ) ;
#57103=CARTESIAN_POINT ( 'NONE',  ( -21.50832034731008591, -57.67247026516260178, 42.43288772392129715 ) ) ;
#57108=CARTESIAN_POINT ( 'NONE',  ( -79.45587154498480231, -59.99999999999991473, -31.00068500363164858 ) ) ;
#57111=CARTESIAN_POINT ( 'NONE',  ( -51.66175631953248626, -46.44323033348981511, 56.12883151261869585 ) ) ;
#57114=CARTESIAN_POINT ( 'NONE',  ( -100.9488071816703325, -60.26389219641809092, 195.1823302269569638 ) ) ;
#57118=CARTESIAN_POINT ( 'NONE',  ( 101.4909721992553386, -38.35592705684496195, 96.87947274763887151 ) ) ;
#57127=CARTESIAN_POINT ( 'NONE',  ( 82.59143751758651320, -29.99999999999999289, 149.9729633368418149 ) ) ;
#57134=CARTESIAN_POINT ( 'NONE',  ( 50.59493527809745927, -22.19395423099893350, 45.92767238662714391 ) ) ;
#57139=CARTESIAN_POINT ( 'NONE',  ( -108.0453605404376418, -38.35628879702573357, 138.1634217362548895 ) ) ;
#57142=CARTESIAN_POINT ( 'NONE',  ( 90.86190182423041506, -38.35175838285157113, 20.64935856576204642 ) ) ;
#57145=CARTESIAN_POINT ( 'NONE',  ( 97.60711786217987651, -45.28277154639692270, 115.8989380571673138 ) ) ;
#57150=CARTESIAN_POINT ( 'NONE',  ( 76.44766553792378261, -60.00000000000000711, 188.7013745601435915 ) ) ;
#57154=CARTESIAN_POINT ( 'NONE',  ( 55.70686534075314000, -39.49626118740381031, 61.84722421453820829 ) ) ;
#57160=CARTESIAN_POINT ( 'NONE',  ( -89.39007834610079328, -38.38716907517502364, -17.33792631335736800 ) ) ;
#57172=CARTESIAN_POINT ( 'NONE',  ( 84.93122466964305772, -28.90423046881255686, 171.9484601080571338 ) ) ;
#57184=CARTESIAN_POINT ( 'NONE',  ( -4.959378720893033332, -18.58292471749708952, 35.08865701613389376 ) ) ;
#57206=CARTESIAN_POINT ( 'NONE',  ( -100.9029158711696255, -59.99999999999999289, 86.33068100717986226 ) ) ;
#57213=CARTESIAN_POINT ( 'NONE',  ( -86.13910310123007719, -18.34493521033569863, 167.7294979905272498 ) ) ;
#57228=CARTESIAN_POINT ( 'NONE',  ( 106.6793784964389289, -14.21045842199433729, 163.7934217252150972 ) ) ;
#57230=CARTESIAN_POINT ( 'NONE',  ( -113.0839934364197887, -60.00000000000005684, 149.3435297534686299 ) ) ;
#57231=CARTESIAN_POINT ( 'NONE',  ( -60.41731799762936816, -53.39197530348098297, 80.04476055597704942 ) ) ;
#57234=CARTESIAN_POINT ( 'NONE',  ( 94.21046238432340658, -60.00000000000971312, 11.80878925958715087 ) ) ;
#57236=CARTESIAN_POINT ( 'NONE',  ( 2.053817364943875123, -60.35891754953962618, 33.94675380999842673 ) ) ;
#57243=CARTESIAN_POINT ( 'NONE',  ( -112.1314382224425401, -60.00000000000002842, 166.9117109934064160 ) ) ;
#57254=CARTESIAN_POINT ( 'NONE',  ( 93.00819039107329900, -59.99999999999998579, 74.24814202458328793 ) ) ;
#57255=CARTESIAN_POINT ( 'NONE',  ( -32.62005641966797498, -46.43469510831215530, 35.44769554474900275 ) ) ;
#57257=CARTESIAN_POINT ( 'NONE',  ( 40.90383831102949586, -56.79723033808241439, 43.40186584424645133 ) ) ;
#57261=CARTESIAN_POINT ( 'NONE',  ( -83.78472431295821821, -38.77414610831009867, 197.6093069242124614 ) ) ;
#57273=CARTESIAN_POINT ( 'NONE',  ( 102.9377691848878840, -60.00000000000000000, 98.21790666211499854 ) ) ;
#57279=CARTESIAN_POINT ( 'NONE',  ( -96.99816414976265833, -29.99999999999981171, 191.0865392925242077 ) ) ;
#57284=CARTESIAN_POINT ( 'NONE',  ( -2.499999999999996447, -30.00000000000000000, -14.79019945774903988 ) ) ;
#57295=CARTESIAN_POINT ( 'NONE',  ( 80.21638703355559130, -49.90724840867629553, 160.3600109673918155 ) ) ;
#57317=CARTESIAN_POINT ( 'NONE',  ( 29.52976757919392270, -32.13639089429810980, 40.30885829581517044 ) ) ;
#57329=ORIENTED_EDGE ( 'NONE', *, *, #36957, .F. ) ;
#57331=CARTESIAN_POINT ( 'NONE',  ( 108.1233463498552680, -57.67127209427924583, 117.1904254369292318 ) ) ;
#57336=CARTESIAN_POINT ( 'NONE',  ( -74.55215148334558251, -59.99999999999999289, 177.5930982106680744 ) ) ;
#57341=CARTESIAN_POINT ( 'NONE',  ( -85.09751082350868501, -42.94669665112929380, 186.0240982620516093 ) ) ;
#57350=CARTESIAN_POINT ( 'NONE',  ( -85.70554460909363570, -52.72876096884451869, -4.541171915920864777 ) ) ;
#57358=CARTESIAN_POINT ( 'NONE',  ( 10.45706415777664411, -1.734723475976807094E-15, 13.60704923275374156 ) ) ;
#57361=CARTESIAN_POINT ( 'NONE',  ( -25.62895382379538489, -60.00000000000000711, -43.76007060795225101 ) ) ;
#57362=CARTESIAN_POINT ( 'NONE',  ( -78.10409042525387235, -36.02680010123066268, 131.9807425273284025 ) ) ;
#57364=CARTESIAN_POINT ( 'NONE',  ( 29.53284356080077444, -60.00000000000004974, 45.26708560465603171 ) ) ;
#57366=CARTESIAN_POINT ( 'NONE',  ( 93.92944981285859285, -57.67333411593723014, 17.34817390334868392 ) ) ;
#57371=ORIENTED_EDGE ( 'NONE', *, *, #5071, .F. ) ;
#57390=CARTESIAN_POINT ( 'NONE',  ( -1.309564884278361513E-05, -14.21045842199434972, 34.36840973699906243 ) ) ;
#57391=CARTESIAN_POINT ( 'NONE',  ( 31.19770315994506404, -42.95952005011717034, 34.19569303745028321 ) ) ;
#57398=CARTESIAN_POINT ( 'NONE',  ( 80.00000000000000000, -38.00000000001091394, -21.09707704303352926 ) ) ;
#57402=CARTESIAN_POINT ( 'NONE',  ( 8.180595432802771683, -59.99999999999999289, -42.48548993661778184 ) ) ;
#57424=CARTESIAN_POINT ( 'NONE',  ( 69.94764612343819010, -18.63634428197197579, 89.84345188368395441 ) ) ;
#57450=CARTESIAN_POINT ( 'NONE',  ( 8.700108653991776464, -60.00000000000000000, 39.63767202453095706 ) ) ;
#57452=CARTESIAN_POINT ( 'NONE',  ( -98.22775549665112749, -30.00000000000000000, 190.2606745111846180 ) ) ;
#57456=CARTESIAN_POINT ( 'NONE',  ( 73.84627813901309423, -57.61934647735279924, 186.2875162611425992 ) ) ;
#57459=CARTESIAN_POINT ( 'NONE',  ( 14.75721006082208575, -24.00293099030797705, -38.53146564288101672 ) ) ;
#57463=CARTESIAN_POINT ( 'NONE',  ( -8.401912187080752048, -60.00000000000000711, 39.63564103648013059 ) ) ;
#57466=CARTESIAN_POINT ( 'NONE',  ( -86.53945512387777228, -17.00671387159180625, 184.4939234780275967 ) ) ;
#57471=CARTESIAN_POINT ( 'NONE',  ( -10.41106923231795101, -53.40263473211271616, 32.80381487082638614 ) ) ;
#57473=CARTESIAN_POINT ( 'NONE',  ( -103.5376772722346459, -60.00000000000000711, 191.8212684384977536 ) ) ;
#57484=CARTESIAN_POINT ( 'NONE',  ( 106.9110190588319540, -14.21045842199441367, 176.0591306608180844 ) ) ;
#57496=EDGE_CURVE ( 'NONE', #93532, #88504, #56156, .T. ) ;
#57506=CARTESIAN_POINT ( 'NONE',  ( -71.71355155960320360, -60.00000000004398970, 173.0691681726769957 ) ) ;
#57509=CARTESIAN_POINT ( 'NONE',  ( 91.91289437223223047, -60.00000000000001421, 16.01571062708334381 ) ) ;
#57510=CARTESIAN_POINT ( 'NONE',  ( -104.0091953780157752, -14.21045842199432663, 192.0632730704776066 ) ) ;
#57511=CARTESIAN_POINT ( 'NONE',  ( 14.77419618374876897, -53.39659763945549997, 32.92159578500137940 ) ) ;
#57515=CARTESIAN_POINT ( 'NONE',  ( -39.39627231840285759, -22.22833841577496727, 34.41038875012783649 ) ) ;
#57527=CARTESIAN_POINT ( 'NONE',  ( 75.98997121514811681, -30.00000000000000711, -17.37669743398828359 ) ) ;
#57531=CARTESIAN_POINT ( 'NONE',  ( 94.94366555557748200, -30.00000000000000711, 117.6622010833369245 ) ) ;
#57546=CARTESIAN_POINT ( 'NONE',  ( 79.86200412043599783, -38.77158211078923955, 192.7350020035291038 ) ) ;
#57559=FILL_AREA_STYLE_COLOUR ( '', #80021 ) ;
#57567=CARTESIAN_POINT ( 'NONE',  ( 84.00255077718880159, -61.04110459592344995, 192.3126038394468367 ) ) ;
#57573=CARTESIAN_POINT ( 'NONE',  ( 93.24448322355969765, -57.65503295969547537, -16.59265381772082648 ) ) ;
#57578=CARTESIAN_POINT ( 'NONE',  ( -80.76340928301335964, -29.99999999999999645, 14.59015454481636631 ) ) ;
#57579=CARTESIAN_POINT ( 'NONE',  ( -73.67282519167521571, -37.99999999999996447, 114.1319439230774293 ) ) ;
#57595=CARTESIAN_POINT ( 'NONE',  ( -70.63365275292957790, -30.00000000000000355, -20.40377125985679285 ) ) ;
#57598=CARTESIAN_POINT ( 'NONE',  ( -69.96807924604867424, -47.40884888655846652, -24.11331608286603867 ) ) ;
#57606=CARTESIAN_POINT ( 'NONE',  ( -33.51294852578469374, -60.00000000000000711, -40.49430134959939664 ) ) ;
#57610=CARTESIAN_POINT ( 'NONE',  ( 96.24277997628448134, -45.27105860737465548, 194.1195206907109707 ) ) ;
#57621=VERTEX_POINT ( 'NONE', #916 ) ;
#57626=CARTESIAN_POINT ( 'NONE',  ( -23.49283269198559765, -57.67355083020559192, 42.82390242447587525 ) ) ;
#57632=CARTESIAN_POINT ( 'NONE',  ( -67.59740049799954420, -60.00000000000004263, -35.88590100950167994 ) ) ;
#57633=CARTESIAN_POINT ( 'NONE',  ( -24.85253352225967660, -29.99999999999996092, 38.32597638696945097 ) ) ;
#57634=CARTESIAN_POINT ( 'NONE',  ( -53.14642949933918459, -32.57121755472948621, 53.87505941010853405 ) ) ;
#57640=CARTESIAN_POINT ( 'NONE',  ( -101.5070894931627237, -60.23655731454778106, 194.7038192617161201 ) ) ;
#57644=ORIENTED_EDGE ( 'NONE', *, *, #99839, .F. ) ;
#57647=CARTESIAN_POINT ( 'NONE',  ( 73.82277771826251467, -38.32584844511357147, 158.7404017193271955 ) ) ;
#57653=CARTESIAN_POINT ( 'NONE',  ( 85.23574709202168265, -29.99999999999999645, 172.5112148116256208 ) ) ;
#57659=CARTESIAN_POINT ( 'NONE',  ( 50.14541849784438909, -42.97498551929375310, 52.14416430124198598 ) ) ;
#57663=CARTESIAN_POINT ( 'NONE',  ( -95.04834772930165343, -38.35492584456250142, 58.17196757228544612 ) ) ;
#57667=CARTESIAN_POINT ( 'NONE',  ( 93.01387217800777307, -38.35490714704352655, 43.55336315142127290 ) ) ;
#57669=CARTESIAN_POINT ( 'NONE',  ( 98.39111451231792671, -45.28270231285164016, 120.6799170848443907 ) ) ;
#57674=CARTESIAN_POINT ( 'NONE',  ( 76.37984825064704353, -59.99999999999997868, 188.4578851984081780 ) ) ;
#57679=CARTESIAN_POINT ( 'NONE',  ( 61.75317836559133866, -42.96044902961888567, 78.62615862502077846 ) ) ;
#57685=CARTESIAN_POINT ( 'NONE',  ( -77.16460649846582953, -38.35595679982836259, -28.07778984955893264 ) ) ;
#57693=CARTESIAN_POINT ( 'NONE',  ( 86.00659031669722765, -21.65052574614072256, 173.2934799618346062 ) ) ;
#57708=CARTESIAN_POINT ( 'NONE',  ( -17.36216298162189275, -24.06244604014566590, 36.30748115442920465 ) ) ;
#57727=CARTESIAN_POINT ( 'NONE',  ( 9.442771828977239323, -34.58963171957248051, -32.44484452317096412 ) ) ;
#57734=CARTESIAN_POINT ( 'NONE',  ( -96.89880926707883191, -60.00000000000000000, 62.01847588090020480 ) ) ;
#57741=CARTESIAN_POINT ( 'NONE',  ( -84.47455154433566804, -32.43567151322172748, 172.8640213309939782 ) ) ;
#57759=CARTESIAN_POINT ( 'NONE',  ( 108.5047413589249032, -30.00000000000003197, 153.5997199437166785 ) ) ;
#57760=CARTESIAN_POINT ( 'NONE',  ( -105.8556346142475064, -14.21045842199439946, 186.2197870760574290 ) ) ;
#57761=CARTESIAN_POINT ( 'NONE',  ( -60.62598618508234694, -49.91629112966251824, 78.91895544919526628 ) ) ;
#57764=CARTESIAN_POINT ( 'NONE',  ( 95.01407385562683316, -60.00000000000486011, -10.13917562263175931 ) ) ;
#57766=CARTESIAN_POINT ( 'NONE',  ( 6.057315617798289864, -32.51038067482491556, 29.29837158373775807 ) ) ;
#57767=CARTESIAN_POINT ( 'NONE',  ( -102.4764807934955684, -52.71020093064566225, 139.6445780999559076 ) ) ;
#57775=CARTESIAN_POINT ( 'NONE',  ( -38.57579099119070776, -59.99999999999998579, 50.19459341522732387 ) ) ;
#57786=CARTESIAN_POINT ( 'NONE',  ( 86.85824047554997662, -59.99999999999997868, -10.30000423349464000 ) ) ;
#57787=CARTESIAN_POINT ( 'NONE',  ( -32.25315245376670248, -39.49381076584415950, 34.00953951823751709 ) ) ;
#57790=CARTESIAN_POINT ( 'NONE',  ( 42.69170054815374726, -56.79417449340447632, 45.32995381252002431 ) ) ;
#57796=CARTESIAN_POINT ( 'NONE',  ( -78.43232732503568627, -38.62599759898719753, 189.4934868374475911 ) ) ;
#57798=CARTESIAN_POINT ( 'NONE',  ( 2.499999999999998224, -15.46059144880916669, 23.70576633280851553 ) ) ;
#57809=CARTESIAN_POINT ( 'NONE',  ( 107.5845383886140070, -60.00000000000002132, 126.3434892167558417 ) ) ;
#57814=CARTESIAN_POINT ( 'NONE',  ( -88.51094613808753309, -30.00000000000004619, 187.8829266376722558 ) ) ;
#57826=CARTESIAN_POINT ( 'NONE',  ( 83.18608112039279945, -22.15294338469834301, 146.6214932445938075 ) ) ;
#57842=CARTESIAN_POINT ( 'NONE',  ( 86.84319104226476327, -46.45793329604330069, 190.7102553128401894 ) ) ;
#57846=CARTESIAN_POINT ( 'NONE',  ( 36.30372750213987842, -36.17305495503135404, 45.48833120993651136 ) ) ;
#57865=CARTESIAN_POINT ( 'NONE',  ( 107.4062233239980628, -57.67121751121231910, 112.8259166854166011 ) ) ;
#57871=CARTESIAN_POINT ( 'NONE',  ( -79.13069157080136051, -59.99999999999999289, 194.8111473548646586 ) ) ;
#57877=CARTESIAN_POINT ( 'NONE',  ( -86.39708987185247224, -17.44928839871576542, 178.9058496263539837 ) ) ;
#57885=CARTESIAN_POINT ( 'NONE',  ( -87.00156809400746738, -60.21405852097385036, -8.689177619207773873 ) ) ;
#57893=CARTESIAN_POINT ( 'NONE',  ( -8.569529079657698389, -1.734723475976807094E-15, -14.86825985027703290 ) ) ;
#57895=CARTESIAN_POINT ( 'NONE',  ( 8.180134260905338905, -14.21045842199436926, -37.25106736021741227 ) ) ;
#57896=CARTESIAN_POINT ( 'NONE',  ( -79.59015944166391421, -29.08934217562258695, 133.2666643165789822 ) ) ;
#57898=CARTESIAN_POINT ( 'NONE',  ( 71.69540001792421435, -59.99999999999999289, 172.8810247122642352 ) ) ;
#57900=CARTESIAN_POINT ( 'NONE',  ( 110.2837989784263044, -57.66912168954863205, 195.5935479797663277 ) ) ;
#57922=CARTESIAN_POINT ( 'NONE',  ( 30.84614831813113511, -36.01525104246629638, 32.80693974661438261 ) ) ;
#57936=CARTESIAN_POINT ( 'NONE',  ( 90.93490407631915673, -60.00000000000000711, -17.09726446340970440 ) ) ;
#57949=CARTESIAN_POINT ( 'NONE',  ( 85.73991738122207096, -52.74049725067960281, -5.625651811223429277 ) ) ;
#57953=EDGE_LOOP ( 'NONE', ( #33493, #29604, #77706, #48700 ) ) ;
#57957=CARTESIAN_POINT ( 'NONE',  ( -86.22319347886272567, -38.62792923045453364, 199.1968256833580995 ) ) ;
#57963=CARTESIAN_POINT ( 'NONE',  ( 6.026974479199131350E-05, -59.99999999999998579, 33.88964995960238014 ) ) ;
#57965=CARTESIAN_POINT ( 'NONE',  ( 70.47143424281389912, -46.43366363250593309, 107.5507350962775490 ) ) ;
#57971=CARTESIAN_POINT ( 'NONE',  ( -99.13865059541491576, -57.67127950436278638, 63.61738387431689290 ) ) ;
#57982=B_SPLINE_CURVE_WITH_KNOTS ( 'NONE', 3,
 ( #42956, #26808, #9500, #25754, #59681, #18710, #11092, #76908, #35970, #17093, #41878, #74767, #4095, #79037, #79564, #37023, #5158, #86630, #62870, #94717, #102249, #103838, #95758, #69892, #70426, #54742, #21897, #4629, #21367, #77978, #87675, #45624, #12694, #78498 ),
 .UNSPECIFIED., .F., .F.,
 ( 4, 2, 2, 2, 2, 2, 2, 2, 2, 2, 2, 2, 2, 2, 2, 2, 4 ),
 ( 0.000000000000000000, 0.03125000000000000000, 0.06250000000000000000, 0.09375000000000000000, 0.1250000000000000000, 0.1562500000000000000, 0.1875000000000000000, 0.2187500000000000000, 0.2500000000000000000, 0.2812500000000000000, 0.3125000000000000000, 0.3437500000000000000, 0.3750000000000000000, 0.4062500000000000000, 0.4375000000000000000, 0.4687500000000000000, 0.5000000000000000000 ),
 .UNSPECIFIED. ) ;
#57994=CARTESIAN_POINT ( 'NONE',  ( -91.21773797973978049, -30.00000000000000711, 190.5815255630674585 ) ) ;
#57996=CARTESIAN_POINT ( 'NONE',  ( 70.42594083886010026, -57.68248469520420230, 157.4904543252067981 ) ) ;
#57999=CARTESIAN_POINT ( 'NONE',  ( 19.29301913843075411, -25.57889320560503066, -38.49290569165957976 ) ) ;
#58002=CARTESIAN_POINT ( 'NONE',  ( -47.20193715881740815, -60.00000000000001421, 65.23073768148172746 ) ) ;
#58006=CARTESIAN_POINT ( 'NONE',  ( -87.01762278567609599, -46.44878082088867188, 190.9316993270498699 ) ) ;
#58010=CARTESIAN_POINT ( 'NONE',  ( -8.339494512690995620, -60.36589398885404023, 33.94454140269643005 ) ) ;
#58024=CARTESIAN_POINT ( 'NONE',  ( 105.3887446370168135, -14.21045842199438347, 188.2131443117102663 ) ) ;
#58047=CARTESIAN_POINT ( 'NONE',  ( -74.29828176229183612, -59.99999999998045297, 190.2516943755762782 ) ) ;
#58050=CARTESIAN_POINT ( 'NONE',  ( 111.9397786006664148, -59.99999999999998579, 163.4467576686174084 ) ) ;
#58051=CARTESIAN_POINT ( 'NONE',  ( -99.17463707058834643, -30.00000000000003908, 199.4944348318372818 ) ) ;
#58052=CARTESIAN_POINT ( 'NONE',  ( 16.89471477245463404, -46.43465090273242879, 31.87823083279425873 ) ) ;
#58053=CARTESIAN_POINT ( 'NONE',  ( 83.27846995605888480, -37.99999999999998579, -8.029241552981964958 ) ) ;
#58056=CARTESIAN_POINT ( 'NONE',  ( -41.83504579204735307, -56.80130521720823111, 44.35147145462004659 ) ) ;
#58065=ORIENTED_EDGE ( 'NONE', *, *, #47430, .T. ) ;
#58068=CARTESIAN_POINT ( 'NONE',  ( 78.46489409920162927, -30.00000000000490630, 185.0055361782710861 ) ) ;
#58073=CARTESIAN_POINT ( 'NONE',  ( 81.06826635177107221, -29.99999999999999645, 22.19813494082483984 ) ) ;
#58091=CARTESIAN_POINT ( 'NONE',  ( 82.51873517505984523, -38.82767313688965061, 196.4555416342311673 ) ) ;
#58116=CARTESIAN_POINT ( 'NONE',  ( 84.46416041085834081, -53.81410151352770299, 189.8017141661123048 ) ) ;
#58119=CARTESIAN_POINT ( 'NONE',  ( 94.60687179076299458, -57.65605773701032888, -9.974991136142552506 ) ) ;
#58125=CARTESIAN_POINT ( 'NONE',  ( -81.41044234058053064, -29.99999999999999645, -9.983906976751161011 ) ) ;
#58137=CARTESIAN_POINT ( 'NONE',  ( -56.85792563227521157, -36.99373425697515216, -26.55165709400334606 ) ) ;
#58144=CARTESIAN_POINT ( 'NONE',  ( -56.83356558749228071, -28.80307005180548074, -26.02374799800344718 ) ) ;
#58155=CARTESIAN_POINT ( 'NONE',  ( -21.65591802733287707, -59.99999999999999289, -41.70210173751639360 ) ) ;
#58157=CARTESIAN_POINT ( 'NONE',  ( 68.38730731139169450, -37.97126955729439857, -23.07194479924394059 ) ) ;
#58159=CARTESIAN_POINT ( 'NONE',  ( 102.9234337200204976, -60.17135737299345521, 192.9571753945863861 ) ) ;
#58160=CARTESIAN_POINT ( 'NONE',  ( 16.15566081772431062, -23.35500082345586037, 27.97597666450196741 ) ) ;
#58161=CARTESIAN_POINT ( 'NONE',  ( -0.004771297262913525017, -57.67120202554433916, -44.61186700141271899 ) ) ;
#58174=CARTESIAN_POINT ( 'NONE',  ( -67.94141844175470624, -57.68152395592925785, 141.0744097219443347 ) ) ;
#58181=CARTESIAN_POINT ( 'NONE',  ( 16.35077622672217146, -14.21045842199431064, -36.83539407110947650 ) ) ;
#58182=CARTESIAN_POINT ( 'NONE',  ( -8.310099524471651122, -29.99999999999994316, 36.98670313214555705 ) ) ;
#58183=CARTESIAN_POINT ( 'NONE',  ( -49.07957144243162162, -53.36799748280911615, 53.76589609654883617 ) ) ;
#58188=CARTESIAN_POINT ( 'NONE',  ( -99.94755020072459217, -60.30543975612710739, 195.8429729570115114 ) ) ;
#58195=CARTESIAN_POINT ( 'NONE',  ( 82.47534791270491894, -38.83477010435220933, 196.4395726495995405 ) ) ;
#58200=CARTESIAN_POINT ( 'NONE',  ( 84.12545104255541162, -30.00000000000000000, 162.1202415754671051 ) ) ;
#58208=CARTESIAN_POINT ( 'NONE',  ( 51.55283957149192986, -49.90428648180873239, 57.17623228211761699 ) ) ;
#58212=CARTESIAN_POINT ( 'NONE',  ( -90.64891522596445839, -38.34438625522449939, 9.494094722409048615 ) ) ;
#58216=CARTESIAN_POINT ( 'NONE',  ( 90.86283834997398401, -38.35177504835404960, 20.66734224468696013 ) ) ;
#58218=CARTESIAN_POINT ( 'NONE',  ( 82.88655854197318718, -37.85212557438806869, 24.55487265319875334 ) ) ;
#58223=CARTESIAN_POINT ( 'NONE',  ( 74.86035044006985117, -59.99999999999997868, 180.1901903545331152 ) ) ;
#58226=CARTESIAN_POINT ( 'NONE',  ( 61.66760480045117987, -32.53592676977203979, 73.28662338893155948 ) ) ;
#58230=CARTESIAN_POINT ( 'NONE',  ( -76.64727008412683062, -30.00000000004703438, 171.7971487496357952 ) ) ;
#58241=CARTESIAN_POINT ( 'NONE',  ( 84.63126334808946183, -32.40349847066813993, 174.3450822652993395 ) ) ;
#58252=CARTESIAN_POINT ( 'NONE',  ( -27.75976893385707100, -28.74496449168539769, -38.27507236928394008 ) ) ;
#58256=CARTESIAN_POINT ( 'NONE',  ( 56.45566465188593241, -60.00000000000000000, 89.52844513896216938 ) ) ;
#58261=CARTESIAN_POINT ( 'NONE',  ( 26.80094985271070485, -20.15100958916939078, 31.71682355366501582 ) ) ;
#58263=CARTESIAN_POINT ( 'NONE',  ( -15.68130581768025245, -23.07453539438714074, 36.03336598945195846 ) ) ;
#58273=CARTESIAN_POINT ( 'NONE',  ( 31.56406999132591906, -34.58956455767763316, -30.69127153837264999 ) ) ;
#58284=CARTESIAN_POINT ( 'NONE',  ( -98.09986721704827062, -60.00000000000000000, 69.54344069125673400 ) ) ;
#58292=CARTESIAN_POINT ( 'NONE',  ( -81.23148066614986362, -56.98058829986878493, 180.4918934137440090 ) ) ;
#58303=( LENGTH_UNIT ( ) NAMED_UNIT ( * ) SI_UNIT ( .MILLI., .METRE. ) );
#58310=CARTESIAN_POINT ( 'NONE',  ( 106.9311160729171917, -14.21045842199435860, 169.9238089813113390 ) ) ;
#58311=CARTESIAN_POINT ( 'NONE',  ( -109.0466421874928074, -29.99999999999997513, 159.8085545269249224 ) ) ;
#58312=CARTESIAN_POINT ( 'NONE',  ( -58.77907907405603538, -56.86410614522492324, 77.19366601566905217 ) ) ;
#58315=CARTESIAN_POINT ( 'NONE',  ( 112.0607394184880548, -60.00000000003897327, 140.7617073482189767 ) ) ;
#58317=CARTESIAN_POINT ( 'NONE',  ( 8.196996272121577221, -42.95368992844134226, 31.04195210901052704 ) ) ;
#58318=CARTESIAN_POINT ( 'NONE',  ( -99.13522008394323848, -45.26542195737069108, 125.4529771320935225 ) ) ;
#58326=CARTESIAN_POINT ( 'NONE',  ( -62.97177311229369678, -60.00000000000002842, 110.5655362465914919 ) ) ;
#58330=CARTESIAN_POINT ( 'NONE',  ( 14.76969908563116540, 0.000000000000000000, -8.521411446762671815 ) ) ;
#58336=CARTESIAN_POINT ( 'NONE',  ( 85.46985710197711228, -60.00000000000000711, -15.19164742138506163 ) ) ;
#58337=CARTESIAN_POINT ( 'NONE',  ( -32.80042515103462364, -49.90467096888802701, 36.16953263397611096 ) ) ;
#58339=CARTESIAN_POINT ( 'NONE',  ( 46.35011507412374954, -53.35108316952277363, 49.29442306384134298 ) ) ;
#58346=CARTESIAN_POINT ( 'NONE',  ( -77.65106118960082426, -38.53234513354232860, 187.0520508371121764 ) ) ;
#58350=CARTESIAN_POINT ( 'NONE',  ( 19.81133971885708789, -59.99999999999996447, 34.40092749390601057 ) ) ;
#58358=CARTESIAN_POINT ( 'NONE',  ( 104.1736618930692515, -60.00000000000000000, 105.4628610393546353 ) ) ;
#58363=CARTESIAN_POINT ( 'NONE',  ( -101.0464925371120160, -30.00000000000000355, 176.9119907885118153 ) ) ;
#58377=CARTESIAN_POINT ( 'NONE',  ( 84.14305783358679491, -29.04061733210153662, 163.8439507599780995 ) ) ;
#58399=CARTESIAN_POINT ( 'NONE',  ( 86.74778042868597083, -20.65970481315351037, 185.3124080711632757 ) ) ;
#58416=DIRECTION ( 'NONE',  ( -0.000000000000000000, -1.000000000000000000, -0.000000000000000000 ) ) ;
#58418=CARTESIAN_POINT ( 'NONE',  ( 111.9393053685597295, -57.67107339064843785, 191.5175075271729099 ) ) ;
#58425=CARTESIAN_POINT ( 'NONE',  ( -75.76033734085729066, -60.00000000000000711, 185.8899872020949999 ) ) ;
#58431=CARTESIAN_POINT ( 'NONE',  ( -85.27549786776644680, -32.22529396608707941, 179.6151387925006873 ) ) ;
#58438=CARTESIAN_POINT ( 'NONE',  ( -86.47380749082138607, -60.23397837094964302, -12.64187964145606990 ) ) ;
#58448=CARTESIAN_POINT ( 'NONE',  ( -52.81151229832320126, -14.21045842199429643, -31.95502044027141153 ) ) ;
#58449=CARTESIAN_POINT ( 'NONE',  ( -76.97108689222071121, -29.08047201166412066, 121.1803976918724999 ) ) ;
#58451=CARTESIAN_POINT ( 'NONE',  ( 77.57360435794387854, -29.99999999999995026, 180.9683789367223596 ) ) ;
#58453=CARTESIAN_POINT ( 'NONE',  ( 94.62282354643079429, -57.66661055993814955, -3.516479676606508953 ) ) ;
#58475=CARTESIAN_POINT ( 'NONE',  ( 31.69331294291215784, -29.07918354051579257, 31.86078741099893108 ) ) ;
#58482=ORIENTED_EDGE ( 'NONE', *, *, #45141, .T. ) ;
#58486=CARTESIAN_POINT ( 'NONE',  ( -87.14767027655014431, -37.99999999998310329, 189.0874028505847662 ) ) ;
#58492=CARTESIAN_POINT ( 'NONE',  ( 90.07666725775354166, -59.99999999999997868, -18.70346304004552707 ) ) ;
#58506=CARTESIAN_POINT ( 'NONE',  ( 84.30730976911441132, -45.28743999684999011, -1.774643925835537317 ) ) ;
#58520=CARTESIAN_POINT ( 'NONE',  ( 77.56784472490384985, -22.13724272177843844, 118.4967285904078835 ) ) ;
#58525=CARTESIAN_POINT ( 'NONE',  ( -94.77678295284667342, -57.67204358354969429, 30.25255809810320429 ) ) ;
#58528=( GEOMETRIC_REPRESENTATION_CONTEXT ( 3 ) GLOBAL_UNCERTAINTY_ASSIGNED_CONTEXT ( ( #91562 ) ) GLOBAL_UNIT_ASSIGNED_CONTEXT ( ( #103295, #72502, #63379 ) ) REPRESENTATION_CONTEXT ( 'NONE', 'WORKASPACE' ) );
#58532=CARTESIAN_POINT ( 'NONE',  ( 102.6154386523218420, -37.84845496389469588, 165.6573751097436684 ) ) ;
#58548=CARTESIAN_POINT ( 'NONE',  ( 8.874007437334798354, -60.00000000000001421, 39.63896389924233432 ) ) ;
#58550=CARTESIAN_POINT ( 'NONE',  ( -96.91417471229229363, -30.00000000000000355, 191.1098736999540790 ) ) ;
#58555=CARTESIAN_POINT ( 'NONE',  ( 70.40112261783126257, -57.68249624625126870, 157.2928848866747842 ) ) ;
#58559=CARTESIAN_POINT ( 'NONE',  ( 8.146578490534659878, -22.18916675789439097, -38.54415778659916469 ) ) ;
#58562=CARTESIAN_POINT ( 'NONE',  ( -29.20644879193481813, -60.00000000000000000, 42.65854192317066662 ) ) ;
#58567=CARTESIAN_POINT ( 'NONE',  ( -86.58668466171424427, -20.72177639861540754, 184.1452794688869687 ) ) ;
#58570=CARTESIAN_POINT ( 'NONE',  ( -6.205792356335741999, -56.88414179012536209, 33.36022572332550595 ) ) ;
#58582=CARTESIAN_POINT ( 'NONE',  ( 114.5718218735923131, -60.00000000000004974, 174.9501719601325078 ) ) ;
#58583=CARTESIAN_POINT ( 'NONE',  ( -84.24555479967482086, -25.58375714794800970, 159.3068062033638626 ) ) ;
#58585=DIRECTION ( 'NONE',  ( 0.000000000000000000, 0.000000000000000000, -1.000000000000000000 ) ) ;
#58590=CARTESIAN_POINT ( 'NONE',  ( 45.71963875501239016, -29.99999999999998934, 56.30994126864623439 ) ) ;
#58602=CARTESIAN_POINT ( 'NONE',  ( 111.5016178170474888, -59.99999999999998579, 184.5246322086984208 ) ) ;
#58603=CARTESIAN_POINT ( 'NONE',  ( -77.40171858393368609, -14.21045842199445630, 153.6868182409262431 ) ) ;
#58604=CARTESIAN_POINT ( 'NONE',  ( 13.22559935364501627, -22.06780710830701864, 27.64041415630501319 ) ) ;
#58610=CARTESIAN_POINT ( 'NONE',  ( -41.39595481026245238, -18.78381775150863930, 34.98783307414403509 ) ) ;
#58621=DIRECTION ( 'NONE',  ( 1.000000000000000000, 0.000000000000000000, -8.673617379884035472E-17 ) ) ;
#58623=CARTESIAN_POINT ( 'NONE',  ( 77.27097837494086718, -30.00000000008570922, 177.5457258123725808 ) ) ;
#58629=CARTESIAN_POINT ( 'NONE',  ( 81.06585882963902634, -30.00000000000000000, 22.15552175282082814 ) ) ;
#58646=CARTESIAN_POINT ( 'NONE',  ( 77.32616938918349092, -38.49326352433806875, 185.8092111286713362 ) ) ;
#58668=CARTESIAN_POINT ( 'NONE',  ( 85.83414240384524874, -35.62221213960832955, 184.8240206695177221 ) ) ;
#58671=CARTESIAN_POINT ( 'NONE',  ( 94.62684802005594520, -57.66657240577455212, -3.586364576938546822 ) ) ;
#58674=CARTESIAN_POINT ( 'NONE',  ( -81.40333483022713779, -30.00000000000000711, -10.03578593830606813 ) ) ;
#58690=CARTESIAN_POINT ( 'NONE',  ( 68.62844179577130888, -29.94534991839561755, -21.42007394527319875 ) ) ;
#58700=CARTESIAN_POINT ( 'NONE',  ( -69.51878337118347417, -21.77025481454749212, -19.67902557026448918 ) ) ;
#58708=CARTESIAN_POINT ( 'NONE',  ( -1.666663072624755992, -29.99999999999999645, 28.88808002246651796 ) ) ;
#58709=CARTESIAN_POINT ( 'NONE',  ( -66.15993367293332028, -60.00000000000000711, -33.83992077223387440 ) ) ;
#58712=CARTESIAN_POINT ( 'NONE',  ( 99.36701900970518864, -37.82354045745693583, 191.5096613616152297 ) ) ;
#58713=CARTESIAN_POINT ( 'NONE',  ( 14.97375118833551788, -22.78136625548523497, 27.82250553508887236 ) ) ;
#58728=CARTESIAN_POINT ( 'NONE',  ( -33.87510863592373767, -57.69360311548409470, 48.02532427896534983 ) ) ;
#58734=CARTESIAN_POINT ( 'NONE',  ( -88.04114847129865495, -29.99999999999995026, -17.07571352811936194 ) ) ;
#58738=CARTESIAN_POINT ( 'NONE',  ( -49.01629296738340003, -56.83013498245147588, 54.79628526633861441 ) ) ;
#58747=CARTESIAN_POINT ( 'NONE',  ( 76.94667806338644311, -38.45205237156240941, 184.1492322625157954 ) ) ;
#58753=CARTESIAN_POINT ( 'NONE',  ( 87.87841627987471327, -30.00000000000000000, 186.4696136827627981 ) ) ;
#58759=CARTESIAN_POINT ( 'NONE',  ( 53.13899645154318563, -46.43671994497447741, 59.08478548976397349 ) ) ;
#58763=CARTESIAN_POINT ( 'NONE',  ( -93.96138925245962525, -38.35488083088926459, 50.68657296838828330 ) ) ;
#58766=CARTESIAN_POINT ( 'NONE',  ( 107.1090246246218385, -38.36360799944018396, 194.6594831697806001 ) ) ;
#58768=CARTESIAN_POINT ( 'NONE',  ( 85.46809269451053126, -37.84908238006404702, 49.13086642071656485 ) ) ;
#58773=CARTESIAN_POINT ( 'NONE',  ( 75.34722298054580847, -60.00000000000000000, 183.6044144055699405 ) ) ;
#58775=VECTOR ( 'NONE', #99381, 1000.000000000000000 ) ;
#58779=CARTESIAN_POINT ( 'NONE',  ( 61.04332100541591188, -42.96093274966459319, 76.66569307471927175 ) ) ;
#58789=CARTESIAN_POINT ( 'NONE',  ( -34.90990072193579863, -24.02533811425226418, 33.43583568697357578 ) ) ;
#58795=CARTESIAN_POINT ( 'NONE',  ( 84.24501642249120437, -39.42684420198852280, 179.9136778439357442 ) ) ;
#58804=CARTESIAN_POINT ( 'NONE',  ( -27.97116258485550944, -28.82356970829601650, -38.26646285370772915 ) ) ;
#58809=CARTESIAN_POINT ( 'NONE',  ( 47.39775995135304498, -60.00000000000000711, 65.66615658238637820 ) ) ;
#58812=CARTESIAN_POINT ( 'NONE',  ( -8.884123413888394438, -19.77486597863934747, 35.29550976858007516 ) ) ;
#58814=COLOUR_RGB ( '', 0.09019608, 0.27058824, 0.51372549) ;
#58819=ORIENTED_EDGE ( 'NONE', *, *, #82452, .T. ) ;
#58821=CARTESIAN_POINT ( 'NONE',  ( -49.50172129736240123, -35.49676079082828295, -36.27236392705374612 ) ) ;
#58826=CARTESIAN_POINT ( 'NONE',  ( 22.38858659560567688, -47.40902890394536939, -33.77719791820585016 ) ) ;
#58836=CARTESIAN_POINT ( 'NONE',  ( -96.18239882089940807, -60.00000000000000000, 57.27770282568545923 ) ) ;
#58843=CARTESIAN_POINT ( 'NONE',  ( -82.82505532928985303, -42.97746237936155467, 173.7292924292479768 ) ) ;
#58855=CARTESIAN_POINT ( 'NONE',  ( -11.25758791135831594, -57.67118876967119689, -44.34807234721190383 ) ) ;
#58861=CARTESIAN_POINT ( 'NONE',  ( 94.21232436905559382, -59.99999999999992895, 13.85190642028294761 ) ) ;
#58864=CARTESIAN_POINT ( 'NONE',  ( -114.5289996431801853, -60.00000000000001421, 168.5344195898668715 ) ) ;
#58865=CARTESIAN_POINT ( 'NONE',  ( -59.97350474172178281, -36.01739892119061182, 70.51521107528617449 ) ) ;
#58867=CARTESIAN_POINT ( 'NONE',  ( 51.84565611112584804, -38.00000000000000711, 53.44666998630373911 ) ) ;
#58868=CARTESIAN_POINT ( 'NONE',  ( 5.684014467335788190, -59.99999999999997868, 39.61781131791439492 ) ) ;
#58870=CARTESIAN_POINT ( 'NONE',  ( 6.142263938024425052, -46.43461817693559368, 31.61885644024033226 ) ) ;
#58871=CARTESIAN_POINT ( 'NONE',  ( -105.0581500925937064, -52.71025171956128474, 179.5698562497290425 ) ) ;
#58874=CARTESIAN_POINT ( 'NONE',  ( -2.500000000000001776, -30.00000000000000000, 30.00000000000000000 ) ) ;
#58875=CARTESIAN_POINT ( 'NONE',  ( -38.12866332992163620, -60.00000000000000000, 49.64653705277643780 ) ) ;
#58882=CARTESIAN_POINT ( 'NONE',  ( 84.71872414438772125, -56.33750704051404767, -15.23125129459240235 ) ) ;
#58887=CARTESIAN_POINT ( 'NONE',  ( 88.37306242433965053, -60.00000000000005684, 42.86595577526252043 ) ) ;
#58888=CARTESIAN_POINT ( 'NONE',  ( -31.76327952289363665, -36.02191956708324483, 33.16672948225943429 ) ) ;
#58890=CARTESIAN_POINT ( 'NONE',  ( 42.83239352544314471, -32.61479595472991377, 39.59629545049001109 ) ) ;
#58896=CARTESIAN_POINT ( 'NONE',  ( -76.78645060016569346, -38.43796788105258599, 183.2978527434968896 ) ) ;
#58900=CARTESIAN_POINT ( 'NONE',  ( 46.08503313555994652, -59.99999999999999289, 50.75047870711125597 ) ) ;
#58907=CARTESIAN_POINT ( 'NONE',  ( 106.3924386375468600, -60.00000000000000000, 118.8468287196073305 ) ) ;
#58910=CARTESIAN_POINT ( 'NONE',  ( -90.43823507282537832, -29.99999999999981171, 190.1885770241697742 ) ) ;
#58922=CARTESIAN_POINT ( 'NONE',  ( 81.07868691173642617, -53.41880775793396197, 174.1642699562374901 ) ) ;
#58956=CARTESIAN_POINT ( 'NONE',  ( 107.1550168409930137, -57.67119843336974583, 111.3111582704399041 ) ) ;
#58965=CARTESIAN_POINT ( 'NONE',  ( -77.43895560779745324, -59.99999999999999289, 191.5917464367579157 ) ) ;
#58970=CARTESIAN_POINT ( 'NONE',  ( -83.68245790527700478, -53.75685130900239272, 188.1406773380694801 ) ) ;
#58977=CARTESIAN_POINT ( 'NONE',  ( -83.18894126570232572, -37.77377736952604437, -9.182727467238077423 ) ) ;
#58983=CARTESIAN_POINT ( 'NONE',  ( -1.309564884278361513E-05, -14.21045842199434972, 34.36840973699906243 ) ) ;
#58985=CARTESIAN_POINT ( 'NONE',  ( -8.309739744518550353, -29.99999999999999289, -39.88085837097889197 ) ) ;
#58986=CARTESIAN_POINT ( 'NONE',  ( -70.47106563611271213, -46.43826247965927223, 107.5521328375196646 ) ) ;
#58988=CARTESIAN_POINT ( 'NONE',  ( 70.37902863207267501, -59.99999999999998579, 160.1157867729151576 ) ) ;
#58990=CARTESIAN_POINT ( 'NONE',  ( 93.55289619466658735, -57.65399935213944360, -15.69912234267622786 ) ) ;
#59001=CARTESIAN_POINT ( 'NONE',  ( 25.05982991920905079, -4.285714285714295357, 3.301565691951511727 ) ) ;
#59010=CARTESIAN_POINT ( 'NONE',  ( 31.01919067370845440, -22.13396283368982509, 30.33425209178049897 ) ) ;
#59024=VERTEX_POINT ( 'NONE', #49789 ) ;
#59025=CARTESIAN_POINT ( 'NONE',  ( 87.62530314318119906, -60.00000000000001421, -22.00415342985933620 ) ) ;
#59040=CARTESIAN_POINT ( 'NONE',  ( 84.53209051610372171, -52.74422840206830898, -14.22539307012042897 ) ) ;
#59053=CARTESIAN_POINT ( 'NONE',  ( 74.57620098502422934, -56.84629149567740569, 131.8975596435294051 ) ) ;
#59057=CARTESIAN_POINT ( 'NONE',  ( -114.2112478298105174, -57.67107988235927252, 175.3835541016526349 ) ) ;
#59063=CARTESIAN_POINT ( 'NONE',  ( 103.3363776539765837, -45.28277147255930402, 183.6174014516545014 ) ) ;
#59067=FACE_OUTER_BOUND ( 'NONE', #35898, .T. ) ;
#59079=CARTESIAN_POINT ( 'NONE',  ( -87.74548785222465597, -29.99999999999999645, 186.1198533190938065 ) ) ;
#59084=CARTESIAN_POINT ( 'NONE',  ( 71.42520752688669461, -57.67999775105185023, 166.3006026438890501 ) ) ;
#59088=CARTESIAN_POINT ( 'NONE',  ( 50.68724043103767940, -35.71711597358190460, -36.05002623880317714 ) ) ;
#59091=CARTESIAN_POINT ( 'NONE',  ( -35.74889062647464755, -60.00000000000000711, 47.10998833530662466 ) ) ;
#59095=CARTESIAN_POINT ( 'NONE',  ( -86.70368346074813815, -35.45285400290258337, 187.4689298322265927 ) ) ;
#59099=CARTESIAN_POINT ( 'NONE',  ( -7.031243609050225274, -25.54944219989091536, 28.13822752949184292 ) ) ;
#59116=CARTESIAN_POINT ( 'NONE',  ( 104.7858654919042465, -14.21045842199433018, 190.1692295410596785 ) ) ;
#59117=CARTESIAN_POINT ( 'NONE',  ( -80.89312144681923655, -39.50098901946147123, 151.8499635546424713 ) ) ;
#59127=VERTEX_POINT ( 'NONE', #22768 ) ;
#59136=CARTESIAN_POINT ( 'NONE',  ( 103.6331730138933835, -59.99999999999997868, 200.2368587013084777 ) ) ;
#59137=CARTESIAN_POINT ( 'NONE',  ( -79.57248154261856143, -14.21045842199419873, 190.0114072710836979 ) ) ;
#59138=CARTESIAN_POINT ( 'NONE',  ( 18.94558499360540438, -35.99294546495131186, 30.30127317126159170 ) ) ;
#59142=CARTESIAN_POINT ( 'NONE',  ( -39.50170393843561811, -46.43499008709606812, 39.80097614461234912 ) ) ;
#59155=CARTESIAN_POINT ( 'NONE',  ( 45.71963875501239016, -29.99999999999998934, 56.30994126864622729 ) ) ;
#59161=CARTESIAN_POINT ( 'NONE',  ( 83.28690719690919764, -30.00000000000000000, 45.18924137544603070 ) ) ;
#59179=CARTESIAN_POINT ( 'NONE',  ( 71.08938320489261287, -38.32842224238075346, 140.5796315854678653 ) ) ;
#59202=CARTESIAN_POINT ( 'NONE',  ( 85.50848406000137913, -39.28767163080398461, 185.4887185101361524 ) ) ;
#59206=CARTESIAN_POINT ( 'NONE',  ( 91.44632344411692770, -57.66251709069995002, -20.24473181102453623 ) ) ;
#59210=CARTESIAN_POINT ( 'NONE',  ( -83.12949059038693633, -29.99999999999998934, 43.93815505698431423 ) ) ;
#59219=DIRECTION ( 'NONE',  ( 0.000000000000000000, -1.000000000000000000, 0.000000000000000000 ) ) ;
#59225=CARTESIAN_POINT ( 'NONE',  ( 58.40792008327016305, -29.03551547989282966, -25.51115080894792442 ) ) ;
#59227=CARTESIAN_POINT ( 'NONE',  ( -24.27889609124726533, -22.08348835334177096, 28.63685605476302953 ) ) ;
#59233=CARTESIAN_POINT ( 'NONE',  ( -47.35410119362553161, -26.87184004367228951, -28.63942663572363045 ) ) ;
#59241=CARTESIAN_POINT ( 'NONE',  ( -90.37139598638705706, -60.00000000000000711, -18.17949969827632017 ) ) ;
#59245=CARTESIAN_POINT ( 'NONE',  ( 101.7209338708262862, -60.22223593363352023, 194.4975265031006586 ) ) ;
#59262=CARTESIAN_POINT ( 'NONE',  ( -28.75444143438830835, -57.68095489456369762, 44.62365432283354494 ) ) ;
#59266=CARTESIAN_POINT ( 'NONE',  ( -89.53165980454747341, -30.00000000000000000, -13.19740150267569767 ) ) ;
#59270=CARTESIAN_POINT ( 'NONE',  ( -49.21489589265689801, -60.29422131675831764, 56.32659531772773676 ) ) ;
#59278=CARTESIAN_POINT ( 'NONE',  ( 92.16345255951654281, -38.49867825655345399, 201.0232676182550620 ) ) ;
#59282=CARTESIAN_POINT ( 'NONE',  ( 94.15963719096482976, -29.99999999999999289, 191.2924193907763311 ) ) ;
#59290=CARTESIAN_POINT ( 'NONE',  ( 52.19444971213442841, -29.11002465084732549, 50.88288585126180408 ) ) ;
#59295=CARTESIAN_POINT ( 'NONE',  ( -89.24754036418538305, -38.38798525287715080, -17.62771086576031365 ) ) ;
#59296=VERTEX_POINT ( 'NONE', #37650 ) ;
#59298=CARTESIAN_POINT ( 'NONE',  ( 110.2493868441466844, -38.35601182983472768, 184.3356547549451818 ) ) ;
#59300=CARTESIAN_POINT ( 'NONE',  ( 83.98334445332307041, -37.85010976468362287, 36.91978127714231306 ) ) ;
#59309=CARTESIAN_POINT ( 'NONE',  ( 60.10615156299768103, -46.43600144855555811, 75.82275319019012727 ) ) ;
#59318=CARTESIAN_POINT ( 'NONE',  ( -46.01638873010887920, -28.64614323415289121, 41.14871410708547472 ) ) ;
#59321=CARTESIAN_POINT ( 'NONE',  ( 85.08258324672883077, -32.28520541998505422, 178.2135383856105761 ) ) ;
#59331=CARTESIAN_POINT ( 'NONE',  ( -19.47912966778427446, -25.64570046021258776, -38.49086459474126087 ) ) ;
#59338=CARTESIAN_POINT ( 'NONE',  ( 44.20361967343200149, -60.00000000000000000, 59.06671950064491483 ) ) ;
#59340=CARTESIAN_POINT ( 'NONE',  ( 7.438636493593315357, -13.23942326510881173, 32.01358503952575774 ) ) ;
#59342=CARTESIAN_POINT ( 'NONE',  ( -27.76376690927586566, -30.93432701297266973, 39.41148924507555051 ) ) ;
#59360=CARTESIAN_POINT ( 'NONE',  ( 31.16062950921062225, -21.77023875782602857, -28.58741295160539053 ) ) ;
#59370=CARTESIAN_POINT ( 'NONE',  ( -102.2988307860546655, -60.00000000000000711, 94.48776800051813041 ) ) ;
#59378=CARTESIAN_POINT ( 'NONE',  ( -85.20515625194583720, -25.43333465146562489, 169.0116749862556276 ) ) ;
#59395=CARTESIAN_POINT ( 'NONE',  ( 94.21214616282756538, -60.00000000000006395, 9.573485886066015027 ) ) ;
#59397=CARTESIAN_POINT ( 'NONE',  ( -86.50885295532998498, -60.00000000000009237, 203.5147570966663011 ) ) ;
#59398=CARTESIAN_POINT ( 'NONE',  ( -58.31099076156637295, -22.13342643865365744, 60.29576011847133543 ) ) ;
#59401=CARTESIAN_POINT ( 'NONE',  ( 92.92862678600012316, -59.99999999999997868, -18.42878329021216643 ) ) ;
#59403=CARTESIAN_POINT ( 'NONE',  ( 2.969152809838174978, -18.58611397292780154, 26.98299902465180367 ) ) ;
#59404=CARTESIAN_POINT ( 'NONE',  ( -104.1964872485443436, -52.71017148545060849, 185.8560034257230598 ) ) ;
#59409=CARTESIAN_POINT ( 'NONE',  ( -44.21061720778400428, -60.00000000000001421, 59.05736679842440395 ) ) ;
#59415=CARTESIAN_POINT ( 'NONE',  ( 14.76977913855438906, -0.000000000000000000, 8.521464936429580916 ) ) ;
#59421=CARTESIAN_POINT ( 'NONE',  ( -30.49126993251524098, -29.07187388107037407, 31.42370632120385920 ) ) ;
#59423=CARTESIAN_POINT ( 'NONE',  ( 45.04133914164980013, -60.25292661424882823, 49.29860799678134953 ) ) ;
#59428=CARTESIAN_POINT ( 'NONE',  ( -78.45624996374505145, -38.62884931123382870, 189.5593364397898313 ) ) ;
#59432=CARTESIAN_POINT ( 'NONE',  ( 26.97198470160383721, -60.00000000000000711, 35.68917358449845523 ) ) ;
#59440=CARTESIAN_POINT ( 'NONE',  ( 110.0424928893739747, -59.99999999999999289, 143.7894636553020007 ) ) ;
#59446=CARTESIAN_POINT ( 'NONE',  ( -72.66216753198708034, -30.00000000000000711, -19.29909516204710229 ) ) ;
#59460=CARTESIAN_POINT ( 'NONE',  ( 84.74724864891217635, -18.65598358680870561, 153.2857099555950526 ) ) ;
#59498=CARTESIAN_POINT ( 'NONE',  ( -79.80355888509041051, -60.00000000000000711, 195.7382001822659845 ) ) ;
#59502=CARTESIAN_POINT ( 'NONE',  ( -83.88690842771663370, -50.15420337227475756, 186.5806298538265082 ) ) ;
#59508=CARTESIAN_POINT ( 'NONE',  ( -82.50475734907109882, -37.83346213134558411, 7.442256542465846003 ) ) ;
#59516=CARTESIAN_POINT ( 'NONE',  ( 65.47680943546976096, -59.99999999999998579, 130.5870305019238913 ) ) ;
#59519=CARTESIAN_POINT ( 'NONE',  ( -78.96607584984282369, -14.21045842199439946, -22.44766605243856361 ) ) ;
#59520=CARTESIAN_POINT ( 'NONE',  ( -67.81647983110465816, -49.91373542098716598, 100.7778688019408833 ) ) ;
#59523=CARTESIAN_POINT ( 'NONE',  ( 69.35339668739648289, -14.21045842199427511, 113.5888189438209537 ) ) ;
#59526=CARTESIAN_POINT ( 'NONE',  ( 29.58605556073463561, -60.00000000000126477, 45.46635059003261858 ) ) ;
#59549=CARTESIAN_POINT ( 'NONE',  ( 30.83049859532185266, -18.66191575932449709, 29.63070459022076619 ) ) ;
#59563=CARTESIAN_POINT ( 'NONE',  ( 88.80472574437827404, -60.00000000000001421, -20.62865011427019368 ) ) ;
#59578=CARTESIAN_POINT ( 'NONE',  ( 84.46485305342990557, -45.28549382349953589, -8.213565521267117475 ) ) ;
#59588=CARTESIAN_POINT ( 'NONE',  ( 76.65407396917700567, -42.96273530073847269, 130.6257724894647083 ) ) ;
#59594=CARTESIAN_POINT ( 'NONE',  ( -98.27571109168336250, -57.67134109913899209, 58.06786128689789450 ) ) ;
#59599=CARTESIAN_POINT ( 'NONE',  ( 102.3723399798224278, -37.84840448700200710, 181.3185192590994461 ) ) ;
#59620=CARTESIAN_POINT ( 'NONE',  ( -85.49209400632499012, -29.99999999999999289, 174.7575250798003594 ) ) ;
#59624=CARTESIAN_POINT ( 'NONE',  ( 72.13773045038885812, -57.67273300135423142, 173.4418561065998290 ) ) ;
#59628=CARTESIAN_POINT ( 'NONE',  ( 62.79636538027480697, -37.67681387382631897, -33.45663682702740971 ) ) ;
#59630=CARTESIAN_POINT ( 'NONE',  ( -31.93456279712680868, -60.00000000000000000, 44.12512568447651518 ) ) ;
#59632=CARTESIAN_POINT ( 'NONE',  ( -86.49709195177823062, -42.82432661300771315, 189.1473926100390202 ) ) ;
#59634=CARTESIAN_POINT ( 'NONE',  ( -3.050654622591071341, -46.43922741216240269, 31.62448634903992328 ) ) ;
#59648=CARTESIAN_POINT ( 'NONE',  ( 109.5313825839763382, -30.00000000000004619, 176.4140126643321196 ) ) ;
#59649=CARTESIAN_POINT ( 'NONE',  ( -79.06061194151560301, -53.37725854339807796, 155.5602507423176064 ) ) ;
#59653=CARTESIAN_POINT ( 'NONE',  ( 41.27118623434287059, -57.68915202794213570, 57.80005340834581062 ) ) ;
#59669=CARTESIAN_POINT ( 'NONE',  ( 102.6668771475679307, -60.00000000000000000, 96.69110907683354128 ) ) ;
#59671=CARTESIAN_POINT ( 'NONE',  ( -78.95080019145578376, -30.00000000000002842, 188.4626203831212479 ) ) ;
#59672=CARTESIAN_POINT ( 'NONE',  ( 20.66686156031881083, -60.35595528423025513, 34.55852652023040861 ) ) ;
#59676=CARTESIAN_POINT ( 'NONE',  ( -42.83329106564534783, -32.61700632504245334, 39.59767786645361554 ) ) ;
#59681=CARTESIAN_POINT ( 'NONE',  ( -8.127057321558263325, -4.285714285714295357, 23.93420880016847718 ) ) ;
#59685=( GEOMETRIC_REPRESENTATION_CONTEXT ( 3 ) GLOBAL_UNCERTAINTY_ASSIGNED_CONTEXT ( ( #95756 ) ) GLOBAL_UNIT_ASSIGNED_CONTEXT ( ( #21727, #37391, #20697 ) ) REPRESENTATION_CONTEXT ( 'NONE', 'WORKASPACE' ) );
#59691=CARTESIAN_POINT ( 'NONE',  ( 100.3476047149571428, -30.00000000000000355, 183.8784433964002574 ) ) ;
#59695=CARTESIAN_POINT ( 'NONE',  ( 86.83990384507222871, -30.00000000000000000, 69.50558600361652850 ) ) ;
#59709=ORIENTED_EDGE ( 'NONE', *, *, #34650, .F. ) ;
#59714=CARTESIAN_POINT ( 'NONE',  ( 74.46552664185318804, -38.32957883525645570, 164.4766580072155193 ) ) ;
#59734=CARTESIAN_POINT ( 'NONE',  ( 84.69561524692119292, -53.82596867418983777, 190.2036044253954117 ) ) ;
#59741=CARTESIAN_POINT ( 'NONE',  ( -10.00000000000000000, 0.000000000000000000, 10.00000000000000178 ) ) ;
#59743=CARTESIAN_POINT ( 'NONE',  ( -83.07394592710599568, -30.00000000000000355, 43.49111805028168476 ) ) ;
#59754=CARTESIAN_POINT ( 'NONE',  ( -23.11910152252719186, -26.95796857353470699, 29.27772215835345548 ) ) ;
#59759=CARTESIAN_POINT ( 'NONE',  ( 56.05738515965948920, -28.67099341655612221, -26.25941955160380203 ) ) ;
#59760=CARTESIAN_POINT ( 'NONE',  ( -22.60355412798201868, -42.95868515067972027, 31.91959776729930098 ) ) ;
#59766=CARTESIAN_POINT ( 'NONE',  ( -19.91006257873084806, -29.03434590422582318, 29.21953239927981016 ) ) ;
#59767=CARTESIAN_POINT ( 'NONE',  ( -43.81237681895566283, -25.95568800022653733, -29.47119608928409207 ) ) ;
#59769=CARTESIAN_POINT ( 'NONE',  ( -74.86581005675350298, -60.22815006648220759, -24.22472159026646210 ) ) ;
#59777=CARTESIAN_POINT ( 'NONE',  ( -17.43438663440721470, -60.00000000000000711, -42.00932408933469731 ) ) ;
#59781=CARTESIAN_POINT ( 'NONE',  ( 98.83619226181630779, -37.79122241413045913, 192.0200725842609017 ) ) ;
#59782=CARTESIAN_POINT ( 'NONE',  ( 5.765378947742160420, -19.37891530848101240, 27.10972434534570397 ) ) ;
#59797=CARTESIAN_POINT ( 'NONE',  ( -99.52194594362661917, -60.00000000003903722, 63.55695574102755074 ) ) ;
#59801=CARTESIAN_POINT ( 'NONE',  ( -92.19364677446148448, -60.00000000000002842, -19.86446420722052153 ) ) ;
#59803=CARTESIAN_POINT ( 'NONE',  ( -49.43394015148312093, -32.59389012172065492, 47.58532889687595002 ) ) ;
#59806=ORIENTED_EDGE ( 'NONE', *, *, #106183, .T. ) ;
#59807=CARTESIAN_POINT ( 'NONE',  ( -96.11536361813142548, -52.81603231299632739, 195.4403539845496880 ) ) ;
#59813=CARTESIAN_POINT ( 'NONE',  ( 97.76259370245983860, -38.48107996425336808, 201.0305891777979070 ) ) ;
#59818=CARTESIAN_POINT ( 'NONE',  ( 85.96525886290406504, -30.00000000000000000, 178.3582022700497021 ) ) ;
#59825=CARTESIAN_POINT ( 'NONE',  ( 53.07978571422346192, -18.70625430049756943, 48.69073338330034062 ) ) ;
#59833=CARTESIAN_POINT ( 'NONE',  ( -91.43458545515113656, -38.37511409388242356, -4.844227564306105904 ) ) ;
#59835=CARTESIAN_POINT ( 'NONE',  ( 108.0216010846900048, -38.35838589254169051, 192.8427407754958836 ) ) ;
#59838=CARTESIAN_POINT ( 'NONE',  ( 88.90319265580640717, -60.14988975799602855, 46.79599450796897742 ) ) ;
#59843=SURFACE_STYLE_FILL_AREA ( #101349 ) ;
#59860=CARTESIAN_POINT ( 'NONE',  ( -35.95693203196412213, -24.51584111823862244, 33.83773937951661281 ) ) ;
#59864=CARTESIAN_POINT ( 'NONE',  ( 85.74124393967994706, -25.14955279151848089, 175.6267594608600007 ) ) ;
#59869=CARTESIAN_POINT ( 'NONE',  ( -90.29365882781722519, -60.15431844855726951, 56.70093613217015616 ) ) ;
#59874=CARTESIAN_POINT ( 'NONE',  ( -27.77336646784004515, -28.75003309865570600, -38.27452486851665014 ) ) ;
#59876=CARTESIAN_POINT ( 'NONE',  ( 43.67329148970010522, -60.00000000000000711, 58.07957383741103286 ) ) ;
#59877=CARTESIAN_POINT ( 'NONE',  ( 29.82243961713350444, -32.33238811108731170, 40.47282013833249437 ) ) ;
#59879=CARTESIAN_POINT ( 'NONE',  ( 6.071286224229995199, -13.01951455890936415, 32.06810514125731260 ) ) ;
#59882=CARTESIAN_POINT ( 'NONE',  ( -27.50695561155405855, -30.75843596377781708, 39.29379600943582318 ) ) ;
#59895=CARTESIAN_POINT ( 'NONE',  ( 21.81973643089116877, -21.77046491071190815, -29.53594053394288466 ) ) ;
#59902=VECTOR ( 'NONE', #42523, 1000.000000000000000 ) ;
#59908=CARTESIAN_POINT ( 'NONE',  ( -92.18718249619901428, -60.00000000000002132, 3.090949594964520042 ) ) ;
#59918=CARTESIAN_POINT ( 'NONE',  ( -81.10093029976930268, -56.96112622887682164, 179.5505663864836947 ) ) ;
#59924=AXIS2_PLACEMENT_3D ( 'NONE', #33822, #44017, #68841 ) ;
#59930=CARTESIAN_POINT ( 'NONE',  ( -72.51657142920434751, -41.65816625502668558, -21.93281331008283175 ) ) ;
#59935=( NAMED_UNIT ( * ) PLANE_ANGLE_UNIT ( ) SI_UNIT ( $, .RADIAN. ) );
#59937=CARTESIAN_POINT ( 'NONE',  ( 89.80793189580856506, -29.99999999999993250, 26.19443836851201723 ) ) ;
#59939=CARTESIAN_POINT ( 'NONE',  ( -78.65018897216694427, -14.21045842199436571, 174.1869015730407000 ) ) ;
#59940=CARTESIAN_POINT ( 'NONE',  ( -59.39683832124948282, -32.54576957150244709, 67.45736975201289454 ) ) ;
#59945=CARTESIAN_POINT ( 'NONE',  ( -103.8271769637748321, -45.26534194648037612, 179.3901650331305859 ) ) ;
#59951=CARTESIAN_POINT ( 'NONE',  ( -77.10094283560533768, -60.00000000000001421, 190.8546130424477667 ) ) ;
#59963=CARTESIAN_POINT ( 'NONE',  ( -29.62358194419280366, -36.01352107502461308, 32.38646520989296107 ) ) ;
#59967=CARTESIAN_POINT ( 'NONE',  ( 42.40293126982735572, -18.78677026436083608, 35.79721704996967446 ) ) ;
#59972=CARTESIAN_POINT ( 'NONE',  ( -94.82196696671130098, -38.48945518997164328, 201.2291303048070290 ) ) ;
#59974=CARTESIAN_POINT ( 'NONE',  ( 84.49906736890430636, -38.35837216793694893, -23.28434020672035842 ) ) ;
#59975=CARTESIAN_POINT ( 'NONE',  ( 61.60681234083082813, -59.99999999999999289, 86.74538964701946497 ) ) ;
#59983=CARTESIAN_POINT ( 'NONE',  ( 108.9514231372410507, -60.00000000000000711, 193.8007399767856498 ) ) ;
#59990=CARTESIAN_POINT ( 'NONE',  ( -80.70619913987853522, -30.00000000000000711, -12.62841071653336122 ) ) ;
#59992=CARTESIAN_POINT ( 'NONE',  ( -46.16323595244445954, -38.31912878070681217, 60.03967466318334800 ) ) ;
#60006=CARTESIAN_POINT ( 'NONE',  ( 84.55948629711632236, -22.11309726741666992, 156.8062503804032417 ) ) ;
#60035=ADVANCED_FACE ( 'NONE', ( #19622 ), #85370, .F. ) ;
#60046=CARTESIAN_POINT ( 'NONE',  ( -90.36280461092469807, -60.00000000000002132, 202.0446456219443689 ) ) ;
#60054=CARTESIAN_POINT ( 'NONE',  ( -83.08181241973555586, -57.30282313777087921, 188.7210544118925668 ) ) ;
#60058=CARTESIAN_POINT ( 'NONE',  ( -83.05971922487898951, -37.81386008383282871, -1.851040229428762451 ) ) ;
#60065=CARTESIAN_POINT ( 'NONE',  ( 69.85392978727392688, -60.00000000000004263, 155.8703566448706113 ) ) ;
#60066=CARTESIAN_POINT ( 'NONE',  ( -95.02173393737120932, -60.00000000000007105, -3.234914688897275070 ) ) ;
#60067=CARTESIAN_POINT ( 'NONE',  ( -72.21540169979105883, -22.11768858647452873, 98.80481924642175784 ) ) ;
#60069=CARTESIAN_POINT ( 'NONE',  ( 75.56757797150578426, -14.21045842199434439, 141.5459454228812319 ) ) ;
#60072=CARTESIAN_POINT ( 'NONE',  ( 33.76319574111100508, -59.99999999999999289, 48.40639849824221130 ) ) ;
#60082=CARTESIAN_POINT ( 'NONE',  ( -64.82079882110336655, -60.00000000003903722, 127.4591902977199567 ) ) ;
#60096=CARTESIAN_POINT ( 'NONE',  ( 32.10088869842463311, -25.61432814849804984, 31.36898226149570235 ) ) ;
#60097=( NAMED_UNIT ( * ) PLANE_ANGLE_UNIT ( ) SI_UNIT ( $, .RADIAN. ) );
#60111=CARTESIAN_POINT ( 'NONE',  ( 81.02257714386620080, -59.99999999999999289, -27.32370658691883136 ) ) ;
#60118=CARTESIAN_POINT ( 'NONE',  ( -106.9243038568529869, -29.99999999998815170, 191.8946513620529970 ) ) ;
#60126=CARTESIAN_POINT ( 'NONE',  ( 85.13361819880341841, -52.75518388885414822, -12.49988904550194135 ) ) ;
#60139=CARTESIAN_POINT ( 'NONE',  ( 73.66839973556383825, -56.84817161155148568, 127.7600820225604537 ) ) ;
#60145=CARTESIAN_POINT ( 'NONE',  ( -104.7047915100801987, -57.67116545479915857, 96.89679091199744221 ) ) ;
#60149=CARTESIAN_POINT ( 'NONE',  ( 104.1886421374867382, -52.71694715348233728, 185.8499235192266497 ) ) ;
#60165=CARTESIAN_POINT ( 'NONE',  ( -89.27843304015721060, -30.00000000000000711, 189.0996331995533524 ) ) ;
#60171=CARTESIAN_POINT ( 'NONE',  ( 86.12462942110903441, -57.57595555861249181, 202.7575993840488593 ) ) ;
#60174=CARTESIAN_POINT ( 'NONE',  ( 57.07624943773998893, -36.90585292959303132, -34.83277310691430984 ) ) ;
#60177=CARTESIAN_POINT ( 'NONE',  ( -41.75932222925875692, -60.00000000000000711, 54.76167985618531731 ) ) ;
#60182=CARTESIAN_POINT ( 'NONE',  ( -85.01242186521922406, -61.08653189438597764, 193.5097775706131245 ) ) ;
#60185=CARTESIAN_POINT ( 'NONE',  ( -1.016815886943048142, -53.40265724237126932, 32.79009283333092384 ) ) ;
#60199=CARTESIAN_POINT ( 'NONE',  ( 96.66679845751455957, -59.99999999999993605, 43.68127598107410847 ) ) ;
#60200=CARTESIAN_POINT ( 'NONE',  ( -82.94229579353957149, -29.08663412309721608, 153.6279066531906494 ) ) ;
#60204=CARTESIAN_POINT ( 'NONE',  ( 14.12267823962728386, -57.67128902998698692, 41.72226490217841643 ) ) ;
#60222=CARTESIAN_POINT ( 'NONE',  ( -103.2140057312332715, -60.00000000000000000, 203.2732544657875167 ) ) ;
#60223=CARTESIAN_POINT ( 'NONE',  ( 20.24742129507015420, -42.95413648879811319, 31.59189836021716857 ) ) ;
#60227=CARTESIAN_POINT ( 'NONE',  ( -38.79755192928217156, -53.35182168183835927, 40.67521693547091388 ) ) ;
#60238=ORIENTED_EDGE ( 'NONE', *, *, #19211, .T. ) ;
#60239=CARTESIAN_POINT ( 'NONE',  ( 101.1293268413511726, -29.99999999999999289, 173.2232745131870786 ) ) ;
#60243=CARTESIAN_POINT ( 'NONE',  ( 86.62138541769266453, -30.00000000000000000, 68.13828909135614254 ) ) ;
#60262=CARTESIAN_POINT ( 'NONE',  ( 74.24099750797692820, -38.32798285832743801, 162.4509745339827589 ) ) ;
#60284=CARTESIAN_POINT ( 'NONE',  ( 86.12526957674350570, -50.15648532675116655, 190.9329294407513089 ) ) ;
#60288=CARTESIAN_POINT ( 'NONE',  ( 76.07691912369757858, -57.67120883703200462, -32.16632477336341367 ) ) ;
#60291=CARTESIAN_POINT ( 'NONE',  ( -81.90484931453705997, -30.00000000000000000, 32.97508095190593025 ) ) ;
#60294=CARTESIAN_POINT ( 'NONE',  ( 32.07628956478022531, -57.68926933952037928, 46.61244027368547194 ) ) ;
#60299=CARTESIAN_POINT ( 'NONE',  ( -21.97839536960432838, -26.35170283925622314, 29.01137685833781532 ) ) ;
#60302=CARTESIAN_POINT ( 'NONE',  ( 57.44923501886911055, -28.89280837408547598, -25.82236834149354721 ) ) ;
#60304=CARTESIAN_POINT ( 'NONE',  ( -21.87228149277378719, -60.36180085709548848, 34.72076190976543586 ) ) ;
#60308=CARTESIAN_POINT ( 'NONE',  ( -18.94606539149997815, -35.99581223526647733, 30.30179149493963919 ) ) ;
#60314=EDGE_LOOP ( 'NONE', ( #39009, #57329, #91911, #4605, #53186, #57371, #83383, #64424, #68179 ) ) ;
#60320=EDGE_CURVE ( 'NONE', #53605, #91474, #17079, .T. ) ;
#60323=CARTESIAN_POINT ( 'NONE',  ( 99.48073951191379649, -45.27021486848132525, 193.0246297540120963 ) ) ;
#60337=CARTESIAN_POINT ( 'NONE',  ( -93.97829082725922945, -60.00000000000243006, -15.75854254785690500 ) ) ;
#60341=CARTESIAN_POINT ( 'NONE',  ( 89.99999999999997158, -60.00000000000000000, 196.0238439516549818 ) ) ;
#60342=CARTESIAN_POINT ( 'NONE',  ( -85.44375122223560481, -14.21045842199445630, -16.44937377337592466 ) ) ;
#60344=CARTESIAN_POINT ( 'NONE',  ( -51.03670451184174794, -49.90889464192031966, 56.18977702641336691 ) ) ;
#60348=VERTEX_POINT ( 'NONE', #10279 ) ;
#60355=CARTESIAN_POINT ( 'NONE',  ( 50.51862023164185445, -38.33298512735416352, 69.71478400885560234 ) ) ;
#60360=CARTESIAN_POINT ( 'NONE',  ( 86.89255445192647187, -30.00000000000000355, 183.2879409112302369 ) ) ;
#60366=CARTESIAN_POINT ( 'NONE',  ( 55.42290428782216338, -36.02733805088502805, 59.79522858329378465 ) ) ;
#60371=CARTESIAN_POINT ( 'NONE',  ( -90.26554477178873981, -38.40034450972390090, -15.28474180237319757 ) ) ;
#60374=CARTESIAN_POINT ( 'NONE',  ( 110.6785498806628851, -38.35606011449173991, 180.6793801968407251 ) ) ;
#60376=CARTESIAN_POINT ( 'NONE',  ( 88.45222707626928127, -52.71650411927125646, 52.49135111675786192 ) ) ;
#60394=CARTESIAN_POINT ( 'NONE',  ( 1.078140322363270668E-05, -30.00000000000000000, 28.88964995960238014 ) ) ;
#60396=CARTESIAN_POINT ( 'NONE',  ( -46.78455459927008064, -28.88905235460685006, 42.05601398093777021 ) ) ;
#60401=CARTESIAN_POINT ( 'NONE',  ( 85.51531819923015121, -28.66246248194799051, 177.8895563405388032 ) ) ;
#60402=LINE ( 'NONE', #19440, #94677 ) ;
#60405=CARTESIAN_POINT ( 'NONE',  ( -97.56669589868897674, -60.15515597314767859, 100.7599927763139505 ) ) ;
#60410=CARTESIAN_POINT ( 'NONE',  ( -23.06278213417854062, -26.97848082407063330, -38.42385101396828873 ) ) ;
#60412=ADVANCED_FACE ( 'NONE', ( #16786 ), #82579, .F. ) ;
#60415=CARTESIAN_POINT ( 'NONE',  ( 41.84377380827102400, -60.00000000000000000, 54.90543347242942218 ) ) ;
#60416=CARTESIAN_POINT ( 'NONE',  ( 36.47095910356380699, -36.25311398404432595, 45.65967941635479121 ) ) ;
#60418=CARTESIAN_POINT ( 'NONE',  ( 27.77029367025814111, -20.61067439569943360, 31.81999448069623071 ) ) ;
#60419=CARTESIAN_POINT ( 'NONE',  ( -36.83723954793523347, -36.42387658263878336, 46.04340430436438680 ) ) ;
#60429=CARTESIAN_POINT ( 'NONE',  ( -2.026006894917399492, -60.00000000000001421, 39.63628641406589992 ) ) ;
#60436=CARTESIAN_POINT ( 'NONE',  ( -3.214504396424240795, -60.22813258367417433, -36.90743551004686651 ) ) ;
#60447=CARTESIAN_POINT ( 'NONE',  ( -92.04877409173086278, -60.00000000000000711, 19.49932517706979240 ) ) ;
#60453=CARTESIAN_POINT ( 'NONE',  ( -82.49914212121935009, -42.97583219876662497, 170.7411135741228918 ) ) ;
#60458=ORIENTED_EDGE ( 'NONE', *, *, #45381, .T. ) ;
#60465=CARTESIAN_POINT ( 'NONE',  ( -90.36739715925041594, -57.66608071200965213, -21.81949331871602382 ) ) ;
#60471=CARTESIAN_POINT ( 'NONE',  ( -97.48274675841855696, -52.68933714276726477, 195.2152360717980741 ) ) ;
#60472=CARTESIAN_POINT ( 'NONE',  ( 90.15648792673195544, -30.00000000000007816, 30.33492934306279309 ) ) ;
#60474=CARTESIAN_POINT ( 'NONE',  ( -80.78871696068775066, -30.00000000000004974, 192.9492619026495390 ) ) ;
#60475=CARTESIAN_POINT ( 'NONE',  ( -60.56849898340908567, -25.59444836810600776, 67.17426576971645602 ) ) ;
#60479=CARTESIAN_POINT ( 'NONE',  ( -105.5953457684452701, -60.15498359724100652, 185.0758216606398321 ) ) ;
#60480=DIRECTION ( 'NONE',  ( 0.000000000000000000, 0.000000000000000000, -1.000000000000000000 ) ) ;
#60490=CARTESIAN_POINT ( 'NONE',  ( 12.81917055448646359, 0.000000000000000000, -11.24487389204835353 ) ) ;
#60496=CARTESIAN_POINT ( 'NONE',  ( -31.99613883384627755, -46.43541966511591568, 35.16710097061795892 ) ) ;
#60497=CARTESIAN_POINT ( 'NONE',  ( 45.48381414773980680, -36.07135055825224157, 43.31344887555280110 ) ) ;
#60501=CARTESIAN_POINT ( 'NONE',  ( -98.19059862094080415, -38.47942618394503711, 200.9491795779894971 ) ) ;
#60512=CARTESIAN_POINT ( 'NONE',  ( 111.2651448867182182, -59.99999999999999289, 185.8803051558543018 ) ) ;
#60516=CIRCLE ( 'NONE', #55316, 8.000000000000000000 ) ;
#60517=CARTESIAN_POINT ( 'NONE',  ( -82.23392483931314700, -29.99999999999997158, 36.79773247150587423 ) ) ;
#60529=CARTESIAN_POINT ( 'NONE',  ( 83.46195034026524695, -29.07547344062109573, 157.7160910814760939 ) ) ;
#60542=CARTESIAN_POINT ( 'NONE',  ( -80.58034289023321151, -29.99999999999999289, -12.88258808325728566 ) ) ;
#60544=CARTESIAN_POINT ( 'NONE',  ( 86.93474114976024225, -53.74889697056932647, 192.8288056809579984 ) ) ;
#60570=CARTESIAN_POINT ( 'NONE',  ( -100.6730827315817010, -59.99999999999999289, 201.6981752365160219 ) ) ;
#60575=CARTESIAN_POINT ( 'NONE',  ( -86.40560123953810034, -17.60749286260778135, 177.3355119052273494 ) ) ;
#60581=CARTESIAN_POINT ( 'NONE',  ( -85.46236302623604786, -52.71435437274617897, -0.4815862223618528892 ) ) ;
#60589=CARTESIAN_POINT ( 'NONE',  ( 66.01776342811430709, -14.21045842199433373, 101.7751388943407989 ) ) ;
#60591=CARTESIAN_POINT ( 'NONE',  ( -77.20948002450832348, -29.99999999999995737, -26.53460153345886496 ) ) ;
#60593=CARTESIAN_POINT ( 'NONE',  ( -74.77681607752303705, -18.65167433089163751, 105.3459956964869235 ) ) ;
#60595=CARTESIAN_POINT ( 'NONE',  ( 78.42622819757743002, -14.21045842199428932, 178.5071270543957951 ) ) ;
#60597=CARTESIAN_POINT ( 'NONE',  ( 44.60816201714979456, -57.67117032717165870, -40.90560715985412799 ) ) ;
#60607=CARTESIAN_POINT ( 'NONE',  ( -33.63572111039716361, -59.99999999999509015, 48.29151853392890104 ) ) ;
#60622=CARTESIAN_POINT ( 'NONE',  ( 32.61996141319230702, -46.43004813113018514, 35.44677629655089390 ) ) ;
#60623=CARTESIAN_POINT ( 'NONE',  ( 24.56594385547430903, -4.285714285713612348, -6.601913983211183279 ) ) ;
#60636=CARTESIAN_POINT ( 'NONE',  ( 92.56520787782876880, -60.00000000000000711, -2.232329057168804365 ) ) ;
#60645=CARTESIAN_POINT ( 'NONE',  ( -105.0046858871420028, -29.99999999999525713, 195.3910615991270561 ) ) ;
#60650=CARTESIAN_POINT ( 'NONE',  ( 86.78321768392551405, -60.22672886896445021, -10.97222102851997150 ) ) ;
#60663=CARTESIAN_POINT ( 'NONE',  ( 71.96604720757427742, -25.59085233378921842, 100.0522785706842228 ) ) ;
#60667=CARTESIAN_POINT ( 'NONE',  ( -103.1324900820093262, -57.63586870064128931, 202.7914362107620434 ) ) ;
#60671=CARTESIAN_POINT ( 'NONE',  ( 102.8080410108812544, -37.84829216994245371, 172.5350295752351713 ) ) ;
#60676=CARTESIAN_POINT ( 'NONE',  ( -45.18794255447445352, -28.36039750011541827, 40.27443962283176404 ) ) ;
#60687=CARTESIAN_POINT ( 'NONE',  ( -86.33424672516723319, -30.00000000000000000, 180.6259601542327857 ) ) ;
#60691=CARTESIAN_POINT ( 'NONE',  ( 81.46498296581839327, -57.51694840548930188, 200.1052016080623162 ) ) ;
#60695=CARTESIAN_POINT ( 'NONE',  ( 58.29968221944096740, -37.09312005238718513, -34.56216655994825970 ) ) ;
#60698=CARTESIAN_POINT ( 'NONE',  ( -71.35988770730575936, -60.00000000000000711, 149.7293370354783804 ) ) ;
#60702=CARTESIAN_POINT ( 'NONE',  ( -86.75334951847432308, -24.36967792699222102, 185.3770496680724875 ) ) ;
#60705=CARTESIAN_POINT ( 'NONE',  ( -1.013597693207653139, -49.92101462973083414, 32.20981906455752153 ) ) ;
#60706=EDGE_CURVE ( 'NONE', #57621, #73170, #73826, .T. ) ;
#60721=CARTESIAN_POINT ( 'NONE',  ( 90.15648792673195544, -30.00000000000007816, 30.33492934306279309 ) ) ;
#60722=CARTESIAN_POINT ( 'NONE',  ( -79.97220600232276411, -49.91032667486920360, 158.2823762716815565 ) ) ;
#60725=( NAMED_UNIT ( * ) SI_UNIT ( $, .STERADIAN. ) SOLID_ANGLE_UNIT ( ) );
#60743=CARTESIAN_POINT ( 'NONE',  ( 44.28326324223792909, -60.00000000000000000, -38.95962436850444988 ) ) ;
#60745=CARTESIAN_POINT ( 'NONE',  ( -48.81109529425772564, -14.21045842199442788, 55.84243332122913017 ) ) ;
#60746=CARTESIAN_POINT ( 'NONE',  ( 19.65438280374391056, -18.59146986454509332, 27.43996338408375379 ) ) ;
#60749=CARTESIAN_POINT ( 'NONE',  ( -33.68155633810341953, -22.16622110500054177, 31.32162176238002971 ) ) ;
#60762=CARTESIAN_POINT ( 'NONE',  ( 98.06547367653239178, -30.00000000000002132, 190.4620094107865498 ) ) ;
#60765=CARTESIAN_POINT ( 'NONE',  ( 81.32474297617858383, -30.00000000000000355, -0.8629055029887053863 ) ) ;
#60777=ORIENTED_EDGE ( 'NONE', *, *, #49369, .T. ) ;
#60781=CARTESIAN_POINT ( 'NONE',  ( 75.83882639694283512, -38.36842668940455070, 177.1099218260232817 ) ) ;
#60800=CARTESIAN_POINT ( 'NONE',  ( 86.01633990920335293, -53.81041820905097239, 191.9596364128520634 ) ) ;
#60804=CARTESIAN_POINT ( 'NONE',  ( 22.43756508786705695, -57.67086147514856265, -43.66263415315633978 ) ) ;
#60805=CARTESIAN_POINT ( 'NONE',  ( 4.338297905010414901, -15.54644901148979486, -35.15006977224143014 ) ) ;
#60810=CARTESIAN_POINT ( 'NONE',  ( -90.21070732519919488, -29.99999999999999645, 89.72569532995613883 ) ) ;
#60815=CARTESIAN_POINT ( 'NONE',  ( 28.02193915076392727, -57.67940780473148266, 44.29223288112500967 ) ) ;
#60819=CARTESIAN_POINT ( 'NONE',  ( -16.18099529597535025, -23.36744278781230477, 27.97947390617177277 ) ) ;
#60822=CARTESIAN_POINT ( 'NONE',  ( 24.91891126693706227, -20.04364040963082516, -33.01464637846507344 ) ) ;
#60823=CARTESIAN_POINT ( 'NONE',  ( -25.12479025497365370, -46.43848000890793770, 32.95526142708619233 ) ) ;
#60827=CARTESIAN_POINT ( 'NONE',  ( -21.32298952633117395, -39.47768505749013457, 31.13619358448382712 ) ) ;
#60838=CARTESIAN_POINT ( 'NONE',  ( -8.679094227360542035, -60.00000000000000000, -42.46732092095059130 ) ) ;
#60842=CARTESIAN_POINT ( 'NONE',  ( 99.72099231572487099, -37.83690929057568297, 191.0453301431148248 ) ) ;
#60858=CARTESIAN_POINT ( 'NONE',  ( -55.85966931448584916, -60.00000000001456613, -39.08074821196408521 ) ) ;
#60863=CARTESIAN_POINT ( 'NONE',  ( -87.19976908022060513, -14.21045842199435860, -12.72659765151139233 ) ) ;
#60866=CARTESIAN_POINT ( 'NONE',  ( -49.15736080366974647, -29.13434467386025872, 46.07356561062454148 ) ) ;
#60876=CARTESIAN_POINT ( 'NONE',  ( 89.97112945879391077, -29.99999999997625721, -10.10510908212382475 ) ) ;
#60881=CARTESIAN_POINT ( 'NONE',  ( 87.73947420500191186, -29.99999999999999289, 186.1036665454039678 ) ) ;
#60887=CARTESIAN_POINT ( 'NONE',  ( 54.96666262631825361, -36.02821829405777976, 58.82418178195225522 ) ) ;
#60892=CARTESIAN_POINT ( 'NONE',  ( -85.46470094257063010, -38.35991919399719308, -22.41886950923507626 ) ) ;
#60895=CARTESIAN_POINT ( 'NONE',  ( 109.0199404443706612, -38.35645241016953833, 190.0871729485212143 ) ) ;
#60897=CARTESIAN_POINT ( 'NONE',  ( 82.62163173485843970, -37.86093661847765901, 4.878488117475526131 ) ) ;
#60919=CARTESIAN_POINT ( 'NONE',  ( 1.154068430507904086, -12.55449340960651483, 32.19352746017464284 ) ) ;
#60922=CARTESIAN_POINT ( 'NONE',  ( 84.92621421947670513, -39.36226118941799967, 183.3512328336199744 ) ) ;
#60926=VECTOR ( 'NONE', #10141, 1000.000000000000000 ) ;
#60928=CARTESIAN_POINT ( 'NONE',  ( -85.46379202683773713, -37.82125448877485496, 49.13329909993041156 ) ) ;
#60934=CARTESIAN_POINT ( 'NONE',  ( 29.99506149210614581, -60.00000000000000711, 43.03431844238033221 ) ) ;
#60935=CARTESIAN_POINT ( 'NONE',  ( 27.15809507750037710, -30.51936720628422961, 39.13764639798584000 ) ) ;
#60937=CARTESIAN_POINT ( 'NONE',  ( 41.55968476715275273, -26.98253679743242017, 37.03168355540274348 ) ) ;
#60938=CARTESIAN_POINT ( 'NONE',  ( -30.01214130291127802, -32.45876557533858175, 40.58130538435680990 ) ) ;
#60955=CARTESIAN_POINT ( 'NONE',  ( 4.642985192297872210, -21.77036161962056937, -30.46305366977244944 ) ) ;
#60965=CARTESIAN_POINT ( 'NONE',  ( -92.23009394491774060, -59.99999999999999289, 2.477879558583810038 ) ) ;
#60973=CARTESIAN_POINT ( 'NONE',  ( -81.51997760136781324, -49.94239916794347067, 172.6801288724093979 ) ) ;
#60975=CARTESIAN_POINT ( 'NONE',  ( -8.521411446768031084, 0.000000000000000000, -14.76969908562668721 ) ) ;
#60981=VERTEX_POINT ( 'NONE', #52206 ) ;
#60984=CARTESIAN_POINT ( 'NONE',  ( -94.73097995338159194, -57.65973493957909568, -7.453110678737913553 ) ) ;
#60990=CARTESIAN_POINT ( 'NONE',  ( 108.2372837266210297, -59.99999999999997868, 115.4707114838127211 ) ) ;
#60991=CARTESIAN_POINT ( 'NONE',  ( -102.9006728679688365, -30.00000000000001421, 197.6531887663732618 ) ) ;
#60993=CARTESIAN_POINT ( 'NONE',  ( -55.56343265448107616, -22.15138794996349247, 54.53997454549021739 ) ) ;
#60997=CARTESIAN_POINT ( 'NONE',  ( -104.5556233096705938, -52.71023842945449189, 183.8341536945831081 ) ) ;
#60998=DIRECTION ( 'NONE',  ( -0.000000000000000000, -1.000000000000000000, -0.000000000000000000 ) ) ;
#61017=CARTESIAN_POINT ( 'NONE',  ( -31.20798807302101707, -25.60670629028073719, 31.04078863611647421 ) ) ;
#61019=CARTESIAN_POINT ( 'NONE',  ( 48.04108913913790246, -39.52162123606319000, 47.68945014315683295 ) ) ;
#61022=CARTESIAN_POINT ( 'NONE',  ( -85.61943167051258285, -38.66581993764706482, 198.8511778627555771 ) ) ;
#61033=CARTESIAN_POINT ( 'NONE',  ( 106.6542038942911148, -59.99999999999999289, 197.5365053951335312 ) ) ;
#61040=CARTESIAN_POINT ( 'NONE',  ( -81.47582811281075976, -30.00000000000000711, -9.499132834538738024 ) ) ;
#61042=CARTESIAN_POINT ( 'NONE',  ( -78.70717280597565946, -38.65874930792139708, 190.2476505887177325 ) ) ;
#61051=CARTESIAN_POINT ( 'NONE',  ( 84.11707923628694061, -32.48599780003080184, 169.3644224162934790 ) ) ;
#61086=( BOUNDED_SURFACE ( )  B_SPLINE_SURFACE ( 2, 3, ( 
 ( #69622, #44279, #93890, #88455, #56043, #32358, #6980, #54993, #15605, #88978, #5918, #87924, #104622, #48495, #31817, #97573, #47439, #38844, #14004, #40418, #90032, #98122, #64701, #23203, #39898, #23739, #73298, #63114, #81390, #72772, #106194, #65230, #79815, #30227, #80332, #24270, #31301, #71708, #56590, #7500, #39380, #89512, #57118, #6445, #16138, #80870, #22678, #30772, #72258, #49026, #63658, #96546, #105678, #96015, #46913, #81923, #8043, #64188, #97057, #40954, #104088, #22142, #55515, #14531, #105159, #15077, #47962, #91642, #34502, #50102, #84611, #83007, #9630, #41480, #33960, #42539, #82477, #66830, #42010, #18848, #99721, #75442, #74893, #50611, #49569, #74368, #59813, #66289, #10695, #25890, #100776, #99173, #59278, #8578, #51153, #106739, #446, #65762, #100247, #33415, #91121, #25332, #17755, #92692, #98643, #1535, #51693, #58195, #92153, #26939, #83529, #24793, #17230, #67367, #75976, #9102, #977, #84071, #58747, #26412, #18298, #67888, #10171, #43087, #2071, #35023, #73845, #57647, #32888, #90567, #16678, #27478, #44152, #94843, #78103, #37155, #93766, #52224, #60355, #86753, #29595, #37693 ),
 ( #93230, #12299, #86227, #19392, #69493, #77041, #45227, #77583, #35559, #20988, #70557, #68433, #11226, #45743, #21494, #4754, #11761, #85135, #70019, #62465, #4221, #101845, #54330, #60876, #12823, #3158, #102379, #36102, #36627, #68972, #102918, #28007, #28531, #87273, #43609, #76501, #19923, #61950, #52765, #94303, #78620, #61411, #20466, #85685, #53821, #44696, #53308, #3701, #29085, #103444, #95356, #2610, #101326, #14408, #47320, #48379, #5802, #22566, #80216, #6863, #72136, #57001, #105045, #38725, #39788, #64588, #88335, #81274, #46800, #31186, #56468, #6321, #105561, #5291, #71592, #104498, #47842, #64071, #97459, #24156, #72663, #13351, #39261, #31700, #23616, #7386, #40300, #89398, #65106, #15492, #73173, #38212, #106078, #96946, #103963, #55404, #79162, #32227, #98003, #23079, #46278, #62997, #88859, #55917, #95893, #14948, #13883, #80748, #71073, #30107, #22019, #54874, #87804, #79693, #30646, #63534, #96431, #58068, #73718, #83411, #1952, #58623, #41360, #100657, #329, #26295, #98528, #41889, #106621, #82887, #32771, #17639, #65643, #8985, #67770, #26818, #89915, #49443, #1413, #74253, #33834, #59155 ),
 ( #74777, #16559, #24674, #857, #57527, #90993, #90448, #17103, #49979, #18172, #82352, #99047, #66707, #9509, #99589, #16022, #25765, #8459, #42422, #34377, #91523, #51033, #33293, #50499, #92038, #75315, #67249, #81797, #66164, #25214, #100128, #83946, #10058, #48902, #42966, #7923, #75858, #34905, #40827, #53706, #86638, #12176, #4639, #69900, #76919, #12702, #19281, #69378, #45108, #28408, #84490, #60239, #102798, #61282, #37570, #59691, #94726, #94177, #37032, #4104, #76376, #86106, #28959, #93650, #101202, #61830, #3030, #35437, #11101, #70435, #60762, #20872, #35980, #45631, #52107, #102259, #77987, #20343, #10583, #93107, #78506, #53189, #103330, #92570, #18721, #51575, #43499, #2487, #68308, #27360, #85017, #19798, #44027, #68851, #101727, #27895, #52634, #85566, #11642, #44572, #77462, #3573, #36510, #13234, #71471, #95243, #47722, #15365, #38608, #48250, #79047, #104927, #72015, #5166, #55280, #29991, #31067, #63420, #21375, #80621, #56336, #54213, #103846, #31583, #7262, #97337, #104371, #46159, #22961, #81151, #63944, #87683, #40173, #46672, #72537, #38095, #88209, #70955, #22440, #62877, #96831, #95768 ) ),
 .UNSPECIFIED., .F., .F., .T. ) 
 B_SPLINE_SURFACE_WITH_KNOTS ( ( 3, 3 ),
 ( 4, 2, 2, 2, 2, 2, 2, 2, 2, 2, 2, 2, 2, 2, 2, 2, 2, 2, 2, 2, 2, 2, 2, 2, 2, 2, 2, 2, 2, 2, 2, 2, 2, 2, 2, 2, 2, 2, 2, 2, 2, 2, 2, 2, 2, 2, 2, 2, 2, 2, 2, 2, 2, 2, 2, 2, 2, 2, 2, 2, 2, 2, 2, 2, 2, 2, 2, 2, 2, 2, 4 ),
 ( 0.000000000000000000, 1.000000000000000000 ),
 ( 0.000000000000000000, 0.002867805938563325763, 0.005735611877126651527, 0.007169514846408315059, 0.008603417815689977724, 0.01003732078497164039, 0.01075427226961247172, 0.01147122375425330305, 0.01182969949657371872, 0.01218817523889413612, 0.01290512672353496745, 0.01433902969281663012, 0.01577293266209829278, 0.01720683563137995545, 0.02007464156994328078, 0.02294244750850660611, 0.02867805938563326024, 0.03441367126275991090, 0.04588489501701321222, 0.06882734252551982179, 0.09176979003402642443, 0.1376546850510396436, 0.1605971325595462462, 0.1720683563137995475, 0.1835395800680528489, 0.1950108038223061779, 0.2007464156994328286, 0.2064820275765594793, 0.2093498335151228185, 0.2107837364844044603, 0.2122176394536861299, 0.2129345909383269508, 0.2136515424229677995, 0.2140100181652881961, 0.2141892560364483944, 0.2143684939076086204, 0.2144581128431887196, 0.2145029223109787830, 0.2145477317787688465, 0.2147269696499290448, 0.2149062075210892431, 0.2150854453922494414, 0.2158023968768902900, 0.2165193483615311110, 0.2172362998461719319, 0.2179532513308127806, 0.2193871543000944502, 0.2201041057847352711, 0.2208210572693761198, 0.2215380087540169407, 0.2222549602386577616, 0.2224341981098179599, 0.2226134359809781860, 0.2229719117232986103, 0.2236888632079394312, 0.2244058146925802522, 0.2251227661772211008, 0.2265566691465027427, 0.2294244750850660819, 0.2322922810236294211, 0.2351600869621927326, 0.2408956988393193832, 0.2466313107164460339, 0.2523669225935726845, 0.2638381463478259858, 0.2753093701020792872, 0.3211942651190924924, 0.3326654888733457938, 0.3441367126275990951, 0.3556079363818523964, 0.3670791601361056977 ),
 .UNSPECIFIED. ) 
 GEOMETRIC_REPRESENTATION_ITEM ( )  RATIONAL_B_SPLINE_SURFACE ( (
 ( 1.000000000000000000, 1.000000000000000000, 1.000000000000000000, 1.000000000000000000, 1.000000000000000000, 1.000000000000000000, 1.000000000000000000, 1.000000000000000000, 1.000000000000000000, 1.000000000000000000, 1.000000000000000000, 1.000000000000000000, 1.000000000000000000, 1.000000000000000000, 1.000000000000000000, 1.000000000000000000, 1.000000000000000000, 1.000000000000000000, 1.000000000000000000, 1.000000000000000000, 1.000000000000000000, 1.000000000000000000, 1.000000000000000000, 1.000000000000000000, 1.000000000000000000, 1.000000000000000000, 1.000000000000000000, 1.000000000000000000, 1.000000000000000000, 1.000000000000000000, 1.000000000000000000, 1.000000000000000000, 1.000000000000000000, 1.000000000000000000, 1.000000000000000000, 1.000000000000000000, 1.000000000000000000, 1.000000000000000000, 1.000000000000000000, 1.000000000000000000, 1.000000000000000000, 1.000000000000000000, 1.000000000000000000, 1.000000000000000000, 1.000000000000000000, 1.000000000000000000, 1.000000000000000000, 1.000000000000000000, 1.000000000000000000, 1.000000000000000000, 1.000000000000000000, 1.000000000000000000, 1.000000000000000000, 1.000000000000000000, 1.000000000000000000, 1.000000000000000000, 1.000000000000000000, 1.000000000000000000, 1.000000000000000000, 1.000000000000000000, 1.000000000000000000, 1.000000000000000000, 1.000000000000000000, 1.000000000000000000, 1.000000000000000000, 1.000000000000000000, 1.000000000000000000, 1.000000000000000000, 1.000000000000000000, 1.000000000000000000, 1.000000000000000000, 1.000000000000000000, 1.000000000000000000, 1.000000000000000000, 1.000000000000000000, 1.000000000000000000, 1.000000000000000000, 1.000000000000000000, 1.000000000000000000, 1.000000000000000000, 1.000000000000000000, 1.000000000000000000, 1.000000000000000000, 1.000000000000000000, 1.000000000000000000, 1.000000000000000000, 1.000000000000000000, 1.000000000000000000, 1.000000000000000000, 1.000000000000000000, 1.000000000000000000, 1.000000000000000000, 1.000000000000000000, 1.000000000000000000, 1.000000000000000000, 1.000000000000000000, 1.000000000000000000, 1.000000000000000000, 1.000000000000000000, 1.000000000000000000, 1.000000000000000000, 1.000000000000000000, 1.000000000000000000, 1.000000000000000000, 1.000000000000000000, 1.000000000000000000, 1.000000000000000000, 1.000000000000000000, 1.000000000000000000, 1.000000000000000000, 1.000000000000000000, 1.000000000000000000, 1.000000000000000000, 1.000000000000000000, 1.000000000000000000, 1.000000000000000000, 1.000000000000000000, 1.000000000000000000, 1.000000000000000000, 1.000000000000000000, 1.000000000000000000, 1.000000000000000000, 1.000000000000000000, 1.000000000000000000, 1.000000000000000000, 1.000000000000000000, 1.000000000000000000, 1.000000000000000000, 1.000000000000000000, 1.000000000000000000, 1.000000000000000000, 1.000000000000000000, 1.000000000000000000, 1.000000000000000000, 1.000000000000000000, 1.000000000000000000, 1.000000000000000000, 1.000000000000000000, 1.000000000000000000, 1.000000000000000000, 1.000000000000000000, 1.000000000000000000),
 ( 1.857142857142858317, 1.857142857142858317, 1.857142857142858317, 1.857142857142858317, 1.857142857142858317, 1.857142857142858317, 1.857142857142858317, 1.857142857142858317, 1.857142857142858317, 1.857142857142858317, 1.857142857142858317, 1.857142857142858317, 1.857142857142858317, 1.857142857142858317, 1.857142857142858317, 1.857142857142858317, 1.857142857142858317, 1.857142857142858317, 1.857142857142858317, 1.857142857142858317, 1.857142857142858317, 1.857142857142858317, 1.857142857142858317, 1.857142857142858317, 1.857142857142858317, 1.857142857142858317, 1.857142857142858317, 1.857142857142858317, 1.857142857142858317, 1.857142857142858317, 1.857142857142858317, 1.857142857142858317, 1.857142857142858317, 1.857142857142858317, 1.857142857142858317, 1.857142857142858317, 1.857142857142858317, 1.857142857142858317, 1.857142857142858317, 1.857142857142858317, 1.857142857142858317, 1.857142857142858317, 1.857142857142858317, 1.857142857142858317, 1.857142857142858317, 1.857142857142858317, 1.857142857142858317, 1.857142857142858317, 1.857142857142858317, 1.857142857142858317, 1.857142857142858317, 1.857142857142858317, 1.857142857142858317, 1.857142857142858317, 1.857142857142858317, 1.857142857142858317, 1.857142857142858317, 1.857142857142858317, 1.857142857142858317, 1.857142857142858317, 1.857142857142858317, 1.857142857142858317, 1.857142857142858317, 1.857142857142858317, 1.857142857142858317, 1.857142857142858317, 1.857142857142858317, 1.857142857142858317, 1.857142857142858317, 1.857142857142858317, 1.857142857142858317, 1.857142857142858317, 1.857142857142858317, 1.857142857142858317, 1.857142857142858317, 1.857142857142858317, 1.857142857142858317, 1.857142857142858317, 1.857142857142858317, 1.857142857142858317, 1.857142857142858317, 1.857142857142858317, 1.857142857142858317, 1.857142857142858317, 1.857142857142858317, 1.857142857142858317, 1.857142857142858317, 1.857142857142858317, 1.857142857142858317, 1.857142857142858317, 1.857142857142858317, 1.857142857142858317, 1.857142857142858317, 1.857142857142858317, 1.857142857142858317, 1.857142857142858317, 1.857142857142858317, 1.857142857142858317, 1.857142857142858317, 1.857142857142858317, 1.857142857142858317, 1.857142857142858317, 1.857142857142858317, 1.857142857142858317, 1.857142857142858317, 1.857142857142858317, 1.857142857142858317, 1.857142857142858317, 1.857142857142858317, 1.857142857142858317, 1.857142857142858317, 1.857142857142858317, 1.857142857142858317, 1.857142857142858317, 1.857142857142858317, 1.857142857142858317, 1.857142857142858317, 1.857142857142858317, 1.857142857142858317, 1.857142857142858317, 1.857142857142858317, 1.857142857142858317, 1.857142857142858317, 1.857142857142858317, 1.857142857142858317, 1.857142857142858317, 1.857142857142858317, 1.857142857142858317, 1.857142857142858317, 1.857142857142858317, 1.857142857142858317, 1.857142857142858317, 1.857142857142858317, 1.857142857142858317, 1.857142857142858317, 1.857142857142858317, 1.857142857142858317, 1.857142857142858317, 1.857142857142858317, 1.857142857142858317, 1.857142857142858317, 1.857142857142858317),
 ( 1.000000000000000000, 1.000000000000000000, 1.000000000000000000, 1.000000000000000000, 1.000000000000000000, 1.000000000000000000, 1.000000000000000000, 1.000000000000000000, 1.000000000000000000, 1.000000000000000000, 1.000000000000000000, 1.000000000000000000, 1.000000000000000000, 1.000000000000000000, 1.000000000000000000, 1.000000000000000000, 1.000000000000000000, 1.000000000000000000, 1.000000000000000000, 1.000000000000000000, 1.000000000000000000, 1.000000000000000000, 1.000000000000000000, 1.000000000000000000, 1.000000000000000000, 1.000000000000000000, 1.000000000000000000, 1.000000000000000000, 1.000000000000000000, 1.000000000000000000, 1.000000000000000000, 1.000000000000000000, 1.000000000000000000, 1.000000000000000000, 1.000000000000000000, 1.000000000000000000, 1.000000000000000000, 1.000000000000000000, 1.000000000000000000, 1.000000000000000000, 1.000000000000000000, 1.000000000000000000, 1.000000000000000000, 1.000000000000000000, 1.000000000000000000, 1.000000000000000000, 1.000000000000000000, 1.000000000000000000, 1.000000000000000000, 1.000000000000000000, 1.000000000000000000, 1.000000000000000000, 1.000000000000000000, 1.000000000000000000, 1.000000000000000000, 1.000000000000000000, 1.000000000000000000, 1.000000000000000000, 1.000000000000000000, 1.000000000000000000, 1.000000000000000000, 1.000000000000000000, 1.000000000000000000, 1.000000000000000000, 1.000000000000000000, 1.000000000000000000, 1.000000000000000000, 1.000000000000000000, 1.000000000000000000, 1.000000000000000000, 1.000000000000000000, 1.000000000000000000, 1.000000000000000000, 1.000000000000000000, 1.000000000000000000, 1.000000000000000000, 1.000000000000000000, 1.000000000000000000, 1.000000000000000000, 1.000000000000000000, 1.000000000000000000, 1.000000000000000000, 1.000000000000000000, 1.000000000000000000, 1.000000000000000000, 1.000000000000000000, 1.000000000000000000, 1.000000000000000000, 1.000000000000000000, 1.000000000000000000, 1.000000000000000000, 1.000000000000000000, 1.000000000000000000, 1.000000000000000000, 1.000000000000000000, 1.000000000000000000, 1.000000000000000000, 1.000000000000000000, 1.000000000000000000, 1.000000000000000000, 1.000000000000000000, 1.000000000000000000, 1.000000000000000000, 1.000000000000000000, 1.000000000000000000, 1.000000000000000000, 1.000000000000000000, 1.000000000000000000, 1.000000000000000000, 1.000000000000000000, 1.000000000000000000, 1.000000000000000000, 1.000000000000000000, 1.000000000000000000, 1.000000000000000000, 1.000000000000000000, 1.000000000000000000, 1.000000000000000000, 1.000000000000000000, 1.000000000000000000, 1.000000000000000000, 1.000000000000000000, 1.000000000000000000, 1.000000000000000000, 1.000000000000000000, 1.000000000000000000, 1.000000000000000000, 1.000000000000000000, 1.000000000000000000, 1.000000000000000000, 1.000000000000000000, 1.000000000000000000, 1.000000000000000000, 1.000000000000000000, 1.000000000000000000, 1.000000000000000000, 1.000000000000000000, 1.000000000000000000, 1.000000000000000000, 1.000000000000000000, 1.000000000000000000, 1.000000000000000000) ) ) 
 REPRESENTATION_ITEM ( '' )  SURFACE ( )  );
#61091=CARTESIAN_POINT ( 'NONE',  ( -108.5714035732085136, -60.00000000000000000, 194.5812896598510520 ) ) ;
#61095=CARTESIAN_POINT ( 'NONE',  ( -84.89423566776963526, -35.82611643478423957, 180.4073639259765969 ) ) ;
#61103=CARTESIAN_POINT ( 'NONE',  ( -84.36863145535683373, -45.27031347337740641, -2.914881809220207121 ) ) ;
#61109=CARTESIAN_POINT ( 'NONE',  ( 73.11766847789152735, -30.00000000000003197, 143.8471250665463117 ) ) ;
#61110=CARTESIAN_POINT ( 'NONE',  ( -86.58264346576902426, -59.99999999999995737, -26.28034805200384838 ) ) ;
#61111=CARTESIAN_POINT ( 'NONE',  ( -74.53378729071185660, -46.43775938986178176, 123.7974631154742866 ) ) ;
#61113=CARTESIAN_POINT ( 'NONE',  ( 106.4941418293696387, -60.00000000000010658, 201.1229827202191984 ) ) ;
#61115=CARTESIAN_POINT ( 'NONE',  ( 2.936182742934462817E-09, -59.99999999999998579, 41.99999999999666755 ) ) ;
#61125=CARTESIAN_POINT ( 'NONE',  ( -92.35142332109028018, -60.00000000000000000, 24.83174829623999713 ) ) ;
#61139=CARTESIAN_POINT ( 'NONE',  ( 32.20288135873296653, -22.14765632207181056, 30.75472695888904440 ) ) ;
#61140=( LENGTH_UNIT ( ) NAMED_UNIT ( * ) SI_UNIT ( .MILLI., .METRE. ) );
#61155=CARTESIAN_POINT ( 'NONE',  ( 92.05911407252800416, -59.99999999999999289, 5.082830299684662378 ) ) ;
#61164=CARTESIAN_POINT ( 'NONE',  ( -99.88742157809630839, -30.00000000021226398, 95.80496660798954167 ) ) ;
#61165=ORIENTED_EDGE ( 'NONE', *, *, #79527, .F. ) ;
#61170=CARTESIAN_POINT ( 'NONE',  ( 86.12633428247868039, -60.22439185339658252, -13.73171497637067517 ) ) ;
#61173=CARTESIAN_POINT ( 'NONE',  ( 72.95844571965780290, -52.66120096372748804, -23.75233168814477480 ) ) ;
#61181=CARTESIAN_POINT ( 'NONE',  ( 82.19117875687653907, -22.15571452471658986, 140.5442402927623675 ) ) ;
#61187=CARTESIAN_POINT ( 'NONE',  ( -108.6808209725780330, -57.66364365951052662, 198.1525503354515081 ) ) ;
#61195=CARTESIAN_POINT ( 'NONE',  ( -45.20342746193760775, -28.36574318593202548, 40.29076024120101351 ) ) ;
#61207=CARTESIAN_POINT ( 'NONE',  ( -62.55951166628249638, -29.54618481767612082, -24.05121344435046637 ) ) ;
#61208=CARTESIAN_POINT ( 'NONE',  ( -84.71380100379134603, -29.99999999999998934, 167.6049798258065664 ) ) ;
#61213=CARTESIAN_POINT ( 'NONE',  ( 77.74182763612704150, -57.51479071948315180, 196.2079078470394222 ) ) ;
#61217=CARTESIAN_POINT ( 'NONE',  ( 47.01191233711254824, -34.86740698265760585, -36.61028653586306092 ) ) ;
#61220=CARTESIAN_POINT ( 'NONE',  ( -72.03623563651683526, -59.99999999999999289, 154.5482511779330537 ) ) ;
#61225=CARTESIAN_POINT ( 'NONE',  ( -84.53966279108223603, -53.82414633558762773, 189.9397737380796229 ) ) ;
#61228=CARTESIAN_POINT ( 'NONE',  ( -3.010010578735510478, -32.51265499686979155, 29.30374655122669836 ) ) ;
#61243=CARTESIAN_POINT ( 'NONE',  ( 24.56594385547430903, -4.285714285713612348, -6.601913983211183279 ) ) ;
#61245=CARTESIAN_POINT ( 'NONE',  ( 91.01367250360885919, -30.00000000000005684, 38.60059757395459457 ) ) ;
#61246=CARTESIAN_POINT ( 'NONE',  ( -78.92021213579246819, -56.84825361667137145, 159.0990771215834343 ) ) ;
#61250=CARTESIAN_POINT ( 'NONE',  ( 37.14872619403364240, -57.69633467219071576, 51.57620306562363055 ) ) ;
#61265=EDGE_LOOP ( 'NONE', ( #63926, #33957, #62475, #106434 ) ) ;
#61266=CARTESIAN_POINT ( 'NONE',  ( 92.36673650245116107, -59.99999999999998579, 0.5857224784561708697 ) ) ;
#61267=CARTESIAN_POINT ( 'NONE',  ( -41.69391581180516937, -30.00000000000004974, 49.76410629065788527 ) ) ;
#61268=CARTESIAN_POINT ( 'NONE',  ( 20.33158520735264219, -46.43450536202994527, 32.18516374921409806 ) ) ;
#61271=CARTESIAN_POINT ( 'NONE',  ( -37.55439227784096090, -29.13175677663839025, 34.71063202183116658 ) ) ;
#61280=CARTESIAN_POINT ( 'NONE',  ( -71.70444520824810297, -38.32814726721150578, 143.9842855213637733 ) ) ;
#61282=CARTESIAN_POINT ( 'NONE',  ( 100.9278572184871479, -29.99999999999998224, 179.0295527065578938 ) ) ;
#61285=CARTESIAN_POINT ( 'NONE',  ( 81.52379479105302096, -30.00000000000000355, -3.957376937645873394 ) ) ;
#61307=CARTESIAN_POINT ( 'NONE',  ( 60.41163985755903099, -38.34247882570736721, 97.70464050350065577 ) ) ;
#61315=CARTESIAN_POINT ( 'NONE',  ( 60.83498899738820853, -46.43599129440129047, 77.79182497454313250 ) ) ;
#61317=ORIENTED_EDGE ( 'NONE', *, *, #25954, .T. ) ;
#61333=CARTESIAN_POINT ( 'NONE',  ( 85.67780798737555870, -46.54417124946874651, 188.9740981328812381 ) ) ;
#61337=CARTESIAN_POINT ( 'NONE',  ( 75.76386167821715389, -57.67120288045602194, -32.30820643211533394 ) ) ;
#61342=CARTESIAN_POINT ( 'NONE',  ( -86.30897805172713788, -29.99999999999998934, 66.16620683248447676 ) ) ;
#61345=CARTESIAN_POINT ( 'NONE',  ( 27.84462555168287778, -57.67905924191398270, 44.21611220939174558 ) ) ;
#61353=CARTESIAN_POINT ( 'NONE',  ( 24.22617517784814112, -19.82454084975979924, -33.12017639804538760 ) ) ;
#61357=CARTESIAN_POINT ( 'NONE',  ( -24.01064210916210229, -49.91863376122307727, 33.32460945998198554 ) ) ;
#61361=CARTESIAN_POINT ( 'NONE',  ( -17.15213637186141682, -60.36485515943083158, 34.22168534330848644 ) ) ;
#61375=CARTESIAN_POINT ( 'NONE',  ( 100.7139165092765722, -45.27943385528230635, 191.7620851108205500 ) ) ;
#61390=CARTESIAN_POINT ( 'NONE',  ( -36.42379736945513002, -59.99999999996140332, -42.51792151884048110 ) ) ;
#61393=CARTESIAN_POINT ( 'NONE',  ( 79.82864494832747937, -60.00000000000971312, -30.74386842393604979 ) ) ;
#61396=CARTESIAN_POINT ( 'NONE',  ( -92.03818768401583839, -29.99999999999997513, 46.84875813697714619 ) ) ;
#61397=CARTESIAN_POINT ( 'NONE',  ( 4.101671097088348539, -53.39668839384628996, 32.78132364643582974 ) ) ;
#61399=CARTESIAN_POINT ( 'NONE',  ( -48.17921737381070102, -18.76214205199974927, 41.56990939206856694 ) ) ;
#61411=CARTESIAN_POINT ( 'NONE',  ( 97.39383678230348096, -30.00000000010727064, 81.91721032156783622 ) ) ;
#61417=CARTESIAN_POINT ( 'NONE',  ( 100.4873323852713867, -29.99999999999999645, 182.9215336627512443 ) ) ;
#61423=CARTESIAN_POINT ( 'NONE',  ( 53.62448839840453729, -56.84308160174793301, 64.25510811246175535 ) ) ;
#61428=CARTESIAN_POINT ( 'NONE',  ( -90.31811283708992732, -38.40091087090596034, -15.13224940126931983 ) ) ;
#61431=CARTESIAN_POINT ( 'NONE',  ( 99.81073769260291328, -38.46674976063415841, 200.5728603240891914 ) ) ;
#61433=CARTESIAN_POINT ( 'NONE',  ( 83.93392681204029770, -45.28697172910836599, 3.738167347945261731 ) ) ;
#61452=CARTESIAN_POINT ( 'NONE',  ( 8.212513060757594019, -15.78310966187656028, 34.62353203711420946 ) ) ;
#61460=CARTESIAN_POINT ( 'NONE',  ( 85.41283022940925207, -32.17522569109155484, 180.5326087057368056 ) ) ;
#61463=ORIENTED_EDGE ( 'NONE', *, *, #18821, .F. ) ;
#61464=CARTESIAN_POINT ( 'NONE',  ( -88.90359386438426270, -60.15364184676742099, 46.79264400712646221 ) ) ;
#61471=CARTESIAN_POINT ( 'NONE',  ( 27.85340566596032374, -60.00000000000001421, 42.07270389097206476 ) ) ;
#61472=CARTESIAN_POINT ( 'NONE',  ( 15.28118917856605563, -22.84720680763436818, 35.97391546425213704 ) ) ;
#61473=CARTESIAN_POINT ( 'NONE',  ( 46.91226987233839907, -28.92226484961306809, 42.23736541826801982 ) ) ;
#61487=VERTEX_POINT ( 'NONE', #106321 ) ;
#61494=CARTESIAN_POINT ( 'NONE',  ( -6.199981704917457925, -21.77037438476674325, -30.42741826779913694 ) ) ;
#61501=CARTESIAN_POINT ( 'NONE',  ( -94.42521480436519710, -60.00000000000000000, 44.71142204259329844 ) ) ;
#61510=CARTESIAN_POINT ( 'NONE',  ( -83.37195354553843174, -36.00313111294963875, 167.8019081912905790 ) ) ;
#61522=CARTESIAN_POINT ( 'NONE',  ( -93.58432581829866592, -57.65368546899212987, -15.63533335066522767 ) ) ;
#61529=CARTESIAN_POINT ( 'NONE',  ( 69.60540008574220394, -30.00000000000001421, -29.89027719438221453 ) ) ;
#61530=CARTESIAN_POINT ( 'NONE',  ( -76.70274796309844589, -29.99999999999996447, 172.7051753936532066 ) ) ;
#61531=CARTESIAN_POINT ( 'NONE',  ( -54.96692882686725312, -36.03106141262587414, 58.82583099766474533 ) ) ;
#61537=CARTESIAN_POINT ( 'NONE',  ( -100.9568756953421342, -52.73574583597550713, 193.4176276002172585 ) ) ;
#61538=CARTESIAN_POINT ( 'NONE',  ( 102.2191329667627713, -37.99999999999999289, 182.8622780301718365 ) ) ;
#61549=CARTESIAN_POINT ( 'NONE',  ( 65.93937847753362291, -29.99999999999999645, 82.94257298685835167 ) ) ;
#61554=CARTESIAN_POINT ( 'NONE',  ( -28.85079751128344938, -32.53587765291774758, 31.52101463460818564 ) ) ;
#61555=CARTESIAN_POINT ( 'NONE',  ( 47.02088286195116495, -36.06800221881119484, 45.21478074418502757 ) ) ;
#61558=CARTESIAN_POINT ( 'NONE',  ( -85.92922987661015100, -38.64615708810908501, 199.0210877423697866 ) ) ;
#61570=CARTESIAN_POINT ( 'NONE',  ( 112.1703215029695286, -59.99999999999999289, 168.8166208195475519 ) ) ;
#61577=CARTESIAN_POINT ( 'NONE',  ( -81.44309280902999149, -30.00000000000002132, 29.19263923180426445 ) ) ;
#61579=FILL_AREA_STYLE ('',( #104946 ) ) ;
#61590=CARTESIAN_POINT ( 'NONE',  ( 85.65051399455167314, -18.54895490038211747, 161.4844583081507778 ) ) ;
#61607=CARTESIAN_POINT ( 'NONE',  ( -76.65309938956929159, -30.00000000000000355, -16.89940168842986878 ) ) ;
#61612=ADVANCED_FACE ( 'NONE', ( #75566 ), #100368, .T. ) ;
#61625=ADVANCED_FACE ( 'NONE', ( #28123 ), #35685, .F. ) ;
#61637=CARTESIAN_POINT ( 'NONE',  ( -106.1374248126797539, -60.00000000000000000, 198.1280823682561447 ) ) ;
#61644=CARTESIAN_POINT ( 'NONE',  ( -84.04979895421557501, -42.98303161459435984, 182.1087557225411899 ) ) ;
#61647=VERTEX_POINT ( 'NONE', #20043 ) ;
#61651=CARTESIAN_POINT ( 'NONE',  ( -86.94550892133041486, -60.17282562918532562, -3.944479883897415995 ) ) ;
#61659=CARTESIAN_POINT ( 'NONE',  ( 70.80389978121282013, -30.00000000000000711, 131.5992258684728995 ) ) ;
#61661=CARTESIAN_POINT ( 'NONE',  ( -87.76943268072510307, -14.21045842199432307, -6.547605000374890238 ) ) ;
#61662=CARTESIAN_POINT ( 'NONE',  ( -64.69100649186263752, -29.05538772269134284, 79.90073128498799804 ) ) ;
#61664=CARTESIAN_POINT ( 'NONE',  ( 100.3457197225335733, -14.21045842199427511, 196.5350150060856720 ) ) ;
#61666=CARTESIAN_POINT ( 'NONE',  ( 35.13867974785705428, -59.99999999999999289, 49.78873796555570408 ) ) ;
#61679=CARTESIAN_POINT ( 'NONE',  ( -88.36461763089066324, -60.00000000000001421, -21.16661413833238825 ) ) ;
#61683=CARTESIAN_POINT ( 'NONE',  ( -1.544427540536530316E-15, -4.285714285714290916, 25.22241582816893057 ) ) ;
#61692=CARTESIAN_POINT ( 'NONE',  ( 34.28021199336672709, -32.56668617693117795, 33.60777154440098968 ) ) ;
#61693=CARTESIAN_POINT ( 'NONE',  ( -25.22241582816893413, -4.285714285714287364, -3.301606509427108982 ) ) ;
#61705=CARTESIAN_POINT ( 'NONE',  ( 92.01607953741286394, -60.00000000000001421, 18.77391487596767661 ) ) ;
#61713=CARTESIAN_POINT ( 'NONE',  ( -102.9438915830126291, -29.99999999999873879, 197.5134625135077613 ) ) ;
#61719=CARTESIAN_POINT ( 'NONE',  ( 84.90240974134064800, -60.18835296399971213, -16.21870115458467865 ) ) ;
#61725=CARTESIAN_POINT ( 'NONE',  ( -24.22231588719698436, -19.79037096225153647, -33.14000009352793086 ) ) ;
#61726=AXIS2_PLACEMENT_3D ( 'NONE', #6462, #14546, #53954 ) ;
#61729=CARTESIAN_POINT ( 'NONE',  ( 79.06124460869463633, -53.37162188482365366, 155.5587481820264202 ) ) ;
#61733=CARTESIAN_POINT ( 'NONE',  ( -105.2191501062491881, -57.64508961356604999, 201.5420537206667291 ) ) ;
#61734=EDGE_CURVE ( 'NONE', #89859, #69966, #19598, .T. ) ;
#61751=CARTESIAN_POINT ( 'NONE',  ( -89.99999999999997158, -60.00000000000000000, 196.0238439516549818 ) ) ;
#61753=CARTESIAN_POINT ( 'NONE',  ( 14.52379002078253301, -19.49130720279776696, -37.81483145485863417 ) ) ;
#61754=CARTESIAN_POINT ( 'NONE',  ( -81.60074597489959558, -29.99999999999999289, 143.5170916637224252 ) ) ;
#61761=CARTESIAN_POINT ( 'NONE',  ( 75.28700688039084810, -57.56648276822033949, 191.4465710134679739 ) ) ;
#61768=CARTESIAN_POINT ( 'NONE',  ( -61.04408880086688782, -60.00000000000000711, 104.0053245555540258 ) ) ;
#61772=CARTESIAN_POINT ( 'NONE',  ( -84.69478162058261717, -53.83175173781702938, 190.2051053124634166 ) ) ;
#61775=CARTESIAN_POINT ( 'NONE',  ( -2.969389021251942484, -18.58608251166780079, 26.98300677151931382 ) ) ;
#61789=CARTESIAN_POINT ( 'NONE',  ( -17.78317311657527000, -3.867350551647862515E-12, 13.66642973271121342 ) ) ;
#61792=CARTESIAN_POINT ( 'NONE',  ( 105.9102621261374253, -29.99999999999996803, 132.9887338302407898 ) ) ;
#61793=CARTESIAN_POINT ( 'NONE',  ( -80.32583173421626555, -25.62118807212741345, 133.8900160517275708 ) ) ;
#61815=CARTESIAN_POINT ( 'NONE',  ( 92.64087237572343270, -60.00000000000000000, -9.951826560658968646 ) ) ;
#61816=CARTESIAN_POINT ( 'NONE',  ( -62.45630560627096628, -29.99999999999992184, 99.43668923270982418 ) ) ;
#61817=CARTESIAN_POINT ( 'NONE',  ( 25.00472155834508925, -42.95520012000800847, 32.33701874286857247 ) ) ;
#61820=CARTESIAN_POINT ( 'NONE',  ( -39.00554263752280093, -36.06017026425686822, 37.16608606929241887 ) ) ;
#61828=CARTESIAN_POINT ( 'NONE',  ( -75.06642738654252867, -38.33958646326993147, 170.1756141881156168 ) ) ;
#61830=CARTESIAN_POINT ( 'NONE',  ( 98.39163834582095092, -29.99999999999995737, 190.0198514090498634 ) ) ;
#61833=CARTESIAN_POINT ( 'NONE',  ( 80.72524915699251835, -30.00000000000000711, -12.58409207385285988 ) ) ;
#61855=CARTESIAN_POINT ( 'NONE',  ( 62.71390290029641079, -60.33891165955828484, 90.28853715842232930 ) ) ;
#61857=CARTESIAN_POINT ( 'NONE',  ( 0.000000000000000000, -8.673617379884035472E-16, -17.01589776168603407 ) ) ;
#61858=CARTESIAN_POINT ( 'NONE',  ( -54.69861804585598719, -36.50581144510210407, -35.32386462939300031 ) ) ;
#61873=CARTESIAN_POINT ( 'NONE',  ( 84.90064340091288386, -57.46992232430159930, 192.0070107122053003 ) ) ;
#61879=CARTESIAN_POINT ( 'NONE',  ( -14.43785825815714752, -17.02022128621486274, -34.43806907934169459 ) ) ;
#61884=CARTESIAN_POINT ( 'NONE',  ( -100.9715102229217365, -30.00000000000000711, 178.1047487978037509 ) ) ;
#61887=CARTESIAN_POINT ( 'NONE',  ( 32.18356949007781509, -57.68957018251984437, 46.69086977585512699 ) ) ;
#61894=CARTESIAN_POINT ( 'NONE',  ( 11.76221606908526240, -16.54900257170227107, -34.66273767363278324 ) ) ;
#61901=CARTESIAN_POINT ( 'NONE',  ( -21.23094043253502150, -35.99698555973125735, 30.53890210230313329 ) ) ;
#61902=CARTESIAN_POINT ( 'NONE',  ( -86.13135164208073036, -59.99999999999992895, -13.61769622756565035 ) ) ;
#61918=CARTESIAN_POINT ( 'NONE',  ( 101.5338889927411827, -45.28223279133771229, 190.3009016725240770 ) ) ;
#61933=CARTESIAN_POINT ( 'NONE',  ( -97.06981497546472326, -60.00000000003904432, 46.90335524957238533 ) ) ;
#61935=CARTESIAN_POINT ( 'NONE',  ( 11.36546102070421149, -60.00000000000001421, 39.66528621601015914 ) ) ;
#61938=CARTESIAN_POINT ( 'NONE',  ( -90.94649322911389788, -14.21045842199428222, 57.96573475225447680 ) ) ;
#61939=CARTESIAN_POINT ( 'NONE',  ( 12.48886139173590593, -46.43473308940932753, 31.68645849438150819 ) ) ;
#61941=CARTESIAN_POINT ( 'NONE',  ( -48.29725705757057597, -46.44452024506328058, 50.22719862630319909 ) ) ;
#61950=CARTESIAN_POINT ( 'NONE',  ( 89.93526870310212473, -30.00000000001337241, 29.02783687399049128 ) ) ;
#61954=CARTESIAN_POINT ( 'NONE',  ( 100.6243693333776434, -30.00000000000000355, 160.8148924688006218 ) ) ;
#61962=CARTESIAN_POINT ( 'NONE',  ( 54.78051204086806791, -29.09201784496401544, 55.71616249050997993 ) ) ;
#61964=DIRECTION ( 'NONE',  ( 0.000000000000000000, -1.000000000000000000, 0.000000000000000000 ) ) ;
#61965=ADVANCED_FACE ( 'NONE', ( #19661 ), #85481, .T. ) ;
#61972=CARTESIAN_POINT ( 'NONE',  ( 94.04204770716727069, -38.49239426584006907, 201.1939902864932037 ) ) ;
#61974=CARTESIAN_POINT ( 'NONE',  ( 86.12722738054240779, -60.13654648131097247, 11.25971878457827913 ) ) ;
#61993=CARTESIAN_POINT ( 'NONE',  ( 38.43315959910751189, -27.95011100668220649, 45.39859000375419384 ) ) ;
#61998=CARTESIAN_POINT ( 'NONE',  ( 84.10550226404134833, -46.55871237661660444, 184.9821644560045399 ) ) ;
#62003=CARTESIAN_POINT ( 'NONE',  ( -96.00081068786835203, -45.26563211955492960, 106.3251220198503120 ) ) ;
#62008=CARTESIAN_POINT ( 'NONE',  ( 7.878783547692759903, -19.41176153434803098, 35.22918882278415964 ) ) ;
#62010=CARTESIAN_POINT ( 'NONE',  ( 39.78494456460381912, -26.23335630279444786, 35.82506221462753615 ) ) ;
#62028=CARTESIAN_POINT ( 'NONE',  ( -1.543626744577732079, -21.77031562861895608, -30.51802372251457385 ) ) ;
#62040=CARTESIAN_POINT ( 'NONE',  ( -91.98068305807049683, -59.99999999999997868, 6.624129181415079337 ) ) ;
#62050=CARTESIAN_POINT ( 'NONE',  ( -81.95665186865053897, -46.45865666940190408, 171.2074146399188237 ) ) ;
#62052=CARTESIAN_POINT ( 'NONE',  ( -10.38447319517632295, -0.000000000000000000, -13.52495681779584302 ) ) ;
#62055=EDGE_CURVE ( 'NONE', #51964, #26612, #675, .T. ) ;
#62062=CARTESIAN_POINT ( 'NONE',  ( -99.13865059541491576, -57.67127950436278638, 63.61738387431689290 ) ) ;
#62069=CARTESIAN_POINT ( 'NONE',  ( 60.74900604410193239, -14.21045842199440301, -29.98664384297035213 ) ) ;
#62070=CARTESIAN_POINT ( 'NONE',  ( -59.93215762506982713, -30.00000000000009592, 91.51900601851320971 ) ) ;
#62071=CARTESIAN_POINT ( 'NONE',  ( -56.07191290525906879, -49.91320329917822107, 67.05920270483053969 ) ) ;
#62075=CARTESIAN_POINT ( 'NONE',  ( -101.2319481900598106, -52.72902908576037362, 193.1221610425403412 ) ) ;
#62084=CARTESIAN_POINT ( 'NONE',  ( 69.72280996538995623, -30.00000000000000711, 94.43922800780518401 ) ) ;
#62088=CARTESIAN_POINT ( 'NONE',  ( -29.32136198015045281, -56.86423622103713882, 35.94540326096643668 ) ) ;
#62091=CARTESIAN_POINT ( 'NONE',  ( 47.74913715125470048, -29.14591046249990924, 44.14729050338506511 ) ) ;
#62096=CARTESIAN_POINT ( 'NONE',  ( -87.23646927575083510, -38.58587952222158179, 199.6458570365388141 ) ) ;
#62098=CARTESIAN_POINT ( 'NONE',  ( 91.43959331831491966, -38.37791452498228040, -4.964256820052830754 ) ) ;
#62107=CARTESIAN_POINT ( 'NONE',  ( 111.2609372169454502, -60.00000000000000711, 185.9044869507005160 ) ) ;
#62117=CARTESIAN_POINT ( 'NONE',  ( -108.9786437150107332, -38.35638155208228994, 190.2319024447106699 ) ) ;
#62128=CARTESIAN_POINT ( 'NONE',  ( 83.79296793638981455, -35.97364189524810740, 171.8120904271870018 ) ) ;
#62141=CARTESIAN_POINT ( 'NONE',  ( -76.69088380834561747, -29.99999999999999645, -16.87249134269979578 ) ) ;
#62168=CARTESIAN_POINT ( 'NONE',  ( -108.5578913194906931, -60.00000000000000711, 194.6075768431653330 ) ) ;
#62173=CARTESIAN_POINT ( 'NONE',  ( -83.57352743474167767, -42.98438523098171515, 179.4517796046237095 ) ) ;
#62182=CARTESIAN_POINT ( 'NONE',  ( -86.18221325923798304, -60.14546413765744859, 16.47069715629995557 ) ) ;
#62190=CARTESIAN_POINT ( 'NONE',  ( 102.0109750195309175, -30.00000000000007816, 198.2012210982776708 ) ) ;
#62193=CARTESIAN_POINT ( 'NONE',  ( -98.75680450758818552, -14.21045842199431064, 105.0421542466116023 ) ) ;
#62194=CARTESIAN_POINT ( 'NONE',  ( -64.12976986942591395, -32.53224925924665456, 80.08508429969118936 ) ) ;
#62196=CARTESIAN_POINT ( 'NONE',  ( 91.59609553898350498, -30.00000000000011013, 199.7677339052814602 ) ) ;
#62198=CARTESIAN_POINT ( 'NONE',  ( 46.36952623917631655, -60.00000000001961098, 69.16733414759707443 ) ) ;
#62209=CARTESIAN_POINT ( 'NONE',  ( -82.63119616871206574, -59.99999999999995737, -26.28467615004301194 ) ) ;
#62213=CARTESIAN_POINT ( 'NONE',  ( 1.650803255657546709, -4.285714285714293581, 25.22241582816891636 ) ) ;
#62222=CARTESIAN_POINT ( 'NONE',  ( 35.05802874304034589, -46.42926842311833013, 36.68586914177578961 ) ) ;
#62238=CARTESIAN_POINT ( 'NONE',  ( 92.58558766009146268, -60.00000000000001421, -2.558238702422552802 ) ) ;
#62245=CARTESIAN_POINT ( 'NONE',  ( -90.93883295786046972, -30.00000000000355271, 199.4788298540976257 ) ) ;
#62249=CARTESIAN_POINT ( 'NONE',  ( 83.69130407765804591, -52.73017012645138379, -15.75844283506252097 ) ) ;
#62257=CARTESIAN_POINT ( 'NONE',  ( 80.74191332831607326, -25.62223386318168039, 135.9007221451898033 ) ) ;
#62263=CARTESIAN_POINT ( 'NONE',  ( -109.9801870187163644, -57.66844046886203756, 196.1568551196091903 ) ) ;
#62264=EDGE_CURVE ( 'NONE', #50990, #25464, #62605, .T. ) ;
#62272=CARTESIAN_POINT ( 'NONE',  ( -49.65412818270985440, -29.62131271632045326, 46.06396428430316803 ) ) ;
#62281=CARTESIAN_POINT ( 'NONE',  ( -53.91796304099374026, -29.20809689804048759, -34.29182838456584648 ) ) ;
#62282=CARTESIAN_POINT ( 'NONE',  ( -84.24486252583190549, -29.99999999999999645, 163.2080965712097509 ) ) ;
#62286=CARTESIAN_POINT ( 'NONE',  ( 83.72989002924066426, -57.54382900384099031, 201.5987905778323181 ) ) ;
#62287=CARTESIAN_POINT ( 'NONE',  ( 68.05335443350816149, -60.22836387010958958, -27.16755064673009201 ) ) ;
#62289=AXIS2_PLACEMENT_3D ( 'NONE', #41255, #74668, #49873 ) ;
#62292=CARTESIAN_POINT ( 'NONE',  ( -65.19869439566309666, -59.99999999999999289, 119.1295691880435896 ) ) ;
#62296=CARTESIAN_POINT ( 'NONE',  ( -86.28001627044659472, -24.64161911929981130, 181.9982194805413656 ) ) ;
#62311=CARTESIAN_POINT ( 'NONE',  ( 86.89874827037927218, -29.99999999999997868, -18.81865104787653920 ) ) ;
#62312=CARTESIAN_POINT ( 'NONE',  ( -80.67225572899188535, -22.15189889752034702, 132.4868695557189540 ) ) ;
#62316=CARTESIAN_POINT ( 'NONE',  ( 65.36663488618646056, -57.67974036715745001, 127.4738114322918392 ) ) ;
#62325=CIRCLE ( 'NONE', #101944, 1.999999999999998224 ) ;
#62335=CARTESIAN_POINT ( 'NONE',  ( -45.38252603333997826, -14.21045842199430354, 49.92404905378138125 ) ) ;
#62336=CARTESIAN_POINT ( 'NONE',  ( 24.52113603086038296, -29.04043804430480691, 29.86937766656776816 ) ) ;
#62344=CARTESIAN_POINT ( 'NONE',  ( 72.06187821828702056, -37.99999999999999289, -21.47593870486667811 ) ) ;
#62356=CARTESIAN_POINT ( 'NONE',  ( 81.28015307217464169, -29.99999999999999645, -0.2274418294518818218 ) ) ;
#62365=DIRECTION ( 'NONE',  ( 0.000000000000000000, 0.000000000000000000, -1.000000000000000000 ) ) ;
#62379=CARTESIAN_POINT ( 'NONE',  ( 63.78764792876993539, -32.53022072251602026, 79.11273379103411685 ) ) ;
#62382=CARTESIAN_POINT ( 'NONE',  ( -62.68570420933652798, -37.65611969153471961, -33.47651594426432808 ) ) ;
#62392=CARTESIAN_POINT ( 'NONE',  ( 85.78379958766628022, -57.44889651991635304, 192.9311378948322329 ) ) ;
#62401=CARTESIAN_POINT ( 'NONE',  ( -100.7581804555464373, -30.00000000000000355, 180.7064422284077807 ) ) ;
#62404=CARTESIAN_POINT ( 'NONE',  ( 13.25658586220136925, -57.67136151655925147, 41.68871071852922228 ) ) ;
#62414=CARTESIAN_POINT ( 'NONE',  ( -87.46061870122996140, -42.74219916028555843, 190.5714494835581831 ) ) ;
#62418=CARTESIAN_POINT ( 'NONE',  ( -12.57806496835559962, -53.40254179854935046, 32.85052738830435004 ) ) ;
#62419=CARTESIAN_POINT ( 'NONE',  ( -106.0619102637862312, -59.99999999999999289, 161.5357636300732338 ) ) ;
#62447=CARTESIAN_POINT ( 'NONE',  ( -89.26291111005475898, -59.99999999997328359, 204.3060666321922270 ) ) ;
#62449=CARTESIAN_POINT ( 'NONE',  ( 71.98594699884088755, -60.00000000001919176, -34.35552695216333063 ) ) ;
#62452=CARTESIAN_POINT ( 'NONE',  ( -99.06514666684596193, -59.99999999999997158, 60.62150588740050949 ) ) ;
#62453=CARTESIAN_POINT ( 'NONE',  ( 10.37487025158898568, -49.91581432402574592, 32.22216560970060328 ) ) ;
#62455=CARTESIAN_POINT ( 'NONE',  ( -49.01032723201429064, -39.52037656706556135, 49.15628037481865675 ) ) ;
#62457=ORIENTED_EDGE ( 'NONE', *, *, #94030, .T. ) ;
#62465=CARTESIAN_POINT ( 'NONE',  ( 89.20714034186237029, -30.00000000001022116, -14.16964046280356015 ) ) ;
#62470=CARTESIAN_POINT ( 'NONE',  ( 95.97260220087535743, -30.00000000000000000, 191.2893859301274802 ) ) ;
#62475=ORIENTED_EDGE ( 'NONE', *, *, #65205, .F. ) ;
#62477=CARTESIAN_POINT ( 'NONE',  ( 53.90771391880598884, -60.31426852269981254, 66.32011985641655372 ) ) ;
#62485=CARTESIAN_POINT ( 'NONE',  ( 93.35170594872228378, -38.49489428715083505, 201.1561598503145376 ) ) ;
#62487=CARTESIAN_POINT ( 'NONE',  ( 82.55926974371887184, -37.86161494215052414, 6.154721773108606797 ) ) ;
#62503=EDGE_CURVE ( 'NONE', #34393, #91694, #101338, .T. ) ;
#62510=CARTESIAN_POINT ( 'NONE',  ( -28.35997571216497803, -31.34280435441244705, 39.68179292875564101 ) ) ;
#62515=CARTESIAN_POINT ( 'NONE',  ( 84.23774194945092120, -42.97611175225988234, 182.9332601167417067 ) ) ;
#62518=CARTESIAN_POINT ( 'NONE',  ( 94.19143966283073155, -57.67257289481475624, 22.55042990271367032 ) ) ;
#62520=CARTESIAN_POINT ( 'NONE',  ( 0.000000000000000000, -30.00000000000000000, 0.000000000000000000 ) ) ;
#62525=CARTESIAN_POINT ( 'NONE',  ( 8.106211149174814778, -19.49056414931506609, 35.24334571562989282 ) ) ;
#62527=CARTESIAN_POINT ( 'NONE',  ( 45.42450008630215308, -28.44167713921813601, 40.52586451359788811 ) ) ;
#62541=CARTESIAN_POINT ( 'NONE',  ( -0.001430412024211547310, -34.58958055692348665, -32.65458004663561553 ) ) ;
#62551=CARTESIAN_POINT ( 'NONE',  ( -92.39013394304011229, -59.99999999999999289, 0.2848972956623299080 ) ) ;
#62558=CARTESIAN_POINT ( 'NONE',  ( -84.34656395696856634, -29.01820936530794626, 165.8801275300401983 ) ) ;
#62572=CARTESIAN_POINT ( 'NONE',  ( -91.26204144827082132, -57.66323380191850845, -20.53964676755072105 ) ) ;
#62579=CARTESIAN_POINT ( 'NONE',  ( 92.19440588371723777, -59.99999999999994316, -19.86251273113072102 ) ) ;
#62581=CARTESIAN_POINT ( 'NONE',  ( -67.91869938964059372, -14.21045842199436571, 108.3284777829519214 ) ) ;
#62582=CARTESIAN_POINT ( 'NONE',  ( -53.76999817631660505, -53.37993369322897763, 63.18917586708445810 ) ) ;
#62586=CARTESIAN_POINT ( 'NONE',  ( -102.5341287361919171, -60.18785315653154555, 193.5342851667064679 ) ) ;
#62597=CARTESIAN_POINT ( 'NONE',  ( 62.29946635938797783, -30.00000000000000000, 72.81714634848326284 ) ) ;
#62601=CARTESIAN_POINT ( 'NONE',  ( -27.93204256690871645, -25.58061032913567701, 30.03670486279004237 ) ) ;
#62604=CARTESIAN_POINT ( 'NONE',  ( 48.13035336012885779, -60.27851473694221340, 54.32458513865176286 ) ) ;
#62605=LINE ( 'NONE', #23218, #62824 ) ;
#62608=CARTESIAN_POINT ( 'NONE',  ( -110.8957197956460163, -38.35621571426651144, 177.5099108999381485 ) ) ;
#62610=CARTESIAN_POINT ( 'NONE',  ( 91.32895771670399654, -38.39937082712951621, -10.08704785443199192 ) ) ;
#62619=CARTESIAN_POINT ( 'NONE',  ( 89.19650734279991866, -59.99999999999997868, 201.7715613159374186 ) ) ;
#62629=CARTESIAN_POINT ( 'NONE',  ( -106.2913668757043268, -38.35584237662276763, 125.9193867242538403 ) ) ;
#62641=CARTESIAN_POINT ( 'NONE',  ( 83.47724775591717616, -35.99455235840694911, 168.8079037484727962 ) ) ;
#62660=CARTESIAN_POINT ( 'NONE',  ( -78.94292291836882214, -30.00000000000000711, -15.09795832904019264 ) ) ;
#62682=CARTESIAN_POINT ( 'NONE',  ( -109.7084241075396704, -60.00000000000000711, 141.1604396081787627 ) ) ;
#62688=CARTESIAN_POINT ( 'NONE',  ( -86.37231359403887154, -18.01014218771245723, 173.0452270788669580 ) ) ;
#62695=CARTESIAN_POINT ( 'NONE',  ( -86.14699410518059608, -60.14324746009915401, 13.86886434169398186 ) ) ;
#62701=CARTESIAN_POINT ( 'NONE',  ( 103.2152402541460248, -59.99999999999995026, 203.2731761476304655 ) ) ;
#62703=CARTESIAN_POINT ( 'NONE',  ( -99.06514666684596193, -59.99999999999997158, 60.62150588740050949 ) ) ;
#62704=CARTESIAN_POINT ( 'NONE',  ( -65.47023038585730603, -22.10278188241376895, 78.54803145069421078 ) ) ;
#62707=CARTESIAN_POINT ( 'NONE',  ( 95.58593148621761770, -60.00000000000116529, 204.9903296923171467 ) ) ;
#62718=CARTESIAN_POINT ( 'NONE',  ( -92.33664849472602043, -60.00000000000000000, 0.9840071046490757034 ) ) ;
#62724=CARTESIAN_POINT ( 'NONE',  ( 2.500000000000000444, -30.00000000000000000, 14.79019945774903810 ) ) ;
#62733=CARTESIAN_POINT ( 'NONE',  ( 33.72764780035902277, -49.89708627978800592, 36.63738911784905383 ) ) ;
#62734=CARTESIAN_POINT ( 'NONE',  ( 17.78317311658683408, 9.642355526980000143E-13, 13.66642973271509831 ) ) ;
#62746=VERTEX_POINT ( 'NONE', #64600 ) ;
#62747=CARTESIAN_POINT ( 'NONE',  ( 91.87505181909152441, -60.00000000000001421, 10.10118637906101213 ) ) ;
#62754=CARTESIAN_POINT ( 'NONE',  ( -82.30107582774267883, -30.00000000000000000, 147.8409899216399310 ) ) ;
#62773=CARTESIAN_POINT ( 'NONE',  ( 76.55139626907627814, -60.31021925763745628, 145.8034420760990315 ) ) ;
#62780=CARTESIAN_POINT ( 'NONE',  ( -91.62307993511501536, -57.61497437271354727, 204.2871689995596967 ) ) ;
#62797=CARTESIAN_POINT ( 'NONE',  ( 2.500000000000002665, -30.00000000000000000, -13.00000000000000000 ) ) ;
#62801=CARTESIAN_POINT ( 'NONE',  ( -64.65451142056612355, -30.13026884046936971, -31.58747142994624824 ) ) ;
#62802=CARTESIAN_POINT ( 'NONE',  ( -84.24488595034571858, -30.00000000000000000, 163.2083109249410597 ) ) ;
#62807=CARTESIAN_POINT ( 'NONE',  ( 91.21542037083939647, -57.61349364694762443, 204.2098944395803812 ) ) ;
#62808=CARTESIAN_POINT ( 'NONE',  ( 64.94639244015790780, -34.58951604102425392, -23.72275273821461994 ) ) ;
#62813=CARTESIAN_POINT ( 'NONE',  ( -50.51290784178923587, -59.99999999999999289, 73.09413085601065063 ) ) ;
#62817=CARTESIAN_POINT ( 'NONE',  ( -85.80693792311036816, -39.24834306964363861, 186.3877018209399523 ) ) ;
#62824=VECTOR ( 'NONE', #97072, 1000.000000000000000 ) ;
#62832=CARTESIAN_POINT ( 'NONE',  ( -12.70248734012553804, -4.285714285715715555, -22.03900363279001340 ) ) ;
#62834=CARTESIAN_POINT ( 'NONE',  ( 95.18118770502717041, -60.00000000000013500, -7.509903379402337542 ) ) ;
#62835=CARTESIAN_POINT ( 'NONE',  ( -79.65920824261152688, -36.03009231341933116, 140.1419517927330389 ) ) ;
#62840=CARTESIAN_POINT ( 'NONE',  ( 71.69458925131347371, -57.67877169993052178, 168.9530237613620045 ) ) ;
#62865=CARTESIAN_POINT ( 'NONE',  ( -57.26243271903199172, -29.99999999999990763, 83.64903429017334702 ) ) ;
#62866=CARTESIAN_POINT ( 'NONE',  ( 28.82484700973959946, -60.33570494953415420, 36.38165799802252565 ) ) ;
#62870=CARTESIAN_POINT ( 'NONE',  ( -25.05982991920904368, -4.285714285714295357, -3.301565691951521053 ) ) ;
#62877=CARTESIAN_POINT ( 'NONE',  ( 56.58891463576402003, -29.99999999999996447, 58.99988038729124185 ) ) ;
#62881=CARTESIAN_POINT ( 'NONE',  ( 81.02036043352956085, -30.00000000000001066, 3.658347682202609974 ) ) ;
#62890=CARTESIAN_POINT ( 'NONE',  ( 80.00000000000000000, -52.00000000000000000, -21.09707704303352926 ) ) ;
#62899=CARTESIAN_POINT ( 'NONE',  ( 51.24056960644092840, -38.33573759255047975, 71.51432244761679158 ) ) ;
#62901=CARTESIAN_POINT ( 'NONE',  ( -80.72588694485581584, -60.00000000000002132, 180.8123989976356825 ) ) ;
#62902=CARTESIAN_POINT ( 'NONE',  ( 62.04802235831051149, -60.33937181082633572, 88.28494246272528301 ) ) ;
#62904=CARTESIAN_POINT ( 'NONE',  ( -0.01393140247697588312, -21.31702117966834109, -38.55283400289633278 ) ) ;
#62906=CARTESIAN_POINT ( 'NONE',  ( -45.81007331173236707, -34.56545578652658435, -36.77482165736895325 ) ) ;
#62913=CARTESIAN_POINT ( 'NONE',  ( -2.472961632485875860, -59.99999999999999289, -36.87415311768745596 ) ) ;
#62921=CARTESIAN_POINT ( 'NONE',  ( 86.73331853478092057, -42.79697935687362076, 189.5367378819176167 ) ) ;
#62923=DIRECTION ( 'NONE',  ( 0.000000000000000000, -1.000000000000000000, 0.000000000000000000 ) ) ;
#62931=CARTESIAN_POINT ( 'NONE',  ( -99.01130425066659768, -30.00000000000000355, 188.8065168094256592 ) ) ;
#62932=CARTESIAN_POINT ( 'NONE',  ( 40.76111137871845358, -57.69046583023251173, 56.94201171814951579 ) ) ;
#62944=CARTESIAN_POINT ( 'NONE',  ( -12.22075746324277468, -25.54981014065818457, 28.19739034840224789 ) ) ;
#62946=CARTESIAN_POINT ( 'NONE',  ( -105.5251249205886097, -60.00000000000000000, 154.7757544112112100 ) ) ;
#62954=CARTESIAN_POINT ( 'NONE',  ( 73.08871575436322132, -60.00000000000000000, 163.2694307510419094 ) ) ;
#62956=ORIENTED_EDGE ( 'NONE', *, *, #13511, .T. ) ;
#62967=EDGE_CURVE ( 'NONE', #49798, #31749, #15841, .T. ) ;
#62974=CARTESIAN_POINT ( 'NONE',  ( -100.2369946233466180, -59.99999999998519229, 204.3298598803837933 ) ) ;
#62976=CARTESIAN_POINT ( 'NONE',  ( 55.50171542583959194, -60.00000000000000000, 86.69625062228917045 ) ) ;
#62980=CARTESIAN_POINT ( 'NONE',  ( -102.0721909215208427, -14.21045842199424314, 125.2231725879975954 ) ) ;
#62981=CARTESIAN_POINT ( 'NONE',  ( 12.62289470629085919, -56.87776700476601377, 33.43110291409266921 ) ) ;
#62984=CARTESIAN_POINT ( 'NONE',  ( -48.95940874045572144, -42.98222722188957334, 50.18422616547311321 ) ) ;
#62997=CARTESIAN_POINT ( 'NONE',  ( 85.58605083099615740, -29.99999999999847944, 197.5044427888071823 ) ) ;
#63002=CARTESIAN_POINT ( 'NONE',  ( 97.25576257169278449, -30.00000000000000000, 190.9957396260108169 ) ) ;
#63011=CARTESIAN_POINT ( 'NONE',  ( -82.90940669858844103, -38.35712835889985683, -24.56897092220943080 ) ) ;
#63014=CARTESIAN_POINT ( 'NONE',  ( 105.2245759065473862, -38.38978177102808331, 197.2557521603409043 ) ) ;
#63016=CARTESIAN_POINT ( 'NONE',  ( 86.30570207415318862, -60.13085251795755681, 5.317764354392895854 ) ) ;
#63034=CARTESIAN_POINT ( 'NONE',  ( -44.64961496624998460, -29.90790381629714290, 54.34366819126163506 ) ) ;
#63038=CARTESIAN_POINT ( 'NONE',  ( 85.33851620155638784, -39.31096730626728686, 184.9291323951870822 ) ) ;
#63043=CARTESIAN_POINT ( 'NONE',  ( 94.12096428010207205, -57.67269879928694820, 21.37994873513087057 ) ) ;
#63051=CARTESIAN_POINT ( 'NONE',  ( 49.55824609672842485, -29.60162563601594599, 45.91477733028057173 ) ) ;
#63063=CARTESIAN_POINT ( 'NONE',  ( -93.54323754964579507, -37.99999999999998579, 99.16270155519150364 ) ) ;
#63070=CARTESIAN_POINT ( 'NONE',  ( -34.70505231949518077, -34.58949826982289011, -30.29862454714900011 ) ) ;
#63077=CARTESIAN_POINT ( 'NONE',  ( -91.70092392707927331, -60.00000000000000711, -15.05504486430357325 ) ) ;
#63082=LINE ( 'NONE', #37246, #21666 ) ;
#63085=CARTESIAN_POINT ( 'NONE',  ( -83.69471021262442889, -29.06694036840339734, 159.7615962780223811 ) ) ;
#63087=CARTESIAN_POINT ( 'NONE',  ( -16.14659623658557308, 0.000000000000000000, 5.483224646664452528 ) ) ;
#63088=ORIENTED_EDGE ( 'NONE', *, *, #72763, .T. ) ;
#63095=FACE_OUTER_BOUND ( 'NONE', #78114, .T. ) ;
#63097=CARTESIAN_POINT ( 'NONE',  ( -81.37675186042847031, -57.51598868027654987, 200.0426579070166895 ) ) ;
#63102=CARTESIAN_POINT ( 'NONE',  ( 84.89432107329884047, -60.00000000000002132, -27.59204247542200505 ) ) ;
#63104=CARTESIAN_POINT ( 'NONE',  ( -74.04808884210443409, -14.21045842199433018, 133.5060932470338741 ) ) ;
#63105=CARTESIAN_POINT ( 'NONE',  ( -54.51511722965400253, -46.44099520825000127, 62.03887026768623514 ) ) ;
#63109=CARTESIAN_POINT ( 'NONE',  ( -99.29800454330434434, -37.79210113977332952, 191.5838778425412841 ) ) ;
#63114=CARTESIAN_POINT ( 'NONE',  ( 91.46570115715213944, -38.37904828772288823, -5.692861098220960869 ) ) ;
#63127=CARTESIAN_POINT ( 'NONE',  ( -27.18296926593496110, -36.00581825497734911, 31.66575979565292087 ) ) ;
#63130=CARTESIAN_POINT ( 'NONE',  ( 47.66081387494537580, -46.44007846935294026, 49.24185928217620756 ) ) ;
#63134=CARTESIAN_POINT ( 'NONE',  ( -110.8469737611757324, -38.35618416066114378, 166.6374178958760410 ) ) ;
#63137=CARTESIAN_POINT ( 'NONE',  ( 91.27230094422854734, -38.36276317364043109, -1.771946917198911731 ) ) ;
#63148=CARTESIAN_POINT ( 'NONE',  ( 81.71125754684067033, -59.99999999999998579, 197.8273229994767064 ) ) ;
#63153=CARTESIAN_POINT ( 'NONE',  ( 58.43184352567574535, -49.90951488237450206, 72.98920087071743978 ) ) ;
#63159=CARTESIAN_POINT ( 'NONE',  ( -106.9302167770077432, -38.36496539244966186, 194.9700385483175467 ) ) ;
#63170=CARTESIAN_POINT ( 'NONE',  ( 85.49456200365183633, -21.96913521486521859, 166.0344729825741581 ) ) ;
#63178=CYLINDRICAL_SURFACE ( 'NONE', #10698, 7.499999999992679633 ) ;
#63184=CARTESIAN_POINT ( 'NONE',  ( -80.77589227446330256, -30.00000000000000000, 10.05485495590529688 ) ) ;
#63188=CARTESIAN_POINT ( 'NONE',  ( -0.4504275197381015783, -18.03418682189721878, 35.00556608437873507 ) ) ;
#63211=UNCERTAINTY_MEASURE_WITH_UNIT (LENGTH_MEASURE( 1.000000000000000082E-05 ), #27598, 'distance_accuracy_value', 'NONE');
#63212=CARTESIAN_POINT ( 'NONE',  ( -112.2209848136311052, -60.00000000000000000, 174.8538164149834699 ) ) ;
#63219=CARTESIAN_POINT ( 'NONE',  ( -83.54734737942287381, -50.12438367015052165, 185.4795622266105113 ) ) ;
#63227=CARTESIAN_POINT ( 'NONE',  ( -86.75379648495294305, -60.15014714565931797, 26.71264858234389195 ) ) ;
#63231=FACE_OUTER_BOUND ( 'NONE', #48271, .T. ) ;
#63233=CARTESIAN_POINT ( 'NONE',  ( 112.2652136917531465, -60.00000000000000000, 191.8488956690686962 ) ) ;
#63235=CARTESIAN_POINT ( 'NONE',  ( -103.2297580319645220, -60.00000000000001421, 85.94764253490394879 ) ) ;
#63236=CARTESIAN_POINT ( 'NONE',  ( -64.80909832733323128, -32.53232063311292421, 82.02485752868588520 ) ) ;
#63237=ORIENTED_EDGE ( 'NONE', *, *, #35634, .F. ) ;
#63239=CARTESIAN_POINT ( 'NONE',  ( 75.83101594479042262, -60.00000000000735412, 194.1828841934077730 ) ) ;
#63250=CARTESIAN_POINT ( 'NONE',  ( -2.798807412529719763, -60.00000000000002132, -42.63907750795410578 ) ) ;
#63257=CARTESIAN_POINT ( 'NONE',  ( 89.99999999999997158, -60.00000000000000000, 196.0238439516549818 ) ) ;
#63265=CARTESIAN_POINT ( 'NONE',  ( 36.01760793315731490, -22.19405214988617203, 32.43296674126499823 ) ) ;
#63266=CARTESIAN_POINT ( 'NONE',  ( -16.57301948836873251, -1.734723475976807094E-15, -4.453875240786733691 ) ) ;
#63279=CARTESIAN_POINT ( 'NONE',  ( 98.00335581387979289, -60.00000000000000000, 68.94697347453431746 ) ) ;
#63285=CARTESIAN_POINT ( 'NONE',  ( -59.74861173715120088, -29.99999999999999289, 66.22430673131081846 ) ) ;
#63292=CARTESIAN_POINT ( 'NONE',  ( 83.48762353522853630, -52.72806324350694496, -16.05720600496736949 ) ) ;
#63305=CARTESIAN_POINT ( 'NONE',  ( 82.19508700470152007, -18.68693059907149490, 137.0968519703368713 ) ) ;
#63313=CARTESIAN_POINT ( 'NONE',  ( -35.73279548032036956, -57.69589661319782437, 49.90756511973714282 ) ) ;
#63325=CARTESIAN_POINT ( 'NONE',  ( -32.55262149376069658, -22.90611988631381024, 32.69735316556134563 ) ) ;
#63328=ADVANCED_FACE ( 'NONE', ( #81953 ), #65795, .T. ) ;
#63331=B_SPLINE_CURVE_WITH_KNOTS ( 'NONE', 3,
 ( #98788, #56737, #82078, #73450, #33042, #57798, #1140, #32510 ),
 .UNSPECIFIED., .F., .F.,
 ( 4, 2, 2, 4 ),
 ( 0.4104551234109616309, 0.4139675920961696232, 0.4174800607813775599, 0.4245049981517935445 ),
 .UNSPECIFIED. ) ;
#63340=CARTESIAN_POINT ( 'NONE',  ( -70.52629063140332732, -29.99999999999998579, -20.46674107074536053 ) ) ;
#63341=CARTESIAN_POINT ( 'NONE',  ( -69.41254636990348104, -30.00000000000000355, 93.44164650999076116 ) ) ;
#63345=CARTESIAN_POINT ( 'NONE',  ( 91.34176007303615563, -57.61388464028566148, 204.2308622945469949 ) ) ;
#63346=CARTESIAN_POINT ( 'NONE',  ( 71.72532340997096867, -34.58959646309544667, -21.02624987897744901 ) ) ;
#63351=CARTESIAN_POINT ( 'NONE',  ( -73.50359396478988572, -60.00000000000000000, 167.2255443349855000 ) ) ;
#63358=CARTESIAN_POINT ( 'NONE',  ( -84.96685468468123759, -50.19859687476371590, 189.1434212840244697 ) ) ;
#63373=( NAMED_UNIT ( * ) PLANE_ANGLE_UNIT ( ) SI_UNIT ( $, .RADIAN. ) );
#63376=CARTESIAN_POINT ( 'NONE',  ( 94.21214616282756538, -60.00000000000006395, 9.573485886066015027 ) ) ;
#63377=CARTESIAN_POINT ( 'NONE',  ( -81.43623979954335823, -29.09389058366499370, 143.4191690805281212 ) ) ;
#63379=( NAMED_UNIT ( * ) SI_UNIT ( $, .STERADIAN. ) SOLID_ANGLE_UNIT ( ) );
#63381=CARTESIAN_POINT ( 'NONE',  ( 104.6988950438752255, -57.64257840656350140, 201.8919179864889770 ) ) ;
#63392=CARTESIAN_POINT ( 'NONE',  ( -102.8019275820111602, -52.71028098699141395, 142.0411747293566407 ) ) ;
#63397=AXIS2_PLACEMENT_3D ( 'NONE', #43490, #66696, #75848 ) ;
#63404=CARTESIAN_POINT ( 'NONE',  ( -31.98280533637225176, -29.99999999999996447, 41.00520926490388263 ) ) ;
#63405=CARTESIAN_POINT ( 'NONE',  ( 25.57206085308608223, -25.56680585492497926, 29.49300859707019740 ) ) ;
#63419=CARTESIAN_POINT ( 'NONE',  ( 40.45747091539019635, -59.99999999999999289, -39.57904950317593062 ) ) ;
#63420=CARTESIAN_POINT ( 'NONE',  ( 86.82001826315290316, -29.99999999999992184, 183.0449992333263936 ) ) ;
#63423=CARTESIAN_POINT ( 'NONE',  ( 73.73040302543078894, -29.99999999999999645, -18.77833202125217582 ) ) ;
#63443=CARTESIAN_POINT ( 'NONE',  ( 61.71159894698526216, -60.33950585225007046, 87.28437287168905812 ) ) ;
#63447=CARTESIAN_POINT ( 'NONE',  ( -52.90880457622053257, -36.17226545501620905, -35.66381235367310865 ) ) ;
#63459=CARTESIAN_POINT ( 'NONE',  ( 86.81267294504679910, -42.78936011489643931, 189.6631950169049219 ) ) ;
#63467=CARTESIAN_POINT ( 'NONE',  ( 35.82122592925417592, -60.00000000000000000, 47.16707035416197868 ) ) ;
#63468=CARTESIAN_POINT ( 'NONE',  ( -98.35766590278744559, -30.00000000000000355, 140.0735935797200682 ) ) ;
#63471=CARTESIAN_POINT ( 'NONE',  ( 41.51254023491689082, -57.68873884886530590, 58.24736279105339776 ) ) ;
#63477=CARTESIAN_POINT ( 'NONE',  ( -14.57895281699998513, -60.00000000000000000, 39.77189858658603328 ) ) ;
#63480=CARTESIAN_POINT ( 'NONE',  ( -87.19698863470328831, -46.43428023365913759, 191.1401204188958900 ) ) ;
#63483=CARTESIAN_POINT ( 'NONE',  ( -14.50479935719362956, -35.99470073277952054, 30.00759979546209522 ) ) ;
#63485=CARTESIAN_POINT ( 'NONE',  ( -86.75607522730589949, -59.99999999999997158, 27.04728030040551445 ) ) ;
#63493=CARTESIAN_POINT ( 'NONE',  ( 73.51685685884034172, -60.00000000000000711, 167.3565946372449957 ) ) ;
#63498=CARTESIAN_POINT ( 'NONE',  ( 46.52147948847155590, -60.00000000000000000, 69.35914673975356948 ) ) ;
#63501=VERTEX_POINT ( 'NONE', #11790 ) ;
#63512=CARTESIAN_POINT ( 'NONE',  ( -109.7149502225919377, -60.00000000005858425, 124.6291749562062989 ) ) ;
#63514=CARTESIAN_POINT ( 'NONE',  ( 77.22884141242977307, -60.00000000000002132, 191.0907396958321272 ) ) ;
#63518=CARTESIAN_POINT ( 'NONE',  ( -105.9103127569300966, -29.99999999999996092, 132.9890815309780123 ) ) ;
#63519=CARTESIAN_POINT ( 'NONE',  ( 10.15756363273992591, -29.02955213285231295, 28.73800426594050350 ) ) ;
#63521=CARTESIAN_POINT ( 'NONE',  ( 86.44549218974457006, -37.99999999999996447, 55.87897762973370419 ) ) ;
#63522=CARTESIAN_POINT ( 'NONE',  ( -47.00724124947766569, -49.90210803779500282, 49.27523530523148310 ) ) ;
#63534=CARTESIAN_POINT ( 'NONE',  ( 79.37892552202683305, -30.00000000001325162, 188.6526249938534647 ) ) ;
#63538=CARTESIAN_POINT ( 'NONE',  ( 99.39107893597980592, -30.00000000000000355, 187.8633685902540833 ) ) ;
#63555=CARTESIAN_POINT ( 'NONE',  ( 103.1879948328108867, -38.42420025606666911, 198.9909334126319891 ) ) ;
#63557=CARTESIAN_POINT ( 'NONE',  ( 87.03046627057608475, -60.19227689608176490, -6.658524423245185453 ) ) ;
#63558=CARTESIAN_POINT ( 'NONE',  ( 58.09934139907505113, -38.00000000000000000, 66.71623766452258053 ) ) ;
#63577=DIRECTION ( 'NONE',  ( 0.000000000000000000, -1.000000000000000000, 0.000000000000000000 ) ) ;
#63579=CARTESIAN_POINT ( 'NONE',  ( -7.032460429402416224, -15.50966336658045819, 34.57368686681926562 ) ) ;
#63582=CARTESIAN_POINT ( 'NONE',  ( 85.87277015767610067, -32.01287046823524207, 183.1770543038046526 ) ) ;
#63588=CARTESIAN_POINT ( 'NONE',  ( 94.41251621664974891, -57.67095265337347598, -0.3265171029545638759 ) ) ;
#63607=CARTESIAN_POINT ( 'NONE',  ( -82.49874227244829683, -38.00000000000002842, 7.946081593716382230 ) ) ;
#63612=CARTESIAN_POINT ( 'NONE',  ( -10.98135972349570721, -16.40382455065010703, -34.73165818216984491 ) ) ;
#63614=CARTESIAN_POINT ( 'NONE',  ( -59.93268390808485435, -47.40894763362151565, -27.52547626314329321 ) ) ;
#63623=CARTESIAN_POINT ( 'NONE',  ( -92.60969381247451793, -60.00000000000000000, -10.21457394295196863 ) ) ;
#63627=CARTESIAN_POINT ( 'NONE',  ( 101.2899080087397437, -60.24371164881011964, 194.9002588125513284 ) ) ;
#63630=CARTESIAN_POINT ( 'NONE',  ( -84.35902549046055299, -25.57579481131011079, 160.3285692841058676 ) ) ;
#63641=CARTESIAN_POINT ( 'NONE',  ( -80.45353917958989598, -57.50988970295517788, 199.2734438750461550 ) ) ;
#63646=CARTESIAN_POINT ( 'NONE',  ( 89.98361085880227961, -30.00000000000001776, -2.850603255620693055 ) ) ;
#63647=CARTESIAN_POINT ( 'NONE',  ( -71.62990520600911282, -30.00000000000002842, 135.6731032779996156 ) ) ;
#63648=CARTESIAN_POINT ( 'NONE',  ( -53.04679035957766331, -60.31687344103399084, 64.32401062991868912 ) ) ;
#63649=CIRCLE ( 'NONE', #17148, 7.500000000001509015 ) ;
#63653=CARTESIAN_POINT ( 'NONE',  ( -100.3133252052276561, -45.25861041073478219, 192.2763107763641983 ) ) ;
#63658=CARTESIAN_POINT ( 'NONE',  ( 110.9222412389008667, -38.35615538830503368, 167.0140503051813141 ) ) ;
#63671=CARTESIAN_POINT ( 'NONE',  ( 49.35569166775938044, -53.36311280355247533, 54.26082778344028412 ) ) ;
#63675=CARTESIAN_POINT ( 'NONE',  ( -110.9162687472649225, -38.35621414700798226, 168.5475671580575465 ) ) ;
#63678=CARTESIAN_POINT ( 'NONE',  ( 86.87566845558653483, -38.36515140496537413, -20.99884072241187383 ) ) ;
#63682=CARTESIAN_POINT ( 'NONE',  ( 95.54615038124083526, -52.71697105530865457, 96.31251485201036644 ) ) ;
#63689=CARTESIAN_POINT ( 'NONE',  ( 92.16328301628017527, -60.00000000000002132, 202.3748522514294450 ) ) ;
#63692=CARTESIAN_POINT ( 'NONE',  ( 57.09500382191800583, -60.32684846654004929, 74.31043819818451368 ) ) ;
#63696=AXIS2_PLACEMENT_3D ( 'NONE', #2452, #101160, #58585 ) ;
#63699=CARTESIAN_POINT ( 'NONE',  ( -109.5143122852008446, -38.35607115667316691, 149.0097679660275674 ) ) ;
#63710=CARTESIAN_POINT ( 'NONE',  ( 83.53591657301284101, -39.46790697894184774, 174.7263257596978576 ) ) ;
#63727=CARTESIAN_POINT ( 'NONE',  ( -0.04262759816315875305, -18.02988087835976927, 35.00498014658149515 ) ) ;
#63746=CARTESIAN_POINT ( 'NONE',  ( -110.1395483373692912, -60.00000000000000000, 144.5712075343598713 ) ) ;
#63751=CARTESIAN_POINT ( 'NONE',  ( -83.03303802707752368, -46.50676638669730067, 179.9281315098355947 ) ) ;
#63757=CARTESIAN_POINT ( 'NONE',  ( -84.06247081757707917, -45.26549463277890339, 23.57487689052427982 ) ) ;
#63764=CARTESIAN_POINT ( 'NONE',  ( 104.4175052224803864, -30.00000000000007105, 196.2185630211469629 ) ) ;
#63766=CARTESIAN_POINT ( 'NONE',  ( -89.60210353745294753, -14.21045842199431597, 48.51666376363581890 ) ) ;
#63768=CARTESIAN_POINT ( 'NONE',  ( -62.79330346830408160, -42.96297999032424286, 81.57255440324702533 ) ) ;
#63771=CARTESIAN_POINT ( 'NONE',  ( 92.02246887588820812, -59.99999999997538680, 204.8145644407424584 ) ) ;
#63773=CARTESIAN_POINT ( 'NONE',  ( 3.091518739326764464, -60.35886547126050772, 33.94409813261457032 ) ) ;
#63782=CARTESIAN_POINT ( 'NONE',  ( -111.4049543193486329, -60.00000000000000000, 185.1671540497623880 ) ) ;
#63793=CARTESIAN_POINT ( 'NONE',  ( 99.65386729655308784, -60.00000000000000000, 195.9220411359386560 ) ) ;
#63794=CARTESIAN_POINT ( 'NONE',  ( -37.34066781863991480, -46.43450374261344393, 38.17834207212992226 ) ) ;
#63797=CARTESIAN_POINT ( 'NONE',  ( 38.65958381579444136, -29.13907093716015950, 35.42191563165732049 ) ) ;
#63798=CARTESIAN_POINT ( 'NONE',  ( 22.23822744035697241, -8.673617379884035472E-16, 2.910977163136220014 ) ) ;
#63802=CARTESIAN_POINT ( 'NONE',  ( -74.13051718845747473, -38.32750755219241512, 161.4754845552919278 ) ) ;
#63809=CARTESIAN_POINT ( 'NONE',  ( 2.500000000000000444, -30.00000000000000000, 28.88619651857252535 ) ) ;
#63813=CARTESIAN_POINT ( 'NONE',  ( 93.34451349968284717, -59.99999999999999289, 35.61397960305716026 ) ) ;
#63818=CARTESIAN_POINT ( 'NONE',  ( -85.26311336406097041, -29.99999999999986855, 172.8326700376237284 ) ) ;
#63834=CARTESIAN_POINT ( 'NONE',  ( 83.49039785751061515, -22.14967886183166712, 148.6536833251738585 ) ) ;
#63840=CARTESIAN_POINT ( 'NONE',  ( -28.75444143438830835, -57.68095489456369762, 44.62365432283354494 ) ) ;
#63854=CARTESIAN_POINT ( 'NONE',  ( -10.85562601347594658, -13.98149544789687759, 31.85028796763797487 ) ) ;
#63860=SHAPE_DEFINITION_REPRESENTATION ( #95797, #16335 ) ;
#63869=CARTESIAN_POINT ( 'NONE',  ( -43.16790182456753655, -33.90049227214078087, -37.13562304484096899 ) ) ;
#63875=CARTESIAN_POINT ( 'NONE',  ( 91.97123957640626202, -57.61548619320129916, 204.3264942780886884 ) ) ;
#63876=CARTESIAN_POINT ( 'NONE',  ( 58.42741290352864780, -21.77006730897359787, -23.50884316932007678 ) ) ;
#63881=CARTESIAN_POINT ( 'NONE',  ( -73.23784728930272081, -60.00000000000000711, 164.6514032014629265 ) ) ;
#63885=CARTESIAN_POINT ( 'NONE',  ( -83.83620841830486370, -61.03244567992550174, 192.0783191055589327 ) ) ;
#63892=FACE_OUTER_BOUND ( 'NONE', #81136, .T. ) ;
#63903=CARTESIAN_POINT ( 'NONE',  ( 90.08848753752288019, -30.00000000000005684, -9.081672415796756326 ) ) ;
#63905=CARTESIAN_POINT ( 'NONE',  ( -78.93788605875903386, -39.49883670821371595, 139.5007675430211123 ) ) ;
#63906=ORIENTED_EDGE ( 'NONE', *, *, #84476, .F. ) ;
#63907=CARTESIAN_POINT ( 'NONE',  ( 40.90273407096766078, -60.00000000000019185, 57.82174102673914007 ) ) ;
#63909=CARTESIAN_POINT ( 'NONE',  ( 76.72290838289761439, -57.52930957181557403, 194.6109501198345413 ) ) ;
#63917=CARTESIAN_POINT ( 'NONE',  ( -106.3498447864860736, -60.15519976726687901, 165.8917114895338329 ) ) ;
#63926=ORIENTED_EDGE ( 'NONE', *, *, #2696, .F. ) ;
#63929=CARTESIAN_POINT ( 'NONE',  ( 27.52884087114259160, -60.34135499268811031, 35.96017823446348416 ) ) ;
#63940=EDGE_CURVE ( 'NONE', #90543, #38839, #104269, .T. ) ;
#63943=CARTESIAN_POINT ( 'NONE',  ( 47.48558071520947976, -60.00000000000001421, -38.38385089910498493 ) ) ;
#63944=CARTESIAN_POINT ( 'NONE',  ( 81.45724438388656097, -29.99999999999998224, 142.5290932105678792 ) ) ;
#63970=CARTESIAN_POINT ( 'NONE',  ( 62.36095931845834173, -49.91109934801575321, 83.85664639578627089 ) ) ;
#63986=B_SPLINE_CURVE_WITH_KNOTS ( 'NONE', 3,
 ( #67434, #35623, #101389, #19453, #27540, #10237 ),
 .UNSPECIFIED., .F., .F.,
 ( 4, 2, 4 ),
 ( 0.4253311034033953608, 0.4347571302760012690, 0.4441831571486072328 ),
 .UNSPECIFIED. ) ;
#63989=CARTESIAN_POINT ( 'NONE',  ( 86.89651759348157611, -28.03138314466304948, 186.5263926684410194 ) ) ;
#64002=CARTESIAN_POINT ( 'NONE',  ( 17.20669968485552559, -60.00000000000000000, 39.93835234338625639 ) ) ;
#64003=CARTESIAN_POINT ( 'NONE',  ( -97.63590237861488674, -29.99999999999999645, 134.9849753005358934 ) ) ;
#64006=CARTESIAN_POINT ( 'NONE',  ( 52.15219236777184619, -57.67660669137886487, 83.12330646720228344 ) ) ;
#64013=CARTESIAN_POINT ( 'NONE',  ( -24.16062877281563459, -59.99999999999999289, 40.95735949052681235 ) ) ;
#64014=CARTESIAN_POINT ( 'NONE',  ( 2.386052322619232946, -15.44095796389983022, -35.20331376883997621 ) ) ;
#64015=CARTESIAN_POINT ( 'NONE',  ( -87.06507237377361719, -50.09467886413911231, 191.9848466096647428 ) ) ;
#64018=B_SPLINE_CURVE_WITH_KNOTS ( 'NONE', 3,
 ( #76632, #83138, #26022, #51287, #83652, #10303, #34630, #2741, #93369, #41620, #67499, #59415, #9235, #75576, #19521, #34098, #51823, #25474, #18979, #84738, #10821, #43743, #58330, #35696, #60490, #92277, #84207, #17363, #68571, #35150, #91254, #101456, #43218, #42679 ),
 .UNSPECIFIED., .F., .F.,
 ( 4, 2, 2, 2, 2, 2, 2, 2, 2, 2, 2, 2, 2, 2, 2, 2, 4 ),
 ( 0.000000000000000000, 0.03124999999999995143, 0.06249999999999990286, 0.09374999999999990286, 0.1249999999999999167, 0.1562499999999999167, 0.1874999999999999167, 0.2187499999999999445, 0.2499999999999999445, 0.2812499999999999445, 0.3124999999999999445, 0.3437499999999999445, 0.3749999999999999445, 0.4062500000000000000, 0.4375000000000000000, 0.4687500000000000000, 0.5000000000000000000 ),
 .UNSPECIFIED. ) ;
#64021=CARTESIAN_POINT ( 'NONE',  ( -12.48886971890022934, -46.43935809921794799, 31.68723845390683636 ) ) ;
#64022=CARTESIAN_POINT ( 'NONE',  ( -90.21012822187128677, -59.99999999999999289, 56.28790610766393598 ) ) ;
#64031=CARTESIAN_POINT ( 'NONE',  ( 65.82730706677887156, -60.00000000000000711, 121.6744210731262825 ) ) ;
#64034=CARTESIAN_POINT ( 'NONE',  ( 0.000000000000000000, 30.00000000000000000, 74.46152422706630603 ) ) ;
#64048=CARTESIAN_POINT ( 'NONE',  ( -113.9570076106580103, -59.99999999998043876, 158.2873460090529534 ) ) ;
#64050=CARTESIAN_POINT ( 'NONE',  ( 44.33732900979256897, -59.99999999999998579, 59.29852098770807345 ) ) ;
#64053=CARTESIAN_POINT ( 'NONE',  ( -106.8236106313706699, -14.21045842199435150, 178.1018237235793151 ) ) ;
#64054=CARTESIAN_POINT ( 'NONE',  ( 12.66751964286181575, -60.35877864777715018, 34.01265280193257468 ) ) ;
#64055=CARTESIAN_POINT ( 'NONE',  ( 99.93939408685974968, -38.00000000000001421, 190.7851520131013388 ) ) ;
#64056=DIRECTION ( 'NONE',  ( 0.000000000000000000, 1.000000000000000000, 0.000000000000000000 ) ) ;
#64057=CARTESIAN_POINT ( 'NONE',  ( -44.07123412536562057, -46.43995785254333697, 44.37406601753968260 ) ) ;
#64065=CARTESIAN_POINT ( 'NONE',  ( 2.500000000000002665, -17.75174924879615546, -25.82778434327287798 ) ) ;
#64071=CARTESIAN_POINT ( 'NONE',  ( 103.0665016853196363, -30.00000000000061462, 197.4198734183501358 ) ) ;
#64075=CARTESIAN_POINT ( 'NONE',  ( 87.07233282619432657, -30.00000000000000000, 70.95073359267735214 ) ) ;
#64089=CARTESIAN_POINT ( 'NONE',  ( 81.01023851859548586, -38.83486255393263775, 194.6255486919564532 ) ) ;
#64092=CARTESIAN_POINT ( 'NONE',  ( 85.62592449253092752, -52.72843542154268448, -2.857092586073228357 ) ) ;
#64093=CARTESIAN_POINT ( 'NONE',  ( 85.96116874757127846, -38.00000000000002842, 186.3684374995824271 ) ) ;
#64095=( NAMED_UNIT ( * ) PLANE_ANGLE_UNIT ( ) SI_UNIT ( $, .RADIAN. ) );
#64111=CARTESIAN_POINT ( 'NONE',  ( 0.9118253755784003767, -18.00287762888658349, 35.00125712497896302 ) ) ;
#64118=CARTESIAN_POINT ( 'NONE',  ( 86.09880483962514575, -24.81058578010869908, 180.0994920548855021 ) ) ;
#64121=CARTESIAN_POINT ( 'NONE',  ( 94.19131188920297859, -57.67257310899840661, 22.54837274470326847 ) ) ;
#64146=CARTESIAN_POINT ( 'NONE',  ( -40.94509419489318702, -34.58952987473475105, -29.39275092839041292 ) ) ;
#64151=CARTESIAN_POINT ( 'NONE',  ( -91.96355247515836595, -59.99999999999998579, -14.08785575593242889 ) ) ;
#64155=CARTESIAN_POINT ( 'NONE',  ( 99.71449018044667412, -52.77652230665619726, 194.3813892764564173 ) ) ;
#64158=CARTESIAN_POINT ( 'NONE',  ( -83.26220561033844092, -32.54356584210299985, 161.2381412266789198 ) ) ;
#64171=CARTESIAN_POINT ( 'NONE',  ( -108.6808209725780330, -57.66364365951052662, 198.1525503354515081 ) ) ;
#64177=CARTESIAN_POINT ( 'NONE',  ( -69.60683966046387638, -29.99999999999998224, -29.88974110699236775 ) ) ;
#64178=CARTESIAN_POINT ( 'NONE',  ( -31.71194513525783165, -14.21045842199430709, 37.70210531190891601 ) ) ;
#64179=CARTESIAN_POINT ( 'NONE',  ( -52.85655506056811959, -25.64035322949781914, 50.79863798127239249 ) ) ;
#64183=CARTESIAN_POINT ( 'NONE',  ( -98.26664012846288188, -37.73380340095903307, 192.3703194023427159 ) ) ;
#64188=CARTESIAN_POINT ( 'NONE',  ( 109.4076176909565845, -38.35605075573632661, 188.6800926733125152 ) ) ;
#64193=CARTESIAN_POINT ( 'NONE',  ( 82.85293946109428020, -30.00000000000000711, 151.7967064736782845 ) ) ;
#64202=CARTESIAN_POINT ( 'NONE',  ( 49.26203278476850755, -42.97728400714042607, 50.67361426740096420 ) ) ;
#64206=CARTESIAN_POINT ( 'NONE',  ( -110.4362257262843059, -38.35609804039832227, 182.9338296351233168 ) ) ;
#64208=CARTESIAN_POINT ( 'NONE',  ( 84.80912723296837896, -38.35879924987171563, -23.01720600995700750 ) ) ;
#64212=CARTESIAN_POINT ( 'NONE',  ( 104.1878238513955353, -52.71701965651387667, 153.9813814288278593 ) ) ;
#64218=CARTESIAN_POINT ( 'NONE',  ( 96.44948892551855124, -60.00000000000000711, 202.5258697066679758 ) ) ;
#64222=CARTESIAN_POINT ( 'NONE',  ( 57.23890203722747572, -42.96409028050587864, 66.85176157112299222 ) ) ;
#64227=CARTESIAN_POINT ( 'NONE',  ( -107.6099443991786444, -38.36026800758562416, 193.7261362466381343 ) ) ;
#64236=CARTESIAN_POINT ( 'NONE',  ( 84.32059328291249756, -32.45894075901123443, 171.3683495658556524 ) ) ;
#64255=CARTESIAN_POINT ( 'NONE',  ( -4.625902140663016304, -18.51163087806139629, 35.07735223482339393 ) ) ;
#64276=CARTESIAN_POINT ( 'NONE',  ( -111.9595133392371622, -60.00000000000000711, 163.3268968678650594 ) ) ;
#64282=CARTESIAN_POINT ( 'NONE',  ( -82.22570924946400339, -53.55338277734435337, 182.7255397530098833 ) ) ;
#64293=CARTESIAN_POINT ( 'NONE',  ( 106.9545358495978036, -14.21045842199422715, 174.0142581296349249 ) ) ;
#64294=CARTESIAN_POINT ( 'NONE',  ( -96.66672766003948425, -59.99999999999999289, 43.67975107286704883 ) ) ;
#64295=CARTESIAN_POINT ( 'NONE',  ( -63.30547496605215230, -29.05771995010201536, 76.03326579632651772 ) ) ;
#64298=CARTESIAN_POINT ( 'NONE',  ( 70.10167902634712789, -59.99999999999998579, 157.8050041458824353 ) ) ;
#64299=ORIENTED_EDGE ( 'NONE', *, *, #64705, .T. ) ;
#64311=CARTESIAN_POINT ( 'NONE',  ( -110.8662299446404518, -60.00000000000001421, 187.9351797466592018 ) ) ;
#64323=CARTESIAN_POINT ( 'NONE',  ( -33.29236794668833710, -53.37323687183614851, 37.05240020734890294 ) ) ;
#64327=CARTESIAN_POINT ( 'NONE',  ( 41.65387604968816504, -25.70000439954323213, 36.84591881860966822 ) ) ;
#64328=CARTESIAN_POINT ( 'NONE',  ( 16.57301948837260497, -3.469446951953614189E-15, -4.453875240779963107 ) ) ;
#64332=CARTESIAN_POINT ( 'NONE',  ( -57.76361387290374694, -38.34427059577949137, 89.53802776920677786 ) ) ;
#64342=CARTESIAN_POINT ( 'NONE',  ( 92.12568682370377360, -60.00000000000000000, 21.31078671776630529 ) ) ;
#64351=CARTESIAN_POINT ( 'NONE',  ( -68.83349455627663360, -30.00000000000000711, 91.58528215561763375 ) ) ;
#64365=CARTESIAN_POINT ( 'NONE',  ( 82.94231461304056552, -29.08498905877214824, 153.6257325888713581 ) ) ;
#64372=CARTESIAN_POINT ( 'NONE',  ( -62.53353137064869571, -57.67819947725070051, 116.5065130283015975 ) ) ;
#64381=CARTESIAN_POINT ( 'NONE',  ( -8.788806404158220786, -13.49444637299766114, 31.95348751068649662 ) ) ;
#64395=CARTESIAN_POINT ( 'NONE',  ( -58.94526255509084933, -30.00000000000000355, 64.40875316220729019 ) ) ;
#64400=CARTESIAN_POINT ( 'NONE',  ( 97.52685887306888901, -57.62337308210403819, 204.3890786062049187 ) ) ;
#64405=CARTESIAN_POINT ( 'NONE',  ( -74.91408771145276546, -60.00000000000002842, 180.6267571641686516 ) ) ;
#64409=CARTESIAN_POINT ( 'NONE',  ( -86.40356866038837325, -17.55479932359841655, 177.8634248572934382 ) ) ;
#64421=CARTESIAN_POINT ( 'NONE',  ( -82.25616362586248442, -37.78509365397592745, -13.24265913212705570 ) ) ;
#64424=ORIENTED_EDGE ( 'NONE', *, *, #91324, .F. ) ;
#64429=CARTESIAN_POINT ( 'NONE',  ( 87.24803233485737053, -14.21045842199430709, -0.3983294879921217557 ) ) ;
#64430=CARTESIAN_POINT ( 'NONE',  ( -77.51929025316718480, -46.43764116288181754, 138.1700848619338728 ) ) ;
#64432=CARTESIAN_POINT ( 'NONE',  ( 4.277780656302746287, -59.99999999999995737, 41.98959578111988122 ) ) ;
#64433=CARTESIAN_POINT ( 'NONE',  ( 77.34876605350574152, -57.51968639827215668, 195.6293917740978827 ) ) ;
#64441=CARTESIAN_POINT ( 'NONE',  ( -103.9496743848372375, -52.71021183741716243, 151.5995497774347029 ) ) ;
#64451=CARTESIAN_POINT ( 'NONE',  ( -32.49743750560201505, -59.99999999999998579, 47.28107978972537495 ) ) ;
#64452=CARTESIAN_POINT ( 'NONE',  ( 28.24466138624848455, -32.53086730938267124, 31.34497064575486647 ) ) ;
#64492=CARTESIAN_POINT ( 'NONE',  ( 67.07649707454891086, -42.95850431900807109, 94.37125772477908470 ) ) ;
#64498=DIRECTION ( 'NONE',  ( -0.000000000000000000, -1.000000000000000000, -0.000000000000000000 ) ) ;
#64515=CARTESIAN_POINT ( 'NONE',  ( 16.39870140197033876, -60.00000000000000000, 39.87645633822717883 ) ) ;
#64516=CARTESIAN_POINT ( 'NONE',  ( -98.88010798912279142, -29.99999999999999289, 189.1023777079059869 ) ) ;
#64519=CARTESIAN_POINT ( 'NONE',  ( 52.48690415104037754, -57.67637498706665866, 84.06783307720677101 ) ) ;
#64522=CARTESIAN_POINT ( 'NONE',  ( -0.01393140247697588312, -21.31702117966834109, -38.55283400289633278 ) ) ;
#64526=CARTESIAN_POINT ( 'NONE',  ( -26.01021955176325662, -60.00000000000000711, 41.44826368662123173 ) ) ;
#64531=CARTESIAN_POINT ( 'NONE',  ( -86.81214770105786727, -42.79374714232908872, 189.6642773476453954 ) ) ;
#64535=CARTESIAN_POINT ( 'NONE',  ( -12.44423993302578779, -42.95776644870394989, 31.10559508463949285 ) ) ;
#64547=CARTESIAN_POINT ( 'NONE',  ( 73.08118796046841226, -60.00000000000000711, 163.2004635648854105 ) ) ;
#64551=PRESENTATION_STYLE_ASSIGNMENT (( #36069 ) ) ;
#64565=CARTESIAN_POINT ( 'NONE',  ( -107.0258504621141640, -59.99999999988283861, 107.9273113137431466 ) ) ;
#64568=CARTESIAN_POINT ( 'NONE',  ( 77.49317349146313916, -59.99999999999997158, 191.7494575080134780 ) ) ;
#64571=CARTESIAN_POINT ( 'NONE',  ( -114.0746799351349665, -60.00000000000000000, 159.9915189542998633 ) ) ;
#64572=CARTESIAN_POINT ( 'NONE',  ( 14.55850093289553548, -39.47278144515117759, 30.59000656356446513 ) ) ;
#64574=CARTESIAN_POINT ( 'NONE',  ( 102.2641418190583096, -37.99999999999998579, 159.8959632408159166 ) ) ;
#64577=CARTESIAN_POINT ( 'NONE',  ( -44.85643671809746991, -46.44168872824101868, 45.33582960114114968 ) ) ;
#64588=CARTESIAN_POINT ( 'NONE',  ( 105.5552223516102828, -29.99999999999804245, 194.5626790352639830 ) ) ;
#64593=CARTESIAN_POINT ( 'NONE',  ( 92.54325103475800063, -29.99999999999999645, 103.3538081942403011 ) ) ;
#64597=ORIENTED_EDGE ( 'NONE', *, *, #62967, .T. ) ;
#64600=CARTESIAN_POINT ( 'NONE',  ( 2.435347819570957628E-07, -57.67120202539301488, -44.61186700419775519 ) ) ;
#64606=CARTESIAN_POINT ( 'NONE',  ( 78.80898649105323273, -38.66954475436662619, 190.4763790698753496 ) ) ;
#64630=CARTESIAN_POINT ( 'NONE',  ( 85.78844419382012632, -32.04248467167011682, 182.7523993070230972 ) ) ;
#64632=CARTESIAN_POINT ( 'NONE',  ( 94.30094425679524761, -57.67269112088474259, 1.199366103519862836 ) ) ;
#64636=CARTESIAN_POINT ( 'NONE',  ( -79.79064827434378060, -37.99999999999993605, 142.8556830992165203 ) ) ;
#64648=CARTESIAN_POINT ( 'NONE',  ( 67.30223688326144327, -29.89188614501962249, -22.05636472815148963 ) ) ;
#64652=CARTESIAN_POINT ( 'NONE',  ( -20.22589539060425778, -18.61607622294231490, -33.69375874054126285 ) ) ;
#64654=CARTESIAN_POINT ( 'NONE',  ( -47.11704795911705190, -34.58946938708281493, -28.29307930567724227 ) ) ;
#64662=CARTESIAN_POINT ( 'NONE',  ( -92.52198040298654291, -59.99999999999999289, -1.574747665964571830 ) ) ;
#64665=AXIS2_PLACEMENT_3D ( 'NONE', #46022, #53576, #29862 ) ;
#64668=CARTESIAN_POINT ( 'NONE',  ( 94.84481684524081402, -45.27023405461187622, 194.1702102290486494 ) ) ;
#64671=CARTESIAN_POINT ( 'NONE',  ( -81.53173708633690353, -46.45041501876503531, 167.1433614008564632 ) ) ;
#64683=DIRECTION ( 'NONE',  ( 0.000000000000000000, 0.000000000000000000, 1.000000000000000000 ) ) ;
#64686=CARTESIAN_POINT ( 'NONE',  ( -111.0360493097450529, -57.67057850706027722, 194.0974529949267549 ) ) ;
#64691=CARTESIAN_POINT ( 'NONE',  ( -2.851760031137707596, -60.00000000000000000, -45.00000000000002132 ) ) ;
#64693=CARTESIAN_POINT ( 'NONE',  ( -37.63111671575072137, -14.21045842199439235, 41.24562198507008759 ) ) ;
#64695=CARTESIAN_POINT ( 'NONE',  ( -53.60733004976390248, -46.44083241526271166, 60.07166913633320604 ) ) ;
#64697=CARTESIAN_POINT ( 'NONE',  ( -95.90005584971282815, -45.25350020261503659, 194.1417000045240968 ) ) ;
#64701=CARTESIAN_POINT ( 'NONE',  ( 91.13477408414057379, -38.40443913744169890, -11.79364926309030892 ) ) ;
#64705=EDGE_CURVE ( 'NONE', #59024, #77351, #16451, .T. ) ;
#64708=CARTESIAN_POINT ( 'NONE',  ( 80.75155016999305246, -30.00000000000000711, 138.6041971985428631 ) ) ;
#64709=FACE_OUTER_BOUND ( 'NONE', #24347, .T. ) ;
#64715=CARTESIAN_POINT ( 'NONE',  ( 50.24668090215569549, -60.29526498424313985, 58.32267405694980056 ) ) ;
#64719=CARTESIAN_POINT ( 'NONE',  ( -109.9674670641295080, -38.35608556422234727, 186.0885245604343083 ) ) ;
#64722=CARTESIAN_POINT ( 'NONE',  ( 98.21170614753282280, -38.35583079657099859, 77.88820735297903752 ) ) ;
#64726=CARTESIAN_POINT ( 'NONE',  ( 97.17576315571548662, -37.84846074978354835, 120.9268184589083717 ) ) ;
#64731=CARTESIAN_POINT ( 'NONE',  ( 77.93163905888464171, -59.99999999999997868, 192.6887321471520238 ) ) ;
#64734=CARTESIAN_POINT ( 'NONE',  ( 56.75702308777373162, -36.02330638279852337, 62.71544796725239479 ) ) ;
#64740=CARTESIAN_POINT ( 'NONE',  ( -91.08926842279480240, -38.40455573169174386, -12.07822636003188954 ) ) ;
#64749=STYLED_ITEM ( 'NONE', ( #64551 ), #88323 ) ;
#64754=CARTESIAN_POINT ( 'NONE',  ( 81.78911868813072772, -53.49039721618134280, 179.9874179505537768 ) ) ;
#64768=CARTESIAN_POINT ( 'NONE',  ( -21.98111356096458024, -27.00318221690102050, 37.33131516330131205 ) ) ;
#64788=CARTESIAN_POINT ( 'NONE',  ( -109.1115345680586586, -60.00000000000000711, 136.7728363596365568 ) ) ;
#64794=CARTESIAN_POINT ( 'NONE',  ( -81.43653422135359676, -57.01209690326547985, 181.8861859459519792 ) ) ;
#64809=CARTESIAN_POINT ( 'NONE',  ( 113.7193001496157052, -60.00000000000001421, 185.6034734595149871 ) ) ;
#64810=CARTESIAN_POINT ( 'NONE',  ( -112.2649012439172793, -59.99999999999995026, 191.8495178741738130 ) ) ;
#64811=CARTESIAN_POINT ( 'NONE',  ( -63.22578340066489488, -36.00976971212025290, 79.28688979505365353 ) ) ;
#64816=CARTESIAN_POINT ( 'NONE',  ( 114.0273069743737295, -59.99999999998534861, 183.4122421493096908 ) ) ;
#64820=CARTESIAN_POINT ( 'NONE',  ( 0.9878741920119958886, -22.06731700408509766, 27.56753612694989997 ) ) ;
#64822=COLOUR_RGB ( '', 0.66274510, 0.83137255, 0.94901961) ;
#64829=CARTESIAN_POINT ( 'NONE',  ( -105.7231067272802107, -60.00000000000002132, 198.5820885245993850 ) ) ;
#64839=CARTESIAN_POINT ( 'NONE',  ( 97.75542164735125539, -59.99999999999992895, 196.5577905707872617 ) ) ;
#64840=CARTESIAN_POINT ( 'NONE',  ( -33.08517237052004134, -32.56037428575159964, 33.08091690792520012 ) ) ;
#64841=CARTESIAN_POINT ( 'NONE',  ( 38.62684451199579172, -49.88772538349552832, 39.81651187074815823 ) ) ;
#64845=CARTESIAN_POINT ( 'NONE',  ( -58.12203222560709293, -38.34410314818605769, 90.61017755120225559 ) ) ;
#64855=CARTESIAN_POINT ( 'NONE',  ( 100.5416370945685287, -59.99999999999999289, 84.20779271781832165 ) ) ;
#64860=CARTESIAN_POINT ( 'NONE',  ( -89.28949256530911782, -29.99999999994691890, 17.42366683985877884 ) ) ;
#64868=CARTESIAN_POINT ( 'NONE',  ( -10.00000000000000000, -15.00000000000000000, 10.00000000000000178 ) ) ;
#64874=CARTESIAN_POINT ( 'NONE',  ( 84.18868867901204567, -18.67344423748746252, 149.2193650899454553 ) ) ;
#64883=CARTESIAN_POINT ( 'NONE',  ( -44.89949488402420030, -57.68324447995585302, 64.92693994880102082 ) ) ;
#64896=CARTESIAN_POINT ( 'NONE',  ( -21.78783193603920765, -17.85986078249778330, 31.47006901580117599 ) ) ;
#64918=CARTESIAN_POINT ( 'NONE',  ( 99.48231450907248075, -57.62624137959831216, 204.0649224731593279 ) ) ;
#64919=ADVANCED_FACE ( 'NONE', ( #103772 ), #29910, .T. ) ;
#64923=CARTESIAN_POINT ( 'NONE',  ( -74.75251265819703406, -60.00000000000001421, 179.3165659446441396 ) ) ;
#64928=CARTESIAN_POINT ( 'NONE',  ( -84.69605050066350316, -46.57368461021737716, 186.7912660905877260 ) ) ;
#64935=CARTESIAN_POINT ( 'NONE',  ( -83.19139743512374707, -37.80357306262363437, -4.125305165967327881 ) ) ;
#64940=CARTESIAN_POINT ( 'NONE',  ( 13.66642973270348627, -9.677049996499534265E-13, 17.78317311657527000 ) ) ;
#64942=CARTESIAN_POINT ( 'NONE',  ( -64.67113474307254251, -14.21045842199435505, -28.81208810413780697 ) ) ;
#64943=CARTESIAN_POINT ( 'NONE',  ( -76.18563976863433140, -60.31830717657551588, 143.7070035543199822 ) ) ;
#64945=CARTESIAN_POINT ( 'NONE',  ( 42.10926113833883022, -14.21045842199418452, 45.52176705710515847 ) ) ;
#64947=CARTESIAN_POINT ( 'NONE',  ( 112.6079886463091100, -57.67117955158271059, 189.1529986196025561 ) ) ;
#64966=CARTESIAN_POINT ( 'NONE',  ( 30.06199366251785676, -32.53957342301957567, 31.90491467160951800 ) ) ;
#64972=PLANE ( 'NONE',  #6137 ) ;
#64981=CARTESIAN_POINT ( 'NONE',  ( 49.18716589317016741, -60.00000000000000000, -38.06278613323081572 ) ) ;
#64999=ORIENTED_EDGE ( 'NONE', *, *, #9570, .F. ) ;
#65008=CARTESIAN_POINT ( 'NONE',  ( -68.97173617594968675, -59.99999999999997868, 110.4809570121333877 ) ) ;
#65009=CARTESIAN_POINT ( 'NONE',  ( 68.05421936547546125, -46.43370952207241942, 99.56240759577892163 ) ) ;
#65013=ADVANCED_FACE ( 'NONE', ( #8252 ), #130, .T. ) ;
#65029=CARTESIAN_POINT ( 'NONE',  ( 4.997114387724912454, -59.99999999999999289, 39.62950257011186039 ) ) ;
#65030=CARTESIAN_POINT ( 'NONE',  ( -98.12941349166321459, -30.00000000000000000, 190.3859582420429888 ) ) ;
#65035=CARTESIAN_POINT ( 'NONE',  ( 35.33287217233590383, -57.69550832373160176, 49.48941122886714794 ) ) ;
#65042=CARTESIAN_POINT ( 'NONE',  ( -12.15260666804171130, -59.99999999999999289, 39.69048265552311250 ) ) ;
#65047=CARTESIAN_POINT ( 'NONE',  ( -86.40926781137700630, -53.79403237629073686, 192.3592306068764515 ) ) ;
#65052=CARTESIAN_POINT ( 'NONE',  ( -10.37493441333220900, -49.92101058743562447, 32.22302584859001229 ) ) ;
#65054=AXIS2_PLACEMENT_3D ( 'NONE', #49433, #16547, #96936 ) ;
#65064=CARTESIAN_POINT ( 'NONE',  ( 69.39616242234656340, -60.00000000000000711, 138.1480787444137661 ) ) ;
#65070=CARTESIAN_POINT ( 'NONE',  ( 12.27067942234224418, -14.21045842199423959, 34.40196113412964962 ) ) ;
#65083=CARTESIAN_POINT ( 'NONE',  ( -14.01278929553941488, -60.00000000000000711, 42.10626255143397856 ) ) ;
#65086=CARTESIAN_POINT ( 'NONE',  ( 74.07531781632955870, -60.00000000000001421, 172.9861120789492475 ) ) ;
#65088=CARTESIAN_POINT ( 'NONE',  ( -114.5769593907454862, -59.99999999999998579, 170.6727965893586827 ) ) ;
#65089=CARTESIAN_POINT ( 'NONE',  ( 16.57071829965135024, -29.03055317263135748, 28.95038203199459659 ) ) ;
#65091=CARTESIAN_POINT ( 'NONE',  ( 85.23752753509168656, -37.99999999999997158, 47.19075432804262960 ) ) ;
#65094=CARTESIAN_POINT ( 'NONE',  ( -46.31354256535421854, -42.98738504804538962, 46.26985113983830900 ) ) ;
#65106=CARTESIAN_POINT ( 'NONE',  ( 95.99808094090420241, -30.00000000000683542, 199.9041741166194868 ) ) ;
#65110=CARTESIAN_POINT ( 'NONE',  ( 98.15759235675383820, -30.00000000000000000, 138.6648893879348350 ) ) ;
#65126=CARTESIAN_POINT ( 'NONE',  ( 81.68106932928363051, -38.84191837104209100, 195.5020664298707800 ) ) ;
#65128=CARTESIAN_POINT ( 'NONE',  ( 51.84565611112584804, -38.00000000000000711, 53.44666998630373911 ) ) ;
#65148=CARTESIAN_POINT ( 'NONE',  ( 84.96212205827315245, -46.56643884038170711, 187.4507856897367049 ) ) ;
#65152=CARTESIAN_POINT ( 'NONE',  ( 82.82192797015540009, -57.67108540965746499, -28.52013474738419774 ) ) ;
#65156=CARTESIAN_POINT ( 'NONE',  ( -81.59886796681669807, -29.99999999999999645, -6.443727801133209532 ) ) ;
#65180=CARTESIAN_POINT ( 'NONE',  ( -21.07344922941815213, -18.86340865632357122, -33.57730334312562803 ) ) ;
#65182=CARTESIAN_POINT ( 'NONE',  ( -50.18744314967482723, -34.58944621710350020, -27.70643596530725716 ) ) ;
#65191=CARTESIAN_POINT ( 'NONE',  ( -50.19229659092784601, -60.00000000000001421, -37.86681916100207701 ) ) ;
#65193=CARTESIAN_POINT ( 'NONE',  ( 5.467818114163457643, -22.30699358996656656, -30.53336729979983488 ) ) ;
#65194=CARTESIAN_POINT ( 'NONE',  ( -71.80342408229677176, -30.00000000000000000, -19.71767938363507966 ) ) ;
#65196=CARTESIAN_POINT ( 'NONE',  ( 97.51699909924960252, -45.26833302863503405, 193.9111182486593066 ) ) ;
#65205=EDGE_CURVE ( 'NONE', #62746, #102908, #93680, .T. ) ;
#65210=CARTESIAN_POINT ( 'NONE',  ( -114.2112478298105174, -57.67107988235927252, 175.3835541016526349 ) ) ;
#65216=CARTESIAN_POINT ( 'NONE',  ( -68.53940498225642841, -14.21045842199433729, -27.47940008941059276 ) ) ;
#65220=CARTESIAN_POINT ( 'NONE',  ( -53.40209911825037636, -39.50465069708222643, 56.96612769989180691 ) ) ;
#65224=CARTESIAN_POINT ( 'NONE',  ( -100.4704357492387601, -52.74943876303672141, 193.8537836153791147 ) ) ;
#65230=CARTESIAN_POINT ( 'NONE',  ( 91.04369531743766686, -38.35020560426966796, 1.585978844074899419 ) ) ;
#65235=CARTESIAN_POINT ( 'NONE',  ( 80.50372827376243379, -29.99999999999999645, 137.2448855364089297 ) ) ;
#65243=CARTESIAN_POINT ( 'NONE',  ( 49.80781392084993087, -29.12675541338599672, 47.03600289386830013 ) ) ;
#65248=CARTESIAN_POINT ( 'NONE',  ( -109.4490193154211966, -38.35608385809126730, 149.1993996903198081 ) ) ;
#65251=CARTESIAN_POINT ( 'NONE',  ( 95.02435692186872984, -38.35555520635520566, 58.02324002954877358 ) ) ;
#65254=CARTESIAN_POINT ( 'NONE',  ( 102.3385178479906443, -60.15132848126114595, 129.8721470524102983 ) ) ;
#65259=CARTESIAN_POINT ( 'NONE',  ( 74.65033017998224807, -60.00000000000001421, 178.4634517001849190 ) ) ;
#65263=CARTESIAN_POINT ( 'NONE',  ( 55.55584471301806104, -60.32186133166744924, 70.31348763753899789 ) ) ;
#65268=CARTESIAN_POINT ( 'NONE',  ( -89.79833081493985958, -38.39354622375766013, -16.47870807438435392 ) ) ;
#65279=CARTESIAN_POINT ( 'NONE',  ( 82.48598427777827169, -50.01050129768884034, 180.4116382470554356 ) ) ;
#65295=CARTESIAN_POINT ( 'NONE',  ( -8.594949192134683003, -19.66686426804723098, 35.27552358496240714 ) ) ;
#65304=B_SPLINE_CURVE_WITH_KNOTS ( 'NONE', 3,
 ( #65128, #71616, #88880, #13906, #63558, #97478, #96451, #22588, #7408, #6340, #55425, #23633, #54896, #39282, #88358, #5826, #39808, #96969, #56490, #46820, #40321, #14434, #14969, #47343, #48402, #105068, #104518, #80236, #72160, #31208, #64093, #47865, #106100, #89420, #80772, #79717 ),
 .UNSPECIFIED., .F., .F.,
 ( 4, 2, 2, 2, 2, 2, 2, 2, 2, 2, 2, 2, 2, 2, 2, 2, 2, 4 ),
 ( 0.000000000000000000, 0.008790666710044045193, 0.01758133342008806957, 0.02637200013013209568, 0.03516266684017610444, 0.05274400026026411503, 0.07032533368035212562, 0.08790666710044017784, 0.09669733381048414844, 0.1054880005205281468, 0.1142786672305721174, 0.1230693339406161019, 0.1274646672956381566, 0.1318600006506601696, 0.1362553340056822104, 0.1384530006831932447, 0.1395518340219487896, 0.1406506673607043345 ),
 .UNSPECIFIED. ) ;
#65321=CARTESIAN_POINT ( 'NONE',  ( -100.8702459599107897, -60.00000000000000000, 86.13901550309863353 ) ) ;
#65323=CARTESIAN_POINT ( 'NONE',  ( 3.789997851623448167E-05, -46.43937203793843338, 31.62954529925878688 ) ) ;
#65329=CARTESIAN_POINT ( 'NONE',  ( -81.08908342379014300, -60.53280594523494784, 183.7735889067742221 ) ) ;
#65342=CARTESIAN_POINT ( 'NONE',  ( 113.5291039388664700, -60.00000000000007105, 153.5981272189337403 ) ) ;
#65344=CARTESIAN_POINT ( 'NONE',  ( -109.5313977869038098, -29.99999999999998934, 176.4136249138144876 ) ) ;
#65345=CARTESIAN_POINT ( 'NONE',  ( -62.66137373571188363, -39.48701201810304440, 79.45161525184568063 ) ) ;
#65348=CARTESIAN_POINT ( 'NONE',  ( 94.21848556752277659, -59.99999999996594369, 13.18754133863892974 ) ) ;
#65360=CARTESIAN_POINT ( 'NONE',  ( -112.2379140073269497, -59.99999999999998579, 175.3422743821848258 ) ) ;
#65363=DIRECTION ( 'NONE',  ( 0.000000000000000000, 0.000000000000000000, 1.000000000000000000 ) ) ;
#65369=CARTESIAN_POINT ( 'NONE',  ( 106.0232194623858106, -59.99999999999999289, 182.0013391524945519 ) ) ;
#65371=CARTESIAN_POINT ( 'NONE',  ( -32.10230308758781348, -25.61542695683890969, 31.36975326410992793 ) ) ;
#65375=CARTESIAN_POINT ( 'NONE',  ( 39.12690398050479246, -60.26094875330049661, 42.39772928756006110 ) ) ;
#65380=CARTESIAN_POINT ( 'NONE',  ( -80.08331211031514840, -38.78820510874865590, 193.1379239215828250 ) ) ;
#65393=CARTESIAN_POINT ( 'NONE',  ( 110.0335605139551234, -59.99999999999999289, 143.7182336800421183 ) ) ;
#65396=CARTESIAN_POINT ( 'NONE',  ( -98.08299448810690535, -29.99999999999990763, 190.4420231606735570 ) ) ;
#65411=CARTESIAN_POINT ( 'NONE',  ( 80.49938719612642046, -42.96636524030287063, 153.2983854078102581 ) ) ;
#65415=EDGE_LOOP ( 'NONE', ( #17806, #39560, #417, #47053, #33306, #51656, #2320 ) ) ;
#65420=CARTESIAN_POINT ( 'NONE',  ( -43.89814859212165743, -59.99999999999997868, -33.20116366665202179 ) ) ;
#65421=CARTESIAN_POINT ( 'NONE',  ( -32.88842731267402542, -57.69106633777249016, 47.18465683205923966 ) ) ;
#65432=CARTESIAN_POINT ( 'NONE',  ( 24.35999770972153300, -28.60365089118337423, 38.05418454928949501 ) ) ;
#65442=CARTESIAN_POINT ( 'NONE',  ( 69.40321497448834975, -38.19972286543485041, -31.40616810314683605 ) ) ;
#65444=EDGE_CURVE ( 'NONE', #94469, #102908, #69319, .T. ) ;
#65450=CARTESIAN_POINT ( 'NONE',  ( 112.1546642664688704, -57.67108995165709473, 190.8163332172947833 ) ) ;
#65456=CARTESIAN_POINT ( 'NONE',  ( -73.49971499675589826, -60.00000000000000000, 167.1873391204008783 ) ) ;
#65460=CARTESIAN_POINT ( 'NONE',  ( -85.90370816398340992, -28.44268232177473621, 181.2109021316425412 ) ) ;
#65468=CARTESIAN_POINT ( 'NONE',  ( -82.96937446443966735, -37.77006566532177345, -10.80790838508248441 ) ) ;
#65475=CARTESIAN_POINT ( 'NONE',  ( 8.569529079651905690, -1.734723475976807094E-15, -14.86825985027703290 ) ) ;
#65479=CARTESIAN_POINT ( 'NONE',  ( -8.554898963428433589, -59.99999999999994316, -44.87740334038038270 ) ) ;
#65480=CARTESIAN_POINT ( 'NONE',  ( -79.07968554265760019, -25.61633390025545864, 127.8515609946744576 ) ) ;
#65482=CARTESIAN_POINT ( 'NONE',  ( 36.05900422978820075, -60.00000000000002132, 50.77828662454974307 ) ) ;
#65484=CARTESIAN_POINT ( 'NONE',  ( 113.8203870463297562, -57.67116299849189431, 161.9121400180774799 ) ) ;
#65503=CARTESIAN_POINT ( 'NONE',  ( 28.19617395168271656, -18.63290521535086697, 28.87333934571989502 ) ) ;
#65517=CARTESIAN_POINT ( 'NONE',  ( 49.73772649942210222, -60.00000000000002132, -37.95607009740780313 ) ) ;
#65536=VERTEX_POINT ( 'NONE', #10138 ) ;
#65542=CARTESIAN_POINT ( 'NONE',  ( 69.00182384322468465, -32.53477014765218911, 94.70385995679106372 ) ) ;
#65545=TOROIDAL_SURFACE ( 'NONE', #105190, 74.46152422706630603, 68.00000000000000000 ) ;
#65564=CARTESIAN_POINT ( 'NONE',  ( 7.006887204118438461, -59.99999999999998579, 39.62928630090096505 ) ) ;
#65565=CARTESIAN_POINT ( 'NONE',  ( -96.67163991703634451, -30.00000000000000000, 191.1777818508784037 ) ) ;
#65568=CARTESIAN_POINT ( 'NONE',  ( 73.76917559204071040, -57.62240879868848964, 185.9086365273194019 ) ) ;
#65573=CARTESIAN_POINT ( 'NONE',  ( 19.15691834943884331, -25.52937350832362995, -38.49469340411490492 ) ) ;
#65578=CARTESIAN_POINT ( 'NONE',  ( -2.469906284812917185, -59.99999999999999289, 39.63522433654287624 ) ) ;
#65581=CARTESIAN_POINT ( 'NONE',  ( -86.50123036836470192, -17.01944231672239383, 184.1032767441589328 ) ) ;
#65582=EDGE_LOOP ( 'NONE', ( #15115, #37249, #75490, #21803, #83865, #105173, #90803 ) ) ;
#65585=CARTESIAN_POINT ( 'NONE',  ( -7.180605313813533286, -46.43926895535531685, 31.61986485186096019 ) ) ;
#65598=CARTESIAN_POINT ( 'NONE',  ( 109.4307067020638726, -30.00000000000001066, 166.0292171922573345 ) ) ;
#65622=CARTESIAN_POINT ( 'NONE',  ( -18.10756586307027050, -59.99999999999510436, 42.37213598781649893 ) ) ;
#65625=CARTESIAN_POINT ( 'NONE',  ( 92.32305526061090006, -60.00000000000002132, 24.43391867025795960 ) ) ;
#65627=CARTESIAN_POINT ( 'NONE',  ( -106.6034117734591860, -29.99999999999999645, 192.6833206840571791 ) ) ;
#65628=CARTESIAN_POINT ( 'NONE',  ( 18.23452885637153997, -56.87686820525264153, 33.72162051064637467 ) ) ;
#65631=CARTESIAN_POINT ( 'NONE',  ( -42.78963735806012636, -60.25406996619459932, 46.28178354334486500 ) ) ;
#65643=CARTESIAN_POINT ( 'NONE',  ( 66.18517126493600244, -29.99999999992071409, 111.4181126619788529 ) ) ;
#65648=CARTESIAN_POINT ( 'NONE',  ( 90.56647543664284683, -29.99999999999999645, 91.80300536945385659 ) ) ;
#65651=ORIENTED_EDGE ( 'NONE', *, *, #55213, .T. ) ;
#65664=CARTESIAN_POINT ( 'NONE',  ( 80.42530181681347301, -38.80960826814366271, 193.7223798169567033 ) ) ;
#65680=CARTESIAN_POINT ( 'NONE',  ( 19.49818721152012202, -25.36617680456863155, 36.68312451770463412 ) ) ;
#65684=CARTESIAN_POINT ( 'NONE',  ( 84.77457301996732042, -53.82917485777404210, 190.3326470173193457 ) ) ;
#65688=CARTESIAN_POINT ( 'NONE',  ( 77.01964372777356971, -57.67122230834739582, -31.73091028824633852 ) ) ;
#65696=CARTESIAN_POINT ( 'NONE',  ( -81.46673774545078572, -29.99999999999999289, -9.566678094518634268 ) ) ;
#65717=CARTESIAN_POINT ( 'NONE',  ( -69.34099659244546388, -29.97784688933757025, -21.09145479153141522 ) ) ;
#65719=CARTESIAN_POINT ( 'NONE',  ( -68.60628786470475404, -47.40885926954825891, -24.67610123206565476 ) ) ;
#65727=AXIS2_PLACEMENT_3D ( 'NONE', #44765, #85206, #77114 ) ;
#65729=CARTESIAN_POINT ( 'NONE',  ( -38.40660055531301253, -60.00000000000000000, -39.85627520488996822 ) ) ;
#65731=CARTESIAN_POINT ( 'NONE',  ( 50.36674964328668835, -35.86795674544367074, -27.86065576867944316 ) ) ;
#65732=CARTESIAN_POINT ( 'NONE',  ( 2.500000000000003109, -8.000000000000000000, 4.679304766526505863E-16 ) ) ;
#65747=CARTESIAN_POINT ( 'NONE',  ( -66.37944403907447111, -57.68041551771388953, 132.8370836190597686 ) ) ;
#65752=CARTESIAN_POINT ( 'NONE',  ( -52.81151229832320126, -14.21045842199429643, -31.95502044027141153 ) ) ;
#65754=CARTESIAN_POINT ( 'NONE',  ( -53.27082796895624739, -42.97299545974212265, 58.02614799047049132 ) ) ;
#65757=CARTESIAN_POINT ( 'NONE',  ( -96.63378167814529718, -37.69171814361656914, 192.9088573962275461 ) ) ;
#65762=CARTESIAN_POINT ( 'NONE',  ( 88.07186593688837206, -38.55612627883184729, 199.9830497965955374 ) ) ;
#65765=CIRCLE ( 'NONE', #34845, 74.46152422706630603 ) ;
#65768=CARTESIAN_POINT ( 'NONE',  ( 83.22245246229280724, -30.00000000000001066, 154.5341563752995171 ) ) ;
#65775=EDGE_LOOP ( 'NONE', ( #80844, #16435, #46062, #63906 ) ) ;
#65776=CARTESIAN_POINT ( 'NONE',  ( 49.92757571601900679, -22.20139394744939310, 44.97315255701366254 ) ) ;
#65782=CARTESIAN_POINT ( 'NONE',  ( -92.49477123227754305, -38.35497500972908114, 39.22377915011799132 ) ) ;
#65785=CARTESIAN_POINT ( 'NONE',  ( 90.85852390707832171, -38.35167856242225781, 20.58440466305621896 ) ) ;
#65787=CARTESIAN_POINT ( 'NONE',  ( 99.60646395647034979, -52.71694380898900079, 120.4330034612430609 ) ) ;
#65792=CARTESIAN_POINT ( 'NONE',  ( 74.21597319742625132, -60.00000000000000000, 174.3876596883068828 ) ) ;
#65793=B_SPLINE_CURVE_WITH_KNOTS ( 'NONE', 3,
 ( #42697, #76119, #2215, #51841, #85840, #35165, #27087, #85282, #59974, #84754, #43755, #3303, #44297, #87423, #14550, #64208, #47459, #12440, #22163, #63678, #96037, #96566, #46420, #54474, #97078, #55012, #71729, #103068, #46932, #45366, #38352, #29224, #21639, #53957, #13497, #79306, #88475, #45890, #62610, #5428, #79831, #31326, #71212, #104106, #87944, #14026, #38863, #70164, #62098, #94990, #30249, #63137, #78249, #86893, #5936, #21128, #22701, #104641, #37833, #55538, #95496, #30793, #4362, #80352, #37298, #6467, #39399, #72277, #105181, #53454, #86374, #12966, #29737, #78768, #4902, #70697, #103588, #80890, #16699, #90590, #65785, #72793, #98141, #23763, #24293, #57142, #58216, #15627, #32379, #90055, #49590, #81943, #74389, #73319, #98663, #42032, #32908, #89536, #40977, #33979, #16159, #8065, #47983, #56611, #24815, #105698, #33436, #57667, #7521, #25353, #65251, #56061, #73865, #64722, #82498, #106760, #8599, #49046, #41501, #74914, #48519, #17251, #81410, #468, #66310, #99191, #7001, #40439, #91141, #50122, #998, #23222, #83031, #9122, #66851, #89001, #39921, #15096, #31840, #97596, #106215, #1555, #83549, #100271, #44173, #27499, #93249, #43105, #34520, #9649, #36122, #85706, #93783, #60374, #19412, #36650, #76520, #52246, #2091, #84093, #85155, #67389, #26433, #68450, #51713, #50631, #77060, #19944, #91664, #59298, #101866, #77602, #60895, #67908, #11244, #18320, #17778, #3176, #51170, #3720, #10193, #92170, #101345, #42559, #75462, #52784, #68991, #59835, #26955, #11783, #99740, #44713, #58766, #28026, #25910, #75993, #35044, #100795, #92709, #18869, #84628, #10715, #43631, #2631, #35577, #87824, #21512, #78123, #53328, #70034, #13903, #103984, #63014, #12842, #4239, #86246, #5822, #55422, #63555, #30126, #95912, #37714, #30667, #54348, #4772, #20490, #22036, #37173, #102938, #38230, #87290, #12319, #46817, #96448, #61431, #29104, #71613, #47339, #22584, #70577, #54893, #94325, #79714, #21004, #80233, #86775, #38742, #61972, #13369, #45244, #62485, #94863, #104515, #53844, #95376, #6337, #69515, #102400, #45761, #88355, #78637, #14431, #103464, #28550, #29613, #46296, #79185, #5310, #71094, #106640, #81815, #47862, #32246, #7406, #91020, #106097, #40847, #40319, #16041, #14966, #39805, #98023, #90466, #89418, #7941, #58091, #48921, #105580, #57020, #50004, #65126, #32790, #24176, #17126, #89934, #15510, #73740, #64089, #31721, #65664, #82909, #72157, #98545, #80769, #24696, #57546, #16579, #48400, #49465, #39279, #72679, #99069, #82372, #96966, #6884, #8479, #41384, #81290, #73194, #55937, #25234, #74275, #64606, #349, #105065, #31205, #23101, #97476, #33317, #23631, #66189, #88877, #56488, #10080, #19822, #10603, #27382, #58646, #2511, #74798, #100678, #1977, #83969, #60781, #75877, #43521, #42989, #92590, #91548, #9531, #101748, #93670, #67792, #34924, #84514, #76397, #101226, #25790, #17656, #50519, #26842, #59714, #52656, #18746, #92058, #51595, #33857, #75335, #35456, #27918, #68330, #60262, #878, #85042, #66729, #3053, #36002, #93130, #9006, #19302, #26318, #52126, #99613, #83434, #11124, #44049, #59179, #76940, #68875, #18195, #41912, #51052, #42444, #1436, #100152, #34397, #67273, #95266, #36533, #103863, #37593, #102822, #61307, #37054, #30542, #86658, #30013, #3596, #46697, #45651, #69398, #20896, #44594, #62899, #87704, #53730, #79594, #70456 ),
 .UNSPECIFIED., .F., .F.,
 ( 4, 2, 2, 2, 1, 1, 2, 2, 1, 1, 2, 2, 2, 2, 1, 2, 2, 2, 2, 2, 2, 1, 2, 2, 1, 1, 2, 2, 2, 2, 1, 2, 2, 1, 2, 2, 1, 1, 2, 2, 1, 1, 2, 2, 2, 2, 1, 1, 1, 2, 2, 1, 1, 2, 2, 2, 2, 1, 1, 1, 2, 2, 1, 1, 1, 1, 2, 2, 2, 2, 1, 1, 2, 2, 1, 1, 1, 1, 1, 2, 2, 2, 2, 2, 2, 1, 1, 1, 1, 1, 1, 1, 1, 2, 2, 2, 2, 2, 2, 2, 1, 1, 1, 1, 1, 1, 1, 1, 2, 2, 2, 2, 2, 1, 1, 1, 1, 1, 1, 1, 2, 2, 2, 2, 2, 1, 1, 1, 1, 1, 2, 2, 2, 2, 2, 1, 1, 1, 1, 2, 2, 2, 2, 1, 1, 1, 1, 1, 1, 1, 2, 2, 2, 2, 2, 2, 2, 1, 1, 1, 1, 1, 2, 2, 2, 2, 2, 2, 1, 1, 1, 1, 1, 1, 2, 2, 2, 2, 1, 1, 1, 1, 1, 1, 2, 2, 2, 2, 2, 1, 1, 1, 1, 2, 2, 2, 2, 1, 1, 1, 1, 1, 1, 2, 2, 2, 2, 2, 1, 1, 1, 1, 2, 2, 2, 2, 2, 1, 1, 1, 2, 2, 2, 2, 2, 2, 2, 1, 1, 1, 1, 1, 2, 2, 2, 2, 2, 1, 1, 1, 1, 1, 1, 2, 2, 2, 2, 2, 2, 1, 1, 1, 1, 2, 2, 2, 2, 2, 2, 2, 1, 1, 1, 1, 1, 1, 1, 2, 2, 2, 2, 2, 4 ),
 ( 0.000000000000000000, 0.007812499999651020474, 0.01562499999930204095, 0.01953124999912755899, 0.02001953124910586107, 0.02026367187409502599, 0.02038574218658967263, 0.02041625976471338547, 0.02044677734283709830, 0.02050781249908453438, 0.02148437499904310224, 0.02343749999896022757, 0.02734374999879447821, 0.02929687499871158965, 0.03027343749867014017, 0.03051757812365977693, 0.03076171874864941369, 0.03124999999862868721, 0.03515624999846280602, 0.03906249999829693176, 0.04003906249825545105, 0.04052734374823471764, 0.04077148437322434399, 0.04083251952947174884, 0.04089355468571915370, 0.04101562499821394953, 0.04296874999813071055, 0.04687499999796423261, 0.05468749999763128367, 0.05859374999746481266, 0.06054687499738157369, 0.06103515624736076395, 0.06127929687235035561, 0.06152343749733995421, 0.06249999999729832778, 0.07812499999663236050, 0.08007812499654912153, 0.08105468749650750204, 0.08154296874648669924, 0.08166503905898149507, 0.08178710937147629090, 0.08203124999646588256, 0.08593749999629947400, 0.09374999999596665690, 0.1093749999953010227, 0.1171874999949682056, 0.1210937499948017831, 0.1220703124947601914, 0.1223144531197498108, 0.1224365234322446344, 0.1224975585884920670, 0.1225585937447394858, 0.1230468749947207785, 0.1249999999946464768, 0.1406249999940512030, 0.1562499999934559569, 0.1601562499933071315, 0.1621093749932327466, 0.1630859374931955263, 0.1632080078056908912, 0.1632385253838147254, 0.1632690429619385319, 0.1633300781181862837, 0.1635742187431770134, 0.1640624999931583616, 0.1718749999928589345, 0.1874999999922599414, 0.2187499999910620663, 0.2499999999898641634, 0.2812499999886662883, 0.2851562499885165192, 0.2856445312384978119, 0.2857055663947454249, 0.2857666015509930380, 0.2858886718634883195, 0.2861328124884786606, 0.2871093749884404134, 0.2890624999883638080, 0.2968749999880570534, 0.3124999999874435996, 0.3749999999849897292, 0.4374999999825360253, 0.4687499999813090623, 0.4843749999806956086, 0.4921874999803889650, 0.4960937499802356987, 0.4980468749801592043, 0.4990234374801209571, 0.4995117187301018058, 0.4997558593550920913, 0.4998779296675873729, 0.4999389648238350414, 0.4999694824019588757, 0.4999847411910207651, 0.4999999999800827100, 0.5156249999794596528, 0.5312499999788367067, 0.5468749999782136495, 0.5546874999779023430, 0.5585937499777469117, 0.5605468749776695292, 0.5615234374776307824, 0.5620117187276114645, 0.5622558593526023607, 0.5623779296650976978, 0.5624389648213454773, 0.5624694823994693671, 0.5624847411885313120, 0.5624923705830626730, 0.5624999999775941451, 0.5703124999778719229, 0.5742187499780107007, 0.5761718749780803117, 0.5771484374781150617, 0.5776367187281322702, 0.5778808593531409299, 0.5780029296656451487, 0.5780639648218971471, 0.5780944824000230353, 0.5781097411890862015, 0.5781173705836177845, 0.5781249999781493676, 0.5800781249782447357, 0.5810546874782923643, 0.5815429687283162341, 0.5817871093533281135, 0.5819091796658339977, 0.5819702148220871063, 0.5820007324002134386, 0.5820159911892766047, 0.5820236205838081878, 0.5820312499783397708, 0.5830078124783841798, 0.5834960937284063842, 0.5837402343534173754, 0.5838623046659229265, 0.5839233398221758131, 0.5839538574003022564, 0.5839691161893653115, 0.5839767455838968946, 0.5839843749784284777, 0.5849609374784705551, 0.5854492187284916493, 0.5856933593535021965, 0.5858154296660074145, 0.5858764648222599680, 0.5859069824003863003, 0.5859222411894494664, 0.5859298705839809385, 0.5859336852812467855, 0.5859355926298795980, 0.5859374999785124105, 0.5878906249786036708, 0.5898437499786948202, 0.5917968749787859695, 0.5927734374788314886, 0.5932617187288543592, 0.5935058593538656835, 0.5936279296663713456, 0.5936889648226242322, 0.5937194824007505645, 0.5937347411898138416, 0.5937423705843454247, 0.5937499999788770078, 0.5957031249789628280, 0.5976562499790486482, 0.5996093749791345795, 0.6005859374791774341, 0.6010742187291988614, 0.6013183593542096306, 0.6014404296667150707, 0.6015014648229677352, 0.6015319824010940675, 0.6015472411901572336, 0.6015548705846888167, 0.6015624999792203997, 0.6035156249793174332, 0.6044921874793659500, 0.6049804687293902639, 0.6052246093544023653, 0.6053466796669084715, 0.6054077148231615801, 0.6054382324012880234, 0.6054534911903513006, 0.6054611205848829947, 0.6054687499794146888, 0.6074218749795251560, 0.6083984374795803340, 0.6088867187296079786, 0.6091308593546217454, 0.6092529296671286287, 0.6093139648233820704, 0.6093444824015088468, 0.6093597411905722350, 0.6093749999796355121, 0.6113281249797379857, 0.6123046874797891670, 0.6127929687298147021, 0.6130371093548275807, 0.6131591796673340200, 0.6132202148235871286, 0.6132507324017136829, 0.6132659911907769601, 0.6132736205853086542, 0.6132812499798403483, 0.6152343749799318307, 0.6162109374799775718, 0.6166992187300004424, 0.6169433593550117667, 0.6170654296675175399, 0.6171264648237704264, 0.6171569824018967587, 0.6171722411909600359, 0.6171874999800233130, 0.6210937499802106077, 0.6230468749803044215, 0.6240234374803512729, 0.6245117187303745876, 0.6247558593553863560, 0.6248779296678921291, 0.6249389648241451267, 0.6249999999803982353, 0.6328124999807902551, 0.6406249999811823859, 0.6484374999815745166, 0.6523437499817704710, 0.6542968749818685037, 0.6552734374819175756, 0.6557617187319422225, 0.6560058593569544350, 0.6561279296694605412, 0.6561889648257135388, 0.6562194824038400931, 0.6562499999819665364, 0.6718749999827752228, 0.6796874999831795661, 0.6835937499833818487, 0.6855468749834829900, 0.6865234374835335052, 0.6870117187335589293, 0.6872558593585716968, 0.6873779296710780251, 0.6874389648273313558, 0.6874694824054579101, 0.6874999999835845754, 0.7187499999852486887, 0.7343749999860806899, 0.7421874999864966904, 0.7460937499867046352, 0.7480468749868086631, 0.7490234374868607325, 0.7495117187368869338, 0.7497558593618999234, 0.7498779296744064737, 0.7499999999869129130, 0.7812499999885803570, 0.8124999999902479120, 0.8437499999919154670, 0.8593749999927492444, 0.8671874999931661332, 0.8710937499933745221, 0.8730468749934786610, 0.8740234374935308415, 0.8745117187435570427, 0.8747558593685700323, 0.8748779296810765826, 0.8749389648373300243, 0.8749694824154565787, 0.8749999999935830219, 0.9062499999951872942, 0.9374999999967915665, 0.9687499999983957277, 1.000000000000000000 ),
 .UNSPECIFIED. ) ;
#65795=CYLINDRICAL_SURFACE ( 'NONE', #97431, 7.499999999992679633 ) ;
#65797=CARTESIAN_POINT ( 'NONE',  ( 61.32899078381009161, -49.91179946772914633, 80.89050486367615633 ) ) ;
#65800=CARTESIAN_POINT ( 'NONE',  ( -76.24902598065085613, -29.99999999995297273, 167.9309681516145361 ) ) ;
#65809=CARTESIAN_POINT ( 'NONE',  ( 84.78850302438281972, -28.94140559783478395, 170.4382928173611447 ) ) ;
#65824=CARTESIAN_POINT ( 'NONE',  ( -5.442530501874275117, -18.69205451546762475, 35.10612107872960053 ) ) ;
#65837=CARTESIAN_POINT ( 'NONE',  ( 64.11807478814075978, -21.77010348245833526, -21.74840280664149716 ) ) ;
#65847=CARTESIAN_POINT ( 'NONE',  ( -103.5524900213308683, -60.00000000000001421, 101.8145487315525770 ) ) ;
#65855=CARTESIAN_POINT ( 'NONE',  ( -83.53549352640362713, -39.47137158060975537, 174.7280617345839460 ) ) ;
#65862=( GEOMETRIC_REPRESENTATION_CONTEXT ( 3 ) GLOBAL_UNCERTAINTY_ASSIGNED_CONTEXT ( ( #27011 ) ) GLOBAL_UNIT_ASSIGNED_CONTEXT ( ( #16054, #31736, #24709 ) ) REPRESENTATION_CONTEXT ( 'NONE', 'WORKASPACE' ) );
#65871=CARTESIAN_POINT ( 'NONE',  ( 106.7878191156923293, -14.21045842199435150, 165.8358245669431597 ) ) ;
#65873=CARTESIAN_POINT ( 'NONE',  ( -114.2223820868815380, -59.99999999999997868, 162.1253058113985048 ) ) ;
#65874=CARTESIAN_POINT ( 'NONE',  ( -64.00514404253527800, -29.05590673187525041, 77.96790845986099328 ) ) ;
#65877=CARTESIAN_POINT ( 'NONE',  ( 109.6214308269799176, -59.99999999999999289, 124.0322540993774396 ) ) ;
#65879=CARTESIAN_POINT ( 'NONE',  ( 1.023254973492224051, -60.35900083628900603, 33.94948343231720855 ) ) ;
#65886=CARTESIAN_POINT ( 'NONE',  ( -94.37463078541230743, -59.99999999999994316, 202.5629720368760616 ) ) ;
#65888=DIRECTION ( 'NONE',  ( -0.000000000000000000, -1.000000000000000000, -0.000000000000000000 ) ) ;
#65898=CARTESIAN_POINT ( 'NONE',  ( -32.78616274675678710, -32.55822851310848876, 32.94897349368736172 ) ) ;
#65900=CARTESIAN_POINT ( 'NONE',  ( 39.33871441765692367, -42.97318751769551426, 38.91929416661629659 ) ) ;
#65906=CARTESIAN_POINT ( 'NONE',  ( -78.35849824112422368, -38.61718390855864413, 189.2875896208779523 ) ) ;
#65919=CARTESIAN_POINT ( 'NONE',  ( 106.0576547319784169, -60.00000000000000000, 116.7836318968619764 ) ) ;
#65926=CARTESIAN_POINT ( 'NONE',  ( -100.0418167452864537, -30.00000000000002132, 185.4816374921457225 ) ) ;
#65939=CARTESIAN_POINT ( 'NONE',  ( 82.46808697483727713, -25.62292026212021057, 146.0453604029042651 ) ) ;
#65953=CARTESIAN_POINT ( 'NONE',  ( 86.31548406937289997, -57.42050482052351157, 193.3910388938697054 ) ) ;
#65957=CARTESIAN_POINT ( 'NONE',  ( 36.55251058255094421, -36.29168913791675521, 45.74408343238721386 ) ) ;
#65970=CARTESIAN_POINT ( 'NONE',  ( 107.8654790820937421, -57.67125328048376787, 115.6101856694811687 ) ) ;
#65977=CARTESIAN_POINT ( 'NONE',  ( -77.55662926993193196, -59.99999999999999289, 191.8679431246135891 ) ) ;
#65984=CARTESIAN_POINT ( 'NONE',  ( -86.02960737348817588, -28.37172899385929625, 182.1171066242029326 ) ) ;
#65992=CARTESIAN_POINT ( 'NONE',  ( -83.25973548172940752, -37.79105956807652689, -6.268593792199344428 ) ) ;
#65996=( GEOMETRIC_REPRESENTATION_CONTEXT ( 3 ) GLOBAL_UNCERTAINTY_ASSIGNED_CONTEXT ( ( #74109 ) ) GLOBAL_UNIT_ASSIGNED_CONTEXT ( ( #35582, #64095, #45248 ) ) REPRESENTATION_CONTEXT ( 'NONE', 'WORKASPACE' ) );
#65999=CARTESIAN_POINT ( 'NONE',  ( 4.453875240780039491, -1.734723475976807094E-15, 16.57301948837323380 ) ) ;
#66001=CARTESIAN_POINT ( 'NONE',  ( -2.727034095388735757, -14.21045842199435860, -37.36840973699904822 ) ) ;
#66002=CARTESIAN_POINT ( 'NONE',  ( -78.51742362413880016, -36.02766478407949080, 134.0155194058749260 ) ) ;
#66004=CARTESIAN_POINT ( 'NONE',  ( 73.20367453073632191, -59.99999999999985789, 185.6239686060362146 ) ) ;
#66006=CARTESIAN_POINT ( 'NONE',  ( 94.29131450443634321, -57.67246088413772043, 24.29571120338738055 ) ) ;
#66022=ORIENTED_EDGE ( 'NONE', *, *, #12182, .T. ) ;
#66026=CARTESIAN_POINT ( 'NONE',  ( 30.91344358666947656, -49.90441520833090294, 35.32657779368672379 ) ) ;
#66041=CARTESIAN_POINT ( 'NONE',  ( 92.73814317491743964, -60.00000000000002132, -7.760776698426044007 ) ) ;
#66055=CARTESIAN_POINT ( 'NONE',  ( 85.33365913786940382, -52.71608586643078098, 1.351353659569916488 ) ) ;
#66066=CARTESIAN_POINT ( 'NONE',  ( -28.97838153899067137, -60.00000000000000000, 36.30225964348677792 ) ) ;
#66068=CARTESIAN_POINT ( 'NONE',  ( 68.22945241178948095, -25.58280432435164542, 88.38472783749070061 ) ) ;
#66073=CARTESIAN_POINT ( 'NONE',  ( -91.67701774657527380, -57.66167918384760327, -19.87712626951747552 ) ) ;
#66091=CARTESIAN_POINT ( 'NONE',  ( 12.78947859897790629, -60.00000000000000000, 39.70829609032173835 ) ) ;
#66093=CARTESIAN_POINT ( 'NONE',  ( -91.95742184699108179, -30.00000000000000000, 190.8556395465993774 ) ) ;
#66099=CARTESIAN_POINT ( 'NONE',  ( 73.33207134919089754, -57.63936585033923876, 183.5250597598029287 ) ) ;
#66102=CARTESIAN_POINT ( 'NONE',  ( 23.69903725379788284, -27.21825735636527455, -38.40810431224176114 ) ) ;
#66104=CARTESIAN_POINT ( 'NONE',  ( -41.23432746627220524, -59.99999999999999289, 53.93406616075787952 ) ) ;
#66108=CARTESIAN_POINT ( 'NONE',  ( -86.80924175235543316, -20.64942504254944922, 185.6736228309295598 ) ) ;
#66112=CARTESIAN_POINT ( 'NONE',  ( -10.23031279217029876, -35.99451456354128709, 29.89987121441171425 ) ) ;
#66125=CARTESIAN_POINT ( 'NONE',  ( 109.1953510978495956, -29.99999999999998934, 161.8808647345001646 ) ) ;
#66144=CARTESIAN_POINT ( 'NONE',  ( -76.06031650297444457, -60.00000000000984812, 194.6114218367068815 ) ) ;
#66147=CARTESIAN_POINT ( 'NONE',  ( 112.1408118161186991, -59.99999999999998579, 167.6738597471375840 ) ) ;
#66148=CARTESIAN_POINT ( 'NONE',  ( -76.30486425386099825, -30.00000000000004619, 168.5691345232379206 ) ) ;
#66149=CARTESIAN_POINT ( 'NONE',  ( 18.30455222202033738, -60.35759502867323079, 34.30908099980990755 ) ) ;
#66152=CARTESIAN_POINT ( 'NONE',  ( -43.22159273586203199, -46.43894676989327763, 43.43051601094587966 ) ) ;
#66164=CARTESIAN_POINT ( 'NONE',  ( 81.56357004051291426, -30.00000000000010303, -4.949223632071581669 ) ) ;
#66170=CARTESIAN_POINT ( 'NONE',  ( 92.70324471557209733, -29.99999999999999645, 104.2926456640488055 ) ) ;
#66189=CARTESIAN_POINT ( 'NONE',  ( 77.60215982985106109, -38.52546103277521894, 186.8513230885473888 ) ) ;
#66204=CARTESIAN_POINT ( 'NONE',  ( 6.482941653187340947, -18.96218766594433092, 35.15061247569060043 ) ) ;
#66210=CARTESIAN_POINT ( 'NONE',  ( 86.39342217817984704, -17.39602584710043587, 179.4229172789653717 ) ) ;
#66214=CARTESIAN_POINT ( 'NONE',  ( 93.08263284641110147, -57.65567480148813928, -17.01414318937586145 ) ) ;
#66216=CARTESIAN_POINT ( 'NONE',  ( -81.12945012041117820, -30.00000000000000711, 23.35381562080259954 ) ) ;
#66219=CARTESIAN_POINT ( 'NONE',  ( -85.15168385860675926, -37.99999999999996447, 183.5647360535557766 ) ) ;
#66228=CARTESIAN_POINT ( 'NONE',  ( -64.10993277136456925, -37.76178193452332010, -24.57515171481401595 ) ) ;
#66237=CARTESIAN_POINT ( 'NONE',  ( -64.59904024412152523, -29.72015457327714572, -23.23336862644748990 ) ) ;
#66241=CARTESIAN_POINT ( 'NONE',  ( -72.01167074608865448, -21.77034257964697872, -18.48521213137105335 ) ) ;
#66251=CARTESIAN_POINT ( 'NONE',  ( -52.47326062800689073, -60.00000000000000000, -37.40410650496403377 ) ) ;
#66256=CARTESIAN_POINT ( 'NONE',  ( 102.8270117144912632, -60.17405004303049765, 193.1076501718758607 ) ) ;
#66257=CARTESIAN_POINT ( 'NONE',  ( 2.499999999999997780, -18.83380486180452706, 27.02532357426314036 ) ) ;
#66260=EDGE_LOOP ( 'NONE', ( #19411, #84781 ) ) ;
#66270=CARTESIAN_POINT ( 'NONE',  ( -44.89949488402420030, -57.68324447995585302, 64.92693994880102082 ) ) ;
#66275=CARTESIAN_POINT ( 'NONE',  ( -25.62895382379538489, -60.00000000000000711, -43.76007060795225101 ) ) ;
#66276=CARTESIAN_POINT ( 'NONE',  ( -34.17891763260271887, -14.21045842199440301, 38.95228509905292924 ) ) ;
#66277=CARTESIAN_POINT ( 'NONE',  ( -51.71596078174152211, -25.65011578757576416, 48.87676497752350713 ) ) ;
#66281=CARTESIAN_POINT ( 'NONE',  ( -97.64691574547987329, -37.71246555177214077, 192.6310394866860349 ) ) ;
#66289=CARTESIAN_POINT ( 'NONE',  ( 96.60812357626146252, -38.48423040734370204, 201.1678166273348722 ) ) ;
#66295=CARTESIAN_POINT ( 'NONE',  ( 82.35949071855475268, -30.00000000000001066, 148.3810521812565923 ) ) ;
#66302=CARTESIAN_POINT ( 'NONE',  ( 52.62853896714921831, -32.57219741345102193, 52.90247569886912515 ) ) ;
#66304=EDGE_CURVE ( 'NONE', #77351, #32439, #11404, .T. ) ;
#66307=CARTESIAN_POINT ( 'NONE',  ( -90.59568090330395762, -38.34730571723916626, 12.65513652691200086 ) ) ;
#66310=CARTESIAN_POINT ( 'NONE',  ( 99.34690486943590315, -38.35585097942631450, 84.62317533721636664 ) ) ;
#66312=CARTESIAN_POINT ( 'NONE',  ( 84.82478036673688848, -37.84938749301726801, 44.26570419945227997 ) ) ;
#66314=DIRECTION ( 'NONE',  ( 0.000000000000000000, -0.000000000000000000, 1.000000000000000000 ) ) ;
#66317=CARTESIAN_POINT ( 'NONE',  ( 75.48311596653083200, -60.00000000000000711, 184.3857932157642949 ) ) ;
#66321=CARTESIAN_POINT ( 'NONE',  ( 61.11682477142169034, -53.38749459719494439, 82.02260153653946873 ) ) ;
#66327=CARTESIAN_POINT ( 'NONE',  ( -78.20651881317490961, -38.35596806284291915, -27.53224245461382935 ) ) ;
#66336=CARTESIAN_POINT ( 'NONE',  ( 81.82114106837175882, -57.06932440951347729, 184.1247409842175387 ) ) ;
#66346=CARTESIAN_POINT ( 'NONE',  ( 53.63423276373041659, -60.00000000000000000, 81.40523378288756362 ) ) ;
#66347=CIRCLE ( 'NONE', #100759, 74.46152422706630603 ) ;
#66349=CARTESIAN_POINT ( 'NONE',  ( 26.83690358097182482, -20.16800216920047006, 31.72032485502600352 ) ) ;
#66350=CARTESIAN_POINT ( 'NONE',  ( -12.34912842698533986, -21.29189974538021701, 35.60347046151010630 ) ) ;
#66365=CARTESIAN_POINT ( 'NONE',  ( 41.98975166001473980, -60.22823911148290676, -33.55402375021320438 ) ) ;
#66374=CARTESIAN_POINT ( 'NONE',  ( -95.53046091001213824, -60.00000000000000000, 52.81045404649977115 ) ) ;
#66381=CARTESIAN_POINT ( 'NONE',  ( -82.14756253037036515, -49.98515285713766332, 178.0770026145764291 ) ) ;
#66385=EDGE_LOOP ( 'NONE', ( #93910, #30553, #74869, #3237 ) ) ;
#66392=CARTESIAN_POINT ( 'NONE',  ( -2.826893917877371987, -57.67120211504744987, -44.61186535421596489 ) ) ;
#66398=CARTESIAN_POINT ( 'NONE',  ( 106.5496036037455809, -14.21045842199433373, 161.7522804960935900 ) ) ;
#66399=CARTESIAN_POINT ( 'NONE',  ( -109.3240689110004524, -30.00000000000000355, 163.9542341103382057 ) ) ;
#66400=CARTESIAN_POINT ( 'NONE',  ( -59.58922826906859171, -29.07209130795614271, 66.35028759016553579 ) ) ;
#66403=CARTESIAN_POINT ( 'NONE',  ( 110.2524109620066355, -59.99999999998756550, 196.4786846540791316 ) ) ;
#66405=CARTESIAN_POINT ( 'NONE',  ( 8.225526725709833897, -46.43474543944358857, 31.62224987670555976 ) ) ;
#66406=CARTESIAN_POINT ( 'NONE',  ( -101.8692908878811352, -45.26559888734792025, 144.5090998712010162 ) ) ;
#66413=CARTESIAN_POINT ( 'NONE',  ( -74.49046798774418221, -60.00000000000002842, 177.0422497158886870 ) ) ;
#66424=CARTESIAN_POINT ( 'NONE',  ( 104.7773608882266529, -59.99999999999998579, 148.0886741368902051 ) ) ;
#66425=CARTESIAN_POINT ( 'NONE',  ( -33.27768848828844028, -36.02923593097368382, 33.82197891432520009 ) ) ;
#66427=CARTESIAN_POINT ( 'NONE',  ( 43.39891897988977121, -53.34186061554017755, 45.35487243743281027 ) ) ;
#66434=CARTESIAN_POINT ( 'NONE',  ( -76.08373685344359671, -38.38310391996776616, 178.9727446662289481 ) ) ;
#66448=CARTESIAN_POINT ( 'NONE',  ( 102.5207257002704608, -59.99999999999998579, 95.78292118410128353 ) ) ;
#66455=CARTESIAN_POINT ( 'NONE',  ( -100.5402992199712600, -29.99999999999999289, 182.6301088287440848 ) ) ;
#66466=CARTESIAN_POINT ( 'NONE',  ( 83.26732716159929737, -36.00583431519718403, 166.7925075315839365 ) ) ;
#66481=CARTESIAN_POINT ( 'NONE',  ( 86.96106181210527097, -35.41080976886706821, 188.0754270986170695 ) ) ;
#66501=CARTESIAN_POINT ( 'NONE',  ( 113.5519812807844033, -57.67142723623354073, 158.0961491198512476 ) ) ;
#66510=CARTESIAN_POINT ( 'NONE',  ( -86.36548893003080707, -60.00000000000000711, 200.7376711920367143 ) ) ;
#66514=CARTESIAN_POINT ( 'NONE',  ( 89.99999999999997158, 500000.0000000000582, 196.0238439516549818 ) ) ;
#66516=CARTESIAN_POINT ( 'NONE',  ( -84.33089495578791173, -42.97883097878487035, 183.3478449006408937 ) ) ;
#66525=CARTESIAN_POINT ( 'NONE',  ( -83.21592982314025733, -37.80011021608530797, -4.677426421150369329 ) ) ;
#66534=CARTESIAN_POINT ( 'NONE',  ( -55.21321105934377726, -60.00000000000002842, -39.23988760269474341 ) ) ;
#66535=CARTESIAN_POINT ( 'NONE',  ( -76.67228451078059948, -32.55182850295351216, 122.5207825894436979 ) ) ;
#66537=CARTESIAN_POINT ( 'NONE',  ( 75.43375447319739635, -30.00000000000006395, 160.3035121353613306 ) ) ;
#66539=CARTESIAN_POINT ( 'NONE',  ( 94.03892859735442755, -57.67587636535527906, 4.912622737924200678 ) ) ;
#66557=CARTESIAN_POINT ( 'NONE',  ( 28.36086065759023001, -22.10831334729735431, 29.53362645638507544 ) ) ;
#66572=CARTESIAN_POINT ( 'NONE',  ( 86.86402307942935863, -60.00000000000000711, -22.80661258863997176 ) ) ;
#66588=CARTESIAN_POINT ( 'NONE',  ( 83.19617777001812442, -37.83149000724398547, -4.129211925961556062 ) ) ;
#66598=VECTOR ( 'NONE', #103153, 1000.000000000000000 ) ;
#66602=CARTESIAN_POINT ( 'NONE',  ( 68.45974218760680685, -22.10775288249442383, 87.18709934866549816 ) ) ;
#66608=CARTESIAN_POINT ( 'NONE',  ( -113.5594301016874539, -57.67117831481159840, 184.0234983118591856 ) ) ;
#66611=CARTESIAN_POINT ( 'NONE',  ( 102.6967805458878047, -37.84840159047918462, 167.9561026369516128 ) ) ;
#66626=CARTESIAN_POINT ( 'NONE',  ( 9.217957586093081801, -59.99999999999999289, 39.64182104935679263 ) ) ;
#66627=CARTESIAN_POINT ( 'NONE',  ( -98.33419151583822782, -30.00000000000000000, 190.1125085183297756 ) ) ;
#66632=CARTESIAN_POINT ( 'NONE',  ( 71.38313853796425690, -57.68021046702090615, 165.8956670029349993 ) ) ;
#66636=CARTESIAN_POINT ( 'NONE',  ( 19.32074472756938022, -25.58899134302987122, -38.49253709561221370 ) ) ;
#66639=CARTESIAN_POINT ( 'NONE',  ( -46.17444693964949920, -60.00000000000000711, 63.00263890028006131 ) ) ;
#66644=CARTESIAN_POINT ( 'NONE',  ( -86.97243100496625345, -42.77928646493604958, 189.9052986841667519 ) ) ;
#66647=CARTESIAN_POINT ( 'NONE',  ( -9.120514393641915518, -29.03121919898077863, 28.72967367393797389 ) ) ;
#66661=FACE_OUTER_BOUND ( 'NONE', #57953, .T. ) ;
#66663=CARTESIAN_POINT ( 'NONE',  ( 106.6845404271915925, -14.21045842199438525, 180.1433801272770836 ) ) ;
#66664=CARTESIAN_POINT ( 'NONE',  ( -81.94379596842044577, -39.49948281330256350, 160.0918886956195308 ) ) ;
#66687=CARTESIAN_POINT ( 'NONE',  ( 110.5157368889957610, -60.00000000000000000, 189.3796442602921672 ) ) ;
#66688=CARTESIAN_POINT ( 'NONE',  ( -78.65018897216694427, -14.21045842199436571, 174.1869015730407000 ) ) ;
#66689=CARTESIAN_POINT ( 'NONE',  ( 15.95816837728402149, -56.87732999964022440, 33.56976140312947621 ) ) ;
#66690=CARTESIAN_POINT ( 'NONE',  ( 83.25561225319275138, -37.99999999999993605, -8.576613537955827482 ) ) ;
#66693=CARTESIAN_POINT ( 'NONE',  ( -41.45979221839193940, -46.43697368219972788, 41.56452721125755545 ) ) ;
#66696=DIRECTION ( 'NONE',  ( 0.000000000000000000, -1.000000000000000000, 0.000000000000000000 ) ) ;
#66704=CARTESIAN_POINT ( 'NONE',  ( -45.30326460949155631, -38.31529918028564907, 58.49194340069017528 ) ) ;
#66707=CARTESIAN_POINT ( 'NONE',  ( 80.23011466839570005, -30.00000000000003197, -13.48167149206803295 ) ) ;
#66713=CARTESIAN_POINT ( 'NONE',  ( 81.06357478099751290, -29.99999999999999645, 22.11501143710179562 ) ) ;
#66729=CARTESIAN_POINT ( 'NONE',  ( 72.82563136666954051, -38.32591977635656377, 151.2887102636987322 ) ) ;
#66754=CARTESIAN_POINT ( 'NONE',  ( 85.28715672339788512, -42.92956674362846314, 186.5443997153789724 ) ) ;
#66758=CARTESIAN_POINT ( 'NONE',  ( 91.50964524610877504, -57.66228111830159975, -20.14352967758682311 ) ) ;
#66759=DIRECTION ( 'NONE',  ( 0.000000000000000000, 0.000000000000000000, 1.000000000000000000 ) ) ;
#66762=CARTESIAN_POINT ( 'NONE',  ( -80.77720312678583525, -30.00000000000000000, 9.967219224732877692 ) ) ;
#66773=CARTESIAN_POINT ( 'NONE',  ( -51.00726465901860252, -36.03376012008488516, -27.78095564560482700 ) ) ;
#66775=CARTESIAN_POINT ( 'NONE',  ( -98.14539993508641658, -37.99999999999994316, 192.4866759319958476 ) ) ;
#66783=CARTESIAN_POINT ( 'NONE',  ( -46.80132320916015232, -26.73529330813730454, -28.77368927080993188 ) ) ;
#66794=CARTESIAN_POINT ( 'NONE',  ( -83.65165148681774099, -60.00000000000000000, -25.56542375944041723 ) ) ;
#66798=CARTESIAN_POINT ( 'NONE',  ( 99.50318429255658259, -37.82977025964015638, 191.3434515804738112 ) ) ;
#66811=CARTESIAN_POINT ( 'NONE',  ( -37.03244656124025624, -57.69633701093174949, 51.43040253561569131 ) ) ;
#66817=CARTESIAN_POINT ( 'NONE',  ( -89.66619014120909981, -60.00000000000001421, -23.31631894612182521 ) ) ;
#66820=CARTESIAN_POINT ( 'NONE',  ( -49.35531877875648377, -53.36885908633350795, 54.26204743392272434 ) ) ;
#66830=CARTESIAN_POINT ( 'NONE',  ( 103.8938049727245669, -38.41582098933665890, 198.4886963997253133 ) ) ;
#66835=CARTESIAN_POINT ( 'NONE',  ( 89.52544717665139729, -30.00000000000000355, 189.4090387211008419 ) ) ;
#66843=CARTESIAN_POINT ( 'NONE',  ( 52.52745653095553280, -49.90442938472995138, 59.15515806098346729 ) ) ;
#66845=CARTESIAN_POINT ( 'NONE',  ( 9.999999999999998224, 0.000000000000000000, -9.999999999999998224 ) ) ;
#66847=CARTESIAN_POINT ( 'NONE',  ( -92.36008094370296817, -38.35495905226510160, 38.05242013568155812 ) ) ;
#66851=CARTESIAN_POINT ( 'NONE',  ( 109.9456817262660877, -38.35603827305180147, 154.1022712922482185 ) ) ;
#66853=CARTESIAN_POINT ( 'NONE',  ( 89.51473135658183367, -45.28271082105466405, 67.81559373879049701 ) ) ;
#66859=CARTESIAN_POINT ( 'NONE',  ( 75.45442456345966775, -60.00000000000002132, 184.2217590398179823 ) ) ;
#66864=CARTESIAN_POINT ( 'NONE',  ( 61.37175430821151423, -60.33933855911503485, 86.28502804520786640 ) ) ;
#66880=CARTESIAN_POINT ( 'NONE',  ( 86.13882259233811567, -18.34482622158760989, 167.7275104523019991 ) ) ;
#66889=CARTESIAN_POINT ( 'NONE',  ( -13.57428064878229890, -23.62732209985536969, -38.53619311655949531 ) ) ;
#66893=CARTESIAN_POINT ( 'NONE',  ( 49.28483115600248965, -60.00000000000000000, 70.03155139212616120 ) ) ;
#66897=CARTESIAN_POINT ( 'NONE',  ( 19.21337042771324377, -16.78003050461148504, 31.49141766188020242 ) ) ;
#66898=VECTOR ( 'NONE', #48533, 1000.000000000000000 ) ;
#66899=CARTESIAN_POINT ( 'NONE',  ( -7.580914931690657887, -19.30281391077188147, 35.20923601663831448 ) ) ;
#66912=CARTESIAN_POINT ( 'NONE',  ( 16.18283418694998588, -60.22807642560611896, -36.38454838023258731 ) ) ;
#66925=CARTESIAN_POINT ( 'NONE',  ( -101.5459148796837212, -60.00000000000000000, 90.09389878889895442 ) ) ;
#66931=CARTESIAN_POINT ( 'NONE',  ( -81.78828991020175465, -53.49607135933386814, 179.9890600379855243 ) ) ;
#66948=CARTESIAN_POINT ( 'NONE',  ( 89.52590460267296635, -30.00000000000006395, 22.04891038916446888 ) ) ;
#66949=CARTESIAN_POINT ( 'NONE',  ( -106.5495191435086468, -14.21045842199437992, 161.7519935124221604 ) ) ;
#66951=CARTESIAN_POINT ( 'NONE',  ( -58.77187156240383814, -29.07515625515527447, 64.41617457802827573 ) ) ;
#66954=CARTESIAN_POINT ( 'NONE',  ( 112.7988352096499369, -60.00000000000001421, 189.9832682156421129 ) ) ;
#66956=CARTESIAN_POINT ( 'NONE',  ( 4.060351201658883191, -42.95350087791473470, 31.04114541283799156 ) ) ;
#66957=CARTESIAN_POINT ( 'NONE',  ( -104.6405814182722480, -60.15514485569779879, 146.7656546127498984 ) ) ;
#66965=CARTESIAN_POINT ( 'NONE',  ( -72.42031090680902139, -60.00000000000001421, 157.4287250850663895 ) ) ;
#66975=CARTESIAN_POINT ( 'NONE',  ( 86.14605752652843762, -59.99999999999999289, 15.79010570469148789 ) ) ;
#66976=CARTESIAN_POINT ( 'NONE',  ( -32.30820442022806560, -46.43510695185953807, 35.30439282640345056 ) ) ;
#66978=CARTESIAN_POINT ( 'NONE',  ( 41.39420356405966572, -18.78398962539201733, 34.98631649356083528 ) ) ;
#66983=CARTESIAN_POINT ( 'NONE',  ( -76.90211361482964492, -38.44896177797908621, 183.8811321853390552 ) ) ;
#66987=CARTESIAN_POINT ( 'NONE',  ( 77.37879385987021408, -60.00000000000004263, 150.9693798004460348 ) ) ;
#66995=CARTESIAN_POINT ( 'NONE',  ( 105.7023782531532134, -60.00000000000000000, 114.6129108351607044 ) ) ;
#67001=CARTESIAN_POINT ( 'NONE',  ( -85.72047231801046507, -29.99999999999986855, 176.6773169481917591 ) ) ;
#67014=CARTESIAN_POINT ( 'NONE',  ( 84.47855945016070223, -18.66665705232763983, 151.2491824433281522 ) ) ;
#67048=CARTESIAN_POINT ( 'NONE',  ( 113.4126431804666311, -57.67118003651737723, 185.0856980667289235 ) ) ;
#67056=CARTESIAN_POINT ( 'NONE',  ( -89.92895766737007079, -60.00000000000002842, 201.9442179873481678 ) ) ;
#67060=CARTESIAN_POINT ( 'NONE',  ( -82.99502123910362172, -60.92268927480029816, 190.5952502046357324 ) ) ;
#67066=CARTESIAN_POINT ( 'NONE',  ( -86.65482536451017381, -60.23408797249618374, -11.84100989679749816 ) ) ;
#67073=CARTESIAN_POINT ( 'NONE',  ( 45.38117173420300787, -14.21045842199442077, 49.92181071548740334 ) ) ;
#67075=CARTESIAN_POINT ( 'NONE',  ( -60.75193363616918418, -14.21045842199437281, -29.98592940458554779 ) ) ;
#67076=CARTESIAN_POINT ( 'NONE',  ( -67.99944868274178589, -29.05959306063812519, 89.58447443812319477 ) ) ;
#67078=CARTESIAN_POINT ( 'NONE',  ( 76.85420403038403947, -14.21045842199429288, 149.6289235591555666 ) ) ;
#67080=CARTESIAN_POINT ( 'NONE',  ( 93.88541012961576371, -57.67354554259142674, 15.96172296223697806 ) ) ;
#67095=UNCERTAINTY_MEASURE_WITH_UNIT (LENGTH_MEASURE( 1.000000000000000082E-05 ), #4598, 'distance_accuracy_value', 'NONE');
#67099=CARTESIAN_POINT ( 'NONE',  ( 31.99307667142880263, -29.08164122046728295, 31.97780603565110980 ) ) ;
#67113=CARTESIAN_POINT ( 'NONE',  ( 91.74875941113400302, -59.99999999999999289, -14.85367483812130551 ) ) ;
#67127=CARTESIAN_POINT ( 'NONE',  ( 85.74599729795382075, -52.74913451446589363, -7.705021881710077736 ) ) ;
#67142=CARTESIAN_POINT ( 'NONE',  ( 72.65174976871776380, -46.43323079597204384, 115.6298787946136599 ) ) ;
#67147=CARTESIAN_POINT ( 'NONE',  ( -85.55066431120862092, -57.67066120584623690, -26.59325976709777706 ) ) ;
#67151=CARTESIAN_POINT ( 'NONE',  ( 102.4821652698666270, -37.84834387798020572, 163.3383496542420801 ) ) ;
#67153=DIRECTION ( 'NONE',  ( -0.000000000000000000, 1.000000000000000000, 0.000000000000000000 ) ) ;
#67171=CARTESIAN_POINT ( 'NONE',  ( -84.30164704855529578, -30.00000000000000000, 163.7302190737703711 ) ) ;
#67177=CARTESIAN_POINT ( 'NONE',  ( 70.41017571245976114, -57.68249222584282165, 157.3648689374751370 ) ) ;
#67183=CARTESIAN_POINT ( 'NONE',  ( 37.43042651949708954, -32.13357833424133503, -37.68003761008185393 ) ) ;
#67186=CARTESIAN_POINT ( 'NONE',  ( -47.26077543882751542, -59.99999999999999289, 65.36119327807321611 ) ) ;
#67190=CARTESIAN_POINT ( 'NONE',  ( -86.71692066761134754, -24.38214587370727671, 185.1863996357423900 ) ) ;
#67193=CARTESIAN_POINT ( 'NONE',  ( -9.152872775044887277, -32.51284889757581453, 29.31026127488318167 ) ) ;
#67209=CARTESIAN_POINT ( 'NONE',  ( 109.0818019194042847, -30.00000000000000355, 182.6293461004923131 ) ) ;
#67210=CARTESIAN_POINT ( 'NONE',  ( -83.35807197383493872, -25.61544833356139250, 152.1595157485745347 ) ) ;
#67219=VERTEX_POINT ( 'NONE', #78027 ) ;
#67231=CARTESIAN_POINT ( 'NONE',  ( 112.0559613019898535, -60.00000000000000000, 178.9342536578935210 ) ) ;
#67232=CARTESIAN_POINT ( 'NONE',  ( -97.13635602990564166, -30.00000000000002842, 199.9106954788804842 ) ) ;
#67233=CARTESIAN_POINT ( 'NONE',  ( 21.50664772083280951, -46.43444599742699808, 32.33001467109113491 ) ) ;
#67238=CARTESIAN_POINT ( 'NONE',  ( -40.62314756017665474, -49.89205973216389367, 41.58854808969374517 ) ) ;
#67249=CARTESIAN_POINT ( 'NONE',  ( 81.59257212631717948, -30.00000000000000711, -7.373243558649345886 ) ) ;
#67254=CARTESIAN_POINT ( 'NONE',  ( 83.46915891402045418, -30.00000000000000000, 46.60997905724752144 ) ) ;
#67272=EDGE_LOOP ( 'NONE', ( #69995, #102586, #40975, #45717 ) ) ;
#67273=CARTESIAN_POINT ( 'NONE',  ( 61.26180592153973237, -38.34168193138184222, 100.4494290447654663 ) ) ;
#67294=CARTESIAN_POINT ( 'NONE',  ( 85.68501797939430276, -39.26251600558322963, 186.0341779385333894 ) ) ;
#67298=CARTESIAN_POINT ( 'NONE',  ( 93.17075602859650019, -57.65531965366547240, -16.78974746904759741 ) ) ;
#67301=CARTESIAN_POINT ( 'NONE',  ( -94.04704852291118300, -29.99999999999999645, 112.2487365680688782 ) ) ;
#67316=CARTESIAN_POINT ( 'NONE',  ( 19.76895601567771266, -18.47386612047070997, -33.76156256446066095 ) ) ;
#67317=CARTESIAN_POINT ( 'NONE',  ( -25.87975877140922520, -18.61425406802221261, 28.34855765540077499 ) ) ;
#67323=CARTESIAN_POINT ( 'NONE',  ( -66.26923848658640281, -29.83372399135324571, -22.51683101449095759 ) ) ;
#67333=CARTESIAN_POINT ( 'NONE',  ( -87.91896268344133603, -59.99999999999997868, -21.67466428380060250 ) ) ;
#67338=CARTESIAN_POINT ( 'NONE',  ( 101.8255536633035092, -60.21687307657023069, 194.3872987722783137 ) ) ;
#67352=CARTESIAN_POINT ( 'NONE',  ( -30.75663703201544408, -57.68613454458090217, 45.71164565728040685 ) ) ;
#67356=CARTESIAN_POINT ( 'NONE',  ( -82.54102867968215662, -60.00000000000007105, -29.20875881225653004 ) ) ;
#67359=CARTESIAN_POINT ( 'NONE',  ( -52.40382998801522518, -22.17894777271752460, 48.78687196755927857 ) ) ;
#67367=CARTESIAN_POINT ( 'NONE',  ( 79.42188716763993739, -38.73604089626370950, 191.9100328722365418 ) ) ;
#67372=CARTESIAN_POINT ( 'NONE',  ( 87.77046421779371599, -29.99999999999999645, 186.1866013582121298 ) ) ;
#67377=ADVANCED_FACE ( 'NONE', ( #21939 ), #53746, .F. ) ;
#67380=CARTESIAN_POINT ( 'NONE',  ( 51.22218799938233502, -60.30135857894056528, 60.32169156076044203 ) ) ;
#67386=CARTESIAN_POINT ( 'NONE',  ( -92.65791048185651846, -38.35495741458606034, 40.59163175469802809 ) ) ;
#67389=CARTESIAN_POINT ( 'NONE',  ( 110.2552427511137267, -38.35601349421322226, 184.2954527649220893 ) ) ;
#67391=CARTESIAN_POINT ( 'NONE',  ( 87.11640230159049736, -52.71607002794502250, 42.63259187033803954 ) ) ;
#67402=CARTESIAN_POINT ( 'NONE',  ( 60.36974275104975618, -29.06706137689814540, 68.28589426947422680 ) ) ;
#67417=CARTESIAN_POINT ( 'NONE',  ( 84.39719784251927592, -39.41516335604673316, 180.8079987764798489 ) ) ;
#67426=CARTESIAN_POINT ( 'NONE',  ( -23.44733519253580667, -27.12328492395885604, -38.41448460140718169 ) ) ;
#67430=CARTESIAN_POINT ( 'NONE',  ( 53.73123005835647348, -60.00000000000000711, 81.67570342333168298 ) ) ;
#67433=CARTESIAN_POINT ( 'NONE',  ( 20.28983781531179531, -17.22150327053471486, 31.47367925788013210 ) ) ;
#67434=CARTESIAN_POINT ( 'NONE',  ( -2.499999999981197707, -21.99834632368703069, -30.53960193249073640 ) ) ;
#67448=CARTESIAN_POINT ( 'NONE',  ( 32.37152068336183675, -60.22820715367447519, -34.89893449057208130 ) ) ;
#67457=CARTESIAN_POINT ( 'NONE',  ( -103.7243948980324006, -60.00000000000000000, 102.8245780598074077 ) ) ;
#67465=CARTESIAN_POINT ( 'NONE',  ( -85.49467086792562043, -21.96977942738778822, 166.0364208305039426 ) ) ;
#67466=ORIENTED_EDGE ( 'NONE', *, *, #48504, .F. ) ;
#67473=CARTESIAN_POINT ( 'NONE',  ( -72.61817094705909881, -45.32535816143199270, -22.56079433717181715 ) ) ;
#67478=( NAMED_UNIT ( * ) SI_UNIT ( $, .STERADIAN. ) SOLID_ANGLE_UNIT ( ) );
#67481=CARTESIAN_POINT ( 'NONE',  ( 89.32114860119857269, -29.99999999999995026, 17.89867789164953393 ) ) ;
#67482=CARTESIAN_POINT ( 'NONE',  ( -106.7759996721837297, -60.00000000000014211, 200.9056163170290858 ) ) ;
#67483=CARTESIAN_POINT ( 'NONE',  ( -57.95451485573907746, -29.07822120235440622, 62.48206156589100857 ) ) ;
#67485=CARTESIAN_POINT ( 'NONE',  ( 47.44000135571184273, -60.00000000002890488, -40.81002596378207414 ) ) ;
#67487=CARTESIAN_POINT ( 'NONE',  ( 7.205507455416617191, -49.91572346798661641, 32.19931394973104233 ) ) ;
#67488=CARTESIAN_POINT ( 'NONE',  ( -106.2891245437193675, -60.15515527080706448, 179.7497780154444058 ) ) ;
#67489=( NAMED_UNIT ( * ) PLANE_ANGLE_UNIT ( ) SI_UNIT ( $, .RADIAN. ) );
#67495=CARTESIAN_POINT ( 'NONE',  ( -79.40048706246868448, -60.00000000000001421, 195.2207880595982772 ) ) ;
#67499=CARTESIAN_POINT ( 'NONE',  ( 13.52487676486885348, 0.000000000000000000, 10.38441970551129501 ) ) ;
#67506=CARTESIAN_POINT ( 'NONE',  ( -30.53886170152374291, -18.65827435953780977, 29.53940708261786341 ) ) ;
#67508=CARTESIAN_POINT ( 'NONE',  ( 44.33516561222944574, -60.24910389432578484, 48.28984989065179434 ) ) ;
#67514=CARTESIAN_POINT ( 'NONE',  ( -81.68379548809339497, -38.84189794985886124, 195.5063719952446775 ) ) ;
#67518=CARTESIAN_POINT ( 'NONE',  ( 34.59539548351714444, -59.99999999999999289, 38.98399512715914028 ) ) ;
#67525=CARTESIAN_POINT ( 'NONE',  ( 106.3113036129748821, -60.00000000000000711, 118.3450711846818422 ) ) ;
#67533=CARTESIAN_POINT ( 'NONE',  ( -97.95549896524885014, -29.99999999999989342, 190.5752664689312894 ) ) ;
#67546=CARTESIAN_POINT ( 'NONE',  ( 80.67535997844298379, -49.91147864860721484, 164.5085625698619936 ) ) ;
#67563=CARTESIAN_POINT ( 'NONE',  ( 87.26958111220818637, -50.07308097134770719, 192.1704676255311881 ) ) ;
#67588=CARTESIAN_POINT ( 'NONE',  ( -79.77917837913028620, -60.00000000000000711, 195.7066188485981399 ) ) ;
#67592=CARTESIAN_POINT ( 'NONE',  ( -84.32939227294266971, -46.57010899852983243, 185.7296267468632607 ) ) ;
#67599=CARTESIAN_POINT ( 'NONE',  ( -85.16386424983127768, -52.70345752972548325, 3.865554627149779154 ) ) ;
#67606=CARTESIAN_POINT ( 'NONE',  ( 58.28796150060976089, -14.21045842199433729, 78.47796032183087789 ) ) ;
#67608=CARTESIAN_POINT ( 'NONE',  ( -85.44375122223560481, -14.21045842199445630, -16.44937377337592466 ) ) ;
#67609=CARTESIAN_POINT ( 'NONE',  ( -68.69079975540086025, -18.63268183060117877, 85.99216174777282617 ) ) ;
#67611=CARTESIAN_POINT ( 'NONE',  ( 69.85392978727392688, -60.00000000000004263, 155.8703566448706113 ) ) ;
#67613=CARTESIAN_POINT ( 'NONE',  ( 44.68316001078914468, -60.00000000001960387, 65.34536827560972938 ) ) ;
#67628=CARTESIAN_POINT ( 'NONE',  ( 3.301565691951519721, -4.285714285714296246, -25.05982991920904723 ) ) ;
#67637=CARTESIAN_POINT ( 'NONE',  ( 30.53703330449200237, -18.65834619125411109, 29.53878724365041464 ) ) ;
#67649=CARTESIAN_POINT ( 'NONE',  ( 81.12437216259647244, -59.99999999999999289, -27.26058583151750270 ) ) ;
#67661=CARTESIAN_POINT ( 'NONE',  ( 85.85151669601329161, -60.21672556079247585, -14.42664014460055988 ) ) ;
#67665=ADVANCED_FACE ( 'NONE', ( #1316 ), #34278, .F. ) ;
#67673=CARTESIAN_POINT ( 'NONE',  ( 72.21471659750817196, -22.11717074490460178, 98.80210365957880470 ) ) ;
#67678=CARTESIAN_POINT ( 'NONE',  ( -92.76317396897962908, -57.65703681568646743, -17.81073576277876569 ) ) ;
#67683=CARTESIAN_POINT ( 'NONE',  ( 103.1592532910830471, -45.28273945504021469, 184.6164784094243032 ) ) ;
#67694=AXIS2_PLACEMENT_3D ( 'NONE', #100179, #18776, #66759 ) ;
#67697=EDGE_LOOP ( 'NONE', ( #68479, #73052 ) ) ;
#67702=CARTESIAN_POINT ( 'NONE',  ( -85.49926595847192345, -30.00000000000000000, 174.8177305309835674 ) ) ;
#67707=CARTESIAN_POINT ( 'NONE',  ( 71.51784493620726835, -57.67947522968200502, 167.2032557688225154 ) ) ;
#67710=CARTESIAN_POINT ( 'NONE',  ( 47.36551243866970395, -34.95418281838176711, -36.56030574305207637 ) ) ;
#67712=CARTESIAN_POINT ( 'NONE',  ( -48.61603543328580912, -60.00000000000000711, 68.43586388735928949 ) ) ;
#67714=CARTESIAN_POINT ( 'NONE',  ( -86.83128596798019316, -35.43248611210681531, 187.7796440410022853 ) ) ;
#67715=ORIENTED_EDGE ( 'NONE', *, *, #48504, .T. ) ;
#67717=CARTESIAN_POINT ( 'NONE',  ( -3.081151406350138178, -56.88415668120669721, 33.36504120651643746 ) ) ;
#67732=CARTESIAN_POINT ( 'NONE',  ( 106.2140667560022536, -14.21045842199435860, 184.2067176257025380 ) ) ;
#67733=CARTESIAN_POINT ( 'NONE',  ( -80.49898587717534326, -42.97031838899095391, 153.3002156829724356 ) ) ;
#67752=CARTESIAN_POINT ( 'NONE',  ( 109.7201212107555222, -60.00000000000001421, 141.0713185866662798 ) ) ;
#67753=CARTESIAN_POINT ( 'NONE',  ( -86.50885295532998498, -60.00000000000009237, 203.5147570966663011 ) ) ;
#67754=CARTESIAN_POINT ( 'NONE',  ( 22.90497520565338618, -53.39364463476709233, 33.72890349766722551 ) ) ;
#67757=CARTESIAN_POINT ( 'NONE',  ( -42.14242943275500153, -39.52740482707008596, 40.59973544904098475 ) ) ;
#67762=LINE ( 'NONE', #85009, #81818 ) ;
#67770=CARTESIAN_POINT ( 'NONE',  ( 59.42959829229317847, -29.99999999993401900, 90.05551113897882942 ) ) ;
#67772=CIRCLE ( 'NONE', #43735, 7.499999999992679633 ) ;
#67775=CARTESIAN_POINT ( 'NONE',  ( 86.61642755793405968, -30.00000000000000355, 68.10716385505197934 ) ) ;
#67792=CARTESIAN_POINT ( 'NONE',  ( 75.45753799503356163, -38.35118960347601558, 173.8236108886823956 ) ) ;
#67816=CARTESIAN_POINT ( 'NONE',  ( 84.74699022287541084, -50.18978294560194797, 188.7071310768435524 ) ) ;
#67824=CARTESIAN_POINT ( 'NONE',  ( -85.87820296494453487, -30.00000000000000000, 63.41064199202992313 ) ) ;
#67829=CARTESIAN_POINT ( 'NONE',  ( -51.84566471874714466, -38.00000000000001421, 53.44666163652544100 ) ) ;
#67834=CARTESIAN_POINT ( 'NONE',  ( 41.91057518544140947, -25.42445561657448394, -29.89054115698944969 ) ) ;
#67836=CARTESIAN_POINT ( 'NONE',  ( -26.36605410305137909, -46.43802873313279633, 33.26382985736353248 ) ) ;
#67838=CARTESIAN_POINT ( 'NONE',  ( -17.45941954208535307, -18.58880440242212018, 27.26036603235977296 ) ) ;
#67840=CARTESIAN_POINT ( 'NONE',  ( -54.44869668617586456, -28.39263527606577853, -26.74396193234344565 ) ) ;
#67856=CARTESIAN_POINT ( 'NONE',  ( 102.7294937518374098, -60.17726499089666703, 193.2519588841914810 ) ) ;
#67872=CARTESIAN_POINT ( 'NONE',  ( -40.46187072321335165, -57.69130470027779012, 56.40641529803505705 ) ) ;
#67876=CARTESIAN_POINT ( 'NONE',  ( -95.23228170574914486, -59.99999999999995737, 30.92731164540345645 ) ) ;
#67878=CARTESIAN_POINT ( 'NONE',  ( -49.37788450122778983, -36.05643262852323261, 48.61507133927151614 ) ) ;
#67888=CARTESIAN_POINT ( 'NONE',  ( 75.89775319832926925, -38.36850784122120928, 177.7196282691413103 ) ) ;
#67893=CARTESIAN_POINT ( 'NONE',  ( 90.32749040348188885, -30.00000000000000000, 190.1148432507463610 ) ) ;
#67900=CARTESIAN_POINT ( 'NONE',  ( 51.44370365268617462, -53.36997065266968576, 58.22489762912441336 ) ) ;
#67905=CARTESIAN_POINT ( 'NONE',  ( -86.58581895693029651, -38.36255730625217808, -21.30046015158363204 ) ) ;
#67908=CARTESIAN_POINT ( 'NONE',  ( 108.8405169039002658, -38.35664350992961147, 190.6511209365205559 ) ) ;
#67910=CARTESIAN_POINT ( 'NONE',  ( 93.88942621708076786, -52.71697813123014953, 86.64237755783022976 ) ) ;
#67924=ORIENTED_EDGE ( 'NONE', *, *, #30573, .F. ) ;
#67930=CARTESIAN_POINT ( 'NONE',  ( 46.68287061863885867, -28.88195831521701962, 41.82624838710184889 ) ) ;
#67935=CARTESIAN_POINT ( 'NONE',  ( 84.60774502086400162, -35.87429910332870975, 178.5856127707324958 ) ) ;
#67946=CARTESIAN_POINT ( 'NONE',  ( -36.53758404866636766, -31.84355814719485522, -37.75376796106051103 ) ) ;
#67950=CARTESIAN_POINT ( 'NONE',  ( 51.50689545266209279, -59.99999999999999289, 75.64874100463009654 ) ) ;
#67951=CARTESIAN_POINT ( 'NONE',  ( 27.11672592962718653, -30.49100857079985261, 39.11945417788622592 ) ) ;
#67953=CARTESIAN_POINT ( 'NONE',  ( 5.701534300459289994, -12.96799601469463958, 32.08129232778961182 ) ) ;
#67954=CARTESIAN_POINT ( 'NONE',  ( -29.17202919767179026, -31.89494080154250355, 40.11040161891606459 ) ) ;
#67966=CARTESIAN_POINT ( 'NONE',  ( 18.93998220273022071, -34.58964014173281498, -31.89241200920337604 ) ) ;
#67978=CARTESIAN_POINT ( 'NONE',  ( -91.89192752807107922, -59.99999999999999289, 9.067612356765010873 ) ) ;
#67985=CARTESIAN_POINT ( 'NONE',  ( -81.36484122651633299, -57.00091329419471009, 181.4273748944744113 ) ) ;
#67992=CARTESIAN_POINT ( 'NONE',  ( 10.00000000000000000, -15.00000000000000000, 10.00000000000000178 ) ) ;
#68002=CARTESIAN_POINT ( 'NONE',  ( 88.10210802036469602, -14.21045842199426090, 36.33415240954661840 ) ) ;
#68004=CARTESIAN_POINT ( 'NONE',  ( -101.7136998165503883, -14.21045842199435150, 195.4607583018654395 ) ) ;
#68005=CARTESIAN_POINT ( 'NONE',  ( -58.40069796809858360, -36.02129440492078061, 66.61610187002420957 ) ) ;
#68009=CARTESIAN_POINT ( 'NONE',  ( -103.9973128897120915, -45.26549305579687399, 174.9173151977936982 ) ) ;
#68012=EDGE_LOOP ( 'NONE', ( #60777, #37052, #6422, #59806 ) ) ;
#68014=CARTESIAN_POINT ( 'NONE',  ( -67.11354318489686932, -59.99999999999998579, 126.9389420720010122 ) ) ;
#68024=CARTESIAN_POINT ( 'NONE',  ( -31.41190527934607246, -60.32878540294149872, 37.39027770532391770 ) ) ;
#68026=CARTESIAN_POINT ( 'NONE',  ( 43.50297803938072860, -22.24728821975209669, 37.57093068451706586 ) ) ;
#68030=CARTESIAN_POINT ( 'NONE',  ( -87.31462566429209460, -38.58291539573046691, 199.6787966471005404 ) ) ;
#68034=CARTESIAN_POINT ( 'NONE',  ( 51.91349542570045372, -60.00000000000000711, 61.65172145578477370 ) ) ;
#68041=CARTESIAN_POINT ( 'NONE',  ( 107.2905653249216300, -60.00000000000000711, 196.7157100397594149 ) ) ;
#68048=CARTESIAN_POINT ( 'NONE',  ( -81.26072837970858131, -30.00000000000007816, -10.92579196702281408 ) ) ;
#68050=( LENGTH_UNIT ( ) NAMED_UNIT ( * ) SI_UNIT ( .MILLI., .METRE. ) );
#68064=CARTESIAN_POINT ( 'NONE',  ( 81.31836778682512090, -46.44211778139398206, 165.0976634020017855 ) ) ;
#68069=EDGE_LOOP ( 'NONE', ( #4786, #78202, #15915, #6629 ) ) ;
#68070=CARTESIAN_POINT ( 'NONE',  ( -80.00000000000000000, -60.00000000000000000, -21.09707704303352926 ) ) ;
#68082=CARTESIAN_POINT ( 'NONE',  ( 86.87595582856886267, -20.64717089365305824, 186.0002144904201202 ) ) ;
#68100=CARTESIAN_POINT ( 'NONE',  ( -88.14079865277417980, -60.00000000000000711, 201.4458585072254664 ) ) ;
#68105=CARTESIAN_POINT ( 'NONE',  ( -82.72409333703991763, -60.87321690922112083, 189.9861444112082438 ) ) ;
#68113=CARTESIAN_POINT ( 'NONE',  ( -82.55444755025907000, -37.83384472315690772, 6.159036853484627372 ) ) ;
#68123=CARTESIAN_POINT ( 'NONE',  ( 70.85242353449750397, -59.99999999999999289, 164.3672743468505359 ) ) ;
#68125=CARTESIAN_POINT ( 'NONE',  ( -86.84190767202800032, -14.21045842199442788, 3.676479754794546473 ) ) ;
#68126=CARTESIAN_POINT ( 'NONE',  ( -70.72062100957347752, -42.96379174276994917, 106.3028856496189292 ) ) ;
#68129=CARTESIAN_POINT ( 'NONE',  ( 59.93162491489189847, -30.00000000000002842, 91.51739161628221098 ) ) ;
#68131=CARTESIAN_POINT ( 'NONE',  ( 2.811255222305522938, -57.67120193607534162, -44.61186864502481342 ) ) ;
#68143=CARTESIAN_POINT ( 'NONE',  ( -38.72040230558515361, -59.99999999998055955, 54.32356401625951037 ) ) ;
#68156=CARTESIAN_POINT ( 'NONE',  ( 30.90820517067947648, -25.60289659773413362, 30.93734601537375184 ) ) ;
#68157=CARTESIAN_POINT ( 'NONE',  ( 3.088855081073062209E-15, -4.285714285714286476, 25.22241582816893413 ) ) ;
#68170=CARTESIAN_POINT ( 'NONE',  ( 86.04389369610818505, -60.00000000000000711, -23.60500139439278655 ) ) ;
#68176=CARTESIAN_POINT ( 'NONE',  ( -86.77091681052317540, -30.00000000002323119, 198.1326347201452336 ) ) ;
#68179=ORIENTED_EDGE ( 'NONE', *, *, #40286, .F. ) ;
#68184=CARTESIAN_POINT ( 'NONE',  ( 83.26455805995850312, -37.81343560710378426, -7.281846265020657682 ) ) ;
#68195=CARTESIAN_POINT ( 'NONE',  ( 78.52207915638700797, -22.14163466735898211, 122.4742839152309557 ) ) ;
#68202=CARTESIAN_POINT ( 'NONE',  ( -94.10527518209565301, -57.67545334945994995, 3.926124123639501029 ) ) ;
#68208=CARTESIAN_POINT ( 'NONE',  ( 105.1856413884972596, -52.71711923733968064, 177.3383578302138233 ) ) ;
#68216=CARTESIAN_POINT ( 'NONE',  ( -36.23827446154780318, -24.64368107998518553, 33.97573338550268573 ) ) ;
#68230=CARTESIAN_POINT ( 'NONE',  ( -89.02034635566286624, -29.99999999999999645, 188.7318756114235896 ) ) ;
#68234=CARTESIAN_POINT ( 'NONE',  ( 81.41097500085039940, -57.51647407579447702, 200.0635567779065411 ) ) ;
#68238=CARTESIAN_POINT ( 'NONE',  ( 69.34622291710002173, -38.18775354531572930, -31.40869740071274663 ) ) ;
#68241=CARTESIAN_POINT ( 'NONE',  ( -41.40363853713615327, -59.99999999999999289, 54.19992334669975520 ) ) ;
#68245=CARTESIAN_POINT ( 'NONE',  ( -86.60038770626319149, -39.13859030795514826, 188.3081612211328206 ) ) ;
#68248=CARTESIAN_POINT ( 'NONE',  ( -1.023259250014928456, -60.36594246766334493, 33.95064037087961850 ) ) ;
#68264=CARTESIAN_POINT ( 'NONE',  ( 108.2372837266210297, -59.99999999999997868, 115.4707114838127211 ) ) ;
#68265=CARTESIAN_POINT ( 'NONE',  ( -78.02770516898169717, -60.31600362760740808, 156.3356691730190846 ) ) ;
#68269=CARTESIAN_POINT ( 'NONE',  ( 9.923022100475872520, -57.67120321077532452, 41.61848498758426729 ) ) ;
#68273=ORIENTED_EDGE ( 'NONE', *, *, #17565, .F. ) ;
#68287=CARTESIAN_POINT ( 'NONE',  ( 90.78097007041577626, -59.99999999999997868, -17.40510296751067187 ) ) ;
#68289=CARTESIAN_POINT ( 'NONE',  ( -102.9006728679688365, -30.00000000000001421, 197.6531887663732618 ) ) ;
#68290=CARTESIAN_POINT ( 'NONE',  ( 21.99398094262454606, -22.07632118128579535, 28.30098176883504735 ) ) ;
#68294=CARTESIAN_POINT ( 'NONE',  ( -35.80230656125740296, -60.29385515264787898, 39.79296061328858514 ) ) ;
#68308=CARTESIAN_POINT ( 'NONE',  ( 95.54086597314230289, -30.00000000000007461, 191.3283643440866513 ) ) ;
#68312=CARTESIAN_POINT ( 'NONE',  ( 81.08533849400782856, -30.00000000000000000, 22.49689936057352568 ) ) ;
#68315=ORIENTED_EDGE ( 'NONE', *, *, #41419, .T. ) ;
#68330=CARTESIAN_POINT ( 'NONE',  ( 74.24161930812724108, -38.32798603758613609, 162.4564917793205439 ) ) ;
#68353=CARTESIAN_POINT ( 'NONE',  ( 86.41301712325638107, -46.49206446395204040, 190.1341371302563346 ) ) ;
#68365=CARTESIAN_POINT ( 'NONE',  ( -94.05936093215517246, -29.99999999999999645, 112.3224062120655304 ) ) ;
#68373=CYLINDRICAL_SURFACE ( 'NONE', #23973, 7.500000000001509015 ) ;
#68380=CARTESIAN_POINT ( 'NONE',  ( 50.21954304836901173, -27.54177712049025928, -27.91686790315894839 ) ) ;
#68381=CARTESIAN_POINT ( 'NONE',  ( -22.19868783087845898, -29.03752594377393592, 29.50702968582816865 ) ) ;
#68386=CARTESIAN_POINT ( 'NONE',  ( -19.33192182939703230, -53.40145674591138913, 33.25391692593370863 ) ) ;
#68394=CARTESIAN_POINT ( 'NONE',  ( 0.000000000000000000, -8.673617379884035472E-16, -22.23822744035697241 ) ) ;
#68400=CARTESIAN_POINT ( 'NONE',  ( 99.57218404754800645, -45.27071417153299393, 192.9608328712945706 ) ) ;
#68416=CARTESIAN_POINT ( 'NONE',  ( -53.08864208271962326, -59.99999999998543387, -39.69027889185369418 ) ) ;
#68420=CARTESIAN_POINT ( 'NONE',  ( -86.55941870227799484, -14.21045842199434439, 7.758091717749037386 ) ) ;
#68422=CARTESIAN_POINT ( 'NONE',  ( -51.52612014391598194, -32.58135107158835808, 50.96622865610893172 ) ) ;
#68426=CARTESIAN_POINT ( 'NONE',  ( -94.65235043456101494, -37.67961520111438745, 193.0070918200965480 ) ) ;
#68433=CARTESIAN_POINT ( 'NONE',  ( 86.98911389379702541, -30.00000000000125411, -18.62703500237973842 ) ) ;
#68438=CARTESIAN_POINT ( 'NONE',  ( 90.09437403127707000, -30.00000000000000355, 189.9480191965106997 ) ) ;
#68441=ORIENTED_EDGE ( 'NONE', *, *, #36235, .F. ) ;
#68443=CARTESIAN_POINT ( 'NONE',  ( 52.16619185189158259, -46.43791850696331380, 57.11334052445853615 ) ) ;
#68448=CARTESIAN_POINT ( 'NONE',  ( -85.63190312002936366, -38.36025793955835184, -22.26003858040750316 ) ) ;
#68450=CARTESIAN_POINT ( 'NONE',  ( 110.2505909221214893, -38.35601218213372476, 184.3274032030269325 ) ) ;
#68453=CARTESIAN_POINT ( 'NONE',  ( 83.72361235177345407, -37.85036601058070005, 34.46266949494848575 ) ) ;
#68458=DIRECTION ( 'NONE',  ( 0.000000000000000000, 1.000000000000000000, 0.000000000000000000 ) ) ;
#68475=FILL_AREA_STYLE ('',( #43651 ) ) ;
#68479=ORIENTED_EDGE ( 'NONE', *, *, #98646, .F. ) ;
#68480=CARTESIAN_POINT ( 'NONE',  ( 82.96302377660713034, -50.06046201639240678, 183.0585499319920757 ) ) ;
#68485=CARTESIAN_POINT ( 'NONE',  ( -93.38272968296267607, -60.15495384420781733, 76.37983926362966258 ) ) ;
#68490=COLOUR_RGB ( '', 0.72549020, 0.75294118, 0.79215686) ;
#68491=CARTESIAN_POINT ( 'NONE',  ( -27.77082267131420323, -28.74908582187916650, -38.27462747494718087 ) ) ;
#68493=CARTESIAN_POINT ( 'NONE',  ( 48.33459193932809228, -60.00000000000000711, 67.79618997339092346 ) ) ;
#68494=CARTESIAN_POINT ( 'NONE',  ( 31.89015935598033025, -33.67774583439580027, 41.76421769273258633 ) ) ;
#68496=CARTESIAN_POINT ( 'NONE',  ( 3.561767179485014090, -12.72028797016299961, 32.14637440348908370 ) ) ;
#68497=CIRCLE ( 'NONE', #23696, 2.000000000000001776 ) ;
#68498=CARTESIAN_POINT ( 'NONE',  ( -27.49170040733129738, -30.74798487600258312, 39.28685883056335371 ) ) ;
#68506=CARTESIAN_POINT ( 'NONE',  ( 2.377971153322278042E-07, -60.00000000000000000, 39.63907915656436387 ) ) ;
#68511=CARTESIAN_POINT ( 'NONE',  ( 47.11570157807129533, -34.58947700826256977, -28.29334103084299556 ) ) ;
#68516=COLOUR_RGB ( '', 0.40784314, 0.44705882, 0.49803922) ;
#68524=CARTESIAN_POINT ( 'NONE',  ( -93.39231211507048158, -60.00000000000000711, 36.05560009178016401 ) ) ;
#68534=CARTESIAN_POINT ( 'NONE',  ( -84.64411001500138809, -28.97345275897948724, 168.9245721654432657 ) ) ;
#68545=CARTESIAN_POINT ( 'NONE',  ( -85.55066431120862092, -57.67066120584623690, -26.59325976709777706 ) ) ;
#68551=CARTESIAN_POINT ( 'NONE',  ( 91.50784380495012726, -29.99999999999993960, 42.72614900145088512 ) ) ;
#68553=CARTESIAN_POINT ( 'NONE',  ( -84.52733067048065152, -59.99999999999991473, 202.7036346196431111 ) ) ;
#68554=CARTESIAN_POINT ( 'NONE',  ( -60.96421378324996709, -18.64597550156105754, 64.94627126466191669 ) ) ;
#68558=CARTESIAN_POINT ( 'NONE',  ( -105.2860375889557076, -52.71044453558685206, 172.7917639000798715 ) ) ;
#68559=FILL_AREA_STYLE_COLOUR ( '', #14443 ) ;
#68566=CARTESIAN_POINT ( 'NONE',  ( -46.69195340547801010, -59.99999999999998579, 64.09799256419935887 ) ) ;
#68571=CARTESIAN_POINT ( 'NONE',  ( 7.540142361526415371, 0.000000000000000000, -15.29459302239930274 ) ) ;
#68577=CARTESIAN_POINT ( 'NONE',  ( -31.94552423878153746, -39.49308952852756960, 33.87865584480293535 ) ) ;
#68581=CARTESIAN_POINT ( 'NONE',  ( 43.99760445235895645, -42.98121213538102836, 43.39625074881774935 ) ) ;
#68585=CARTESIAN_POINT ( 'NONE',  ( -97.92846326097485132, -38.48021779882554938, 200.9938350945185448 ) ) ;
#68589=CARTESIAN_POINT ( 'NONE',  ( 32.75304820937488159, -59.99999999999998579, 37.97536356120721024 ) ) ;
#68596=CARTESIAN_POINT ( 'NONE',  ( 112.1219226975825052, -60.00000000000001421, 177.4905933672216349 ) ) ;
#68619=CARTESIAN_POINT ( 'NONE',  ( 82.18267182277710958, -42.97061699490445363, 167.7090913738393567 ) ) ;
#68637=CARTESIAN_POINT ( 'NONE',  ( 87.01843083760033437, -46.44379687455451489, 190.9307336648631406 ) ) ;
#68647=CARTESIAN_POINT ( 'NONE',  ( 1.494050070974696619E-08, -60.00000000000001421, -44.99999999996100541 ) ) ;
#68661=CARTESIAN_POINT ( 'NONE',  ( -94.42299775263619210, -60.00000000000000000, 202.5617398974961247 ) ) ;
#68667=CARTESIAN_POINT ( 'NONE',  ( -85.89786254057293036, -25.01153798521900384, 177.6387691999012475 ) ) ;
#68671=CARTESIAN_POINT ( 'NONE',  ( -83.76838281802336894, -45.26691656702287503, 6.940423426407160257 ) ) ;
#68678=CARTESIAN_POINT ( 'NONE',  ( 55.31236231582965956, -60.00000000000003553, 93.46951393418744658 ) ) ;
#68680=CARTESIAN_POINT ( 'NONE',  ( -89.66254536497091010, -30.00000000000007461, 1.293233577394788725 ) ) ;
#68681=CARTESIAN_POINT ( 'NONE',  ( -71.58537349543678374, -60.33171839608677800, 120.7708638787018742 ) ) ;
#68683=CARTESIAN_POINT ( 'NONE',  ( 81.96363334812492951, -30.00000000000004263, 194.6668941393791386 ) ) ;
#68686=CARTESIAN_POINT ( 'NONE',  ( 79.64422146358542420, -57.67118961797744703, -30.40228359957061599 ) ) ;
#68698=CARTESIAN_POINT ( 'NONE',  ( -42.76485599677753413, -59.99999999998050271, 61.36626925380817710 ) ) ;
#68711=CARTESIAN_POINT ( 'NONE',  ( 33.47252721207472348, -56.83589283137767012, 37.78155003957702007 ) ) ;
#68712=CARTESIAN_POINT ( 'NONE',  ( -3.301606509414339641, -4.285714285714286476, -25.22241582816893413 ) ) ;
#68713=ORIENTED_EDGE ( 'NONE', *, *, #23177, .T. ) ;
#68725=CARTESIAN_POINT ( 'NONE',  ( 92.46921543868899107, -60.00000000000001421, -0.8085169714401274632 ) ) ;
#68731=CARTESIAN_POINT ( 'NONE',  ( -105.5920425955938384, -29.99999999999728928, 194.5055816160023028 ) ) ;
#68737=CARTESIAN_POINT ( 'NONE',  ( 86.47354485262529522, -60.23000014668301105, -12.63761204200946153 ) ) ;
#68742=ORIENTED_EDGE ( 'NONE', *, *, #105601, .F. ) ;
#68746=SURFACE_STYLE_FILL_AREA ( #101090 ) ;
#68749=B_SPLINE_CURVE_WITH_KNOTS ( 'NONE', 3,
 ( #2670, #51213, #50672, #68496, #91704, #9695, #42604, #76033, #51755, #67953, #59879, #50167, #59340, #83585, #74958, #19452, #83069, #75501, #18361, #101386, #52287, #42073, #509, #33476, #1597, #34559, #1050, #27539, #34023, #11282, #66897, #26470, #99233, #99782, #84670, #67433, #84138, #10235, #43150, #74432, #2129, #43671, #58261, #66349, #25401, #100835, #76559, #60418, #91186, #17293, #44215, #45282, #5351, #20528, #4280, #79223, #53365, #45804, #36692, #103503, #77103, #93827, #104023, #22078, #21044, #37750, #62010, #94365, #78681, #52825, #38272, #4814, #12357, #70612, #60937, #28590, #30165, #78162, #19980, #3221, #28064, #86286, #29655, #21553, #62527, #95412, #85752, #29140, #61473, #44755, #95954, #11824, #37209, #94903, #71131, #54933, #63051, #54389, #86811, #70078, #102979, #77643, #87861, #3760, #36162, #69555, #53878, #69032, #102445, #87335, #12884, #13411, #46335, #101906, #98586, #97509, #81328 ),
 .UNSPECIFIED., .F., .F.,
 ( 4, 2, 2, 2, 1, 1, 1, 1, 2, 2, 2, 1, 1, 1, 1, 1, 2, 2, 2, 2, 1, 1, 1, 1, 1, 2, 2, 2, 2, 1, 1, 1, 1, 2, 2, 2, 2, 1, 1, 1, 1, 2, 2, 2, 2, 1, 1, 1, 1, 1, 2, 2, 2, 2, 1, 1, 1, 1, 1, 2, 2, 2, 2, 1, 1, 1, 1, 1, 1, 2, 2, 2, 1, 1, 1, 1, 1, 2, 2, 4 ),
 ( 0.5037612912634689133, 0.5192687509114792821, 0.5347762105594896509, 0.5352608186734899576, 0.5357454267874903753, 0.5367146430154909886, 0.5386530754714922153, 0.5425299403834946688, 0.5502836702074995756, 0.5657911298555096113, 0.5660334339125097092, 0.5662757379695099180, 0.5667603460835102247, 0.5677295623115108381, 0.5696679947675119537, 0.5735448596795142961, 0.5812985895035190920, 0.5968060491515284616, 0.6278209684475473118, 0.6280632725045475206, 0.6283055765615477295, 0.6287901846755481472, 0.6297594009035489826, 0.6316978333595504314, 0.6355746982715534399, 0.6433284280955595680, 0.6588358877435718242, 0.6898508070395963365, 0.6903354151535967542, 0.6908200232675971719, 0.6917892394955980073, 0.6937276719515996781, 0.6976045368636032418, 0.7053582666876103691, 0.7208657263356246236, 0.7518806456316531328, 0.7523652537456535505, 0.7528498618596540792, 0.7538190780876552477, 0.7557575105436572516, 0.7596343754556612593, 0.7673881052796691637, 0.7828955649276855278, 0.8139104842237181447, 0.8141527882807184646, 0.8143950923377187845, 0.8148797004517192022, 0.8158489166797204817, 0.8177873491357228186, 0.8216642140477272704, 0.8294179438717363961, 0.8449254035197544255, 0.8759403228157905952, 0.8761826268727910261, 0.8764249309297913459, 0.8769095390437922077, 0.8778787552717941534, 0.8798171877277980446, 0.8836940526398056051, 0.8914477824638205039, 0.9069552421118506347, 0.9379701614079103411, 0.9380913134364107231, 0.9382124654649108830, 0.9384547695219115360, 0.9389393776359126198, 0.9399085938639146764, 0.9418470263199185677, 0.9457238912319263502, 0.9534776210559416931, 0.9689850807039722680, 0.9691062327324724279, 0.9692273847609724768, 0.9694696888179727967, 0.9699542969319729924, 0.9709235131599739388, 0.9728619456159757206, 0.9767388105279791732, 0.9844925403519861895, 1.000000000000000000 ),
 .UNSPECIFIED. ) ;
#68752=CARTESIAN_POINT ( 'NONE',  ( 78.83263402278350895, -18.67162436856858676, 121.1150609631452539 ) ) ;
#68760=CARTESIAN_POINT ( 'NONE',  ( -76.77372030740811226, -57.52889592737719227, 194.6762175334667972 ) ) ;
#68763=CARTESIAN_POINT ( 'NONE',  ( 106.5029100764443513, -60.15152792750651400, 170.5906469400855201 ) ) ;
#68768=CARTESIAN_POINT ( 'NONE',  ( -49.89404489861477288, -29.66878297426404387, 46.44302417657395665 ) ) ;
#68779=CARTESIAN_POINT ( 'NONE',  ( -85.97022708240267264, -30.00000000000000711, 178.4417459103200088 ) ) ;
#68782=CARTESIAN_POINT ( 'NONE',  ( 86.24777464318049169, -57.57757783600133195, 202.8079723600879163 ) ) ;
#68785=CARTESIAN_POINT ( 'NONE',  ( 36.00270731313416661, -31.67306530563417155, -37.80042584635362601 ) ) ;
#68788=CARTESIAN_POINT ( 'NONE',  ( -59.99645216862890607, -59.99999999999999289, 100.5209178649575961 ) ) ;
#68791=CARTESIAN_POINT ( 'NONE',  ( -85.42895892553163151, -50.19694353309194668, 189.9724354759997311 ) ) ;
#68794=CARTESIAN_POINT ( 'NONE',  ( -2.007454225884796717, -35.99435325406362551, 29.88636456374760186 ) ) ;
#68801=EDGE_LOOP ( 'NONE', ( #10786, #68713, #85542, #56152 ) ) ;
#68810=CARTESIAN_POINT ( 'NONE',  ( 103.2975989548790494, -14.21045842199431064, 133.3107955441116985 ) ) ;
#68811=CARTESIAN_POINT ( 'NONE',  ( -79.16567614127620800, -49.90816960768657395, 152.0318120169229985 ) ) ;
#68814=CARTESIAN_POINT ( 'NONE',  ( 52.71793837654925596, -57.67618728593465960, 84.69386162797044904 ) ) ;
#68833=CARTESIAN_POINT ( 'NONE',  ( 76.22636411394974232, -60.00000000000002132, -29.93832294592251131 ) ) ;
#68834=CARTESIAN_POINT ( 'NONE',  ( -69.92584042677506773, -30.00000000000002842, 127.5397447585766599 ) ) ;
#68835=CARTESIAN_POINT ( 'NONE',  ( 19.02302005367418758, -39.47349632058700308, 30.89158363994719281 ) ) ;
#68838=CARTESIAN_POINT ( 'NONE',  ( -35.05923457201825499, -25.64776234952272560, 32.62731220559753353 ) ) ;
#68841=DIRECTION ( 'NONE',  ( 0.000000000000000000, 0.000000000000000000, 1.000000000000000000 ) ) ;
#68851=CARTESIAN_POINT ( 'NONE',  ( 92.90552581771817131, -29.99999999999993960, 191.0990075023869394 ) ) ;
#68856=CARTESIAN_POINT ( 'NONE',  ( 80.78006440248529429, -30.00000000000000000, 9.594317255054795268 ) ) ;
#68875=CARTESIAN_POINT ( 'NONE',  ( 70.17483447761377136, -38.33017349177596600, 135.4944106953618075 ) ) ;
#68897=CARTESIAN_POINT ( 'NONE',  ( 86.44384447875494004, -17.06518992601345275, 183.2574884712147139 ) ) ;
#68901=CARTESIAN_POINT ( 'NONE',  ( 2.807699812566442521, -57.67114347947145347, -44.61185890016353284 ) ) ;
#68902=CARTESIAN_POINT ( 'NONE',  ( 8.125792988224667113, -15.92269399258319851, -34.96259303599431689 ) ) ;
#68906=CARTESIAN_POINT ( 'NONE',  ( -82.07453358999418924, -30.00000000000000000, 34.72976722373532255 ) ) ;
#68908=CARTESIAN_POINT ( 'NONE',  ( 4.154708322984369194E-08, -57.67120202538961138, 41.61186700422869933 ) ) ;
#68913=CARTESIAN_POINT ( 'NONE',  ( -15.00532868743633230, -22.79648478323108662, 27.82648325657085664 ) ) ;
#68917=CARTESIAN_POINT ( 'NONE',  ( 42.59497354870452313, -25.61862108974249708, -29.74171580790378044 ) ) ;
#68919=CARTESIAN_POINT ( 'NONE',  ( -21.99509306790069729, -22.07688988618103920, 28.30121125513787561 ) ) ;
#68922=CARTESIAN_POINT ( 'NONE',  ( -16.01663249378604803, -60.36515267375860816, 34.15509718080474499 ) ) ;
#68937=CARTESIAN_POINT ( 'NONE',  ( 102.5259657431785456, -45.28272343595455141, 187.4750528580337345 ) ) ;
#68954=CARTESIAN_POINT ( 'NONE',  ( -69.57556824456027300, -60.00000000001938361, -35.22474675930589427 ) ) ;
#68959=CARTESIAN_POINT ( 'NONE',  ( -86.49433777984398830, -14.21045842199439946, 11.85125679505764928 ) ) ;
#68962=CARTESIAN_POINT ( 'NONE',  ( -48.44050217894999832, -32.60199816967398334, 46.13225639932870337 ) ) ;
#68972=CARTESIAN_POINT ( 'NONE',  ( 89.93155271925053285, -30.00000000000346745, -2.506699656231715867 ) ) ;
#68977=CARTESIAN_POINT ( 'NONE',  ( 87.06181006619939922, -30.00000000000000000, 183.9460334166788016 ) ) ;
#68983=CARTESIAN_POINT ( 'NONE',  ( 53.79279109633859690, -29.09796998240493693, 53.78371313197352777 ) ) ;
#68987=CARTESIAN_POINT ( 'NONE',  ( -91.45622412403105272, -38.38807348690984611, -7.605349006447526428 ) ) ;
#68991=CARTESIAN_POINT ( 'NONE',  ( 108.2517700566951646, -38.35773586447793804, 192.2691011081020349 ) ) ;
#68993=CARTESIAN_POINT ( 'NONE',  ( 82.59045073928865577, -37.86127578031408802, 5.516604945292076678 ) ) ;
#69012=( NAMED_UNIT ( * ) PLANE_ANGLE_UNIT ( ) SI_UNIT ( $, .RADIAN. ) );
#69017=CARTESIAN_POINT ( 'NONE',  ( 84.33010434533966304, -46.56536763441548743, 185.7282459068632932 ) ) ;
#69021=CARTESIAN_POINT ( 'NONE',  ( -99.21263190360249951, -60.15509383132980048, 110.4768515106927396 ) ) ;
#69026=CARTESIAN_POINT ( 'NONE',  ( -23.19062926906127231, -27.02661850035177693, -38.42076749808039438 ) ) ;
#69030=CARTESIAN_POINT ( 'NONE',  ( 39.17414499517634852, -60.00000000000001421, 50.97255646505768567 ) ) ;
#69031=CARTESIAN_POINT ( 'NONE',  ( 27.19894980877528567, -30.54737125749132787, 39.15565882474543713 ) ) ;
#69032=CARTESIAN_POINT ( 'NONE',  ( 51.39917057842919945, -29.90070880694079136, 48.99695014035973628 ) ) ;
#69047=CARTESIAN_POINT ( 'NONE',  ( -0.001384332131796172554, -60.22811001523060526, -36.92766828953757141 ) ) ;
#69058=CARTESIAN_POINT ( 'NONE',  ( -92.21137906100017290, -60.00000000000002132, 2.742975087226245723 ) ) ;
#69065=CARTESIAN_POINT ( 'NONE',  ( -85.11760744219132846, -22.05730720455698801, 161.9244985632302871 ) ) ;
#69075=CARTESIAN_POINT ( 'NONE',  ( -93.33808876947477984, -57.65441397348698160, -16.37300446327261128 ) ) ;
#69082=CARTESIAN_POINT ( 'NONE',  ( 89.06755727843562909, -14.21045842199420939, 44.45805076957166335 ) ) ;
#69084=CARTESIAN_POINT ( 'NONE',  ( -83.30586888084981467, -14.21045842199414011, 194.5088339777059332 ) ) ;
#69085=CARTESIAN_POINT ( 'NONE',  ( -53.47679039029645054, -60.31905840357084259, 65.32239846319221499 ) ) ;
#69090=CARTESIAN_POINT ( 'NONE',  ( -101.6861282671374624, -45.26497370855512514, 189.9345094133276746 ) ) ;
#69094=CARTESIAN_POINT ( 'NONE',  ( -2.822539341787094980, -59.99999999999998579, 39.63907887523128437 ) ) ;
#69107=CARTESIAN_POINT ( 'NONE',  ( -30.60580106567836722, -56.85883406477462643, 36.44144671480716369 ) ) ;
#69110=CARTESIAN_POINT ( 'NONE',  ( 47.00049515621073937, -53.35381624944555057, 50.28993904774486623 ) ) ;
#69115=CARTESIAN_POINT ( 'NONE',  ( -88.28417624129785679, -38.54991672500991484, 200.0595944994497870 ) ) ;
#69126=CARTESIAN_POINT ( 'NONE',  ( 106.0955882055216080, -60.00000000000000711, 198.2014181196565801 ) ) ;
#69132=CARTESIAN_POINT ( 'NONE',  ( -80.03095223124314828, -29.99999999999999289, -13.76337047395467117 ) ) ;
#69134=CARTESIAN_POINT ( 'NONE',  ( -88.40077111556168177, -38.54200826082194453, 200.1329272985095429 ) ) ;
#69149=CARTESIAN_POINT ( 'NONE',  ( 85.95997101110781102, -18.45075829103920384, 165.1113332624142345 ) ) ;
#69189=CARTESIAN_POINT ( 'NONE',  ( -111.1411582638900200, -60.00000000000000000, 186.5650987214990266 ) ) ;
#69194=CARTESIAN_POINT ( 'NONE',  ( -82.39105173393342341, -53.57895264400556812, 183.5905530224347331 ) ) ;
#69200=CARTESIAN_POINT ( 'NONE',  ( -84.05233785748785635, -45.26991514358498847, 1.856990868721440480 ) ) ;
#69208=CARTESIAN_POINT ( 'NONE',  ( 55.43986775084101737, -14.21045842199435860, 70.80752230913886081 ) ) ;
#69211=CARTESIAN_POINT ( 'NONE',  ( -76.02716361407355805, -14.21045842199433018, -24.18402117868763312 ) ) ;
#69213=CARTESIAN_POINT ( 'NONE',  ( -65.92007518974624247, -60.34191306316107983, 100.3556483961110501 ) ) ;
#69215=CARTESIAN_POINT ( 'NONE',  ( 78.81966326594580607, -14.21045842199438347, 187.8133603351751333 ) ) ;
#69217=CARTESIAN_POINT ( 'NONE',  ( 5.615082869220882955, -57.67118258056662938, -44.55225991330173230 ) ) ;
#69227=CARTESIAN_POINT ( 'NONE',  ( -84.33588122351162042, -60.00000000000000000, -25.03827388917266106 ) ) ;
#69239=CARTESIAN_POINT ( 'NONE',  ( 31.20659673062720785, -25.60560110436567172, 31.04007313146203728 ) ) ;
#69240=CARTESIAN_POINT ( 'NONE',  ( -20.16952962162108065, -4.285714285713656757, 15.50035291838862683 ) ) ;
#69252=CARTESIAN_POINT ( 'NONE',  ( 92.26840822479495330, -60.00000000000002842, 1.944625616427832826 ) ) ;
#69263=CARTESIAN_POINT ( 'NONE',  ( -84.45944469708555857, -29.99999999999518252, 196.7683117583226533 ) ) ;
#69268=CARTESIAN_POINT ( 'NONE',  ( 85.28627536060220393, -60.19927222349419793, -15.58279874029676471 ) ) ;
#69277=ORIENTED_EDGE ( 'NONE', *, *, #14417, .F. ) ;
#69281=CARTESIAN_POINT ( 'NONE',  ( 81.43616672422064084, -29.09222109329241945, 143.4168869114997165 ) ) ;
#69285=CARTESIAN_POINT ( 'NONE',  ( -109.5878728966581832, -57.66746364524283308, 196.8330158634452118 ) ) ;
#69295=CARTESIAN_POINT ( 'NONE',  ( -45.76875562652180207, -28.55789701437204542, 40.90047540029672035 ) ) ;
#69307=CARTESIAN_POINT ( 'NONE',  ( 74.41155834966481564, -38.35600210799680809, -29.41977220444294261 ) ) ;
#69308=CARTESIAN_POINT ( 'NONE',  ( -86.31537193578998313, -29.99999999999998934, 180.5207776403601372 ) ) ;
#69311=CARTESIAN_POINT ( 'NONE',  ( 73.89615930086935691, -57.61735591279438751, 186.5259515469176108 ) ) ;
#69313=CARTESIAN_POINT ( 'NONE',  ( 28.39691108350841375, -28.98146926308949389, -38.24856420472010399 ) ) ;
#69316=CARTESIAN_POINT ( 'NONE',  ( -56.17991941645016141, -60.00000000000000000, 88.71135144568317799 ) ) ;
#69318=CARTESIAN_POINT ( 'NONE',  ( -86.75643894772611020, -28.06581177804503824, 186.0048141377419881 ) ) ;
#69319=B_SPLINE_CURVE_WITH_KNOTS ( 'NONE', 3,
 ( #68506, #71534, #36702, #104435, #27549, #51767, #60429, #52837, #93307, #19461, #65578, #40762, #106556, #32708, #89332, #14352, #49374, #98462, #81207, #16493, #32162, #7323, #39723, #96890, #47779, #57463, #23025, #90384, #56933, #82282, #55855, #8395, #41297, #65042, #105505, #23554, #73650, #22506, #24614, #40234, #74184, #30584, #63477, #96376, #55345, #73107, #88274, #80684, #106016, #48313, #47258, #80158, #6261, #56396, #39197, #72075, #104984, #97940, #24090, #31128, #89853, #81730, #88796, #64013, #15425, #14886, #6804, #72600, #31645, #97394, #64526, #15962, #48840, #7856, #92502, #82822, #58562, #74714, #84955, #10520, #59630, #27294, #18654, #98981, #75246, #18109, #26230, #51513, #43436, #59091, #93045, #41827, #25701, #19210, #84428, #100065, #100595, #83349, #25146, #76316, #1346, #42359, #49914, #8921, #91461, #101134, #26755, #2428, #9440, #66104, #792, #34841, #91975, #35372, #68241, #60177, #52042, #11043, #50968, #90925, #43961, #33765, #1888, #263, #83879, #9993, #34309, #66639, #17575, #33231, #99522, #58002, #17039, #50437, #67186, #42899, #75793, #67712, #45046, #69835, #87091, #21314, #21844, #62813, #4569, #76853, #13168, #2958, #78979, #12637, #101669, #94106, #45571, #94663, #95703, #70894, #46094, #102735, #38033, #87619, #103784, #70369, #3509, #69316, #20273, #53123, #28894, #68788, #29926, #61768, #36450, #85496, #20809, #13703, #53643, #103264, #37506, #102195, #62292, #29413, #35916, #12115, #95182, #86040, #77928, #93584, #27829, #54151, #54685, #78446, #44504, #4037, #86574, #36969, #5102, #60698, #19735, #52572, #77395, #11576, #28342, #61220, #14228, #96251, #14759, #88670, #89204, #104856, #6677, #47134, #48190, #7731, #23427, #56267, #55737, #6142, #63881, #73522, #39071, #106423, #72990, #15303, #65456, #5621, #96770, #63351, #22377, #71952, #22899, #97808, #98349, #32582, #81093, #46614, #89739, #79511, #48716, #7206, #71409, #47661, #40114, #23972, #24503, #80557, #39605, #105896, #32043, #57336, #81604, #64923, #80029, #30999, #72478, #105384, #31523, #38544, #40638, #64405, #97278, #55222, #56814, #15834, #90259, #104308, #30458, #88148, #41179, #17451, #16912, #58425, #42764, #33632, #91336, #33113, #8266, #9852, #35234, #91850, #90798, #99385, #26108, #2285, #50317, #16361, #74058, #17976, #43302, #146, #58965, #65977, #101000, #49248, #25017, #98856, #76186, #34714, #57871, #83221, #34178, #42226, #67588, #59498, #82153, #49790, #82695, #9316, #50837, #8800, #27158, #41708, #83742, #74590, #18517, #666, #75113, #66510, #25567, #1209, #10385, #75655, #68100, #92368, #67056, #84291, #60046, #99933, #1757, #100466, #26626, #51376, #44914, #37372, #52438, #2827, #11983, #68661, #103137, #29285, #85355, #52990, #94529, #20680, #19607, #78314, #45438, #29807, #11441, #4972, #35783, #60570, #93460, #101540, #4430, #37901, #93980, #70762, #70236, #86967, #44368, #78843, #20136, #84825, #61637, #13034, #10905, #28755, #43824, #103657, #92904, #27693, #76716, #45962, #62168, #77265, #61091, #3910, #77798, #95058, #21192, #36842, #19071, #51911, #85910, #53519, #3377, #36319, #69189, #86447, #102061, #54023, #28220, #69709, #102602, #12508, #14095, #56680, #89070, #105769, #38934, #21710, #63212, #23291, #89602, #15696, #30320, #5498, #30867, #104712, #105252, #47002, #22769, #96104, #64276, #23835, #39470, #72349, #71805, #22238, #79900, #48585, #55087, #54547, #38420, #31398, #81473, #87490, #6010, #79376, #71283, #88016, #63746, #7072, #7591, #40509, #97144, #62682, #31909, #95574, #64788, #56128, #13571, #73386, #39988, #72860, #46487, #97667, #96633, #47533, #55605, #104178, #48055, #88542, #14622, #80426, #106283, #6537, #15168, #80957, #99805, #26499, #92232, #42631, #1624, #34586, #91210, #16225, #51237, #67457, #83094, #18386, #34048, #73927, #65847, #9, #9717, #84166, #100335, #74982, #24362, #82012, #1073, #59370, #10261, #66925, #537, #25426, #75530, #57206, #43175, #42097, #76056, #91730, #74457, #32449, #65321, #8668, #98209, #33498, #90125, #83613, #49112, #8133, #41044, #58284, #32977, #98726, #24880, #50192, #25975, #57734, #58836, #17317, #90658, #16765, #49656, #9187, #82564, #41571, #66374, #99254, #17848, #50699, #36719, #35648, #94393, #61501, #45833, #101416, #21067, #51781, #76586, #2700, #10778, #20559, #53905, #3249, #86836, #53395, #103007, #68524, #94931, #36189, #11853, #93320, #12907, #86316, #84694, #60447, #27567, #2157, #12381, #45309, #78190, #4304, #19477, #52314, #37241, #44783, #93851, #20010, #70101, #35111, #43697, #85222, #67978, #29165, #101930, #102473, #11311, #44243, #100865, #62040, #28090, #28620, #77131, #27027, #59908, #69058, #52853, #60965, #85780, #77673, #92778, #18939, #3783, #69584, #37774, #79249, #6407, #71674, #47925, #6945, #88940, #80832, #39864, #30737, #62551, #97537, #72736, #22645, #64662, #55480, #88417, #87887, #38294, #95977, #105640, #71155, #31780, #105126, #23698, #104050, #56550, #89477, #80296, #46875, #104581, #15035, #70636, #15572, #14490, #39345, #78705, #4840, #103530, #29679, #47401, #95437, #22103, #72224, #96512, #21580, #54416, #87359, #63623, #13439, #46360, #5375, #31267, #64151, #30188, #54958, #13967, #97022, #63077, #79777, #23164, #5879, #38806, #56004, #59241, #410, #41972, #82972, #81885, #33922, #941, #92117, #40915, #67333, #98085, #48986, #57084, #66794, #100213, #49530, #26379, #99681, #42505, #16104, #34463, #82439, #48463, #40380, #17190, #75402, #73259, #91082, #106159, #81352, #7463, #25852, #91609, #58709, #73806, #106701, #17715, #50064, #33377, #66251, #50576, #32320, #65191, #83494, #24235, #89997, #99134, #9592, #8005, #1499, #65729, #41444, #32852, #98608, #24758, #57606, #90530, #25297, #16641, #8539, #74336, #58155, #9066, #74856, #59777, #51655, #92653, #102343, #37117, #20425, #60838, #44658, #45192, #43574, #78065, #102880, #19882, #93194 ),
 .UNSPECIFIED., .F., .F.,
 ( 4, 1, 1, 1, 1, 1, 2, 2, 1, 1, 1, 1, 1, 2, 2, 1, 1, 1, 1, 1, 1, 1, 2, 2, 1, 1, 1, 1, 1, 1, 1, 2, 2, 1, 1, 1, 1, 1, 1, 2, 2, 1, 1, 1, 1, 1, 1, 2, 2, 1, 1, 1, 1, 1, 2, 2, 1, 1, 1, 1, 2, 2, 1, 1, 1, 1, 2, 2, 1, 1, 1, 1, 1, 2, 2, 1, 1, 1, 1, 1, 1, 2, 2, 1, 1, 1, 1, 1, 1, 2, 2, 1, 1, 1, 1, 1, 1, 2, 2, 1, 1, 1, 1, 1, 1, 1, 2, 2, 1, 1, 1, 1, 1, 1, 1, 2, 2, 1, 1, 1, 1, 1, 1, 1, 2, 2, 1, 1, 1, 2, 2, 1, 1, 1, 1, 1, 1, 2, 2, 1, 1, 1, 1, 1, 1, 2, 2, 1, 1, 1, 1, 2, 2, 1, 1, 1, 1, 1, 1, 1, 2, 2, 1, 1, 1, 1, 1, 1, 1, 2, 2, 1, 1, 1, 1, 1, 1, 1, 2, 2, 1, 1, 1, 1, 2, 2, 1, 1, 1, 1, 1, 1, 1, 1, 2, 2, 1, 1, 1, 1, 1, 1, 1, 2, 2, 1, 1, 1, 1, 1, 1, 1, 2, 2, 1, 1, 1, 1, 1, 1, 2, 2, 1, 1, 1, 1, 2, 2, 1, 1, 1, 1, 2, 2, 1, 1, 1, 1, 2, 2, 1, 1, 1, 1, 2, 2, 1, 1, 1, 1, 1, 2, 2, 1, 1, 1, 2, 2, 1, 1, 2, 2, 1, 1, 1, 2, 2, 1, 1, 1, 1, 1, 2, 2, 1, 1, 1, 1, 2, 2, 1, 1, 1, 1, 1, 2, 2, 1, 1, 1, 1, 1, 1, 1, 2, 2, 1, 1, 1, 1, 1, 1, 1, 1, 2, 2, 1, 1, 1, 1, 1, 1, 1, 2, 2, 1, 1, 1, 1, 1, 1, 1, 1, 2, 2, 1, 1, 1, 1, 1, 1, 1, 1, 2, 2, 1, 1, 1, 1, 1, 1, 1, 2, 2, 1, 1, 1, 1, 1, 1, 1, 2, 2, 1, 1, 1, 1, 1, 1, 1, 1, 1, 2, 2, 1, 1, 1, 1, 1, 1, 1, 1, 1, 1, 2, 2, 1, 1, 1, 1, 1, 1, 2, 2, 1, 1, 1, 1, 1, 1, 1, 1, 1, 2, 2, 1, 1, 1, 1, 1, 1, 1, 1, 1, 2, 2, 1, 1, 1, 1, 1, 1, 1, 1, 2, 2, 1, 1, 1, 1, 1, 1, 2, 2, 1, 1, 1, 1, 1, 1, 1, 2, 2, 1, 1, 1, 1, 1, 1, 1, 1, 2, 2, 1, 1, 1, 1, 1, 1, 2, 2, 1, 1, 1, 1, 1, 1, 2, 2, 1, 1, 1, 1, 1, 1, 1, 1, 1, 2, 2, 1, 1, 1, 1, 1, 1, 1, 2, 2, 1, 1, 1, 1, 1, 1, 2, 2, 1, 1, 1, 1, 1, 2, 2, 1, 1, 1, 1, 1, 2, 2, 1, 1, 1, 1, 1, 1, 2, 2, 1, 1, 1, 1, 1, 2, 2, 1, 1, 1, 2, 2, 1, 1, 1, 1, 1, 1, 2, 2, 1, 1, 1, 1, 1, 1, 1, 1, 2, 2, 1, 1, 1, 1, 1, 1, 1, 1, 1, 2, 2, 1, 1, 1, 1, 1, 1, 1, 1, 2, 2, 1, 1, 1, 1, 1, 1, 1, 2, 2, 1, 1, 2, 2, 1, 1, 1, 1, 1, 1, 2, 2, 4 ),
 ( 0.000000000000000000, 0.001953124999994617153, 0.002929687499991924862, 0.003417968749990578717, 0.003662109374989905210, 0.003784179687489569541, 0.003845214843739401707, 0.003906249999989233872, 0.005859374999983863602, 0.006835937499981179118, 0.007324218749979836442, 0.007568359374979166838, 0.007690429687478832037, 0.007751464843728667238, 0.007812499999978501572, 0.01171874999996791455, 0.01367187499996262018, 0.01464843749995997299, 0.01513671874995865113, 0.01538085937495798847, 0.01550292968745766234, 0.01556396484370749927, 0.01559448242183242295, 0.01562499999995734662, 0.01953124999994798605, 0.02148437499994329883, 0.02246093749994096389, 0.02294921874993979469, 0.02319335937493920835, 0.02331542968743891692, 0.02337646484368876773, 0.02340698242181369487, 0.02343749999993862201, 0.02734374999992915389, 0.02929687499992441463, 0.03027343749992204847, 0.03076171874992086192, 0.03100585937492025823, 0.03112792968741995639, 0.03118896484366980026, 0.03124999999991964761, 0.03515624999990984989, 0.03710937499990496491, 0.03808593749990252242, 0.03857421874990130117, 0.03881835937490069055, 0.03894042968740039218, 0.03900146484365024646, 0.03906249999990010074, 0.04296874999989073324, 0.04492187499988607030, 0.04589843749988371802, 0.04638671874988255922, 0.04663085937488198329, 0.04675292968738167798, 0.04687499999988137961, 0.05078124999987168597, 0.05273437499986684263, 0.05371093749986441401, 0.05419921874986322052, 0.05444335937486263766, 0.05468749999986205479, 0.05859374999985263177, 0.06054687499984789251, 0.06152343749984554716, 0.06201171874984434673, 0.06225585937484374999, 0.06249999999984315324, 0.06640624999983363308, 0.06835937499982885912, 0.06933593749982645826, 0.06982421874982525090, 0.07006835937482468191, 0.07019042968732440435, 0.07031249999982411292, 0.07421874999981531440, 0.07617187499981092902, 0.07714843749980873633, 0.07763671874980763998, 0.07788085937480709875, 0.07800292968730684895, 0.07806396484355672405, 0.07812499999980659915, 0.08203124999979773124, 0.08398437499979329035, 0.08496093749979106990, 0.08544921874978994580, 0.08569335937478939069, 0.08581542968728912701, 0.08587646484353898824, 0.08593749999978883558, 0.08984374999977955134, 0.09179687499977487453, 0.09277343749977254306, 0.09326171874977139120, 0.09350585937477079446, 0.09362792968727050302, 0.09368896484352036425, 0.09374999999977022547, 0.1015624999997554456, 0.1054687499997480626, 0.1074218749997443711, 0.1083984374997425532, 0.1088867187497416511, 0.1091308593747411515, 0.1092529296872409572, 0.1093139648434908601, 0.1093749999997407629, 0.1171874999997305072, 0.1210937499997254280, 0.1230468749997228883, 0.1240234374997216116, 0.1245117187497209732, 0.1247558593747206124, 0.1248779296872204042, 0.1249389648434702932, 0.1249999999997201960, 0.1328124999997058742, 0.1367187499996986855, 0.1386718749996950495, 0.1396484374996932731, 0.1401367187496924127, 0.1403808593746919409, 0.1405029296871916911, 0.1405639648434415523, 0.1406249999996913858, 0.1484374999996694588, 0.1523437499996584676, 0.1542968749996529720, 0.1552734374996502242, 0.1562499999996474764, 0.1718749999996030120, 0.1796874999995808353, 0.1835937499995697331, 0.1855468749995641820, 0.1865234374995614064, 0.1870117187495600464, 0.1872558593745593802, 0.1874999999995587141, 0.2031249999995167199, 0.2109374999994957089, 0.2148437499994851896, 0.2167968749994799160, 0.2177734374994772515, 0.2182617187494758915, 0.2185058593744751976, 0.2187499999994745037, 0.2343749999994305389, 0.2421874999994086675, 0.2460937499993977040, 0.2480468749993922917, 0.2490234374993895161, 0.2499999999993867683, 0.2656249999993429700, 0.2734374999993210986, 0.2773437499993101074, 0.2792968749993046118, 0.2802734374993018363, 0.2807617187493005040, 0.2810058593742998378, 0.2811279296867994493, 0.2812499999992990052, 0.2890624999992653654, 0.2929687499992484900, 0.2949218749992400523, 0.2958984374992357780, 0.2963867187492336130, 0.2966308593742324473, 0.2967529296867319477, 0.2968139648429816146, 0.2968749999992312816, 0.3007812499992075228, 0.3027343749991956989, 0.3037109374991898147, 0.3041992187491868171, 0.3044433593741853183, 0.3045654296866845967, 0.3046264648429341526, 0.3046569824210589306, 0.3046874999991837640, 0.3085937499991546207, 0.3105468749991400768, 0.3115234374991328603, 0.3120117187491293076, 0.3122558593741275312, 0.3124999999991257549, 0.3164062499990981658, 0.3183593749990843991, 0.3193359374990775157, 0.3198242187490740185, 0.3200683593740721866, 0.3201904296865712984, 0.3202514648428208544, 0.3202819824209456323, 0.3202972412100081323, 0.3203124999990706323, 0.3242187499990919486, 0.3261718749991026067, 0.3271484374991079358, 0.3276367187491106558, 0.3278808593741120991, 0.3280029296866128208, 0.3280639648428630983, 0.3280944824209881538, 0.3281249999991131538, 0.3320312499991172617, 0.3339843749991192046, 0.3349609374991203148, 0.3354492187491209254, 0.3356933593741212585, 0.3358154296866214250, 0.3358764648428715915, 0.3359069824209966471, 0.3359374999991216471, 0.3398437499991351363, 0.3417968749991417976, 0.3427734374991450728, 0.3432617187491466271, 0.3435058593741474597, 0.3436279296866479593, 0.3436889648428982369, 0.3437499999991484589, 0.3457031249991600608, 0.3466796874991657784, 0.3471679687491686650, 0.3474121093741702193, 0.3475341796866709965, 0.3476562499991717736, 0.3496093749991845412, 0.3505859374991909250, 0.3510742187491941446, 0.3513183593741958655, 0.3514404296866966981, 0.3515624999991975308, 0.3554687499992247313, 0.3574218749992383315, 0.3583984374992451039, 0.3588867187492485455, 0.3591308593742503219, 0.3593749999992520983, 0.3632812499992802424, 0.3652343749992943978, 0.3662109374993013922, 0.3666992187493048894, 0.3669433593743067212, 0.3671874999993085531, 0.3710937499993385846, 0.3730468749993535726, 0.3740234374993610666, 0.3745117187493647859, 0.3747558593743665623, 0.3748779296868675059, 0.3749999999993684496, 0.3789062499993985922, 0.3808593749994136357, 0.3818359374994211852, 0.3823242187494248490, 0.3828124999994285682, 0.3847656249994435562, 0.3857421874994511057, 0.3862304687494548250, 0.3867187499994585997, 0.3886718749994738098, 0.3896484374994814703, 0.3901367187494852451, 0.3903808593744871325, 0.3906249999994890199, 0.3945312499995182742, 0.3964843749995329292, 0.3974609374995403122, 0.3979492187495439759, 0.3981933593745456967, 0.3983154296870465849, 0.3984374999995474731, 0.4023437499995760613, 0.4042968749995903277, 0.4052734374995974886, 0.4057617187496010414, 0.4060058593746028732, 0.4062499999996046496, 0.4101562499996342925, 0.4121093749996490030, 0.4130859374996563860, 0.4135742187496600497, 0.4138183593746619371, 0.4139404296871629363, 0.4140624999996639355, 0.4179687499996955768, 0.4199218749997114530, 0.4208984374997194466, 0.4213867187497234434, 0.4216308593747254974, 0.4217529296872264966, 0.4218139648434769962, 0.4218444824216022182, 0.4218749999997274958, 0.4296874999997709055, 0.4335937499997924993, 0.4355468749998033240, 0.4365234374998085976, 0.4370117187498112621, 0.4372558593748125944, 0.4373779296873132605, 0.4374389648435635936, 0.4374694824216888156, 0.4374999999998139821, 0.4453124999998648303, 0.4492187499998902545, 0.4511718749999029665, 0.4521484374999093503, 0.4526367187499124589, 0.4528808593749141242, 0.4530029296874149014, 0.4530639648436652900, 0.4531249999999156786, 0.4609374999999559797, 0.4648437499999760747, 0.4667968749999861222, 0.4677734374999912292, 0.4682617187499937828, 0.4685058593749951150, 0.4686279296874957256, 0.4686889648437460032, 0.4687194824218710587, 0.4687499999999961142, 0.4843750000000557332, 0.4921875000000855982, 0.4960937500001005307, 0.4980468750001079137, 0.4990234375001115774, 0.4995117187501134648, 0.4997558593751144085, 0.4998779296876148526, 0.4999389648438650746, 0.5000000000001153522, 0.5078125000001506573, 0.5117187500001684208, 0.5136718750001773026, 0.5146484375001816325, 0.5151367187501839640, 0.5153808593751850742, 0.5155029296876856293, 0.5155639648439359624, 0.5156250000001861844, 0.5234375000002311484, 0.5273437500002536860, 0.5292968750002650102, 0.5302734375002706724, 0.5307617187502734479, 0.5310058593752747802, 0.5311279296877753353, 0.5311889648440256684, 0.5312500000002758904, 0.5468750000003493872, 0.5546875000003861356, 0.5585937500004045653, 0.5605468750004138911, 0.5615234375004185541, 0.5620117187504208855, 0.5622558593754219958, 0.5623779296879225509, 0.5624389648441727729, 0.5624694824222978840, 0.5625000000004229950, 0.5781250000004987122, 0.5859375000005365708, 0.5898437500005554446, 0.5917968750005648815, 0.5927734375005696554, 0.5932617187505719869, 0.5935058593755730971, 0.5936279296880737633, 0.5936889648443239853, 0.5937194824224492073, 0.5937347412115117073, 0.5937500000005743184, 0.6015625000005714318, 0.6054687500005699885, 0.6074218750005692113, 0.6083984375005688783, 0.6088867187505687673, 0.6091308593755686562, 0.6092529296880686562, 0.6093750000005686562, 0.6171875000005672129, 0.6210937500005664358, 0.6230468750005659917, 0.6240234375005658807, 0.6245117187505657697, 0.6247558593755656586, 0.6248779296880656586, 0.6249389648443157697, 0.6249694824224407697, 0.6249847412115031586, 0.6250000000005656586, 0.6406250000005540013, 0.6484375000005482281, 0.6523437500005453415, 0.6542968750005440093, 0.6552734375005432321, 0.6557617187505427880, 0.6560058593755425660, 0.6561279296880424550, 0.6561889648442924550, 0.6562194824224174550, 0.6562500000005424550, 0.6718750000005199174, 0.6796875000005085932, 0.6835937500005029310, 0.6855468750005001555, 0.6865234375004988232, 0.6870117187504981571, 0.6872558593754978240, 0.6873779296879976020, 0.6874389648442474909, 0.6875000000004973799, 0.6953125000004835021, 0.6992187500004765077, 0.7011718750004729550, 0.7021484375004711787, 0.7026367187504702905, 0.7028808593754698464, 0.7030029296879696243, 0.7031250000004694023, 0.7109375000004556355, 0.7148437500004487521, 0.7167968750004453105, 0.7177734375004436451, 0.7182617187504427569, 0.7185058593754423129, 0.7186279296879420908, 0.7186889648441919798, 0.7187500000004419798, 0.7343750000004218847, 0.7421875000004117817, 0.7460937500004067857, 0.7480468750004042322, 0.7490234375004030110, 0.7495117187504024558, 0.7497558593754021228, 0.7498779296879020118, 0.7499389648441520118, 0.7500000000004019007, 0.7578125000003932410, 0.7617187500003889111, 0.7636718750003868017, 0.7646484375003855805, 0.7651367187503850253, 0.7653808593753848033, 0.7655029296878846923, 0.7656250000003845813, 0.7695312500003802514, 0.7714843750003781420, 0.7724609375003770317, 0.7729492187503764766, 0.7731933593753762546, 0.7733154296878761436, 0.7733764648441261436, 0.7734375000003760325, 0.7773437500003719247, 0.7792968750003699263, 0.7802734375003688161, 0.7807617187503682610, 0.7810058593753680389, 0.7811279296878679279, 0.7811889648441179279, 0.7812194824222428169, 0.7812347412113053169, 0.7812423706058364559, 0.7812500000003677059, 0.7832031250003650413, 0.7841796875003637091, 0.7846679687503629319, 0.7849121093753625988, 0.7850341796878624878, 0.7850952148441124878, 0.7851257324222373768, 0.7851409912112998768, 0.7851562500003622658, 0.7871093750003591571, 0.7880859375003576028, 0.7885742187503567147, 0.7888183593753563816, 0.7889404296878561595, 0.7890014648441061595, 0.7890319824222310485, 0.7890625000003559375, 0.7910156250003529399, 0.7919921875003514966, 0.7924804687503506084, 0.7927246093753502754, 0.7928466796878500533, 0.7929077148441000533, 0.7929687500003499423, 0.7949218750003470557, 0.7958984375003456124, 0.7963867187503447242, 0.7966308593753443912, 0.7967529296878441691, 0.7968139648440941691, 0.7968750000003440581, 0.8007812500003379519, 0.8027343750003349543, 0.8037109375003335110, 0.8041992187503327338, 0.8044433593753322898, 0.8045654296878320677, 0.8046264648440820677, 0.8046875000003319567, 0.8085937500003258505, 0.8105468750003228529, 0.8115234375003212985, 0.8120117187503205214, 0.8122558593753200773, 0.8123779296878198553, 0.8125000000003195222, 0.8164062500003130829, 0.8183593750003097522, 0.8193359375003080869, 0.8198242187503073097, 0.8203125000003065326, 0.8242187500003000933, 0.8261718750002967626, 0.8271484375002952083, 0.8276367187502944311, 0.8278808593752939871, 0.8280029296877937650, 0.8280639648440435430, 0.8281250000002934319, 0.8359375000002851053, 0.8398437500002808864, 0.8417968750002787770, 0.8427734375002777778, 0.8432617187502772227, 0.8435058593752770006, 0.8436279296877768896, 0.8436889648440267786, 0.8437194824221518896, 0.8437500000002768896, 0.8593750000002475797, 0.8671875000002329248, 0.8710937500002255973, 0.8730468750002218226, 0.8740234375002200462, 0.8745117187502191580, 0.8747558593752187139, 0.8748779296877184919, 0.8749389648439683809, 0.8749694824220932698, 0.8750000000002181588, 0.8906250000001916245, 0.8984375000001784128, 0.9023437500001717515, 0.9042968750001685319, 0.9052734375001667555, 0.9057617187501659783, 0.9060058593751655343, 0.9061279296876653122, 0.9061889648439152012, 0.9062500000001649791, 0.9218750000001372236, 0.9296875000001233458, 0.9335937500001163514, 0.9355468750001129097, 0.9365234375001112443, 0.9370117187501103562, 0.9372558593751099121, 0.9373779296876096900, 0.9375000000001093570, 0.9531250000000818234, 0.9609375000000680567, 0.9648437500000611733, 0.9687500000000542899, 0.9765625000000405231, 0.9804687500000336398, 0.9824218750000300870, 0.9833984375000284217, 0.9838867187500275335, 0.9841308593750270894, 0.9842529296875268674, 0.9843750000000266454, 1.000000000000000000 ),
 .UNSPECIFIED. ) ;
#69323=CARTESIAN_POINT ( 'NONE',  ( -2.027236533537560614, -46.43928285645216647, 31.62702113814393101 ) ) ;
#69340=CARTESIAN_POINT ( 'NONE',  ( 102.6948251682922404, -14.21045842199434084, 129.2649694714442035 ) ) ;
#69341=CARTESIAN_POINT ( 'NONE',  ( -81.85444700155652242, -36.03095774481810309, 154.5099837279508392 ) ) ;
#69345=SURFACE_SIDE_STYLE ('',( #20839 ) ) ;
#69362=CARTESIAN_POINT ( 'NONE',  ( 19.44199974951657239, -60.00000000000000000, -41.87985567335064019 ) ) ;
#69363=CARTESIAN_POINT ( 'NONE',  ( -42.11059216458311028, -14.21045842199439946, 45.52377215771286245 ) ) ;
#69364=CARTESIAN_POINT ( 'NONE',  ( 22.80451961301133679, -49.91397639351992410, 33.12551050153431476 ) ) ;
#69366=CARTESIAN_POINT ( 'NONE',  ( -34.67237354032933894, -39.50196040766881822, 35.14490241457752262 ) ) ;
#69375=CARTESIAN_POINT ( 'NONE',  ( -75.89053735638948694, -38.37146565025459211, 177.5147526201425876 ) ) ;
#69378=CARTESIAN_POINT ( 'NONE',  ( 99.84112142693871306, -30.00000000000001066, 152.0655077736769840 ) ) ;
#69381=CARTESIAN_POINT ( 'NONE',  ( 76.78203937826565095, -30.00000000000000000, -16.80719657136269163 ) ) ;
#69398=CARTESIAN_POINT ( 'NONE',  ( 57.75597479282357227, -38.34392537241339483, 89.45883036084909179 ) ) ;
#69403=CARTESIAN_POINT ( 'NONE',  ( 61.12256913293067839, -29.06402845109642286, 70.22293933626255580 ) ) ;
#69421=CARTESIAN_POINT ( 'NONE',  ( 84.85594123159673074, -53.83118547258817443, 190.4596540335761006 ) ) ;
#69427=CARTESIAN_POINT ( 'NONE',  ( 2.396333687459205386, -15.43569997946047501, -35.20659080967024579 ) ) ;
#69428=CARTESIAN_POINT ( 'NONE',  ( 0.000000000000000000, -30.00000000000000000, 0.000000000000000000 ) ) ;
#69433=CARTESIAN_POINT ( 'NONE',  ( -86.41920866340555563, -29.99999999999998934, 66.86452767883984905 ) ) ;
#69434=COLOUR_RGB ( '', 0.08235294, 0.09019608, 0.10196078) ;
#69436=CARTESIAN_POINT ( 'NONE',  ( 18.91792220226865595, -57.67176294956599492, 42.07977622032543508 ) ) ;
#69439=CARTESIAN_POINT ( 'NONE',  ( -3.160872658147570124, -18.90246149285938770, 27.03534335979194836 ) ) ;
#69443=CARTESIAN_POINT ( 'NONE',  ( 55.93697197481172623, -28.65094093527318364, -26.29639216960241299 ) ) ;
#69445=CARTESIAN_POINT ( 'NONE',  ( -21.89279155696590706, -18.59654525183585605, 27.69851634783955419 ) ) ;
#69449=CARTESIAN_POINT ( 'NONE',  ( -18.23433844066610376, -56.88320978890689616, 33.72260518641856208 ) ) ;
#69453=EDGE_LOOP ( 'NONE', ( #42758, #74766, #88759, #95430 ) ) ;
#69460=CARTESIAN_POINT ( 'NONE',  ( 102.7253553271523998, -52.71898453613229663, 190.6752664090827523 ) ) ;
#69475=CARTESIAN_POINT ( 'NONE',  ( -51.70258171882510112, -60.00000000001934808, -39.97716527442499768 ) ) ;
#69477=CARTESIAN_POINT ( 'NONE',  ( 83.63626497911887725, -60.00000000000972733, -28.47872482695956364 ) ) ;
#69480=CARTESIAN_POINT ( 'NONE',  ( -98.48977711285814962, -30.00000000000000355, 87.89215492326917456 ) ) ;
#69481=CARTESIAN_POINT ( 'NONE',  ( 4.032806863568136890, -35.99137585659471483, 29.88102657759840497 ) ) ;
#69483=CARTESIAN_POINT ( 'NONE',  ( -48.16068817031700178, -22.22324342221773819, 42.58818931081837889 ) ) ;
#69486=ORIENTED_EDGE ( 'NONE', *, *, #75605, .T. ) ;
#69493=CARTESIAN_POINT ( 'NONE',  ( 80.65654643016394232, -29.99999999999668887, -24.45529829233118235 ) ) ;
#69498=CARTESIAN_POINT ( 'NONE',  ( 100.4860052063238669, -30.00000000000000000, 182.9306020357272189 ) ) ;
#69506=CARTESIAN_POINT ( 'NONE',  ( 54.66621465509991395, -42.96697404677267684, 60.96662553234383353 ) ) ;
#69511=CARTESIAN_POINT ( 'NONE',  ( -90.78511700306292198, -38.40471106913319232, -13.56408848029241199 ) ) ;
#69515=CARTESIAN_POINT ( 'NONE',  ( 89.26648953270368736, -38.52947843327230260, 200.3703952722973440 ) ) ;
#69517=CARTESIAN_POINT ( 'NONE',  ( 83.79989767149710644, -45.28464700058749060, 6.294244894805590462 ) ) ;
#69525=EDGE_CURVE ( 'NONE', #4466, #38791, #77273, .T. ) ;
#69535=CARTESIAN_POINT ( 'NONE',  ( -38.00604678449891338, -25.45322539771995807, 34.78474724553195330 ) ) ;
#69539=CARTESIAN_POINT ( 'NONE',  ( 85.81934268588042869, -25.08133184341231114, 176.6321996554005977 ) ) ;
#69545=CARTESIAN_POINT ( 'NONE',  ( -97.19992022187756220, -52.71041065253648839, 105.9731406578079032 ) ) ;
#69549=CARTESIAN_POINT ( 'NONE',  ( -9.569753713556142571, -22.51754484451500815, -38.54307148179644571 ) ) ;
#69552=CARTESIAN_POINT ( 'NONE',  ( 35.03412771863278152, -60.00000000000000711, 46.43457060836758643 ) ) ;
#69553=CARTESIAN_POINT ( 'NONE',  ( -3.672464763049774796E-06, -18.02989419364509516, 35.00496915990722613 ) ) ;
#69555=CARTESIAN_POINT ( 'NONE',  ( 51.38078702772865824, -29.89861756130085979, 48.96396542489893733 ) ) ;
#69556=CARTESIAN_POINT ( 'NONE',  ( -33.81973378879969516, -34.85196562608981452, 43.20933532560730583 ) ) ;
#69574=CARTESIAN_POINT ( 'NONE',  ( -12.77240031018320288, -47.40885967665541756, -34.44485374093346763 ) ) ;
#69584=CARTESIAN_POINT ( 'NONE',  ( -92.23642043756412079, -60.00000000000000000, 2.389009461067983953 ) ) ;
#69592=CARTESIAN_POINT ( 'NONE',  ( -80.54183813965836691, -56.90184267136208973, 174.6177441223669291 ) ) ;
#69594=CARTESIAN_POINT ( 'NONE',  ( -7.540142361522498504, 0.000000000000000000, 15.29459302240409002 ) ) ;
#69602=CARTESIAN_POINT ( 'NONE',  ( -93.98392372475152001, -57.65316015971099972, -14.13389826495936141 ) ) ;
#69608=CARTESIAN_POINT ( 'NONE',  ( 73.45964196357411424, -30.00000000000000355, -28.33384050355910588 ) ) ;
#69609=CARTESIAN_POINT ( 'NONE',  ( -85.76719879059909601, -14.21045842199445630, 195.9089143291284074 ) ) ;
#69610=CARTESIAN_POINT ( 'NONE',  ( -56.50716156543574442, -22.14567382208074164, 56.45488485479982899 ) ) ;
#69614=CARTESIAN_POINT ( 'NONE',  ( -105.1976808963021313, -60.15494405590796134, 187.0891470627859405 ) ) ;
#69622=CARTESIAN_POINT ( 'NONE',  ( 76.12557658274094763, -38.35599704320051728, -28.58424740099940919 ) ) ;
#69633=CARTESIAN_POINT ( 'NONE',  ( -27.12260435713527684, -49.91548920431219472, 34.05356483041720139 ) ) ;
#69634=CARTESIAN_POINT ( 'NONE',  ( 47.58705169032300830, -56.81477742123609431, 52.30342271811583288 ) ) ;
#69637=CARTESIAN_POINT ( 'NONE',  ( -89.80356045261119391, -38.51850677248155108, 200.5196326713219719 ) ) ;
#69645=FACE_OUTER_BOUND ( 'NONE', #68801, .T. ) ;
#69646=CARTESIAN_POINT ( 'NONE',  ( 112.1210090530907024, -60.00000000000002132, 177.5107359543562779 ) ) ;
#69654=CARTESIAN_POINT ( 'NONE',  ( -81.60154244327691231, -30.00000000000000000, -6.159883939146816090 ) ) ;
#69656=CARTESIAN_POINT ( 'NONE',  ( -64.84495818255328459, -38.33846756661721855, 112.5933220119225666 ) ) ;
#69664=ORIENTED_EDGE ( 'NONE', *, *, #74452, .F. ) ;
#69665=CARTESIAN_POINT ( 'NONE',  ( 82.28231359831326586, -46.46483616827516272, 174.1978786872764431 ) ) ;
#69679=CARTESIAN_POINT ( 'NONE',  ( -76.11217929027031914, -30.00000000000000355, -17.27491633377325186 ) ) ;
#69709=CARTESIAN_POINT ( 'NONE',  ( -112.0091148159200856, -60.00000000000000000, 179.5044317187202125 ) ) ;
#69714=CARTESIAN_POINT ( 'NONE',  ( -86.00678846258095689, -21.65130990580026449, 173.2951746391152881 ) ) ;
#69722=CARTESIAN_POINT ( 'NONE',  ( -83.72505494025215000, -45.26660870684003868, 8.238952501196534328 ) ) ;
#69726=CARTESIAN_POINT ( 'NONE',  ( 109.3513501059324255, -30.00000000000000000, 179.6549720493207190 ) ) ;
#69729=CARTESIAN_POINT ( 'NONE',  ( 75.88724551625310255, -29.99999999999989697, 164.4338130987444231 ) ) ;
#69730=CARTESIAN_POINT ( 'NONE',  ( -82.74168755217822024, -14.21045842199452203, -19.52755005266771349 ) ) ;
#69731=CARTESIAN_POINT ( 'NONE',  ( -63.48454154046918774, -53.39210001124775573, 88.97591336427868214 ) ) ;
#69733=CARTESIAN_POINT ( 'NONE',  ( 104.0082629745172653, -14.21045842199441012, 192.0643512960946282 ) ) ;
#69735=CARTESIAN_POINT ( 'NONE',  ( 31.23755223876165132, -60.00000000000493827, 46.45901925853441128 ) ) ;
#69745=CARTESIAN_POINT ( 'NONE',  ( -79.05509554772149272, -60.00000000000000000, -28.49194458007684005 ) ) ;
#69758=CARTESIAN_POINT ( 'NONE',  ( 34.57993830756027620, -60.29654495889643329, 39.05213902588479158 ) ) ;
#69759=CARTESIAN_POINT ( 'NONE',  ( -6.601913983200961233, -4.285714285712858285, -24.56594385547797543 ) ) ;
#69774=CARTESIAN_POINT ( 'NONE',  ( 92.43235373876116512, -60.00000000000000711, -0.2938010258920950579 ) ) ;
#69782=CARTESIAN_POINT ( 'NONE',  ( -89.68653756732776117, -29.99999999999227640, 199.1857044332254247 ) ) ;
#69786=CARTESIAN_POINT ( 'NONE',  ( 82.26020361419449500, -37.81322313179484951, -13.24491807084091555 ) ) ;
#69796=CARTESIAN_POINT ( 'NONE',  ( 77.45305305485931058, -42.96330883344779039, 134.7310727137066522 ) ) ;
#69801=CARTESIAN_POINT ( 'NONE',  ( -80.45353917958989598, -57.50988970295517788, 199.2734438750461550 ) ) ;
#69809=CARTESIAN_POINT ( 'NONE',  ( -45.16073431462941556, -28.35099063806825725, 40.24582607710122062 ) ) ;
#69819=EDGE_CURVE ( 'NONE', #65536, #59024, #44718, .T. ) ;
#69822=CARTESIAN_POINT ( 'NONE',  ( 69.36755836386646479, -30.21241150966188016, -29.99922498068983145 ) ) ;
#69823=CARTESIAN_POINT ( 'NONE',  ( -69.99800859030240474, -30.00000000000000355, 95.31859612160674544 ) ) ;
#69828=CARTESIAN_POINT ( 'NONE',  ( 74.87226039639872965, -57.58023860409628725, 190.2883175146000383 ) ) ;
#69835=CARTESIAN_POINT ( 'NONE',  ( -50.05807582380210619, -60.00000000000000711, 71.95124345659672827 ) ) ;
#69841=CARTESIAN_POINT ( 'NONE',  ( -86.09249853775514794, -31.93869936210829508, 184.2230114830187517 ) ) ;
#69844=CARTESIAN_POINT ( 'NONE',  ( -3.977975743268641118, -22.06767091311041540, 27.56089423025632001 ) ) ;
#69859=CARTESIAN_POINT ( 'NONE',  ( -5.820808985964939453, -8.673617379884035472E-16, 21.65942590380532451 ) ) ;
#69861=CARTESIAN_POINT ( 'NONE',  ( 89.80793189580856506, -29.99999999999993250, 26.19443836851201723 ) ) ;
#69862=CARTESIAN_POINT ( 'NONE',  ( -80.30188067886301440, -39.50080336238898582, 147.7263073883484310 ) ) ;
#69866=CARTESIAN_POINT ( 'NONE',  ( 46.16030844547664458, -57.68192973205171370, 67.73425372236864916 ) ) ;
#69883=CARTESIAN_POINT ( 'NONE',  ( 92.74728809772592797, -60.00000000000000000, -7.135771891692349378 ) ) ;
#69884=CARTESIAN_POINT ( 'NONE',  ( -68.99627713242672655, -30.00000000000000355, 123.4899896973233808 ) ) ;
#69885=CARTESIAN_POINT ( 'NONE',  ( 27.03448325452836443, -18.62296646550320389, 28.59903465579650828 ) ) ;
#69889=CARTESIAN_POINT ( 'NONE',  ( -34.65605967281282318, -18.71474442840510477, 31.05779364914194929 ) ) ;
#69892=CARTESIAN_POINT ( 'NONE',  ( -20.05453516056601515, -4.285714285714296246, -15.38541618194247995 ) ) ;
#69899=CARTESIAN_POINT ( 'NONE',  ( -68.79315106226179921, -38.33280406146015906, 128.9874879556798248 ) ) ;
#69900=CARTESIAN_POINT ( 'NONE',  ( 95.57908735654217480, -29.99999999999999289, 121.4573267557989595 ) ) ;
#69903=CARTESIAN_POINT ( 'NONE',  ( 81.43457655364417747, -30.00000000000000000, -9.796964337323872840 ) ) ;
#69928=CARTESIAN_POINT ( 'NONE',  ( 63.57049037775179556, -36.00627426888244287, 80.25959675227277046 ) ) ;
#69931=CARTESIAN_POINT ( 'NONE',  ( -55.68886407967555385, -36.67780875632375626, -35.12440533619799510 ) ) ;
#69940=DIRECTION ( 'NONE',  ( 0.000000000000000000, 0.000000000000000000, -1.000000000000000000 ) ) ;
#69944=CARTESIAN_POINT ( 'NONE',  ( 85.61863528710425442, -42.90344064078778530, 187.3753977056170470 ) ) ;
#69948=CARTESIAN_POINT ( 'NONE',  ( 28.03203034650283598, -57.67082107358243093, -43.15016037083558587 ) ) ;
#69949=CARTESIAN_POINT ( 'NONE',  ( 71.80342808059911874, -29.99999999999997868, -19.71766482350836824 ) ) ;
#69955=CARTESIAN_POINT ( 'NONE',  ( -100.3088744048629906, -30.00000000000000000, 156.9982617682830153 ) ) ;
#69957=CARTESIAN_POINT ( 'NONE',  ( 19.17204277030731774, -57.67181344388957598, 42.10895013444159218 ) ) ;
#69966=VERTEX_POINT ( 'NONE', #91991 ) ;
#69968=CARTESIAN_POINT ( 'NONE',  ( -17.67175098956017010, -29.03273846940966507, 29.02266591207046531 ) ) ;
#69969=CARTESIAN_POINT ( 'NONE',  ( -86.88889009608627134, -60.00000000000000711, -3.512934530641961928 ) ) ;
#69978=ORIENTED_EDGE ( 'NONE', *, *, #43782, .F. ) ;
#69982=CARTESIAN_POINT ( 'NONE',  ( 101.8615519058133572, -52.72503690623052819, 192.2815353188802874 ) ) ;
#69995=ORIENTED_EDGE ( 'NONE', *, *, #57496, .F. ) ;
#69998=CARTESIAN_POINT ( 'NONE',  ( -22.48210626068904361, -59.99999999999999289, -44.04839377960101388 ) ) ;
#70000=CARTESIAN_POINT ( 'NONE',  ( 22.40836378693191477, -60.00000000001930545, -44.01644647174431668 ) ) ;
#70003=AXIS2_PLACEMENT_3D ( 'NONE', #42035, #8071, #90593 ) ;
#70004=CARTESIAN_POINT ( 'NONE',  ( -99.88998825557715122, -14.21045842199445808, 111.7645417027540304 ) ) ;
#70005=CARTESIAN_POINT ( 'NONE',  ( 8.311083903413562624, -56.87791216858510523, 33.36314354383234360 ) ) ;
#70006=CARTESIAN_POINT ( 'NONE',  ( -47.66079575541817803, -46.44466184579120949, 49.24308826707560627 ) ) ;
#70019=CARTESIAN_POINT ( 'NONE',  ( 88.95789393506666443, -29.99999999999496936, -14.90288515927673174 ) ) ;
#70022=CARTESIAN_POINT ( 'NONE',  ( 101.0502629568186421, -30.00000000000000000, 167.9018042051803263 ) ) ;
#70027=CARTESIAN_POINT ( 'NONE',  ( 55.11625962268163192, -32.55886939003519132, 57.75275617000808381 ) ) ;
#70034=CARTESIAN_POINT ( 'NONE',  ( 105.3592957826458587, -38.38743339881243344, 197.1096209424719632 ) ) ;
#70036=CARTESIAN_POINT ( 'NONE',  ( 83.82860702337691805, -45.28512348765533346, 5.649739562308606189 ) ) ;
#70057=CARTESIAN_POINT ( 'NONE',  ( -32.39494539084744673, -25.32206235645057646, 40.19353790443526009 ) ) ;
#70063=CARTESIAN_POINT ( 'NONE',  ( 85.04864020517048573, -35.79319779513708966, 181.2967254180193777 ) ) ;
#70067=CARTESIAN_POINT ( 'NONE',  ( -96.39296834135954839, -37.82067409071415653, 116.1803817724870100 ) ) ;
#70073=CARTESIAN_POINT ( 'NONE',  ( -0.01393140247697588312, -21.31702117966834109, -38.55283400289633278 ) ) ;
#70076=CARTESIAN_POINT ( 'NONE',  ( 11.30126247058972666, -20.79179180331792054, 35.49637522244798760 ) ) ;
#70078=CARTESIAN_POINT ( 'NONE',  ( 50.01436079198998641, -29.69237965549699965, 46.63421092844703963 ) ) ;
#70086=CARTESIAN_POINT ( 'NONE',  ( -82.94541017858439602, -38.00000000000004263, 0.2650007619690297189 ) ) ;
#70093=CARTESIAN_POINT ( 'NONE',  ( -3.132749564764621297, -34.58960321509062652, -32.63485548209730069 ) ) ;
#70101=CARTESIAN_POINT ( 'NONE',  ( -91.86565372589397782, -60.00000000000001421, 10.89366606999959330 ) ) ;
#70110=CARTESIAN_POINT ( 'NONE',  ( -85.21609695689519981, -22.03875263890091674, 162.9510693786682509 ) ) ;
#70112=ORIENTED_EDGE ( 'NONE', *, *, #28403, .T. ) ;
#70113=CARTESIAN_POINT ( 'NONE',  ( -1.113934713178898139, -0.000000000000000000, 17.01589776168603763 ) ) ;
#70114=EDGE_LOOP ( 'NONE', ( #19797, #81302 ) ) ;
#70122=CARTESIAN_POINT ( 'NONE',  ( -96.68549010014578471, -57.67144976548149771, 46.95518404347522079 ) ) ;
#70130=CARTESIAN_POINT ( 'NONE',  ( 64.66821620130598092, -14.21045842199433373, -28.81313120037184916 ) ) ;
#70131=CARTESIAN_POINT ( 'NONE',  ( -62.45630560627096628, -29.99999999999992184, 99.43668923270982418 ) ) ;
#70132=CARTESIAN_POINT ( 'NONE',  ( -54.20616908285522584, -42.97143615225327551, 59.98809675918620599 ) ) ;
#70138=CARTESIAN_POINT ( 'NONE',  ( -103.2098837543867660, -60.16809070699064677, 192.4864521153085377 ) ) ;
#70139=CARTESIAN_POINT ( 'NONE',  ( 102.6011607304368027, -37.99999999999997868, 179.5962889347694613 ) ) ;
#70150=CARTESIAN_POINT ( 'NONE',  ( 66.20789329592186334, -30.00000000000000355, 83.72596625502930578 ) ) ;
#70156=CARTESIAN_POINT ( 'NONE',  ( -28.53269844911218200, -53.39016512961349292, 35.08051764473837864 ) ) ;
#70158=CARTESIAN_POINT ( 'NONE',  ( 48.01372197413871845, -42.98097658514403463, 48.71122713025049222 ) ) ;
#70162=CARTESIAN_POINT ( 'NONE',  ( -94.01096082434968082, -38.49234416915790291, 201.1924522757551017 ) ) ;
#70164=CARTESIAN_POINT ( 'NONE',  ( 91.47297658247813956, -38.38308769809394505, -6.128389452813496341 ) ) ;
#70172=CARTESIAN_POINT ( 'NONE',  ( 112.1739726238778161, -59.99999999999999289, 168.9510083732245675 ) ) ;
#70178=CARTESIAN_POINT ( 'NONE',  ( -80.87453322288685342, -30.00000000000003908, 6.258431868449455315 ) ) ;
#70180=CARTESIAN_POINT ( 'NONE',  ( -82.77499858381615638, -38.82538985791964592, 196.7482481615944891 ) ) ;
#70190=CARTESIAN_POINT ( 'NONE',  ( 80.54825481451001679, -60.43138345613007800, 180.0438305313103058 ) ) ;
#70226=ORIENTED_EDGE ( 'NONE', *, *, #103922, .T. ) ;
#70236=CARTESIAN_POINT ( 'NONE',  ( -103.5078833138821182, -59.99999999999999289, 200.3335383992328786 ) ) ;
#70241=CARTESIAN_POINT ( 'NONE',  ( -83.18122759319267345, -46.51677116687196190, 180.8298306939889812 ) ) ;
#70247=CARTESIAN_POINT ( 'NONE',  ( -83.66823586964305548, -45.26509719214853078, 13.41398437886814143 ) ) ;
#70252=CARTESIAN_POINT ( 'NONE',  ( 2.499999999999997335, -30.00000000000000000, 30.00000000000000000 ) ) ;
#70255=CARTESIAN_POINT ( 'NONE',  ( 93.93534938131868728, -14.21045842199442433, 198.1410878059230072 ) ) ;
#70257=CARTESIAN_POINT ( 'NONE',  ( -95.23228170574914486, -59.99999999999995737, 30.92731164540345645 ) ) ;
#70258=CARTESIAN_POINT ( 'NONE',  ( -63.91133421294225059, -36.00889000299856235, 81.23570399580073342 ) ) ;
#70260=CARTESIAN_POINT ( 'NONE',  ( 80.26999927900735088, -59.99999999999982947, 200.1019127161866606 ) ) ;
#70262=CARTESIAN_POINT ( 'NONE',  ( 89.69739047552775446, -59.99999999999509015, 204.4076188194097483 ) ) ;
#70275=CARTESIAN_POINT ( 'NONE',  ( -92.73282884694502570, -60.00000000000001421, -8.836575342051251170 ) ) ;
#70291=CARTESIAN_POINT ( 'NONE',  ( 36.59678287535385266, -32.58377898008321694, 34.88015138182827712 ) ) ;
#70306=CARTESIAN_POINT ( 'NONE',  ( 92.68036264477171926, -60.00000000000002132, -4.335246237957126603 ) ) ;
#70313=CARTESIAN_POINT ( 'NONE',  ( -92.59962393262327396, -29.99999999998227551, 199.7669230624210002 ) ) ;
#70319=CARTESIAN_POINT ( 'NONE',  ( 81.77433114748801302, -37.82765095025914093, -14.17082202020662152 ) ) ;
#70328=CARTESIAN_POINT ( 'NONE',  ( 79.32494501487229854, -39.49602140262202710, 141.5487238132834023 ) ) ;
#70330=EDGE_LOOP ( 'NONE', ( #51982, #25307 ) ) ;
#70333=CARTESIAN_POINT ( 'NONE',  ( -104.1916751217198822, -57.64030415157957066, 202.2041723927455905 ) ) ;
#70344=CARTESIAN_POINT ( 'NONE',  ( -49.53127930048969318, -29.59600273485972366, 45.87288584322060103 ) ) ;
#70356=CARTESIAN_POINT ( 'NONE',  ( 54.29649119386410661, -29.25829085814808650, -34.21479539254390545 ) ) ;
#70357=CARTESIAN_POINT ( 'NONE',  ( -82.84466124429486911, -30.00000000000000355, 151.7715457259677976 ) ) ;
#70363=CARTESIAN_POINT ( 'NONE',  ( 81.75912227876649752, -57.51972024110150983, 200.3275499453189070 ) ) ;
#70364=CARTESIAN_POINT ( 'NONE',  ( 74.86755951436030898, -60.22812835740788273, -24.22374349095017365 ) ) ;
#70369=CARTESIAN_POINT ( 'NONE',  ( -55.88924746550470957, -60.00000000000000711, 87.85475180783302562 ) ) ;
#70374=CARTESIAN_POINT ( 'NONE',  ( -86.09514901757498251, -28.33536443523890114, 182.5650114012098300 ) ) ;
#70377=CARTESIAN_POINT ( 'NONE',  ( 4.364333581248146211E-05, -49.92101465095216639, 32.20981906809440432 ) ) ;
#70389=CARTESIAN_POINT ( 'NONE',  ( 20.16952962162617879, -4.285714285716217375, 15.50035291838605467 ) ) ;
#70393=CARTESIAN_POINT ( 'NONE',  ( 94.21232436905559382, -59.99999999999992895, 13.85190642028294761 ) ) ;
#70394=CARTESIAN_POINT ( 'NONE',  ( -80.01377271962273596, -32.56088685926365400, 138.7306771739739588 ) ) ;
#70398=CARTESIAN_POINT ( 'NONE',  ( 79.02477813168630405, -57.50590731851511350, 197.8598049514260708 ) ) ;
#70419=CARTESIAN_POINT ( 'NONE',  ( 38.79242140487948376, -60.00000000000000000, -39.81019021691462001 ) ) ;
#70420=CARTESIAN_POINT ( 'NONE',  ( -44.76022593139747840, -29.99999999999992539, 54.38475608328532473 ) ) ;
#70421=CARTESIAN_POINT ( 'NONE',  ( 24.64265655959308177, -32.51917606842599184, 30.48593585286307928 ) ) ;
#70426=CARTESIAN_POINT ( 'NONE',  ( -19.00223544648544305, -4.285714285714295357, -16.66764709352488083 ) ) ;
#70435=CARTESIAN_POINT ( 'NONE',  ( 98.10535912706410500, -29.99999999999996447, 190.4157711056429889 ) ) ;
#70439=CARTESIAN_POINT ( 'NONE',  ( 78.36382142249493654, -29.99999999999999645, -15.57094275508443815 ) ) ;
#70456=CARTESIAN_POINT ( 'NONE',  ( 44.47534377888507606, -38.31160956920668070, 57.00192013341546016 ) ) ;
#70461=CARTESIAN_POINT ( 'NONE',  ( 64.34760809152027150, -29.05394656327659675, 78.93212883145818637 ) ) ;
#70464=CARTESIAN_POINT ( 'NONE',  ( -46.37470752763751847, -34.70867711623044016, -36.69855284394721195 ) ) ;
#70478=CARTESIAN_POINT ( 'NONE',  ( 85.54013868611671967, -53.83156724899034629, 191.4350006523445984 ) ) ;
#70486=CARTESIAN_POINT ( 'NONE',  ( -97.58969750147805655, -30.00000000000000355, 134.6660703783357746 ) ) ;
#70490=CARTESIAN_POINT ( 'NONE',  ( 19.90515936436859334, -57.67199060621977225, 42.19861848689678396 ) ) ;
#70503=CARTESIAN_POINT ( 'NONE',  ( -86.89094463637313481, -60.98404555833182172, 194.8809632880474680 ) ) ;
#70507=CARTESIAN_POINT ( 'NONE',  ( -13.71681562663793841, -56.88406381427680003, 33.46245320680461788 ) ) ;
#70508=CARTESIAN_POINT ( 'NONE',  ( -103.3239848065108930, -60.00000000000002842, 136.7923039559513825 ) ) ;
#70511=B_SPLINE_CURVE_WITH_KNOTS ( 'NONE', 3,
 ( #66257, #43058, #415, #26908, #59782, #92658, #84583, #18818, #43579, #58713, #58160, #76466, #33382, #99142, #25302, #91088, #17195, #82977, #53792, #52728, #87238, #30075, #94810, #37122, #71039, #45197, #77547, #20432, #4186, #13317, #94267, #29562, #86193, #103930 ),
 .UNSPECIFIED., .F., .F.,
 ( 4, 2, 2, 2, 2, 2, 2, 2, 2, 2, 2, 2, 2, 2, 2, 2, 4 ),
 ( 0.06792443330486737374, 0.06987512198849422929, 0.07182581067212108483, 0.07572718803937480980, 0.07962856540662852090, 0.08352994277388223199, 0.09133269750838966805, 0.09913545224289710411, 0.1010861409265239735, 0.1030368296101508430, 0.1069382069774045818, 0.1108395843446583068, 0.1127902730282851762, 0.1147409617119120595, 0.1225437164464195927, 0.1264450938136733593, 0.1303464711809270982 ),
 .UNSPECIFIED. ) ;
#70534=CARTESIAN_POINT ( 'NONE',  ( -99.84173967043324183, -59.99999999999388223, 204.4316739029779342 ) ) ;
#70537=CARTESIAN_POINT ( 'NONE',  ( 75.93419637478046980, -59.99999999999036504, -32.67258319081769713 ) ) ;
#70540=CARTESIAN_POINT ( 'NONE',  ( -98.01432676219248208, -59.99999999999999289, 53.56972733528865405 ) ) ;
#70541=CARTESIAN_POINT ( 'NONE',  ( 10.08504398947854064, -22.06746529747525187, 27.57661867756857532 ) ) ;
#70546=CARTESIAN_POINT ( 'NONE',  ( -48.47199924648073477, -29.14092461735632966, 45.10971830478670341 ) ) ;
#70554=ORIENTED_EDGE ( 'NONE', *, *, #84476, .T. ) ;
#70557=CARTESIAN_POINT ( 'NONE',  ( 86.11313230656898554, -29.99999999999747047, -19.76934824123757295 ) ) ;
#70562=CARTESIAN_POINT ( 'NONE',  ( 99.08546831463196725, -30.00000000000000000, 188.6244390898592087 ) ) ;
#70564=CARTESIAN_POINT ( 'NONE',  ( -80.00000000000000000, -60.00000000000000000, -21.09707704303352926 ) ) ;
#70569=CARTESIAN_POINT ( 'NONE',  ( 54.06147519409380919, -46.43629282806927705, 61.05405196347986418 ) ) ;
#70577=CARTESIAN_POINT ( 'NONE',  ( 95.33069953613802738, -38.48758898485506563, 201.2218942298954403 ) ) ;
#70579=CARTESIAN_POINT ( 'NONE',  ( 85.20578200364217025, -52.71162868700685777, 3.232510328549902834 ) ) ;
#70594=CARTESIAN_POINT ( 'NONE',  ( 36.53097960655163234, -27.14942307569473812, 43.41884094172100106 ) ) ;
#70599=CARTESIAN_POINT ( 'NONE',  ( 86.13523834728314910, -21.45781864377238080, 175.8968767354805891 ) ) ;
#70602=CARTESIAN_POINT ( 'NONE',  ( 93.83738680290022671, -57.67473493691561970, 11.13690244224351744 ) ) ;
#70606=CARTESIAN_POINT ( 'NONE',  ( -10.39125135082022133, -22.71708686573491676, -38.54243321615867046 ) ) ;
#70610=CARTESIAN_POINT ( 'NONE',  ( 14.34351097178316792, -22.32601165078034100, 35.84233650071320909 ) ) ;
#70612=CARTESIAN_POINT ( 'NONE',  ( 40.88865618426756754, -26.70336337441984398, 36.55245364840668287 ) ) ;
#70622=CARTESIAN_POINT ( 'NONE',  ( -82.92878276329815890, -38.00000000000002132, -11.27138431556246445 ) ) ;
#70627=CARTESIAN_POINT ( 'NONE',  ( -3.091876355183101222, -21.77033853492639892, -30.49856546722038075 ) ) ;
#70636=CARTESIAN_POINT ( 'NONE',  ( -92.72129515489801577, -59.99999999999999289, -5.456489434213922074 ) ) ;
#70644=CARTESIAN_POINT ( 'NONE',  ( -84.90416487719758720, -22.08403841940192791, 159.8761325681244898 ) ) ;
#70655=CARTESIAN_POINT ( 'NONE',  ( -77.41886385744251697, -57.67119865640713527, -31.55546021046578531 ) ) ;
#70663=CARTESIAN_POINT ( 'NONE',  ( 89.66268371970539874, -30.00000000000002487, 1.291492552605954858 ) ) ;
#70665=CARTESIAN_POINT ( 'NONE',  ( -70.37903440132366484, -60.00000000000007816, 160.1141433014324207 ) ) ;
#70667=CARTESIAN_POINT ( 'NONE',  ( -55.11144128549652521, -42.97100987774245340, 61.94656224094574526 ) ) ;
#70670=CARTESIAN_POINT ( 'NONE',  ( -100.8738977265185639, -45.26319457549800518, 191.5258224205792601 ) ) ;
#70687=CARTESIAN_POINT ( 'NONE',  ( -29.33270313108591054, -42.96186199998404476, 33.51438719604331595 ) ) ;
#70691=CARTESIAN_POINT ( 'NONE',  ( 48.13898221510520159, -25.68296270444842833, 43.60581086135196216 ) ) ;
#70695=CARTESIAN_POINT ( 'NONE',  ( -108.9040701096337642, -38.35651194470214165, 190.4373969938603750 ) ) ;
#70697=CARTESIAN_POINT ( 'NONE',  ( 90.70450050837293077, -38.34778541823943243, 17.01427291654408691 ) ) ;
#70704=CARTESIAN_POINT ( 'NONE',  ( 95.81331084581961477, -60.00000000000000711, 202.5570423909187241 ) ) ;
#70714=CARTESIAN_POINT ( 'NONE',  ( -104.7804267488673702, -38.39777790597128160, 197.7088218984990249 ) ) ;
#70723=CARTESIAN_POINT ( 'NONE',  ( 82.82554601665236760, -42.97346742193234093, 173.7275920582182209 ) ) ;
#70733=CARTESIAN_POINT ( 'NONE',  ( -76.70973338117516960, -29.99999999999999645, -16.85903177628167171 ) ) ;
#70762=CARTESIAN_POINT ( 'NONE',  ( -102.8445772722775757, -60.00000000000001421, 200.7018563251100716 ) ) ;
#70767=CARTESIAN_POINT ( 'NONE',  ( -85.74133566425317099, -25.15092753419028426, 175.6283754751043205 ) ) ;
#70768=ADVANCED_FACE ( 'NONE', ( #80718 ), #55890, .F. ) ;
#70774=CARTESIAN_POINT ( 'NONE',  ( -0.01393140247697588312, -21.31702117966834109, -38.55283400289633278 ) ) ;
#70776=CARTESIAN_POINT ( 'NONE',  ( -85.09173559602810144, -52.70611635879131285, 20.05387495587346791 ) ) ;
#70781=DIRECTION ( 'NONE',  ( 0.000000000000000000, 1.000000000000000000, 0.000000000000000000 ) ) ;
#70783=CARTESIAN_POINT ( 'NONE',  ( 83.30384756245543088, -14.21045842199437992, 194.5080389997825137 ) ) ;
#70786=CARTESIAN_POINT ( 'NONE',  ( -93.38368407206768040, -29.99999999999995026, 56.44986585522355682 ) ) ;
#70787=CARTESIAN_POINT ( 'NONE',  ( -63.36831511047880383, -60.34524114802070471, 92.29660992010968812 ) ) ;
#70790=CARTESIAN_POINT ( 'NONE',  ( 83.02744550429022752, -59.99999999998394884, 201.8714438680229080 ) ) ;
#70795=VERTEX_POINT ( 'NONE', #103418 ) ;
#70797=EDGE_LOOP ( 'NONE', ( #75866, #69277, #41008, #81676 ) ) ;
#70800=CARTESIAN_POINT ( 'NONE',  ( -92.44597693169667707, -60.00000000000000000, -0.4208892430063501111 ) ) ;
#70816=CARTESIAN_POINT ( 'NONE',  ( 33.65780094057635097, -42.96203205001530279, 35.30807191987746307 ) ) ;
#70818=CARTESIAN_POINT ( 'NONE',  ( 2.227375807148842313, -1.734723475976807094E-15, -17.01589776168603407 ) ) ;
#70832=CARTESIAN_POINT ( 'NONE',  ( 92.00147787190707049, -59.99999999999999289, 6.177437106672091005 ) ) ;
#70839=CARTESIAN_POINT ( 'NONE',  ( -75.51516288543771793, -30.00000000000000000, -27.33247042156349593 ) ) ;
#70845=CARTESIAN_POINT ( 'NONE',  ( 81.92498789339509813, -37.82295742025830521, -13.91723281769504261 ) ) ;
#70851=ORIENTED_EDGE ( 'NONE', *, *, #6254, .T. ) ;
#70855=CARTESIAN_POINT ( 'NONE',  ( 78.02883230765388589, -60.30886709744162744, 156.3352327953801932 ) ) ;
#70863=CARTESIAN_POINT ( 'NONE',  ( -97.80441453946778552, -57.62343821539597855, 204.4198989768915453 ) ) ;
#70872=CARTESIAN_POINT ( 'NONE',  ( -4.628935241158544933, -12.82406801309825362, 32.11820816612952711 ) ) ;
#70880=CARTESIAN_POINT ( 'NONE',  ( -58.44719103041130381, -29.04876852297121204, -25.50753101827990577 ) ) ;
#70881=CARTESIAN_POINT ( 'NONE',  ( -81.05591908368936060, -29.99999999999999645, 140.3178133568220005 ) ) ;
#70886=CARTESIAN_POINT ( 'NONE',  ( 106.5916955408424371, -57.65224678697860128, 200.4434517509536988 ) ) ;
#70888=CARTESIAN_POINT ( 'NONE',  ( 65.15535363651697764, -60.22825919689577034, -28.17460905593080511 ) ) ;
#70889=CARTESIAN_POINT ( 'NONE',  ( 74.41005759311713064, -38.35600211243141899, -29.42050377152623497 ) ) ;
#70892=B_SPLINE_CURVE_WITH_KNOTS ( 'NONE', 3,
 ( #3759, #94364, #31755, #55457, #98055, #66219, #80804, #15006, #6919, #106674, #105616, #33350, #23671, #49502, #73774, #32822, #41413, #64636, #56520, #89972, #7976, #57579, #16076, #55978, #97507, #88912, #24729, #39840, #14463, #90501, #48434, #47898, #31241, #73230, #22624, #81327 ),
 .UNSPECIFIED., .F., .F.,
 ( 4, 2, 2, 2, 2, 2, 2, 2, 2, 2, 2, 2, 2, 2, 2, 2, 2, 4 ),
 ( 0.2332227355109234568, 0.2353943896690517124, 0.2375660438271799679, 0.2419093521434364791, 0.2462526604596929902, 0.2505959687759495291, 0.2592825854084624404, 0.2679692020409754072, 0.2766558186734883185, 0.2853424353060012852, 0.3027156685710271078, 0.3200889018360528748, 0.3287755184685657861, 0.3374621351010786974, 0.3461487517335915531, 0.3548353683661044644, 0.3635219849986173202, 0.3722086016311302314 ),
 .UNSPECIFIED. ) ;
#70894=CARTESIAN_POINT ( 'NONE',  ( -53.50019290532922156, -60.00000000000001421, 81.03251237504147753 ) ) ;
#70899=CARTESIAN_POINT ( 'NONE',  ( -86.13874000985406099, -31.92344543271792645, 184.4244860863919655 ) ) ;
#70912=CARTESIAN_POINT ( 'NONE',  ( -21.65942590379792776, -9.659702761776270386E-13, -5.820808985972203864 ) ) ;
#70914=CARTESIAN_POINT ( 'NONE',  ( 86.49463782384169974, -14.21045842199436215, 11.84774393978288742 ) ) ;
#70915=CARTESIAN_POINT ( 'NONE',  ( -76.86963417182471403, -56.84750332144378149, 144.4150324011044120 ) ) ;
#70919=CARTESIAN_POINT ( 'NONE',  ( 70.80457761868248667, -57.68231074300476990, 160.5472033026200336 ) ) ;
#70940=CARTESIAN_POINT ( 'NONE',  ( -64.23299091672136285, -59.99999999999999289, 125.0187485388276656 ) ) ;
#70941=CARTESIAN_POINT ( 'NONE',  ( 28.03697802430866659, -56.86230969446410910, 35.51620881315012923 ) ) ;
#70955=CARTESIAN_POINT ( 'NONE',  ( 61.04765681913714559, -30.00000000000000000, 69.49378535683561608 ) ) ;
#70957=CARTESIAN_POINT ( 'NONE',  ( 81.10659294315915702, -29.99999999999999645, 2.312534082856741779 ) ) ;
#70980=CARTESIAN_POINT ( 'NONE',  ( 61.92817443706537972, -56.86333258057452156, 86.14193829594731255 ) ) ;
#70991=CARTESIAN_POINT ( 'NONE',  ( 52.47345282232834762, -59.99999999999999289, -31.55443244153824267 ) ) ;
#70994=CARTESIAN_POINT ( 'NONE',  ( 86.71742706962844238, -20.66538005307103987, 185.1322602298917843 ) ) ;
#71005=CARTESIAN_POINT ( 'NONE',  ( -99.82224909337540453, -29.99999999999999645, 186.3256874041514948 ) ) ;
#71008=CARTESIAN_POINT ( 'NONE',  ( 28.11522601640037777, -57.67959711521903898, 44.33298562067892590 ) ) ;
#71017=CARTESIAN_POINT ( 'NONE',  ( 0.9578037757747321912, -15.40093288537109295, -35.22475077049247005 ) ) ;
#71023=CARTESIAN_POINT ( 'NONE',  ( -15.60285226952893822, -35.99487615058492906, 30.06479306797814743 ) ) ;
#71024=CARTESIAN_POINT ( 'NONE',  ( -102.0018013446515681, -60.00000000000001421, 127.8252749486858448 ) ) ;
#71028=COLOUR_RGB ( '', 0.40784314, 0.44705882, 0.49803922) ;
#71033=CARTESIAN_POINT ( 'NONE',  ( 66.39989526219071081, -59.99999999999998579, 124.0569035276217136 ) ) ;
#71039=CARTESIAN_POINT ( 'NONE',  ( 41.09910603910869042, -35.58342714853350230, 38.74414947838628365 ) ) ;
#71054=CARTESIAN_POINT ( 'NONE',  ( -101.4188503834094774, -59.99999999999139533, 203.9653219413819727 ) ) ;
#71056=CARTESIAN_POINT ( 'NONE',  ( 84.85800574570012600, -59.99999999999998579, -27.63310012610692823 ) ) ;
#71059=CARTESIAN_POINT ( 'NONE',  ( -96.14371828217340976, -60.00000000000000711, 39.43406270914149303 ) ) ;
#71060=CARTESIAN_POINT ( 'NONE',  ( 11.36735780710606392, -42.95370621829134450, 31.07683940958586888 ) ) ;
#71063=CARTESIAN_POINT ( 'NONE',  ( -48.40688107547297392, -36.06281915256160886, 47.15551163693150727 ) ) ;
#71073=CARTESIAN_POINT ( 'NONE',  ( 82.77223023685738212, -30.00000000002606271, 195.2202738952123582 ) ) ;
#71077=CARTESIAN_POINT ( 'NONE',  ( 98.38941629421586299, -30.00000000000000711, 190.0212863901236346 ) ) ;
#71090=ORIENTED_EDGE ( 'NONE', *, *, #65205, .T. ) ;
#71094=CARTESIAN_POINT ( 'NONE',  ( 87.97245158076984239, -38.55863593782331122, 199.9496566671098776 ) ) ;
#71096=CARTESIAN_POINT ( 'NONE',  ( 82.43075110611209766, -37.85957831011834429, 10.65854084798032986 ) ) ;
#71116=CARTESIAN_POINT ( 'NONE',  ( -35.32368133270053079, -35.72353222546922780, 44.44765049649346622 ) ) ;
#71119=CARTESIAN_POINT ( 'NONE',  ( 84.07839313513588309, -57.41987416485399365, 190.7915766117616556 ) ) ;
#71123=CARTESIAN_POINT ( 'NONE',  ( 95.57197061297391372, -57.67170093465097125, 37.80234372629790585 ) ) ;
#71131=CARTESIAN_POINT ( 'NONE',  ( 49.51030389795987219, -29.59163284775611302, 45.84054346467660679 ) ) ;
#71140=CARTESIAN_POINT ( 'NONE',  ( -82.71960126402635183, -38.00000000000000711, 3.558503230223199143 ) ) ;
#71149=CARTESIAN_POINT ( 'NONE',  ( -1.605081721621855584, -60.22810981620649784, -36.92765560991468732 ) ) ;
#71155=CARTESIAN_POINT ( 'NONE',  ( -92.56479762031210612, -60.00000000000000711, -2.220767633544127762 ) ) ;
#71162=CARTESIAN_POINT ( 'NONE',  ( -81.41430060195118301, -49.93828882406421599, 171.6694044221305830 ) ) ;
#71164=CARTESIAN_POINT ( 'NONE',  ( -16.46930219882042934, 0.000000000000000000, -4.418206560268989058 ) ) ;
#71175=CARTESIAN_POINT ( 'NONE',  ( -100.1205506810183152, -57.62746089781320791, 203.8952656938035091 ) ) ;
#71180=CARTESIAN_POINT ( 'NONE',  ( 87.61417445234833679, -14.21045842199449716, -10.69449287335903342 ) ) ;
#71182=CARTESIAN_POINT ( 'NONE',  ( -70.38749560794603610, -14.21045842199435860, 117.5518806561683078 ) ) ;
#71184=CARTESIAN_POINT ( 'NONE',  ( -55.26730358396395815, -39.50059391399134512, 60.87172762752346955 ) ) ;
#71188=CARTESIAN_POINT ( 'NONE',  ( -101.0485842489931940, -52.73349511294460967, 193.3212840139921127 ) ) ;
#71192=FACE_OUTER_BOUND ( 'NONE', #86654, .T. ) ;
#71197=CARTESIAN_POINT ( 'NONE',  ( 66.18720266095957072, -30.00000000000000000, 83.66546625751099953 ) ) ;
#71203=CARTESIAN_POINT ( 'NONE',  ( -27.89559576334529467, -53.39171285254504795, 34.87437243777274176 ) ) ;
#71206=CARTESIAN_POINT ( 'NONE',  ( 47.77420556706847066, -22.22698538295941262, 42.11322263999190341 ) ) ;
#71209=ADVANCED_FACE ( 'NONE', ( #91372 ), #27740, .F. ) ;
#71210=CARTESIAN_POINT ( 'NONE',  ( -110.8389214075725988, -38.35618062369555759, 166.4464234148499031 ) ) ;
#71212=CARTESIAN_POINT ( 'NONE',  ( 91.34032523538760984, -38.39886032400823268, -9.955676214931663992 ) ) ;
#71221=CARTESIAN_POINT ( 'NONE',  ( 92.68958050770518753, -60.00000000000001421, 202.4387916161230692 ) ) ;
#71226=CARTESIAN_POINT ( 'NONE',  ( 58.23846566418407633, -53.38279051962974364, 74.09562710507131555 ) ) ;
#71231=CARTESIAN_POINT ( 'NONE',  ( -104.2759569493203458, -38.40773243213855892, 198.1659664498641860 ) ) ;
#71241=CARTESIAN_POINT ( 'NONE',  ( 82.39478451168702122, -46.46901798477522050, 175.1825464717589398 ) ) ;
#71256=CARTESIAN_POINT ( 'NONE',  ( -79.94288123161219062, -30.00000000000000000, -13.90860458798707633 ) ) ;
#71260=CARTESIAN_POINT ( 'NONE',  ( -0.2244703346847722603, -18.03092902646604756, 35.00512146036130900 ) ) ;
#71262=EDGE_CURVE ( 'NONE', #37867, #25171, #63649, .T. ) ;
#71278=VERTEX_POINT ( 'NONE', #94019 ) ;
#71283=CARTESIAN_POINT ( 'NONE',  ( -110.1690392527196565, -60.00000000000001421, 144.8104088435783012 ) ) ;
#71289=CARTESIAN_POINT ( 'NONE',  ( -85.21113657438505129, -32.24608462764727079, 179.1484755246043505 ) ) ;
#71298=CARTESIAN_POINT ( 'NONE',  ( -86.28712359338396709, -52.70879326618576499, 35.16763926569588961 ) ) ;
#71303=CARTESIAN_POINT ( 'NONE',  ( 106.4941418293696387, -60.00000000000010658, 201.1229827202191984 ) ) ;
#71305=CARTESIAN_POINT ( 'NONE',  ( -104.4271118349969498, -14.21045842199436926, 141.4138186051453090 ) ) ;
#71306=CARTESIAN_POINT ( 'NONE',  ( -65.12520086583974432, -53.39111017842260765, 93.95656328253419076 ) ) ;
#71309=CARTESIAN_POINT ( 'NONE',  ( 91.24502176991838098, -60.00000000000494538, 204.7032358451281482 ) ) ;
#71320=CARTESIAN_POINT ( 'NONE',  ( -91.98242746288742921, -60.00000000000001421, -14.02575605693079375 ) ) ;
#71334=CARTESIAN_POINT ( 'NONE',  ( 33.27692946845811406, -36.02636644479590444, 33.82109768178349896 ) ) ;
#71335=CARTESIAN_POINT ( 'NONE',  ( -8.569529079657698389, -1.734723475976807094E-15, -14.86825985027703290 ) ) ;
#71336=VERTEX_POINT ( 'NONE', #76227 ) ;
#71347=CARTESIAN_POINT ( 'NONE',  ( 97.98312614813336552, -59.99999999999999289, 68.82170008167646813 ) ) ;
#71352=CARTESIAN_POINT ( 'NONE',  ( -82.18314241283663080, -30.00000000000575184, -23.35998342603787137 ) ) ;
#71368=CARTESIAN_POINT ( 'NONE',  ( 81.82597684722991005, -22.15511354699349411, 138.5255780189167751 ) ) ;
#71375=CARTESIAN_POINT ( 'NONE',  ( -49.73192663144240555, -57.67846088945594829, 76.49129250627629517 ) ) ;
#71383=CARTESIAN_POINT ( 'NONE',  ( -34.94743244184756037, -24.04089725522681320, 33.47236368172110588 ) ) ;
#71385=CARTESIAN_POINT ( 'NONE',  ( 0.8333333341588072818, -30.00000000000000355, -31.89470715492279140 ) ) ;
#71391=CARTESIAN_POINT ( 'NONE',  ( 0.000000000000000000, -30.00000000000000000, -8.000000000000000000 ) ) ;
#71396=CARTESIAN_POINT ( 'NONE',  ( -58.50943875393205929, -29.71222703585479863, -33.25288336754142904 ) ) ;
#71397=CARTESIAN_POINT ( 'NONE',  ( -66.67257040218905217, -30.00000000000000000, 85.09162466317252438 ) ) ;
#71404=CARTESIAN_POINT ( 'NONE',  ( 91.20819292822160662, -57.61347045221073415, 204.2086795226624076 ) ) ;
#71409=CARTESIAN_POINT ( 'NONE',  ( -74.32166848140413151, -59.99999999999999289, 175.4192060893726364 ) ) ;
#71413=CARTESIAN_POINT ( 'NONE',  ( -85.54972613292714811, -42.91353616863772658, 187.2157232925927133 ) ) ;
#71424=CARTESIAN_POINT ( 'NONE',  ( -25.22241582816893413, -4.285714285714287364, -3.301606509427108982 ) ) ;
#71427=CARTESIAN_POINT ( 'NONE',  ( 91.01458086108723933, -60.00000000000020606, -21.64996939806972520 ) ) ;
#71428=CARTESIAN_POINT ( 'NONE',  ( -80.72224628703636995, -25.62261740639140584, 135.9075979048819249 ) ) ;
#71431=CARTESIAN_POINT ( 'NONE',  ( 39.73542184579525838, -14.21045842199450782, 43.02758494329003014 ) ) ;
#71433=CARTESIAN_POINT ( 'NONE',  ( 102.9288018374504077, -57.63504169932654264, 202.8890457415012634 ) ) ;
#71444=CARTESIAN_POINT ( 'NONE',  ( -102.6920302767066318, -37.82049116696702384, 167.9539667898588959 ) ) ;
#71457=CARTESIAN_POINT ( 'NONE',  ( -17.10644827616429708, -60.00000000000001421, 42.25319189086976479 ) ) ;
#71458=CARTESIAN_POINT ( 'NONE',  ( 27.25886883392396953, -53.38735016083550988, 34.68802301658027432 ) ) ;
#71471=CARTESIAN_POINT ( 'NONE',  ( 90.17098323280204397, -29.99999999999950617, 190.0045134580199999 ) ) ;
#71473=CARTESIAN_POINT ( 'NONE',  ( -81.98196232622828461, -37.99999999999996447, -13.86369433938586582 ) ) ;
#71496=CARTESIAN_POINT ( 'NONE',  ( -81.86715632375494067, -59.99999999999992895, 186.9285674509132207 ) ) ;
#71497=CARTESIAN_POINT ( 'NONE',  ( 63.65739376113187120, -29.05497423747783259, 76.99861434842904373 ) ) ;
#71501=CARTESIAN_POINT ( 'NONE',  ( -72.67455277886013221, -38.32345021738819923, -30.15491327014585821 ) ) ;
#71507=CARTESIAN_POINT ( 'NONE',  ( -2.275180367705706086, -60.00000000000001421, -36.87650252253413186 ) ) ;
#71515=CARTESIAN_POINT ( 'NONE',  ( 85.88596471057849158, -57.44479720796045541, 193.0254570140299961 ) ) ;
#71523=CARTESIAN_POINT ( 'NONE',  ( 37.16605791060757724, -60.00000000000000000, 48.55182899660729845 ) ) ;
#71524=CARTESIAN_POINT ( 'NONE',  ( -99.16645489262339197, -30.00000000000001066, 146.3472804026664278 ) ) ;
#71527=CARTESIAN_POINT ( 'NONE',  ( 45.01508081842917619, -57.68314626598579054, 65.19425546680545835 ) ) ;
#71534=CARTESIAN_POINT ( 'NONE',  ( -0.2874569003302878678, -60.00000000000002842, 39.63907912791243859 ) ) ;
#71540=CARTESIAN_POINT ( 'NONE',  ( -13.52097269965777571, -42.95778303387159269, 31.13366671246901163 ) ) ;
#71541=VECTOR ( 'NONE', #100448, 1000.000000000000000 ) ;
#71542=CARTESIAN_POINT ( 'NONE',  ( -105.7334699303116849, -59.99999999999997868, 184.1712277148149610 ) ) ;
#71545=VERTEX_POINT ( 'NONE', #5011 ) ;
#71550=CARTESIAN_POINT ( 'NONE',  ( 73.61179401698619529, -60.00000000000000711, 168.2994255929738756 ) ) ;
#71556=CARTESIAN_POINT ( 'NONE',  ( 39.49823726628140719, -30.00000000000007461, 47.07845324830893929 ) ) ;
#71570=CARTESIAN_POINT ( 'NONE',  ( -104.4110070364954623, -59.99999999999994316, 202.5758496764194945 ) ) ;
#71572=CARTESIAN_POINT ( 'NONE',  ( 94.45509314101606435, -59.99999999999993605, 202.5749630227759326 ) ) ;
#71576=CARTESIAN_POINT ( 'NONE',  ( -97.37795077744138439, -14.21045842199441722, 96.97852642953840530 ) ) ;
#71577=CARTESIAN_POINT ( 'NONE',  ( 12.39938652094127036, -39.47271121152019902, 30.52336634656487035 ) ) ;
#71579=CARTESIAN_POINT ( 'NONE',  ( -46.25826378782726778, -32.61579050286022863, 43.25093016562399839 ) ) ;
#71592=CARTESIAN_POINT ( 'NONE',  ( 103.7182182521570013, -29.99999999999979750, 196.8382105665609743 ) ) ;
#71598=CARTESIAN_POINT ( 'NONE',  ( 99.09559260544375547, -29.99999999999999645, 188.5993032172692381 ) ) ;
#71613=CARTESIAN_POINT ( 'NONE',  ( 97.81756293420689019, -38.47728072526631138, 201.0337594294088888 ) ) ;
#71615=CARTESIAN_POINT ( 'NONE',  ( 86.74466300583080169, -60.15137282943332764, -0.9961456128505913332 ) ) ;
#71616=CARTESIAN_POINT ( 'NONE',  ( 53.26377392596668159, -38.00000000000000000, 56.03167726914934121 ) ) ;
#71632=CARTESIAN_POINT ( 'NONE',  ( 7.451599765851676160, -15.61856177235541487, 34.59380785664056646 ) ) ;
#71635=CARTESIAN_POINT ( 'NONE',  ( 83.62748053872782350, -57.37324410372879413, 189.9579150913779699 ) ) ;
#71640=CARTESIAN_POINT ( 'NONE',  ( 95.57056055828975616, -57.67170150759548619, 37.78996498690358408 ) ) ;
#71644=EDGE_CURVE ( 'NONE', #34393, #89859, #80940, .T. ) ;
#71647=CARTESIAN_POINT ( 'NONE',  ( 4.761285474643048410, -18.53359912731012216, 35.08063092172267261 ) ) ;
#71659=VECTOR ( 'NONE', #84179, 1000.000000000000000 ) ;
#71660=CARTESIAN_POINT ( 'NONE',  ( -100.9479196034361905, -37.99999999999996447, 146.8164339967658236 ) ) ;
#71666=CARTESIAN_POINT ( 'NONE',  ( -58.43662215619989553, -47.40888653656140406, -27.93294337827289908 ) ) ;
#71674=CARTESIAN_POINT ( 'NONE',  ( -92.35218344474584740, -59.99999999999998579, 0.8031026304253716663 ) ) ;
#71675=ORIENTED_EDGE ( 'NONE', *, *, #94307, .F. ) ;
#71677=CARTESIAN_POINT ( 'NONE',  ( 97.42904766945321171, -60.35211980451472158, 196.6984442979972982 ) ) ;
#71681=CARTESIAN_POINT ( 'NONE',  ( -84.05660459919248240, -22.13859885683705286, 152.7253703305752879 ) ) ;
#71692=CARTESIAN_POINT ( 'NONE',  ( -109.9801870187163644, -57.66844046886203756, 196.1568551196091903 ) ) ;
#71697=CARTESIAN_POINT ( 'NONE',  ( 88.92118937161633596, -29.99999999999996092, -15.18954496189254755 ) ) ;
#71698=CARTESIAN_POINT ( 'NONE',  ( -48.02140427201592132, -30.00000000000008527, 60.50294052774201958 ) ) ;
#71699=CARTESIAN_POINT ( 'NONE',  ( -52.04820441236028472, -49.90957493855300697, 58.16687430699108319 ) ) ;
#71703=CARTESIAN_POINT ( 'NONE',  ( -102.2352430864713284, -60.20054222074153927, 193.9234359043284428 ) ) ;
#71708=CARTESIAN_POINT ( 'NONE',  ( 91.32429202933356294, -38.35421070491497630, 28.90131162905761286 ) ) ;
#71723=CARTESIAN_POINT ( 'NONE',  ( 50.96143459282708221, -32.58239369279106512, 49.99714469605078193 ) ) ;
#71725=DIRECTION ( 'NONE',  ( -0.000000000000000000, -1.000000000000000000, -0.000000000000000000 ) ) ;
#71727=CARTESIAN_POINT ( 'NONE',  ( -110.7820348957689305, -38.35618030932103295, 179.6175950015601757 ) ) ;
#71729=CARTESIAN_POINT ( 'NONE',  ( 89.37870489931546558, -38.38696938715336415, -17.35345262173043679 ) ) ;
#71734=CARTESIAN_POINT ( 'NONE',  ( 97.56555718646720265, -60.15121296667719264, 100.7618488147239333 ) ) ;
#71740=CARTESIAN_POINT ( 'NONE',  ( 90.23526155271706273, -60.00000000000000000, 202.0276669837681709 ) ) ;
#71743=AXIS2_PLACEMENT_3D ( 'NONE', #66514, #56816, #25569 ) ;
#71746=CARTESIAN_POINT ( 'NONE',  ( 59.20395090875183541, -36.01664205692539866, 68.56248700397097195 ) ) ;
#71752=CARTESIAN_POINT ( 'NONE',  ( -105.3108324701758107, -38.38841466978784212, 197.1710578805450211 ) ) ;
#71761=CARTESIAN_POINT ( 'NONE',  ( 85.73810161015232723, -21.86527338768217632, 169.1334664433469754 ) ) ;
#71775=CARTESIAN_POINT ( 'NONE',  ( -81.74144244633359335, -29.99999999999999645, 31.24147803549975677 ) ) ;
#71805=CARTESIAN_POINT ( 'NONE',  ( -111.1441913338302356, -59.99999999999999289, 153.5661079110527680 ) ) ;
#71816=CARTESIAN_POINT ( 'NONE',  ( -83.24037337117431434, -42.98078370665466963, 177.1168375766181384 ) ) ;
#71824=CARTESIAN_POINT ( 'NONE',  ( -83.68625982447714762, -45.26552441130044713, 14.69813845894242199 ) ) ;
#71829=CARTESIAN_POINT ( 'NONE',  ( 80.78816237064734196, -29.99999999999997513, 192.9482874834278903 ) ) ;
#71830=CARTESIAN_POINT ( 'NONE',  ( -93.27866288726950472, -14.21045842199433373, 72.78127944122930160 ) ) ;
#71831=CARTESIAN_POINT ( 'NONE',  ( -62.59898750523465338, -56.86926829012708851, 88.13743897392122051 ) ) ;
#71834=CARTESIAN_POINT ( 'NONE',  ( 47.96672227968453939, -59.99999999998527045, 73.04161892766875042 ) ) ;
#71836=CARTESIAN_POINT ( 'NONE',  ( 2.027295390931008967, -46.43466668287893384, 31.62625868155275555 ) ) ;
#71842=EDGE_LOOP ( 'NONE', ( #84587, #55968, #30812, #19776, #77957 ) ) ;
#71845=CARTESIAN_POINT ( 'NONE',  ( -93.99879809186631974, -60.00000000000000000, 41.63443083181508797 ) ) ;
#71858=CARTESIAN_POINT ( 'NONE',  ( -36.59723990820980788, -53.36088228589063931, 39.00306241562584830 ) ) ;
#71861=CARTESIAN_POINT ( 'NONE',  ( 36.40464493058440354, -29.12080053541245661, 34.06312112947962589 ) ) ;
#71862=CARTESIAN_POINT ( 'NONE',  ( -17.01589776168603407, -1.734723475976807094E-15, -2.227375807157456755 ) ) ;
#71868=CARTESIAN_POINT ( 'NONE',  ( -67.51048420570765529, -38.33477690727864484, 123.4165462485304658 ) ) ;
#71880=CARTESIAN_POINT ( 'NONE',  ( 95.43964957209735189, -60.00000000000000000, 52.17412195945332343 ) ) ;
#71887=CARTESIAN_POINT ( 'NONE',  ( -77.54319449862920521, -29.99999999999670308, -26.30707014989112125 ) ) ;
#71907=CARTESIAN_POINT ( 'NONE',  ( 80.77733221968003363, -42.96683419437847107, 155.3669859002530700 ) ) ;
#71928=CARTESIAN_POINT ( 'NONE',  ( -12.33464901170365380, -14.37923961157706998, 31.77351814907940053 ) ) ;
#71930=DIRECTION ( 'NONE',  ( 0.000000000000000000, 0.000000000000000000, -1.000000000000000000 ) ) ;
#71941=CARTESIAN_POINT ( 'NONE',  ( -81.07140313541336241, -30.00000000000001421, 140.4064320514307553 ) ) ;
#71946=CARTESIAN_POINT ( 'NONE',  ( 106.7290742229372853, -57.65299249569456208, 200.3188922580204689 ) ) ;
#71947=CARTESIAN_POINT ( 'NONE',  ( 60.63806777930422243, -34.58949756339826820, -25.09002054893269573 ) ) ;
#71949=CARTESIAN_POINT ( 'NONE',  ( -80.00000000000000000, -60.00000000000000000, -21.09707704303352926 ) ) ;
#71952=CARTESIAN_POINT ( 'NONE',  ( -73.64776945840979749, -60.00000000000000711, 168.6562425123320565 ) ) ;
#71958=CARTESIAN_POINT ( 'NONE',  ( -84.39490293580904279, -57.45156777692785965, 191.2983715192742409 ) ) ;
#71972=CARTESIAN_POINT ( 'NONE',  ( 17.78317311657530553, -8.673617379884035472E-16, -13.66642973271117256 ) ) ;
#71974=CARTESIAN_POINT ( 'NONE',  ( 65.67877680238373728, -29.99999999999995026, -31.25179767064105363 ) ) ;
#71975=CARTESIAN_POINT ( 'NONE',  ( -81.42972324512007276, -18.68455707043344205, 133.0837277777090435 ) ) ;
#71977=CARTESIAN_POINT ( 'NONE',  ( 17.10696384799877379, -59.99999999999999289, 42.25337809451749393 ) ) ;
#71978=CARTESIAN_POINT ( 'NONE',  ( 72.25192046840727755, -57.67049155165763352, 174.5922148356693810 ) ) ;
#71987=CARTESIAN_POINT ( 'NONE',  ( -101.8255872164643989, -52.71004081795416596, 134.8513848411543279 ) ) ;
#71998=CARTESIAN_POINT ( 'NONE',  ( -34.32536616635837845, -30.00000000000003553, 42.48815186199111338 ) ) ;
#71999=CARTESIAN_POINT ( 'NONE',  ( 28.67944596121853706, -56.86006578928314070, 35.73029098294846051 ) ) ;
#72007=DIRECTION ( 'NONE',  ( 0.000000000000000000, -0.000000000000000000, -1.000000000000000000 ) ) ;
#72014=CARTESIAN_POINT ( 'NONE',  ( 48.62243493482748846, -60.00000000000000711, -38.17079728251586346 ) ) ;
#72015=CARTESIAN_POINT ( 'NONE',  ( 88.69399320309210566, -29.99999999999992539, 188.2041074686423485 ) ) ;
#72037=ORIENTED_EDGE ( 'NONE', *, *, #13511, .F. ) ;
#72042=CARTESIAN_POINT ( 'NONE',  ( 63.30499805623622223, -29.05601916271744756, 76.03110060700105066 ) ) ;
#72057=CARTESIAN_POINT ( 'NONE',  ( 86.95935682309162473, -39.09230861363683118, 189.0019964014885261 ) ) ;
#72064=CARTESIAN_POINT ( 'NONE',  ( 30.54863829050838220, -60.00000000000000000, 43.31763207389616355 ) ) ;
#72065=CARTESIAN_POINT ( 'NONE',  ( -100.3740574807695651, -30.00000000000000355, 157.7342760147397769 ) ) ;
#72066=DIRECTION ( 'NONE',  ( 0.000000000000000000, 0.000000000000000000, 1.000000000000000000 ) ) ;
#72067=CARTESIAN_POINT ( 'NONE',  ( 35.88008981787920959, -57.69592402444057200, 50.07942547625698637 ) ) ;
#72069=FACE_OUTER_BOUND ( 'NONE', #84620, .T. ) ;
#72075=CARTESIAN_POINT ( 'NONE',  ( -20.85295009280099876, -60.00000000000000000, 40.33826634902553110 ) ) ;
#72079=CARTESIAN_POINT ( 'NONE',  ( -86.36538439990067673, -61.02622103470842774, 194.5654814187428201 ) ) ;
#72082=CARTESIAN_POINT ( 'NONE',  ( -12.62263043180945665, -56.88413384736368528, 33.43217295346193652 ) ) ;
#72093=CARTESIAN_POINT ( 'NONE',  ( 69.82668593885752273, -59.99999999999998579, 140.4683949244069368 ) ) ;
#72099=CARTESIAN_POINT ( 'NONE',  ( 34.32456002071940304, -30.00000000000004263, 42.48759634994703305 ) ) ;
#72113=CARTESIAN_POINT ( 'NONE',  ( -109.9238538444930526, -59.99999999999752021, 197.0382354099203610 ) ) ;
#72115=CARTESIAN_POINT ( 'NONE',  ( 83.40983118009236819, -59.99999999999992895, 199.1200332089420044 ) ) ;
#72119=CARTESIAN_POINT ( 'NONE',  ( -106.4002951517535536, -14.21045842199431242, 159.7122570458138284 ) ) ;
#72120=CARTESIAN_POINT ( 'NONE',  ( 12.53354992101991883, -49.91574432760546642, 32.26800626715709086 ) ) ;
#72121=CARTESIAN_POINT ( 'NONE',  ( 95.03805679281244068, -38.00000000000000000, 107.7969437180587136 ) ) ;
#72123=CARTESIAN_POINT ( 'NONE',  ( -44.27417758264619607, -56.80246321600215964, 47.31014526494450934 ) ) ;
#72136=CARTESIAN_POINT ( 'NONE',  ( 107.2611508641872859, -29.99999999998129852, 190.9996382533202279 ) ) ;
#72139=CARTESIAN_POINT ( 'NONE',  ( 88.61328692016215314, -29.99999999999999289, 80.34149805594043414 ) ) ;
#72143=B_SPLINE_CURVE_WITH_KNOTS ( 'NONE', 3,
 ( #55988, #55468, #15018, #80281, #87343, #88928, #70622, #5864, #104031, #94915, #47387, #47910, #21052, #37757, #72209, #70086, #31252, #71140, #53889, #63607, #102990, #103511, #30172, #6392, #29664, #54398, #38789, #86819, #12891, #45817, #96492, #63063, #95962, #78688, #13420, #46344, #79233, #71660, #105110, #104565, #5360, #22087, #54942, #87869, #13954, #79759, #30720, #88402, #89463, #24741, #15554, #7992, #40363, #89982, #396, #40901, #99664, #48966, #106686, #33363, #98595, #50561, #32833, #66775, #32301, #25280, #81338, #17174 ),
 .UNSPECIFIED., .F., .F.,
 ( 4, 2, 2, 2, 2, 2, 2, 2, 2, 2, 2, 2, 2, 2, 2, 2, 2, 2, 2, 2, 2, 2, 2, 2, 2, 2, 2, 2, 2, 2, 2, 2, 2, 4 ),
 ( 0.01355025249921910056, 0.01436585972314286322, 0.01518146694706662414, 0.01681268139491414251, 0.01844389584276166089, 0.02007511029060918273, 0.02333753918630421947, 0.02659996808199925622, 0.02986239697769429297, 0.03312482587338932971, 0.03964968366477939626, 0.05269939924755953631, 0.06574911483033968329, 0.07879883041311983027, 0.09184854599589996338, 0.1179479771614602573, 0.1440474083270205652, 0.1570971239098006844, 0.1701468394925808314, 0.1831965550753610061, 0.1897214128667510658, 0.1962462706581411254, 0.2027711284495312127, 0.2092959862409213001, 0.2125584151366162744, 0.2158208440323112765, 0.2174520584801587497, 0.2182676657040824864, 0.2190832729280062230, 0.2194910765399680774, 0.2198988801519299319, 0.2207144873758536130, 0.2215300945997772664, 0.2223457018237009197 ),
 .UNSPECIFIED. ) ;
#72157=CARTESIAN_POINT ( 'NONE',  ( 80.09828699751943759, -38.78935091380522238, 193.1656444472805845 ) ) ;
#72159=CARTESIAN_POINT ( 'NONE',  ( 86.69934304271014014, -60.14804486455665256, -0.3912972893063921820 ) ) ;
#72160=CARTESIAN_POINT ( 'NONE',  ( 85.13988909840620067, -38.00000000000004974, 183.5158871499416477 ) ) ;
#72186=CARTESIAN_POINT ( 'NONE',  ( 84.13229308240822490, -50.16608149856336496, 187.2769468085622862 ) ) ;
#72191=CARTESIAN_POINT ( 'NONE',  ( 95.67875834985767369, -57.67165897752772707, 38.73083894233180757 ) ) ;
#72204=CARTESIAN_POINT ( 'NONE',  ( -17.01158861293394509, -25.30155750122309044, -30.48162244162692858 ) ) ;
#72209=CARTESIAN_POINT ( 'NONE',  ( -83.09784762163468486, -38.00000000000002842, -1.930924322092125278 ) ) ;
#72213=CARTESIAN_POINT ( 'NONE',  ( -17.03013798833078241, -17.73699097705837247, -34.10471246031885073 ) ) ;
#72216=CARTESIAN_POINT ( 'NONE',  ( -31.56605086575277852, -34.58954922973804713, -30.69102488358296199 ) ) ;
#72224=CARTESIAN_POINT ( 'NONE',  ( -92.63211006453688867, -59.99999999999997158, -9.950981327657569153 ) ) ;
#72228=CARTESIAN_POINT ( 'NONE',  ( 96.88789730132712918, -45.26984529354276532, 194.0225460405672209 ) ) ;
#72230=CARTESIAN_POINT ( 'NONE',  ( -85.23051947703226006, -18.61638337422625966, 157.3767952312193472 ) ) ;
#72232=VERTEX_POINT ( 'NONE', #58486 ) ;
#72240=CARTESIAN_POINT ( 'NONE',  ( -74.02244645645996002, -57.61166141858229395, 187.2311674206319765 ) ) ;
#72246=CARTESIAN_POINT ( 'NONE',  ( 24.89419722466787022, -30.00000000000004974, -38.80375014483585261 ) ) ;
#72247=CARTESIAN_POINT ( 'NONE',  ( -54.44990204170284898, -30.00000000000008882, 75.82925260777241760 ) ) ;
#72248=CARTESIAN_POINT ( 'NONE',  ( -53.51057452807305026, -22.16812215901368432, 50.70531185769669236 ) ) ;
#72253=CARTESIAN_POINT ( 'NONE',  ( -102.0339308600683097, -60.20990888865522095, 194.1617984564381629 ) ) ;
#72258=CARTESIAN_POINT ( 'NONE',  ( 110.0576603816093950, -38.35596508152210049, 154.9619461380562200 ) ) ;
#72262=CARTESIAN_POINT ( 'NONE',  ( 84.26804285766414182, -30.00000000000000000, 163.4126049098225621 ) ) ;
#72270=CARTESIAN_POINT ( 'NONE',  ( 49.29183012222615901, -18.74727630053224914, 42.99191983216383761 ) ) ;
#72275=CARTESIAN_POINT ( 'NONE',  ( -110.3499448355333215, -38.35608688738442140, 183.6271486024410251 ) ) ;
#72277=CARTESIAN_POINT ( 'NONE',  ( 90.74655439557324144, -38.34261265473484315, 6.503296633511228997 ) ) ;
#72281=CARTESIAN_POINT ( 'NONE',  ( 101.2281462999901152, -37.84858859627455274, 149.3017034182498435 ) ) ;
#72285=CARTESIAN_POINT ( 'NONE',  ( 93.22046886666203136, -59.99999999999999289, 202.4896487005214851 ) ) ;
#72288=CARTESIAN_POINT ( 'NONE',  ( 55.90058340703467366, -53.37925634193300795, 68.14343119493420886 ) ) ;
#72294=CARTESIAN_POINT ( 'NONE',  ( -110.3148016707792465, -38.35598278249073445, 183.9770048744294115 ) ) ;
#72306=CARTESIAN_POINT ( 'NONE',  ( 83.24093056157693127, -42.97671957674801035, 177.1152172873732695 ) ) ;
#72349=CARTESIAN_POINT ( 'NONE',  ( -111.2112538145483143, -59.99999999999999289, 154.2509436529097115 ) ) ;
#72354=CARTESIAN_POINT ( 'NONE',  ( -85.70070447472639330, -21.88688739919286164, 168.6176033816253153 ) ) ;
#72365=CARTESIAN_POINT ( 'NONE',  ( 89.23375057675741573, -59.99999999999977973, 204.3679297810271862 ) ) ;
#72367=CARTESIAN_POINT ( 'NONE',  ( -100.7780794135568954, -14.21045842199427156, 117.1455274902871366 ) ) ;
#72368=CARTESIAN_POINT ( 'NONE',  ( -60.90366851421529759, -56.86960161935190428, 83.15536174215863241 ) ) ;
#72371=CARTESIAN_POINT ( 'NONE',  ( 72.84044669408135064, -60.00000000000491696, 183.1815887110867607 ) ) ;
#72373=CARTESIAN_POINT ( 'NONE',  ( 3.030313384945461763, -39.47248979064079322, 30.46354856792267896 ) ) ;
#72381=CARTESIAN_POINT ( 'NONE',  ( -87.16287115447597955, -59.99999999999998579, 201.0813553807005576 ) ) ;
#72394=CARTESIAN_POINT ( 'NONE',  ( -32.43755732417693594, -42.96442599306529075, 34.72761510847016098 ) ) ;
#72397=CARTESIAN_POINT ( 'NONE',  ( 41.90357024077690085, -32.61324066414001521, 38.71707398534343980 ) ) ;
#72398=CARTESIAN_POINT ( 'NONE',  ( 13.60704923275002010, -1.734723475976807094E-15, -10.45706415777842935 ) ) ;
#72404=CARTESIAN_POINT ( 'NONE',  ( -55.77509681992000878, -38.34453011954626334, 83.68376476757157434 ) ) ;
#72415=CARTESIAN_POINT ( 'NONE',  ( 94.25213324963540629, -59.99999999999998579, 43.35550940579889101 ) ) ;
#72421=CARTESIAN_POINT ( 'NONE',  ( -89.88336266018133358, -29.99999999998671640, -1.794731794580948003 ) ) ;
#72436=CARTESIAN_POINT ( 'NONE',  ( 81.98252987595192565, -32.55966453745716649, 150.9950225902835825 ) ) ;
#72444=CARTESIAN_POINT ( 'NONE',  ( -29.62390339563712160, -57.68322450639401211, 45.06481242858825453 ) ) ;
#72454=CARTESIAN_POINT ( 'NONE',  ( -24.30786747476509291, -18.98229748144842688, 31.52624602878413640 ) ) ;
#72465=CARTESIAN_POINT ( 'NONE',  ( -76.12537862032620239, -38.35598417008156957, -28.58435412235104423 ) ) ;
#72466=CARTESIAN_POINT ( 'NONE',  ( -59.15011143018023887, -30.00000000000000355, 64.89418600812079774 ) ) ;
#72472=CARTESIAN_POINT ( 'NONE',  ( 101.7590372865866755, -57.63143884806530792, 203.3630881935354182 ) ) ;
#72473=CIRCLE ( 'NONE', #5349, 18.07003550757956845 ) ;
#72478=CARTESIAN_POINT ( 'NONE',  ( -74.80865327367102680, -59.99999999999999289, 179.7763745376072677 ) ) ;
#72481=CARTESIAN_POINT ( 'NONE',  ( -84.23794301257443351, -53.80601704703899912, 189.3816763263162102 ) ) ;
#72488=CARTESIAN_POINT ( 'NONE',  ( -85.09719550378922293, -60.19746287038491062, -15.90597616068271591 ) ) ;
#72498=CARTESIAN_POINT ( 'NONE',  ( 84.06490631893382215, -29.99999999999999645, -21.85721834217820714 ) ) ;
#72500=CARTESIAN_POINT ( 'NONE',  ( -73.37834811148371728, -60.32685699175659266, 129.0820052624678169 ) ) ;
#72502=( NAMED_UNIT ( * ) PLANE_ANGLE_UNIT ( ) SI_UNIT ( $, .RADIAN. ) );
#72504=CARTESIAN_POINT ( 'NONE',  ( 92.08262379307400636, -57.61612071740184859, 204.3519813252348456 ) ) ;
#72512=CARTESIAN_POINT ( 'NONE',  ( -105.1034263385044198, -52.71031197673006830, 165.8127315669447910 ) ) ;
#72524=CARTESIAN_POINT ( 'NONE',  ( 32.52394736240458428, -56.84213397606195883, 37.29594050141937345 ) ) ;
#72536=CARTESIAN_POINT ( 'NONE',  ( 36.20485447879452323, -59.99999999999999289, -40.16702231068630624 ) ) ;
#72537=CARTESIAN_POINT ( 'NONE',  ( 67.45855122657930281, -29.99999999999999289, 87.38540783980748472 ) ) ;
#72564=CARTESIAN_POINT ( 'NONE',  ( -34.63715291467956092, -59.99999999999998579, 39.00976837571851519 ) ) ;
#72565=CARTESIAN_POINT ( 'NONE',  ( 66.70725985424147098, -29.05557763954682926, 85.69813299201692303 ) ) ;
#72580=CARTESIAN_POINT ( 'NONE',  ( 86.21108316312455599, -53.80016052557698458, 192.1608066663390844 ) ) ;
#72586=CARTESIAN_POINT ( 'NONE',  ( 17.08697247429566346, -60.00000000000000000, 39.92904733170480824 ) ) ;
#72587=CARTESIAN_POINT ( 'NONE',  ( -91.20471926501998894, -30.00000000000000000, 190.5760516518613485 ) ) ;
#72591=CARTESIAN_POINT ( 'NONE',  ( 52.19818328693233411, -57.67656952867285014, 83.25269862765968298 ) ) ;
#72600=CARTESIAN_POINT ( 'NONE',  ( -25.22310183047458310, -60.00000000000000000, 41.23078497591944114 ) ) ;
#72602=CARTESIAN_POINT ( 'NONE',  ( -86.48546161092085072, -17.02960564313559999, 183.8964038825536704 ) ) ;
#72607=CARTESIAN_POINT ( 'NONE',  ( -15.48413422138503037, -29.03194011403549624, 28.89617789578369411 ) ) ;
#72617=CYLINDRICAL_SURFACE ( 'NONE', #38194, 2.000000000000001776 ) ;
#72621=CARTESIAN_POINT ( 'NONE',  ( 73.56186416953940466, -60.00000000000000000, 167.8023059681976861 ) ) ;
#72626=CARTESIAN_POINT ( 'NONE',  ( 8.555523463203789092, -60.00000000000005684, 41.98724916707659816 ) ) ;
#72640=CARTESIAN_POINT ( 'NONE',  ( -78.30174078941652738, -60.00000000000486011, 197.9974431830838455 ) ) ;
#72642=CARTESIAN_POINT ( 'NONE',  ( 75.98234489927602908, -60.00000000000001421, 186.9997704955459596 ) ) ;
#72645=CARTESIAN_POINT ( 'NONE',  ( -108.8241353627135055, -30.00000000000001421, 157.0475095860343515 ) ) ;
#72646=CARTESIAN_POINT ( 'NONE',  ( 13.17625921126869670, -18.58681922276355536, 27.05832475667332915 ) ) ;
#72648=CARTESIAN_POINT ( 'NONE',  ( 101.6217879588726447, -38.00000000000002132, 186.1188645697355355 ) ) ;
#72651=CARTESIAN_POINT ( 'NONE',  ( -46.35736043082792435, -56.81302380653085748, 50.30497149764946130 ) ) ;
#72663=CARTESIAN_POINT ( 'NONE',  ( 101.9844698653622714, -29.99999999999932143, 198.1683824175306086 ) ) ;
#72665=CARTESIAN_POINT ( 'NONE',  ( 93.60111843194438563, -30.00000000000000355, 109.5859247788262820 ) ) ;
#72668=ORIENTED_EDGE ( 'NONE', *, *, #71262, .T. ) ;
#72679=CARTESIAN_POINT ( 'NONE',  ( 79.75840094887199427, -38.76322012846202369, 192.5408423534894666 ) ) ;
#72701=CARTESIAN_POINT ( 'NONE',  ( 30.54121840989820669, -32.81349016368368154, 40.87587671059132077 ) ) ;
#72705=CARTESIAN_POINT ( 'NONE',  ( 86.01665704136831891, -24.89204632129366246, 179.1268479360217327 ) ) ;
#72708=CARTESIAN_POINT ( 'NONE',  ( 94.41008270668507407, -57.67099569795677638, -0.2925677098450494840 ) ) ;
#72724=CARTESIAN_POINT ( 'NONE',  ( 68.00294669520873470, -29.92123893200863094, -21.72257178417913792 ) ) ;
#72728=CARTESIAN_POINT ( 'NONE',  ( -10.67412802623772983, -16.34922207018503570, -34.75766904438820148 ) ) ;
#72731=CARTESIAN_POINT ( 'NONE',  ( -63.67534439124898427, -60.22833768822253830, -28.64743048599374831 ) ) ;
#72736=CARTESIAN_POINT ( 'NONE',  ( -92.46340183990984940, -59.99999999999999289, -0.7256272337619585899 ) ) ;
#72740=CARTESIAN_POINT ( 'NONE',  ( 95.99736947783486585, -37.71600262711182694, 192.9724029575287716 ) ) ;
#72743=CARTESIAN_POINT ( 'NONE',  ( -82.50772378166941223, -39.49606204731786363, 165.2126353373692496 ) ) ;
#72755=CARTESIAN_POINT ( 'NONE',  ( -108.1850948662969216, -57.66112862901258751, 198.7856339303252753 ) ) ;
#72761=CARTESIAN_POINT ( 'NONE',  ( -59.37491258674359784, -59.99999999999998579, -38.24906085379748788 ) ) ;
#72762=CARTESIAN_POINT ( 'NONE',  ( -1.425880015568740777, -60.00000000000000711, 42.00000000000002132 ) ) ;
#72763=EDGE_CURVE ( 'NONE', #89315, #81125, #24231, .T. ) ;
#72764=CARTESIAN_POINT ( 'NONE',  ( -53.13873901080162909, -46.44135197877653809, 59.08599850147474086 ) ) ;
#72767=CARTESIAN_POINT ( 'NONE',  ( -95.34023284422563904, -37.68404846173547895, 193.0124814966931694 ) ) ;
#72772=CARTESIAN_POINT ( 'NONE',  ( 91.31681156736948424, -38.36314778512125656, -2.424099829648139082 ) ) ;
#72777=CARTESIAN_POINT ( 'NONE',  ( 85.21185514236475456, -29.99999999999999645, 172.2923490395237707 ) ) ;
#72785=CARTESIAN_POINT ( 'NONE',  ( 49.24857862907958150, -22.20931426737695702, 44.01793639162288230 ) ) ;
#72788=DIRECTION ( 'NONE',  ( -8.673617379884035472E-17, -0.000000000000000000, -1.000000000000000000 ) ) ;
#72790=CARTESIAN_POINT ( 'NONE',  ( -108.7991622881044123, -38.35665266207558943, 190.7632732821325874 ) ) ;
#72793=CARTESIAN_POINT ( 'NONE',  ( 90.86072268490488568, -38.35173073395984744, 20.62671579895992835 ) ) ;
#72797=CARTESIAN_POINT ( 'NONE',  ( 101.8886451212922566, -45.28289133281111134, 144.5137924623328729 ) ) ;
#72801=CARTESIAN_POINT ( 'NONE',  ( 99.70625480700427090, -60.00000000000000000, 201.9673764616556184 ) ) ;
#72804=CARTESIAN_POINT ( 'NONE',  ( 56.19429422314115641, -18.67854215501002813, 54.41800084858584086 ) ) ;
#72810=CARTESIAN_POINT ( 'NONE',  ( -89.24293106356928718, -38.38520225817266152, -17.61820809038416513 ) ) ;
#72822=CARTESIAN_POINT ( 'NONE',  ( 83.59357190745099331, -39.46543166661771807, 175.2130931883967833 ) ) ;
#72860=CARTESIAN_POINT ( 'NONE',  ( -109.0244361759819327, -60.00000000000000000, 136.1499024773399924 ) ) ;
#72863=CARTESIAN_POINT ( 'NONE',  ( 3.439834737513524090E-06, -25.54951635985603531, 28.14790268624504677 ) ) ;
#72868=CARTESIAN_POINT ( 'NONE',  ( -81.16717396890126679, -60.54721624790309420, 184.2208889243687793 ) ) ;
#72880=CARTESIAN_POINT ( 'NONE',  ( 106.1778528577414704, -14.21045842199435150, 156.9945530843897075 ) ) ;
#72881=CARTESIAN_POINT ( 'NONE',  ( -113.3391396720030428, -60.00000000000005684, 187.7090405971777898 ) ) ;
#72883=CARTESIAN_POINT ( 'NONE',  ( -61.25147057187043487, -39.48936545682737176, 75.54103842554776804 ) ) ;
#72886=CARTESIAN_POINT ( 'NONE',  ( 105.2797116528661974, -60.00000000000249401, 202.0183772298807412 ) ) ;
#72898=CARTESIAN_POINT ( 'NONE',  ( -83.41754797870378013, -59.99999999999998579, 199.1391409242881139 ) ) ;
#72909=CARTESIAN_POINT ( 'NONE',  ( -33.46790549732532583, -39.49766074888488276, 34.56548730633365807 ) ) ;
#72912=CARTESIAN_POINT ( 'NONE',  ( 38.45571508739885758, -46.42947195434589247, 38.95870930491370387 ) ) ;
#72913=CARTESIAN_POINT ( 'NONE',  ( 10.45706415778036025, -1.734723475976807094E-15, -13.60704923275195455 ) ) ;
#72916=CARTESIAN_POINT ( 'NONE',  ( -73.93668673393140978, -38.32666573519513520, 159.8187507061171857 ) ) ;
#72925=B_SPLINE_CURVE_WITH_KNOTS ( 'NONE', 3,
 ( #19220, #91469, #18666, #51520, #9455, #75255, #52050, #8932 ),
 .UNSPECIFIED., .F., .F.,
 ( 4, 2, 2, 4 ),
 ( 2.384759638366321710E-15, 0.01120533138725377485, 0.01680799708087945751, 0.02241066277450514191 ),
 .UNSPECIFIED. ) ;
#72926=CARTESIAN_POINT ( 'NONE',  ( 100.3075067269979428, -59.99999999999999289, 82.82790229349259903 ) ) ;
#72934=CARTESIAN_POINT ( 'NONE',  ( -83.36175203672824807, -30.00000000000000000, 155.5103389558694289 ) ) ;
#72950=CARTESIAN_POINT ( 'NONE',  ( 79.97290194383445794, -49.90522762054754224, 158.2806676109657928 ) ) ;
#72959=CARTESIAN_POINT ( 'NONE',  ( -56.21986590610479340, -57.67573674557218766, 94.99882904018191709 ) ) ;
#72968=CARTESIAN_POINT ( 'NONE',  ( -14.15215018753299780, -14.92673834348265061, 31.67970770892681287 ) ) ;
#72985=CARTESIAN_POINT ( 'NONE',  ( 105.3688122440774464, -57.64581400391074339, 201.4821763970232098 ) ) ;
#72990=CARTESIAN_POINT ( 'NONE',  ( -73.48687785542945505, -60.00000000000000711, 167.0610275913660416 ) ) ;
#72992=CYLINDRICAL_SURFACE ( 'NONE', #71743, 7.499999999992679633 ) ;
#72994=CARTESIAN_POINT ( 'NONE',  ( -83.95403480896771953, -53.78288136489426563, 188.7750542527096798 ) ) ;
#73003=CARTESIAN_POINT ( 'NONE',  ( -83.69066969828963920, -52.72359143521253344, -15.75783544347118159 ) ) ;
#73009=CARTESIAN_POINT ( 'NONE',  ( 16.57301948837260497, -3.469446951953614189E-15, -4.453875240779963107 ) ) ;
#73011=CARTESIAN_POINT ( 'NONE',  ( 89.53125762993630588, -30.00000000000007461, -13.19907884436577561 ) ) ;
#73012=CARTESIAN_POINT ( 'NONE',  ( -79.40447720853664748, -22.14626824436577124, 126.4748337375811786 ) ) ;
#73014=CARTESIAN_POINT ( 'NONE',  ( 4.090242245409069888, -14.21045842199428932, 34.36068907045891763 ) ) ;
#73016=CARTESIAN_POINT ( 'NONE',  ( 94.65517944311366705, -57.65681286589507692, -9.358892355265044927 ) ) ;
#73033=CARTESIAN_POINT ( 'NONE',  ( -31.71194513525783165, -14.21045842199430709, 37.70210531190891601 ) ) ;
#73034=CARTESIAN_POINT ( 'NONE',  ( 28.08771105297372728, -29.05517447130626962, 30.69056992575482568 ) ) ;
#73046=CARTESIAN_POINT ( 'NONE',  ( 65.38219241326270037, -59.99999999999999289, -34.08627437347746536 ) ) ;
#73049=CARTESIAN_POINT ( 'NONE',  ( -85.18896233714281152, -59.99999999999995737, -15.68185129854840554 ) ) ;
#73052=ORIENTED_EDGE ( 'NONE', *, *, #18492, .F. ) ;
#73070=CARTESIAN_POINT ( 'NONE',  ( -72.90163493338778267, -60.00000000000000711, 126.5439322136281675 ) ) ;
#73071=CARTESIAN_POINT ( 'NONE',  ( 67.99901078833072177, -29.05790011282407193, 89.58219462804794375 ) ) ;
#73078=CARTESIAN_POINT ( 'NONE',  ( -53.00838388237266940, -57.67116150918030115, -39.31046371713402721 ) ) ;
#73093=CARTESIAN_POINT ( 'NONE',  ( -92.31907403475642582, -30.00000000000000355, 190.9581983028909349 ) ) ;
#73097=CARTESIAN_POINT ( 'NONE',  ( 53.06187785988736749, -57.67613140857140763, 85.70582740418153378 ) ) ;
#73107=CARTESIAN_POINT ( 'NONE',  ( -16.64288181053317928, -60.00000000000000000, 39.89607924062331534 ) ) ;
#73114=CARTESIAN_POINT ( 'NONE',  ( -86.51221272467716972, -53.78683390949667142, 192.4548174909675708 ) ) ;
#73118=CARTESIAN_POINT ( 'NONE',  ( -5.972684422919853020, -18.58610353171744123, 26.97790868950432497 ) ) ;
#73131=CARTESIAN_POINT ( 'NONE',  ( 70.25724432519014329, -60.00000000000000000, 142.8801060964537726 ) ) ;
#73136=CARTESIAN_POINT ( 'NONE',  ( 40.90273407096766078, -60.00000000000019185, 57.82174102673914007 ) ) ;
#73153=CARTESIAN_POINT ( 'NONE',  ( -31.10001900035964439, -60.00000000000245848, 46.36770439546862121 ) ) ;
#73155=CARTESIAN_POINT ( 'NONE',  ( 52.67981547313412705, -60.00000000000002842, 78.74676858557705827 ) ) ;
#73158=CARTESIAN_POINT ( 'NONE',  ( -108.8021899934185086, -29.99999999999995026, 184.6878429379334534 ) ) ;
#73159=CARTESIAN_POINT ( 'NONE',  ( 18.02386892498230964, -46.43468589485836873, 31.95930805262861440 ) ) ;
#73162=CARTESIAN_POINT ( 'NONE',  ( -44.80343625002662833, -42.98650238651817546, 44.34706117140887471 ) ) ;
#73164=ORIENTED_EDGE ( 'NONE', *, *, #101156, .T. ) ;
#73170=VERTEX_POINT ( 'NONE', #23248 ) ;
#73173=CARTESIAN_POINT ( 'NONE',  ( 94.54924656135277417, -30.00000000000334310, 199.9234823381102899 ) ) ;
#73177=CARTESIAN_POINT ( 'NONE',  ( 94.35141610110464683, -30.00000000000000355, 114.0755648428526001 ) ) ;
#73194=CARTESIAN_POINT ( 'NONE',  ( 78.85737667306543131, -38.67488751151257276, 190.5950933815901749 ) ) ;
#73214=SURFACE_STYLE_FILL_AREA ( #98037 ) ;
#73218=CARTESIAN_POINT ( 'NONE',  ( 5.128989308823689974, -18.61194742579494132, 35.09291343390540874 ) ) ;
#73221=CARTESIAN_POINT ( 'NONE',  ( 84.67559614028348847, -50.18795068039596430, 188.5560178073191082 ) ) ;
#73225=CARTESIAN_POINT ( 'NONE',  ( 83.08230946783562842, -57.67107110472222331, -28.35002488624179406 ) ) ;
#73230=CARTESIAN_POINT ( 'NONE',  ( -54.55306156724233091, -38.00000000000002132, 58.68193799101367603 ) ) ;
#73247=CARTESIAN_POINT ( 'NONE',  ( -12.84829414594153718, -16.74545646077213235, -34.56912337068381902 ) ) ;
#73250=CARTESIAN_POINT ( 'NONE',  ( -64.34419054092482781, -47.40884698333244529, -26.19182566128564105 ) ) ;
#73259=CARTESIAN_POINT ( 'NONE',  ( -68.79428259631640685, -60.00000000000000000, -32.96147483378281606 ) ) ;
#73261=CARTESIAN_POINT ( 'NONE',  ( 53.28488084350904330, -36.41999201664042118, -27.31396571457552724 ) ) ;
#73265=CARTESIAN_POINT ( 'NONE',  ( 95.75131951580081591, -52.82440587276369826, 195.4613675494113068 ) ) ;
#73267=CARTESIAN_POINT ( 'NONE',  ( -0.009542807171270463462, -57.67120202564520071, -44.61186682692561334 ) ) ;
#73269=CARTESIAN_POINT ( 'NONE',  ( -79.82837926754650937, -56.86146518977977848, 167.4549986377173241 ) ) ;
#73282=CARTESIAN_POINT ( 'NONE',  ( -93.91996415714238822, -57.61928231945634593, 204.5092364001214946 ) ) ;
#73287=CARTESIAN_POINT ( 'NONE',  ( -72.33650272884364085, -14.21045842199437992, -25.95337777301578797 ) ) ;
#73289=CARTESIAN_POINT ( 'NONE',  ( -51.76998541488613625, -42.97695565422467467, 55.08012004277745888 ) ) ;
#73293=CARTESIAN_POINT ( 'NONE',  ( -98.35819475468484541, -37.73781679060022043, 192.3236476725261923 ) ) ;
#73298=CARTESIAN_POINT ( 'NONE',  ( 91.46124806493796200, -38.38747635837011529, -7.532907868879641811 ) ) ;
#73304=UNCERTAINTY_MEASURE_WITH_UNIT (LENGTH_MEASURE( 1.000000000000000082E-05 ), #7352, 'distance_accuracy_value', 'NONE');
#73305=CARTESIAN_POINT ( 'NONE',  ( 84.64623062946745335, -29.99999999999999645, 166.9594626320265718 ) ) ;
#73311=CARTESIAN_POINT ( 'NONE',  ( 49.48743286625204973, -29.12953531296649246, 46.55428020132097799 ) ) ;
#73316=CARTESIAN_POINT ( 'NONE',  ( -99.05629584364598372, -38.35566002928235463, 82.90449515628614563 ) ) ;
#73319=CARTESIAN_POINT ( 'NONE',  ( 91.74760752124998930, -38.35367829061644329, 32.25783006298658506 ) ) ;
#73322=CARTESIAN_POINT ( 'NONE',  ( 105.8789942812274347, -60.15140141051522704, 158.7628738880897004 ) ) ;
#73327=CARTESIAN_POINT ( 'NONE',  ( 76.37025012973165872, -60.00000000000000000, 188.4228991859059477 ) ) ;
#73332=CARTESIAN_POINT ( 'NONE',  ( 56.18747785061527367, -29.08556120447800097, 58.61083588748905271 ) ) ;
#73338=CARTESIAN_POINT ( 'NONE',  ( -78.82921310057996322, -29.99999999998994937, 186.5840926925319536 ) ) ;
#73349=CARTESIAN_POINT ( 'NONE',  ( 85.29287252500783723, -25.40231041538968526, 170.0305094119342471 ) ) ;
#73364=CARTESIAN_POINT ( 'NONE',  ( -26.01198988472668105, -29.73227193545200109, 38.65812357631961049 ) ) ;
#73386=CARTESIAN_POINT ( 'NONE',  ( -109.0325503311019446, -60.00000000000000000, 136.2077695858294817 ) ) ;
#73394=CARTESIAN_POINT ( 'NONE',  ( -86.20327847884676942, -18.29549290550911778, 168.7810058706911889 ) ) ;
#73410=CARTESIAN_POINT ( 'NONE',  ( 114.3489886862215883, -60.00000000000002842, 164.2602920347584359 ) ) ;
#73411=CARTESIAN_POINT ( 'NONE',  ( -106.7878682580589071, -14.21045842199432663, 165.8353880188381027 ) ) ;
#73412=CARTESIAN_POINT ( 'NONE',  ( -64.43939551583753200, -22.10274715365727261, 75.67409506763341653 ) ) ;
#73416=CARTESIAN_POINT ( 'NONE',  ( 112.9852162270515379, -60.00000000000000000, 189.2447496387153478 ) ) ;
#73420=CARTESIAN_POINT ( 'NONE',  ( 2.066515801291814188E-05, -35.99156565065722191, 29.88824423471190883 ) ) ;
#73430=CARTESIAN_POINT ( 'NONE',  ( -107.3076241182627228, -59.99999999999998579, 196.6869121037917978 ) ) ;
#73441=CARTESIAN_POINT ( 'NONE',  ( 106.4540643960806818, -59.99999999999999289, 175.2089101670526645 ) ) ;
#73442=CARTESIAN_POINT ( 'NONE',  ( -32.69629451572926371, -25.62164330307078686, 31.60428463432279145 ) ) ;
#73444=CARTESIAN_POINT ( 'NONE',  ( 41.83556152829600450, -56.79490171586785863, 44.35057537570739328 ) ) ;
#73448=CARTESIAN_POINT ( 'NONE',  ( -84.03771973047440724, -38.76031024263880909, 197.8063387002864886 ) ) ;
#73450=CARTESIAN_POINT ( 'NONE',  ( 2.499999999999999556, -11.82938852550672593, 20.68569722764979701 ) ) ;
#73460=CARTESIAN_POINT ( 'NONE',  ( 97.79592197825088817, -59.99999999999998579, 67.65900241341216770 ) ) ;
#73466=CARTESIAN_POINT ( 'NONE',  ( -95.68750834249433979, -29.99999999999991473, 191.3192462275344781 ) ) ;
#73479=CARTESIAN_POINT ( 'NONE',  ( 82.15109098281409672, -25.62403950325144208, 144.0112107024839077 ) ) ;
#73488=CARTESIAN_POINT ( 'NONE',  ( 21.19369299071200174, -60.00000000000002132, -35.98201359092684015 ) ) ;
#73490=CARTESIAN_POINT ( 'NONE',  ( -14.02841258157142690, -57.67128452586098319, 41.71853563109401364 ) ) ;
#73500=CARTESIAN_POINT ( 'NONE',  ( 26.50624775675402134, -30.07146743491984253, 38.85830190916826155 ) ) ;
#73511=CARTESIAN_POINT ( 'NONE',  ( 8.560863513991206375, -22.26022726792948347, -38.54397950491892288 ) ) ;
#73517=CARTESIAN_POINT ( 'NONE',  ( 111.7166322225655932, -57.67144568547145411, 141.1164683676901461 ) ) ;
#73520=CARTESIAN_POINT ( 'NONE',  ( 73.50474219086036953, -59.99999999999997158, -24.84696050693406022 ) ) ;
#73522=CARTESIAN_POINT ( 'NONE',  ( -73.36883549988228026, -59.99999999999997868, 165.9088962234452254 ) ) ;
#73527=CARTESIAN_POINT ( 'NONE',  ( -86.05794333201590973, -24.85278311144536190, 179.6146324082043861 ) ) ;
#73535=CARTESIAN_POINT ( 'NONE',  ( -84.43672636148829724, -45.26723741285099578, -8.687404643540368454 ) ) ;
#73542=CARTESIAN_POINT ( 'NONE',  ( -10.45706415777859455, -1.734723475976807094E-15, 13.60704923275178935 ) ) ;
#73544=CARTESIAN_POINT ( 'NONE',  ( 2.726837646490497757, -14.21045842199434794, -37.36840973699905533 ) ) ;
#73545=CARTESIAN_POINT ( 'NONE',  ( -77.58900850978491803, -32.55426609391764714, 126.5529035919531538 ) ) ;
#73547=CARTESIAN_POINT ( 'NONE',  ( 32.49824730387988581, -59.99999999999999289, 47.28149596916139075 ) ) ;
#73549=CARTESIAN_POINT ( 'NONE',  ( 109.2379923685197127, -57.67120357111281947, 124.0924491272076011 ) ) ;
#73550=ORIENTED_EDGE ( 'NONE', *, *, #104411, .F. ) ;
#73570=CARTESIAN_POINT ( 'NONE',  ( 30.23427007269342681, -36.01284674722493406, 32.58737572666365878 ) ) ;
#73581=DIRECTION ( 'NONE',  ( -0.000000000000000000, -1.000000000000000000, -0.000000000000000000 ) ) ;
#73585=CARTESIAN_POINT ( 'NONE',  ( 9.708955930194042239, -60.00000000000000711, -42.43033358671466004 ) ) ;
#73612=CARTESIAN_POINT ( 'NONE',  ( -42.44423885992037526, -60.00000000000002842, 45.81425615931330952 ) ) ;
#73613=CARTESIAN_POINT ( 'NONE',  ( 66.61458672392836888, -49.90900424519782064, 96.76507275318283519 ) ) ;
#73639=CARTESIAN_POINT ( 'NONE',  ( -97.74289867503729567, -29.99999999999999645, 190.7460677368483459 ) ) ;
#73641=STYLED_ITEM ( 'NONE', ( #30475 ), #26496 ) ;
#73644=CARTESIAN_POINT ( 'NONE',  ( 59.91412286587753755, -57.67713599549763615, 107.0922378007342672 ) ) ;
#73647=CARTESIAN_POINT ( 'NONE',  ( 10.51353532556417214, -22.75354294893093865, -38.54225802751280838 ) ) ;
#73650=CARTESIAN_POINT ( 'NONE',  ( -12.63134323606425191, -60.00000000000000000, 39.70362636174434101 ) ) ;
#73657=CARTESIAN_POINT ( 'NONE',  ( -86.30857863919766260, -53.80050282809293094, 192.2617187078320171 ) ) ;
#73661=CARTESIAN_POINT ( 'NONE',  ( -8.254083131201605639, -49.92098614289960068, 32.20337770899964625 ) ) ;
#73677=CARTESIAN_POINT ( 'NONE',  ( 108.8020855619825653, -30.00000000000001066, 184.6883589252716433 ) ) ;
#73697=CARTESIAN_POINT ( 'NONE',  ( -55.85648761906974613, -60.00000000001953282, 95.11638450465373751 ) ) ;
#73700=CARTESIAN_POINT ( 'NONE',  ( 93.94670038468932205, -60.00000000000001421, 41.20803089316482470 ) ) ;
#73701=CARTESIAN_POINT ( 'NONE',  ( -109.5916892278405470, -30.00000000000001776, 172.2591039824585550 ) ) ;
#73702=CARTESIAN_POINT ( 'NONE',  ( 16.01724265899924049, -60.35821680913219467, 34.15402070262287282 ) ) ;
#73704=CARTESIAN_POINT ( 'NONE',  ( 87.09402098694862104, -38.00000000000002132, 60.21609768695862641 ) ) ;
#73706=CARTESIAN_POINT ( 'NONE',  ( -46.15598990074098396, -18.78241605370739009, 39.24116979527025251 ) ) ;
#73718=CARTESIAN_POINT ( 'NONE',  ( 78.24277327743527621, -29.99999999990264499, 183.8761278456963453 ) ) ;
#73722=CARTESIAN_POINT ( 'NONE',  ( 100.5432165947128453, -30.00000000000000711, 159.7633814667663330 ) ) ;
#73740=CARTESIAN_POINT ( 'NONE',  ( 81.30285530623764600, -38.84117475569783551, 195.0272007915274060 ) ) ;
#73764=CARTESIAN_POINT ( 'NONE',  ( 86.32898320831061767, -21.03587308976179671, 180.4856531993580973 ) ) ;
#73768=CARTESIAN_POINT ( 'NONE',  ( 92.45459292580818556, -57.65848211217247865, -18.44663115571118439 ) ) ;
#73772=CARTESIAN_POINT ( 'NONE',  ( -81.53069149982411545, -30.00000000000001421, -8.902666450183531310 ) ) ;
#73774=CARTESIAN_POINT ( 'NONE',  ( -81.88346289758811736, -38.00000000000000000, 157.3757661605745284 ) ) ;
#73795=CARTESIAN_POINT ( 'NONE',  ( -62.72865154022586154, -21.76998117876125960, -22.22417429766882080 ) ) ;
#73806=CARTESIAN_POINT ( 'NONE',  ( -66.14779852596444698, -60.00000000000000000, -33.84381125176143001 ) ) ;
#73808=CARTESIAN_POINT ( 'NONE',  ( 56.93684650526180491, -37.03532724266435849, -26.56149101784519928 ) ) ;
#73811=CARTESIAN_POINT ( 'NONE',  ( 94.99852919210989910, -37.71004738711080506, 193.0139001793616558 ) ) ;
#73826=LINE ( 'NONE', #32869, #59902 ) ;
#73827=CARTESIAN_POINT ( 'NONE',  ( -39.01690548088378563, -57.69424739071683916, 54.12508632231112671 ) ) ;
#73832=CARTESIAN_POINT ( 'NONE',  ( 25.62974135805828979, -60.00000000000002132, -43.76006462505735328 ) ) ;
#73833=CARTESIAN_POINT ( 'NONE',  ( -35.98784834194372451, -29.99999999999998934, 43.73664282352994803 ) ) ;
#73835=CARTESIAN_POINT ( 'NONE',  ( -51.81172722203650949, -56.84363277413236659, 60.27128131545431700 ) ) ;
#73839=CARTESIAN_POINT ( 'NONE',  ( -100.1592349301962628, -52.75790702199028459, 194.0880419080440618 ) ) ;
#73845=CARTESIAN_POINT ( 'NONE',  ( 74.44968402934742358, -38.32904790398288952, 164.3025046429760323 ) ) ;
#73850=CARTESIAN_POINT ( 'NONE',  ( 84.64943319986461745, -30.00000000000001066, 166.9899077754115808 ) ) ;
#73856=ORIENTED_EDGE ( 'NONE', *, *, #96705, .T. ) ;
#73857=CARTESIAN_POINT ( 'NONE',  ( 48.95189267709701397, -60.28532577491037614, 55.82551791209952796 ) ) ;
#73862=CARTESIAN_POINT ( 'NONE',  ( -92.64563826212697961, -38.35495884179172066, 40.48894988335383260 ) ) ;
#73865=CARTESIAN_POINT ( 'NONE',  ( 97.20990545091203217, -38.35580220330457024, 71.88490386968666712 ) ) ;
#73867=CARTESIAN_POINT ( 'NONE',  ( 103.1286089144194733, -52.71713921426092497, 144.4394181523613554 ) ) ;
#73873=CARTESIAN_POINT ( 'NONE',  ( 76.72974224477856353, -59.99999999999997868, 189.6511138508473095 ) ) ;
#73876=CARTESIAN_POINT ( 'NONE',  ( 60.16448956355160504, -18.65125552583483071, 63.02594496277924918 ) ) ;
#73880=CARTESIAN_POINT ( 'NONE',  ( -57.17200305705274133, -29.99999999999333866, 83.43905756859183498 ) ) ;
#73891=CARTESIAN_POINT ( 'NONE',  ( 83.11751895291531866, -42.97626541852498860, 176.1565397990591464 ) ) ;
#73903=CARTESIAN_POINT ( 'NONE',  ( -12.27450249641863245, -21.25525156901051815, 35.59543369205189123 ) ) ;
#73916=CARTESIAN_POINT ( 'NONE',  ( 72.23675078389933901, -60.22819274490537822, -25.48594946497165026 ) ) ;
#73927=CARTESIAN_POINT ( 'NONE',  ( -103.7172116487474938, -60.00000000000002132, 102.7823711783175469 ) ) ;
#73935=CARTESIAN_POINT ( 'NONE',  ( -86.07252144299347663, -18.39191110879000490, 166.6798528094340952 ) ) ;
#73952=CARTESIAN_POINT ( 'NONE',  ( 109.5313825839763382, -30.00000000000004619, 176.4140126643321196 ) ) ;
#73953=CARTESIAN_POINT ( 'NONE',  ( -114.3490076612200568, -60.00000000000000000, 164.2604626692111367 ) ) ;
#73954=CARTESIAN_POINT ( 'NONE',  ( -61.66793082946371385, -32.53820867738551215, 73.28858974252342762 ) ) ;
#73957=CARTESIAN_POINT ( 'NONE',  ( 94.71960157893720123, -59.99999999999998579, 0.7631219686126513579 ) ) ;
#73959=CARTESIAN_POINT ( 'NONE',  ( 2.640755779914924649E-05, -39.47262781682785970, 30.46842126240701631 ) ) ;
#73967=CARTESIAN_POINT ( 'NONE',  ( -108.2395898723600851, -60.00000000000000000, 130.5556691422416975 ) ) ;
#73976=CARTESIAN_POINT ( 'NONE',  ( 106.3740829544859565, -59.99999999999997868, 177.4779890160187961 ) ) ;
#73977=CARTESIAN_POINT ( 'NONE',  ( -31.99426222591429081, -29.08333287831730019, 31.97858915124429657 ) ) ;
#73981=CARTESIAN_POINT ( 'NONE',  ( 39.39460558282306835, -22.22791209051591466, 34.40903791641994047 ) ) ;
#73987=CARTESIAN_POINT ( 'NONE',  ( -77.04287001588842543, -38.46292279798635860, 184.5679294465321050 ) ) ;
#73998=CARTESIAN_POINT ( 'NONE',  ( 103.6056036519425021, -60.00000000000000000, 102.1281063761447996 ) ) ;
#74004=CARTESIAN_POINT ( 'NONE',  ( -87.13860669537896797, -30.00000000000003908, 184.2824706449898144 ) ) ;
#74020=CARTESIAN_POINT ( 'NONE',  ( 82.52664522055025031, -32.55557495989385330, 155.0942886860429155 ) ) ;
#74030=CARTESIAN_POINT ( 'NONE',  ( 66.17605003987134182, -60.00000000000000000, -27.79200239227810698 ) ) ;
#74040=CARTESIAN_POINT ( 'NONE',  ( 38.04269904239736633, -36.98679888056368981, 47.30367013139319710 ) ) ;
#74044=PRODUCT_CONTEXT ( 'NONE', #10721, 'mechanical' ) ;
#74052=CARTESIAN_POINT ( 'NONE',  ( 114.0943401353945603, -57.67137920739276780, 166.6188124564318116 ) ) ;
#74058=CARTESIAN_POINT ( 'NONE',  ( -76.89441695137394106, -59.99999999999999289, 190.1397586532095545 ) ) ;
#74061=CARTESIAN_POINT ( 'NONE',  ( -84.82604425270216097, -46.57314820510289621, 187.1285925919904116 ) ) ;
#74071=CARTESIAN_POINT ( 'NONE',  ( -85.75027484506800590, -52.74039826046678314, -7.195638168032203907 ) ) ;
#74079=CARTESIAN_POINT ( 'NONE',  ( -4.453875240779026079, -1.734723475976807094E-15, 16.57301948836938621 ) ) ;
#74082=CARTESIAN_POINT ( 'NONE',  ( -2.851760031137707596, -60.00000000000000000, -45.00000000000002132 ) ) ;
#74083=CARTESIAN_POINT ( 'NONE',  ( -77.85220176464979147, -42.96760201762617015, 136.7854011922409256 ) ) ;
#74085=CARTESIAN_POINT ( 'NONE',  ( 76.30472591814422856, -30.00000000000007105, 168.5677193688796649 ) ) ;
#74087=CARTESIAN_POINT ( 'NONE',  ( 106.5469097212175171, -57.67120316527606150, 107.4300699905816714 ) ) ;
#74103=CARTESIAN_POINT ( 'NONE',  ( 28.71054976466791331, -42.95721924763428490, 33.31278848725109043 ) ) ;
#74109=UNCERTAINTY_MEASURE_WITH_UNIT (LENGTH_MEASURE( 1.000000000000000082E-05 ), #35582, 'distance_accuracy_value', 'NONE');
#74119=CARTESIAN_POINT ( 'NONE',  ( 91.72933629761578800, -60.00000000000000000, -14.91791294062407758 ) ) ;
#74123=( BOUNDED_CURVE ( )  B_SPLINE_CURVE ( 2, ( #75823, #58590, #1919 ),
 .UNSPECIFIED., .F., .F. ) 
 B_SPLINE_CURVE_WITH_KNOTS ( ( 3, 3 ),
 ( 0.000000000000000000, 1.000000000000000000 ),
 .UNSPECIFIED. ) 
 CURVE ( )  GEOMETRIC_REPRESENTATION_ITEM ( )  RATIONAL_B_SPLINE_CURVE ( ( 1.000000000000000000, 1.857142857142858317, 1.000000000000000000 ) ) 
 REPRESENTATION_ITEM ( '' )  );
#74135=CARTESIAN_POINT ( 'NONE',  ( 85.70657369333201814, -52.73561151911660971, -4.539914901182836360 ) ) ;
#74146=CARTESIAN_POINT ( 'NONE',  ( -49.24092377949861543, -59.99999999999996447, 56.22341034505959811 ) ) ;
#74148=CARTESIAN_POINT ( 'NONE',  ( 63.81336088806118312, -53.38611597571917855, 89.97107311934965423 ) ) ;
#74153=CARTESIAN_POINT ( 'NONE',  ( -77.41886385744251697, -57.67119865640713527, -31.55546021046578531 ) ) ;
#74174=CARTESIAN_POINT ( 'NONE',  ( 4.289501753560038821, -60.00000000000000000, 39.63072196994962582 ) ) ;
#74175=CARTESIAN_POINT ( 'NONE',  ( -94.42958044472295853, -29.99999999999999645, 191.3151220890198374 ) ) ;
#74177=CARTESIAN_POINT ( 'NONE',  ( 70.41099422567990018, -57.68249184797887352, 157.3713819725495853 ) ) ;
#74180=CARTESIAN_POINT ( 'NONE',  ( 14.50404474426535906, -23.92104523642918679, -38.53261106116733714 ) ) ;
#74184=CARTESIAN_POINT ( 'NONE',  ( -12.69242650814801365, -59.99999999999999289, 39.70541446682850761 ) ) ;
#74188=CARTESIAN_POINT ( 'NONE',  ( -85.88719281955947338, -61.05569566503563550, 194.2292230513385505 ) ) ;
#74192=CARTESIAN_POINT ( 'NONE',  ( -9.185217898028438910, -35.99447867802918921, 29.89084909448629190 ) ) ;
#74207=CARTESIAN_POINT ( 'NONE',  ( 106.1778528577414704, -14.21045842199435150, 156.9945530843897075 ) ) ;
#74229=CARTESIAN_POINT ( 'NONE',  ( -72.13545514535530856, -59.99999999997070432, 177.2956874472480990 ) ) ;
#74233=CARTESIAN_POINT ( 'NONE',  ( 110.6907876672333657, -60.00000000000001421, 188.6866862957170667 ) ) ;
#74235=CARTESIAN_POINT ( 'NONE',  ( -109.5128114756446109, -29.99999999999999289, 168.1048973186342437 ) ) ;
#74236=CARTESIAN_POINT ( 'NONE',  ( 19.48570689116957411, -60.35677515645173941, 34.43380376002015453 ) ) ;
#74239=CARTESIAN_POINT ( 'NONE',  ( -43.56207904828443844, -60.25507094030576383, 47.28631016918702556 ) ) ;
#74253=CARTESIAN_POINT ( 'NONE',  ( 48.93247286101075844, -30.00000000006591350, 62.56579767259364644 ) ) ;
#74257=CARTESIAN_POINT ( 'NONE',  ( 90.42596699330265153, -30.00000000000000000, 90.98457831099128157 ) ) ;
#74273=VERTEX_POINT ( 'NONE', #100570 ) ;
#74275=CARTESIAN_POINT ( 'NONE',  ( 78.81272654805164279, -38.66995965544662539, 190.4856035335980664 ) ) ;
#74295=CARTESIAN_POINT ( 'NONE',  ( 85.74559076837111604, -39.25363284317074175, 186.2120581904971175 ) ) ;
#74299=CARTESIAN_POINT ( 'NONE',  ( 91.47088685542546216, -57.66242603154207558, -20.20556468422682883 ) ) ;
#74301=CYLINDRICAL_SURFACE ( 'NONE', #67694, 15.00000000000000000 ) ;
#74305=CARTESIAN_POINT ( 'NONE',  ( -81.41118343893772646, -30.00000000000000000, -9.978428732768641396 ) ) ;
#74317=CARTESIAN_POINT ( 'NONE',  ( -68.37927364716395573, -37.97112778231701213, -23.07505795230966683 ) ) ;
#74324=CARTESIAN_POINT ( 'NONE',  ( -38.96813603250004832, -24.55621239451162907, -30.50670703037211950 ) ) ;
#74326=CARTESIAN_POINT ( 'NONE',  ( -70.42419927718661654, -34.58954792057054561, -21.61483060261837252 ) ) ;
#74331=VERTEX_POINT ( 'NONE', #90901 ) ;
#74334=ADVANCED_FACE ( 'NONE', ( #59067 ), #26733, .T. ) ;
#74336=CARTESIAN_POINT ( 'NONE',  ( -26.53069809822883585, -60.00000000000000711, -41.28480351003638305 ) ) ;
#74338=CARTESIAN_POINT ( 'NONE',  ( 31.08825020654288096, -30.41363042624472257, -30.04296242939974704 ) ) ;
#74340=CARTESIAN_POINT ( 'NONE',  ( 99.23206058371319216, -37.81684522924224012, 191.6622011877896057 ) ) ;
#74352=CARTESIAN_POINT ( 'NONE',  ( -18.14395573440383203, -57.67158919250769600, 41.98617601139094546 ) ) ;
#74357=CARTESIAN_POINT ( 'NONE',  ( 49.63358250961842799, -60.00000000000001421, -40.41868810089377462 ) ) ;
#74358=CARTESIAN_POINT ( 'NONE',  ( -34.32536616635837845, -30.00000000000003553, 42.48815186199111338 ) ) ;
#74359=CARTESIAN_POINT ( 'NONE',  ( -51.90208491409480018, -18.71866842149948695, 46.78754088036709646 ) ) ;
#74362=CARTESIAN_POINT ( 'NONE',  ( -98.06883061208564811, -45.24973764535013032, 193.7416408753538235 ) ) ;
#74368=CARTESIAN_POINT ( 'NONE',  ( 98.38089941204171396, -38.47856758464003946, 200.9301062742698605 ) ) ;
#74374=CARTESIAN_POINT ( 'NONE',  ( 85.56723171479005430, -30.00000000000000355, 175.4130121643509597 ) ) ;
#74380=CARTESIAN_POINT ( 'NONE',  ( 53.02351809876299882, -36.03604319102321085, 54.92990362263699211 ) ) ;
#74386=CARTESIAN_POINT ( 'NONE',  ( -107.8813328617326874, -38.35631905857745494, 136.9743310841232642 ) ) ;
#74389=CARTESIAN_POINT ( 'NONE',  ( 91.67123410567980102, -38.35356722036148369, 31.46187313383635242 ) ) ;
#74391=CARTESIAN_POINT ( 'NONE',  ( 87.75812269781596342, -52.71627564034628222, 47.57411664421275788 ) ) ;
#74396=CARTESIAN_POINT ( 'NONE',  ( 77.13274333098043201, -60.00000000000001421, 190.8571566051506636 ) ) ;
#74399=CARTESIAN_POINT ( 'NONE',  ( 61.80202793844345877, -53.38729615061397737, 84.00710957604638907 ) ) ;
#74406=CARTESIAN_POINT ( 'NONE',  ( -53.29442438667957305, -30.00000000005343992, 72.87987713644304222 ) ) ;
#74418=CARTESIAN_POINT ( 'NONE',  ( 82.57840738188596674, -53.59987598830502975, 184.4164446621147704 ) ) ;
#74430=CARTESIAN_POINT ( 'NONE',  ( 50.66975656709965392, -60.00000000000000000, 73.49217170142772204 ) ) ;
#74432=CARTESIAN_POINT ( 'NONE',  ( 24.24390522887371802, -18.95292958071728151, 31.52331660755031706 ) ) ;
#74433=CARTESIAN_POINT ( 'NONE',  ( -12.95257293317843228, -21.59228805338226920, 35.67007454052365034 ) ) ;
#74445=CARTESIAN_POINT ( 'NONE',  ( 25.26525204496489252, -34.58978890963047093, -31.37000190431579583 ) ) ;
#74452=EDGE_CURVE ( 'NONE', #49798, #22652, #100489, .T. ) ;
#74457=CARTESIAN_POINT ( 'NONE',  ( -100.8708696091340897, -60.00000000000001421, 86.14267496683164893 ) ) ;
#74464=CARTESIAN_POINT ( 'NONE',  ( -80.98092848404644428, -56.94632824160903795, 178.5830683470894655 ) ) ;
#74475=SURFACE_STYLE_FILL_AREA ( #25994 ) ;
#74482=CARTESIAN_POINT ( 'NONE',  ( 114.5768552918926986, -59.99999999999997868, 170.6725192690976485 ) ) ;
#74483=EDGE_CURVE ( 'NONE', #102392, #61647, #32319, .T. ) ;
#74484=CARTESIAN_POINT ( 'NONE',  ( -108.4361608695136994, -30.00000000000004974, 186.7333242197273080 ) ) ;
#74485=CARTESIAN_POINT ( 'NONE',  ( -63.73445214523361102, -22.10497644405380768, 73.75391651273872640 ) ) ;
#74488=CARTESIAN_POINT ( 'NONE',  ( 114.6102123966894055, -60.00000000000000000, 174.7595319735745818 ) ) ;
#74490=CARTESIAN_POINT ( 'NONE',  ( 5.993569525592590708, -22.06720269990192307, 27.55800827838890399 ) ) ;
#74491=CARTESIAN_POINT ( 'NONE',  ( -103.7138855257204995, -60.15497775133528791, 139.5353567617456463 ) ) ;
#74499=CARTESIAN_POINT ( 'NONE',  ( -55.39551486789333978, -59.99999999999998579, 86.38772855768377212 ) ) ;
#74511=CARTESIAN_POINT ( 'NONE',  ( -32.86356798609371310, -39.49558199937673919, 34.28045917445315638 ) ) ;
#74513=CARTESIAN_POINT ( 'NONE',  ( 43.56271327712536845, -60.24810023598861619, 47.28533951050904705 ) ) ;
#74517=CARTESIAN_POINT ( 'NONE',  ( -76.01953405358801774, -38.37905128380688069, 178.5008278763145313 ) ) ;
#74521=CARTESIAN_POINT ( 'NONE',  ( 80.33268691154432872, -59.99999999999999289, 177.7134108711020133 ) ) ;
#74529=CARTESIAN_POINT ( 'NONE',  ( 111.0024401811853210, -60.00000000000000000, 152.1606877285774715 ) ) ;
#74536=CARTESIAN_POINT ( 'NONE',  ( -98.19961658146921479, -29.99999999999990763, 190.3012536825193308 ) ) ;
#74550=CARTESIAN_POINT ( 'NONE',  ( 81.95403812627554885, -46.45362839144696920, 171.2155095704361543 ) ) ;
#74554=EDGE_CURVE ( 'NONE', #72232, #45904, #70892, .T. ) ;
#74559=CARTESIAN_POINT ( 'NONE',  ( 11.74185064025517100, -59.99999999999997868, -36.59818147136398636 ) ) ;
#74568=CARTESIAN_POINT ( 'NONE',  ( 85.99101760945637807, -57.43956396353277682, 193.1180272415432739 ) ) ;
#74584=CARTESIAN_POINT ( 'NONE',  ( 106.9239920550738958, -57.67118183550353905, 109.9283693084385760 ) ) ;
#74590=CARTESIAN_POINT ( 'NONE',  ( -84.26043389055706712, -60.00000000000001421, 199.6846189265752116 ) ) ;
#74594=CARTESIAN_POINT ( 'NONE',  ( -83.31161619671260610, -53.71026484535321543, 187.1193032696220655 ) ) ;
#74601=CARTESIAN_POINT ( 'NONE',  ( -84.32710418608468217, -45.26462801463393504, -10.05937244304523759 ) ) ;
#74610=CARTESIAN_POINT ( 'NONE',  ( -40.75117554026711275, -14.21045842199432663, -34.22202116092960011 ) ) ;
#74611=CARTESIAN_POINT ( 'NONE',  ( -75.17510521376654253, -49.90938227346595113, 129.2199156371341360 ) ) ;
#74613=CARTESIAN_POINT ( 'NONE',  ( 57.26188992556405566, -30.00000000000000355, 83.64747613098029433 ) ) ;
#74615=CARTESIAN_POINT ( 'NONE',  ( 94.74039510923110186, -57.67204590878498749, 29.85737974855511112 ) ) ;
#74637=CARTESIAN_POINT ( 'NONE',  ( 30.11862666518024767, -46.43205139143292826, 34.40975861721332762 ) ) ;
#74648=CARTESIAN_POINT ( 'NONE',  ( 92.56322867397322796, -59.99999999999999289, -10.69608963466881235 ) ) ;
#74661=CARTESIAN_POINT ( 'NONE',  ( 82.81677989675817741, -37.85377912558440983, 1.740399077028625063 ) ) ;
#74668=DIRECTION ( 'NONE',  ( -0.000000000000000000, -1.000000000000000000, -0.000000000000000000 ) ) ;
#74669=CARTESIAN_POINT ( 'NONE',  ( -81.02582043684626001, -38.83538064993233263, 194.6489687308902887 ) ) ;
#74672=CARTESIAN_POINT ( 'NONE',  ( -31.86600978156343444, -60.00000000000000000, 37.52812459344517748 ) ) ;
#74674=CARTESIAN_POINT ( 'NONE',  ( 63.36932946075098272, -60.33828791889990129, 92.29599462647620101 ) ) ;
#74682=CARTESIAN_POINT ( 'NONE',  ( -113.9602498558271719, -57.67115345197749576, 163.9892394128282262 ) ) ;
#74685=CARTESIAN_POINT ( 'NONE',  ( 101.8543654623573929, -37.84848643670019896, 184.8799554269737371 ) ) ;
#74702=CARTESIAN_POINT ( 'NONE',  ( -94.11789465525937715, -29.99999999999999289, 191.2872302807874689 ) ) ;
#74707=CARTESIAN_POINT ( 'NONE',  ( 62.06629429558737598, -57.67807194442349328, 114.8863211712005210 ) ) ;
#74709=DIRECTION ( 'NONE',  ( 1.871721906610600077E-16, 0.000000000000000000, -1.000000000000000000 ) ) ;
#74711=CARTESIAN_POINT ( 'NONE',  ( 23.88087707229235335, -27.28680826393994607, -38.40335539918089580 ) ) ;
#74714=CARTESIAN_POINT ( 'NONE',  ( -29.24377091299251674, -60.00000000000000000, 42.67557265589431381 ) ) ;
#74717=CARTESIAN_POINT ( 'NONE',  ( -87.17749325152986728, -39.07517086902483072, 189.3868324704938573 ) ) ;
#74720=CARTESIAN_POINT ( 'NONE',  ( -7.006332439432221726, -22.06780448926463123, 27.55795484604703560 ) ) ;
#74735=CARTESIAN_POINT ( 'NONE',  ( 103.8765618273974951, -14.21045842199444209, 137.3601107225250360 ) ) ;
#74758=CARTESIAN_POINT ( 'NONE',  ( 102.0894480219289591, -59.99999999999998579, 201.1080374328564915 ) ) ;
#74759=CARTESIAN_POINT ( 'NONE',  ( -100.5643661290868209, -60.00000000000009237, 204.3458358344470582 ) ) ;
#74760=CARTESIAN_POINT ( 'NONE',  ( 13.42259877889314801, -35.99176036207357754, 29.96878892533495886 ) ) ;
#74764=CARTESIAN_POINT ( 'NONE',  ( -40.33367101206530947, -42.97933796220600300, 39.77954886268002355 ) ) ;
#74766=ORIENTED_EDGE ( 'NONE', *, *, #5143, .T. ) ;
#74767=CARTESIAN_POINT ( 'NONE',  ( -21.88880945939638778, -4.285714285714296246, 12.64023069600373717 ) ) ;
#74777=CARTESIAN_POINT ( 'NONE',  ( 71.80342808059910453, -30.00000000000000000, -19.71766482350837535 ) ) ;
#74783=CARTESIAN_POINT ( 'NONE',  ( 82.12584806139965110, -30.00000000000000000, 35.18806641379789824 ) ) ;
#74798=CARTESIAN_POINT ( 'NONE',  ( 76.76261672097879796, -38.43742884780580482, 183.2131921944575765 ) ) ;
#74820=CARTESIAN_POINT ( 'NONE',  ( 84.39583363381976255, -57.44525944421299357, 191.2968279531777398 ) ) ;
#74824=CARTESIAN_POINT ( 'NONE',  ( 91.48089852627707330, -57.66238869088599728, -20.18956347066234258 ) ) ;
#74828=CARTESIAN_POINT ( 'NONE',  ( -80.99455166116037219, -30.00000000000000711, 4.108193232890078761 ) ) ;
#74841=CARTESIAN_POINT ( 'NONE',  ( 71.80342808059909032, -30.00000000000000000, -19.71766482350836469 ) ) ;
#74843=ORIENTED_EDGE ( 'NONE', *, *, #94998, .F. ) ;
#74846=CARTESIAN_POINT ( 'NONE',  ( -52.81788617984520329, -28.08527092621403298, -27.21337244879998707 ) ) ;
#74852=ORIENTED_EDGE ( 'NONE', *, *, #80100, .F. ) ;
#74853=DIRECTION ( 'NONE',  ( -0.000000000000000000, -1.000000000000000000, -0.000000000000000000 ) ) ;
#74856=CARTESIAN_POINT ( 'NONE',  ( -18.14215405046660834, -60.00000000000000000, -41.96107740640177042 ) ) ;
#74859=CARTESIAN_POINT ( 'NONE',  ( 101.7724625413487018, -52.72604442183713758, 192.4186900641388434 ) ) ;
#74861=CARTESIAN_POINT ( 'NONE',  ( -0.01431428620034891179, -57.67120202577072519, -44.61186648040676772 ) ) ;
#74869=ORIENTED_EDGE ( 'NONE', *, *, #12261, .T. ) ;
#74874=CARTESIAN_POINT ( 'NONE',  ( 1.494050070974696619E-08, -60.00000000000000711, -44.99999999996101252 ) ) ;
#74879=CARTESIAN_POINT ( 'NONE',  ( -86.74711523299461646, -14.21045842199446518, 20.03206905870895227 ) ) ;
#74882=CARTESIAN_POINT ( 'NONE',  ( -50.52096995421375425, -49.90828412712392748, 55.20216876667482353 ) ) ;
#74893=CARTESIAN_POINT ( 'NONE',  ( 101.8192011966949337, -38.44775644747127075, 199.7746753136944449 ) ) ;
#74900=CARTESIAN_POINT ( 'NONE',  ( 91.51571527023273234, -30.00000000000001066, 190.6995551984874737 ) ) ;
#74907=CARTESIAN_POINT ( 'NONE',  ( 52.40231891019367083, -53.37153954349100360, 60.21125311485567977 ) ) ;
#74911=CARTESIAN_POINT ( 'NONE',  ( -99.53716699256776224, -38.35579409513464100, 85.73697495571477134 ) ) ;
#74914=CARTESIAN_POINT ( 'NONE',  ( 98.49355459790156431, -38.35583652005738742, 79.56885252902853267 ) ) ;
#74916=CARTESIAN_POINT ( 'NONE',  ( 91.54334141914280565, -37.84851935321219685, 87.62289096787682752 ) ) ;
#74922=CARTESIAN_POINT ( 'NONE',  ( 73.95865299267170201, -59.99999999999999289, 171.8011999975828417 ) ) ;
#74923=CARTESIAN_POINT ( 'NONE',  ( -2.500000000000001332, -15.46059980043578541, 23.70577374505222679 ) ) ;
#74927=CARTESIAN_POINT ( 'NONE',  ( 62.44672187089501847, -42.95944451888637161, 80.58943253863333211 ) ) ;
#74933=CARTESIAN_POINT ( 'NONE',  ( -75.43382409620862461, -30.00000000032916958, 160.3244271219596726 ) ) ;
#74941=B_SPLINE_CURVE_WITH_KNOTS ( 'NONE', 3,
 ( #77179, #58882, #43219, #11354, #76102, #18433 ),
 .UNSPECIFIED., .F., .F.,
 ( 4, 2, 4 ),
 ( 2.322283588913139083E-15, 0.01115492851740942232, 0.02230985703481652010 ),
 .UNSPECIFIED. ) ;
#74944=CARTESIAN_POINT ( 'NONE',  ( 83.96313902567902687, -39.44727629013741677, 178.0741200447442054 ) ) ;
#74953=CARTESIAN_POINT ( 'NONE',  ( -13.94654863431429348, -23.74387561856928031, -38.53487845396338685 ) ) ;
#74956=CARTESIAN_POINT ( 'NONE',  ( 53.11837506377438700, -60.00000000000000711, 79.96834070773113012 ) ) ;
#74958=CARTESIAN_POINT ( 'NONE',  ( 9.531068631029500082, -13.65597988659789763, 31.91744325619306366 ) ) ;
#74959=CARTESIAN_POINT ( 'NONE',  ( -16.64300274584347861, -23.63378944864288300, 36.18542074223226734 ) ) ;
#74975=CARTESIAN_POINT ( 'NONE',  ( 38.30684875469531647, -47.40885643735987998, -31.93458248487312545 ) ) ;
#74982=CARTESIAN_POINT ( 'NONE',  ( -102.3610540385565173, -59.99999999999999289, 94.85075420443190808 ) ) ;
#74989=CARTESIAN_POINT ( 'NONE',  ( -80.94085204086121621, -60.50534541559768797, 182.8664948990503660 ) ) ;
#75006=CARTESIAN_POINT ( 'NONE',  ( 108.4360931436784767, -30.00000000000001066, 186.7338794867829677 ) ) ;
#75008=CARTESIAN_POINT ( 'NONE',  ( -114.5769593907454862, -59.99999999999998579, 170.6727965893586827 ) ) ;
#75009=CARTESIAN_POINT ( 'NONE',  ( -59.01117578513747475, -39.49325923892655510, 69.67093582982462863 ) ) ;
#75012=CARTESIAN_POINT ( 'NONE',  ( 106.9295305114262931, -59.99999999999999289, 107.3648086918558420 ) ) ;
#75014=CARTESIAN_POINT ( 'NONE',  ( 3.963954421596001421, -18.58606326360312266, 26.98072944107077831 ) ) ;
#75015=CARTESIAN_POINT ( 'NONE',  ( -101.5623509475985173, -45.26550195618241901, 142.1330721071399239 ) ) ;
#75019=DIRECTION ( 'NONE',  ( 1.871721906610600077E-16, 0.000000000000000000, -1.000000000000000000 ) ) ;
#75021=CARTESIAN_POINT ( 'NONE',  ( -26.66627763802065232, -60.00000000000002842, 41.62965253161740264 ) ) ;
#75032=CARTESIAN_POINT ( 'NONE',  ( 88.95618763265999007, -60.00000000000002842, 47.35786141365969115 ) ) ;
#75033=CARTESIAN_POINT ( 'NONE',  ( -30.11868724977495759, -46.43670190743181792, 34.41063938579866033 ) ) ;
#75035=CARTESIAN_POINT ( 'NONE',  ( 44.95488294866025569, -53.34550232067736886, 47.31495729669310180 ) ) ;
#75039=CARTESIAN_POINT ( 'NONE',  ( -80.51573996916087594, -38.81441202086065090, 193.8693134589343572 ) ) ;
#75043=CARTESIAN_POINT ( 'NONE',  ( 52.76369956428789720, -60.00000000000002132, 63.53480520484748695 ) ) ;
#75052=CARTESIAN_POINT ( 'NONE',  ( 110.2341470348194719, -60.00000000000000000, 145.3203655816352580 ) ) ;
#75061=CARTESIAN_POINT ( 'NONE',  ( -90.33647909625912575, -29.99999999999991473, 190.1235012576946986 ) ) ;
#75073=CARTESIAN_POINT ( 'NONE',  ( 85.45692222432249707, -18.59276221248585159, 159.4212664435137015 ) ) ;
#75105=CARTESIAN_POINT ( 'NONE',  ( 107.5561821168135879, -57.67122918346473170, 113.7335151422611972 ) ) ;
#75113=CARTESIAN_POINT ( 'NONE',  ( -86.21883104017021537, -60.00000000000000000, 200.6728299286499180 ) ) ;
#75120=CARTESIAN_POINT ( 'NONE',  ( -84.74688199002078193, -42.96560158919115224, 184.9204503371174155 ) ) ;
#75126=CARTESIAN_POINT ( 'NONE',  ( -83.16184401887252875, -37.80642310000339990, -3.564082901337037868 ) ) ;
#75135=CARTESIAN_POINT ( 'NONE',  ( 25.54731711030018815, -59.99999999999990763, 43.65505808401614019 ) ) ;
#75137=EDGE_CURVE ( 'NONE', #60348, #59296, #21095, .T. ) ;
#75138=CARTESIAN_POINT ( 'NONE',  ( 32.64290048136811606, -14.21045842199427867, -35.33280650708731230 ) ) ;
#75139=CARTESIAN_POINT ( 'NONE',  ( -67.07628553758745227, -42.96253981622765394, 94.37277177135563022 ) ) ;
#75141=CARTESIAN_POINT ( 'NONE',  ( 69.92546618954501980, -29.99999999999995026, 127.5380661880360975 ) ) ;
#75143=CARTESIAN_POINT ( 'NONE',  ( 94.60551969766011382, -57.65569557003564682, -10.10694943204270047 ) ) ;
#75158=CARTESIAN_POINT ( 'NONE',  ( 25.22241582816893057, -4.285714285714295357, -1.650803255657548707 ) ) ;
#75166=CARTESIAN_POINT ( 'NONE',  ( 31.99605376666647771, -46.43077180847059537, 35.16619386691120752 ) ) ;
#75179=CARTESIAN_POINT ( 'NONE',  ( 80.24245568983633348, -60.00000000000000711, -27.79638001884161014 ) ) ;
#75193=CARTESIAN_POINT ( 'NONE',  ( 86.65316178196621877, -60.14505102782934642, 0.2230932978307594572 ) ) ;
#75209=CARTESIAN_POINT ( 'NONE',  ( 71.21928858210435465, -36.01210335758921133, 103.8020605858352212 ) ) ;
#75215=CARTESIAN_POINT ( 'NONE',  ( -94.22037892716120666, -57.65324192061454056, -13.00879341737615569 ) ) ;
#75218=CARTESIAN_POINT ( 'NONE',  ( 103.0706911096362717, -45.28272344628067714, 185.1160168883092183 ) ) ;
#75235=CARTESIAN_POINT ( 'NONE',  ( -84.36810463635728752, -30.00000000000000000, 164.3467819408754451 ) ) ;
#75240=CARTESIAN_POINT ( 'NONE',  ( 72.42338011058984648, -57.66707912199269970, 176.2281522364783655 ) ) ;
#75243=CARTESIAN_POINT ( 'NONE',  ( 6.366465994463423428, -21.85545340215044519, -38.54589836641859080 ) ) ;
#75246=CARTESIAN_POINT ( 'NONE',  ( -32.89843394316242353, -59.99999999999999289, 44.77189468774703585 ) ) ;
#75250=CARTESIAN_POINT ( 'NONE',  ( -86.21536416698982919, -35.54068135687334262, 186.1489417679863152 ) ) ;
#75253=CARTESIAN_POINT ( 'NONE',  ( -6.078692300985167662, -35.99430252327623947, 29.87896141239675174 ) ) ;
#75255=CARTESIAN_POINT ( 'NONE',  ( 86.73932400000002474, -41.70651791337262893, 189.2637588004315319 ) ) ;
#75270=CARTESIAN_POINT ( 'NONE',  ( 106.8235258757864869, -14.21045842199432307, 178.1026719309843429 ) ) ;
#75271=CARTESIAN_POINT ( 'NONE',  ( -84.55966185417285885, -22.11373329182813308, 156.8083849470275197 ) ) ;
#75276=FACE_OUTER_BOUND ( 'NONE', #61265, .T. ) ;
#75296=CARTESIAN_POINT ( 'NONE',  ( 111.2971332976971581, -59.99999999999998579, 155.0290638565942629 ) ) ;
#75297=CARTESIAN_POINT ( 'NONE',  ( -101.1248876217780719, -29.99999999999996803, 198.7487848662925387 ) ) ;
#75298=CARTESIAN_POINT ( 'NONE',  ( 18.55641751059849298, -18.59015957681733866, 27.35011673974152657 ) ) ;
#75301=CARTESIAN_POINT ( 'NONE',  ( -41.90450118112109124, -32.61544904257455357, 38.71841112228458570 ) ) ;
#75315=CARTESIAN_POINT ( 'NONE',  ( 81.58172074487495706, -30.00000000000000000, -7.858416217283744842 ) ) ;
#75320=CARTESIAN_POINT ( 'NONE',  ( 86.61791453296140730, -30.00000000000000000, 68.11649954288937181 ) ) ;
#75335=CARTESIAN_POINT ( 'NONE',  ( 74.24703944025202418, -38.32801400578732398, 162.5046052861644625 ) ) ;
#75359=CARTESIAN_POINT ( 'NONE',  ( 85.23953769841214978, -46.56070485338828036, 188.0803264966071140 ) ) ;
#75363=CARTESIAN_POINT ( 'NONE',  ( 94.14372550659786043, -57.65224881985284355, -13.67576374388242044 ) ) ;
#75369=CARTESIAN_POINT ( 'NONE',  ( -81.39596208340545047, -30.00000000000000711, -1.917334220413669188 ) ) ;
#75383=CARTESIAN_POINT ( 'NONE',  ( 13.46238992380946442, -16.89357091335954664, -34.49996823829238934 ) ) ;
#75386=CARTESIAN_POINT ( 'NONE',  ( -21.78122564462103483, -56.88112741419036666, 34.12320410153837713 ) ) ;
#75392=CARTESIAN_POINT ( 'NONE',  ( -62.37515747485122830, -29.51886346143869844, -24.10950783783387763 ) ) ;
#75395=CARTESIAN_POINT ( 'NONE',  ( -71.32987062739258022, -47.40883850356869544, -23.55053093366642614 ) ) ;
#75402=CARTESIAN_POINT ( 'NONE',  ( -71.33171024911513314, -59.99999999999999289, -32.04526279259148680 ) ) ;
#75406=CARTESIAN_POINT ( 'NONE',  ( 102.3341614162330728, -60.19240241467774410, 193.7986361862069771 ) ) ;
#75424=CARTESIAN_POINT ( 'NONE',  ( -52.60809588292248407, -57.67627119646954981, 84.38067992663381744 ) ) ;
#75428=VECTOR ( 'NONE', #18379, 1000.000000000000000 ) ;
#75430=CARTESIAN_POINT ( 'NONE',  ( -87.30967359867977962, -14.21045842199447229, 28.19474181966119275 ) ) ;
#75432=CARTESIAN_POINT ( 'NONE',  ( -50.83579864079804622, -56.83981948626792757, 58.27881635844277497 ) ) ;
#75436=CARTESIAN_POINT ( 'NONE',  ( -94.29814206750670280, -37.67726954591325494, 192.9876237923781730 ) ) ;
#75442=CARTESIAN_POINT ( 'NONE',  ( 102.0795561180093358, -38.44427582207561045, 199.6449008483751584 ) ) ;
#75447=CARTESIAN_POINT ( 'NONE',  ( 87.64837357284261543, -29.99999999999999289, 185.8567712199668449 ) ) ;
#75453=CARTESIAN_POINT ( 'NONE',  ( 53.14594722454222619, -32.56895425823870482, 53.87332140664673830 ) ) ;
#75457=CARTESIAN_POINT ( 'NONE',  ( -90.65532507562996045, -38.34410233969092019, 9.200892734119188177 ) ) ;
#75461=CARTESIAN_POINT ( 'NONE',  ( 1.405425595346621037E-06, -60.00000000000000000, -42.63907915653317104 ) ) ;
#75462=CARTESIAN_POINT ( 'NONE',  ( 108.2517954523928267, -38.35773579516970955, 192.2690374787310077 ) ) ;
#75464=CARTESIAN_POINT ( 'NONE',  ( 87.44082029972511805, -60.14831745977613764, 34.29351510052578789 ) ) ;
#75470=CARTESIAN_POINT ( 'NONE',  ( -2.499999999999999112, -9.944422831621025693, 19.25618869330389060 ) ) ;
#75473=CARTESIAN_POINT ( 'NONE',  ( 61.25147495611365400, -39.48591661841823708, 75.53939267858287110 ) ) ;
#75484=CARTESIAN_POINT ( 'NONE',  ( 13.11091740201548284, -14.49516756936109374, 31.73904586483237367 ) ) ;
#75487=CARTESIAN_POINT ( 'NONE',  ( 83.69513508649264111, -46.54032163251969223, 183.4101359782732743 ) ) ;
#75490=ORIENTED_EDGE ( 'NONE', *, *, #81811, .T. ) ;
#75495=CARTESIAN_POINT ( 'NONE',  ( -27.89011194084447354, -28.79345919575957424, -38.26979258636463044 ) ) ;
#75497=CARTESIAN_POINT ( 'NONE',  ( 43.79854525262764753, -60.00000000000000000, 58.31034945498838340 ) ) ;
#75501=CARTESIAN_POINT ( 'NONE',  ( 10.41373344803106171, -13.87117582527802817, 31.87275171603477730 ) ) ;
#75504=CARTESIAN_POINT ( 'NONE',  ( -28.52852425489989585, -31.45698047945067444, 39.78088916245284423 ) ) ;
#75513=CARTESIAN_POINT ( 'NONE',  ( 2.054367089437916238, -21.36431346866936920, -38.55161551619058002 ) ) ;
#75519=CARTESIAN_POINT ( 'NONE',  ( 53.90248938814917778, -47.40883931113200589, -29.08432012930690647 ) ) ;
#75529=CARTESIAN_POINT ( 'NONE',  ( -10.00000000000000000, 0.000000000000000000, 10.00000000000000178 ) ) ;
#75530=CARTESIAN_POINT ( 'NONE',  ( -100.9373344200095772, -60.00000000000000000, 86.53253016253701446 ) ) ;
#75538=CARTESIAN_POINT ( 'NONE',  ( -82.71515938753303487, -42.97701944449982392, 172.7384417419264082 ) ) ;
#75541=ORIENTED_EDGE ( 'NONE', *, *, #4191, .T. ) ;
#75553=SURFACE_SIDE_STYLE ('',( #27050 ) ) ;
#75556=CARTESIAN_POINT ( 'NONE',  ( 92.03798523278891253, -30.00000000000002842, 46.84723268580137301 ) ) ;
#75558=CARTESIAN_POINT ( 'NONE',  ( -72.58684158890253002, -59.99999999999995026, 181.3884362157535008 ) ) ;
#75559=CARTESIAN_POINT ( 'NONE',  ( -58.21460221941013202, -39.49442887122282997, 67.71575742886867033 ) ) ;
#75562=CARTESIAN_POINT ( 'NONE',  ( 77.24101806708192441, -59.99999999999518252, -32.07091152847338122 ) ) ;
#75564=CARTESIAN_POINT ( 'NONE',  ( 7.180584945291298204, -46.43466603162036677, 31.61912980851609589 ) ) ;
#75565=CARTESIAN_POINT ( 'NONE',  ( -103.1989685349693673, -52.71063798620885166, 189.5257644198029539 ) ) ;
#75566=FACE_OUTER_BOUND ( 'NONE', #22775, .T. ) ;
#75572=CARTESIAN_POINT ( 'NONE',  ( -39.86639569183807907, -59.99999999999998579, 51.86916670227435588 ) ) ;
#75576=CARTESIAN_POINT ( 'NONE',  ( 16.14668631625571393, -0.000000000000000000, 5.483261958891903376 ) ) ;
#75582=CARTESIAN_POINT ( 'NONE',  ( 99.13158141131964385, -59.99999999999998579, 109.9887192217465213 ) ) ;
#75583=CARTESIAN_POINT ( 'NONE',  ( -29.95191136813465604, -18.65114050358700837, 29.35552943215963850 ) ) ;
#75585=CARTESIAN_POINT ( 'NONE',  ( 44.80321014283884296, -42.98249604127523327, 44.34580923176882550 ) ) ;
#75589=CARTESIAN_POINT ( 'NONE',  ( -76.83632878065965599, -38.44263010941451597, 183.5527664238933596 ) ) ;
#75594=CARTESIAN_POINT ( 'NONE',  ( 79.51214466678966630, -60.00000000000007105, 169.4709273215115388 ) ) ;
#75602=CARTESIAN_POINT ( 'NONE',  ( 106.3525110532974480, -60.00000000000000000, 118.5997609402804756 ) ) ;
#75605=EDGE_CURVE ( 'NONE', #57621, #30532, #23965, .T. ) ;
#75607=CARTESIAN_POINT ( 'NONE',  ( -100.9483554910953416, -29.99999999999999289, 178.8210981605607799 ) ) ;
#75619=CARTESIAN_POINT ( 'NONE',  ( 80.00145041154991077, -60.36562354243974227, 175.0908152758545668 ) ) ;
#75634=CARTESIAN_POINT ( 'NONE',  ( 87.15768292724222022, -24.32275648668401047, 187.0112092941248534 ) ) ;
#75638=LINE ( 'NONE', #18497, #71541 ) ;
#75655=CARTESIAN_POINT ( 'NONE',  ( -87.15574825653149560, -60.00000000000000711, 201.0783104021778342 ) ) ;
#75661=CARTESIAN_POINT ( 'NONE',  ( -85.48278714503372555, -32.15310639930356018, 180.9904824015285385 ) ) ;
#75668=CARTESIAN_POINT ( 'NONE',  ( -84.03992301111506436, -45.26188587547530773, -11.64691007556465507 ) ) ;
#75678=CARTESIAN_POINT ( 'NONE',  ( 57.89978660429063240, -59.99999999999999289, 101.6248911977562699 ) ) ;
#75681=CARTESIAN_POINT ( 'NONE',  ( -65.68019474265784652, -30.00000000000001776, -31.25134080541240422 ) ) ;
#75682=CARTESIAN_POINT ( 'NONE',  ( -74.82224136490378896, -42.96559528526920246, 122.4759379343339134 ) ) ;
#75684=CARTESIAN_POINT ( 'NONE',  ( 69.27313422356952799, -59.99999999999999289, 151.6321682696899984 ) ) ;
#75686=CARTESIAN_POINT ( 'NONE',  ( 42.26132763977452100, -59.99999999999998579, 60.38387368011249379 ) ) ;
#75710=CARTESIAN_POINT ( 'NONE',  ( 31.50514675153943855, -25.60841695546642782, 31.14698023900106350 ) ) ;
#75726=CARTESIAN_POINT ( 'NONE',  ( 91.76163772444834876, -60.00000000000002132, -14.81080705115953577 ) ) ;
#75739=CARTESIAN_POINT ( 'NONE',  ( 86.65522219368004642, -60.23071133352890882, -11.83452115418482897 ) ) ;
#75751=CARTESIAN_POINT ( 'NONE',  ( 74.27602980505658081, -60.31745848623394579, 133.2367107689713066 ) ) ;
#75756=CARTESIAN_POINT ( 'NONE',  ( -94.60030117187078247, -57.66721437216608592, -3.115894729640209526 ) ) ;
#75764=CARTESIAN_POINT ( 'NONE',  ( 103.9999019992000342, -45.28271188782171919, 174.9196668792254172 ) ) ;
#75782=CARTESIAN_POINT ( 'NONE',  ( -86.17540505562507747, -30.00000000000000355, 179.7358132287471904 ) ) ;
#75786=CARTESIAN_POINT ( 'NONE',  ( 72.44228326075131008, -57.66666666020200438, 176.4071323493450620 ) ) ;
#75790=CARTESIAN_POINT ( 'NONE',  ( 41.29501498917274205, -33.32507052358980815, -37.31402353058274457 ) ) ;
#75793=CARTESIAN_POINT ( 'NONE',  ( -47.80564746871677073, -60.00000000000000000, 66.57118741872818646 ) ) ;
#75797=CARTESIAN_POINT ( 'NONE',  ( -86.38853201505308732, -17.19521753330991487, 181.4521117774834522 ) ) ;
#75800=CARTESIAN_POINT ( 'NONE',  ( -0.9975258024604992668, -32.51280156655929687, 29.30845022069559391 ) ) ;
#75815=CARTESIAN_POINT ( 'NONE',  ( 114.2222497212829495, -60.00000000000000000, 162.1251737369585726 ) ) ;
#75816=CARTESIAN_POINT ( 'NONE',  ( -78.76406686447538164, -60.31995527695700332, 162.6514910654201742 ) ) ;
#75823=CARTESIAN_POINT ( 'NONE',  ( 53.08934989192464826, -30.00000000000000000, 52.21148837440648549 ) ) ;
#75836=CARTESIAN_POINT ( 'NONE',  ( 105.6057910669374422, -60.00000000000002842, 198.6986277786460562 ) ) ;
#75837=CARTESIAN_POINT ( 'NONE',  ( -72.58684158890253002, -59.99999999999995026, 181.3884362157535008 ) ) ;
#75838=CARTESIAN_POINT ( 'NONE',  ( 20.85967906329956989, -22.07355929854739074, 28.15013364495181492 ) ) ;
#75839=PRODUCT_DEFINITION_CONTEXT ( 'detailed design', #21797, 'design' ) ;
#75842=AXIS2_PLACEMENT_3D ( 'NONE', #49368, #41291, #74709 ) ;
#75844=CARTESIAN_POINT ( 'NONE',  ( -40.03125687598254956, -36.06455305613715012, 37.97989534578266557 ) ) ;
#75848=DIRECTION ( 'NONE',  ( 0.000000000000000000, 0.000000000000000000, 1.000000000000000000 ) ) ;
#75858=CARTESIAN_POINT ( 'NONE',  ( 80.84629483389447557, -30.00000000000000000, 18.24997580178345657 ) ) ;
#75862=CARTESIAN_POINT ( 'NONE',  ( 83.28217346054918835, -30.00000000000000000, 45.15196306360270739 ) ) ;
#75866=ORIENTED_EDGE ( 'NONE', *, *, #62967, .F. ) ;
#75877=CARTESIAN_POINT ( 'NONE',  ( 75.76114055863986607, -38.36421291546669465, 176.4736164422936895 ) ) ;
#75900=CARTESIAN_POINT ( 'NONE',  ( 85.56644655141936084, -39.27954688708853581, 185.6724605245946407 ) ) ;
#75903=CARTESIAN_POINT ( 'NONE',  ( 11.22734410610833145, -57.67099979598874882, -44.34944396839206604 ) ) ;
#75908=CARTESIAN_POINT ( 'NONE',  ( -93.78806885821806816, -30.00000000000000000, 110.7017565295546859 ) ) ;
#75917=CARTESIAN_POINT ( 'NONE',  ( -5.791862111366527621, -19.38500976431717149, 27.11074324704184235 ) ) ;
#75922=CARTESIAN_POINT ( 'NONE',  ( 59.06535827412803030, -29.12722259196854679, -25.29134694357246005 ) ) ;
#75923=CARTESIAN_POINT ( 'NONE',  ( -25.60069973378831776, -60.35510020081476767, 35.42683911583728218 ) ) ;
#75929=CARTESIAN_POINT ( 'NONE',  ( -62.95843149965692476, -29.57568813394581042, -23.88512804728211947 ) ) ;
#75932=CARTESIAN_POINT ( 'NONE',  ( -70.79846966789600060, -21.77035841021276852, -19.10124222137329753 ) ) ;
#75945=CARTESIAN_POINT ( 'NONE',  ( 100.6710202544833521, -52.75082832554577550, 193.6882445870123206 ) ) ;
#75953=DIRECTION ( 'NONE',  ( 0.000000000000000000, 1.000000000000000000, 0.000000000000000000 ) ) ;
#75959=CARTESIAN_POINT ( 'NONE',  ( -56.21986590610479340, -57.67573674557218766, 94.99882904018191709 ) ) ;
#75963=CARTESIAN_POINT ( 'NONE',  ( -94.33288967953484416, -60.00000000000004263, 18.12646456170910625 ) ) ;
#75965=CARTESIAN_POINT ( 'NONE',  ( -50.78802596981626039, -39.51418944723420168, 52.08018486103266298 ) ) ;
#75976=CARTESIAN_POINT ( 'NONE',  ( 79.09173631814320515, -38.70095664295953242, 191.1748961264769093 ) ) ;
#75980=CARTESIAN_POINT ( 'NONE',  ( 92.89497987163872494, -30.00000000000000355, 191.0944421695535027 ) ) ;
#75986=CARTESIAN_POINT ( 'NONE',  ( 51.42960542931152901, -36.04405707132738712, 52.00941032663666874 ) ) ;
#75990=CARTESIAN_POINT ( 'NONE',  ( -90.39311681537722620, -38.40169232996368720, -14.90399125691173587 ) ) ;
#75993=CARTESIAN_POINT ( 'NONE',  ( 106.9399123034084766, -38.36500875113367925, 194.9488307172588009 ) ) ;
#75995=CARTESIAN_POINT ( 'NONE',  ( 89.89766059151314437, -37.84859365328757974, 78.06384706745211588 ) ) ;
#75998=FACE_OUTER_BOUND ( 'NONE', #47921, .T. ) ;
#76003=EDGE_LOOP ( 'NONE', ( #30770, #68742, #10435, #49124 ) ) ;
#76012=CARTESIAN_POINT ( 'NONE',  ( 38.66969219575074845, -25.75017430485813108, 35.13927043512571657 ) ) ;
#76017=CARTESIAN_POINT ( 'NONE',  ( 82.78694254221720428, -50.04262524950087965, 182.2087751002529501 ) ) ;
#76026=CARTESIAN_POINT ( 'NONE',  ( -18.63186175455728844, -25.33939609445413410, -38.50114773520279243 ) ) ;
#76030=CARTESIAN_POINT ( 'NONE',  ( 53.68073265722826193, -60.00000000000000711, 81.53482892392325709 ) ) ;
#76031=CARTESIAN_POINT ( 'NONE',  ( 27.25585338856197737, -30.58637391271707173, 39.18084608107302103 ) ) ;
#76033=CARTESIAN_POINT ( 'NONE',  ( 5.437019438593272191, -12.93285032667489709, 32.09035593251934415 ) ) ;
#76034=CARTESIAN_POINT ( 'NONE',  ( -27.50278574530640441, -30.75557938056827467, 39.29189916433056595 ) ) ;
#76046=CARTESIAN_POINT ( 'NONE',  ( 34.25937177855836069, -21.77016779706914917, -28.20208921661981449 ) ) ;
#76056=CARTESIAN_POINT ( 'NONE',  ( -100.8737896469964426, -60.00000000000000000, 86.15980893726860756 ) ) ;
#76062=CARTESIAN_POINT ( 'NONE',  ( -85.99911114356302733, -18.43252915325882313, 165.6345971928553240 ) ) ;
#76075=( NAMED_UNIT ( * ) SI_UNIT ( $, .STERADIAN. ) SOLID_ANGLE_UNIT ( ) );
#76080=CARTESIAN_POINT ( 'NONE',  ( -97.53417455291598515, -56.34874176541392643, 195.8863760079639462 ) ) ;
#76082=CARTESIAN_POINT ( 'NONE',  ( 90.16383085397569630, -14.21045842199434084, 52.56522323202336366 ) ) ;
#76084=CARTESIAN_POINT ( 'NONE',  ( -98.15060533238310825, -14.21045842199422715, 197.6136055373540614 ) ) ;
#76085=CARTESIAN_POINT ( 'NONE',  ( -59.17778066530962633, -49.91509818790471087, 74.96796009585710863 ) ) ;
#76089=CARTESIAN_POINT ( 'NONE',  ( -102.1119726963908079, -37.82064582844866152, 183.3968591677531208 ) ) ;
#76094=EDGE_LOOP ( 'NONE', ( #1010, #68441, #78582, #4549 ) ) ;
#76096=CARTESIAN_POINT ( 'NONE',  ( -74.06050393588230918, -60.00000000000000000, 172.8376900993954735 ) ) ;
#76102=CARTESIAN_POINT ( 'NONE',  ( 82.57687275821095341, -41.66704177847501001, -14.02669740995510494 ) ) ;
#76108=CARTESIAN_POINT ( 'NONE',  ( -30.76582839458128049, -60.33262561358965570, 37.12003127044696527 ) ) ;
#76112=CARTESIAN_POINT ( 'NONE',  ( 43.67629986226869221, -29.16024730390979869, 39.50635445105871923 ) ) ;
#76117=CARTESIAN_POINT ( 'NONE',  ( -86.44246846762395364, -38.61868829427960748, 199.2842396746591760 ) ) ;
#76119=CARTESIAN_POINT ( 'NONE',  ( 77.87040428542300674, -38.35599188746820687, -27.73370404319807037 ) ) ;
#76128=CARTESIAN_POINT ( 'NONE',  ( 109.7562981413315697, -59.99999999999999289, 141.5450222497400148 ) ) ;
#76133=CARTESIAN_POINT ( 'NONE',  ( -99.71302761529223346, -29.99999999999998224, 150.1575047744225913 ) ) ;
#76144=CARTESIAN_POINT ( 'NONE',  ( 83.49137038316719384, -32.53379486668217169, 163.2796185419070696 ) ) ;
#76175=CIRCLE ( 'NONE', #53779, 7.499999999992679633 ) ;
#76186=CARTESIAN_POINT ( 'NONE',  ( -77.98089275376243279, -60.00000000000000000, 192.8200721109930669 ) ) ;
#76191=CARTESIAN_POINT ( 'NONE',  ( -85.02386936141340357, -39.35437566379916063, 183.7573501001193961 ) ) ;
#76197=CARTESIAN_POINT ( 'NONE',  ( -84.01129673064754400, -45.26989356464081027, 2.482293978573416826 ) ) ;
#76205=CARTESIAN_POINT ( 'NONE',  ( 71.62958147348905413, -29.99999999999999645, 135.6714503744467493 ) ) ;
#76207=CARTESIAN_POINT ( 'NONE',  ( -80.19882167783929106, -30.00000000000005684, -24.77908391697505053 ) ) ;
#76208=CARTESIAN_POINT ( 'NONE',  ( -73.18360275706602636, -39.49101380701564068, 113.0608591253020876 ) ) ;
#76210=CARTESIAN_POINT ( 'NONE',  ( 67.91784306603950938, -14.21045842199442077, 108.3249851056250321 ) ) ;
#76212=CARTESIAN_POINT ( 'NONE',  ( 22.25033068898240174, -60.00000000000493827, 42.95758340851298840 ) ) ;
#76224=CARTESIAN_POINT ( 'NONE',  ( -52.24845625772812951, -60.00000000001954703, 84.50696348291317861 ) ) ;
#76227=CARTESIAN_POINT ( 'NONE',  ( -85.18896233714281152, -59.99999999999995737, -15.68185129854840554 ) ) ;
#76238=CARTESIAN_POINT ( 'NONE',  ( 33.15956608574755649, -56.83790991451342478, 37.61396027134895803 ) ) ;
#76239=CARTESIAN_POINT ( 'NONE',  ( 22.03900363279161567, -4.285714285712638016, 12.70248734011606828 ) ) ;
#76254=CARTESIAN_POINT ( 'NONE',  ( 90.46693666255114863, -59.99999999999999289, -18.03047012885635780 ) ) ;
#76261=CARTESIAN_POINT ( 'NONE',  ( -81.87262150750494527, -30.00000000000330402, 194.0511874815462079 ) ) ;
#76263=ORIENTED_EDGE ( 'NONE', *, *, #66304, .T. ) ;
#76267=CARTESIAN_POINT ( 'NONE',  ( 85.37367768935722268, -60.20197548581520408, -15.42114807968834889 ) ) ;
#76280=CARTESIAN_POINT ( 'NONE',  ( 74.51115553146181014, -22.12425664901256184, 106.6295879739541874 ) ) ;
#76285=CARTESIAN_POINT ( 'NONE',  ( -90.36739715925041594, -57.66608071200965213, -21.81949331871602382 ) ) ;
#76290=CARTESIAN_POINT ( 'NONE',  ( 105.2361638501777321, -52.71710886096133208, 175.0655424517120764 ) ) ;
#76305=CARTESIAN_POINT ( 'NONE',  ( -89.01444542118139225, -30.00000000000000711, 188.7229723381737756 ) ) ;
#76309=CARTESIAN_POINT ( 'NONE',  ( 80.41579346481609036, -57.50937429630823061, 199.2392246321336415 ) ) ;
#76313=CARTESIAN_POINT ( 'NONE',  ( 68.10834181227042450, -38.11564430089239863, -31.83369359602357918 ) ) ;
#76316=CARTESIAN_POINT ( 'NONE',  ( -38.80661513268031371, -59.99999999999999289, 50.49608698167829601 ) ) ;
#76318=CARTESIAN_POINT ( 'NONE',  ( -86.79595722784087286, -31.74947768238279977, 186.8232286397415862 ) ) ;
#76321=CARTESIAN_POINT ( 'NONE',  ( -3.991702196745004372, -25.54931392864318340, 28.14104528548392636 ) ) ;
#76336=CARTESIAN_POINT ( 'NONE',  ( 100.4059631369621570, -60.00000000000003553, 69.07260714096372567 ) ) ;
#76337=CARTESIAN_POINT ( 'NONE',  ( -83.25441183928721500, -18.68590906670072371, 143.1452550271331177 ) ) ;
#76341=CARTESIAN_POINT ( 'NONE',  ( 23.63580155301217189, -57.67366959424659711, 42.85678083413705508 ) ) ;
#76351=EDGE_CURVE ( 'NONE', #40837, #24456, #98471, .T. ) ;
#76357=CARTESIAN_POINT ( 'NONE',  ( -78.25705875637353870, -14.21045842199447939, 182.3370610225134953 ) ) ;
#76358=CARTESIAN_POINT ( 'NONE',  ( 21.41473547131232991, -42.95433426084449735, 31.73274252099677639 ) ) ;
#76362=CARTESIAN_POINT ( 'NONE',  ( -40.12004793384570434, -60.26222130539476041, 43.34212177527130194 ) ) ;
#76376=CARTESIAN_POINT ( 'NONE',  ( 99.27928464162405930, -30.00000000000000000, 188.1417282079006839 ) ) ;
#76381=CARTESIAN_POINT ( 'NONE',  ( 83.66451334722914623, -30.00000000000000711, 48.10376369561402754 ) ) ;
#76397=CARTESIAN_POINT ( 'NONE',  ( 75.45370944691039483, -38.35105784206446344, 173.7888497777023815 ) ) ;
#76422=CARTESIAN_POINT ( 'NONE',  ( 85.55340563104743978, -61.06305125096141495, 193.9660559021026813 ) ) ;
#76426=CARTESIAN_POINT ( 'NONE',  ( 61.19758744976927289, -57.67094294300110136, -37.37908601888510418 ) ) ;
#76430=CARTESIAN_POINT ( 'NONE',  ( -90.85589696943300453, -30.00000000000000711, 93.50266285681084355 ) ) ;
#76438=CARTESIAN_POINT ( 'NONE',  ( -8.966563029945419316, -20.28652515761861608, 27.26759621302640824 ) ) ;
#76444=CARTESIAN_POINT ( 'NONE',  ( 52.95862039844607239, -28.11919995386964644, -27.17888508974323614 ) ) ;
#76446=CARTESIAN_POINT ( 'NONE',  ( -24.40073486819268211, -25.56284969913130567, 29.25320355220248203 ) ) ;
#76450=CARTESIAN_POINT ( 'NONE',  ( -20.33180723614214358, -46.43912101697812744, 32.18596333272415677 ) ) ;
#76452=CARTESIAN_POINT ( 'NONE',  ( -48.68264843209982473, -27.19707998762441292, -28.31473230945048059 ) ) ;
#76465=CARTESIAN_POINT ( 'NONE',  ( 99.83641921256408125, -45.27153168086159241, 192.7518997590976539 ) ) ;
#76466=CARTESIAN_POINT ( 'NONE',  ( 19.65497437631472977, -25.11138553214667368, 28.50946425220601554 ) ) ;
#76469=ORIENTED_EDGE ( 'NONE', *, *, #12182, .F. ) ;
#76480=VECTOR ( 'NONE', #89024, 1000.000000000000000 ) ;
#76483=CARTESIAN_POINT ( 'NONE',  ( -83.34872437439757675, -59.99999999999513278, -28.64704504306356370 ) ) ;
#76487=CARTESIAN_POINT ( 'NONE',  ( -86.89976874444957389, -30.00000000000007105, -18.81729257278660583 ) ) ;
#76491=CARTESIAN_POINT ( 'NONE',  ( -50.66715319276153195, -18.73003936557022797, 44.89420085366170809 ) ) ;
#76501=CARTESIAN_POINT ( 'NONE',  ( 89.19545386432166367, -30.00000000004024159, 14.25136593696676179 ) ) ;
#76507=CARTESIAN_POINT ( 'NONE',  ( 89.77911554397552152, -29.99999999999999645, 189.6830308129038087 ) ) ;
#76514=CARTESIAN_POINT ( 'NONE',  ( 52.39836483974727344, -39.50506518785934418, 55.00803164924739974 ) ) ;
#76518=CARTESIAN_POINT ( 'NONE',  ( -87.73394717290364042, -38.36776824219355575, -19.93160110628211967 ) ) ;
#76520=CARTESIAN_POINT ( 'NONE',  ( 110.3445969107558824, -38.35603028189417785, 183.6558594675337872 ) ) ;
#76522=CARTESIAN_POINT ( 'NONE',  ( 87.30608338596761087, -45.28275021690784286, 53.23273715140581430 ) ) ;
#76540=PRESENTATION_STYLE_ASSIGNMENT (( #44196 ) ) ;
#76544=CARTESIAN_POINT ( 'NONE',  ( 85.66370408561847682, -25.20792820135650203, 174.6146224505659177 ) ) ;
#76548=CARTESIAN_POINT ( 'NONE',  ( -89.51184282953521176, -45.26536304831822122, 67.81581898571103295 ) ) ;
#76552=CARTESIAN_POINT ( 'NONE',  ( -27.80883096284195588, -28.76322849883876742, -38.27309149394403676 ) ) ;
#76556=CARTESIAN_POINT ( 'NONE',  ( 41.54280867975291613, -60.00000000000000711, 54.42080625159498197 ) ) ;
#76557=CARTESIAN_POINT ( 'NONE',  ( 30.67417392544069443, -32.89657424032979804, 40.97062061678585820 ) ) ;
#76559=CARTESIAN_POINT ( 'NONE',  ( 27.26803836058585517, -20.37211081801200052, 31.76419521842516858 ) ) ;
#76560=CARTESIAN_POINT ( 'NONE',  ( -27.47606363769024185, -30.73727070043888432, 39.27975643966717456 ) ) ;
#76575=CARTESIAN_POINT ( 'NONE',  ( 9.686630580550103176, -60.22816686990648805, -36.71166719284434521 ) ) ;
#76578=LINE ( 'NONE', #11845, #75428 ) ;
#76586=CARTESIAN_POINT ( 'NONE',  ( -94.20106335591412972, -60.00000000000000711, 42.96664062321771382 ) ) ;
#76596=CARTESIAN_POINT ( 'NONE',  ( -83.25572694177012067, -39.48114288256212490, 172.2748129000959239 ) ) ;
#76606=CARTESIAN_POINT ( 'NONE',  ( -112.4702214903622490, -57.67117150189849895, 147.0458187677821797 ) ) ;
#76612=CARTESIAN_POINT ( 'NONE',  ( 107.3070812967312833, -60.00000000000004263, 109.8435067956896063 ) ) ;
#76614=CARTESIAN_POINT ( 'NONE',  ( -71.28683113122063730, -60.00000000000007816, 168.6212938583825292 ) ) ;
#76615=CARTESIAN_POINT ( 'NONE',  ( -59.37701284200993967, -46.44061691160312222, 73.85501160776004781 ) ) ;
#76619=CARTESIAN_POINT ( 'NONE',  ( -104.3760552791074616, -52.71020495745255374, 184.8450785601530981 ) ) ;
#76625=CARTESIAN_POINT ( 'NONE',  ( -46.09484555436212361, -60.00000000000000000, 62.82384042436929406 ) ) ;
#76632=CARTESIAN_POINT ( 'NONE',  ( 2.083846472846741813E-15, -8.673617379884035472E-16, 17.01589776168603407 ) ) ;
#76640=CARTESIAN_POINT ( 'NONE',  ( -29.80762567245044181, -53.38692201229141432, 35.51366752434432073 ) ) ;
#76642=CARTESIAN_POINT ( 'NONE',  ( 45.35554677126504686, -25.70144366515250312, 40.33168379963065320 ) ) ;
#76645=CARTESIAN_POINT ( 'NONE',  ( -97.66009619792869501, -38.48092223747977414, 201.0359958989743348 ) ) ;
#76649=CARTESIAN_POINT ( 'NONE',  ( 80.86587616991319294, -60.00000000000004263, 181.8178842116407736 ) ) ;
#76656=CARTESIAN_POINT ( 'NONE',  ( 112.2398407305392283, -59.99999999999999289, 172.8131785719580478 ) ) ;
#76662=CARTESIAN_POINT ( 'NONE',  ( -78.22574516621017438, -30.00000000000003197, -15.67709204907202469 ) ) ;
#76664=( NAMED_UNIT ( * ) SI_UNIT ( $, .STERADIAN. ) SOLID_ANGLE_UNIT ( ) );
#76679=CARTESIAN_POINT ( 'NONE',  ( 84.05649254118333147, -22.13809807529134588, 152.7230919644917435 ) ) ;
#76693=CARTESIAN_POINT ( 'NONE',  ( 0.000000000000000000, 0.000000000000000000, 0.000000000000000000 ) ) ;
#76695=CARTESIAN_POINT ( 'NONE',  ( 86.90659302068790737, -24.33240570756411714, 186.0895709266965525 ) ) ;
#76716=CARTESIAN_POINT ( 'NONE',  ( -108.5008973690249263, -60.00000000000000000, 194.7175470961265091 ) ) ;
#76720=CARTESIAN_POINT ( 'NONE',  ( -84.42943966653459142, -42.97677127786843698, 183.7511723405210660 ) ) ;
#76728=CARTESIAN_POINT ( 'NONE',  ( -86.70007003831202042, -60.15181208265720869, -0.3940414372618840644 ) ) ;
#76736=CARTESIAN_POINT ( 'NONE',  ( 75.43375447319739635, -30.00000000000006395, 160.3035121353613306 ) ) ;
#76738=CARTESIAN_POINT ( 'NONE',  ( -89.98348853342757536, -29.99999999999992184, -2.848863062743723695 ) ) ;
#76739=CARTESIAN_POINT ( 'NONE',  ( -67.10393046265450323, -60.34011039881914940, 104.4197148593212745 ) ) ;
#76741=CARTESIAN_POINT ( 'NONE',  ( 78.42589391212746364, -14.21045842199428222, 185.4806485215488010 ) ) ;
#76743=CARTESIAN_POINT ( 'NONE',  ( 61.10636555069866205, -57.67115655538963637, -37.40363315934200727 ) ) ;
#76756=CARTESIAN_POINT ( 'NONE',  ( -68.05622514284931412, -60.00000000002930278, 143.8904575097929524 ) ) ;
#76771=CARTESIAN_POINT ( 'NONE',  ( 32.34925479044390073, -53.37185119530935395, 36.58498206500041050 ) ) ;
#76772=CARTESIAN_POINT ( 'NONE',  ( -13.66642973271509831, 3.860411657743955287E-12, 17.78317311657911404 ) ) ;
#76783=CARTESIAN_POINT ( 'NONE',  ( 91.87114596397952937, -59.99999999999999289, 10.38462266140972901 ) ) ;
#76790=CARTESIAN_POINT ( 'NONE',  ( -82.19042405889051395, -29.99999999993295319, 194.5077282965602308 ) ) ;
#76796=CARTESIAN_POINT ( 'NONE',  ( 83.64821297929979949, -45.27682201357416858, -13.05452488542865908 ) ) ;
#76809=CARTESIAN_POINT ( 'NONE',  ( 77.86593331225071779, -18.66659222900301529, 117.1557179363761776 ) ) ;
#76815=CARTESIAN_POINT ( 'NONE',  ( -71.68202686650683120, -57.67896093159416893, 168.8233993379761557 ) ) ;
#76821=CARTESIAN_POINT ( 'NONE',  ( 106.4724362242300231, -60.15149996984498415, 175.2116150193959925 ) ) ;
#76827=CARTESIAN_POINT ( 'NONE',  ( -50.11900266124489889, -29.71120325244069704, 46.80446231702884319 ) ) ;
#76841=CARTESIAN_POINT ( 'NONE',  ( -84.86665315508184904, -30.00000000000000000, 169.0604416911780845 ) ) ;
#76846=CARTESIAN_POINT ( 'NONE',  ( 81.23040402425959883, -57.51494128387065530, 199.9225175390093057 ) ) ;
#76849=CARTESIAN_POINT ( 'NONE',  ( 66.47564502340144088, -38.00297273520690311, -32.36529662817321196 ) ) ;
#76853=CARTESIAN_POINT ( 'NONE',  ( -50.53461628407922035, -60.00000000000000000, 73.14908014348027621 ) ) ;
#76856=CARTESIAN_POINT ( 'NONE',  ( -86.57471651473815655, -42.81671748233412700, 189.2810910813386158 ) ) ;
#76859=CARTESIAN_POINT ( 'NONE',  ( -1.000736805672570284, -35.99444417918818573, 29.88872398946706710 ) ) ;
#76872=CARTESIAN_POINT ( 'NONE',  ( 93.27827242126578255, -14.21045842199433729, 72.77868743038563082 ) ) ;
#76873=CARTESIAN_POINT ( 'NONE',  ( -82.15122001469303825, -25.62513163106009983, 144.0135065024727510 ) ) ;
#76877=CARTESIAN_POINT ( 'NONE',  ( 35.39667604442171012, -57.69563824998493118, 49.54500168928262127 ) ) ;
#76897=CARTESIAN_POINT ( 'NONE',  ( 56.55061434549805455, -59.99999999999997868, -36.49602911317763443 ) ) ;
#76899=CARTESIAN_POINT ( 'NONE',  ( -78.42710814205257464, -14.21045842199423070, 185.4825180806740548 ) ) ;
#76900=CARTESIAN_POINT ( 'NONE',  ( 23.79183319049619172, -42.95491878026204091, 32.10493902695667856 ) ) ;
#76904=CARTESIAN_POINT ( 'NONE',  ( -37.87181877912480843, -56.81674967764890027, 40.67228283883505213 ) ) ;
#76908=CARTESIAN_POINT ( 'NONE',  ( -15.38541618194247640, -4.285714285714296246, 20.05453516056600805 ) ) ;
#76912=TOROIDAL_SURFACE ( 'NONE', #7991, 74.46152422706630603, 60.00000000000000000 ) ;
#76919=CARTESIAN_POINT ( 'NONE',  ( 96.80237214965333692, -29.99999999999995737, 129.0906176702744119 ) ) ;
#76924=CARTESIAN_POINT ( 'NONE',  ( 86.64224646343546965, -29.99999999999998934, 68.26920213384829594 ) ) ;
#76940=CARTESIAN_POINT ( 'NONE',  ( 71.08629748639575041, -38.32842814543181476, 140.5624642575193661 ) ) ;
#76960=CARTESIAN_POINT ( 'NONE',  ( 85.99589102735485824, -35.58585133369340525, 185.3973540908802988 ) ) ;
#76965=CARTESIAN_POINT ( 'NONE',  ( 53.00244648738614472, -57.67085655565274749, -39.32701979258551006 ) ) ;
#76969=CARTESIAN_POINT ( 'NONE',  ( -89.54384241208562401, -30.00000000000000355, 85.81002042860349377 ) ) ;
#76973=CARTESIAN_POINT ( 'NONE',  ( 0.03252858621208985779, -57.67120202567194553, 41.61186624302497705 ) ) ;
#76979=CARTESIAN_POINT ( 'NONE',  ( -26.51146395532327205, -28.75509375596147166, 30.19052060091659229 ) ) ;
#76986=CARTESIAN_POINT ( 'NONE',  ( 64.09672519251849110, -29.67724580561281300, -23.43488640169166715 ) ) ;
#76987=CARTESIAN_POINT ( 'NONE',  ( -23.57229190052912315, -35.99927206564916560, 30.88733768663876589 ) ) ;
#76994=CARTESIAN_POINT ( 'NONE',  ( -18.63541348317560420, -22.07126658726433988, 27.94047467926784023 ) ) ;
#77005=CARTESIAN_POINT ( 'NONE',  ( 104.9449258806604064, -60.15148239079525183, 188.0245670500678443 ) ) ;
#77006=SURFACE_STYLE_FILL_AREA ( #54841 ) ;
#77021=CARTESIAN_POINT ( 'NONE',  ( -39.20652242405842713, -59.99999999998065903, -42.13619399682325906 ) ) ;
#77025=CARTESIAN_POINT ( 'NONE',  ( -94.49493096136262693, -59.99999999999997158, -13.89135613746328701 ) ) ;
#77030=CARTESIAN_POINT ( 'NONE',  ( -47.84767795939104218, -60.28261157666721459, 53.82599118737805810 ) ) ;
#77041=CARTESIAN_POINT ( 'NONE',  ( 82.23984288647631047, -30.00000000000165912, -23.31778023025261248 ) ) ;
#77046=CARTESIAN_POINT ( 'NONE',  ( 88.94591903970945168, -30.00000000000000000, 188.6279831367985764 ) ) ;
#77052=CARTESIAN_POINT ( 'NONE',  ( 53.32874875972302675, -53.37299379156652890, 62.19724302110672198 ) ) ;
#77053=CARTESIAN_POINT ( 'NONE',  ( 89.99999999999997158, 500000.0000000000582, 188.5238439516623146 ) ) ;
#77057=CARTESIAN_POINT ( 'NONE',  ( -88.31393190425067985, -38.37506173642456275, -19.13771254034035607 ) ) ;
#77060=CARTESIAN_POINT ( 'NONE',  ( 110.2492766163225184, -38.35601179711003539, 184.3364095030646865 ) ) ;
#77063=CARTESIAN_POINT ( 'NONE',  ( 86.38361104131109869, -60.13166636963751444, 4.011411551973763423 ) ) ;
#77083=CARTESIAN_POINT ( 'NONE',  ( -16.93153427181588100, -15.84522097637744409, 31.52956385905993031 ) ) ;
#77087=CARTESIAN_POINT ( 'NONE',  ( 86.38910116964329688, -17.91566640048721482, 174.1185442106061032 ) ) ;
#77092=CARTESIAN_POINT ( 'NONE',  ( -93.17158877072618850, -37.82072235447289899, 97.15439343368484515 ) ) ;
#77097=CARTESIAN_POINT ( 'NONE',  ( -27.77832180966715114, -28.75187696444542595, -38.27432471080516052 ) ) ;
#77100=CARTESIAN_POINT ( 'NONE',  ( 36.36503303793942621, -59.99999999999998579, 47.71482123089194261 ) ) ;
#77101=CARTESIAN_POINT ( 'NONE',  ( 30.26725086609628335, -32.62914588997867327, 40.72554252228815130 ) ) ;
#77103=CARTESIAN_POINT ( 'NONE',  ( 34.89228459837880791, -24.01504711961399607, 33.45256225496395786 ) ) ;
#77111=CARTESIAN_POINT ( 'NONE',  ( 71.17283260602091843, -38.00000000000000000, -21.88484610531455488 ) ) ;
#77114=DIRECTION ( 'NONE',  ( 0.000000000000000000, 0.000000000000000000, 1.000000000000000000 ) ) ;
#77122=CARTESIAN_POINT ( 'NONE',  ( -19.18585068438267882, -47.40892052979416604, -34.01666544723598662 ) ) ;
#77131=CARTESIAN_POINT ( 'NONE',  ( -92.06016183752583970, -60.00000000000002132, 5.047127910554535468 ) ) ;
#77139=CARTESIAN_POINT ( 'NONE',  ( -85.31458647159905695, -22.02019807324484546, 163.9776401941061863 ) ) ;
#77152=CARTESIAN_POINT ( 'NONE',  ( -94.22037892716120666, -57.65324192061454056, -13.00879341737615569 ) ) ;
#77158=CARTESIAN_POINT ( 'NONE',  ( 94.42187179517443951, -29.99999999999998934, 63.29523499578382228 ) ) ;
#77160=CARTESIAN_POINT ( 'NONE',  ( -77.10962715007582347, -30.00000000000002842, 176.8398472105207020 ) ) ;
#77161=CARTESIAN_POINT ( 'NONE',  ( -58.62493915070122341, -46.44083934075592879, 71.88410043818807083 ) ) ;
#77167=CARTESIAN_POINT ( 'NONE',  ( -103.9498368666699832, -45.26547174848818855, 177.1723940409133604 ) ) ;
#77170=AXIS2_PLACEMENT_3D ( 'NONE', #78632, #61964, #4767 ) ;
#77179=CARTESIAN_POINT ( 'NONE',  ( 85.18902050349326771, -60.00000000000000000, -15.68190703514374107 ) ) ;
#77184=CARTESIAN_POINT ( 'NONE',  ( -31.09282792621365132, -29.07633572334400185, 31.64039428921726227 ) ) ;
#77186=CARTESIAN_POINT ( 'NONE',  ( 47.76287223254053771, -25.68661234867465382, 43.12975209083432304 ) ) ;
#77190=CARTESIAN_POINT ( 'NONE',  ( -100.2185995264695322, -38.46493287070022404, 200.4360577060224955 ) ) ;
#77201=EDGE_CURVE ( 'NONE', #74331, #50990, #60402, .T. ) ;
#77202=CARTESIAN_POINT ( 'NONE',  ( 112.1773567419170377, -59.99999999999999289, 169.0791235005425790 ) ) ;
#77206=CARTESIAN_POINT ( 'NONE',  ( -81.57272358321040429, -29.99999999999999289, -5.204509085996302353 ) ) ;
#77208=CARTESIAN_POINT ( 'NONE',  ( -55.85004154032156265, -38.34489998747773143, 83.90154939705580261 ) ) ;
#77222=CARTESIAN_POINT ( 'NONE',  ( 84.69268008423972560, -28.96262395815541524, 169.4286736083946892 ) ) ;
#77237=CARTESIAN_POINT ( 'NONE',  ( 86.57905893650337248, -16.99609905251657338, 184.8754976615798284 ) ) ;
#77265=CARTESIAN_POINT ( 'NONE',  ( -108.5660005441912972, -60.00000000000000711, 194.5918078993309166 ) ) ;
#77271=CARTESIAN_POINT ( 'NONE',  ( -82.96224355738017664, -50.06567045369714464, 183.0600446902855083 ) ) ;
#77273=( BOUNDED_CURVE ( )  B_SPLINE_CURVE ( 2, ( #36058, #68394, #52183 ),
 .UNSPECIFIED., .F., .F. ) 
 B_SPLINE_CURVE_WITH_KNOTS ( ( 3, 3 ),
 ( 0.000000000000000000, 1.000000000000000000 ),
 .UNSPECIFIED. ) 
 CURVE ( )  GEOMETRIC_REPRESENTATION_ITEM ( )  RATIONAL_B_SPLINE_CURVE ( ( 1.000000000000000000, 1.857142857142858317, 1.000000000000000000 ) ) 
 REPRESENTATION_ITEM ( '' )  );
#77277=CARTESIAN_POINT ( 'NONE',  ( -82.58559367277240426, -37.83348976570933075, 5.520925785892475623 ) ) ;
#77285=CARTESIAN_POINT ( 'NONE',  ( 73.20367453073632191, -59.99999999999985789, 185.6239686060362146 ) ) ;
#77287=CARTESIAN_POINT ( 'NONE',  ( -86.49433777984398830, -14.21045842199439946, 11.85125679505764928 ) ) ;
#77288=CARTESIAN_POINT ( 'NONE',  ( -69.97160914037661428, -53.38730675860333719, 110.0502627141849956 ) ) ;
#77290=CARTESIAN_POINT ( 'NONE',  ( 79.57068731991196842, -14.21045842199434794, 190.0104166006057085 ) ) ;
#77292=CARTESIAN_POINT ( 'NONE',  ( 81.55124166166723398, -57.67115036738129419, -29.31836794746244124 ) ) ;
#77301=CARTESIAN_POINT ( 'NONE',  ( -91.90915390750564029, -59.99999999999997158, 16.42317985402541325 ) ) ;
#77315=CARTESIAN_POINT ( 'NONE',  ( 32.18313561787557120, -32.55190988895232351, 32.69763082105384200 ) ) ;
#77316=CARTESIAN_POINT ( 'NONE',  ( 3.301606509414619861, -4.285714285714286476, 25.22241582816893413 ) ) ;
#77330=CARTESIAN_POINT ( 'NONE',  ( 92.00718413779456739, -60.00000000000000711, 6.061572897356207967 ) ) ;
#77338=CARTESIAN_POINT ( 'NONE',  ( -107.6467995412221939, -30.00000000000500222, 189.8238950325566918 ) ) ;
#77345=CARTESIAN_POINT ( 'NONE',  ( 83.26603652480599749, -45.27681178268631612, -13.97111306700649180 ) ) ;
#77348=CLOSED_SHELL ( 'NONE', ( #61965, #61625, #60035, #14100, #40125, #82826, #63328, #5453, #37161, #45875, #52834, #70768, #96497, #104197, #65013, #8664, #34817, #15924, #9224, #61612, #88323, #36850, #14323, #21377, #94617, #104040, #51156, #102410, #60412, #84099, #12955, #46395, #80780, #83387, #33651, #15256, #30390, #39950, #74334, #64919, #92362, #34430, #22656, #21139, #28191, #44640, #71209, #15596, #26496, #85165, #102368, #67377, #79170, #105478, #28146, #22773, #67665, #90210, #26724 ) ) ;
#77351=VERTEX_POINT ( 'NONE', #25117 ) ;
#77356=CARTESIAN_POINT ( 'NONE',  ( 74.24595519639049712, -25.59685389213801443, 107.9157497212091528 ) ) ;
#77361=CARTESIAN_POINT ( 'NONE',  ( -71.40526007946631637, -57.68007955256489083, 166.0300312729133623 ) ) ;
#77370=CARTESIAN_POINT ( 'NONE',  ( -52.75365474858949000, -30.00000000000000711, 51.53900060926203253 ) ) ;
#77382=CARTESIAN_POINT ( 'NONE',  ( -75.51516288543760425, -29.99999999999999289, -27.33247042156351725 ) ) ;
#77383=CARTESIAN_POINT ( 'NONE',  ( -84.87290633932420292, -30.00000000000000000, 169.1199384629161102 ) ) ;
#77388=CARTESIAN_POINT ( 'NONE',  ( 81.43375511528206800, -57.51667291745025778, 200.0811565040724815 ) ) ;
#77392=CARTESIAN_POINT ( 'NONE',  ( 28.29337419442703094, -28.94310075340867172, -38.25297961115466450 ) ) ;
#77395=CARTESIAN_POINT ( 'NONE',  ( -71.96544483848215634, -60.00000000000000000, 154.0212030161015946 ) ) ;
#77397=CARTESIAN_POINT ( 'NONE',  ( -84.89981489726106645, -57.47619647151204703, 192.0086891560063407 ) ) ;
#77400=CARTESIAN_POINT ( 'NONE',  ( -5.051437835758245676, -35.99424957357602040, 29.87887688983398959 ) ) ;
#77417=CARTESIAN_POINT ( 'NONE',  ( 99.88996038257948840, -14.21045842199439946, 111.7630621600675198 ) ) ;
#77418=CARTESIAN_POINT ( 'NONE',  ( -80.37466735423569730, -46.44052868790205935, 156.8257416479256960 ) ) ;
#77422=CARTESIAN_POINT ( 'NONE',  ( 43.21692225861351488, -57.68546145064757980, 61.44301319263212235 ) ) ;
#77441=CARTESIAN_POINT ( 'NONE',  ( 55.19382646853485141, -60.00000000000000000, -36.81090248795683806 ) ) ;
#77442=CARTESIAN_POINT ( 'NONE',  ( -40.90223414571102012, -60.00000000000005684, 57.82070650035302606 ) ) ;
#77443=CARTESIAN_POINT ( 'NONE',  ( 23.23955225627396359, -25.55842996810111956, 29.06036204385301502 ) ) ;
#77446=CARTESIAN_POINT ( 'NONE',  ( -34.47814148916032906, -36.03572155392134135, 34.37536576405466349 ) ) ;
#77451=CARTESIAN_POINT ( 'NONE',  ( 71.17283260602091843, -38.00000000000000000, -21.88484610531455488 ) ) ;
#77462=CARTESIAN_POINT ( 'NONE',  ( 90.62888254124575838, -30.00000000000016698, 190.3062381107464205 ) ) ;
#77465=CARTESIAN_POINT ( 'NONE',  ( 81.36361026003625341, -30.00000000000001066, -10.37120595110931198 ) ) ;
#77488=CARTESIAN_POINT ( 'NONE',  ( 59.57614690027234161, -42.96215887157280378, 72.74039141137150466 ) ) ;
#77506=CARTESIAN_POINT ( 'NONE',  ( 86.42926278269462159, -20.84806595176807775, 182.4259795259146131 ) ) ;
#77515=CARTESIAN_POINT ( 'NONE',  ( -95.80473717211435769, -30.00000000000001066, 122.9249465891220154 ) ) ;
#77518=CARTESIAN_POINT ( 'NONE',  ( 19.25747578669735560, -57.67183159647834856, 42.11888666598880349 ) ) ;
#77526=CARTESIAN_POINT ( 'NONE',  ( 18.03091750576567165, -17.98938779324448589, -33.98685254711978843 ) ) ;
#77527=CARTESIAN_POINT ( 'NONE',  ( -24.33670979648132260, -60.35801636503134660, 35.15369266868731302 ) ) ;
#77529=CARTESIAN_POINT ( 'NONE',  ( 9.797174393178825657E-16, -30.00000000000000000, 8.000000000000000000 ) ) ;
#77531=CARTESIAN_POINT ( 'NONE',  ( -19.10073062131051813, -42.95807464531029041, 31.48258065302363917 ) ) ;
#77546=CARTESIAN_POINT ( 'NONE',  ( 99.87804525097007513, -37.83975434610595556, 190.7999962905255416 ) ) ;
#77547=CARTESIAN_POINT ( 'NONE',  ( 42.46716861921755282, -36.08067099156355795, 40.09748578553070075 ) ) ;
#77562=CARTESIAN_POINT ( 'NONE',  ( -81.47225727030453868, -60.00000000000972022, -29.83846400447649572 ) ) ;
#77565=CARTESIAN_POINT ( 'NONE',  ( 1.494050092659831947E-08, -60.00000000000000000, -44.99999999996099120 ) ) ;
#77568=CARTESIAN_POINT ( 'NONE',  ( -88.10255448128359035, -14.21045842199438347, 36.33746784607973268 ) ) ;
#77569=CARTESIAN_POINT ( 'NONE',  ( 6.078557589344583789, -35.99144002894028205, 29.87849275132226623 ) ) ;
#77571=CARTESIAN_POINT ( 'NONE',  ( -48.53286934315175216, -22.21852483483064944, 43.06535966011481520 ) ) ;
#77583=CARTESIAN_POINT ( 'NONE',  ( 83.85445948688673923, -30.00000000001250555, -22.01549710744075128 ) ) ;
#77587=CARTESIAN_POINT ( 'NONE',  ( 100.4840130108101590, -29.99999999999999289, 182.9441996911958199 ) ) ;
#77593=CARTESIAN_POINT ( 'NONE',  ( 53.88422520731434417, -39.49949140040651940, 57.94306328001776052 ) ) ;
#77599=CARTESIAN_POINT ( 'NONE',  ( -91.30995688543926292, -38.40037703328827945, -10.42389467339130427 ) ) ;
#77602=CARTESIAN_POINT ( 'NONE',  ( 109.5686109773386079, -38.35602074723220767, 188.1120185359518189 ) ) ;
#77604=CARTESIAN_POINT ( 'NONE',  ( 86.42441512864074582, -60.13267006415080829, 3.363400338305296167 ) ) ;
#77620=CARTESIAN_POINT ( 'NONE',  ( 1.078140322363270668E-05, -30.00000000000000000, 28.88964995960238014 ) ) ;
#77623=CARTESIAN_POINT ( 'NONE',  ( 21.54994887520524216, -17.71005473222516002, 31.43420972831726701 ) ) ;
#77626=CARTESIAN_POINT ( 'NONE',  ( 85.13153603772909150, -35.77587323764717553, 181.7315888882555441 ) ) ;
#77630=CARTESIAN_POINT ( 'NONE',  ( -95.54514223258487959, -52.71027819635147438, 96.31137204281640152 ) ) ;
#77639=CARTESIAN_POINT ( 'NONE',  ( 25.49733103399898937, -59.99999999999998579, 41.30705873576198428 ) ) ;
#77643=CARTESIAN_POINT ( 'NONE',  ( 50.71626818303565898, -29.81274633916111938, 47.79517027631969484 ) ) ;
#77662=CARTESIAN_POINT ( 'NONE',  ( 3.170868525710598185, -47.40887100352247785, -34.77119744858119788 ) ) ;
#77673=CARTESIAN_POINT ( 'NONE',  ( -92.23484866504666968, -60.00000000000000000, 2.411054607516263992 ) ) ;
#77681=CARTESIAN_POINT ( 'NONE',  ( -82.61596774746847416, -39.49479684367577903, 166.2316737952538688 ) ) ;
#77683=CARTESIAN_POINT ( 'NONE',  ( -16.90642566761263410, 0.000000000000000000, 2.220638482676595693 ) ) ;
#77691=CARTESIAN_POINT ( 'NONE',  ( -87.28812347660355897, -57.67005709194983609, -25.16891244813248818 ) ) ;
#77697=CARTESIAN_POINT ( 'NONE',  ( 94.33250250775739687, -60.00000000000007105, 18.12814013139226077 ) ) ;
#77698=CARTESIAN_POINT ( 'NONE',  ( -78.26172670240529783, -14.21045842199445275, 161.8221046207387985 ) ) ;
#77699=CARTESIAN_POINT ( 'NONE',  ( -57.60680526892024744, -18.66794027853511295, 57.28622852526675047 ) ) ;
#77703=CARTESIAN_POINT ( 'NONE',  ( -103.3338068315771210, -45.26544286762020874, 183.6154355829563372 ) ) ;
#77704=CARTESIAN_POINT ( 'NONE',  ( -89.99999999999997158, -52.00000000000000000, 196.0238439516549818 ) ) ;
#77706=ORIENTED_EDGE ( 'NONE', *, *, #85574, .T. ) ;
#77721=CARTESIAN_POINT ( 'NONE',  ( -27.52811649691203755, -60.34835150324916242, 35.96130197689507924 ) ) ;
#77724=CARTESIAN_POINT ( 'NONE',  ( 47.01846914081971107, -42.98288543070874823, 47.24321920347014725 ) ) ;
#77730=CARTESIAN_POINT ( 'NONE',  ( -87.32121499277974408, -38.58266683294037591, 199.6815565422783152 ) ) ;
#77741=CARTESIAN_POINT ( 'NONE',  ( 108.8449848764237373, -60.00000000000002132, 194.0276147426650653 ) ) ;
#77746=CARTESIAN_POINT ( 'NONE',  ( -81.42503152479930861, -30.00000000000000000, -2.337591129561404912 ) ) ;
#77754=TOROIDAL_SURFACE ( 'NONE', #65727, 74.46152422706630603, 68.00000000000000000 ) ;
#77758=CARTESIAN_POINT ( 'NONE',  ( 84.97744274634288786, -25.49365950938402037, 166.4570684673164749 ) ) ;
#77798=CARTESIAN_POINT ( 'NONE',  ( -109.1326555875536286, -60.00000000000000000, 193.4862587518598502 ) ) ;
#77804=CARTESIAN_POINT ( 'NONE',  ( -84.24460074213088490, -39.43037569060520298, 179.9152917709095050 ) ) ;
#77809=CARTESIAN_POINT ( 'NONE',  ( -86.38463748994981017, -60.13544983588694492, 4.008287378961288283 ) ) ;
#77818=CARTESIAN_POINT ( 'NONE',  ( 67.17255777190595722, -60.00000000000001421, 138.9727001947898941 ) ) ;
#77820=CARTESIAN_POINT ( 'NONE',  ( -86.89976874444957389, -30.00000000000007105, -18.81729257278660583 ) ) ;
#77822=CARTESIAN_POINT ( 'NONE',  ( -63.37298395216151192, -49.91547941956211787, 86.82718669228569297 ) ) ;
#77824=CARTESIAN_POINT ( 'NONE',  ( 94.89952817683000319, -60.00000000000002842, 205.0337064426678921 ) ) ;
#77826=CARTESIAN_POINT ( 'NONE',  ( 57.00552557303263512, -57.67115621451332430, -38.41573049067468304 ) ) ;
#77835=CARTESIAN_POINT ( 'NONE',  ( -71.42284278233368866, -60.00000000000001421, -32.04182544189346515 ) ) ;
#77839=CARTESIAN_POINT ( 'NONE',  ( 24.41571844174603356, -4.285714285714296246, 6.539732759932823214 ) ) ;
#77846=CARTESIAN_POINT ( 'NONE',  ( 32.39821730551995671, -25.61740565494374167, 31.48411120452532330 ) ) ;
#77847=CARTESIAN_POINT ( 'NONE',  ( 24.56594385547636605, -4.285714285715934047, 6.601913983210457637 ) ) ;
#77859=ORIENTED_EDGE ( 'NONE', *, *, #47430, .F. ) ;
#77860=CARTESIAN_POINT ( 'NONE',  ( 91.87201142978150870, -60.00000000000000000, 10.31812443270822222 ) ) ;
#77872=CARTESIAN_POINT ( 'NONE',  ( -84.78418355050577304, -30.00000000000874678, 197.0029753287615222 ) ) ;
#77878=CARTESIAN_POINT ( 'NONE',  ( 82.82716448943715193, -37.79852848148829025, -11.55289307985657210 ) ) ;
#77882=CARTESIAN_POINT ( 'NONE',  ( 72.50181414422412729, -37.99999999999997868, -21.26202816386757277 ) ) ;
#77890=CARTESIAN_POINT ( 'NONE',  ( 81.44888424073813837, -18.68565686739217924, 133.0755223295938663 ) ) ;
#77894=CARTESIAN_POINT ( 'NONE',  ( -82.98668029349501296, -57.53378708018315280, 201.1759417985833238 ) ) ;
#77904=CARTESIAN_POINT ( 'NONE',  ( -45.30276295077697313, -28.39995151607098478, 40.39584832702679762 ) ) ;
#77905=CARTESIAN_POINT ( 'NONE',  ( -2.500000000000097256, -24.66556416602881896, -30.98418060188836876 ) ) ;
#77917=CARTESIAN_POINT ( 'NONE',  ( -17.02376466190710858, -20.13787694001170792, -37.76456291957570954 ) ) ;
#77918=CARTESIAN_POINT ( 'NONE',  ( -59.62543477322416408, -30.00000000000001066, 66.02805493078550114 ) ) ;
#77923=CARTESIAN_POINT ( 'NONE',  ( 77.62028495137472817, -57.51624882744770417, 196.0320499155326672 ) ) ;
#77928=CARTESIAN_POINT ( 'NONE',  ( -65.76787259454413004, -60.00000000000000000, 121.4293818171927200 ) ) ;
#77932=CARTESIAN_POINT ( 'NONE',  ( -84.85514074054155742, -53.83695654295202360, 190.4612003849218240 ) ) ;
#77936=CARTESIAN_POINT ( 'NONE',  ( -2.047037499957236051, -56.88421240858798456, 33.36767775095443511 ) ) ;
#77948=CARTESIAN_POINT ( 'NONE',  ( 95.73610373016691710, -30.00000000000000355, 71.50072510963239836 ) ) ;
#77949=CARTESIAN_POINT ( 'NONE',  ( -77.54683902299700549, -53.37720965911378812, 145.1088727403986525 ) ) ;
#77951=CARTESIAN_POINT ( 'NONE',  ( 6.243930039575695118E-05, -60.00000000000000000, 42.00000000000000711 ) ) ;
#77953=CARTESIAN_POINT ( 'NONE',  ( 15.51076798754675679, -57.67136409421777188, 41.78720178657271589 ) ) ;
#77957=ORIENTED_EDGE ( 'NONE', *, *, #40555, .T. ) ;
#77969=CARTESIAN_POINT ( 'NONE',  ( 5.563457319916096822, -59.99999999999998579, -42.58005360022414720 ) ) ;
#77971=CARTESIAN_POINT ( 'NONE',  ( -37.55014638933011639, -30.00000000000003553, 45.10809268468624111 ) ) ;
#77972=CARTESIAN_POINT ( 'NONE',  ( 27.12275927623064220, -49.91024972011634020, 34.05263844785792315 ) ) ;
#77975=CARTESIAN_POINT ( 'NONE',  ( -38.96414789418697211, -56.81010691829630588, 41.53583478051260869 ) ) ;
#77978=CARTESIAN_POINT ( 'NONE',  ( -8.127057321558243785, -4.285714285714296246, -23.93420880016848784 ) ) ;
#77986=CARTESIAN_POINT ( 'NONE',  ( -65.34381883650611655, -38.33780668462405572, 114.6597469430721219 ) ) ;
#77987=CARTESIAN_POINT ( 'NONE',  ( 97.90175465450766978, -29.99999999999976907, 190.6242977259294094 ) ) ;
#77991=CARTESIAN_POINT ( 'NONE',  ( 81.59117427061555361, -29.99999999999999645, -6.241865967097711021 ) ) ;
#78008=CARTESIAN_POINT ( 'NONE',  ( 2.377971153322278042E-07, -60.00000000000000000, 39.63907915656436387 ) ) ;
#78014=CARTESIAN_POINT ( 'NONE',  ( 64.90979689770158245, -25.57766637826449241, 78.74366095350538330 ) ) ;
#78018=CARTESIAN_POINT ( 'NONE',  ( -74.39710941758080764, -38.35602968779575406, -29.42678671130902401 ) ) ;
#78027=CARTESIAN_POINT ( 'NONE',  ( -2.499999999999996891, -8.000000000000000000, -17.89626171146327493 ) ) ;
#78031=CARTESIAN_POINT ( 'NONE',  ( 86.38940954400048611, -17.29237249855646397, 180.4464348139406979 ) ) ;
#78035=CARTESIAN_POINT ( 'NONE',  ( 14.03172653833942007, -57.67096042263639077, -44.20628230871724895 ) ) ;
#78039=CARTESIAN_POINT ( 'NONE',  ( -97.43753319845056637, -29.99999999999999645, 133.6227268290389247 ) ) ;
#78044=CARTESIAN_POINT ( 'NONE',  ( 10.20446870609379708, -57.67128174344939140, 41.61875012191181611 ) ) ;
#78053=CARTESIAN_POINT ( 'NONE',  ( -86.71810255127751077, -53.77243697590854055, 192.6459912591498096 ) ) ;
#78056=CARTESIAN_POINT ( 'NONE',  ( -20.58320923621259624, -56.88195280983516255, 33.96619711972437017 ) ) ;
#78065=CARTESIAN_POINT ( 'NONE',  ( -8.401895502683421668, -59.99999999999998579, -42.47750708342923787 ) ) ;
#78069=CARTESIAN_POINT ( 'NONE',  ( 99.57578696694601206, -37.83214993661866998, 191.2440777680208157 ) ) ;
#78084=CARTESIAN_POINT ( 'NONE',  ( -92.02125586894585751, -59.99999999999631228, -20.08360105537134643 ) ) ;
#78086=CARTESIAN_POINT ( 'NONE',  ( 55.71811758917225887, -60.00000000000965628, -39.11301512399793978 ) ) ;
#78090=CARTESIAN_POINT ( 'NONE',  ( -106.4977058212534189, -30.00000000000001776, 137.1023255444873428 ) ) ;
#78091=CARTESIAN_POINT ( 'NONE',  ( 4.981165396653468136, -22.06714069377673582, 27.55817400068765721 ) ) ;
#78093=CARTESIAN_POINT ( 'NONE',  ( -49.11024409948323211, -32.59653215272530957, 47.10069971812693268 ) ) ;
#78103=CARTESIAN_POINT ( 'NONE',  ( 58.10017903397120875, -38.34421737741784852, 90.49762462764655879 ) ) ;
#78107=CARTESIAN_POINT ( 'NONE',  ( 100.8967648887429789, -30.00000000000000711, 180.1179238002322336 ) ) ;
#78114=EDGE_LOOP ( 'NONE', ( #97963, #29918 ) ) ;
#78115=CARTESIAN_POINT ( 'NONE',  ( 54.70282561401326404, -18.68954287160401151, 51.55838953990642182 ) ) ;
#78121=CARTESIAN_POINT ( 'NONE',  ( -91.44391289275247914, -38.39053751225738864, -8.102761395347648943 ) ) ;
#78123=CARTESIAN_POINT ( 'NONE',  ( 105.5497290054224209, -38.38417664786370409, 196.8944578755671841 ) ) ;
#78125=CARTESIAN_POINT ( 'NONE',  ( 85.28997562300351376, -52.71456239550101941, 1.971080634725701719 ) ) ;
#78142=CARTESIAN_POINT ( 'NONE',  ( -34.70053457442661937, -26.34900356544920186, 41.82054189507673669 ) ) ;
#78147=CARTESIAN_POINT ( 'NONE',  ( 83.76870840018638376, -50.13968266632630844, 186.2246346821466432 ) ) ;
#78152=CARTESIAN_POINT ( 'NONE',  ( -91.05637678035618876, -45.26547174173002475, 77.50340589454103224 ) ) ;
#78156=CARTESIAN_POINT ( 'NONE',  ( -9.478872174808550710, -22.49572152134529546, -38.54313998132425212 ) ) ;
#78160=CARTESIAN_POINT ( 'NONE',  ( 7.563307719629934311, -19.30494957266906653, 35.21016297361445169 ) ) ;
#78162=CARTESIAN_POINT ( 'NONE',  ( 44.23667573787285789, -28.03029836076050429, 39.27938594101296843 ) ) ;
#78170=ORIENTED_EDGE ( 'NONE', *, *, #62055, .F. ) ;
#78180=CARTESIAN_POINT ( 'NONE',  ( 6.441795335963374391, -60.22817737698583329, -36.83328242771759164 ) ) ;
#78190=CARTESIAN_POINT ( 'NONE',  ( -92.03676806442638281, -59.99999999999999289, 19.23821862839820440 ) ) ;
#78198=CARTESIAN_POINT ( 'NONE',  ( -80.10560773978777149, -60.38361758132244006, 176.0919189731656900 ) ) ;
#78202=ORIENTED_EDGE ( 'NONE', *, *, #62264, .F. ) ;
#78211=CARTESIAN_POINT ( 'NONE',  ( -94.31942352638992588, -57.67240272246704791, 24.69011299903190704 ) ) ;
#78216=CARTESIAN_POINT ( 'NONE',  ( 68.53628924694606894, -14.21045842199431597, -27.48009014525527860 ) ) ;
#78217=CARTESIAN_POINT ( 'NONE',  ( -73.20747738243755975, -14.21045842199437992, 129.5005664428163641 ) ) ;
#78218=CARTESIAN_POINT ( 'NONE',  ( -53.91561090801278056, -49.91042375249266883, 62.12222278454709112 ) ) ;
#78223=CARTESIAN_POINT ( 'NONE',  ( -100.1861007398734529, -37.81597759049645902, 190.2366006595198940 ) ) ;
#78224=CARTESIAN_POINT ( 'NONE',  ( 97.86690513680532888, -37.99999999999998579, 125.1103042162925760 ) ) ;
#78228=CARTESIAN_POINT ( 'NONE',  ( 44.47534377888507606, -38.31160956920668070, 57.00192013341546016 ) ) ;
#78234=CARTESIAN_POINT ( 'NONE',  ( 67.76059040313977277, -29.99999999999999645, 88.32474484931194070 ) ) ;
#78241=CARTESIAN_POINT ( 'NONE',  ( -27.61573564706210249, -18.62757927915192369, 28.73073199747976503 ) ) ;
#78243=CARTESIAN_POINT ( 'NONE',  ( 48.37073679748882427, -39.52005737407285579, 48.17779182794379977 ) ) ;
#78247=CARTESIAN_POINT ( 'NONE',  ( -84.29785342784349211, -38.74543721064067370, 198.0007389996342795 ) ) ;
#78249=CARTESIAN_POINT ( 'NONE',  ( 91.24894573165114764, -38.36097309605214178, -1.409743066707331627 ) ) ;
#78256=DIRECTION ( 'NONE',  ( 0.000000000000000000, 1.000000000000000000, 0.000000000000000000 ) ) ;
#78257=CARTESIAN_POINT ( 'NONE',  ( 111.0077917343090235, -60.00000000000000000, 152.2127138817539844 ) ) ;
#78266=CARTESIAN_POINT ( 'NONE',  ( -44.47534256803313468, -38.31161230092084935, 57.00189278798902137 ) ) ;
#78276=CARTESIAN_POINT ( 'NONE',  ( 83.36672125823241686, -39.47416250888723965, 173.2576703317640465 ) ) ;
#78279=ORIENTED_EDGE ( 'NONE', *, *, #35634, .T. ) ;
#78288=CARTESIAN_POINT ( 'NONE',  ( -80.50284847417118783, -29.99999999999999645, -13.02832369715059357 ) ) ;
#78314=CARTESIAN_POINT ( 'NONE',  ( -98.63189375226259870, -59.99999999999999289, 202.2227958148920095 ) ) ;
#78320=CARTESIAN_POINT ( 'NONE',  ( -84.47965975623978352, -35.89726040385875194, 177.6434332425895093 ) ) ;
#78327=CARTESIAN_POINT ( 'NONE',  ( -85.24568900165127161, -52.70636524970269221, 2.598678943497877647 ) ) ;
#78333=CARTESIAN_POINT ( 'NONE',  ( 91.09720049356627669, -14.21045842199416143, 197.8400994950010272 ) ) ;
#78335=CARTESIAN_POINT ( 'NONE',  ( -88.56648999577124926, -14.21045842199433018, 40.40162738224969274 ) ) ;
#78336=CARTESIAN_POINT ( 'NONE',  ( -65.80396453374501675, -42.96215446677902605, 90.41881760261397005 ) ) ;
#78338=CARTESIAN_POINT ( 'NONE',  ( 96.06638400950703272, -14.21045842199450426, 198.0643409056117434 ) ) ;
#78340=CARTESIAN_POINT ( 'NONE',  ( 45.81799851979177873, -59.99999999998037481, 67.88348539002272730 ) ) ;
#78350=CARTESIAN_POINT ( 'NONE',  ( -5.591075928466159084, -60.00000000000000000, -42.57939663618462589 ) ) ;
#78366=CARTESIAN_POINT ( 'NONE',  ( 34.86627658960016163, -42.96414815358550499, 35.91348275393595912 ) ) ;
#78367=CARTESIAN_POINT ( 'NONE',  ( 3.088855081073062209E-15, -4.285714285714286476, 25.22241582816893413 ) ) ;
#78383=CARTESIAN_POINT ( 'NONE',  ( 92.64166564108928981, -60.00000000000000711, -3.519352460692061424 ) ) ;
#78391=CARTESIAN_POINT ( 'NONE',  ( -81.04890366060243423, -29.99999999999316813, 192.7446792250348722 ) ) ;
#78408=CARTESIAN_POINT ( 'NONE',  ( 78.59144040420308386, -39.49479029591388013, 137.4423273624143746 ) ) ;
#78413=CARTESIAN_POINT ( 'NONE',  ( -77.37445547080469055, -57.51897485848058977, 195.6910618928241092 ) ) ;
#78420=CARTESIAN_POINT ( 'NONE',  ( -2.500000000000011990, -30.00000000000000000, -31.87333704504306908 ) ) ;
#78430=CARTESIAN_POINT ( 'NONE',  ( -35.79466378710967689, -25.44173586393017672, -36.80375087642579501 ) ) ;
#78431=CARTESIAN_POINT ( 'NONE',  ( -62.52618473358160855, -30.00000000000000355, 73.41945751082272409 ) ) ;
#78438=CARTESIAN_POINT ( 'NONE',  ( 73.86952552712314457, -57.61841923349722094, 186.3992556594028542 ) ) ;
#78439=CARTESIAN_POINT ( 'NONE',  ( 57.70227852311749217, -34.58945965303971093, -25.91729053135263072 ) ) ;
#78441=EDGE_CURVE ( 'NONE', #61647, #31749, #6065, .T. ) ;
#78446=CARTESIAN_POINT ( 'NONE',  ( -69.13297650054198584, -60.00000000000000711, 136.7714041556835411 ) ) ;
#78451=EDGE_CURVE ( 'NONE', #60981, #67219, #63986, .T. ) ;
#78453=CARTESIAN_POINT ( 'NONE',  ( -85.35106076031452460, -42.92912420381342287, 186.7164831997029353 ) ) ;
#78469=CARTESIAN_POINT ( 'NONE',  ( -24.56594385547200687, -4.285714285715344296, -6.601913983219908744 ) ) ;
#78470=CARTESIAN_POINT ( 'NONE',  ( 88.10210802036469602, -14.21045842199426090, 36.33415240954661840 ) ) ;
#78471=CARTESIAN_POINT ( 'NONE',  ( -79.60561737478720090, -42.96939065557461390, 147.0952876792103723 ) ) ;
#78475=CARTESIAN_POINT ( 'NONE',  ( 35.84708862202803914, -57.69601094548832521, 50.03348472163382610 ) ) ;
#78491=CARTESIAN_POINT ( 'NONE',  ( -70.37903440132366484, -60.00000000000007816, 160.1141433014324207 ) ) ;
#78492=CARTESIAN_POINT ( 'NONE',  ( 25.43823788892170512, -22.08888639596277059, 28.86576217263490918 ) ) ;
#78498=CARTESIAN_POINT ( 'NONE',  ( 1.544427540536530710E-15, -4.285714285714290916, -25.22241582816893057 ) ) ;
#78506=CARTESIAN_POINT ( 'NONE',  ( 97.64160974789494674, -30.00000000000016698, 190.8108562078370767 ) ) ;
#78509=CARTESIAN_POINT ( 'NONE',  ( 81.59429082848517112, -30.00000000000000000, -6.732068947242803247 ) ) ;
#78517=CARTESIAN_POINT ( 'NONE',  ( -89.99999999999997158, -60.00000000000000000, 194.0238439516549818 ) ) ;
#78534=CARTESIAN_POINT ( 'NONE',  ( 63.87320186146764911, -25.57903068207289010, 75.85531773732697047 ) ) ;
#78539=CARTESIAN_POINT ( 'NONE',  ( -55.39206909923246513, -36.62708581283116160, -35.18495517365747105 ) ) ;
#78553=CARTESIAN_POINT ( 'NONE',  ( 85.42961103274494405, -50.19169959065673225, 189.9708901157421508 ) ) ;
#78558=DIRECTION ( 'NONE',  ( 0.000000000000000000, -1.000000000000000000, 0.000000000000000000 ) ) ;
#78559=CARTESIAN_POINT ( 'NONE',  ( -100.3697800338488690, -30.00000000000000355, 157.6853798804383757 ) ) ;
#78561=CARTESIAN_POINT ( 'NONE',  ( 2.872543100939889182, -57.67120699056544453, 41.60709250352346089 ) ) ;
#78574=CARTESIAN_POINT ( 'NONE',  ( -19.74050068906625910, -22.07241655641780298, 28.03316789096357908 ) ) ;
#78577=CARTESIAN_POINT ( 'NONE',  ( -97.58016201383395583, -60.00000000000002132, 100.9982337082133625 ) ) ;
#78582=ORIENTED_EDGE ( 'NONE', *, *, #28311, .F. ) ;
#78590=CARTESIAN_POINT ( 'NONE',  ( 101.6883679399455360, -45.28236933294770239, 189.9366059431119140 ) ) ;
#78591=STYLED_ITEM ( 'NONE', ( #92800 ), #37161 ) ;
#78602=CARTESIAN_POINT ( 'NONE',  ( -95.11134242253905313, -60.00000000001936939, -8.936519196967090295 ) ) ;
#78605=CARTESIAN_POINT ( 'NONE',  ( 36.83392883285972630, -60.00000000000000000, 48.18703564933022676 ) ) ;
#78608=CARTESIAN_POINT ( 'NONE',  ( -93.38368407206768040, -29.99999999999995026, 56.44986585522355682 ) ) ;
#78609=CARTESIAN_POINT ( 'NONE',  ( 8.139917744429576274, -35.99157900641900198, 29.88135676800304807 ) ) ;
#78611=CARTESIAN_POINT ( 'NONE',  ( -48.14002044170912598, -25.68398854815584187, 43.60758539631409292 ) ) ;
#78620=CARTESIAN_POINT ( 'NONE',  ( 93.77331375627365162, -29.99999999994636113, 59.18492225089448056 ) ) ;
#78624=CARTESIAN_POINT ( 'NONE',  ( 95.61654509437354932, -30.00000000000000000, 191.3219847211079241 ) ) ;
#78630=CARTESIAN_POINT ( 'NONE',  ( 54.17857857744175476, -18.69473100391316933, 50.60200713917969040 ) ) ;
#78632=CARTESIAN_POINT ( 'NONE',  ( -80.00000000000000000, -52.00000000000000000, -21.09707704303352926 ) ) ;
#78637=CARTESIAN_POINT ( 'NONE',  ( 88.66533242839328466, -38.54123067826672155, 200.1820925585725206 ) ) ;
#78639=CARTESIAN_POINT ( 'NONE',  ( 85.02584152012659047, -52.70748002918131192, 6.452569411773205310 ) ) ;
#78659=CARTESIAN_POINT ( 'NONE',  ( -39.73807737788186500, -28.46602993620439648, 46.96015580672782619 ) ) ;
#78665=CARTESIAN_POINT ( 'NONE',  ( 82.47298783150054646, -60.81518142251732684, 189.3310907902461224 ) ) ;
#78670=CARTESIAN_POINT ( 'NONE',  ( -83.97903783031063085, -37.82227734234454886, 36.92279524269413571 ) ) ;
#78681=CARTESIAN_POINT ( 'NONE',  ( 39.81984205663119525, -26.24841966675792193, 35.84685613074071142 ) ) ;
#78688=CARTESIAN_POINT ( 'NONE',  ( -97.17403402573184223, -38.00000000000000711, 120.7837554639863384 ) ) ;
#78697=CARTESIAN_POINT ( 'NONE',  ( 4.826816438350578942, -60.22815652793605778, -36.87038698696663630 ) ) ;
#78705=CARTESIAN_POINT ( 'NONE',  ( -92.73353799494898908, -60.00000000000002132, -5.996388734087326533 ) ) ;
#78712=CARTESIAN_POINT ( 'NONE',  ( -84.57683538449640537, -25.55585145918435686, 162.3719968557960840 ) ) ;
#78724=CARTESIAN_POINT ( 'NONE',  ( -104.7047915100801987, -57.67116545479915857, 96.89679091199744221 ) ) ;
#78730=CARTESIAN_POINT ( 'NONE',  ( 78.96299857857128757, -14.21045842199439946, -22.44940295094700033 ) ) ;
#78731=CARTESIAN_POINT ( 'NONE',  ( -43.57786082180619047, -59.99999999999987921, 62.86006299602857439 ) ) ;
#78733=CARTESIAN_POINT ( 'NONE',  ( -55.42316588243139108, -36.03017795024024394, 59.79689301410119384 ) ) ;
#78739=CARTESIAN_POINT ( 'NONE',  ( -101.2069807466581750, -45.26418589157207606, 190.9419624999435996 ) ) ;
#78752=CARTESIAN_POINT ( 'NONE',  ( 69.76690891810729056, -30.00000000000001421, 94.57972461657990948 ) ) ;
#78758=CARTESIAN_POINT ( 'NONE',  ( -27.32632706500987751, -39.48308634739166934, 32.30687911778738908 ) ) ;
#78762=CARTESIAN_POINT ( 'NONE',  ( 48.69037531413704301, -39.51851888690750769, 48.66629101439573191 ) ) ;
#78764=CYLINDRICAL_SURFACE ( 'NONE', #61726, 7.500000000001509015 ) ;
#78765=CARTESIAN_POINT ( 'NONE',  ( -105.2287569084031418, -38.38999224387904974, 197.2639937961484407 ) ) ;
#78768=CARTESIAN_POINT ( 'NONE',  ( 90.61125330831669089, -38.34432070828795958, 12.49403374418715273 ) ) ;
#78777=CARTESIAN_POINT ( 'NONE',  ( 108.8393071453071315, -59.99999999999999289, 194.0395522074744576 ) ) ;
#78786=CARTESIAN_POINT ( 'NONE',  ( -90.68541565423112161, -38.35038405383468074, 17.37308604620570662 ) ) ;
#78799=CARTESIAN_POINT ( 'NONE',  ( 83.04247666559754748, -39.48343404634957210, 170.2731162165301555 ) ) ;
#78843=CARTESIAN_POINT ( 'NONE',  ( -105.7694337438876317, -59.99999999999999289, 198.5129163904271934 ) ) ;
#78845=FACE_OUTER_BOUND ( 'NONE', #14543, .T. ) ;
#78848=CARTESIAN_POINT ( 'NONE',  ( -84.73791746677021308, -32.38247958360803835, 175.3255226634325084 ) ) ;
#78851=CARTESIAN_POINT ( 'NONE',  ( -0.01431428620034891179, -57.67120202577072519, -44.61186648040676772 ) ) ;
#78855=CARTESIAN_POINT ( 'NONE',  ( -84.90780823601593852, -52.70144861668445913, 11.02726620768325638 ) ) ;
#78863=CARTESIAN_POINT ( 'NONE',  ( 88.91505260351625850, -29.99999999999995381, 199.0551756924508879 ) ) ;
#78865=CARTESIAN_POINT ( 'NONE',  ( -95.99503958615204624, -14.21045842199434794, 88.91558689677049188 ) ) ;
#78867=CARTESIAN_POINT ( 'NONE',  ( -66.48194133918796922, -32.53344480627807656, 86.88017675495862591 ) ) ;
#78870=CARTESIAN_POINT ( 'NONE',  ( 71.31866560408677458, -59.99999999996072830, 168.9897809639343791 ) ) ;
#78881=CARTESIAN_POINT ( 'NONE',  ( -92.75956059744693505, -59.99999999999998579, -7.438970123485077579 ) ) ;
#78885=CARTESIAN_POINT ( 'NONE',  ( 22.67073868809949033, -4.285714285714296246, 11.17734400176826348 ) ) ;
#78897=CARTESIAN_POINT ( 'NONE',  ( 36.97211274858098307, -39.50748652884733758, 36.52538937020025855 ) ) ;
#78898=CARTESIAN_POINT ( 'NONE',  ( -17.78317311658302202, -3.469446951953614189E-15, -13.66642973270732142 ) ) ;
#78912=CARTESIAN_POINT ( 'NONE',  ( 92.13009336766872082, -59.99999999999999289, 3.893291599061448061 ) ) ;
#78920=CARTESIAN_POINT ( 'NONE',  ( -92.52610172686061674, -29.99999999989381649, 50.79198441316200530 ) ) ;
#78926=CARTESIAN_POINT ( 'NONE',  ( 83.04580959076339752, -45.27726561227110125, -14.40480725557183206 ) ) ;
#78937=CARTESIAN_POINT ( 'NONE',  ( 79.72836144202692310, -18.67635071187021012, 125.0949995831272474 ) ) ;
#78943=CARTESIAN_POINT ( 'NONE',  ( -108.1850948662969216, -57.66112862901258751, 198.7856339303252753 ) ) ;
#78953=CARTESIAN_POINT ( 'NONE',  ( -40.22137457019058360, -26.42085694424761044, 36.10270639820529226 ) ) ;
#78964=CARTESIAN_POINT ( 'NONE',  ( -63.12118703508443929, -30.05855728996417398, -32.04057825768840928 ) ) ;
#78965=CARTESIAN_POINT ( 'NONE',  ( -66.41877331073435187, -30.00000000000001066, 84.34413472128925093 ) ) ;
#78971=CARTESIAN_POINT ( 'NONE',  ( 96.56796194465512428, -57.62221250710192777, 204.4799581288910986 ) ) ;
#78973=CARTESIAN_POINT ( 'NONE',  ( 69.51775844058592213, -21.77030775744987068, -19.67941227880303856 ) ) ;
#78979=CARTESIAN_POINT ( 'NONE',  ( -51.75140944414650335, -60.00000000000002132, 76.27795920913510486 ) ) ;
#78983=CARTESIAN_POINT ( 'NONE',  ( -84.31464934120297983, -57.44558481396982330, 191.1750344329549307 ) ) ;
#78992=CARTESIAN_POINT ( 'NONE',  ( -83.65529993258698482, -45.25817475319772143, -13.07161437908048462 ) ) ;
#79001=CARTESIAN_POINT ( 'NONE',  ( 6.601913983210295100, -4.285714285714226079, 24.56594385547514747 ) ) ;
#79005=CARTESIAN_POINT ( 'NONE',  ( 82.73925898424661796, -14.21045842199433373, -19.52984640694043250 ) ) ;
#79006=CARTESIAN_POINT ( 'NONE',  ( -78.56154225647874512, -49.90730404993688296, 147.8671053437099374 ) ) ;
#79010=CARTESIAN_POINT ( 'NONE',  ( 83.32454909816027566, -57.53833991724482644, 201.3685442388917863 ) ) ;
#79019=DIRECTION ( 'NONE',  ( -3.673940397442057649E-17, 0.000000000000000000, -1.000000000000000000 ) ) ;
#79023=CARTESIAN_POINT ( 'NONE',  ( -44.47534256803313468, -38.31161230092084224, 57.00189278798902137 ) ) ;
#79031=CARTESIAN_POINT ( 'NONE',  ( -66.35297339498846725, -60.00000000000000000, 134.7723483620486888 ) ) ;
#79032=CARTESIAN_POINT ( 'NONE',  ( 28.53304972825587527, -53.38433873617589143, 35.07953571996775111 ) ) ;
#79034=( BOUNDED_SURFACE ( )  B_SPLINE_SURFACE ( 2, 3, ( 
 ( #18957, #66392, #51800, #58855, #8156, #99271, #41060, #25450, #27, #32997, #50209, #91746, #4325, #11328, #101950, #19495, #28639, #103550, #2720, #53415, #70655, #3267, #28108, #21086, #93344, #36739, #68545, #77691, #27584, #12399, #60465, #3800, #62572, #21603, #95457, #44260, #103030, #69075, #61522, #53923, #69602, #102495, #77152, #94951, #36208, #94415, #60984, #52332, #20576, #85245, #52871, #93871, #85801, #11874, #12930, #20030, #44802, #86334, #78211, #45330, #84711, #37260, #70122, #29184, #62062, #86854, #45850, #78724, #4862, #37794, #29700, #10798, #76606, #43716, #35667, #101432, #39363, #31798, #65210, #80851, #54434, #55498, #6964, #105662, #48481, #81373, #39882, #106177, #64686, #71692, #7484, #13989, #64171, #72755, #23182, #79269, #54975, #97558, #56029, #32340, #87381, #89495, #88960, #23718, #56571, #71175, #15590, #40400, #88437, #95998, #73282, #104600, #30212, #5897, #98104, #14511, #13458, #5392, #46379, #47422, #38313, #96529, #104069, #63097, #22123, #63641, #87906, #46894, #15056, #97041, #79799, #80313, #38828, #47945, #6424, #30755, #22661, #72240, #105142, #31285, #26397, #2057, #92135, #99157, #8023, #17737, #43070, #99701, #82457, #35005, #50597, #34484, #58174, #65747, #1517, #41462, #106721, #8560, #75959, #25315, #75424, #49006, #18283, #91101, #40933, #66270, #90017, #42524, #10157, #33399, #67872, #73827, #25871, #66811, #32870, #50084, #24777, #58728, #17209, #16122, #67352, #51138, #81907, #98627, #59262, #24255, #84054, #82990, #57626, #83513, #57103, #91627, #74352, #90551, #430, #100230, #16660, #9085, #49550, #41994 ),
 ( #74874, #962, #9612, #33942, #36610, #69998, #11737, #61390, #77021, #4734, #3138, #69475, #68416, #60858, #102360, #2591, #93748, #68954, #45721, #19900, #28507, #101826, #77562, #76483, #101309, #86732, #93212, #37672, #52742, #20969, #19376, #86207, #35541, #78084, #26923, #27458, #92673, #20444, #60337, #11204, #52207, #44676, #12807, #18831, #94280, #78602, #85120, #12280, #44137, #102899, #3678, #85665, #36084, #53287, #100755, #27991, #53803, #45210, #51674, #4203, #37132, #29063, #61933, #94822, #59797, #84596, #10678, #43594, #64565, #63512, #54853, #22541, #87255, #23594, #64048, #30624, #104478, #31679, #81250, #97433, #29575, #39239, #80723, #6299, #39764, #88313, #31162, #46779, #7365, #79674, #72113, #38195, #96410, #105022, #79142, #55384, #38706, #15464, #14388, #96923, #71570, #47299, #46256, #71054, #56442, #62974, #70534, #80195, #89375, #95875, #55898, #5268, #47819, #103425, #103945, #62447, #23059, #30091, #87782, #22000, #88833, #48357, #95338, #14927, #21474, #13865, #6841, #5784, #72640, #105541, #54309, #13331, #66144, #93498, #40804, #101577, #58047, #97981, #81775, #90970, #43864, #90429, #74229, #51946, #57506, #101037, #49423, #35817, #33274, #24654, #99026, #76756, #49956, #24135, #60082, #25189, #48881, #56978, #73697, #92946, #76224, #35272, #16532, #7898, #89893, #84861, #27736, #68698, #2330, #17080, #82864, #68143, #10943, #106054, #19108, #8961, #2864, #60607, #16005, #73153, #82326, #19645, #307, #106600, #27192, #52478, #8437, #85396, #40277, #41338, #32206, #43341, #65622, #32750, #65083, #98505, #53026, #85949, #87001, #3416 ),
 ( #86486, #63250, #78350, #13071, #12544, #95092, #94016, #12020, #104214, #3946, #22276, #4472, #38454, #36878, #103695, #44952, #95607, #44407, #77835, #36358, #37940, #69745, #28796, #102639, #62209, #30359, #69227, #46001, #96143, #61679, #29841, #94567, #87524, #21228, #103174, #20717, #37411, #55123, #53555, #71320, #29317, #102096, #45479, #54057, #13606, #70275, #78881, #21749, #5008, #70800, #62718, #5528, #54585, #46519, #79416, #11479, #77301, #28255, #61125, #20176, #96669, #71845, #88576, #32489, #15739, #81508, #31434, #22805, #104751, #24405, #73967, #82056, #48622, #7109, #97708, #7629, #57243, #47037, #65360, #23873, #90163, #16267, #63782, #14134, #64311, #8177, #15205, #55641, #40547, #106322, #23327, #73430, #98251, #97183, #49152, #64829, #6575, #14658, #56167, #41083, #47567, #80463, #56717, #79936, #30902, #47, #33020, #48093, #80992, #65886, #98768, #24921, #6046, #89638, #88053, #38972, #39507, #105808, #72381, #89109, #105287, #40025, #72898, #31948, #100900, #43737, #51817, #92273, #83647, #67495, #18426, #27068, #16812, #35144, #100374, #59951, #92817, #33540, #90702, #34092, #84733, #91767, #66413, #10298, #76096, #99843, #43211, #51281, #66965, #84202, #34624, #83133, #99296, #26015, #68014, #25470, #58326, #26537, #49699, #74499, #10816, #2197, #17889, #50741, #18974, #68566, #76625, #82603, #59409, #2736, #35691, #101451, #75572, #57775, #58875, #8707, #9758, #41615, #91250, #42673, #576, #17357, #1667, #50231, #9230, #42135, #75021, #1118, #4343, #3285, #28128, #13476, #20047, #38331, #20595, #54451, #52895, #12946, #69094, #4879 ) ),
 .UNSPECIFIED., .F., .F., .F. ) 
 B_SPLINE_SURFACE_WITH_KNOTS ( ( 3, 3 ),
 ( 4, 2, 2, 2, 2, 2, 2, 2, 2, 2, 2, 2, 2, 2, 2, 2, 2, 2, 2, 2, 2, 2, 2, 2, 2, 2, 2, 2, 2, 2, 2, 2, 2, 2, 2, 2, 2, 2, 2, 2, 2, 2, 2, 2, 2, 2, 2, 2, 2, 2, 2, 2, 2, 2, 2, 2, 2, 2, 2, 2, 2, 2, 2, 2, 2, 2, 2, 2, 2, 2, 2, 2, 2, 2, 2, 2, 2, 2, 2, 2, 2, 2, 2, 2, 2, 2, 2, 2, 2, 2, 2, 2, 2, 2, 2, 2, 2, 2, 2, 4 ),
 ( 0.000000000000000000, 1.000000000000000000 ),
 ( 0.000000000000000000, 0.008346361953628917210, 0.01669272390725783442, 0.03338544781451566884, 0.04173180976814458432, 0.05007817172177350673, 0.05425135269858796794, 0.05842453367540242221, 0.06677089562903133768, 0.07511725758266024622, 0.07929043855947470743, 0.08346361953628916863, 0.08555021002469639924, 0.08763680051310362984, 0.09180998148991809105, 0.09389657197832532165, 0.09493986722252893695, 0.09598316246673255225, 0.09806975295513978286, 0.1001563434435470135, 0.1011996386877506288, 0.1022429339319542441, 0.1043295244203614747, 0.1085027053971759359, 0.1126758863739903971, 0.1168490673508048444, 0.1210222483276192917, 0.1251954293044337529, 0.1335417912580626754, 0.1418881532116915700, 0.1502345151653204924, 0.1669272390725783373, 0.1836199629798361821, 0.2003126868870940269, 0.2336981347016096888, 0.2503908586088675059, 0.2670835825161253507, 0.2754299444697542176, 0.2837763064233831400, 0.2921226683770120625, 0.2962958493538265237, 0.3004690303306409849, 0.3025556208190481877, 0.3046422113074554461, 0.3088153922842699073, 0.3109019827726771101, 0.3119452780168807671, 0.3129885732610843685, 0.3150751637494916269, 0.3161184589936952283, 0.3171617542378988297, 0.3192483447263060325, 0.3202916399705096895, 0.3213349352147132909, 0.3255081161915277521, 0.3265514114357313535, 0.3275947066799349550, 0.3296812971683422133, 0.3317678876567494717, 0.3338544781451566745, 0.3359410686335638774, 0.3380276591219711357, 0.3390709543661747372, 0.3401142496103783941, 0.3422008400987855969, 0.3442874305871927998, 0.3453307258313964567, 0.3463740210756000582, 0.3505472020524145194, 0.3547203830292289806, 0.3588935640060434418, 0.3630667449828579030, 0.3672399259596723642, 0.3755862879133012866, 0.3839326498669302090, 0.3922790118205591314, 0.4006253737741880538, 0.4173180976814458987, 0.4340108215887037435, 0.4507035454959615883, 0.4590499074495905107, 0.4673962694032193776, 0.4757426313568482446, 0.4799158123336627058, 0.4840889933104771670, 0.4882621742872916282, 0.4924353552641060894, 0.4945219457525132922, 0.4966085362409205506, 0.5007817172177350118, 0.5028683077061422146, 0.5039116029503458716, 0.5049548981945495285, 0.5091280791713639342, 0.5112146696597711371, 0.5133012601481783399, 0.5174744411249928566, 0.5216476221018073733, 0.5258208030786217790, 0.5341671650322507015 ),
 .UNSPECIFIED. ) 
 GEOMETRIC_REPRESENTATION_ITEM ( )  RATIONAL_B_SPLINE_SURFACE ( (
 ( 1.000000000000000000, 1.000000000000000000, 1.000000000000000000, 1.000000000000000000, 1.000000000000000000, 1.000000000000000000, 1.000000000000000000, 1.000000000000000000, 1.000000000000000000, 1.000000000000000000, 1.000000000000000000, 1.000000000000000000, 1.000000000000000000, 1.000000000000000000, 1.000000000000000000, 1.000000000000000000, 1.000000000000000000, 1.000000000000000000, 1.000000000000000000, 1.000000000000000000, 1.000000000000000000, 1.000000000000000000, 1.000000000000000000, 1.000000000000000000, 1.000000000000000000, 1.000000000000000000, 1.000000000000000000, 1.000000000000000000, 1.000000000000000000, 1.000000000000000000, 1.000000000000000000, 1.000000000000000000, 1.000000000000000000, 1.000000000000000000, 1.000000000000000000, 1.000000000000000000, 1.000000000000000000, 1.000000000000000000, 1.000000000000000000, 1.000000000000000000, 1.000000000000000000, 1.000000000000000000, 1.000000000000000000, 1.000000000000000000, 1.000000000000000000, 1.000000000000000000, 1.000000000000000000, 1.000000000000000000, 1.000000000000000000, 1.000000000000000000, 1.000000000000000000, 1.000000000000000000, 1.000000000000000000, 1.000000000000000000, 1.000000000000000000, 1.000000000000000000, 1.000000000000000000, 1.000000000000000000, 1.000000000000000000, 1.000000000000000000, 1.000000000000000000, 1.000000000000000000, 1.000000000000000000, 1.000000000000000000, 1.000000000000000000, 1.000000000000000000, 1.000000000000000000, 1.000000000000000000, 1.000000000000000000, 1.000000000000000000, 1.000000000000000000, 1.000000000000000000, 1.000000000000000000, 1.000000000000000000, 1.000000000000000000, 1.000000000000000000, 1.000000000000000000, 1.000000000000000000, 1.000000000000000000, 1.000000000000000000, 1.000000000000000000, 1.000000000000000000, 1.000000000000000000, 1.000000000000000000, 1.000000000000000000, 1.000000000000000000, 1.000000000000000000, 1.000000000000000000, 1.000000000000000000, 1.000000000000000000, 1.000000000000000000, 1.000000000000000000, 1.000000000000000000, 1.000000000000000000, 1.000000000000000000, 1.000000000000000000, 1.000000000000000000, 1.000000000000000000, 1.000000000000000000, 1.000000000000000000, 1.000000000000000000, 1.000000000000000000, 1.000000000000000000, 1.000000000000000000, 1.000000000000000000, 1.000000000000000000, 1.000000000000000000, 1.000000000000000000, 1.000000000000000000, 1.000000000000000000, 1.000000000000000000, 1.000000000000000000, 1.000000000000000000, 1.000000000000000000, 1.000000000000000000, 1.000000000000000000, 1.000000000000000000, 1.000000000000000000, 1.000000000000000000, 1.000000000000000000, 1.000000000000000000, 1.000000000000000000, 1.000000000000000000, 1.000000000000000000, 1.000000000000000000, 1.000000000000000000, 1.000000000000000000, 1.000000000000000000, 1.000000000000000000, 1.000000000000000000, 1.000000000000000000, 1.000000000000000000, 1.000000000000000000, 1.000000000000000000, 1.000000000000000000, 1.000000000000000000, 1.000000000000000000, 1.000000000000000000, 1.000000000000000000, 1.000000000000000000, 1.000000000000000000, 1.000000000000000000, 1.000000000000000000, 1.000000000000000000, 1.000000000000000000, 1.000000000000000000, 1.000000000000000000, 1.000000000000000000, 1.000000000000000000, 1.000000000000000000, 1.000000000000000000, 1.000000000000000000, 1.000000000000000000, 1.000000000000000000, 1.000000000000000000, 1.000000000000000000, 1.000000000000000000, 1.000000000000000000, 1.000000000000000000, 1.000000000000000000, 1.000000000000000000, 1.000000000000000000, 1.000000000000000000, 1.000000000000000000, 1.000000000000000000, 1.000000000000000000, 1.000000000000000000, 1.000000000000000000, 1.000000000000000000, 1.000000000000000000, 1.000000000000000000, 1.000000000000000000, 1.000000000000000000, 1.000000000000000000, 1.000000000000000000, 1.000000000000000000, 1.000000000000000000, 1.000000000000000000, 1.000000000000000000, 1.000000000000000000, 1.000000000000000000, 1.000000000000000000, 1.000000000000000000, 1.000000000000000000, 1.000000000000000000, 1.000000000000000000, 1.000000000000000000, 1.000000000000000000, 1.000000000000000000, 1.000000000000000000, 1.000000000000000000, 1.000000000000000000, 1.000000000000000000, 1.000000000000000000, 1.000000000000000000, 1.000000000000000000, 1.000000000000000000, 1.000000000000000000, 1.000000000000000000, 1.000000000000000000),
 ( 1.857142857142858317, 1.857142857142858317, 1.857142857142858317, 1.857142857142858317, 1.857142857142858317, 1.857142857142858317, 1.857142857142858317, 1.857142857142858317, 1.857142857142858317, 1.857142857142858317, 1.857142857142858317, 1.857142857142858317, 1.857142857142858317, 1.857142857142858317, 1.857142857142858317, 1.857142857142858317, 1.857142857142858317, 1.857142857142858317, 1.857142857142858317, 1.857142857142858317, 1.857142857142858317, 1.857142857142858317, 1.857142857142858317, 1.857142857142858317, 1.857142857142858317, 1.857142857142858317, 1.857142857142858317, 1.857142857142858317, 1.857142857142858317, 1.857142857142858317, 1.857142857142858317, 1.857142857142858317, 1.857142857142858317, 1.857142857142858317, 1.857142857142858317, 1.857142857142858317, 1.857142857142858317, 1.857142857142858317, 1.857142857142858317, 1.857142857142858317, 1.857142857142858317, 1.857142857142858317, 1.857142857142858317, 1.857142857142858317, 1.857142857142858317, 1.857142857142858317, 1.857142857142858317, 1.857142857142858317, 1.857142857142858317, 1.857142857142858317, 1.857142857142858317, 1.857142857142858317, 1.857142857142858317, 1.857142857142858317, 1.857142857142858317, 1.857142857142858317, 1.857142857142858317, 1.857142857142858317, 1.857142857142858317, 1.857142857142858317, 1.857142857142858317, 1.857142857142858317, 1.857142857142858317, 1.857142857142858317, 1.857142857142858317, 1.857142857142858317, 1.857142857142858317, 1.857142857142858317, 1.857142857142858317, 1.857142857142858317, 1.857142857142858317, 1.857142857142858317, 1.857142857142858317, 1.857142857142858317, 1.857142857142858317, 1.857142857142858317, 1.857142857142858317, 1.857142857142858317, 1.857142857142858317, 1.857142857142858317, 1.857142857142858317, 1.857142857142858317, 1.857142857142858317, 1.857142857142858317, 1.857142857142858317, 1.857142857142858317, 1.857142857142858317, 1.857142857142858317, 1.857142857142858317, 1.857142857142858317, 1.857142857142858317, 1.857142857142858317, 1.857142857142858317, 1.857142857142858317, 1.857142857142858317, 1.857142857142858317, 1.857142857142858317, 1.857142857142858317, 1.857142857142858317, 1.857142857142858317, 1.857142857142858317, 1.857142857142858317, 1.857142857142858317, 1.857142857142858317, 1.857142857142858317, 1.857142857142858317, 1.857142857142858317, 1.857142857142858317, 1.857142857142858317, 1.857142857142858317, 1.857142857142858317, 1.857142857142858317, 1.857142857142858317, 1.857142857142858317, 1.857142857142858317, 1.857142857142858317, 1.857142857142858317, 1.857142857142858317, 1.857142857142858317, 1.857142857142858317, 1.857142857142858317, 1.857142857142858317, 1.857142857142858317, 1.857142857142858317, 1.857142857142858317, 1.857142857142858317, 1.857142857142858317, 1.857142857142858317, 1.857142857142858317, 1.857142857142858317, 1.857142857142858317, 1.857142857142858317, 1.857142857142858317, 1.857142857142858317, 1.857142857142858317, 1.857142857142858317, 1.857142857142858317, 1.857142857142858317, 1.857142857142858317, 1.857142857142858317, 1.857142857142858317, 1.857142857142858317, 1.857142857142858317, 1.857142857142858317, 1.857142857142858317, 1.857142857142858317, 1.857142857142858317, 1.857142857142858317, 1.857142857142858317, 1.857142857142858317, 1.857142857142858317, 1.857142857142858317, 1.857142857142858317, 1.857142857142858317, 1.857142857142858317, 1.857142857142858317, 1.857142857142858317, 1.857142857142858317, 1.857142857142858317, 1.857142857142858317, 1.857142857142858317, 1.857142857142858317, 1.857142857142858317, 1.857142857142858317, 1.857142857142858317, 1.857142857142858317, 1.857142857142858317, 1.857142857142858317, 1.857142857142858317, 1.857142857142858317, 1.857142857142858317, 1.857142857142858317, 1.857142857142860093, 1.857142857142860093, 1.857142857142858317, 1.857142857142858317, 1.857142857142858317, 1.857142857142858317, 1.857142857142858317, 1.857142857142858317, 1.857142857142858317, 1.857142857142858317, 1.857142857142858317, 1.857142857142858317, 1.857142857142858317, 1.857142857142858317, 1.857142857142858317, 1.857142857142858317, 1.857142857142858317, 1.857142857142858317, 1.857142857142858317, 1.857142857142858317, 1.857142857142858317, 1.857142857142858317, 1.857142857142858317, 1.857142857142858317, 1.857142857142860981, 1.857142857142860981, 1.857142857142858317, 1.857142857142858317),
 ( 1.000000000000000000, 1.000000000000000000, 1.000000000000000000, 1.000000000000000000, 1.000000000000000000, 1.000000000000000000, 1.000000000000000000, 1.000000000000000000, 1.000000000000000000, 1.000000000000000000, 1.000000000000000000, 1.000000000000000000, 1.000000000000000000, 1.000000000000000000, 1.000000000000000000, 1.000000000000000000, 1.000000000000000000, 1.000000000000000000, 1.000000000000000000, 1.000000000000000000, 1.000000000000000000, 1.000000000000000000, 1.000000000000000000, 1.000000000000000000, 1.000000000000000000, 1.000000000000000000, 1.000000000000000000, 1.000000000000000000, 1.000000000000000000, 1.000000000000000000, 1.000000000000000000, 1.000000000000000000, 1.000000000000000000, 1.000000000000000000, 1.000000000000000000, 1.000000000000000000, 1.000000000000000000, 1.000000000000000000, 1.000000000000000000, 1.000000000000000000, 1.000000000000000000, 1.000000000000000000, 1.000000000000000000, 1.000000000000000000, 1.000000000000000000, 1.000000000000000000, 1.000000000000000000, 1.000000000000000000, 1.000000000000000000, 1.000000000000000000, 1.000000000000000000, 1.000000000000000000, 1.000000000000000000, 1.000000000000000000, 1.000000000000000000, 1.000000000000000000, 1.000000000000000000, 1.000000000000000000, 1.000000000000000000, 1.000000000000000000, 1.000000000000000000, 1.000000000000000000, 1.000000000000000000, 1.000000000000000000, 1.000000000000000000, 1.000000000000000000, 1.000000000000000000, 1.000000000000000000, 1.000000000000000000, 1.000000000000000000, 1.000000000000000000, 1.000000000000000000, 1.000000000000000000, 1.000000000000000000, 1.000000000000000000, 1.000000000000000000, 1.000000000000000000, 1.000000000000000000, 1.000000000000000000, 1.000000000000000000, 1.000000000000000000, 1.000000000000000000, 1.000000000000000000, 1.000000000000000000, 1.000000000000000000, 1.000000000000000000, 1.000000000000000000, 1.000000000000000000, 1.000000000000000000, 1.000000000000000000, 1.000000000000000000, 1.000000000000000000, 1.000000000000000000, 1.000000000000000000, 1.000000000000000000, 1.000000000000000000, 1.000000000000000000, 1.000000000000000000, 1.000000000000000000, 1.000000000000000000, 1.000000000000000000, 1.000000000000000000, 1.000000000000000000, 1.000000000000000000, 1.000000000000000000, 1.000000000000000000, 1.000000000000000000, 1.000000000000000000, 1.000000000000000000, 1.000000000000000000, 1.000000000000000000, 1.000000000000000000, 1.000000000000000000, 1.000000000000000000, 1.000000000000000000, 1.000000000000000000, 1.000000000000000000, 1.000000000000000000, 1.000000000000000000, 1.000000000000000000, 1.000000000000000000, 1.000000000000000000, 1.000000000000000000, 1.000000000000000000, 1.000000000000000000, 1.000000000000000000, 1.000000000000000000, 1.000000000000000000, 1.000000000000000000, 1.000000000000000000, 1.000000000000000000, 1.000000000000000000, 1.000000000000000000, 1.000000000000000000, 1.000000000000000000, 1.000000000000000000, 1.000000000000000000, 1.000000000000000000, 1.000000000000000000, 1.000000000000000000, 1.000000000000000000, 1.000000000000000000, 1.000000000000000000, 1.000000000000000000, 1.000000000000000000, 1.000000000000000000, 1.000000000000000000, 1.000000000000000000, 1.000000000000000000, 1.000000000000000000, 1.000000000000000000, 1.000000000000000000, 1.000000000000000000, 1.000000000000000000, 1.000000000000000000, 1.000000000000000000, 1.000000000000000000, 1.000000000000000000, 1.000000000000000000, 1.000000000000000000, 1.000000000000000000, 1.000000000000000000, 1.000000000000000000, 1.000000000000000000, 1.000000000000000000, 1.000000000000000000, 1.000000000000000000, 1.000000000000000000, 1.000000000000000000, 1.000000000000000000, 1.000000000000000000, 1.000000000000000000, 1.000000000000000000, 1.000000000000000000, 1.000000000000000000, 1.000000000000000000, 1.000000000000000000, 1.000000000000000000, 1.000000000000000000, 1.000000000000000000, 1.000000000000000000, 1.000000000000000000, 1.000000000000000000, 1.000000000000000000, 1.000000000000000000, 1.000000000000000000, 1.000000000000000000, 1.000000000000000000, 1.000000000000000000, 1.000000000000000000, 1.000000000000000000, 1.000000000000000000, 1.000000000000000000, 1.000000000000000000, 1.000000000000000000, 1.000000000000000000, 1.000000000000000000, 1.000000000000000000, 1.000000000000000000, 1.000000000000000000) ) ) 
 REPRESENTATION_ITEM ( '' )  SURFACE ( )  );
#79037=CARTESIAN_POINT ( 'NONE',  ( -23.93420880016847008, -4.285714285714296246, 8.127057321558250891 ) ) ;
#79047=CARTESIAN_POINT ( 'NONE',  ( 89.07481883248233601, -29.99999999999995737, 188.8186571231210564 ) ) ;
#79050=CARTESIAN_POINT ( 'NONE',  ( 81.13650333864865161, -30.00000000000000711, 1.865448809746575343 ) ) ;
#79073=CARTESIAN_POINT ( 'NONE',  ( 63.13592217280013585, -42.95845782474785324, 82.55303697426595022 ) ) ;
#79077=CARTESIAN_POINT ( 'NONE',  ( -54.10267422029167506, -36.39685484491198508, -35.43891616374990861 ) ) ;
#79087=CARTESIAN_POINT ( 'NONE',  ( 87.02613672383397159, -35.40267602311793382, 188.2183129969156994 ) ) ;
#79095=CARTESIAN_POINT ( 'NONE',  ( -97.53946591935846300, -30.00000000000000000, 134.3205009627786524 ) ) ;
#79099=CARTESIAN_POINT ( 'NONE',  ( 4.499670101681318535, -57.67121445897252130, 41.60302808447698908 ) ) ;
#79111=CARTESIAN_POINT ( 'NONE',  ( -87.26825944249861777, -50.07870994218606597, 192.1711060702807572 ) ) ;
#79115=CARTESIAN_POINT ( 'NONE',  ( -11.52844523698097667, -56.88420388045057052, 33.40189270011925515 ) ) ;
#79116=CARTESIAN_POINT ( 'NONE',  ( -106.4182805671071606, -60.00000000000000000, 168.3060419393721929 ) ) ;
#79127=FACE_OUTER_BOUND ( 'NONE', #91504, .T. ) ;
#79142=CARTESIAN_POINT ( 'NONE',  ( -108.2304173386098114, -60.00000000000612488, 199.3584347283029956 ) ) ;
#79143=B_SPLINE_CURVE_WITH_KNOTS ( 'NONE', 1,
 ( #45780, #85728, #27516 ),
 .UNSPECIFIED., .F., .F.,
 ( 2, 1, 2 ),
 ( 0.07762659915682808276, 1.000000000000000000, 1.399003598253852676 ),
 .UNSPECIFIED. ) ;
#79145=CARTESIAN_POINT ( 'NONE',  ( 61.20638430029620736, -59.99999999999997868, -37.77879205856383749 ) ) ;
#79148=CARTESIAN_POINT ( 'NONE',  ( -100.7780794135568954, -14.21045842199427156, 117.1455274902871366 ) ) ;
#79149=CARTESIAN_POINT ( 'NONE',  ( 12.57823845030392995, -53.39675556580161242, 32.84955403993266998 ) ) ;
#79152=CARTESIAN_POINT ( 'NONE',  ( -48.37106977321703738, -39.52344964594737320, 48.17924728568779358 ) ) ;
#79162=CARTESIAN_POINT ( 'NONE',  ( 89.41588365431587704, -29.99999999999777245, 199.0983604411771068 ) ) ;
#79165=CARTESIAN_POINT ( 'NONE',  ( 94.55558776287254830, -30.00000000000000000, 191.3215855683534983 ) ) ;
#79170=ADVANCED_FACE ( 'NONE', ( #52037 ), #99517, .T. ) ;
#79185=CARTESIAN_POINT ( 'NONE',  ( 88.55819102178084279, -38.54384100792545098, 200.1464042754968489 ) ) ;
#79187=CARTESIAN_POINT ( 'NONE',  ( 84.90898523671995690, -52.70835617166946463, 11.02871142132924120 ) ) ;
#79207=CARTESIAN_POINT ( 'NONE',  ( 5.895225616202836250, -15.33049738696555586, 34.54478832876725392 ) ) ;
#79211=CARTESIAN_POINT ( 'NONE',  ( 84.83276708130827615, -39.37258369601807573, 182.9372201221722491 ) ) ;
#79215=CARTESIAN_POINT ( 'NONE',  ( 95.92657667454260206, -57.67157085294456209, 40.82693322936258795 ) ) ;
#79221=CARTESIAN_POINT ( 'NONE',  ( 15.10968165226510784, -22.75080798962788720, 35.94916242595005684 ) ) ;
#79223=CARTESIAN_POINT ( 'NONE',  ( 33.65952191125959558, -23.43196893441297846, 33.04094279894314923 ) ) ;
#79233=CARTESIAN_POINT ( 'NONE',  ( -99.81141058005968603, -37.99999999999998579, 138.1247188685539413 ) ) ;
#79240=CARTESIAN_POINT ( 'NONE',  ( -4.707071514954599856, -34.58962144921125770, -32.59876395530876891 ) ) ;
#79249=CARTESIAN_POINT ( 'NONE',  ( -92.26459300646831707, -60.00000000000002132, 2.000424519725360284 ) ) ;
#79258=CARTESIAN_POINT ( 'NONE',  ( -85.65078221568934680, -18.54887076467624141, 161.4868767356897195 ) ) ;
#79269=CARTESIAN_POINT ( 'NONE',  ( -107.1080015683288025, -57.65528894494657663, 199.9870551016494744 ) ) ;
#79276=CARTESIAN_POINT ( 'NONE',  ( 90.08848753752288019, -30.00000000000005684, -9.081672415796756326 ) ) ;
#79277=CARTESIAN_POINT ( 'NONE',  ( -55.31183857750818333, -60.00000000000000000, 93.46795725556545165 ) ) ;
#79279=CARTESIAN_POINT ( 'NONE',  ( -56.58626023515411418, -39.49787623006356796, 63.80283036987835743 ) ) ;
#79283=CARTESIAN_POINT ( 'NONE',  ( -98.89625630335217465, -37.76835372157881210, 191.9674801915058140 ) ) ;
#79287=SURFACE_STYLE_USAGE ( .BOTH. , #85818 ) ;
#79292=CARTESIAN_POINT ( 'NONE',  ( 65.07902261671387123, -29.99999999999999645, 80.45956481633361079 ) ) ;
#79297=CARTESIAN_POINT ( 'NONE',  ( -27.94118946956361427, -39.48418884341392499, 32.48209851497355061 ) ) ;
#79301=CARTESIAN_POINT ( 'NONE',  ( 48.73357450832351390, -36.05786625502788212, 47.64037412505590652 ) ) ;
#79304=CARTESIAN_POINT ( 'NONE',  ( -110.9857816620232001, -38.35624345773422306, 171.1830732495621135 ) ) ;
#79306=CARTESIAN_POINT ( 'NONE',  ( 91.26056446089212670, -38.40160960025664849, -10.77111187304667617 ) ) ;
#79314=CARTESIAN_POINT ( 'NONE',  ( 95.49222815291510358, -60.00000000000000000, 202.5659028883012525 ) ) ;
#79326=CARTESIAN_POINT ( 'NONE',  ( -110.4574577157169131, -38.35609589571208033, 182.8352804127118532 ) ) ;
#79328=CARTESIAN_POINT ( 'NONE',  ( -2.499999999999998224, -8.000000000000000000, 14.79019945774904166 ) ) ;
#79336=CARTESIAN_POINT ( 'NONE',  ( 83.68669337585905055, -35.98195733051991141, 170.8185300273958092 ) ) ;
#79369=CIRCLE ( 'NONE', #103482, 2.000000000000001776 ) ;
#79376=CARTESIAN_POINT ( 'NONE',  ( -110.2080847442849176, -59.99999999999998579, 145.1285909512942283 ) ) ;
#79382=CARTESIAN_POINT ( 'NONE',  ( -86.39811128889826364, -17.86889493908928017, 174.6576044378396944 ) ) ;
#79390=CARTESIAN_POINT ( 'NONE',  ( -84.98226205003312828, -52.70557095620105770, 17.49892321904152226 ) ) ;
#79398=CARTESIAN_POINT ( 'NONE',  ( 78.18398495971976558, -30.00000000000001421, 185.0784753857526539 ) ) ;
#79400=CARTESIAN_POINT ( 'NONE',  ( -107.0562774193554816, -30.00000000000000355, 141.2195909136805767 ) ) ;
#79401=CARTESIAN_POINT ( 'NONE',  ( -65.12971609318923072, -22.10221659701648633, 77.59119750484730105 ) ) ;
#79404=CARTESIAN_POINT ( 'NONE',  ( 101.9590430895730861, -60.00000000001238476, 203.7674679764209031 ) ) ;
#79416=CARTESIAN_POINT ( 'NONE',  ( -91.87920463863368070, -59.99999999999998579, 9.409623471143431672 ) ) ;
#79423=CARTESIAN_POINT ( 'NONE',  ( 102.8042200330476277, -59.99999999999999289, 193.0926654062890861 ) ) ;
#79428=CARTESIAN_POINT ( 'NONE',  ( 36.95859885022851898, -60.27851612577346430, 40.61549778638487851 ) ) ;
#79430=CARTESIAN_POINT ( 'NONE',  ( -2.910977163135976653, -8.673617379884035472E-16, -22.23822744035697241 ) ) ;
#79443=CARTESIAN_POINT ( 'NONE',  ( 97.58552689470138830, -59.99999999999999289, 66.34462866920253532 ) ) ;
#79451=CARTESIAN_POINT ( 'NONE',  ( -90.00142789408454291, -29.99999999997103828, -9.692338486264096886 ) ) ;
#79465=CARTESIAN_POINT ( 'NONE',  ( 77.19329776267699117, -60.30815103425013035, 150.0154352435695557 ) ) ;
#79487=CARTESIAN_POINT ( 'NONE',  ( -1.816965407639463237, -12.60722515422099121, 32.17792230897330796 ) ) ;
#79498=CARTESIAN_POINT ( 'NONE',  ( -41.74004629104351238, -25.39692756236595272, -29.94283237742294901 ) ) ;
#79499=CARTESIAN_POINT ( 'NONE',  ( -84.24535704145247905, -30.00000000000000355, 163.2126184220585685 ) ) ;
#79504=CARTESIAN_POINT ( 'NONE',  ( 106.6623973988415486, -57.65263066412270376, 200.3796240358551586 ) ) ;
#79506=CARTESIAN_POINT ( 'NONE',  ( 68.19648835047706825, -21.77029766163251523, -20.22171886456733247 ) ) ;
#79511=CARTESIAN_POINT ( 'NONE',  ( -74.13159945279534213, -59.99999999999999289, 173.5497442450795802 ) ) ;
#79515=CARTESIAN_POINT ( 'NONE',  ( -86.00256373658280040, -31.97000255027745297, 183.8091090326766732 ) ) ;
#79521=CARTESIAN_POINT ( 'NONE',  ( -83.19058701941813183, -45.25941601734338349, -14.11641135335829844 ) ) ;
#79527=EDGE_CURVE ( 'NONE', #41900, #59127, #44476, .T. ) ;
#79528=CARTESIAN_POINT ( 'NONE',  ( -25.22241582816893413, -4.285714285714285587, 3.301606509427073455 ) ) ;
#79530=CARTESIAN_POINT ( 'NONE',  ( 87.61417445234833679, -14.21045842199449716, -10.69449287335903342 ) ) ;
#79531=CARTESIAN_POINT ( 'NONE',  ( -78.86360919887746945, -49.90773682881172846, 149.9494586803164680 ) ) ;
#79533=CARTESIAN_POINT ( 'NONE',  ( 28.84074934710125859, -30.00000000000002842, 39.52209614246421410 ) ) ;
#79535=CARTESIAN_POINT ( 'NONE',  ( 100.6487164681503970, -57.62854788423276631, 203.7452194625044228 ) ) ;
#79545=CARTESIAN_POINT ( 'NONE',  ( -102.3387829128316184, -60.15503256459196280, 129.8700687430441292 ) ) ;
#79548=STYLED_ITEM ( 'NONE', ( #76540 ), #51156 ) ;
#79557=CARTESIAN_POINT ( 'NONE',  ( -52.56680815376439853, -59.99999999999999289, 85.36473592189453541 ) ) ;
#79558=CARTESIAN_POINT ( 'NONE',  ( 25.12474446974736608, -46.43382705368295404, 32.95440499086974739 ) ) ;
#79564=CARTESIAN_POINT ( 'NONE',  ( -24.41571844174604067, -4.285714285714295357, 6.539732759932823214 ) ) ;
#79570=CARTESIAN_POINT ( 'NONE',  ( 65.64504852076265706, -60.00000000000000711, -34.00365457729831320 ) ) ;
#79574=CARTESIAN_POINT ( 'NONE',  ( 81.59412642177187536, -30.00000000000000000, -6.882760467535725013 ) ) ;
#79594=CARTESIAN_POINT ( 'NONE',  ( 45.89060600365420584, -38.31793543208539177, 59.54903041405342634 ) ) ;
#79597=CARTESIAN_POINT ( 'NONE',  ( 63.51939168307682593, -25.58021191660321847, 74.89133063105313681 ) ) ;
#79610=CARTESIAN_POINT ( 'NONE',  ( 86.89624646361832561, -35.41998960442577982, 187.9270345319939395 ) ) ;
#79619=CARTESIAN_POINT ( 'NONE',  ( 36.35123893432750464, -59.99999999999999289, 47.70089417776525664 ) ) ;
#79620=CARTESIAN_POINT ( 'NONE',  ( -98.78384617981630811, -29.99999999999999645, 143.3060070716083203 ) ) ;
#79623=CARTESIAN_POINT ( 'NONE',  ( 52.81362779437819910, -57.67621448248372218, 84.99611232883394507 ) ) ;
#79634=CARTESIAN_POINT ( 'NONE',  ( -87.42610337103299400, -31.68231154847087794, 188.4209481024660420 ) ) ;
#79638=CARTESIAN_POINT ( 'NONE',  ( -11.12563101218981920, -22.06807209563270433, 27.59097960060775634 ) ) ;
#79640=CARTESIAN_POINT ( 'NONE',  ( -86.47393794408476708, -60.00000000000003553, 2.142859354767555402 ) ) ;
#79648=CARTESIAN_POINT ( 'NONE',  ( -89.99999999999997158, -60.00000000000000000, 196.0238439516549818 ) ) ;
#79652=CARTESIAN_POINT ( 'NONE',  ( 73.13425705143828282, -60.00000000000000000, 163.6887274309862619 ) ) ;
#79659=CARTESIAN_POINT ( 'NONE',  ( 39.04758850296788353, -59.99999999999992184, 54.77506993285218329 ) ) ;
#79674=CARTESIAN_POINT ( 'NONE',  ( -110.3226427399711582, -60.00000000000000000, 196.3480137812436510 ) ) ;
#79676=CARTESIAN_POINT ( 'NONE',  ( 46.81529435896409552, -59.99999999999998579, 64.36527784653102913 ) ) ;
#79679=CARTESIAN_POINT ( 'NONE',  ( -89.06819603267832974, -14.21045842199437637, 44.46121640280500031 ) ) ;
#79680=CARTESIAN_POINT ( 'NONE',  ( 10.19381490664068401, -32.51059560698807616, 29.31869721906751991 ) ) ;
#79682=CARTESIAN_POINT ( 'NONE',  ( -46.99000847530295033, -56.81688643933499350, 51.30717529515786168 ) ) ;
#79693=CARTESIAN_POINT ( 'NONE',  ( 80.42360447295121162, -30.00000000008963141, 191.4221980076535488 ) ) ;
#79697=CARTESIAN_POINT ( 'NONE',  ( 97.40260387833026812, -30.00000000000000000, 190.9330021436813354 ) ) ;
#79714=CARTESIAN_POINT ( 'NONE',  ( 94.49521094355745277, -38.49073831966759940, 201.2139497919614541 ) ) ;
#79716=CARTESIAN_POINT ( 'NONE',  ( 86.87161160163347517, -60.16194407056408977, -2.782513919925455603 ) ) ;
#79717=CARTESIAN_POINT ( 'NONE',  ( 87.14793098496349444, -38.00000000001091394, 189.0872956505646414 ) ) ;
#79725=AXIS2_PLACEMENT_3D ( 'NONE', #83590, #51216, #84142 ) ;
#79738=CARTESIAN_POINT ( 'NONE',  ( -25.78771796013805329, -29.58065814986082032, 38.51179907014376624 ) ) ;
#79741=CARTESIAN_POINT ( 'NONE',  ( 85.55570978684414740, -32.12474902453483594, 181.4378247361170224 ) ) ;
#79745=CARTESIAN_POINT ( 'NONE',  ( 94.34689964474569024, -57.67206129154387639, 0.5814794534858416242 ) ) ;
#79748=CARTESIAN_POINT ( 'NONE',  ( -4.727711470032256003, -21.61685501870519843, -38.54800715255733223 ) ) ;
#79749=CARTESIAN_POINT ( 'NONE',  ( 7.760496920029347656, -19.37151928998484607, 35.22200866297285415 ) ) ;
#79759=CARTESIAN_POINT ( 'NONE',  ( -102.7253320651412594, -38.00000000000000000, 177.4151174456301590 ) ) ;
#79765=CARTESIAN_POINT ( 'NONE',  ( -20.87337508428412747, -18.80453388489061339, -33.60507608888688935 ) ) ;
#79767=CARTESIAN_POINT ( 'NONE',  ( -55.49686579569075917, -21.76997890922551449, -24.27064579473665873 ) ) ;
#79777=CARTESIAN_POINT ( 'NONE',  ( -91.36484985775511802, -59.99999999999998579, -16.05759115015808192 ) ) ;
#79785=CARTESIAN_POINT ( 'NONE',  ( -81.27817128073411368, -42.97173453030836754, 159.5003095331300926 ) ) ;
#79795=ORIENTED_EDGE ( 'NONE', *, *, #64705, .F. ) ;
#79796=CARTESIAN_POINT ( 'NONE',  ( -89.99999999999997158, -52.00000000000000000, 196.0238439516549818 ) ) ;
#79799=CARTESIAN_POINT ( 'NONE',  ( -77.37445547080469055, -57.51897485848058977, 195.6910618928241092 ) ) ;
#79805=CARTESIAN_POINT ( 'NONE',  ( 89.90448154148772630, -29.99999999999993605, -11.15250327688899645 ) ) ;
#79806=CARTESIAN_POINT ( 'NONE',  ( -42.11059216458311028, -14.21045842199439946, 45.52377215771286245 ) ) ;
#79807=CARTESIAN_POINT ( 'NONE',  ( -53.66382358242866246, -32.56797292521762444, 54.84591734512859773 ) ) ;
#79811=CARTESIAN_POINT ( 'NONE',  ( -102.2165018913519674, -52.71483860031027291, 191.6989155236728664 ) ) ;
#79815=CARTESIAN_POINT ( 'NONE',  ( 90.90483875302744821, -38.34416586328904941, 3.443830408584400704 ) ) ;
#79820=PLANE ( 'NONE',  #14524 ) ;
#79825=CARTESIAN_POINT ( 'NONE',  ( 50.70033520295613272, -42.97491282521573908, 53.11945173217547023 ) ) ;
#79827=CARTESIAN_POINT ( 'NONE',  ( -80.00000000000000000, -52.00000000000000000, -23.09707704303352926 ) ) ;
#79829=CARTESIAN_POINT ( 'NONE',  ( -104.5126905089380074, -38.40291115105728181, 197.9553537318547853 ) ) ;
#79831=CARTESIAN_POINT ( 'NONE',  ( 91.33644327358868509, -38.39903790272940398, -10.00103075991728829 ) ) ;
#79842=CARTESIAN_POINT ( 'NONE',  ( 91.63830261790323561, -60.00000000000000000, 202.2915991548087220 ) ) ;
#79846=CARTESIAN_POINT ( 'NONE',  ( 57.95396635055557510, -29.07655056746734701, 62.48005105517134439 ) ) ;
#79850=CARTESIAN_POINT ( 'NONE',  ( -110.9986318115168018, -38.35598781044485150, 173.1127387114688645 ) ) ;
#79859=CARTESIAN_POINT ( 'NONE',  ( 84.12090616306510071, -35.94182022319192527, 174.7657314699721098 ) ) ;
#79875=CARTESIAN_POINT ( 'NONE',  ( -81.31126947214923462, -29.99999999999999645, 26.13564777162193309 ) ) ;
#79877=DIRECTION ( 'NONE',  ( 0.000000000000000000, 1.000000000000000000, 0.000000000000000000 ) ) ;
#79889=MECHANICAL_DESIGN_GEOMETRIC_PRESENTATION_REPRESENTATION('',(#29973),#83361);
#79900=CARTESIAN_POINT ( 'NONE',  ( -111.0927031282581225, -59.99999999999998579, 153.0492826848410459 ) ) ;
#79903=PLANE ( 'NONE',  #92464 ) ;
#79905=CARTESIAN_POINT ( 'NONE',  ( -84.37166457177885093, -32.45306040212211940, 171.8685867912538185 ) ) ;
#79914=CARTESIAN_POINT ( 'NONE',  ( -84.94869132047828941, -52.70034892481147182, 8.410862686292052359 ) ) ;
#79921=CARTESIAN_POINT ( 'NONE',  ( 107.9653405324804680, -30.00000000000002132, 188.7583403580863717 ) ) ;
#79922=CARTESIAN_POINT ( 'NONE',  ( -92.03818768401583839, -29.99999999999997513, 46.84875813697714619 ) ) ;
#79923=CARTESIAN_POINT ( 'NONE',  ( -63.25552657885100416, -46.43896528863776751, 84.68699370951671312 ) ) ;
#79926=CARTESIAN_POINT ( 'NONE',  ( 87.39880973402036091, -60.00000000001985967, 203.7820402037370684 ) ) ;
#79928=CARTESIAN_POINT ( 'NONE',  ( 1.994190048904284973, -29.02935297365003464, 28.72563985546674914 ) ) ;
#79936=CARTESIAN_POINT ( 'NONE',  ( -100.6329257265545749, -59.99999999999997868, 201.6847065643074188 ) ) ;
#79945=CARTESIAN_POINT ( 'NONE',  ( 105.5351503390431844, -60.00000000000002132, 185.3579240910585497 ) ) ;
#79947=CARTESIAN_POINT ( 'NONE',  ( -36.98928843693574464, -18.74377913183838729, 32.19268859513226033 ) ) ;
#79950=CARTESIAN_POINT ( 'NONE',  ( 36.41154140541230078, -49.89264740158284184, 38.19905247078427379 ) ) ;
#79951=CARTESIAN_POINT ( 'NONE',  ( -11.19959342722916951, 9.651029144387260302E-13, -19.43146043915260179 ) ) ;
#79955=CARTESIAN_POINT ( 'NONE',  ( -74.48071276423321763, -38.33020298555444327, 164.6109856697501925 ) ) ;
#79966=CARTESIAN_POINT ( 'NONE',  ( 92.80923683822102532, -60.00000000000001421, 30.31541718318534606 ) ) ;
#79973=CARTESIAN_POINT ( 'NONE',  ( -87.59720537968154019, -30.00000000000068212, -17.71635471304703557 ) ) ;
#79978=CARTESIAN_POINT ( 'NONE',  ( 82.80415505393953879, -45.27777509290327629, -14.83251382924433237 ) ) ;
#79989=CARTESIAN_POINT ( 'NONE',  ( 79.23531459263197974, -46.43389914412935582, 148.5210349803398344 ) ) ;
#80008=CARTESIAN_POINT ( 'NONE',  ( -9.718871381506426488, -13.69778559267061802, 31.90811388817558480 ) ) ;
#80019=CARTESIAN_POINT ( 'NONE',  ( -69.98795449185568884, -30.00000000000000000, 95.28635153949326764 ) ) ;
#80021=COLOUR_RGB ( '', 0.40784314, 0.44705882, 0.49803922) ;
#80024=CARTESIAN_POINT ( 'NONE',  ( 103.1126816730884173, -57.63601659308862679, 202.8018784190458916 ) ) ;
#80029=CARTESIAN_POINT ( 'NONE',  ( -74.78472009158446099, -60.00000000000000711, 179.5816843754311094 ) ) ;
#80033=CARTESIAN_POINT ( 'NONE',  ( -86.34127813042697142, -21.01238092349332831, 180.7339398568655042 ) ) ;
#80041=CARTESIAN_POINT ( 'NONE',  ( -81.59149017617403388, -37.80312470321176477, -14.43359743736064971 ) ) ;
#80051=CARTESIAN_POINT ( 'NONE',  ( 89.98361085880227961, -30.00000000000001776, -2.850603255620693055 ) ) ;
#80052=CARTESIAN_POINT ( 'NONE',  ( -81.08683376277613775, -29.09337554716583796, 141.3844950506220925 ) ) ;
#80055=CARTESIAN_POINT ( 'NONE',  ( 1.363418823244991529, -14.21045842199435150, 34.36840973699906954 ) ) ;
#80057=CARTESIAN_POINT ( 'NONE',  ( 107.5465923744455665, -57.65770870721873109, 199.5374833259203342 ) ) ;
#80068=CARTESIAN_POINT ( 'NONE',  ( -105.2601448406410327, -52.71030778888786728, 170.4775048412932961 ) ) ;
#80079=CARTESIAN_POINT ( 'NONE',  ( 25.30379516431261067, -18.61089036987345224, 28.23902632360290355 ) ) ;
#80100=EDGE_CURVE ( 'NONE', #71336, #65536, #36672, .T. ) ;
#80120=CARTESIAN_POINT ( 'NONE',  ( 62.87606824768278102, -36.00767307724900945, 78.31049006666825107 ) ) ;
#80137=CARTESIAN_POINT ( 'NONE',  ( 86.58291375612756724, -50.12654805533016855, 191.4789541590376984 ) ) ;
#80149=CARTESIAN_POINT ( 'NONE',  ( 26.06770421271730953, -59.99999999999999289, 41.47426653923610473 ) ) ;
#80150=CARTESIAN_POINT ( 'NONE',  ( -97.62704972254648794, -30.00000000000000711, 134.9237959675543550 ) ) ;
#80152=CARTESIAN_POINT ( 'NONE',  ( 41.16726445008557533, -57.68949799089449471, 57.63647873290717172 ) ) ;
#80158=CARTESIAN_POINT ( 'NONE',  ( -17.68517609946639979, -60.00000000000001421, 39.97351463475433064 ) ) ;
#80159=B_SPLINE_CURVE_WITH_KNOTS ( 'NONE', 3,
 ( #2408, #45025, #101652, #85475, #18087, #50948 ),
 .UNSPECIFIED., .F., .F.,
 ( 4, 2, 4 ),
 ( 0.02053414304140307317, 0.03170133459815401011, 0.04286852615490495400 ),
 .UNSPECIFIED. ) ;
#80160=CARTESIAN_POINT ( 'NONE',  ( 3.807551310283626034, -15.50932548558135693, -35.16743972384818306 ) ) ;
#80164=CARTESIAN_POINT ( 'NONE',  ( -15.36525660533068205, -22.06900397672482939, 27.72757744622246534 ) ) ;
#80165=CARTESIAN_POINT ( 'NONE',  ( -105.0449526092814665, -60.00000000000002842, 150.2760437015073478 ) ) ;
#80173=CARTESIAN_POINT ( 'NONE',  ( 8.061685236282825271E-09, -15.39512265162600535, -35.22781471665102515 ) ) ;
#80175=CARTESIAN_POINT ( 'NONE',  ( 57.96890702122141192, -60.00000000000000000, 94.09620601737630352 ) ) ;
#80180=CARTESIAN_POINT ( 'NONE',  ( 1.295095875561511761E-05, -30.00000000000000000, 37.00000000000000711 ) ) ;
#80184=ORIENTED_EDGE ( 'NONE', *, *, #14417, .T. ) ;
#80195=CARTESIAN_POINT ( 'NONE',  ( -97.86455770250910291, -60.00000000002447820, 204.8732123382124826 ) ) ;
#80197=CARTESIAN_POINT ( 'NONE',  ( 80.95387373043369905, -60.00000000000000000, 197.0855688607617822 ) ) ;
#80200=CARTESIAN_POINT ( 'NONE',  ( -109.5811972119284690, -29.99999999999999289, 174.3366342583755113 ) ) ;
#80201=CARTESIAN_POINT ( 'NONE',  ( 10.12131235883916958, -25.54850865871655330, 28.15731131281348709 ) ) ;
#80202=CARTESIAN_POINT ( 'NONE',  ( 82.50885711773439368, -37.99999999999995737, 16.62692665718585516 ) ) ;
#80203=CARTESIAN_POINT ( 'NONE',  ( -45.04059857025013969, -60.25991841825150175, 49.29949777491053453 ) ) ;
#80215=ORIENTED_EDGE ( 'NONE', *, *, #74483, .F. ) ;
#80216=CARTESIAN_POINT ( 'NONE',  ( 107.8908516830521336, -30.00000000000169820, 188.9791561279670873 ) ) ;
#80220=CARTESIAN_POINT ( 'NONE',  ( 90.49494987202336915, -30.00000000000000355, 91.38635056579792604 ) ) ;
#80225=ORIENTED_EDGE ( 'NONE', *, *, #78451, .T. ) ;
#80233=CARTESIAN_POINT ( 'NONE',  ( 94.14369787774502640, -38.49202524632631395, 201.1992593668043412 ) ) ;
#80235=CARTESIAN_POINT ( 'NONE',  ( 84.47908901077074972, -45.28586178760942005, -7.723303808647219881 ) ) ;
#80236=CARTESIAN_POINT ( 'NONE',  ( 84.84573287372256800, -38.00000000000007816, 182.0739377323602071 ) ) ;
#80252=CARTESIAN_POINT ( 'NONE',  ( -20.45424608527195787, -19.94684262238009254, 35.83346515895529905 ) ) ;
#80256=CARTESIAN_POINT ( 'NONE',  ( 84.39531239231617121, -50.17912663769864423, 187.9369569292725544 ) ) ;
#80261=CARTESIAN_POINT ( 'NONE',  ( 93.89123455727428791, -57.67342034595336742, 16.20923714071724575 ) ) ;
#80281=CARTESIAN_POINT ( 'NONE',  ( -82.46010706263061252, -37.99999999999999289, -12.85786253404099000 ) ) ;
#80285=CARTESIAN_POINT ( 'NONE',  ( -3.762156792001841055, -15.48433094664021503, -35.17833216663523643 ) ) ;
#80287=CARTESIAN_POINT ( 'NONE',  ( -44.04665276855927658, -34.58949255706212966, -28.87972264604723094 ) ) ;
#80296=CARTESIAN_POINT ( 'NONE',  ( -92.66085178039205061, -59.99999999999997868, -3.913123054519065391 ) ) ;
#80298=CARTESIAN_POINT ( 'NONE',  ( 22.67522056483525006, -27.32510663572569598, -30.38798232809733690 ) ) ;
#80300=CARTESIAN_POINT ( 'NONE',  ( 97.87950285349613466, -37.74667525479749486, 192.5555229186351767 ) ) ;
#80302=CARTESIAN_POINT ( 'NONE',  ( -80.66628790925550163, -53.40400959498802536, 170.0955033780085444 ) ) ;
#80313=CARTESIAN_POINT ( 'NONE',  ( -76.77372030740811226, -57.52889592737719227, 194.6762175334667972 ) ) ;
#80318=CARTESIAN_POINT ( 'NONE',  ( -53.63968661800659277, -29.99999999999997158, -34.46705067659466692 ) ) ;
#80320=CARTESIAN_POINT ( 'NONE',  ( -57.26243271903199172, -29.99999999999990763, 83.64903429017334702 ) ) ;
#80321=CARTESIAN_POINT ( 'NONE',  ( -52.16595314293665098, -46.44255072620141789, 57.11458137737905361 ) ) ;
#80325=CARTESIAN_POINT ( 'NONE',  ( -99.99287224920719552, -45.25595435666994604, 192.6068234404419570 ) ) ;
#80332=CARTESIAN_POINT ( 'NONE',  ( 90.65073698084890452, -38.34357974882981779, 8.850807137404535396 ) ) ;
#80337=CARTESIAN_POINT ( 'NONE',  ( 66.21888218963562167, -30.00000000000000000, 83.75810960045656373 ) ) ;
#80346=CARTESIAN_POINT ( 'NONE',  ( 49.62059425776106281, -39.51416815500159174, 50.13166883492932868 ) ) ;
#80350=CARTESIAN_POINT ( 'NONE',  ( -108.8790446731752724, -38.35654071153614098, 190.5160550575546381 ) ) ;
#80352=CARTESIAN_POINT ( 'NONE',  ( 90.76152638017529739, -38.34260793734441108, 6.174342487980118754 ) ) ;
#80356=CARTESIAN_POINT ( 'NONE',  ( 96.39769212010490662, -37.84852860063914903, 116.1806559511277044 ) ) ;
#80364=CARTESIAN_POINT ( 'NONE',  ( 83.25757091423945155, -60.00000000000000711, 199.0109655462719900 ) ) ;
#80369=CARTESIAN_POINT ( 'NONE',  ( 55.86761055447268376, -36.02599416152285983, 60.76863504461332610 ) ) ;
#80376=CARTESIAN_POINT ( 'NONE',  ( -104.4634795451426186, -38.40382459815164395, 198.0021900029066444 ) ) ;
#80387=CARTESIAN_POINT ( 'NONE',  ( 81.16830495754287256, -60.54032804279978563, 184.2195180690823406 ) ) ;
#80401=CARTESIAN_POINT ( 'NONE',  ( -4.447288604842995596, -18.47525482061914204, 35.07162955131727955 ) ) ;
#80426=CARTESIAN_POINT ( 'NONE',  ( -106.5012798387082142, -59.99999999999999289, 119.5216608596331298 ) ) ;
#80433=CARTESIAN_POINT ( 'NONE',  ( -83.43473808630078281, -42.98247295588366512, 178.5312127204583419 ) ) ;
#80441=CARTESIAN_POINT ( 'NONE',  ( -86.16836316469820645, -60.13563296699030047, 8.610485354239809652 ) ) ;
#80447=CARTESIAN_POINT ( 'NONE',  ( 112.8608516834554649, -60.00000000000000000, 189.7942083920301855 ) ) ;
#80448=CARTESIAN_POINT ( 'NONE',  ( -88.10255448128359035, -14.21045842199438347, 36.33746784607973268 ) ) ;
#80449=CARTESIAN_POINT ( 'NONE',  ( -63.87384138004166800, -25.58014744444937705, 75.85766445878087438 ) ) ;
#80452=CARTESIAN_POINT ( 'NONE',  ( 73.31980294431531320, -59.99999999999508304, 186.0766219959947705 ) ) ;
#80454=CARTESIAN_POINT ( 'NONE',  ( 1.000716238102184574, -35.99156567037908871, 29.88824423799887953 ) ) ;
#80463=CARTESIAN_POINT ( 'NONE',  ( -102.2674112109930888, -59.99999999999998579, 201.0223749624553307 ) ) ;
#80473=CARTESIAN_POINT ( 'NONE',  ( -36.78691999813820956, -36.04881776531558302, 35.70211516714942235 ) ) ;
#80475=CARTESIAN_POINT ( 'NONE',  ( 39.97211509376299432, -56.79955896029697016, 42.45315631278550228 ) ) ;
#80476=CARTESIAN_POINT ( 'NONE',  ( 17.01589776168603407, -1.734723475976807094E-15, -2.227375807149030162 ) ) ;
#80480=CARTESIAN_POINT ( 'NONE',  ( -73.93043056857301565, -38.32664425143800457, 159.7661319727351383 ) ) ;
#80491=CARTESIAN_POINT ( 'NONE',  ( 93.34040896384792063, -60.00000000000002842, 35.57582133924940138 ) ) ;
#80497=CARTESIAN_POINT ( 'NONE',  ( -89.60745021536853017, -30.00000000000670397, -12.65992882304214895 ) ) ;
#80504=AXIS2_PLACEMENT_3D ( 'NONE', #55100, #81488, #56143 ) ;
#80516=CARTESIAN_POINT ( 'NONE',  ( 82.07463894558122774, -29.09153447962462025, 147.4962313882754756 ) ) ;
#80525=CARTESIAN_POINT ( 'NONE',  ( -29.04643245788701122, -57.68166065953202093, 44.76603692081018693 ) ) ;
#80547=CARTESIAN_POINT ( 'NONE',  ( 49.93561212394431692, -35.59291040412786344, -36.20314293518854498 ) ) ;
#80551=CARTESIAN_POINT ( 'NONE',  ( 100.9016562759859426, -57.62918874011371173, 203.6651917875242930 ) ) ;
#80557=CARTESIAN_POINT ( 'NONE',  ( -74.34387358700993786, -59.99999999999999289, 175.6333023556407227 ) ) ;
#80562=CARTESIAN_POINT ( 'NONE',  ( -83.59396215382736273, -61.00678146017968118, 191.7067536044777398 ) ) ;
#80569=CARTESIAN_POINT ( 'NONE',  ( -84.10008721281353417, -60.17582440984561742, -17.33015767790280037 ) ) ;
#80577=CARTESIAN_POINT ( 'NONE',  ( 11.19959342721965179, -3.864748466433897305E-12, 19.43146043915186993 ) ) ;
#80579=CARTESIAN_POINT ( 'NONE',  ( 88.92118937161633596, -29.99999999999996092, -15.18954496189254755 ) ) ;
#80580=CARTESIAN_POINT ( 'NONE',  ( -77.26988927366080873, -25.60911552037473626, 119.8400127943013018 ) ) ;
#80582=CARTESIAN_POINT ( 'NONE',  ( 21.36200998601213641, -60.00000000000005684, 42.72826288236584702 ) ) ;
#80584=CARTESIAN_POINT ( 'NONE',  ( 89.80416004794994933, -57.60826090897426610, 203.9417383441736149 ) ) ;
#80595=CARTESIAN_POINT ( 'NONE',  ( -101.2390777639338637, -45.26542400508802189, 139.7538116451968051 ) ) ;
#80603=VERTEX_POINT ( 'NONE', #78517 ) ;
#80606=CARTESIAN_POINT ( 'NONE',  ( 30.13134821053596113, -22.12450956031193883, 30.04249343119618132 ) ) ;
#80621=CARTESIAN_POINT ( 'NONE',  ( 86.25826092630657627, -30.00000000000007461, 180.2437358770224307 ) ) ;
#80622=CARTESIAN_POINT ( 'NONE',  ( -84.20864119875632525, -52.67321261282354072, -14.85889068594910256 ) ) ;
#80646=CARTESIAN_POINT ( 'NONE',  ( 69.71140032424059996, -22.11089216996448314, 91.05876745230327174 ) ) ;
#80652=EDGE_CURVE ( 'NONE', #61487, #93158, #91427, .T. ) ;
#80663=CARTESIAN_POINT ( 'NONE',  ( 86.45523760431080973, -17.05172403587358687, 183.4746797687946014 ) ) ;
#80671=CARTESIAN_POINT ( 'NONE',  ( 29.51551548483486798, -60.00000000000000000, 42.80185321029230039 ) ) ;
#80672=CARTESIAN_POINT ( 'NONE',  ( -96.33434547725939012, -30.00000000000000000, 191.2481680440488958 ) ) ;
#80675=CARTESIAN_POINT ( 'NONE',  ( 40.82139093095994298, -57.69032097903409806, 57.04468382372385094 ) ) ;
#80684=CARTESIAN_POINT ( 'NONE',  ( -16.85308237588828106, -59.99999999999999289, 39.91134413746445375 ) ) ;
#80687=CARTESIAN_POINT ( 'NONE',  ( -86.84973327953595401, -28.04380161740479949, 186.3552575792517416 ) ) ;
#80691=CARTESIAN_POINT ( 'NONE',  ( -14.82749242237660425, -56.88391391158748434, 33.50551569215675585 ) ) ;
#80703=CARTESIAN_POINT ( 'NONE',  ( 73.32284281756166422, -59.99999999999999289, 165.4600895165735039 ) ) ;
#80708=CARTESIAN_POINT ( 'NONE',  ( 37.39695856105412730, -59.99999999999995737, 52.44754946039245880 ) ) ;
#80718=FACE_OUTER_BOUND ( 'NONE', #76003, .T. ) ;
#80723=CARTESIAN_POINT ( 'NONE',  ( -113.7384774196253971, -60.00000000001956835, 185.5332954700592438 ) ) ;
#80725=CARTESIAN_POINT ( 'NONE',  ( 38.69880557139828881, -59.99999999999998579, 50.34886149390489152 ) ) ;
#80728=CARTESIAN_POINT ( 'NONE',  ( -105.8556346142475064, -14.21045842199439946, 186.2197870760574290 ) ) ;
#80729=CARTESIAN_POINT ( 'NONE',  ( 9.346812867641324019, -53.39685740252094348, 32.79285266721333159 ) ) ;
#80732=CARTESIAN_POINT ( 'NONE',  ( 82.45662180681927111, -37.99999999999996447, 14.43516799643988868 ) ) ;
#80734=CARTESIAN_POINT ( 'NONE',  ( -47.73610249163328945, -32.60741693219772230, 45.16641798069752411 ) ) ;
#80748=CARTESIAN_POINT ( 'NONE',  ( 83.22744612763000305, -29.99999999997350741, 195.7235398707221634 ) ) ;
#80753=CARTESIAN_POINT ( 'NONE',  ( 100.5470196648521153, -29.99999999999999645, 159.8114828581198026 ) ) ;
#80769=CARTESIAN_POINT ( 'NONE',  ( 79.90910546643618773, -38.77530854556393791, 192.8225656864368034 ) ) ;
#80771=CARTESIAN_POINT ( 'NONE',  ( 85.42134923721152973, -52.71934788913637959, 0.1208844820147615962 ) ) ;
#80772=CARTESIAN_POINT ( 'NONE',  ( 86.96752660269400792, -37.99999999999972999, 188.7629342415843610 ) ) ;
#80780=ADVANCED_FACE ( 'NONE', ( #36523 ), #65545, .T. ) ;
#80791=CARTESIAN_POINT ( 'NONE',  ( 10.39775555965807285, -20.26676808020434706, 35.38161163148800625 ) ) ;
#80795=CARTESIAN_POINT ( 'NONE',  ( 83.43892566183167503, -60.98069388147631287, 191.4419204983608438 ) ) ;
#80799=CARTESIAN_POINT ( 'NONE',  ( 94.19775022482500049, -57.67256254209210908, 22.65169980652741799 ) ) ;
#80804=CARTESIAN_POINT ( 'NONE',  ( -84.85721030251472996, -37.99999999999993605, 182.1326420535735906 ) ) ;
#80824=CARTESIAN_POINT ( 'NONE',  ( -49.54934986436142452, -21.77002013510745115, -25.65681709438414160 ) ) ;
#80832=CARTESIAN_POINT ( 'NONE',  ( -92.38785827711156173, -59.99999999999999289, 0.3159652731796530611 ) ) ;
#80835=CARTESIAN_POINT ( 'NONE',  ( -76.12537862032631608, -38.35598417008158378, -28.58435412235099804 ) ) ;
#80841=CARTESIAN_POINT ( 'NONE',  ( -81.31780443015183835, -46.44658433287104060, 165.0995960706320034 ) ) ;
#80843=VERTEX_POINT ( 'NONE', #100540 ) ;
#80844=ORIENTED_EDGE ( 'NONE', *, *, #62503, .F. ) ;
#80849=DIRECTION ( 'NONE',  ( -0.000000000000000000, 1.000000000000000000, 0.000000000000000000 ) ) ;
#80851=CARTESIAN_POINT ( 'NONE',  ( -113.9839795500101332, -57.67115229137139210, 179.6907882865009185 ) ) ;
#80857=CARTESIAN_POINT ( 'NONE',  ( -47.47011933289886088, -14.21045842199439946, -33.05967481147064291 ) ) ;
#80859=CARTESIAN_POINT ( 'NONE',  ( -20.43766876253514653, -14.21045842199441012, 34.90391904204521012 ) ) ;
#80860=CARTESIAN_POINT ( 'NONE',  ( -53.92306173273154002, -25.63130525233928481, 52.72527914939674787 ) ) ;
#80864=CARTESIAN_POINT ( 'NONE',  ( -100.4547888263544024, -60.28510889581524879, 195.5192978447599614 ) ) ;
#80870=CARTESIAN_POINT ( 'NONE',  ( 108.2055158922219817, -38.35604994730526585, 139.2463622293343519 ) ) ;
#80876=CARTESIAN_POINT ( 'NONE',  ( 80.78126285191066813, -30.00000000000000355, 138.7691592692428912 ) ) ;
#80883=CARTESIAN_POINT ( 'NONE',  ( 50.29923733747742887, -36.04821958570228446, 50.07162713147780408 ) ) ;
#80888=CARTESIAN_POINT ( 'NONE',  ( -104.8255383870086632, -38.39704354203259840, 197.6632266025270894 ) ) ;
#80890=CARTESIAN_POINT ( 'NONE',  ( 90.79437873324295083, -38.35012829369840404, 19.27249926157240978 ) ) ;
#80894=CARTESIAN_POINT ( 'NONE',  ( 104.8029988399297423, -52.71705893269023591, 161.0984590988129526 ) ) ;
#80901=CARTESIAN_POINT ( 'NONE',  ( 82.53461625975002391, -60.00000000000002132, 198.4989634257764237 ) ) ;
#80904=CARTESIAN_POINT ( 'NONE',  ( 57.59701642329373072, -36.02025670668500368, 64.66622269765490216 ) ) ;
#80911=CARTESIAN_POINT ( 'NONE',  ( -90.66174681505526678, -38.34313144972409759, 8.451963012734573510 ) ) ;
#80923=CARTESIAN_POINT ( 'NONE',  ( 85.99887890796605916, -18.43241006622161748, 165.6326649775408839 ) ) ;
#80940=CIRCLE ( 'NONE', #8569, 7.499999999992679633 ) ;
#80957=CARTESIAN_POINT ( 'NONE',  ( -106.4884117741187595, -60.00000000000000000, 119.4417209971499290 ) ) ;
#80959=CARTESIAN_POINT ( 'NONE',  ( 2.641326394094752755E-05, -39.47608681191096736, 30.46899776158753426 ) ) ;
#80963=CARTESIAN_POINT ( 'NONE',  ( -86.10701541242173107, -18.36965636274899083, 167.2037440504452661 ) ) ;
#80976=CARTESIAN_POINT ( 'NONE',  ( 114.2391797980453276, -59.99999999999998579, 181.3573912910646015 ) ) ;
#80979=CARTESIAN_POINT ( 'NONE',  ( -108.8021899934185086, -29.99999999999995026, 184.6878429379334534 ) ) ;
#80980=CARTESIAN_POINT ( 'NONE',  ( -63.23540892387794088, -18.63157451083668903, 70.70009706107828151 ) ) ;
#80983=CARTESIAN_POINT ( 'NONE',  ( 95.12161555340847485, -59.99999999999024425, -7.142421816251681044 ) ) ;
#80985=CARTESIAN_POINT ( 'NONE',  ( 1.007147449337442158, -42.95369000350973465, 31.04859829352065503 ) ) ;
#80992=CARTESIAN_POINT ( 'NONE',  ( -96.14679540281859715, -59.99999999999994316, 202.5905596799929356 ) ) ;
#81000=CIRCLE ( 'NONE', #55, 7.499999999992679633 ) ;
#81004=CARTESIAN_POINT ( 'NONE',  ( 102.3020614934086723, -59.99999999999993605, 193.7906591577538222 ) ) ;
#81005=CARTESIAN_POINT ( 'NONE',  ( -31.69449164194474022, -29.08087705339919538, 31.86155386896254171 ) ) ;
#81007=CARTESIAN_POINT ( 'NONE',  ( 41.32804380067809547, -42.97744930290995313, 40.63765321593970725 ) ) ;
#81008=CARTESIAN_POINT ( 'NONE',  ( 17.78317311657530553, -8.673617379884035472E-16, -13.66642973271117256 ) ) ;
#81012=CARTESIAN_POINT ( 'NONE',  ( -68.03595486504397627, -38.33397274148195777, 125.6715106722867148 ) ) ;
#81023=CARTESIAN_POINT ( 'NONE',  ( 95.28179702667202378, -60.00000000000000711, 51.05854659839798870 ) ) ;
#81029=CARTESIAN_POINT ( 'NONE',  ( -83.78196859787340145, -29.99999999999755929, -22.07823983344261976 ) ) ;
#81046=CARTESIAN_POINT ( 'NONE',  ( 81.37985195669844529, -32.56063285680090047, 146.8991821570098182 ) ) ;
#81055=CARTESIAN_POINT ( 'NONE',  ( -31.30247466046573379, -57.68739127208316120, 46.06264550376279487 ) ) ;
#81067=CARTESIAN_POINT ( 'NONE',  ( -16.31924431152875954, -15.65188151249610371, 31.57746562531465173 ) ) ;
#81081=CARTESIAN_POINT ( 'NONE',  ( 72.73175990828099202, -38.32562016310332353, -30.13089435840664976 ) ) ;
#81082=CARTESIAN_POINT ( 'NONE',  ( -53.08935917470201815, -30.00000000000000000, 52.21147893555080799 ) ) ;
#81086=CARTESIAN_POINT ( 'NONE',  ( 2.500000000000001776, -30.00000000000000000, -14.79019945774903633 ) ) ;
#81087=CARTESIAN_POINT ( 'NONE',  ( 91.21982970888714704, -57.61350775420689274, 204.2106347837803071 ) ) ;
#81093=CARTESIAN_POINT ( 'NONE',  ( -73.91169935318824002, -60.00000000000000000, 171.3249817331451084 ) ) ;
#81097=CARTESIAN_POINT ( 'NONE',  ( -86.40020525432112208, -17.50209429613323309, 178.3865162827522113 ) ) ;
#81104=CARTESIAN_POINT ( 'NONE',  ( -84.37622072227169667, -52.73398876249148515, -14.54299705149653832 ) ) ;
#81108=VERTEX_POINT ( 'NONE', #89148 ) ;
#81113=CARTESIAN_POINT ( 'NONE',  ( -13.60704923275180711, -1.734723475976807094E-15, 10.45706415777857679 ) ) ;
#81116=CARTESIAN_POINT ( 'NONE',  ( 89.32114860119857269, -29.99999999999995026, 17.89867789164953393 ) ) ;
#81118=CARTESIAN_POINT ( 'NONE',  ( -76.02915898839707154, -49.90876059677169962, 133.3426292687217369 ) ) ;
#81120=CARTESIAN_POINT ( 'NONE',  ( 94.39688282193469604, -57.61984102425716969, 204.5389246678256256 ) ) ;
#81125=VERTEX_POINT ( 'NONE', #57284 ) ;
#81136=EDGE_LOOP ( 'NONE', ( #98248, #50479, #74852, #37014 ) ) ;
#81138=CARTESIAN_POINT ( 'NONE',  ( -20.43766876253514653, -14.21045842199441012, 34.90391904204521012 ) ) ;
#81139=CARTESIAN_POINT ( 'NONE',  ( 28.78019115065667322, -18.63880091324738686, 29.02949882689319949 ) ) ;
#81150=CARTESIAN_POINT ( 'NONE',  ( 49.67928414888689304, -59.99999999999997868, -37.96746462862734006 ) ) ;
#81151=CARTESIAN_POINT ( 'NONE',  ( 82.06105073464702571, -29.99999999999996447, 146.2738422045464119 ) ) ;
#81153=CARTESIAN_POINT ( 'NONE',  ( -83.13706915486389448, -45.33804393721257497, -14.25701659862332171 ) ) ;
#81154=CARTESIAN_POINT ( 'NONE',  ( 71.80342808059909032, -30.00000000000000000, -19.71766482350836469 ) ) ;
#81177=CARTESIAN_POINT ( 'NONE',  ( -32.81683603912411229, -59.99999999999996447, 37.99185413034007297 ) ) ;
#81178=CARTESIAN_POINT ( 'NONE',  ( 66.48165699634022019, -32.53116164569385660, 86.87811383088407524 ) ) ;
#81198=CARTESIAN_POINT ( 'NONE',  ( 4.309564269304543949, -60.00000000000002132, 39.63068050932632502 ) ) ;
#81199=CARTESIAN_POINT ( 'NONE',  ( -96.89808418466809314, -29.99999999999999645, 191.1144671784673505 ) ) ;
#81201=CARTESIAN_POINT ( 'NONE',  ( 50.53031853463637901, -57.67793883620915807, 78.60926899548999813 ) ) ;
#81204=CARTESIAN_POINT ( 'NONE',  ( 19.63219237063851352, -25.70262390305547129, -38.48832213154430093 ) ) ;
#81207=CARTESIAN_POINT ( 'NONE',  ( -4.221541119508299467, -59.99999999999998579, 39.63083687578825476 ) ) ;
#81210=CARTESIAN_POINT ( 'NONE',  ( -86.20315129297270573, -57.43435110080902462, 193.3030521547261742 ) ) ;
#81215=CARTESIAN_POINT ( 'NONE',  ( -9.055784372474096955, -22.06795988364936534, 27.56849869070046921 ) ) ;
#81218=CARTESIAN_POINT ( 'NONE',  ( -99.66151320157483440, -59.99999999999997158, 195.9182448172588238 ) ) ;
#81230=CARTESIAN_POINT ( 'NONE',  ( 73.10382484696803829, -60.00000000000000711, 163.4081499180699097 ) ) ;
#81235=CARTESIAN_POINT ( 'NONE',  ( 43.57856552656106430, -59.99999999999991473, 62.86110226080823793 ) ) ;
#81250=CARTESIAN_POINT ( 'NONE',  ( -114.5996607398657403, -60.00000000003901590, 175.3916813916542310 ) ) ;
#81252=CARTESIAN_POINT ( 'NONE',  ( 51.69788177101781201, -59.99999999999997158, 76.10749672676838884 ) ) ;
#81256=CARTESIAN_POINT ( 'NONE',  ( -113.5293469826316084, -59.99999999999994316, 153.5981017735323633 ) ) ;
#81257=CARTESIAN_POINT ( 'NONE',  ( 14.23383089391777645, -18.58706205641739828, 27.09268482856279903 ) ) ;
#81259=CARTESIAN_POINT ( 'NONE',  ( 102.8324458336581841, -38.00000000000000000, 173.0407927310912441 ) ) ;
#81261=CARTESIAN_POINT ( 'NONE',  ( -47.01177656439008246, -25.69492208876496164, 42.17939420022488406 ) ) ;
#81274=CARTESIAN_POINT ( 'NONE',  ( 105.0447870504740848, -30.00000000000308731, 195.3166338682954972 ) ) ;
#81276=CARTESIAN_POINT ( 'NONE',  ( 94.32107141816914009, -30.00000000000000711, 113.8930112096862644 ) ) ;
#81290=CARTESIAN_POINT ( 'NONE',  ( 78.90889072956846917, -38.68051256261696835, 190.7199075547812015 ) ) ;
#81302=ORIENTED_EDGE ( 'NONE', *, *, #38045, .F. ) ;
#81304=SHAPE_REPRESENTATION_RELATIONSHIP ( 'NONE' , 'NONE' ,  #16335, #43474 ) ;
#81309=CARTESIAN_POINT ( 'NONE',  ( 7.145435414194573731, -19.16271036021109353, 35.18478150345621458 ) ) ;
#81315=CARTESIAN_POINT ( 'NONE',  ( 86.14124937075833088, -24.76901598059708220, 180.5798086085166574 ) ) ;
#81320=CARTESIAN_POINT ( 'NONE',  ( 94.19163151293176384, -57.67257257346210508, 22.55351835139595806 ) ) ;
#81327=CARTESIAN_POINT ( 'NONE',  ( -51.84566471874714466, -38.00000000000001421, 53.44666163652544100 ) ) ;
#81328=CARTESIAN_POINT ( 'NONE',  ( 53.08934989192464826, -30.00000000000000000, 52.21148837440648549 ) ) ;
#81338=CARTESIAN_POINT ( 'NONE',  ( -97.09057885222009077, -37.99999999999984368, 192.8439867981303735 ) ) ;
#81345=CARTESIAN_POINT ( 'NONE',  ( -61.30845488575270963, -21.77000553945882899, -22.67001081305290811 ) ) ;
#81352=CARTESIAN_POINT ( 'NONE',  ( -66.47461584428864967, -60.00000000000000000, -33.73856253821774231 ) ) ;
#81354=CARTESIAN_POINT ( 'NONE',  ( 9.889416687731754863, -23.16239103124826926, -30.52333014326384131 ) ) ;
#81356=CARTESIAN_POINT ( 'NONE',  ( 98.97281587209958786, -52.79378276922967927, 194.7734842299395552 ) ) ;
#81359=CARTESIAN_POINT ( 'NONE',  ( 2.435347819570957628E-07, -57.67120202539301488, -44.61186700419775519 ) ) ;
#81360=CARTESIAN_POINT ( 'NONE',  ( -82.17563137770380877, -39.49871834766265977, 162.1473386807309680 ) ) ;
#81373=CARTESIAN_POINT ( 'NONE',  ( -112.4426759231622270, -57.67115411723771956, 189.8075418672916044 ) ) ;
#81381=CARTESIAN_POINT ( 'NONE',  ( -73.46108764834735894, -30.00000000000002132, -28.33320811291743269 ) ) ;
#81382=CARTESIAN_POINT ( 'NONE',  ( -4.277630366265612771, -59.99999999999996447, 41.98954236073067392 ) ) ;
#81383=CARTESIAN_POINT ( 'NONE',  ( -53.26811894799450897, -29.10352339782401998, 52.81850898772155034 ) ) ;
#81386=CARTESIAN_POINT ( 'NONE',  ( -97.47867875887877176, -52.80715018427295604, 195.2329016805694835 ) ) ;
#81390=CARTESIAN_POINT ( 'NONE',  ( 91.42363583869570220, -38.37299437492562504, -4.571104111833916406 ) ) ;
#81394=CARTESIAN_POINT ( 'NONE',  ( 84.62708170603004021, -29.99999999999998579, 166.7775509064786945 ) ) ;
#81402=CARTESIAN_POINT ( 'NONE',  ( 49.31972742781113794, -39.51545095625337467, 49.64355539421404728 ) ) ;
#81407=CARTESIAN_POINT ( 'NONE',  ( -91.20514477336200798, -38.35364638569411255, 26.38587643249713821 ) ) ;
#81410=CARTESIAN_POINT ( 'NONE',  ( 98.59472948510774870, -38.35583824562067434, 80.17062742606734105 ) ) ;
#81413=CARTESIAN_POINT ( 'NONE',  ( 105.4324068091576123, -60.15130706364090685, 153.9750241106484054 ) ) ;
#81418=CARTESIAN_POINT ( 'NONE',  ( 75.95252160951538656, -59.99999999999998579, 186.7850688652185340 ) ) ;
#81422=CARTESIAN_POINT ( 'NONE',  ( 56.33911714990668429, -60.32421506786621279, 72.31300496870655081 ) ) ;
#81428=CARTESIAN_POINT ( 'NONE',  ( -45.71963733757685588, -30.00000000000000000, 56.30991746768096817 ) ) ;
#81438=CARTESIAN_POINT ( 'NONE',  ( 83.17827088202682262, -42.97663241860097116, 176.6375309832781113 ) ) ;
#81454=CARTESIAN_POINT ( 'NONE',  ( -22.28878110947537650, -27.20780569876249189, 37.41599501972370945 ) ) ;
#81473=CARTESIAN_POINT ( 'NONE',  ( -110.7216341579778032, -60.00000000000000000, 149.4927839103214637 ) ) ;
#81481=CARTESIAN_POINT ( 'NONE',  ( -81.92653451457113079, -53.51318851167744839, 180.9174972423841439 ) ) ;
#81488=DIRECTION ( 'NONE',  ( -0.000000000000000000, -1.000000000000000000, -0.000000000000000000 ) ) ;
#81493=CARTESIAN_POINT ( 'NONE',  ( 109.5675852999991662, -29.99999999999999645, 170.1819856699497961 ) ) ;
#81494=CARTESIAN_POINT ( 'NONE',  ( -109.5916892278405470, -30.00000000000001776, 172.2591039824585550 ) ) ;
#81495=CARTESIAN_POINT ( 'NONE',  ( -61.37073833729998995, -60.34629577541569034, 86.28566146466783948 ) ) ;
#81498=CARTESIAN_POINT ( 'NONE',  ( 97.01038254189587917, -60.00000000003893064, 46.46193752217217110 ) ) ;
#81508=CARTESIAN_POINT ( 'NONE',  ( -98.98947487261378342, -60.00000000000000000, 75.03658297502093433 ) ) ;
#81517=CARTESIAN_POINT ( 'NONE',  ( 102.0111507166176921, -60.00000000000002132, 127.8858238654740944 ) ) ;
#81518=CARTESIAN_POINT ( 'NONE',  ( -32.84146244817398497, -56.84655200642422557, 37.45245214281151647 ) ) ;
#81521=CARTESIAN_POINT ( 'NONE',  ( 39.71597467038597529, -29.14573511708929132, 36.18980527160656635 ) ) ;
#81525=CARTESIAN_POINT ( 'NONE',  ( -73.90592356584222955, -38.32656427293123613, 159.5603895101343426 ) ) ;
#81535=CARTESIAN_POINT ( 'NONE',  ( 93.48957285444535614, -60.00000000000001421, 36.96153506271591027 ) ) ;
#81540=CARTESIAN_POINT ( 'NONE',  ( -2.500000000000000444, -12.75203052241420743, 21.42349665395800073 ) ) ;
#81543=CARTESIAN_POINT ( 'NONE',  ( -89.14514748770606900, -29.99999999999991473, 188.9207774528190384 ) ) ;
#81557=CARTESIAN_POINT ( 'NONE',  ( 81.85470369756671971, -36.02805305272049452, 154.5082235924975578 ) ) ;
#81565=CARTESIAN_POINT ( 'NONE',  ( 49.37224559707967586, -60.00000000000000711, -32.19427091295325738 ) ) ;
#81566=CARTESIAN_POINT ( 'NONE',  ( -40.46187072321335165, -57.69130470027779012, 56.40641529803505705 ) ) ;
#81579=CARTESIAN_POINT ( 'NONE',  ( 26.68896952748668383, -30.19711848523571263, 38.93503799944183186 ) ) ;
#81594=CARTESIAN_POINT ( 'NONE',  ( 13.25260485096620933, -23.44304414601906927, -38.53988249343816364 ) ) ;
#81599=CARTESIAN_POINT ( 'NONE',  ( 111.9947854193034402, -57.67108030077226033, 191.3410972543836408 ) ) ;
#81604=CARTESIAN_POINT ( 'NONE',  ( -74.68708113791835501, -60.00000000000000000, 178.7673637760337613 ) ) ;
#81608=CARTESIAN_POINT ( 'NONE',  ( -83.28797064766409619, -60.96659139404700767, 191.1653894862643597 ) ) ;
#81618=CARTESIAN_POINT ( 'NONE',  ( -84.93482623333412107, -52.74702798847152962, -13.23012522214947317 ) ) ;
#81626=CARTESIAN_POINT ( 'NONE',  ( -2.227375807148842313, -1.734723475976807094E-15, -17.01589776168603407 ) ) ;
#81628=CARTESIAN_POINT ( 'NONE',  ( 57.68379620845067279, -29.99999999999995026, -33.51799637603287607 ) ) ;
#81629=CARTESIAN_POINT ( 'NONE',  ( -76.34156285824845156, -46.43775314653531439, 131.9850733549745883 ) ) ;
#81631=CARTESIAN_POINT ( 'NONE',  ( 54.44934741818074286, -29.99999999999998224, 75.82777139632159447 ) ) ;
#81633=CARTESIAN_POINT ( 'NONE',  ( 93.16704160177832250, -57.65532162308603858, -16.80702944056087844 ) ) ;
#81652=CARTESIAN_POINT ( 'NONE',  ( -4.277630366265612771, -59.99999999999996447, 41.98954236073067392 ) ) ;
#81653=CARTESIAN_POINT ( 'NONE',  ( 31.24783293400658835, -56.84949674888247984, 36.70056667471371981 ) ) ;
#81668=CARTESIAN_POINT ( 'NONE',  ( 23.69449890484973054, -59.99999999999999289, -41.54738999840723324 ) ) ;
#81676=ORIENTED_EDGE ( 'NONE', *, *, #101156, .F. ) ;
#81687=EDGE_LOOP ( 'NONE', ( #52999, #47494, #82110, #95684 ) ) ;
#81692=CARTESIAN_POINT ( 'NONE',  ( 66.15239626261548267, -56.85959143212516409, 99.15857335605178946 ) ) ;
#81698=CARTESIAN_POINT ( 'NONE',  ( -72.13200937809398283, -57.67118076099990986, -33.88443861317198724 ) ) ;
#81707=EDGE_CURVE ( 'NONE', #35136, #61647, #79143, .T. ) ;
#81720=CARTESIAN_POINT ( 'NONE',  ( -98.13696214071765667, -30.00000000000000000, 190.3767244705021824 ) ) ;
#81722=CARTESIAN_POINT ( 'NONE',  ( 56.98335268332530745, -57.67624654868168932, 97.45941025163602944 ) ) ;
#81725=CARTESIAN_POINT ( 'NONE',  ( 16.22921596069147654, -24.49376654032824874, -38.52325167225695424 ) ) ;
#81730=CARTESIAN_POINT ( 'NONE',  ( -21.88569129304039862, -60.00000000000001421, 40.49459113871581195 ) ) ;
#81736=CARTESIAN_POINT ( 'NONE',  ( -87.07927923840189521, -31.70337234844439323, 187.6114794693314423 ) ) ;
#81740=CARTESIAN_POINT ( 'NONE',  ( -8.083102543024720532, -29.03117134383523634, 28.72105206599581351 ) ) ;
#81743=CARTESIAN_POINT ( 'NONE',  ( -104.0121244633587878, -59.99999999999999289, 190.7717994844543909 ) ) ;
#81753=CARTESIAN_POINT ( 'NONE',  ( 72.07026148667476662, -59.99999999999998579, 154.8034499132735675 ) ) ;
#81754=CARTESIAN_POINT ( 'NONE',  ( 114.5925949185997439, -60.00000000000001421, 172.8113841322393682 ) ) ;
#81760=CARTESIAN_POINT ( 'NONE',  ( 34.17730524443083340, -14.21045842199440656, 38.95112099893761837 ) ) ;
#81775=CARTESIAN_POINT ( 'NONE',  ( -73.28166430171110335, -59.99999999999997868, 185.8704270832439818 ) ) ;
#81777=CARTESIAN_POINT ( 'NONE',  ( 84.62254331935226048, -60.00000000000000000, 199.8705729347711610 ) ) ;
#81778=CARTESIAN_POINT ( 'NONE',  ( -107.3650189024811681, -30.00000000000002842, 190.7478110277085648 ) ) ;
#81779=CARTESIAN_POINT ( 'NONE',  ( 17.08831453699968961, -56.87710783578985030, 33.63502463005767851 ) ) ;
#81780=CARTESIAN_POINT ( 'NONE',  ( 89.12305573924987812, -37.99999999999999289, 73.21436059126565965 ) ) ;
#81783=CARTESIAN_POINT ( 'NONE',  ( -47.01588246310362251, -29.15368591072060411, 43.19123847651081149 ) ) ;
#81797=CARTESIAN_POINT ( 'NONE',  ( 81.59718390748527383, -30.00000000000000711, -5.918344230650005144 ) ) ;
#81800=CARTESIAN_POINT ( 'NONE',  ( 92.42131551263139499, -30.00000000000000355, 102.6390630386317326 ) ) ;
#81811=EDGE_CURVE ( 'NONE', #16675, #85958, #82966, .T. ) ;
#81815=CARTESIAN_POINT ( 'NONE',  ( 86.53517077683734726, -38.61542584032831371, 199.3319270115290749 ) ) ;
#81818=VECTOR ( 'NONE', #26809, 1000.000000000000000 ) ;
#81834=( NAMED_UNIT ( * ) SI_UNIT ( $, .STERADIAN. ) SOLID_ANGLE_UNIT ( ) );
#81843=CARTESIAN_POINT ( 'NONE',  ( 85.63209264575189650, -32.09773112560883845, 181.8786679553494139 ) ) ;
#81846=CARTESIAN_POINT ( 'NONE',  ( 80.85454081142110283, -57.67117862881983825, -29.75008775089105839 ) ) ;
#81852=CARTESIAN_POINT ( 'NONE',  ( -81.23006925269818623, -30.00000000000000000, 0.5274897246537498807 ) ) ;
#81862=CARTESIAN_POINT ( 'NONE',  ( -18.42187549159172733, -25.79542283499425892, -30.46429929900222078 ) ) ;
#81871=CARTESIAN_POINT ( 'NONE',  ( -21.15837276345346041, -18.88847407013843949, -33.56547457277724078 ) ) ;
#81873=CARTESIAN_POINT ( 'NONE',  ( -24.94440323778573543, -21.77047479305005595, -29.25379890206748712 ) ) ;
#81875=ORIENTED_EDGE ( 'NONE', *, *, #85574, .F. ) ;
#81876=B_SPLINE_CURVE_WITH_KNOTS ( 'NONE', 3,
 ( #16643, #25299, #58157, #91084, #39866, #105128, #73808, #73261, #32854, #90000, #65731, #49532, #82441, #15574, #47403, #31782, #74338, #106161, #80298, #412, #81887, #32322, #48466, #81354, #16106, #105642, #65193, #6948, #8007, #33379 ),
 .UNSPECIFIED., .F., .F.,
 ( 4, 2, 2, 2, 2, 2, 2, 2, 2, 2, 2, 2, 2, 2, 4 ),
 ( 0.000000000000000000, 0.004502481766811746930, 0.009004963533623493860, 0.01800992706724694262, 0.02026116795065281695, 0.02251240883405868781, 0.02701489060087041219, 0.03601985413449383666, 0.04502481766811725766, 0.05402978120174068560, 0.05853226296855238570, 0.06303474473536410660, 0.06753722650217582057, 0.06978846738558167062, 0.07203970826898753455 ),
 .UNSPECIFIED. ) ;
#81885=CARTESIAN_POINT ( 'NONE',  ( -88.32040418460222497, -60.00000000000000711, -21.20476073071671763 ) ) ;
#81887=CARTESIAN_POINT ( 'NONE',  ( 17.04335540256958481, -25.31244954732083130, -30.48127871544292589 ) ) ;
#81907=CARTESIAN_POINT ( 'NONE',  ( -29.62390339563712160, -57.68322450639401211, 45.06481242858825453 ) ) ;
#81912=CARTESIAN_POINT ( 'NONE',  ( 33.15797435408901350, -29.99999999999994671, -37.92174772678599481 ) ) ;
#81913=CARTESIAN_POINT ( 'NONE',  ( -25.54656159126955117, -59.99999999999990763, 43.65498583421084788 ) ) ;
#81914=CARTESIAN_POINT ( 'NONE',  ( -54.70400683262975861, -18.68943135379251785, 51.56070947385185121 ) ) ;
#81917=CARTESIAN_POINT ( 'NONE',  ( -95.67593075084288046, -37.68573934914535783, 192.9981947302272260 ) ) ;
#81923=CARTESIAN_POINT ( 'NONE',  ( 110.0758566615390919, -38.35596056441075774, 185.5239908131719062 ) ) ;
#81929=CARTESIAN_POINT ( 'NONE',  ( 84.45385566677610711, -30.00000000000000355, 165.1424632750193382 ) ) ;
#81936=CARTESIAN_POINT ( 'NONE',  ( 48.74081811396350616, -56.82235822615641041, 54.29662734949555158 ) ) ;
#81940=CARTESIAN_POINT ( 'NONE',  ( -96.80470072259791436, -38.35514435266657074, 69.38109125240286801 ) ) ;
#81943=CARTESIAN_POINT ( 'NONE',  ( 91.32288730115537589, -38.35303533275899213, 27.69273911151131529 ) ) ;
#81946=CARTESIAN_POINT ( 'NONE',  ( 100.6486840550021640, -37.84864322520951418, 144.5881869147006000 ) ) ;
#81950=CARTESIAN_POINT ( 'NONE',  ( 74.36630564409178135, -60.00000000000000000, 175.8464028054124810 ) ) ;
#81953=FACE_OUTER_BOUND ( 'NONE', #53336, .T. ) ;
#81955=CARTESIAN_POINT ( 'NONE',  ( 61.32550633558473407, -25.58970342268792209, 69.10268843958327523 ) ) ;
#81957=CARTESIAN_POINT ( 'NONE',  ( -2.499999999999996003, -8.000000000000000000, -14.79019945774904166 ) ) ;
#81960=CARTESIAN_POINT ( 'NONE',  ( -69.83122382787961158, -29.99999999991972999, 126.8444822361123130 ) ) ;
#81973=CARTESIAN_POINT ( 'NONE',  ( 81.36577150990262908, -56.99468229981764722, 181.4257631377957125 ) ) ;
#81990=CARTESIAN_POINT ( 'NONE',  ( -11.33263781917016466, -20.80137080723078213, 35.49740132007826077 ) ) ;
#82012=CARTESIAN_POINT ( 'NONE',  ( -102.3130725222324173, -60.00000000000000000, 94.57084542267037364 ) ) ;
#82019=CARTESIAN_POINT ( 'NONE',  ( -85.33556072388859093, -25.38633735136824399, 170.5422650236019990 ) ) ;
#82021=EDGE_LOOP ( 'NONE', ( #87943, #60238, #51064, #103801, #70226, #56707 ) ) ;
#82037=CARTESIAN_POINT ( 'NONE',  ( 110.2448519957423940, -60.00000000000004974, 128.1456905595833575 ) ) ;
#82038=CARTESIAN_POINT ( 'NONE',  ( -109.5128114756446109, -29.99999999999999289, 168.1048973186342437 ) ) ;
#82039=CARTESIAN_POINT ( 'NONE',  ( -61.32847699634096017, -49.91700379991620906, 80.89165352633736461 ) ) ;
#82043=CARTESIAN_POINT ( 'NONE',  ( 94.41996065847817476, -60.00000000002924594, 4.935578748710270247 ) ) ;
#82047=CARTESIAN_POINT ( 'NONE',  ( 3.789235738929097472E-05, -46.43475214916913529, 31.62877531779723839 ) ) ;
#82056=CARTESIAN_POINT ( 'NONE',  ( -109.8027852057873304, -60.00000000000000000, 141.6978195183435787 ) ) ;
#82069=CARTESIAN_POINT ( 'NONE',  ( 105.7114380630162032, -60.00000000000002132, 157.1102875351544981 ) ) ;
#82070=CARTESIAN_POINT ( 'NONE',  ( -33.96339871129490007, -60.30850206294380200, 38.68848327799536690 ) ) ;
#82073=CARTESIAN_POINT ( 'NONE',  ( 40.12088697054482367, -60.25518400732138957, 43.34133863879944926 ) ) ;
#82076=CARTESIAN_POINT ( 'NONE',  ( -76.85615192407949792, -38.44451095924269168, 183.6527095178624336 ) ) ;
#82078=CARTESIAN_POINT ( 'NONE',  ( 2.499999999999999112, -9.944420556259451871, 19.25618705785077722 ) ) ;
#82088=CARTESIAN_POINT ( 'NONE',  ( 110.9798546403277442, -60.00000000000000711, 151.9418731052118403 ) ) ;
#82093=CARTESIAN_POINT ( 'NONE',  ( -97.76776492929941753, -29.99999999999996447, 190.7297597677326166 ) ) ;
#82107=CARTESIAN_POINT ( 'NONE',  ( 79.39643088476593391, -56.84711113037113961, 163.2850302358858983 ) ) ;
#82110=ORIENTED_EDGE ( 'NONE', *, *, #7708, .F. ) ;
#82115=CARTESIAN_POINT ( 'NONE',  ( -16.34903003639686503, -60.00000000000001421, -36.33396904264586880 ) ) ;
#82128=CARTESIAN_POINT ( 'NONE',  ( 23.25461545940108721, -27.85505135366320317, 37.69763505033436957 ) ) ;
#82147=CARTESIAN_POINT ( 'NONE',  ( 113.8984031219851545, -57.67123714865640949, 180.8430928919092935 ) ) ;
#82153=CARTESIAN_POINT ( 'NONE',  ( -80.26644129451693743, -59.99999999999999289, 196.3324352422349364 ) ) ;
#82158=CARTESIAN_POINT ( 'NONE',  ( -84.15525122082756582, -57.43313533274019989, 190.9243139192301442 ) ) ;
#82165=CARTESIAN_POINT ( 'NONE',  ( -84.40018563635376836, -45.26636761344531124, -9.144727243375324832 ) ) ;
#82170=CARTESIAN_POINT ( 'NONE',  ( 53.08934989192464826, -30.00000000000000000, 52.21148837440648549 ) ) ;
#82171=CARTESIAN_POINT ( 'NONE',  ( -14.86825985028395181, -1.734723475976807094E-15, -8.569529079644194525 ) ) ;
#82174=CARTESIAN_POINT ( 'NONE',  ( -32.64482578944674884, -14.21045842199435150, -35.33261186109891128 ) ) ;
#82175=CARTESIAN_POINT ( 'NONE',  ( -74.27483541950718404, -60.32442628959149999, 133.2375759543508025 ) ) ;
#82177=CARTESIAN_POINT ( 'NONE',  ( 77.40131791002600892, -14.21045842199445630, 153.6837402093314324 ) ) ;
#82179=CARTESIAN_POINT ( 'NONE',  ( 104.6107560558906471, -57.67118654542982625, 96.35458815996260284 ) ) ;
#82198=CARTESIAN_POINT ( 'NONE',  ( 29.96487401954387764, -56.85533909424443522, 36.18029637999577375 ) ) ;
#82215=CARTESIAN_POINT ( 'NONE',  ( 92.56707009034266775, -60.00000000000000000, -10.65961130115607247 ) ) ;
#82236=ORIENTED_EDGE ( 'NONE', *, *, #22220, .T. ) ;
#82237=CIRCLE ( 'NONE', #102879, 18.07003550757956845 ) ;
#82242=CARTESIAN_POINT ( 'NONE',  ( -58.93042220256725017, -59.99999999999997158, 79.07426381573431229 ) ) ;
#82244=CARTESIAN_POINT ( 'NONE',  ( 65.12589038046561996, -53.38532643392667865, 93.95558868601008840 ) ) ;
#82248=CARTESIAN_POINT ( 'NONE',  ( -94.73097995338159194, -57.65973493957909568, -7.453110678737913553 ) ) ;
#82270=CARTESIAN_POINT ( 'NONE',  ( -98.14828879091820113, -30.00000000000000355, 190.3627818008955899 ) ) ;
#82272=MECHANICAL_DESIGN_GEOMETRIC_PRESENTATION_REPRESENTATION('',(#73641),#9904);
#82275=CARTESIAN_POINT ( 'NONE',  ( 69.01947847511793555, -57.68200961577189645, 147.4487533431950226 ) ) ;
#82279=CARTESIAN_POINT ( 'NONE',  ( 5.739522349644341048, -21.75746304180372093, -38.54665207307362351 ) ) ;
#82282=CARTESIAN_POINT ( 'NONE',  ( -8.461568262860977185, -59.99999999999998579, 39.63601601260060647 ) ) ;
#82287=CARTESIAN_POINT ( 'NONE',  ( -86.21016422779933919, -53.80605556536726652, 192.1622240966613049 ) ) ;
#82291=CARTESIAN_POINT ( 'NONE',  ( -8.197116350937552198, -42.95771439283771542, 31.04260219330700465 ) ) ;
#82295=CARTESIAN_POINT ( 'NONE',  ( -98.59376555388014651, -59.99999999999996447, 196.3422130118438531 ) ) ;
#82307=CARTESIAN_POINT ( 'NONE',  ( 112.0515757376121542, -60.00000000000002842, 140.8507904390172598 ) ) ;
#82320=( BOUNDED_CURVE ( )  B_SPLINE_CURVE ( 2, ( #103848, #14827, #29994 ),
 .UNSPECIFIED., .F., .F. ) 
 B_SPLINE_CURVE_WITH_KNOTS ( ( 3, 3 ),
 ( 0.000000000000000000, 1.000000000000000000 ),
 .UNSPECIFIED. ) 
 CURVE ( )  GEOMETRIC_REPRESENTATION_ITEM ( )  RATIONAL_B_SPLINE_CURVE ( ( 1.000000000000000000, 1.857142857142858317, 1.000000000000000000 ) ) 
 REPRESENTATION_ITEM ( '' )  );
#82326=CARTESIAN_POINT ( 'NONE',  ( -30.56258723643923503, -59.99999999998762945, 46.02415584283473038 ) ) ;
#82330=CARTESIAN_POINT ( 'NONE',  ( 95.88519897241275203, -60.00000000000002842, 202.5558118362681626 ) ) ;
#82331=CARTESIAN_POINT ( 'NONE',  ( -108.4361608695136994, -30.00000000000004974, 186.7333242197273080 ) ) ;
#82332=CARTESIAN_POINT ( 'NONE',  ( 13.32414351401617303, -29.02978351584501837, 28.80459947957771760 ) ) ;
#82339=CARTESIAN_POINT ( 'NONE',  ( -43.48272077847599348, -56.80150791866010707, 46.32055055518623732 ) ) ;
#82352=CARTESIAN_POINT ( 'NONE',  ( 79.65125166320837025, -30.00000000000000000, -14.25942181426082556 ) ) ;
#82357=CARTESIAN_POINT ( 'NONE',  ( 90.43235478266818461, -29.99999999999999645, 91.02177936252034840 ) ) ;
#82372=CARTESIAN_POINT ( 'NONE',  ( 79.35189136647100838, -38.72593919592400624, 191.7211272454419202 ) ) ;
#82389=CARTESIAN_POINT ( 'NONE',  ( 35.12853135170308860, -35.58808086419043093, 44.33031536753241397 ) ) ;
#82396=CARTESIAN_POINT ( 'NONE',  ( 84.47753516669979490, -57.45055748378986493, 191.4165636158805057 ) ) ;
#82402=CARTESIAN_POINT ( 'NONE',  ( 94.71006489888094393, -57.65966216332807903, -7.938468930687816005 ) ) ;
#82407=CARTESIAN_POINT ( 'NONE',  ( -81.39487957031619203, -30.00000000000000355, -10.09601113538941597 ) ) ;
#82439=CARTESIAN_POINT ( 'NONE',  ( -81.46780060742058538, -60.00000000000000000, -27.04454207428921464 ) ) ;
#82441=CARTESIAN_POINT ( 'NONE',  ( 46.74337182782031164, -35.07991228416439355, -28.45280748186943853 ) ) ;
#82452=EDGE_CURVE ( 'NONE', #45904, #100031, #65765, .T. ) ;
#82457=CARTESIAN_POINT ( 'NONE',  ( -70.46077158043857480, -57.68242143155622159, 157.6729293506350018 ) ) ;
#82463=CARTESIAN_POINT ( 'NONE',  ( -32.64482578944674884, -14.21045842199435150, -35.33261186109891128 ) ) ;
#82467=CARTESIAN_POINT ( 'NONE',  ( -49.55661329154894901, -42.98050903381213317, 51.16523380042725222 ) ) ;
#82471=CARTESIAN_POINT ( 'NONE',  ( -99.19657323886772815, -45.25086945323192111, 193.2043375118490189 ) ) ;
#82477=CARTESIAN_POINT ( 'NONE',  ( 104.3671382054701269, -38.40621937790043461, 198.0855672510112981 ) ) ;
#82483=CARTESIAN_POINT ( 'NONE',  ( 84.80995380922897198, -30.00000000000000000, 168.5163431953775444 ) ) ;
#82490=CARTESIAN_POINT ( 'NONE',  ( 51.13673169834419241, -46.43880812507573808, 55.14390178788891461 ) ) ;
#82495=CARTESIAN_POINT ( 'NONE',  ( -92.68075250878385418, -38.35495479572327326, 40.78232060307920648 ) ) ;
#82498=CARTESIAN_POINT ( 'NONE',  ( 98.33859083302846216, -38.35583377044250852, 78.64617500602120970 ) ) ;
#82500=CARTESIAN_POINT ( 'NONE',  ( 96.00343290813454189, -45.28274520479027387, 106.3261782004091174 ) ) ;
#82501=CARTESIAN_POINT ( 'NONE',  ( -89.99999999999997158, -52.00000000000000000, 194.0238439516549818 ) ) ;
#82505=CARTESIAN_POINT ( 'NONE',  ( 74.38028640914956213, -60.00000000000000711, 175.9798948562111889 ) ) ;
#82509=CARTESIAN_POINT ( 'NONE',  ( 62.17692095058880142, -36.00921868072364163, 76.36134944486762777 ) ) ;
#82513=CARTESIAN_POINT ( 'NONE',  ( -87.05474304109419847, -38.36446612063756589, -20.80080902016944577 ) ) ;
#82526=CARTESIAN_POINT ( 'NONE',  ( 82.76483955553528915, -53.62660239749297375, 185.2436993791692998 ) ) ;
#82539=CARTESIAN_POINT ( 'NONE',  ( -8.340838532639699210, -19.57404221892459617, 35.25850611839925364 ) ) ;
#82554=CARTESIAN_POINT ( 'NONE',  ( 55.49475206934125282, -21.76998406339067671, -24.27117048680137756 ) ) ;
#82564=CARTESIAN_POINT ( 'NONE',  ( -95.53743085115178246, -59.99999999999999289, 52.85914003497030933 ) ) ;
#82572=CARTESIAN_POINT ( 'NONE',  ( -85.40752079689818288, -21.99789027431144461, 165.0058301840674915 ) ) ;
#82579=PLANE ( 'NONE',  #30660 ) ;
#82580=PRESENTATION_STYLE_ASSIGNMENT (( #50719 ) ) ;
#82587=CARTESIAN_POINT ( 'NONE',  ( 109.4365241820779460, -29.99999999999997158, 178.4894931318444264 ) ) ;
#82588=CARTESIAN_POINT ( 'NONE',  ( -103.0033221043092482, -14.21045842199434084, 193.8525198385365798 ) ) ;
#82589=CARTESIAN_POINT ( 'NONE',  ( -64.65631851940639763, -18.62622571681349015, 74.52696835048116952 ) ) ;
#82592=CARTESIAN_POINT ( 'NONE',  ( 114.3145214074224612, -60.00000000001458744, 180.5198259458585142 ) ) ;
#82594=CARTESIAN_POINT ( 'NONE',  ( 4.115445282636351898, -56.87775089494874692, 33.36138305263114745 ) ) ;
#82596=CARTESIAN_POINT ( 'NONE',  ( -100.6278159255352023, -37.82081252527048321, 144.5841055454753246 ) ) ;
#82603=CARTESIAN_POINT ( 'NONE',  ( -44.85383984935189972, -60.00000000000000000, 60.30378881490838694 ) ) ;
#82615=CARTESIAN_POINT ( 'NONE',  ( 86.91792654137822183, -60.00000000000002132, 29.36145308659259712 ) ) ;
#82616=CARTESIAN_POINT ( 'NONE',  ( -33.23717309666378128, -46.43422961256527515, 35.74388805338151798 ) ) ;
#82619=CARTESIAN_POINT ( 'NONE',  ( 42.14189753562169471, -39.52400511673570094, 40.59849300099191538 ) ) ;
#82624=CARTESIAN_POINT ( 'NONE',  ( -76.80863678880248813, -38.44002279010879164, 183.4121976866223918 ) ) ;
#82635=CARTESIAN_POINT ( 'NONE',  ( 108.2925581171813434, -59.99999999999999289, 131.0643579034831134 ) ) ;
#82641=CARTESIAN_POINT ( 'NONE',  ( -97.61388050977055286, -29.99999999999991118, 190.8267997822536302 ) ) ;
#82655=CARTESIAN_POINT ( 'NONE',  ( 80.02940799275995687, -53.38023646017801838, 163.9019173082060661 ) ) ;
#82663=CARTESIAN_POINT ( 'NONE',  ( -66.35471210918942120, -60.00000000000000000, -27.72999305472536236 ) ) ;
#82667=DIRECTION ( 'NONE',  ( 0.000000000000000000, -0.000000000000000000, 1.000000000000000000 ) ) ;
#82670=CARTESIAN_POINT ( 'NONE',  ( 86.58330031195315257, -46.47876529169381143, 190.3702665925659119 ) ) ;
#82688=CARTESIAN_POINT ( 'NONE',  ( 107.5635267603475143, -57.67122975978698918, 113.7780230091279492 ) ) ;
#82695=CARTESIAN_POINT ( 'NONE',  ( -81.88052546256818687, -59.99999999999998579, 197.9492418936315232 ) ) ;
#82698=CARTESIAN_POINT ( 'NONE',  ( -84.53199363263830435, -50.18958262607095122, 188.2551344591533109 ) ) ;
#82708=CARTESIAN_POINT ( 'NONE',  ( -84.20675286544745575, -45.26271561791529052, -10.90008403679102678 ) ) ;
#82718=CARTESIAN_POINT ( 'NONE',  ( 8.309465130445103043, -30.00000000000003197, -39.88086614825118659 ) ) ;
#82719=CARTESIAN_POINT ( 'NONE',  ( -76.37321092434198988, -36.02324841633205210, 123.8609354419510566 ) ) ;
#82720=ORIENTED_EDGE ( 'NONE', *, *, #11707, .T. ) ;
#82721=CARTESIAN_POINT ( 'NONE',  ( 74.38357847894150154, -30.00000000000000711, 152.0601407382578429 ) ) ;
#82723=CARTESIAN_POINT ( 'NONE',  ( 101.7828819589541496, -57.67122312341045642, 79.74621725149124529 ) ) ;
#82740=CARTESIAN_POINT ( 'NONE',  ( 28.40064430096010639, -36.00640833670148311, 32.00032701160584026 ) ) ;
#82744=ORIENTED_EDGE ( 'NONE', *, *, #14937, .T. ) ;
#82750=DIRECTION ( 'NONE',  ( 1.000000000000000000, 0.000000000000000000, 1.871721906610600077E-16 ) ) ;
#82756=CARTESIAN_POINT ( 'NONE',  ( 88.12498868022365173, -60.00000000000001421, -21.45487254486462447 ) ) ;
#82763=B_SPLINE_CURVE_WITH_KNOTS ( 'NONE', 3,
 ( #88905, #91574, #99644, #100703 ),
 .UNSPECIFIED., .F., .F.,
 ( 4, 4 ),
 ( 0.000000000000000000, 0.001455730951134404224 ),
 .UNSPECIFIED. ) ;
#82771=CARTESIAN_POINT ( 'NONE',  ( 87.02528036306804893, -60.18762643930987366, -6.133291105691159650 ) ) ;
#82780=CARTESIAN_POINT ( 'NONE',  ( -51.98383481243817528, -38.33605321803858601, 73.39120586448642314 ) ) ;
#82782=CARTESIAN_POINT ( 'NONE',  ( -61.64506658729265354, -59.99999999999998579, 86.85893902245692288 ) ) ;
#82784=CARTESIAN_POINT ( 'NONE',  ( 66.02827394672999617, -18.62689932795539960, 78.34043094791800854 ) ) ;
#82790=CARTESIAN_POINT ( 'NONE',  ( -113.3221076330293471, -57.67118219814813784, 155.4948299128208191 ) ) ;
#82800=DIRECTION ( 'NONE',  ( 0.000000000000000000, 0.000000000000000000, -1.000000000000000000 ) ) ;
#82810=CARTESIAN_POINT ( 'NONE',  ( 4.276117748942277252, -60.00000000000000711, 39.63074977821929679 ) ) ;
#82811=CARTESIAN_POINT ( 'NONE',  ( -96.93821243838389989, -30.00000000000000000, 191.1029387296386517 ) ) ;
#82815=CARTESIAN_POINT ( 'NONE',  ( 70.82442282108941356, -57.68208708914901450, 160.7729576061657610 ) ) ;
#82820=CARTESIAN_POINT ( 'NONE',  ( 5.331005461825221836, -21.69790887411561187, -38.54718089058046360 ) ) ;
#82822=CARTESIAN_POINT ( 'NONE',  ( -29.12862619358356753, -60.00000000000001421, 42.62327244784807334 ) ) ;
#82825=CARTESIAN_POINT ( 'NONE',  ( -86.89610268328752340, -35.42331563151877560, 187.9280089145808574 ) ) ;
#82826=ADVANCED_FACE ( 'NONE', ( #4938 ), #63178, .T. ) ;
#82830=CARTESIAN_POINT ( 'NONE',  ( -8.054587700577721776, -25.54953564508612729, 28.14066466568578662 ) ) ;
#82833=CARTESIAN_POINT ( 'NONE',  ( -102.1400935414211801, -60.00000000000002132, 193.9895109154659849 ) ) ;
#82843=CARTESIAN_POINT ( 'NONE',  ( 111.4777457387739048, -59.99999999999993605, 136.6117272317642630 ) ) ;
#82846=CYLINDRICAL_SURFACE ( 'NONE', #98774, 8.000000000000000000 ) ;
#82864=CARTESIAN_POINT ( 'NONE',  ( -40.15229402368767353, -60.00000000001941203, 56.59167717116910268 ) ) ;
#82868=CARTESIAN_POINT ( 'NONE',  ( 98.90601695972424068, -60.00000000000001421, 74.53410781496819482 ) ) ;
#82869=CARTESIAN_POINT ( 'NONE',  ( -71.69513722905418263, -59.99999999999990763, 172.8795092261717912 ) ) ;
#82870=CARTESIAN_POINT ( 'NONE',  ( 15.48353078592144172, -29.03023710598939289, 28.89585879851779282 ) ) ;
#82874=CARTESIAN_POINT ( 'NONE',  ( -40.33321577437346406, -18.77737895441734040, 34.22531594715925252 ) ) ;
#82887=CARTESIAN_POINT ( 'NONE',  ( 73.71532767159492039, -29.99999999990776445, 147.5689089691210540 ) ) ;
#82891=CARTESIAN_POINT ( 'NONE',  ( 81.97453080922707613, -30.00000000000000000, 33.68671043929276010 ) ) ;
#82909=CARTESIAN_POINT ( 'NONE',  ( 80.20710674972620779, -38.79645419531406958, 193.3540812050024158 ) ) ;
#82915=CARTESIAN_POINT ( 'NONE',  ( 96.81745522565726958, -37.99999999999980815, 192.8977754549547967 ) ) ;
#82926=ORIENTED_EDGE ( 'NONE', *, *, #18362, .F. ) ;
#82928=CARTESIAN_POINT ( 'NONE',  ( 85.16920355399095399, -46.56241956317034436, 187.9255957375985986 ) ) ;
#82932=CARTESIAN_POINT ( 'NONE',  ( 91.38762156947538529, -57.66273077560735771, -20.33768330290320137 ) ) ;
#82937=CARTESIAN_POINT ( 'NONE',  ( -81.36189305868806798, -30.00000000000000711, -1.402050496001596480 ) ) ;
#82960=CARTESIAN_POINT ( 'NONE',  ( -37.65422233906284077, -24.15452973042363638, -30.77166073587790507 ) ) ;
#82966=B_SPLINE_CURVE_WITH_KNOTS ( 'NONE', 3,
 ( #77620, #86263, #101363, #21022 ),
 .UNSPECIFIED., .F., .F.,
 ( 4, 4 ),
 ( 0.002500010780266304685, 0.005000000000000250772 ),
 .UNSPECIFIED. ) ;
#82972=CARTESIAN_POINT ( 'NONE',  ( -88.71913443814118239, -60.00000000000000711, -20.71346367143210188 ) ) ;
#82976=CARTESIAN_POINT ( 'NONE',  ( 101.5940187986382028, -52.72865695923380969, 192.6689692413239641 ) ) ;
#82977=CARTESIAN_POINT ( 'NONE',  ( 33.06001105660368466, -32.07477916797628126, 32.97354630382984197 ) ) ;
#82990=CARTESIAN_POINT ( 'NONE',  ( -24.14082041284044422, -57.67406494483144286, 42.97874410022470215 ) ) ;
#82995=CARTESIAN_POINT ( 'NONE',  ( -89.32121524059635931, -30.00000000000006750, 17.90039431539770121 ) ) ;
#82999=CARTESIAN_POINT ( 'NONE',  ( -50.59602062303963521, -22.19444373152758132, 45.92958069296322776 ) ) ;
#83002=CARTESIAN_POINT ( 'NONE',  ( -95.99521439327702410, -37.68773228063575687, 192.9684156188939994 ) ) ;
#83007=CARTESIAN_POINT ( 'NONE',  ( 105.0832242103311103, -38.39226450554996717, 197.4063297836361812 ) ) ;
#83014=CARTESIAN_POINT ( 'NONE',  ( 79.60966642660856962, -30.00000000000000711, 132.5630840557917054 ) ) ;
#83022=CARTESIAN_POINT ( 'NONE',  ( 52.60578561560112831, -60.30795294419101538, 63.32323424420151525 ) ) ;
#83029=CARTESIAN_POINT ( 'NONE',  ( -99.77955803787557443, -38.35585648701670891, 87.15852475401679555 ) ) ;
#83031=CARTESIAN_POINT ( 'NONE',  ( 109.4400761579602630, -38.35602592254275578, 149.2467366083292291 ) ) ;
#83033=CARTESIAN_POINT ( 'NONE',  ( 89.14633145472258491, -52.71673259819623070, 57.40858558930295885 ) ) ;
#83038=CARTESIAN_POINT ( 'NONE',  ( 74.01235824150077747, -59.99999999999999289, 172.3450624796163595 ) ) ;
#83041=CARTESIAN_POINT ( 'NONE',  ( 61.54115679619849288, -46.43610433826334827, 79.75840819081285815 ) ) ;
#83046=CARTESIAN_POINT ( 'NONE',  ( -87.97678914366765923, -38.37031391392313395, -19.61794280459611528 ) ) ;
#83058=CARTESIAN_POINT ( 'NONE',  ( 82.18972579398030121, -57.13749140910870494, 185.7775781806303428 ) ) ;
#83065=CARTESIAN_POINT ( 'NONE',  ( -16.85537930133409645, -24.70995007397846166, -38.51870997018118459 ) ) ;
#83067=CARTESIAN_POINT ( 'NONE',  ( 53.64466222910518667, -60.00000000000000711, 81.43429093339135250 ) ) ;
#83069=CARTESIAN_POINT ( 'NONE',  ( 10.39041109297083842, -13.86547299437372693, 31.87393420377066633 ) ) ;
#83071=CARTESIAN_POINT ( 'NONE',  ( -24.90621635141948076, -28.97586686355563401, 38.24361932259525787 ) ) ;
#83086=CARTESIAN_POINT ( 'NONE',  ( 43.48352109543510835, -21.77010373675058474, -26.80878052041629900 ) ) ;
#83094=CARTESIAN_POINT ( 'NONE',  ( -103.7206433085268884, -60.00000000000000000, 102.8025343256433075 ) ) ;
#83100=CARTESIAN_POINT ( 'NONE',  ( -83.36631949438019262, -39.47759878546305856, 173.2594340369611814 ) ) ;
#83114=DIRECTION ( 'NONE',  ( 0.000000000000000000, 1.000000000000000000, 0.000000000000000000 ) ) ;
#83115=CARTESIAN_POINT ( 'NONE',  ( -96.81748461682487061, -38.00000000001091394, 192.8978395531862020 ) ) ;
#83116=CARTESIAN_POINT ( 'NONE',  ( 106.9110190588319540, -14.21045842199441367, 176.0591306608180844 ) ) ;
#83119=CARTESIAN_POINT ( 'NONE',  ( -112.8607363433238930, -60.00000000000000000, 189.7948125560051551 ) ) ;
#83120=CARTESIAN_POINT ( 'NONE',  ( -58.58645841253417075, -32.54820420886014176, 65.51623946639922735 ) ) ;
#83123=CARTESIAN_POINT ( 'NONE',  ( 95.12578209733513290, -60.00000000000000000, 29.82219071690604295 ) ) ;
#83125=CARTESIAN_POINT ( 'NONE',  ( 2.989533877731477496, -25.54823926333440198, 28.14318220232473777 ) ) ;
#83126=CARTESIAN_POINT ( 'NONE',  ( -104.8017842743203119, -52.71024585296110132, 161.0970186293872075 ) ) ;
#83133=CARTESIAN_POINT ( 'NONE',  ( -70.37085192190031080, -60.00000000000000000, 143.4956404103314753 ) ) ;
#83138=CARTESIAN_POINT ( 'NONE',  ( 1.113440987313467412, 0.000000000000000000, 17.01589776168603763 ) ) ;
#83144=CARTESIAN_POINT ( 'NONE',  ( 86.47130672191026690, -60.00000000000002132, 2.175088770990013742 ) ) ;
#83145=CARTESIAN_POINT ( 'NONE',  ( -31.19799008952052333, -42.96357907512983587, 34.19655186448147788 ) ) ;
#83147=CARTESIAN_POINT ( 'NONE',  ( 46.29580480807258169, -39.52690699740247027, 45.26178483514620865 ) ) ;
#83148=CARTESIAN_POINT ( 'NONE',  ( 75.51533756583152979, -30.00000000000000355, -27.33238513093788669 ) ) ;
#83152=CARTESIAN_POINT ( 'NONE',  ( -78.18292533485022489, -38.59614680129968889, 188.7774352412195924 ) ) ;
#83156=CARTESIAN_POINT ( 'NONE',  ( 28.94718799180013491, -60.00000000000001421, 36.29242255566038722 ) ) ;
#83165=CARTESIAN_POINT ( 'NONE',  ( 103.6184096593837722, -60.00000000000000000, 102.2032741284876209 ) ) ;
#83169=CARTESIAN_POINT ( 'NONE',  ( -93.04034664274190902, -30.00000000000006040, 191.1271326182357768 ) ) ;
#83181=CARTESIAN_POINT ( 'NONE',  ( 82.36683156209987544, -36.02441109180747958, 158.6170004785897447 ) ) ;
#83208=EDGE_CURVE ( 'NONE', #100031, #91474, #82763, .T. ) ;
#83216=CARTESIAN_POINT ( 'NONE',  ( 114.0018284431585158, -57.67125466430193370, 179.4230632101373430 ) ) ;
#83221=CARTESIAN_POINT ( 'NONE',  ( -79.47475843766400772, -59.99999999999999289, 195.3002843663804242 ) ) ;
#83226=CARTESIAN_POINT ( 'NONE',  ( -86.15886759315432641, -21.41452658127618491, 176.4203065748977792 ) ) ;
#83234=CARTESIAN_POINT ( 'NONE',  ( -85.72908938792220113, -52.74455777896098141, -8.197128046888657593 ) ) ;
#83244=CARTESIAN_POINT ( 'NONE',  ( 40.74889026577078965, -14.21045842199439591, -34.22240887780809260 ) ) ;
#83245=CARTESIAN_POINT ( 'NONE',  ( -66.38286384437266463, -53.39006811827730559, 97.96284202452183365 ) ) ;
#83247=CARTESIAN_POINT ( 'NONE',  ( 57.89978660429063240, -59.99999999999999289, 101.6248911977562699 ) ) ;
#83249=CARTESIAN_POINT ( 'NONE',  ( 112.9340808439821586, -57.67120886779220257, 187.7003644414459416 ) ) ;
#83255=( GEOMETRIC_REPRESENTATION_CONTEXT ( 3 ) GLOBAL_UNCERTAINTY_ASSIGNED_CONTEXT ( ( #25767 ) ) GLOBAL_UNIT_ASSIGNED_CONTEXT ( ( #98562, #90486, #81834 ) ) REPRESENTATION_CONTEXT ( 'NONE', 'WORKASPACE' ) );
#83262=CARTESIAN_POINT ( 'NONE',  ( 25.05982991920904723, -4.285714285714296246, -3.301565691951509063 ) ) ;
#83272=CARTESIAN_POINT ( 'NONE',  ( 32.48479210146626173, -32.55386965233949326, 32.82066705911088178 ) ) ;
#83285=CARTESIAN_POINT ( 'NONE',  ( 87.61970871457796761, -60.00000000000001421, -22.01029353022440915 ) ) ;
#83299=CARTESIAN_POINT ( 'NONE',  ( 87.01069706264078718, -60.18282985975657340, -5.594890968212038018 ) ) ;
#83311=CARTESIAN_POINT ( 'NONE',  ( 76.80106626567913963, -49.90288268850643760, 137.4826183850342716 ) ) ;
#83317=CARTESIAN_POINT ( 'NONE',  ( -93.58432581829866592, -57.65368546899212987, -15.63533335066522767 ) ) ;
#83320=CARTESIAN_POINT ( 'NONE',  ( 105.1047905290744069, -52.71716997988711029, 165.8147597789577219 ) ) ;
#83336=CARTESIAN_POINT ( 'NONE',  ( -85.73097066636680097, -30.00000000000000355, 176.6817774525824802 ) ) ;
#83342=CARTESIAN_POINT ( 'NONE',  ( 71.53995275910023111, -57.67933612627984274, 167.4204919677856651 ) ) ;
#83346=CARTESIAN_POINT ( 'NONE',  ( 14.71715038006082565, -23.98991972335265999, -38.53165203909080105 ) ) ;
#83349=CARTESIAN_POINT ( 'NONE',  ( -38.20449057446243302, -60.00000000000000000, 49.74468476614604384 ) ) ;
#83352=CARTESIAN_POINT ( 'NONE',  ( -86.01546372622856040, -53.81628179863218975, 191.9611049542646128 ) ) ;
#83355=CARTESIAN_POINT ( 'NONE',  ( -9.379110170255547274, -56.88425848943947472, 33.37437879445704425 ) ) ;
#83361=( GEOMETRIC_REPRESENTATION_CONTEXT ( 3 ) GLOBAL_UNCERTAINTY_ASSIGNED_CONTEXT ( ( #63211 ) ) GLOBAL_UNIT_ASSIGNED_CONTEXT ( ( #27598, #67489, #43205 ) ) REPRESENTATION_CONTEXT ( 'NONE', 'WORKASPACE' ) );
#83370=CARTESIAN_POINT ( 'NONE',  ( 105.8555784348092885, -14.21045842199437637, 186.2209013957143782 ) ) ;
#83371=CARTESIAN_POINT ( 'NONE',  ( -83.03324683123243233, -32.55097867281028812, 159.1947170929300341 ) ) ;
#83383=ORIENTED_EDGE ( 'NONE', *, *, #18177, .T. ) ;
#83387=ADVANCED_FACE ( 'NONE', ( #33883 ), #74301, .T. ) ;
#83392=CARTESIAN_POINT ( 'NONE',  ( 104.7899765806434402, -60.00000000000002842, 199.3996562082950845 ) ) ;
#83393=CARTESIAN_POINT ( 'NONE',  ( -74.93456164446882894, -30.00000000000001421, 156.1801137937684985 ) ) ;
#83394=CARTESIAN_POINT ( 'NONE',  ( 16.76529464264830338, -39.47301229123248589, 30.70707182303599936 ) ) ;
#83398=CARTESIAN_POINT ( 'NONE',  ( -43.12859200516710700, -42.98411729920026403, 42.46969394239560103 ) ) ;
#83411=CARTESIAN_POINT ( 'NONE',  ( 77.85795165744811186, -30.00000000009750778, 181.6895375475956769 ) ) ;
#83416=CARTESIAN_POINT ( 'NONE',  ( 80.95702466713376566, -30.00000000000000355, 4.788817681754167666 ) ) ;
#83434=CARTESIAN_POINT ( 'NONE',  ( 71.12902128746809183, -38.32834665643905936, 140.8005624972594774 ) ) ;
#83455=CARTESIAN_POINT ( 'NONE',  ( 85.62573226540682469, -39.27103144633588272, 185.8533192315640008 ) ) ;
#83460=CARTESIAN_POINT ( 'NONE',  ( 94.64336416359569171, -57.65696167691804419, -9.478012974654758338 ) ) ;
#83464=CARTESIAN_POINT ( 'NONE',  ( -81.25802617709217657, -30.00000000000000711, -10.90515713852204271 ) ) ;
#83478=CARTESIAN_POINT ( 'NONE',  ( 68.12539969591429667, -29.92624738978073751, -21.66398342862366988 ) ) ;
#83482=CARTESIAN_POINT ( 'NONE',  ( -41.71284618355627316, -25.37309400074422072, -29.93689894554868758 ) ) ;
#83494=CARTESIAN_POINT ( 'NONE',  ( -50.02737965620911353, -60.00000000000000711, -37.89930100465098661 ) ) ;
#83497=CARTESIAN_POINT ( 'NONE',  ( 101.9301734557807322, -60.21151021950694116, 194.2770710414559687 ) ) ;
#83513=CARTESIAN_POINT ( 'NONE',  ( -22.17556693859086536, -57.67274538812966256, 42.55074624272938877 ) ) ;
#83517=CARTESIAN_POINT ( 'NONE',  ( -94.55497525217361954, -59.99999999999993605, 22.39874202688834615 ) ) ;
#83518=CARTESIAN_POINT ( 'NONE',  ( -51.04693240308429125, -29.11976890750409197, 48.95828090291404067 ) ) ;
#83522=CARTESIAN_POINT ( 'NONE',  ( -96.70315692490667914, -60.36316151395556773, 196.8125950864377387 ) ) ;
#83529=CARTESIAN_POINT ( 'NONE',  ( 80.86154658310535126, -38.83032902587230950, 194.4093053065819845 ) ) ;
#83533=CARTESIAN_POINT ( 'NONE',  ( 93.08106583031154457, -30.00000000000000000, 191.1326281931611106 ) ) ;
#83541=CARTESIAN_POINT ( 'NONE',  ( 53.38895677506906168, -25.63475069958329655, 51.75996385648595322 ) ) ;
#83546=CARTESIAN_POINT ( 'NONE',  ( -90.72424882750010511, -38.34306975412113161, 6.969030681448126430 ) ) ;
#83549=CARTESIAN_POINT ( 'NONE',  ( 110.3706048748884427, -38.35605039672871186, 158.9118694323576619 ) ) ;
#83551=CARTESIAN_POINT ( 'NONE',  ( 86.61308833284006425, -45.28267297219348819, 48.35240368102819986 ) ) ;
#83554=CARTESIAN_POINT ( 'NONE',  ( 74.76516655405903578, -59.99999999999997868, 179.4311784582239682 ) ) ;
#83555=CARTESIAN_POINT ( 'NONE',  ( -2.500000000000000888, -17.18734298064772759, 25.31896405944760531 ) ) ;
#83561=CARTESIAN_POINT ( 'NONE',  ( 63.02317967037522806, -22.10708017086810173, 71.83048262152487951 ) ) ;
#83570=CARTESIAN_POINT ( 'NONE',  ( 83.03373258142163138, -46.50209328944929865, 179.9266600372746723 ) ) ;
#83580=CARTESIAN_POINT ( 'NONE',  ( -21.34091502998213485, -26.33362732275400475, -38.46055773294248326 ) ) ;
#83583=CARTESIAN_POINT ( 'NONE',  ( 47.45147319089161897, -60.00000000000002132, 65.78626815950619289 ) ) ;
#83585=CARTESIAN_POINT ( 'NONE',  ( 8.695822068310066655, -13.47502420773152920, 31.95796511938647200 ) ) ;
#83588=CARTESIAN_POINT ( 'NONE',  ( -12.03844305070917997, -21.14040406273131012, 35.57043951055553066 ) ) ;
#83590=CARTESIAN_POINT ( 'NONE',  ( 0.000000000000000000, -8.000000000000000000, 0.000000000000000000 ) ) ;
#83598=CARTESIAN_POINT ( 'NONE',  ( -2.965789724133574889, -21.40052483609195022, -38.55044985044033012 ) ) ;
#83604=CARTESIAN_POINT ( 'NONE',  ( 28.05109246044522564, -21.77036439436171023, -28.92073443998052795 ) ) ;
#83613=CARTESIAN_POINT ( 'NONE',  ( -98.25489335440740035, -60.00000000000000711, 70.49837245525611706 ) ) ;
#83620=CARTESIAN_POINT ( 'NONE',  ( -83.42161577068522149, -39.47582673691351829, 173.7517446053938102 ) ) ;
#83630=CARTESIAN_POINT ( 'NONE',  ( -73.50473004590615744, -60.00000000000000000, -24.84693947030580574 ) ) ;
#83636=CARTESIAN_POINT ( 'NONE',  ( 87.30924545702741568, -14.21045842199429998, 28.19131950638903206 ) ) ;
#83637=CARTESIAN_POINT ( 'NONE',  ( -80.26890325034752038, -59.99999999999982947, 200.1011331233653721 ) ) ;
#83638=CARTESIAN_POINT ( 'NONE',  ( -57.23881194926001115, -42.96809999363954091, 66.85320747466838043 ) ) ;
#83641=CARTESIAN_POINT ( 'NONE',  ( 92.57024406876091405, -60.00000000000966338, -19.13806900009738499 ) ) ;
#83643=CARTESIAN_POINT ( 'NONE',  ( 7.155655305952319800, -42.95360862942818159, 31.03894574562138686 ) ) ;
#83644=CARTESIAN_POINT ( 'NONE',  ( -104.6942319917173450, -60.15544093628119526, 188.9572098072957829 ) ) ;
#83647=CARTESIAN_POINT ( 'NONE',  ( -80.26108746176230113, -60.00000000000001421, 196.3255223119888342 ) ) ;
#83652=CARTESIAN_POINT ( 'NONE',  ( 5.483224646671643221, 0.000000000000000000, 16.14659623658214116 ) ) ;
#83661=CARTESIAN_POINT ( 'NONE',  ( -32.52340609234104107, -56.84855274590991314, 37.29694331777213279 ) ) ;
#83663=CARTESIAN_POINT ( 'NONE',  ( 46.32781807547821984, -46.43946234991636857, 47.27666961722683681 ) ) ;
#83669=CARTESIAN_POINT ( 'NONE',  ( -78.44477202083649559, -38.62748133887316015, 189.5277942107175306 ) ) ;
#83683=CARTESIAN_POINT ( 'NONE',  ( 108.9316662144759817, -60.00000000000001421, 135.4909546950748904 ) ) ;
#83690=CARTESIAN_POINT ( 'NONE',  ( -96.41186482556817339, -29.99999999999981526, 191.2305605891251901 ) ) ;
#83701=CARTESIAN_POINT ( 'NONE',  ( 84.31892941953071841, -22.12908237796155220, 154.7626912266840975 ) ) ;
#83706=CARTESIAN_POINT ( 'NONE',  ( 89.99999999999997158, -52.00000000000000000, 198.0238439516549818 ) ) ;
#83717=CARTESIAN_POINT ( 'NONE',  ( 87.30971457308248773, -31.67967750561784968, 188.1757596176438199 ) ) ;
#83733=DIRECTION ( 'NONE',  ( 0.000000000000000000, 0.000000000000000000, -1.000000000000000000 ) ) ;
#83742=CARTESIAN_POINT ( 'NONE',  ( -83.39409730309102997, -59.99999999999998579, 199.1218053928312770 ) ) ;
#83749=CARTESIAN_POINT ( 'NONE',  ( -86.01685430178015679, -24.89350102973689971, 179.1283417026938878 ) ) ;
#83756=CARTESIAN_POINT ( 'NONE',  ( -84.49387577902174939, -45.26915323538062808, -6.724149892752078195 ) ) ;
#83764=CARTESIAN_POINT ( 'NONE',  ( 74.10901235487826000, -60.00000000000013500, 189.8092491115571647 ) ) ;
#83766=CARTESIAN_POINT ( 'NONE',  ( -56.79577812574758156, -14.21045842199439591, -31.02744264688941556 ) ) ;
#83767=CARTESIAN_POINT ( 'NONE',  ( -68.46050526737764130, -22.10827440420577616, 87.18976234775816181 ) ) ;
#83769=CARTESIAN_POINT ( 'NONE',  ( 78.18398495971976558, -30.00000000000001421, 185.0784753857526539 ) ) ;
#83771=CARTESIAN_POINT ( 'NONE',  ( 94.37133057941774439, -57.65304023162428138, -12.34840853396864269 ) ) ;
#83794=CARTESIAN_POINT ( 'NONE',  ( 32.17265427855518567, -49.90131150188997822, 35.87558796595580901 ) ) ;
#83811=CARTESIAN_POINT ( 'NONE',  ( 91.38620944121281298, -60.00000000000000711, -15.95155868622245521 ) ) ;
#83827=CARTESIAN_POINT ( 'NONE',  ( 82.19860323403510449, -37.81518911496591784, -13.38202468312296389 ) ) ;
#83842=CARTESIAN_POINT ( 'NONE',  ( 71.46833319993017142, -32.53831864036357047, 102.5522570331628458 ) ) ;
#83849=CARTESIAN_POINT ( 'NONE',  ( -93.81425292840387442, -57.67376786465794680, 13.59058164905135513 ) ) ;
#83852=CARTESIAN_POINT ( 'NONE',  ( 104.7030407962678282, -52.71701985175332794, 182.7871775134649113 ) ) ;
#83865=ORIENTED_EDGE ( 'NONE', *, *, #88264, .T. ) ;
#83870=CARTESIAN_POINT ( 'NONE',  ( -84.25106516082894359, -30.00000000000000355, 163.2648472752855184 ) ) ;
#83874=CARTESIAN_POINT ( 'NONE',  ( 67.63584330748660989, -57.68118349180133464, 139.1929817678663994 ) ) ;
#83877=CARTESIAN_POINT ( 'NONE',  ( 46.71504066713215053, -34.79384376595470485, -36.65170777883916031 ) ) ;
#83879=CARTESIAN_POINT ( 'NONE',  ( -43.53171589075616055, -60.00000000000002132, 57.82064124434394614 ) ) ;
#83884=CARTESIAN_POINT ( 'NONE',  ( -86.68224123219718535, -24.39526350757373052, 184.9923197224934484 ) ) ;
#83887=CARTESIAN_POINT ( 'NONE',  ( -1.994277754766871968, -29.03106682059618748, 28.72592687327638217 ) ) ;
#83900=FILL_AREA_STYLE ('',( #26251 ) ) ;
#83902=CARTESIAN_POINT ( 'NONE',  ( 114.5100518737696689, -60.00000000000002132, 177.0882855716755557 ) ) ;
#83903=CARTESIAN_POINT ( 'NONE',  ( -83.89923350218229814, -18.67999242611703536, 147.1925220706413597 ) ) ;
#83906=CARTESIAN_POINT ( 'NONE',  ( 0.000000000000000000, 0.000000000000000000, 0.000000000000000000 ) ) ;
#83927=CARTESIAN_POINT ( 'NONE',  ( 97.11419591411292629, -60.00000000000001421, 63.44341482763463347 ) ) ;
#83928=CARTESIAN_POINT ( 'NONE',  ( -78.42690035548760363, -14.21045842199427156, 178.5095186877798028 ) ) ;
#83929=CARTESIAN_POINT ( 'NONE',  ( 21.04530086232624342, -29.03383587574997904, 29.34416034787003724 ) ) ;
#83932=CARTESIAN_POINT ( 'NONE',  ( -42.40463338888051226, -18.78660199041541290, 35.79879680396032171 ) ) ;
#83946=CARTESIAN_POINT ( 'NONE',  ( 81.20719313386280191, -29.99999999999995026, 0.8620750168147771619 ) ) ;
#83952=CARTESIAN_POINT ( 'NONE',  ( 81.50579677117252686, -29.99999999999999645, 28.64214509496276051 ) ) ;
#83969=CARTESIAN_POINT ( 'NONE',  ( 76.07586837099985644, -38.38264828878220669, 178.9567494468272741 ) ) ;
#83994=CARTESIAN_POINT ( 'NONE',  ( 84.61807758326956730, -53.82215636532191638, 190.0709679738065745 ) ) ;
#83999=CARTESIAN_POINT ( 'NONE',  ( 91.48116923616865392, -57.66238768136772563, -20.18913141313222681 ) ) ;
#84002=CARTESIAN_POINT ( 'NONE',  ( -82.36074577633510785, -30.00000000000000355, 37.46041508329808778 ) ) ;
#84012=CARTESIAN_POINT ( 'NONE',  ( -19.67392556837618400, -25.14117008353909455, 28.53997366849857542 ) ) ;
#84017=CARTESIAN_POINT ( 'NONE',  ( 46.14432154257043806, -26.57843610561197423, -28.93710014874023528 ) ) ;
#84020=CARTESIAN_POINT ( 'NONE',  ( -23.46199991564613896, -32.51939257062084465, 30.27833130048637855 ) ) ;
#84025=CARTESIAN_POINT ( 'NONE',  ( -63.85241486307079128, -29.65655549946883340, -23.53290650701330833 ) ) ;
#84039=CARTESIAN_POINT ( 'NONE',  ( 99.38929497627960075, -45.26971556542965658, 193.0884266367296505 ) ) ;
#84043=AXIS2_PLACEMENT_3D ( 'NONE', #46715, #22999, #69940 ) ;
#84054=CARTESIAN_POINT ( 'NONE',  ( -26.05015581842503991, -57.67603816461070920, 43.50693983564572420 ) ) ;
#84061=CARTESIAN_POINT ( 'NONE',  ( -94.38155987036965655, -60.00000000000007105, 5.296623108471039565 ) ) ;
#84063=CARTESIAN_POINT ( 'NONE',  ( -50.96199133419289495, -32.58464942492616956, 49.99883352212385290 ) ) ;
#84071=CARTESIAN_POINT ( 'NONE',  ( 77.19326105945918925, -38.47784706899123819, 185.3049776433571765 ) ) ;
#84076=CARTESIAN_POINT ( 'NONE',  ( 86.97982282064982940, -29.99999999999999645, 183.6336763072494023 ) ) ;
#84083=CARTESIAN_POINT ( 'NONE',  ( 51.23517877398742826, -42.97391562393161024, 54.09909760496220343 ) ) ;
#84089=CARTESIAN_POINT ( 'NONE',  ( -90.00912977251989844, -38.39750930754247094, -15.99775578366946149 ) ) ;
#84093=CARTESIAN_POINT ( 'NONE',  ( 110.2760654704705416, -38.35601861863470674, 184.1510513626866441 ) ) ;
#84095=CARTESIAN_POINT ( 'NONE',  ( 83.49139130404353182, -37.85069686451048909, 31.99470159126698121 ) ) ;
#84096=FACE_OUTER_BOUND ( 'NONE', #60314, .T. ) ;
#84099=ADVANCED_FACE ( 'NONE', ( #22508 ), #91983, .F. ) ;
#84104=CARTESIAN_POINT ( 'NONE',  ( 60.69206503066401126, -60.33900397284496364, 84.28633839224548296 ) ) ;
#84115=CARTESIAN_POINT ( 'NONE',  ( 24.08218120605116397, -18.86977045670454700, 31.47062207553021906 ) ) ;
#84121=CARTESIAN_POINT ( 'NONE',  ( 84.23407561538746791, -35.92907227037686368, 175.7388898281075740 ) ) ;
#84129=CARTESIAN_POINT ( 'NONE',  ( -18.81654674752487821, -25.40603723063000530, -38.49895005552811256 ) ) ;
#84133=CARTESIAN_POINT ( 'NONE',  ( 47.86266428647820703, -60.00000000000000000, 66.71390725780067044 ) ) ;
#84135=CARTESIAN_POINT ( 'NONE',  ( 35.96520222810764267, -36.00751560667545448, 45.14789304285356053 ) ) ;
#84138=CARTESIAN_POINT ( 'NONE',  ( 20.76631208310896781, -17.42254526309043072, 31.47037444563865449 ) ) ;
#84140=CARTESIAN_POINT ( 'NONE',  ( -38.04692939061810364, -36.94347500124628425, 47.39189219977645706 ) ) ;
#84142=DIRECTION ( 'NONE',  ( 0.000000000000000000, -0.000000000000000000, 1.000000000000000000 ) ) ;
#84153=CARTESIAN_POINT ( 'NONE',  ( 48.31748088701653643, -60.22827261165075896, -32.41382024327764100 ) ) ;
#84166=CARTESIAN_POINT ( 'NONE',  ( -102.5570158079410135, -60.00000000000000711, 95.99420030246923830 ) ) ;
#84173=CARTESIAN_POINT ( 'NONE',  ( -82.08609670664580449, -49.97993307730780543, 177.5978396368247729 ) ) ;
#84179=DIRECTION ( 'NONE',  ( -0.000000000000000000, 1.000000000000000000, -0.000000000000000000 ) ) ;
#84183=FACE_OUTER_BOUND ( 'NONE', #40123, .T. ) ;
#84188=FACE_OUTER_BOUND ( 'NONE', #5580, .T. ) ;
#84190=CARTESIAN_POINT ( 'NONE',  ( 102.0720237449618679, -14.21045842199434439, 125.2221798637976349 ) ) ;
#84191=CARTESIAN_POINT ( 'NONE',  ( -72.11328378729270128, -60.00000000000007816, 177.1367255069332316 ) ) ;
#84192=CARTESIAN_POINT ( 'NONE',  ( -59.49377889082170867, -56.86590393334827098, 79.18203250951856376 ) ) ;
#84196=CARTESIAN_POINT ( 'NONE',  ( -102.7734312727401829, -37.82045702703825185, 170.2527634601842976 ) ) ;
#84202=CARTESIAN_POINT ( 'NONE',  ( -71.67561706003607469, -60.00000000000001421, 151.8435231814522126 ) ) ;
#84207=CARTESIAN_POINT ( 'NONE',  ( 10.38441970550273119, 0.000000000000000000, -13.52487676487348978 ) ) ;
#84214=CARTESIAN_POINT ( 'NONE',  ( -30.28151271900150832, -49.91080145115500244, 35.08722031216328929 ) ) ;
#84216=CARTESIAN_POINT ( 'NONE',  ( 45.70191470550344093, -60.25745932227290069, 50.30639238928311130 ) ) ;
#84221=CARTESIAN_POINT ( 'NONE',  ( -93.08574300709510396, -38.49591865938590729, 201.1221301499342360 ) ) ;
#84225=CARTESIAN_POINT ( 'NONE',  ( 22.91543575571316183, -60.00000000000000711, 34.83253428109101435 ) ) ;
#84226=CARTESIAN_POINT ( 'NONE',  ( -10.00000000000000178, -15.00000000000000000, -9.999999999999998224 ) ) ;
#84233=CARTESIAN_POINT ( 'NONE',  ( 102.1238087080854626, -60.00000000000000000, 93.46745215179672073 ) ) ;
#84251=CARTESIAN_POINT ( 'NONE',  ( 81.09979694935459804, -49.92208873302202221, 168.6177104633348449 ) ) ;
#84267=CARTESIAN_POINT ( 'NONE',  ( 86.77293047539107818, -57.38694033980660691, 193.7425620307543284 ) ) ;
#84291=CARTESIAN_POINT ( 'NONE',  ( -90.18900329953886796, -59.99999999999999289, 202.0050657913863574 ) ) ;
#84292=VECTOR ( 'NONE', #29278, 1000.000000000000000 ) ;
#84297=CARTESIAN_POINT ( 'NONE',  ( -85.78622453063103137, -28.51040679079540396, 180.2837960777752926 ) ) ;
#84303=CARTESIAN_POINT ( 'NONE',  ( -82.89586554537308416, -37.82252042144357773, 0.5134924856167544238 ) ) ;
#84312=CARTESIAN_POINT ( 'NONE',  ( 70.38659604113041723, -14.21045842199445808, 117.5484250040930050 ) ) ;
#84314=CARTESIAN_POINT ( 'NONE',  ( -89.90470572912276737, -30.00000000000002842, -11.15078749779565825 ) ) ;
#84315=CARTESIAN_POINT ( 'NONE',  ( -73.44956775615928279, -36.01767715975007178, 111.7754548667898860 ) ) ;
#84317=CARTESIAN_POINT ( 'NONE',  ( 73.11766847789152735, -30.00000000000003197, 143.8471250665463117 ) ) ;
#84319=VERTEX_POINT ( 'NONE', #25431 ) ;
#84320=CARTESIAN_POINT ( 'NONE',  ( 30.73846156699857346, -57.67116533035498094, -42.81922766351370058 ) ) ;
#84345=CARTESIAN_POINT ( 'NONE',  ( 31.94500641777023375, -39.48962315678958390, 33.87780594823525604 ) ) ;
#84346=CARTESIAN_POINT ( 'NONE',  ( -25.22241582816893413, -4.285714285714285587, 3.301606509427073455 ) ) ;
#84361=CARTESIAN_POINT ( 'NONE',  ( 87.53966758494706824, -59.99999999999999289, -22.09775139173853731 ) ) ;
#84375=CARTESIAN_POINT ( 'NONE',  ( 85.54848234686721753, -60.20738201045722349, -15.09784675847152613 ) ) ;
#84389=CARTESIAN_POINT ( 'NONE',  ( 77.90007794136121788, -29.08184770833722865, 125.1920107075117983 ) ) ;
#84394=CARTESIAN_POINT ( 'NONE',  ( -91.87475470944771416, -57.66094841159801376, -19.53952869114660373 ) ) ;
#84398=CARTESIAN_POINT ( 'NONE',  ( 102.2581492532549419, -37.84842508405214545, 182.3710817063251568 ) ) ;
#84415=CARTESIAN_POINT ( 'NONE',  ( -89.14411627724076936, -30.00000000000000711, 188.9134825190658944 ) ) ;
#84420=CARTESIAN_POINT ( 'NONE',  ( 72.55415673912993668, -57.66409419474867093, 177.4493738948018233 ) ) ;
#84421=DIRECTION ( 'NONE',  ( 0.000000000000000000, -1.000000000000000000, 0.000000000000000000 ) ) ;
#84426=CARTESIAN_POINT ( 'NONE',  ( 46.69156559559471731, -34.78800018587544685, -36.65496307456758984 ) ) ;
#84428=CARTESIAN_POINT ( 'NONE',  ( -36.18825654482056819, -59.99999999999999289, 47.53788091366800472 ) ) ;
#84433=CARTESIAN_POINT ( 'NONE',  ( -86.45107053092409899, -35.49386078015379553, 186.8406724003439763 ) ) ;
#84436=CARTESIAN_POINT ( 'NONE',  ( -3.964250166353671112, -18.58602789357551544, 26.98074317074543416 ) ) ;
#84449=CARTESIAN_POINT ( 'NONE',  ( 100.7779335074592524, -14.21045842199434084, 117.1442511085924565 ) ) ;
#84450=CARTESIAN_POINT ( 'NONE',  ( -80.99376376317795234, -36.03179907666569193, 148.3448988380689286 ) ) ;
#84454=CARTESIAN_POINT ( 'NONE',  ( 49.85179264443584657, -57.67837586547972961, 76.80686450657027819 ) ) ;
#84468=VERTEX_POINT ( 'NONE', #44786 ) ;
#84469=CARTESIAN_POINT ( 'NONE',  ( 111.1380688386296356, -59.99999999999998579, 186.6089157120882192 ) ) ;
#84470=CARTESIAN_POINT ( 'NONE',  ( -75.52856519143354319, -59.99999999999994316, 193.8568173627997737 ) ) ;
#84471=CARTESIAN_POINT ( 'NONE',  ( 24.22882282971767864, -56.87184356490050163, 34.54272924709754733 ) ) ;
#84476=EDGE_CURVE ( 'NONE', #91694, #6703, #67772, .T. ) ;
#84477=CARTESIAN_POINT ( 'NONE',  ( -41.77985743548467923, -29.15823557948370492, 37.78287941733934474 ) ) ;
#84490=CARTESIAN_POINT ( 'NONE',  ( 101.0624751218346660, -29.99999999999999289, 167.4344596707726680 ) ) ;
#84494=CARTESIAN_POINT ( 'NONE',  ( 81.97181451191005408, -30.00000000000001066, 33.65921166970361611 ) ) ;
#84514=CARTESIAN_POINT ( 'NONE',  ( 75.45453868462554681, -38.35108631456310491, 173.7963811085962789 ) ) ;
#84527=ORIENTED_EDGE ( 'NONE', *, *, #106672, .T. ) ;
#84538=CARTESIAN_POINT ( 'NONE',  ( 86.39088408274903941, -17.34302421594473742, 179.9388769400421779 ) ) ;
#84542=CARTESIAN_POINT ( 'NONE',  ( 5.615325946863288564, -57.67109132440626240, -44.55232355965021185 ) ) ;
#84546=CARTESIAN_POINT ( 'NONE',  ( -94.02980808522455902, -30.00000000000000711, 112.1455996697054900 ) ) ;
#84547=AXIS2_PLACEMENT_3D ( 'NONE', #70564, #5297, #88343 ) ;
#84554=CARTESIAN_POINT ( 'NONE',  ( -32.00612393675804412, -31.56328806623667660, 32.42231260273467086 ) ) ;
#84559=CARTESIAN_POINT ( 'NONE',  ( 56.43757173888357670, -28.73354875062528890, -26.14196234985615064 ) ) ;
#84560=CARTESIAN_POINT ( 'NONE',  ( -26.15948994066758715, -25.57049903555443748, 29.61355792721284175 ) ) ;
#84566=CARTESIAN_POINT ( 'NONE',  ( -16.83015825594305426, -42.95785322665913952, 31.29329447951673870 ) ) ;
#84568=CARTESIAN_POINT ( 'NONE',  ( -60.15663760392290982, -29.26964696484472483, -24.92025292455906893 ) ) ;
#84572=CARTESIAN_POINT ( 'NONE',  ( -64.94678499638771996, -34.58945069958795671, -23.72257533880744873 ) ) ;
#84573=ORIENTED_EDGE ( 'NONE', *, *, #105601, .T. ) ;
#84582=CARTESIAN_POINT ( 'NONE',  ( 101.0491831504412659, -52.74036209462195046, 193.3224896004936681 ) ) ;
#84583=CARTESIAN_POINT ( 'NONE',  ( 8.922146979286338819, -20.27139005636187008, 27.26475389761597512 ) ) ;
#84587=ORIENTED_EDGE ( 'NONE', *, *, #78451, .F. ) ;
#84596=CARTESIAN_POINT ( 'NONE',  ( -101.3184166277729048, -59.99999999996092725, 74.64939812631605776 ) ) ;
#84600=CARTESIAN_POINT ( 'NONE',  ( -85.55948822751662419, -29.99999999999991829, -20.40846083852196813 ) ) ;
#84602=CARTESIAN_POINT ( 'NONE',  ( -50.14550149790785838, -42.97898697507390153, 52.14561158908378502 ) ) ;
#84611=CARTESIAN_POINT ( 'NONE',  ( 105.4486652112230018, -38.38584500015401346, 197.0171471424765173 ) ) ;
#84615=CARTESIAN_POINT ( 'NONE',  ( 87.76354976536211439, -30.00000000000000711, 186.1681723011733993 ) ) ;
#84619=VECTOR ( 'NONE', #38101, 1000.000000000000000 ) ;
#84620=EDGE_LOOP ( 'NONE', ( #4065, #7170, #85935, #37365, #62457 ) ) ;
#84622=CARTESIAN_POINT ( 'NONE',  ( 51.80856163756618571, -22.18394510151134469, 47.83007306119799296 ) ) ;
#84626=CARTESIAN_POINT ( 'NONE',  ( -85.43130989759367822, -38.35985338504925579, -22.45028662619849058 ) ) ;
#84628=CARTESIAN_POINT ( 'NONE',  ( 106.8950603560237482, -38.36540817785023449, 195.0234272126446342 ) ) ;
#84630=CARTESIAN_POINT ( 'NONE',  ( 87.99907843909515748, -45.28282746162219752, 58.11307062178342875 ) ) ;
#84634=EDGE_CURVE ( 'NONE', #90543, #85237, #9198, .T. ) ;
#84652=CARTESIAN_POINT ( 'NONE',  ( 50.79025413206112205, -29.86198917105789619, 47.81129180970600601 ) ) ;
#84656=CARTESIAN_POINT ( 'NONE',  ( 83.72818806616849940, -42.97983555213142637, 180.3459984342655957 ) ) ;
#84661=CARTESIAN_POINT ( 'NONE',  ( -100.3578242334469337, -52.71019514449881882, 125.2399389498935136 ) ) ;
#84665=CARTESIAN_POINT ( 'NONE',  ( -18.18925383356936720, -25.18032758874422683, -38.50619832935123554 ) ) ;
#84666=CARTESIAN_POINT ( 'NONE',  ( 41.57491510848411309, -60.00000000000000000, 54.47207502686755021 ) ) ;
#84668=CARTESIAN_POINT ( 'NONE',  ( 27.30418487774501202, -30.61949767632602715, 39.20238763744198707 ) ) ;
#84670=CARTESIAN_POINT ( 'NONE',  ( 19.73225841471719022, -16.99122103950224627, 31.48169930546135120 ) ) ;
#84671=CARTESIAN_POINT ( 'NONE',  ( -35.29827408586819359, -35.67579097495918461, 44.48726958153784494 ) ) ;
#84684=CARTESIAN_POINT ( 'NONE',  ( 38.79056939014538585, -60.22819850092196958, -34.02320223531833676 ) ) ;
#84694=CARTESIAN_POINT ( 'NONE',  ( -92.06170028002134131, -60.00000000000000000, 19.77329225891599407 ) ) ;
#84700=CARTESIAN_POINT ( 'NONE',  ( -81.96316505919669737, -49.96949351764808256, 176.6395136813214606 ) ) ;
#84704=EDGE_LOOP ( 'NONE', ( #33178, #41697, #2065, #17660 ) ) ;
#84711=CARTESIAN_POINT ( 'NONE',  ( -95.04855897266367037, -57.67186573470212352, 33.03592761066350647 ) ) ;
#84718=CARTESIAN_POINT ( 'NONE',  ( 94.55541571559547265, -59.99999999999990763, 22.40038052076814878 ) ) ;
#84720=CARTESIAN_POINT ( 'NONE',  ( -75.43392636619238090, -30.00000000000003553, 160.3050061908775206 ) ) ;
#84722=CARTESIAN_POINT ( 'NONE',  ( -57.28148858968405222, -56.86046258776218565, 73.21236583999979075 ) ) ;
#84726=CARTESIAN_POINT ( 'NONE',  ( -101.5550978881653776, -37.82069211984403978, 186.3190918155810891 ) ) ;
#84727=SURFACE_STYLE_USAGE ( .BOTH. , #44817 ) ;
#84733=CARTESIAN_POINT ( 'NONE',  ( -74.98993051287176570, -60.00000000000002132, 181.2383444034526292 ) ) ;
#84737=DIRECTION ( 'NONE',  ( 0.000000000000000000, -1.000000000000000000, 0.000000000000000000 ) ) ;
#84738=CARTESIAN_POINT ( 'NONE',  ( 16.46939662768644652, -0.000000000000000000, -4.418225343323719301 ) ) ;
#84744=CARTESIAN_POINT ( 'NONE',  ( -30.11975150981648852, -60.33646582423781979, 36.84978483557001994 ) ) ;
#84748=CARTESIAN_POINT ( 'NONE',  ( 45.39934709178754701, -29.15827231024250921, 41.32491508119058210 ) ) ;
#84752=CARTESIAN_POINT ( 'NONE',  ( -85.96729481479134449, -38.64372570064532653, 199.0413494251739337 ) ) ;
#84754=CARTESIAN_POINT ( 'NONE',  ( 84.55232465008280940, -38.35844130464479207, -23.23874272793522877 ) ) ;
#84756=CARTESIAN_POINT ( 'NONE',  ( 38.00499196079799447, -59.99999999999999289, 41.32896168422335847 ) ) ;
#84763=CARTESIAN_POINT ( 'NONE',  ( 112.2172298700076283, -60.00000000000000711, 170.6121558011703598 ) ) ;
#84771=( NAMED_UNIT ( * ) PLANE_ANGLE_UNIT ( ) SI_UNIT ( $, .RADIAN. ) );
#84775=CARTESIAN_POINT ( 'NONE',  ( 89.99999999999997158, -60.00000000000000000, 194.0238439516549818 ) ) ;
#84781=ORIENTED_EDGE ( 'NONE', *, *, #57496, .T. ) ;
#84782=CARTESIAN_POINT ( 'NONE',  ( 83.05514034890428832, -36.01272047364142992, 164.7561459065111364 ) ) ;
#84799=FACE_OUTER_BOUND ( 'NONE', #9527, .T. ) ;
#84801=CARTESIAN_POINT ( 'NONE',  ( 86.36684635806597043, -61.01915684967102038, 194.5641491802014968 ) ) ;
#84813=EDGE_CURVE ( 'NONE', #40814, #70795, #32855, .T. ) ;
#84814=STYLED_ITEM ( 'NONE', ( #48936 ), #43474 ) ;
#84825=CARTESIAN_POINT ( 'NONE',  ( -106.0920714368447193, -60.00000000000001421, 198.1769906956861860 ) ) ;
#84831=CARTESIAN_POINT ( 'NONE',  ( -85.93749938942525546, -24.97245962735015112, 178.1374030527065599 ) ) ;
#84836=CARTESIAN_POINT ( 'NONE',  ( -82.65196724022408148, -37.83200599901501704, 4.245451695380549673 ) ) ;
#84842=CARTESIAN_POINT ( 'NONE',  ( 67.91784306603950938, -14.21045842199442077, 108.3249851056250321 ) ) ;
#84844=CARTESIAN_POINT ( 'NONE',  ( -79.45587154498480231, -59.99999999999991473, -31.00068500363164858 ) ) ;
#84845=CARTESIAN_POINT ( 'NONE',  ( -72.65146387209594536, -46.43774402763246911, 115.6314650919494511 ) ) ;
#84847=CARTESIAN_POINT ( 'NONE',  ( 99.17368802223589341, -30.00000000000007816, 199.4946398670649046 ) ) ;
#84849=CARTESIAN_POINT ( 'NONE',  ( 40.27502314868564071, -59.99999999999023714, 56.79790577732133272 ) ) ;
#84861=CARTESIAN_POINT ( 'NONE',  ( -44.56219100001479205, -59.99999999999020162, 65.08294012514838300 ) ) ;
#84871=ORIENTED_EDGE ( 'NONE', *, *, #74452, .T. ) ;
#84875=CARTESIAN_POINT ( 'NONE',  ( 31.71202031379651842, -18.67338479681879448, 29.92500649697927528 ) ) ;
#84876=CARTESIAN_POINT ( 'NONE',  ( 6.601913983210295100, -4.285714285714226079, 24.56594385547514747 ) ) ;
#84877=ORIENTED_EDGE ( 'NONE', *, *, #48546, .T. ) ;
#84888=CARTESIAN_POINT ( 'NONE',  ( 92.42023922870691877, -60.00000000000000000, -0.1265986644637803749 ) ) ;
#84898=CARTESIAN_POINT ( 'NONE',  ( -108.5592049839054454, -29.99999999999999289, 186.0944184388078781 ) ) ;
#84905=CARTESIAN_POINT ( 'NONE',  ( 85.19561819474900233, -60.19663697381487566, -15.74138277301408451 ) ) ;
#84918=CARTESIAN_POINT ( 'NONE',  ( 75.11061747473844719, -39.49004629203866301, 121.1523287295283779 ) ) ;
#84924=CARTESIAN_POINT ( 'NONE',  ( -72.68483858684419374, -57.66063987133676960, 178.6659478268091163 ) ) ;
#84928=CARTESIAN_POINT ( 'NONE',  ( 101.6546115610671563, -37.84847036870517911, 185.8343739213452466 ) ) ;
#84943=CARTESIAN_POINT ( 'NONE',  ( -86.32322474925454969, -30.00000000000000711, 180.5646619429487316 ) ) ;
#84948=CARTESIAN_POINT ( 'NONE',  ( 83.05975511330255756, -57.53496370214478617, 201.2049058628653597 ) ) ;
#84950=CARTESIAN_POINT ( 'NONE',  ( 80.00000000000000000, -52.00000000000000000, -23.09707704303352926 ) ) ;
#84953=CARTESIAN_POINT ( 'NONE',  ( 28.54446013220072942, -29.03608049721292517, -38.24221999424131013 ) ) ;
#84955=CARTESIAN_POINT ( 'NONE',  ( -29.92793289100823984, -60.00000000000000711, 42.99008754467271842 ) ) ;
#84958=CARTESIAN_POINT ( 'NONE',  ( -86.49309358683535720, -20.77578434039007149, 183.3212683181210707 ) ) ;
#84962=CARTESIAN_POINT ( 'NONE',  ( -4.998953709602685258, -25.54932396112263859, 28.13843181039721131 ) ) ;
#84979=CARTESIAN_POINT ( 'NONE',  ( 97.09801539114592117, -30.00000000000000711, 79.69841507686976456 ) ) ;
#84980=CARTESIAN_POINT ( 'NONE',  ( -78.28590395464601670, -60.31583579356012592, 158.4450162056950262 ) ) ;
#84983=DIRECTION ( 'NONE',  ( 0.000000000000000000, 0.000000000000000000, -1.000000000000000000 ) ) ;
#84984=CARTESIAN_POINT ( 'NONE',  ( 30.05171975993012623, -57.68438312713176686, 45.30126411961221322 ) ) ;
#85001=CARTESIAN_POINT ( 'NONE',  ( -78.54456454054628978, -14.21045842199430709, 165.9065210845421348 ) ) ;
#85002=CARTESIAN_POINT ( 'NONE',  ( 20.16305471169097174, -39.47376339469866480, 30.99867996556357141 ) ) ;
#85005=CARTESIAN_POINT ( 'NONE',  ( -38.66081106768926645, -29.14070258423828719, 35.42311757073793643 ) ) ;
#85009=CARTESIAN_POINT ( 'NONE',  ( -2.499999999999996003, -8.000000000000000000, -4.679304766526493044E-16 ) ) ;
#85017=CARTESIAN_POINT ( 'NONE',  ( 94.81216642829221541, -30.00000000000000000, 191.3357916152312725 ) ) ;
#85022=CARTESIAN_POINT ( 'NONE',  ( 82.04623972355572903, -30.00000000000000000, 34.40552157734605032 ) ) ;
#85042=CARTESIAN_POINT ( 'NONE',  ( 73.58237775803615932, -38.32580639661416200, 156.7707483651560949 ) ) ;
#85065=CARTESIAN_POINT ( 'NONE',  ( 84.61252253634089016, -61.08059672144357677, 193.0962152012025683 ) ) ;
#85073=CARTESIAN_POINT ( 'NONE',  ( -86.16358238103411793, -30.00000000000000000, 65.24097969989436763 ) ) ;
#85076=CARTESIAN_POINT ( 'NONE',  ( 33.19742037143350188, -57.69209351129511987, 47.48252466582053444 ) ) ;
#85081=CARTESIAN_POINT ( 'NONE',  ( -18.51494887344581741, -24.53949113939198412, 28.33608110197982555 ) ) ;
#85086=CARTESIAN_POINT ( 'NONE',  ( 39.41494875793583930, -24.69103780450011598, -30.41528609289981944 ) ) ;
#85087=COLOUR_RGB ( '', 0.31764706, 0.68627451, 0.89019608) ;
#85088=CARTESIAN_POINT ( 'NONE',  ( -24.52207515261177662, -29.04217159202778831, 29.86984086181256970 ) ) ;
#85091=CARTESIAN_POINT ( 'NONE',  ( -16.44160279200490749, -22.06944590909828818, 27.77945804026875010 ) ) ;
#85102=CARTESIAN_POINT ( 'NONE',  ( 103.9186714964248637, -60.15547946887917874, 191.0484277881152195 ) ) ;
#85120=CARTESIAN_POINT ( 'NONE',  ( -95.13513732309382931, -60.00000000000000000, -7.455916306700166807 ) ) ;
#85124=CARTESIAN_POINT ( 'NONE',  ( -88.18129031808710749, -59.99999999999997158, -24.85705915495453411 ) ) ;
#85125=CARTESIAN_POINT ( 'NONE',  ( 72.50181414422412729, -37.99999999999997868, -21.26202816386757277 ) ) ;
#85126=CARTESIAN_POINT ( 'NONE',  ( -48.25703249655036586, -49.90483171777201932, 51.25166225055939151 ) ) ;
#85135=CARTESIAN_POINT ( 'NONE',  ( 88.86616235159861787, -30.00000000000552802, -15.15331224089027806 ) ) ;
#85140=CARTESIAN_POINT ( 'NONE',  ( 85.96440179497020040, -30.00000000000000000, 178.3523970025662493 ) ) ;
#85146=CARTESIAN_POINT ( 'NONE',  ( 55.56247616277558876, -22.15090731089991039, 54.53775895343569147 ) ) ;
#85151=CARTESIAN_POINT ( 'NONE',  ( -85.10638907240416984, -38.35927573440125116, -22.75109318859258067 ) ) ;
#85155=CARTESIAN_POINT ( 'NONE',  ( 110.2617929913287185, -38.35601522437976740, 184.2502704656793640 ) ) ;
#85158=CARTESIAN_POINT ( 'NONE',  ( 86.34280695398143735, -60.13066267512422058, 4.659422765642229791 ) ) ;
#85165=ADVANCED_FACE ( 'NONE', ( #75276 ), #93334, .T. ) ;
#85179=CARTESIAN_POINT ( 'NONE',  ( 6.499001506047761723, -13.07634269194914722, 32.05319514180078500 ) ) ;
#85182=CARTESIAN_POINT ( 'NONE',  ( 85.89771287621293538, -25.01010825923657777, 177.6372282980652813 ) ) ;
#85187=CARTESIAN_POINT ( 'NONE',  ( -87.30325485981414602, -45.26540918670090718, 53.23313115482674363 ) ) ;
#85191=CARTESIAN_POINT ( 'NONE',  ( -36.90887455182773635, -31.96477001361924764, -37.72354277451468363 ) ) ;
#85195=CARTESIAN_POINT ( 'NONE',  ( 13.45774757525579268, -59.99999999999997158, 39.73009970327057516 ) ) ;
#85196=CARTESIAN_POINT ( 'NONE',  ( 28.93001008276146635, -31.73066402266886499, 39.98636524211740806 ) ) ;
#85198=CARTESIAN_POINT ( 'NONE',  ( -29.97844425214491082, -32.43635721192953270, 40.56189535855136796 ) ) ;
#85206=DIRECTION ( 'NONE',  ( 0.000000000000000000, 1.000000000000000000, 0.000000000000000000 ) ) ;
#85213=CARTESIAN_POINT ( 'NONE',  ( -15.98142407300128021, -47.40881529994586430, -34.25628805530171661 ) ) ;
#85222=CARTESIAN_POINT ( 'NONE',  ( -91.87273713405024012, -60.00000000000000000, 10.11626477920355249 ) ) ;
#85231=CARTESIAN_POINT ( 'NONE',  ( -82.72299685417047499, -39.49295184692452665, 167.2469102829343797 ) ) ;
#85237=VERTEX_POINT ( 'NONE', #11084 ) ;
#85245=CARTESIAN_POINT ( 'NONE',  ( -94.41342216801938036, -57.67108681604360498, -0.2751897739404595700 ) ) ;
#85251=CARTESIAN_POINT ( 'NONE',  ( 91.97789438503755832, -14.21045842199438880, 64.70176211216229945 ) ) ;
#85252=CARTESIAN_POINT ( 'NONE',  ( -97.13635602990564166, -30.00000000000002842, 199.9106954788804842 ) ) ;
#85253=CARTESIAN_POINT ( 'NONE',  ( -56.51892958678620715, -56.85846262883293178, 71.22199430594528735 ) ) ;
#85257=CARTESIAN_POINT ( 'NONE',  ( -102.2780374498291849, -45.26529867060920509, 188.3692498935314177 ) ) ;
#85258=DIRECTION ( 'NONE',  ( 0.000000000000000000, -0.000000000000000000, 1.000000000000000000 ) ) ;
#85275=CARTESIAN_POINT ( 'NONE',  ( -30.74555747973485964, -46.43642797045591664, 34.64107672549393158 ) ) ;
#85277=CARTESIAN_POINT ( 'NONE',  ( 45.65249901139200261, -53.34829274510006769, 48.30469018026722239 ) ) ;
#85280=CARTESIAN_POINT ( 'NONE',  ( -98.93768687063476364, -38.47564685778473148, 200.7974262912544816 ) ) ;
#85282=CARTESIAN_POINT ( 'NONE',  ( 84.45160259173304951, -38.35831399414499998, -23.32470882673439405 ) ) ;
#85284=CARTESIAN_POINT ( 'NONE',  ( 81.19995102473650661, -60.00000000000004974, 183.8609189267522481 ) ) ;
#85291=CARTESIAN_POINT ( 'NONE',  ( 106.9310636521288558, -60.00000000000000711, 197.1921110703508191 ) ) ;
#85300=CARTESIAN_POINT ( 'NONE',  ( -80.75557906412130649, -30.00000000000003197, -12.51863527975343438 ) ) ;
#85302=CARTESIAN_POINT ( 'NONE',  ( -74.65037011510671050, -38.33113839674835788, 166.1707960067358272 ) ) ;
#85316=CARTESIAN_POINT ( 'NONE',  ( 83.84610521665520366, -35.96948417761220185, 172.3088706270825696 ) ) ;
#85332=CARTESIAN_POINT ( 'NONE',  ( 87.07023238404832455, -24.31684118448634280, 186.7349181601837245 ) ) ;
#85355=CARTESIAN_POINT ( 'NONE',  ( -94.68332376739145673, -60.00000000000000000, 202.5677762804762949 ) ) ;
#85361=CARTESIAN_POINT ( 'NONE',  ( -84.83234346679212479, -39.37621439949131030, 182.9386712835791116 ) ) ;
#85369=CARTESIAN_POINT ( 'NONE',  ( -82.98397381039904985, -37.81828557849092221, -0.6893747078036359666 ) ) ;
#85370=CYLINDRICAL_SURFACE ( 'NONE', #80504, 1.999999999999998224 ) ;
#85378=CARTESIAN_POINT ( 'NONE',  ( 78.26152162121309175, -14.21045842199439946, 161.8191806974193696 ) ) ;
#85380=CARTESIAN_POINT ( 'NONE',  ( -89.53165980454747341, -30.00000000000000000, -13.19740150267569767 ) ) ;
#85381=CARTESIAN_POINT ( 'NONE',  ( -69.47164100847101054, -60.33650507013528852, 112.5478477857417232 ) ) ;
#85384=CARTESIAN_POINT ( 'NONE',  ( 108.4902253387283793, -59.99999999999992184, 199.0859659658876524 ) ) ;
#85385=CARTESIAN_POINT ( 'NONE',  ( 14.00414139509130784, -57.67120807224324608, -44.20775937555332291 ) ) ;
#85396=CARTESIAN_POINT ( 'NONE',  ( -24.04720975275586881, -60.00000000000493827, 43.35146360697347490 ) ) ;
#85411=CARTESIAN_POINT ( 'NONE',  ( 31.12421421041707248, -18.66565208751482174, 29.72625561025419572 ) ) ;
#85412=CARTESIAN_POINT ( 'NONE',  ( 6.601913983208107517, -4.285714285714895766, -24.56594385547655790 ) ) ;
#85423=CARTESIAN_POINT ( 'NONE',  ( 91.85465987230205087, -59.99999999999999289, 11.69882378743306717 ) ) ;
#85432=CARTESIAN_POINT ( 'NONE',  ( -109.4058916485573576, -30.00000000000661871, 179.3849327511039178 ) ) ;
#85438=CARTESIAN_POINT ( 'NONE',  ( 83.86240317988412585, -45.27766788077440197, -12.38235677868432205 ) ) ;
#85443=CARTESIAN_POINT ( 'NONE',  ( 72.51657123412842054, -41.65836498953471079, -21.93284144621084053 ) ) ;
#85446=ORIENTED_EDGE ( 'NONE', *, *, #90712, .T. ) ;
#85451=CARTESIAN_POINT ( 'NONE',  ( 74.24571010611629163, -49.90480856335479132, 125.1173812749847514 ) ) ;
#85456=CARTESIAN_POINT ( 'NONE',  ( -101.2734545671114290, -57.63007487344309254, 203.5435050992661843 ) ) ;
#85462=CARTESIAN_POINT ( 'NONE',  ( 106.4261979399583993, -60.15152501556619313, 168.2421470263708159 ) ) ;
#85469=CARTESIAN_POINT ( 'NONE',  ( -41.60704211633953520, -27.00187119801606173, 37.06697387215593409 ) ) ;
#85475=CARTESIAN_POINT ( 'NONE',  ( 97.48272865599727766, -52.68889013459489945, 195.2151372445526647 ) ) ;
#85478=VERTEX_POINT ( 'NONE', #21762 ) ;
#85481=( BOUNDED_SURFACE ( )  B_SPLINE_SURFACE ( 2, 3, ( 
 ( #78367, #10961, #37426, #101593, #44421, #69240, #20190, #102654, #84346, #61693, #53044, #103189, #44966, #27750, #94584, #69759, #68712, #29333, #85412, #51432, #36892, #10440, #43355, #60623, #11494, #12037, #77847, #76239, #2348, #3961, #19123, #84876, #77316, #68157 ),
 ( #101052, #27208, #92962, #51960, #76772, #54599, #22822, #95623, #95107, #56184, #46017, #54075, #78898, #105304, #79951, #6062, #79430, #104229, #5024, #87017, #55656, #81008, #30917, #29856, #21242, #63798, #96161, #46536, #62734, #38988, #15222, #6592, #47051, #31447 ),
 ( #5542, #30376, #37957, #13088, #88593, #7124, #96685, #21764, #38468, #71862, #63266, #88069, #22293, #104768, #71335, #40038, #47581, #70818, #13621, #87540, #72913, #72398, #14674, #64328, #80476, #55139, #14148, #39523, #97199, #23344, #89123, #48107, #103709, #105822 ) ),
 .UNSPECIFIED., .F., .T., .F. ) 
 B_SPLINE_SURFACE_WITH_KNOTS ( ( 3, 3 ),
 ( 4, 2, 2, 2, 2, 2, 2, 2, 2, 2, 2, 2, 2, 2, 2, 2, 4 ),
 ( 0.000000000000000000, 1.000000000000000000 ),
 ( -3.141592653589793116, -2.748893571891068976, -2.356194490192344837, -1.963495408493620697, -1.570796326794896558, -1.178097245096172418, -0.7853981633974482790, -0.3926990816987241395, 0.000000000000000000, 0.3926990816987241395, 0.7853981633974482790, 1.178097245096172418, 1.570796326794896558, 1.963495408493620697, 2.356194490192344837, 2.748893571891068976, 3.141592653589793116 ),
 .UNSPECIFIED. ) 
 GEOMETRIC_REPRESENTATION_ITEM ( )  RATIONAL_B_SPLINE_SURFACE ( (
 ( 1.000000000000000000, 1.000000000000000000, 1.000000000000000000, 1.000000000000000000, 1.000000000000000000, 1.000000000000000000, 1.000000000000000000, 1.000000000000000000, 1.000000000000000000, 1.000000000000000000, 1.000000000000000000, 1.000000000000000000, 1.000000000000000000, 1.000000000000000000, 1.000000000000000000, 1.000000000000000000, 1.000000000000000000, 1.000000000000000000, 1.000000000000000000, 1.000000000000000000, 1.000000000000000000, 1.000000000000000000, 1.000000000000000000, 1.000000000000000000, 1.000000000000000000, 1.000000000000000000, 1.000000000000000000, 1.000000000000000000, 1.000000000000000000, 1.000000000000000000, 1.000000000000000000, 1.000000000000000000, 1.000000000000000000, 1.000000000000000000),
 ( 1.857142857142858317, 1.857142857142858317, 1.857142857142858317, 1.857142857142858317, 1.857142857142858317, 1.857142857142858317, 1.857142857142858317, 1.857142857142858317, 1.857142857142858317, 1.857142857142858317, 1.857142857142858317, 1.857142857142858317, 1.857142857142858317, 1.857142857142858317, 1.857142857142858317, 1.857142857142858317, 1.857142857142858317, 1.857142857142858317, 1.857142857142858317, 1.857142857142858317, 1.857142857142858317, 1.857142857142858317, 1.857142857142858317, 1.857142857142858317, 1.857142857142858317, 1.857142857142858317, 1.857142857142858317, 1.857142857142858317, 1.857142857142858317, 1.857142857142858317, 1.857142857142858317, 1.857142857142858317, 1.857142857142858317, 1.857142857142858317),
 ( 1.000000000000000000, 1.000000000000000000, 1.000000000000000000, 1.000000000000000000, 1.000000000000000000, 1.000000000000000000, 1.000000000000000000, 1.000000000000000000, 1.000000000000000000, 1.000000000000000000, 1.000000000000000000, 1.000000000000000000, 1.000000000000000000, 1.000000000000000000, 1.000000000000000000, 1.000000000000000000, 1.000000000000000000, 1.000000000000000000, 1.000000000000000000, 1.000000000000000000, 1.000000000000000000, 1.000000000000000000, 1.000000000000000000, 1.000000000000000000, 1.000000000000000000, 1.000000000000000000, 1.000000000000000000, 1.000000000000000000, 1.000000000000000000, 1.000000000000000000, 1.000000000000000000, 1.000000000000000000, 1.000000000000000000, 1.000000000000000000) ) ) 
 REPRESENTATION_ITEM ( '' )  SURFACE ( )  );
#85483=CARTESIAN_POINT ( 'NONE',  ( 17.78280590860698140, -20.33637464548202445, -37.74591371100264325 ) ) ;
#85484=CARTESIAN_POINT ( 'NONE',  ( -86.31380317257726631, -29.99999999999999645, 180.5119918063797115 ) ) ;
#85490=CARTESIAN_POINT ( 'NONE',  ( 86.18040502910800171, -57.57669570564139860, 202.7805009680767512 ) ) ;
#85492=CARTESIAN_POINT ( 'NONE',  ( 60.34209228246672296, -37.37745114556734194, -34.08145293111767415 ) ) ;
#85496=CARTESIAN_POINT ( 'NONE',  ( -61.30040684021128072, -60.00000000000001421, 104.8731119092859529 ) ) ;
#85499=CARTESIAN_POINT ( 'NONE',  ( -86.74136516792933094, -31.76096988859487169, 186.6536333241581644 ) ) ;
#85502=CARTESIAN_POINT ( 'NONE',  ( -5.016449219528405834, -29.03096582929385505, 28.71858016739311381 ) ) ;
#85520=CARTESIAN_POINT ( 'NONE',  ( 94.33250250775739687, -60.00000000000007105, 18.12814013139226077 ) ) ;
#85521=CARTESIAN_POINT ( 'NONE',  ( -82.11053578525284991, -36.02907692299217501, 156.5644557899646543 ) ) ;
#85542=ORIENTED_EDGE ( 'NONE', *, *, #77201, .T. ) ;
#85543=CARTESIAN_POINT ( 'NONE',  ( 52.47548216836918300, -60.00000000000000000, -37.40658969025393787 ) ) ;
#85545=CARTESIAN_POINT ( 'NONE',  ( -37.39630343064651186, -60.00000000000003553, 52.44675545814470041 ) ) ;
#85546=CARTESIAN_POINT ( 'NONE',  ( 19.99411887364738050, -32.51301298576517240, 29.81229016983529689 ) ) ;
#85548=CARTESIAN_POINT ( 'NONE',  ( -34.03134722860705352, -49.90169853283954637, 36.80301113731194107 ) ) ;
#85566=CARTESIAN_POINT ( 'NONE',  ( 91.51003720985690393, -29.99999999999987921, 190.7004568425288653 ) ) ;
#85571=CARTESIAN_POINT ( 'NONE',  ( 76.82090249591115594, -29.99999999999999645, -16.77916451698828482 ) ) ;
#85574=EDGE_CURVE ( 'NONE', #86580, #63501, #104344, .T. ) ;
#85609=CARTESIAN_POINT ( 'NONE',  ( 86.53304295523901146, -28.12513539782037952, 185.0945772042086048 ) ) ;
#85616=CARTESIAN_POINT ( 'NONE',  ( -82.96469731869161990, -30.00000000000000355, 42.60355304050059289 ) ) ;
#85619=CARTESIAN_POINT ( 'NONE',  ( 35.16921309548814634, -57.69533892213389947, 49.31795818493156958 ) ) ;
#85630=CARTESIAN_POINT ( 'NONE',  ( 64.30247150797818279, -29.69425787713660014, -23.35221998356511364 ) ) ;
#85631=CARTESIAN_POINT ( 'NONE',  ( -26.75657867810697965, -56.87252330840309611, 35.15284453816919097 ) ) ;
#85637=CARTESIAN_POINT ( 'NONE',  ( -21.41503862012732640, -42.95838455524901178, 31.73348506666451385 ) ) ;
#85650=CARTESIAN_POINT ( 'NONE',  ( 100.1894145001407708, -37.84390723933621103, 190.2404321465731982 ) ) ;
#85665=CARTESIAN_POINT ( 'NONE',  ( -94.48669138886810970, -60.00000000000000000, 3.951815744481825821 ) ) ;
#85667=CARTESIAN_POINT ( 'NONE',  ( 2.841596995776060286, -59.99999999999998579, 39.63907943748999685 ) ) ;
#85670=CARTESIAN_POINT ( 'NONE',  ( -107.0562774193554816, -30.00000000000000355, 141.2195909136805767 ) ) ;
#85671=CARTESIAN_POINT ( 'NONE',  ( 4.129220113709654250, -60.35881339298138926, 33.94144245523071390 ) ) ;
#85673=CARTESIAN_POINT ( 'NONE',  ( -48.06896637034827791, -36.06506752110366421, 46.66918921588193570 ) ) ;
#85685=CARTESIAN_POINT ( 'NONE',  ( 103.9415641081996569, -29.99999999993293187, 120.1036003625780069 ) ) ;
#85689=CARTESIAN_POINT ( 'NONE',  ( 100.4127377726602219, -30.00000000000000000, 183.4147967980347858 ) ) ;
#85696=CARTESIAN_POINT ( 'NONE',  ( 54.81643864070908734, -39.49759617041522830, 59.89540365714804437 ) ) ;
#85704=CARTESIAN_POINT ( 'NONE',  ( -91.45944082887925219, -38.38696142436580061, -7.377240623632893346 ) ) ;
#85706=CARTESIAN_POINT ( 'NONE',  ( 110.9829524794310487, -38.35607303365373610, 174.7672866423136497 ) ) ;
#85709=CARTESIAN_POINT ( 'NONE',  ( 82.48695905097841319, -37.86100049745743235, 8.080848905333057886 ) ) ;
#85728=CARTESIAN_POINT ( 'NONE',  ( 1.295095875561511761E-05, -30.00000000000000000, 37.00000000000000711 ) ) ;
#85731=CARTESIAN_POINT ( 'NONE',  ( 5.618858407243280340, -12.94760482173810878, 32.08621218712340806 ) ) ;
#85736=CARTESIAN_POINT ( 'NONE',  ( 83.34476608070126247, -57.33726856256456728, 189.3581896335610111 ) ) ;
#85742=CARTESIAN_POINT ( 'NONE',  ( -87.58810446347557388, -37.82077815364313267, 63.64187444496401014 ) ) ;
#85747=CARTESIAN_POINT ( 'NONE',  ( -4.121118778969612428, -21.54458145684739634, -38.54885555910615125 ) ) ;
#85749=CARTESIAN_POINT ( 'NONE',  ( 21.93441337368819077, -59.99999999999999289, 40.50886425770784172 ) ) ;
#85752=CARTESIAN_POINT ( 'NONE',  ( 46.00628356782431894, -28.63590054676348728, 41.16915987473818461 ) ) ;
#85754=CARTESIAN_POINT ( 'NONE',  ( -31.50084319533580413, -33.43140129536075023, 41.49735270624054806 ) ) ;
#85768=CARTESIAN_POINT ( 'NONE',  ( -22.67421649284328566, -60.22830675361940678, -35.89770680791995972 ) ) ;
#85778=CARTESIAN_POINT ( 'NONE',  ( 80.00000000000000000, -60.00000000000000000, -19.09707704303353282 ) ) ;
#85780=CARTESIAN_POINT ( 'NONE',  ( -92.23326038059701659, -60.00000000000000711, 2.433354083156913816 ) ) ;
#85789=CARTESIAN_POINT ( 'NONE',  ( -81.74441236244950915, -46.45436576172757270, 169.1830579053890347 ) ) ;
#85791=CARTESIAN_POINT ( 'NONE',  ( -13.52495681779062764, -0.000000000000000000, 10.38447319518036238 ) ) ;
#85801=CARTESIAN_POINT ( 'NONE',  ( -94.01586347659660703, -57.67588051021766660, 5.310313041227479935 ) ) ;
#85807=CARTESIAN_POINT ( 'NONE',  ( 87.68135845022958108, -14.21045842199445275, 32.26523303912966156 ) ) ;
#85808=CARTESIAN_POINT ( 'NONE',  ( -91.09862910994078788, -14.21045842199425380, 197.8399937059591309 ) ) ;
#85809=CARTESIAN_POINT ( 'NONE',  ( -55.38459995159444560, -46.44143365808177037, 64.00544807844242712 ) ) ;
#85812=CARTESIAN_POINT ( 'NONE',  ( -106.5272989890566748, -60.15536930867855858, 172.9214709365080012 ) ) ;
#85818=SURFACE_SIDE_STYLE ('',( #28657 ) ) ;
#85830=CARTESIAN_POINT ( 'NONE',  ( -27.77433481921273284, -22.10417860528052714, 29.38320212662867803 ) ) ;
#85833=CARTESIAN_POINT ( 'NONE',  ( 46.15439516824530841, -18.78259881707839796, 39.23926396323135890 ) ) ;
#85837=EDGE_CURVE ( 'NONE', #74331, #35775, #9581, .T. ) ;
#85838=CARTESIAN_POINT ( 'NONE',  ( -89.89686455004155619, -38.51728769248722983, 200.5441032878415797 ) ) ;
#85840=CARTESIAN_POINT ( 'NONE',  ( 82.74320640397530724, -38.35695998739068102, -24.68618422736320994 ) ) ;
#85849=CARTESIAN_POINT ( 'NONE',  ( 104.3686754364753853, -60.00000000000000711, 199.7312357621291596 ) ) ;
#85851=B_SPLINE_CURVE_WITH_KNOTS ( 'NONE', 3,
 ( #71473, #21906, #81153, #80622, #14292, #73049 ),
 .UNSPECIFIED., .F., .F.,
 ( 4, 2, 4 ),
 ( 0.02035271886645138514, 0.03148701738111871901, 0.04262131589578604940 ),
 .UNSPECIFIED. ) ;
#85855=CARTESIAN_POINT ( 'NONE',  ( -79.59097844331863314, -29.99999999999999289, -14.32855134736868585 ) ) ;
#85857=CARTESIAN_POINT ( 'NONE',  ( -70.02821094524227874, -38.33024996013831043, 134.5064181467811295 ) ) ;
#85870=CARTESIAN_POINT ( 'NONE',  ( 82.94047458007501916, -42.97468312252637190, 174.7032502363410629 ) ) ;
#85910=CARTESIAN_POINT ( 'NONE',  ( -111.1105008086674388, -60.00000000000000000, 186.7259703680355472 ) ) ;
#85916=CARTESIAN_POINT ( 'NONE',  ( -86.06160377997784394, -21.58091379659038722, 174.3369035936914884 ) ) ;
#85923=CARTESIAN_POINT ( 'NONE',  ( -83.79706745093385223, -45.26740093649807761, 6.296018886061934161 ) ) ;
#85931=CARTESIAN_POINT ( 'NONE',  ( 60.31460910868286618, -60.00000000000004263, 109.8329304423809702 ) ) ;
#85933=CARTESIAN_POINT ( 'NONE',  ( -89.21220262753612928, -29.99999999999994316, 13.74661749290507906 ) ) ;
#85934=CARTESIAN_POINT ( 'NONE',  ( -64.70029564103292330, -39.48557291963400928, 85.32163151726285832 ) ) ;
#85935=ORIENTED_EDGE ( 'NONE', *, *, #5587, .T. ) ;
#85936=CARTESIAN_POINT ( 'NONE',  ( 103.0033180414816343, -14.21045842199429643, 193.8537495780579150 ) ) ;
#85938=CARTESIAN_POINT ( 'NONE',  ( 30.70107235603070706, -60.00000000001240608, 46.11011145243585219 ) ) ;
#85949=CARTESIAN_POINT ( 'NONE',  ( -5.653164214226177542, -59.99999999997061906, 41.97898663223412541 ) ) ;
#85958=VERTEX_POINT ( 'NONE', #52333 ) ;
#85961=CARTESIAN_POINT ( 'NONE',  ( -80.00000000000000000, -52.00000000000000000, -23.09707704303352926 ) ) ;
#85962=CARTESIAN_POINT ( 'NONE',  ( 33.47661863257818737, -18.69765052410563655, 30.56412019559146742 ) ) ;
#85978=CARTESIAN_POINT ( 'NONE',  ( 91.92166457297645366, -60.00000000000000711, 16.22366861495048695 ) ) ;
#85985=CARTESIAN_POINT ( 'NONE',  ( -96.81373938066217022, -30.00000000000823164, 199.8413627685791312 ) ) ;
#85991=CARTESIAN_POINT ( 'NONE',  ( 85.48529165631397575, -52.75865074998397830, -10.94020551895792970 ) ) ;
#86003=CARTESIAN_POINT ( 'NONE',  ( 78.25203214054160128, -42.96388236615710809, 138.8363729379485960 ) ) ;
#86009=CARTESIAN_POINT ( 'NONE',  ( -111.0360493097450529, -57.67057850706027722, 194.0974529949267549 ) ) ;
#86018=CARTESIAN_POINT ( 'NONE',  ( -39.94456049126967656, -26.30212818477839321, 35.92538891840626292 ) ) ;
#86030=CARTESIAN_POINT ( 'NONE',  ( 73.94814338752382810, -30.09466847450056903, -28.11389532863423568 ) ) ;
#86031=CARTESIAN_POINT ( 'NONE',  ( -82.93722998966033799, -30.00000000000000000, 152.4467691388267951 ) ) ;
#86036=CARTESIAN_POINT ( 'NONE',  ( 76.00644063775833104, -57.54596990661518419, 193.1823216553611076 ) ) ;
#86038=CARTESIAN_POINT ( 'NONE',  ( 57.28004366725042473, -36.93788119843549822, -34.78852087230680468 ) ) ;
#86040=CARTESIAN_POINT ( 'NONE',  ( -65.75807407283386397, -60.00000000000000711, 121.3892982347636007 ) ) ;
#86044=CARTESIAN_POINT ( 'NONE',  ( -86.35312816053438212, -20.98790165847923461, 180.9809247037294142 ) ) ;
#86047=CARTESIAN_POINT ( 'NONE',  ( -4.046613933372436023, -39.47588596367953784, 30.46164947777460696 ) ) ;
#86063=CARTESIAN_POINT ( 'NONE',  ( -15.50035291838927876, -4.285714285714916194, 20.16952962162167395 ) ) ;
#86066=CARTESIAN_POINT ( 'NONE',  ( 102.4475954893556633, -30.00000000000004263, 111.1011446524310742 ) ) ;
#86067=CARTESIAN_POINT ( 'NONE',  ( -79.16702777562869642, -56.85000040143994937, 161.1953825210129878 ) ) ;
#86088=CARTESIAN_POINT ( 'NONE',  ( 68.54330978433023347, -60.00000000000000000, -33.08258948747816675 ) ) ;
#86089=CARTESIAN_POINT ( 'NONE',  ( -68.63253095932553549, -60.00000000000002842, 147.4008728361381486 ) ) ;
#86090=CARTESIAN_POINT ( 'NONE',  ( 25.48282336132001191, -56.86957850576434481, 34.80755836682993021 ) ) ;
#86093=CARTESIAN_POINT ( 'NONE',  ( -36.01933158121845935, -22.19451844719506184, 32.43403767349134625 ) ) ;
#86104=CARTESIAN_POINT ( 'NONE',  ( -75.84932468004862471, -38.36924633978998145, 177.1874917199713195 ) ) ;
#86106=CARTESIAN_POINT ( 'NONE',  ( 99.00547121574200560, -30.00000000000000000, 188.8237953836635654 ) ) ;
#86109=CARTESIAN_POINT ( 'NONE',  ( 81.59236582409479865, -29.99999999999999289, -7.441647983982530690 ) ) ;
#86133=CARTESIAN_POINT ( 'NONE',  ( 64.43859380035580386, -22.10221476649115502, 75.67156401609979355 ) ) ;
#86150=CARTESIAN_POINT ( 'NONE',  ( 86.32943948890100216, -46.49832263646349162, 190.0111496207520361 ) ) ;
#86158=CARTESIAN_POINT ( 'NONE',  ( -9.073678795326815205, -16.06358835070689750, -34.89371268523018443 ) ) ;
#86162=CARTESIAN_POINT ( 'NONE',  ( -90.20584754825765117, -30.00000000000000711, 89.69724495916204887 ) ) ;
#86164=CARTESIAN_POINT ( 'NONE',  ( 0.01856856229768925892, -57.67120202543696905, 41.61186673337733311 ) ) ;
#86169=CARTESIAN_POINT ( 'NONE',  ( -49.19868921488087210, -37.82012451832441968, 48.88653370302302648 ) ) ;
#86173=CARTESIAN_POINT ( 'NONE',  ( -24.88460094139896839, -39.48002255589691600, 31.72060110609164241 ) ) ;
#86177=CARTESIAN_POINT ( 'NONE',  ( -21.13863729395087887, -32.51627878024107332, 29.94168239066533133 ) ) ;
#86192=CARTESIAN_POINT ( 'NONE',  ( 102.8835412338887352, -52.71848775370781226, 190.2923971475949827 ) ) ;
#86193=CARTESIAN_POINT ( 'NONE',  ( 51.20698849084796223, -38.00000000000000711, 52.28247866703643609 ) ) ;
#86207=CARTESIAN_POINT ( 'NONE',  ( -91.37266855712616120, -59.99999999999998579, -21.09057864729411946 ) ) ;
#86210=CARTESIAN_POINT ( 'NONE',  ( 69.31621320414066645, -59.99999999998080114, -35.31426391149900468 ) ) ;
#86213=CARTESIAN_POINT ( 'NONE',  ( -108.0662369917864680, -29.99999999999997513, 149.4678941581608740 ) ) ;
#86214=CARTESIAN_POINT ( 'NONE',  ( 5.972312261546847800, -18.58614341180641816, 26.97788726184341357 ) ) ;
#86216=CARTESIAN_POINT ( 'NONE',  ( -48.69069850261567467, -39.52191310650646727, 48.66776383025324293 ) ) ;
#86217=VECTOR ( 'NONE', #74853, 1000.000000000000000 ) ;
#86227=CARTESIAN_POINT ( 'NONE',  ( 77.56003102942109706, -30.00000000000500577, -26.29825542485684053 ) ) ;
#86232=CARTESIAN_POINT ( 'NONE',  ( 96.01405531091515400, -30.00000000000000711, 191.2846317128013993 ) ) ;
#86237=CARTESIAN_POINT ( 'NONE',  ( 55.20647631999140970, -18.68557819068131565, 52.51210417480952941 ) ) ;
#86242=CARTESIAN_POINT ( 'NONE',  ( -88.03604560337967655, -38.37098769885366067, -19.52574164018452407 ) ) ;
#86246=CARTESIAN_POINT ( 'NONE',  ( 105.2091447253385468, -38.39005253448742394, 197.2722285801829116 ) ) ;
#86249=CARTESIAN_POINT ( 'NONE',  ( 85.09130552977511286, -52.70812209273635318, 5.152046609888252249 ) ) ;
#86263=CARTESIAN_POINT ( 'NONE',  ( 0.8333405213146051205, -30.00000000000001421, 28.88964995960238369 ) ) ;
#86265=CARTESIAN_POINT ( 'NONE',  ( 22.16406547723535070, -20.70551619972588142, 36.17276813359887910 ) ) ;
#86270=CARTESIAN_POINT ( 'NONE',  ( 83.19851726930752989, -53.68871273878280448, 186.7541703894078466 ) ) ;
#86274=CARTESIAN_POINT ( 'NONE',  ( -87.75695610596812912, -52.70950093229972566, 47.57269196313494319 ) ) ;
#86282=CARTESIAN_POINT ( 'NONE',  ( 14.11578347234595654, -59.99999999999998579, 39.75482815772654988 ) ) ;
#86283=CARTESIAN_POINT ( 'NONE',  ( 11.71459821192806672, -20.98522750155807515, 35.53716617024250723 ) ) ;
#86286=CARTESIAN_POINT ( 'NONE',  ( 45.15274496246701119, -28.34823788395991429, 40.23751332069821984 ) ) ;
#86287=CARTESIAN_POINT ( 'NONE',  ( -37.53089333674191153, -36.72970239472569887, 46.80208549195887713 ) ) ;
#86302=CARTESIAN_POINT ( 'NONE',  ( 1.602313057358263348, -60.22811021425470557, -36.92768096916045550 ) ) ;
#86316=CARTESIAN_POINT ( 'NONE',  ( -92.08870864087261054, -60.00000000000000711, 20.32441657550419123 ) ) ;
#86320=FACE_OUTER_BOUND ( 'NONE', #12452, .T. ) ;
#86322=CARTESIAN_POINT ( 'NONE',  ( -81.08330333408508750, -53.42614166648503726, 174.1528431049000005 ) ) ;
#86324=CARTESIAN_POINT ( 'NONE',  ( -11.24494283604955491, -0.000000000000000000, 12.81923949847508837 ) ) ;
#86334=CARTESIAN_POINT ( 'NONE',  ( -94.13300556333170732, -57.67265947060198528, 21.91134835779649137 ) ) ;
#86340=CARTESIAN_POINT ( 'NONE',  ( 85.44123078815633221, -14.21045842199435505, -16.45204874176463150 ) ) ;
#86342=CARTESIAN_POINT ( 'NONE',  ( -66.35297339498846725, -60.00000000000000000, 134.7723483620486888 ) ) ;
#86343=CARTESIAN_POINT ( 'NONE',  ( -55.41494957456509951, -25.62128524555114240, 55.61161846345970616 ) ) ;
#86347=CARTESIAN_POINT ( 'NONE',  ( -100.8637650043404221, -52.73819914637954298, 193.5090766411508980 ) ) ;
#86348=CARTESIAN_POINT ( 'NONE',  ( 101.7408511833992009, -38.00000000000000000, 185.5768760481534514 ) ) ;
#86359=CARTESIAN_POINT ( 'NONE',  ( 66.08383350088368502, -30.00000000000000000, 83.36352947276506598 ) ) ;
#86365=CARTESIAN_POINT ( 'NONE',  ( -26.60308663855274602, -22.09595682646055081, 29.10650421446171165 ) ) ;
#86367=CARTESIAN_POINT ( 'NONE',  ( 48.43983201128956040, -32.59978484401640486, 46.13064193097132915 ) ) ;
#86372=CARTESIAN_POINT ( 'NONE',  ( -87.14751124570071283, -38.58929230054740600, 199.6078792464353171 ) ) ;
#86374=CARTESIAN_POINT ( 'NONE',  ( 90.70427241161488041, -38.34270740108069475, 7.520233764197877591 ) ) ;
#86382=CARTESIAN_POINT ( 'NONE',  ( 111.2603429936217339, -60.00000000000000711, 185.9078983323155398 ) ) ;
#86389=CARTESIAN_POINT ( 'NONE',  ( -47.71178637004413758, -38.32472025489722256, 63.29349205809943157 ) ) ;
#86402=CARTESIAN_POINT ( 'NONE',  ( 81.65977408556862827, -53.47473748660239323, 179.0429556740298835 ) ) ;
#86432=DIRECTION ( 'NONE',  ( -3.700743415416444046E-15, 0.000000000000000000, 1.000000000000000000 ) ) ;
#86447=CARTESIAN_POINT ( 'NONE',  ( -111.1425918653686864, -60.00000000000000000, 186.5575091249358763 ) ) ;
#86453=CARTESIAN_POINT ( 'NONE',  ( -83.33205040470181757, -50.10390547248005078, 184.7201514412779488 ) ) ;
#86459=CARTESIAN_POINT ( 'NONE',  ( -82.69027687505180779, -37.83053627336025215, 3.614385560145078724 ) ) ;
#86465=SURFACE_SIDE_STYLE ('',( #104194 ) ) ;
#86467=CARTESIAN_POINT ( 'NONE',  ( 78.81966326594580607, -14.21045842199438347, 187.8133603351751333 ) ) ;
#86470=CARTESIAN_POINT ( 'NONE',  ( -81.17775171884230190, -14.21045842199422005, -20.84891578014651259 ) ) ;
#86472=CARTESIAN_POINT ( 'NONE',  ( -64.25667017276946069, -46.43867898611913603, 87.64705215544989869 ) ) ;
#86474=CARTESIAN_POINT ( 'NONE',  ( 85.76531507393636389, -14.21045842199426801, 195.9085670305863118 ) ) ;
#86476=CARTESIAN_POINT ( 'NONE',  ( 72.15333944293220725, -60.00000000002454215, 177.4635911251213827 ) ) ;
#86486=CARTESIAN_POINT ( 'NONE',  ( 1.405425597968214055E-06, -60.00000000000002132, -42.63907915653317815 ) ) ;
#86500=CARTESIAN_POINT ( 'NONE',  ( 37.87242778715787495, -56.81031238840315467, 40.67136584880061179 ) ) ;
#86514=CARTESIAN_POINT ( 'NONE',  ( 92.72621184031598318, -60.00000000000000000, -5.596747031044355225 ) ) ;
#86520=CARTESIAN_POINT ( 'NONE',  ( -85.82535587192259641, -29.99999999998809130, 197.6421767587684997 ) ) ;
#86526=CARTESIAN_POINT ( 'NONE',  ( 82.96525807848877321, -45.27743543914848345, -14.54737611346266846 ) ) ;
#86537=CARTESIAN_POINT ( 'NONE',  ( 77.12720002150464893, -46.43306016149463034, 136.1069725533496921 ) ) ;
#86544=CARTESIAN_POINT ( 'NONE',  ( -100.1205506810183152, -57.62746089781320791, 203.8952656938035091 ) ) ;
#86553=CARTESIAN_POINT ( 'NONE',  ( -37.78143777952784887, -25.35208823665809774, 34.67056976772743582 ) ) ;
#86564=CARTESIAN_POINT ( 'NONE',  ( 7.677589009493908101, -18.26067908012137053, -37.91149814823734943 ) ) ;
#86565=CARTESIAN_POINT ( 'NONE',  ( -77.43986148285553384, -30.00000000000000000, 121.9463532134702461 ) ) ;
#86569=CARTESIAN_POINT ( 'NONE',  ( 83.25052031436327127, -57.53743629746287525, 201.3212271054727580 ) ) ;
#86570=CARTESIAN_POINT ( 'NONE',  ( 62.09620979924952167, -34.58946247023943954, -24.66282284637085453 ) ) ;
#86574=CARTESIAN_POINT ( 'NONE',  ( -69.32805405156442191, -60.00000000000000000, 137.7891073056175060 ) ) ;
#86578=CARTESIAN_POINT ( 'NONE',  ( -86.25609154892794095, -24.66340834717759023, 181.7636524898530865 ) ) ;
#86580=VERTEX_POINT ( 'NONE', #330 ) ;
#86596=CARTESIAN_POINT ( 'NONE',  ( -17.78317311658302202, -3.469446951953614189E-15, -13.66642973270732142 ) ) ;
#86598=CARTESIAN_POINT ( 'NONE',  ( 97.37780541404315215, -14.21045842199443143, 96.97658560636448044 ) ) ;
#86599=CARTESIAN_POINT ( 'NONE',  ( -81.09943103650151386, -25.62393341775641531, 137.9297325403806553 ) ) ;
#86601=SURFACE_SIDE_STYLE ('',( #102758 ) ) ;
#86603=CARTESIAN_POINT ( 'NONE',  ( 2.851084197991860414, -57.67120200768756888, 41.61186728490002906 ) ) ;
#86622=CARTESIAN_POINT ( 'NONE',  ( 90.46769687319441289, -60.00000000000001421, -18.02911679486343743 ) ) ;
#86624=CARTESIAN_POINT ( 'NONE',  ( -55.31183857750818333, -60.00000000000000000, 93.46795725556545165 ) ) ;
#86625=CARTESIAN_POINT ( 'NONE',  ( 25.70524614496113358, -29.04465569019870586, 30.12072865786996090 ) ) ;
#86629=VERTEX_POINT ( 'NONE', #11102 ) ;
#86630=CARTESIAN_POINT ( 'NONE',  ( -25.22241582816893057, -4.285714285714296246, -1.650803255657555146 ) ) ;
#86638=CARTESIAN_POINT ( 'NONE',  ( 85.39867414124013578, -29.99999999999999289, 60.46109300951300725 ) ) ;
#86642=CARTESIAN_POINT ( 'NONE',  ( 80.95908799317884075, -30.00000000000000711, 4.750023924636396444 ) ) ;
#86654=EDGE_LOOP ( 'NONE', ( #88066, #50204, #70112, #71675 ) ) ;
#86658=CARTESIAN_POINT ( 'NONE',  ( 60.37928884598232315, -38.34250802169606942, 97.60144182010409963 ) ) ;
#86663=CARTESIAN_POINT ( 'NONE',  ( 63.48522851496006325, -53.38631336116730353, 88.97494422768454569 ) ) ;
#86667=CARTESIAN_POINT ( 'NONE',  ( -61.85959367383505736, -37.56337504497723501, -33.69606644638567161 ) ) ;
#86679=CARTESIAN_POINT ( 'NONE',  ( 86.31913262548056309, -39.17055256143338937, 187.7253881214433875 ) ) ;
#86687=CARTESIAN_POINT ( 'NONE',  ( -97.63324830393105458, -30.00000000000000000, 134.9666292763866977 ) ) ;
#86691=CARTESIAN_POINT ( 'NONE',  ( 19.24463328355616909, -57.67182880030375003, 42.11738475777909230 ) ) ;
#86694=EDGE_CURVE ( 'NONE', #32439, #71545, #47377, .T. ) ;
#86699=CARTESIAN_POINT ( 'NONE',  ( 11.73848531063677569, -16.54446083686769242, -34.66488886015380189 ) ) ;
#86705=CARTESIAN_POINT ( 'NONE',  ( -20.24774297161117431, -42.95817207100498081, 31.59261033110390926 ) ) ;
#86706=CARTESIAN_POINT ( 'NONE',  ( -86.12427509053026142, -60.00000000000003553, 8.940647230371650878 ) ) ;
#86717=CARTESIAN_POINT ( 'NONE',  ( 100.7952419678079821, -37.84774286652142905, 188.8884646472686200 ) ) ;
#86732=CARTESIAN_POINT ( 'NONE',  ( -85.18694157166503089, -59.99999999999020162, -27.35932843724341978 ) ) ;
#86734=CARTESIAN_POINT ( 'NONE',  ( 35.33767613680186059, -60.00000000000000000, 46.68008179612595399 ) ) ;
#86738=CARTESIAN_POINT ( 'NONE',  ( -98.75680450758818552, -14.21045842199431064, 105.0421542466116023 ) ) ;
#86739=CARTESIAN_POINT ( 'NONE',  ( 13.52092337146004475, -42.95373788567773943, 31.13298423633953504 ) ) ;
#86742=CARTESIAN_POINT ( 'NONE',  ( -47.71978414336781782, -36.06698018952960183, 46.18487447919529387 ) ) ;
#86753=CARTESIAN_POINT ( 'NONE',  ( 47.64963052949291011, -38.32453750017476324, 63.16317949360573891 ) ) ;
#86759=CARTESIAN_POINT ( 'NONE',  ( 100.4511241798009564, -30.00000000000000000, 183.1650932517458159 ) ) ;
#86767=CARTESIAN_POINT ( 'NONE',  ( 55.71012702596955535, -18.68161350975861978, 53.46581880971264411 ) ) ;
#86775=CARTESIAN_POINT ( 'NONE',  ( 94.08446777513815107, -38.49224043567311071, 201.1962447641767540 ) ) ;
#86777=CARTESIAN_POINT ( 'NONE',  ( 83.68965721369660571, -45.28337549153452102, 9.534655265776285304 ) ) ;
#86793=CARTESIAN_POINT ( 'NONE',  ( -33.88587854726462467, -34.92297979730529534, 43.18992221583581426 ) ) ;
#86798=CARTESIAN_POINT ( 'NONE',  ( 85.85839205898065529, -25.04722136935922450, 177.1349197526708679 ) ) ;
#86802=CARTESIAN_POINT ( 'NONE',  ( -93.98801953623500083, -37.82080309286048703, 101.9196238546772548 ) ) ;
#86809=CARTESIAN_POINT ( 'NONE',  ( 1.343583726616268681, -18.03024427876663793, 35.00504070719485838 ) ) ;
#86811=CARTESIAN_POINT ( 'NONE',  ( 49.75182367352914525, -29.64110475095384700, 46.21721366459617286 ) ) ;
#86819=CARTESIAN_POINT ( 'NONE',  ( -86.44795749754025849, -38.00000000000003553, 55.89569772577183215 ) ) ;
#86827=CARTESIAN_POINT ( 'NONE',  ( -9.567179087380816682, -47.40889396972781356, -34.57814075494444950 ) ) ;
#86833=ORIENTED_EDGE ( 'NONE', *, *, #16415, .F. ) ;
#86836=CARTESIAN_POINT ( 'NONE',  ( -93.40600019352365280, -60.00000000000000000, 36.18128804451619374 ) ) ;
#86843=CARTESIAN_POINT ( 'NONE',  ( -85.74753642962151901, -18.52699961319207134, 162.5183481292275758 ) ) ;
#86845=CARTESIAN_POINT ( 'NONE',  ( -2.220638482700625804, -0.000000000000000000, -16.90642566760435983 ) ) ;
#86854=CARTESIAN_POINT ( 'NONE',  ( -100.9355741078537676, -57.67123050614609525, 74.71304529006944506 ) ) ;
#86860=CARTESIAN_POINT ( 'NONE',  ( 82.54285424309888697, -59.99999999999997868, -29.20801037391389698 ) ) ;
#86862=CARTESIAN_POINT ( 'NONE',  ( -69.85357985695409866, -59.99999999999993605, 155.8687211249902873 ) ) ;
#86863=CARTESIAN_POINT ( 'NONE',  ( -54.66613860792094926, -42.97099802834101467, 60.96799278605171679 ) ) ;
#86868=CARTESIAN_POINT ( 'NONE',  ( -102.3879661117660334, -52.71380871076068786, 191.3657242593055798 ) ) ;
#86884=CARTESIAN_POINT ( 'NONE',  ( -28.17640869695596706, -60.34565798028340566, 36.16065794429692204 ) ) ;
#86887=CARTESIAN_POINT ( 'NONE',  ( 48.45783950018828534, -56.82067350140248152, 53.79819978640338718 ) ) ;
#86891=CARTESIAN_POINT ( 'NONE',  ( -110.8707848989685516, -38.35619458718431929, 167.2301363532564267 ) ) ;
#86893=CARTESIAN_POINT ( 'NONE',  ( 91.22471603993383837, -38.35915892665957472, -1.047709165501598427 ) ) ;
#86901=CARTESIAN_POINT ( 'NONE',  ( 109.7065984538688923, -60.00000000000000711, 191.9969423268659057 ) ) ;
#86912=CARTESIAN_POINT ( 'NONE',  ( -91.33478035347820878, -38.36421997627891045, -2.728810306399620078 ) ) ;
#86924=CARTESIAN_POINT ( 'NONE',  ( 85.91903949933247020, -18.46740127454976843, 164.5912266175255070 ) ) ;
#86967=CARTESIAN_POINT ( 'NONE',  ( -104.3903561930018355, -60.00000000000000000, 199.7463460733462171 ) ) ;
#86971=CARTESIAN_POINT ( 'NONE',  ( -83.96270013590550718, -39.45081235419423393, 178.0757026163669821 ) ) ;
#86977=CARTESIAN_POINT ( 'NONE',  ( -84.64863869684523934, -45.26546037518905052, 31.07901721422380703 ) ) ;
#86983=CARTESIAN_POINT ( 'NONE',  ( 100.3457197225335733, -14.21045842199427511, 196.5350150060856720 ) ) ;
#86986=CARTESIAN_POINT ( 'NONE',  ( -101.2960459709432826, -29.99999999999998579, 104.2733491104911963 ) ) ;
#86988=CARTESIAN_POINT ( 'NONE',  ( -64.78455580451337426, -22.10248187533688125, 76.63264628624035879 ) ) ;
#86991=CARTESIAN_POINT ( 'NONE',  ( 68.99430565880821575, -59.99999999999998579, 149.4797282245464203 ) ) ;
#87001=CARTESIAN_POINT ( 'NONE',  ( -2.833865952193512783, -59.99999999997060485, 41.99999969629084973 ) ) ;
#87015=CARTESIAN_POINT ( 'NONE',  ( 33.67987230928347486, -22.16572803534493019, 31.32075179795772257 ) ) ;
#87017=CARTESIAN_POINT ( 'NONE',  ( 11.19959342722337681, 2.897043466792154898E-12, -19.43146043914873289 ) ) ;
#87032=CARTESIAN_POINT ( 'NONE',  ( 92.20688357260412715, -60.00000000000002132, 2.776348851982239463 ) ) ;
#87042=CARTESIAN_POINT ( 'NONE',  ( -86.00551523489100703, -29.99999999999667821, -19.89116246976540481 ) ) ;
#87046=CARTESIAN_POINT ( 'NONE',  ( 81.59424421858821574, -37.83104312327714780, -14.43779184493780399 ) ) ;
#87054=CARTESIAN_POINT ( 'NONE',  ( 77.75032079266158291, -60.30862840971112604, 154.2286336114433141 ) ) ;
#87060=CARTESIAN_POINT ( 'NONE',  ( -105.5530292394789882, -57.64680470462099038, 201.3003284212183246 ) ) ;
#87068=CARTESIAN_POINT ( 'NONE',  ( -40.94175040987683190, -26.72553514667153962, 36.58944239903460982 ) ) ;
#87080=CARTESIAN_POINT ( 'NONE',  ( 75.51533756583158663, -29.99999999999997868, -27.33238513093786537 ) ) ;
#87081=CARTESIAN_POINT ( 'NONE',  ( -68.54014073437507193, -30.00000000000000000, 90.70798278420799932 ) ) ;
#87086=CARTESIAN_POINT ( 'NONE',  ( 82.51619662115577114, -57.52811307887816383, 200.8615502966897566 ) ) ;
#87087=CARTESIAN_POINT ( 'NONE',  ( 72.96298303301223598, -34.58959179241216475, -20.39840084324062985 ) ) ;
#87091=CARTESIAN_POINT ( 'NONE',  ( -50.30040434326485155, -60.00000000000000711, 72.55815636389731083 ) ) ;
#87097=CARTESIAN_POINT ( 'NONE',  ( -85.94079226153354512, -35.60111559732363418, 185.2110495663119991 ) ) ;
#87098=EDGE_LOOP ( 'NONE', ( #58482, #29624, #42904, #24825, #56689, #2620, #39081, #72037, #18170, #55491 ) ) ;
#87107=CARTESIAN_POINT ( 'NONE',  ( -84.30038697636420864, -52.73262689129283842, -14.69966796222219862 ) ) ;
#87115=CARTESIAN_POINT ( 'NONE',  ( 85.55833380596646975, -30.00000000000001776, -20.40969086358413520 ) ) ;
#87116=CARTESIAN_POINT ( 'NONE',  ( -81.01834315243938534, -18.68267671355141601, 131.0834654034409823 ) ) ;
#87120=CARTESIAN_POINT ( 'NONE',  ( 62.69693952681404170, -57.67812735391505896, 116.6625076095181726 ) ) ;
#87139=CARTESIAN_POINT ( 'NONE',  ( 92.68765510100411120, -60.00000000000002132, -9.247194546651380520 ) ) ;
#87140=CARTESIAN_POINT ( 'NONE',  ( -69.85357985695409866, -59.99999999999993605, 155.8687211249902873 ) ) ;
#87141=CARTESIAN_POINT ( 'NONE',  ( 26.45493447348655991, -18.61830836965839353, 28.46775629927182294 ) ) ;
#87157=CARTESIAN_POINT ( 'NONE',  ( 81.21951335026766117, -29.99999999999999645, -11.15224753138006264 ) ) ;
#87180=CARTESIAN_POINT ( 'NONE',  ( 63.94774550461288243, -18.62871603261821818, 72.61133700325008533 ) ) ;
#87184=CARTESIAN_POINT ( 'NONE',  ( -46.34826540902298575, -34.70201877029627724, -36.70216098910028535 ) ) ;
#87195=CARTESIAN_POINT ( 'NONE',  ( 86.96496777674417444, -31.71578965763157498, 187.3089302373552982 ) ) ;
#87202=CARTESIAN_POINT ( 'NONE',  ( 53.23435742203598409, -28.20034973435990011, -27.12572715517088184 ) ) ;
#87207=CARTESIAN_POINT ( 'NONE',  ( -100.7566295605840594, -29.99999999999999645, 180.7218492552073599 ) ) ;
#87209=CARTESIAN_POINT ( 'NONE',  ( 19.28957066462841752, -57.67183861258752131, 42.12264632805888454 ) ) ;
#87222=CARTESIAN_POINT ( 'NONE',  ( -13.37379485725665162, -32.51307406780899356, 29.38708954896887704 ) ) ;
#87223=CARTESIAN_POINT ( 'NONE',  ( -90.88575953229592130, -59.99999999999998579, 60.76790198270563792 ) ) ;
#87237=MECHANICAL_DESIGN_GEOMETRIC_PRESENTATION_REPRESENTATION('',(#78591),#54482);
#87238=CARTESIAN_POINT ( 'NONE',  ( 36.20918625285742110, -33.55288256454751661, 34.82669593431387511 ) ) ;
#87255=CARTESIAN_POINT ( 'NONE',  ( -112.8557562759809798, -60.00000000003905853, 147.0001122092953381 ) ) ;
#87258=CARTESIAN_POINT ( 'NONE',  ( 26.81477069726286544, -60.00000000000001421, 41.67871456507009498 ) ) ;
#87261=CARTESIAN_POINT ( 'NONE',  ( -95.66383100604464573, -60.00000000000002132, 35.18327952992021324 ) ) ;
#87262=CARTESIAN_POINT ( 'NONE',  ( 11.48827963599770285, -53.39680579818115547, 32.81982166506503518 ) ) ;
#87263=CARTESIAN_POINT ( 'NONE',  ( -48.90657022356846539, -46.44393484032057984, 51.21248264059143196 ) ) ;
#87273=CARTESIAN_POINT ( 'NONE',  ( 89.30885607944193794, -29.99999999992603250, 7.018915378132053462 ) ) ;
#87278=CARTESIAN_POINT ( 'NONE',  ( 96.30119089153456002, -30.00000000000000000, 191.2506517886558299 ) ) ;
#87280=ORIENTED_EDGE ( 'NONE', *, *, #84813, .T. ) ;
#87290=CARTESIAN_POINT ( 'NONE',  ( 101.5729318683832361, -38.45079819966511536, 199.8890759196411011 ) ) ;
#87292=CARTESIAN_POINT ( 'NONE',  ( 84.90889233706131733, -52.71069020251738380, 13.63360479297925032 ) ) ;
#87313=CARTESIAN_POINT ( 'NONE',  ( -22.77004263405657625, -20.97328029508773639, 36.31169601591036411 ) ) ;
#87318=CARTESIAN_POINT ( 'NONE',  ( 83.21382037009784938, -57.31687954804421281, 189.0388902036028185 ) ) ;
#87323=CARTESIAN_POINT ( 'NONE',  ( 94.40785360964090955, -57.67103502906764589, -0.2615027077762412944 ) ) ;
#87333=CARTESIAN_POINT ( 'NONE',  ( 9.408375277128495640, -19.97193506209725200, 35.33198514726674944 ) ) ;
#87335=CARTESIAN_POINT ( 'NONE',  ( 51.47742418153980282, -29.90942068293205480, 49.13780789315548247 ) ) ;
#87343=CARTESIAN_POINT ( 'NONE',  ( -82.55502573126497623, -38.00000000000004263, -12.59846151849247420 ) ) ;
#87352=CARTESIAN_POINT ( 'NONE',  ( -7.863041645572806715, -34.58964495997116728, -32.51031543117136380 ) ) ;
#87359=CARTESIAN_POINT ( 'NONE',  ( -92.61039005374894373, -59.99999999999997868, -10.20672413289644531 ) ) ;
#87367=CARTESIAN_POINT ( 'NONE',  ( -84.14012639669060434, -29.03968219319695976, 163.8444925067498730 ) ) ;
#87381=CARTESIAN_POINT ( 'NONE',  ( -104.1916751217198822, -57.64030415157957066, 202.2041723927455905 ) ) ;
#87390=CARTESIAN_POINT ( 'NONE',  ( 76.02438791174152755, -14.21045842199433729, -24.18563911012876844 ) ) ;
#87391=CARTESIAN_POINT ( 'NONE',  ( -68.99627713242672655, -30.00000000000000355, 123.4899896973233808 ) ) ;
#87392=CARTESIAN_POINT ( 'NONE',  ( -54.78113597286795056, -29.09368185507433324, 55.71807950450840252 ) ) ;
#87399=CARTESIAN_POINT ( 'NONE',  ( -100.5507501323638735, -45.26067218560441319, 191.9851517464235542 ) ) ;
#87413=CARTESIAN_POINT ( 'NONE',  ( -28.68834382076860479, -29.06026199098176832, 30.85835075655344895 ) ) ;
#87416=CARTESIAN_POINT ( 'NONE',  ( 48.25720115522312881, -49.89967198185726716, 51.25044237583277607 ) ) ;
#87419=CARTESIAN_POINT ( 'NONE',  ( -108.8776466121674247, -38.35654235866562090, 190.5204387342744496 ) ) ;
#87422=VERTEX_POINT ( 'NONE', #25451 ) ;
#87423=CARTESIAN_POINT ( 'NONE',  ( 84.59625264859418792, -38.35850040426321783, -23.20098218201213314 ) ) ;
#87432=CARTESIAN_POINT ( 'NONE',  ( 103.4822615650508482, -59.99999999999999289, 200.3271293562201834 ) ) ;
#87439=CARTESIAN_POINT ( 'NONE',  ( -91.45565477381764197, -38.38900636631056074, -7.819068096363136711 ) ) ;
#87450=CARTESIAN_POINT ( 'NONE',  ( 80.98187379999048119, -56.93991788919779395, 178.5819717544341358 ) ) ;
#87490=CARTESIAN_POINT ( 'NONE',  ( -110.4357402000322992, -60.00000000000000711, 147.0196122877912330 ) ) ;
#87491=FACE_OUTER_BOUND ( 'NONE', #76094, .T. ) ;
#87493=DIRECTION ( 'NONE',  ( -1.000000000000000000, 0.000000000000000000, -0.000000000000000000 ) ) ;
#87495=CARTESIAN_POINT ( 'NONE',  ( -82.96961521666786155, -53.66285722192446173, 186.0285578845195857 ) ) ;
#87501=CARTESIAN_POINT ( 'NONE',  ( -86.21150843268111430, -60.13471841444653876, 7.287450485273263112 ) ) ;
#87509=CARTESIAN_POINT ( 'NONE',  ( 78.68869634200761709, -14.21045842199439591, 170.0117969751115652 ) ) ;
#87510=CARTESIAN_POINT ( 'NONE',  ( -111.4777060157506128, -60.00000000000003553, 136.6114436209108760 ) ) ;
#87511=CARTESIAN_POINT ( 'NONE',  ( -65.69038446180861968, -18.62633488832963380, 77.38884398866117920 ) ) ;
#87514=CARTESIAN_POINT ( 'NONE',  ( 101.5656943390243043, -59.99999999999504752, 203.9136707109788063 ) ) ;
#87524=CARTESIAN_POINT ( 'NONE',  ( -89.61226365779903347, -59.99999999999998579, -19.45967901788216281 ) ) ;
#87533=CARTESIAN_POINT ( 'NONE',  ( 102.1218162488970052, -59.99999999999997868, 194.0110499945668892 ) ) ;
#87539=CARTESIAN_POINT ( 'NONE',  ( 35.84311413758839393, -39.50387582939524833, 35.79840239775683841 ) ) ;
#87540=CARTESIAN_POINT ( 'NONE',  ( 8.569529079651905690, -1.734723475976807094E-15, -14.86825985027703290 ) ) ;
#87554=CARTESIAN_POINT ( 'NONE',  ( 93.32736978825312235, -59.99999999999999289, 35.45440158309499168 ) ) ;
#87561=CARTESIAN_POINT ( 'NONE',  ( -85.43970026633695625, -30.00000000001166711, -20.50169416853363913 ) ) ;
#87566=CARTESIAN_POINT ( 'NONE',  ( 84.79608313886490123, -60.18564194205600160, -16.37796101195803899 ) ) ;
#87575=CARTESIAN_POINT ( 'NONE',  ( 81.45652690482418734, -25.62336553616171386, 139.9540395895450615 ) ) ;
#87581=CARTESIAN_POINT ( 'NONE',  ( -67.94141844175470624, -57.68152395592925785, 141.0744097219443347 ) ) ;
#87593=CARTESIAN_POINT ( 'NONE',  ( -19.40485415781282441, -16.85763090055889180, 31.48763308485285606 ) ) ;
#87608=CARTESIAN_POINT ( 'NONE',  ( -67.72357546289919128, -30.20750568365551914, -30.58700924850430525 ) ) ;
#87609=CARTESIAN_POINT ( 'NONE',  ( -82.85790275495963897, -30.00000000000000355, 151.8675718132654708 ) ) ;
#87614=CARTESIAN_POINT ( 'NONE',  ( 90.68632663689517415, -57.61165737844666523, 204.1158738846914105 ) ) ;
#87615=CARTESIAN_POINT ( 'NONE',  ( 60.68635431291335891, -60.22842679285083278, -29.53366749605343244 ) ) ;
#87619=CARTESIAN_POINT ( 'NONE',  ( -54.67094165204726153, -59.99999999999999289, 84.31617412822056679 ) ) ;
#87624=CARTESIAN_POINT ( 'NONE',  ( -85.88675850019390623, -35.61340147578555104, 185.0195460185883007 ) ) ;
#87629=CARTESIAN_POINT ( 'NONE',  ( -83.04293233812605024, -45.25987585949575731, -14.40421945740175502 ) ) ;
#87639=CARTESIAN_POINT ( 'NONE',  ( -19.43146043914380172, -4.830718742626120971E-12, 11.19959342723174522 ) ) ;
#87643=CARTESIAN_POINT ( 'NONE',  ( 72.33341283407553135, -14.21045842199439235, -25.95464913363236548 ) ) ;
#87644=CARTESIAN_POINT ( 'NONE',  ( -80.37542441551636330, -32.56178760357695268, 140.7699095010514441 ) ) ;
#87648=CARTESIAN_POINT ( 'NONE',  ( 95.57460276385096165, -57.62113478352900842, 204.5314498424847329 ) ) ;
#87655=PLANE ( 'NONE',  #103524 ) ;
#87656=CARTESIAN_POINT ( 'NONE',  ( -102.6106292806730949, -37.82052530689579584, 165.6551701195334658 ) ) ;
#87669=CARTESIAN_POINT ( 'NONE',  ( -48.02140427201592132, -30.00000000000008527, 60.50294052774201958 ) ) ;
#87670=CARTESIAN_POINT ( 'NONE',  ( 27.39423346129563441, -56.86438257397906426, 35.32388413555721485 ) ) ;
#87675=CARTESIAN_POINT ( 'NONE',  ( -6.539732759932824102, -4.285714285714295357, -24.41571844174603712 ) ) ;
#87683=CARTESIAN_POINT ( 'NONE',  ( 78.10340256886549071, -29.99999999999998224, 123.8744046566280161 ) ) ;
#87686=CARTESIAN_POINT ( 'NONE',  ( 81.59416543435395397, -30.00000000000000000, -6.868947773689183300 ) ) ;
#87689=B_SPLINE_CURVE_WITH_KNOTS ( 'NONE', 3,
 ( #91389, #17505, #1270, #99992 ),
 .UNSPECIFIED., .F., .F.,
 ( 4, 4 ),
 ( 0.04383972994809587354, 1.043839729948095485 ),
 .UNSPECIFIED. ) ;
#87700=EDGE_LOOP ( 'NONE', ( #6911, #46605 ) ) ;
#87704=CARTESIAN_POINT ( 'NONE',  ( 49.92867099129379227, -38.33222471381543528, 68.31434411807451568 ) ) ;
#87707=CARTESIAN_POINT ( 'NONE',  ( -82.88816647256838621, -60.00000000000002132, 189.8675524425106005 ) ) ;
#87708=CARTESIAN_POINT ( 'NONE',  ( 62.93388706622030071, -56.86266190362758977, 89.13451098117751314 ) ) ;
#87711=CARTESIAN_POINT ( 'NONE',  ( -67.61735429566955702, -38.09521185367891860, -32.01360535522618989 ) ) ;
#87718=CARTESIAN_POINT ( 'NONE',  ( -22.49475958402852172, -60.00000000000000711, -35.87305261535499312 ) ) ;
#87725=CARTESIAN_POINT ( 'NONE',  ( 86.71645349442924555, -24.38046412487985393, 185.1854681036936370 ) ) ;
#87732=CARTESIAN_POINT ( 'NONE',  ( 15.26317471455340602, -17.21745123649166231, -34.34608131406640297 ) ) ;
#87737=CARTESIAN_POINT ( 'NONE',  ( -100.8735123380655949, -29.99999999999999645, 179.4413083801154301 ) ) ;
#87740=CARTESIAN_POINT ( 'NONE',  ( 52.23423719002784793, -57.67654141413034807, 83.35420455408277007 ) ) ;
#87751=CARTESIAN_POINT ( 'NONE',  ( -86.68846525915618884, -17.00810435402869913, 185.5403106198691887 ) ) ;
#87755=CARTESIAN_POINT ( 'NONE',  ( -11.28694547044951868, -35.99452350529739419, 29.91534077212351761 ) ) ;
#87763=CARTESIAN_POINT ( 'NONE',  ( 65.89100576562174183, -60.00000000000002842, 121.9363084267107809 ) ) ;
#87782=CARTESIAN_POINT ( 'NONE',  ( -86.26287741613369064, -59.99999999999507594, 203.3882217285910201 ) ) ;
#87785=CARTESIAN_POINT ( 'NONE',  ( 74.21466443961692505, -60.00000000000000000, 174.3944259474788510 ) ) ;
#87788=CARTESIAN_POINT ( 'NONE',  ( -110.8742113967375928, -60.00000000000001421, 132.3764718065442594 ) ) ;
#87789=CARTESIAN_POINT ( 'NONE',  ( 8.111369670363336226, -32.51052359539890801, 29.30105919468876152 ) ) ;
#87792=CARTESIAN_POINT ( 'NONE',  ( -45.59210809638418027, -46.44287893288203151, 46.30682524688919699 ) ) ;
#87804=CARTESIAN_POINT ( 'NONE',  ( 80.99227329964719502, -29.99999999995507238, 192.5733771533335812 ) ) ;
#87808=CARTESIAN_POINT ( 'NONE',  ( 99.00617620828374754, -29.99999999999999645, 188.8169106426751966 ) ) ;
#87824=CARTESIAN_POINT ( 'NONE',  ( 105.8687044990643500, -38.37890680998027904, 196.5118811510903640 ) ) ;
#87826=CARTESIAN_POINT ( 'NONE',  ( 87.01625201393999021, -60.20567772451860122, -8.192381583340527129 ) ) ;
#87843=CARTESIAN_POINT ( 'NONE',  ( 43.54313159148357926, -29.68436378173572265, 52.44550087950238293 ) ) ;
#87848=CARTESIAN_POINT ( 'NONE',  ( 83.13947484406011768, -60.93864057100361009, 190.8861806389487867 ) ) ;
#87852=CARTESIAN_POINT ( 'NONE',  ( 95.57416616939285348, -57.67170004321813082, 37.82161414657011989 ) ) ;
#87856=CARTESIAN_POINT ( 'NONE',  ( -9.288740593950837621, -22.45067348962094300, -38.54328090126934114 ) ) ;
#87861=CARTESIAN_POINT ( 'NONE',  ( 51.04048647703990582, -29.85962867422984246, 48.35404991630245775 ) ) ;
#87869=CARTESIAN_POINT ( 'NONE',  ( -102.8125839197916775, -37.99999999999999289, 170.8447077551169002 ) ) ;
#87877=CARTESIAN_POINT ( 'NONE',  ( -47.71675376065731200, -47.40886959700829806, -30.35352467222949358 ) ) ;
#87887=CARTESIAN_POINT ( 'NONE',  ( -92.53668747331201416, -60.00000000000000711, -1.795014215929801260 ) ) ;
#87892=DIRECTION ( 'NONE',  ( -0.000000000000000000, 1.000000000000000000, -0.000000000000000000 ) ) ;
#87894=CARTESIAN_POINT ( 'NONE',  ( -79.61189064004022953, -56.85762575183416345, 165.3701725720323736 ) ) ;
#87898=ORIENTED_EDGE ( 'NONE', *, *, #46622, .T. ) ;
#87906=CARTESIAN_POINT ( 'NONE',  ( -80.15954706948889452, -57.50857130571672826, 199.0044224626226139 ) ) ;
#87911=CARTESIAN_POINT ( 'NONE',  ( 86.58362542449755495, -60.00000000000002132, -26.27920600484676683 ) ) ;
#87912=CARTESIAN_POINT ( 'NONE',  ( -48.81109529425772564, -14.21045842199442788, 55.84243332122913017 ) ) ;
#87913=CARTESIAN_POINT ( 'NONE',  ( -54.79799674529369469, -49.91194600308500640, 64.09558544181255968 ) ) ;
#87918=CARTESIAN_POINT ( 'NONE',  ( -102.3353922011937556, -60.19607622334896035, 193.7979307818540349 ) ) ;
#87924=CARTESIAN_POINT ( 'NONE',  ( 88.11249734486904117, -38.37137927187098541, -19.43261626278027521 ) ) ;
#87934=CARTESIAN_POINT ( 'NONE',  ( -27.64215802503290575, -32.53081356062803309, 31.18544280887772757 ) ) ;
#87938=CARTESIAN_POINT ( 'NONE',  ( 48.77471784688194134, -32.59704705468854513, 46.61485220210019520 ) ) ;
#87942=CARTESIAN_POINT ( 'NONE',  ( -104.5350828174626798, -38.40247479459341662, 197.9350992758817540 ) ) ;
#87943=ORIENTED_EDGE ( 'NONE', *, *, #94030, .F. ) ;
#87944=CARTESIAN_POINT ( 'NONE',  ( 91.38818257286023083, -38.39638879886640410, -9.329338805212154639 ) ) ;
#87954=CARTESIAN_POINT ( 'NONE',  ( 93.39948790556088909, -59.99999999999999289, 202.5047245700688450 ) ) ;
#87960=CARTESIAN_POINT ( 'NONE',  ( 58.40048366602277952, -36.01844938180519762, 66.61435485081292995 ) ) ;
#87966=CARTESIAN_POINT ( 'NONE',  ( -105.0601071971127993, -38.35601112544424751, 118.3067828870811553 ) ) ;
#87976=CARTESIAN_POINT ( 'NONE',  ( 82.07540746790368758, -53.52673662087732964, 181.8248042487631437 ) ) ;
#87986=EDGE_CURVE ( 'NONE', #6442, #85478, #63082, .T. ) ;
#87988=CARTESIAN_POINT ( 'NONE',  ( -81.02915809513567069, -30.00000000000000355, 21.48644426250730533 ) ) ;
#87993=CARTESIAN_POINT ( 'NONE',  ( -3.554850123176898080, -18.30354541650124389, 35.04484280488642156 ) ) ;
#88015=UNCERTAINTY_MEASURE_WITH_UNIT (LENGTH_MEASURE( 1.000000000000000082E-05 ), #61140, 'distance_accuracy_value', 'NONE');
#88016=CARTESIAN_POINT ( 'NONE',  ( -110.1493983374076464, -60.00000000000000000, 144.6509950877594690 ) ) ;
#88021=CARTESIAN_POINT ( 'NONE',  ( -82.38425619239932018, -57.17888456031388955, 186.5847884272003228 ) ) ;
#88029=CARTESIAN_POINT ( 'NONE',  ( -83.66837389949749593, -45.26505878923314441, 10.83132005844547940 ) ) ;
#88037=CARTESIAN_POINT ( 'NONE',  ( 104.7858654919042465, -14.21045842199433018, 190.1692295410596785 ) ) ;
#88039=CARTESIAN_POINT ( 'NONE',  ( -90.15663891815873399, -29.99999999999996447, 30.33658191415442573 ) ) ;
#88040=CARTESIAN_POINT ( 'NONE',  ( -65.35149797169954411, -49.91477803733943830, 92.77736392452831637 ) ) ;
#88043=CARTESIAN_POINT ( 'NONE',  ( 64.99933408347442310, -60.00000000015575097, 127.5571855012964733 ) ) ;
#88045=CARTESIAN_POINT ( 'NONE',  ( 2.020670042218083218, -42.95360395253835861, 31.04613490824499067 ) ) ;
#88053=CARTESIAN_POINT ( 'NONE',  ( -91.22230685359441793, -60.00000000000002132, 202.2302250722651706 ) ) ;
#88063=CARTESIAN_POINT ( 'NONE',  ( 104.7431539673617493, -60.00000000000000000, 188.6673425520828573 ) ) ;
#88064=CARTESIAN_POINT ( 'NONE',  ( -36.59778291639800329, -32.58603346802485135, 34.88119437908692078 ) ) ;
#88066=ORIENTED_EDGE ( 'NONE', *, *, #62055, .T. ) ;
#88068=CARTESIAN_POINT ( 'NONE',  ( 36.59759212853143850, -53.35504654647210998, 39.00208765491442620 ) ) ;
#88069=CARTESIAN_POINT ( 'NONE',  ( -14.86825985028395181, -1.734723475976807094E-15, -8.569529079644194525 ) ) ;
#88073=CARTESIAN_POINT ( 'NONE',  ( -67.36060469812591123, -38.33500041653474710, 122.7867264952750475 ) ) ;
#88083=CARTESIAN_POINT ( 'NONE',  ( 94.50007956662228992, -60.00000000000000711, 45.30279473861475026 ) ) ;
#88089=CARTESIAN_POINT ( 'NONE',  ( -84.45496583931854673, -29.99999999999999645, 165.1288136768957031 ) ) ;
#88103=CARTESIAN_POINT ( 'NONE',  ( 80.30221349524663310, -39.49731160925162499, 147.7246413452121487 ) ) ;
#88124=CARTESIAN_POINT ( 'NONE',  ( -29.69263446058518596, -21.53086560699351892, 32.09607384880168723 ) ) ;
#88136=CARTESIAN_POINT ( 'NONE',  ( -72.03391849934671143, -30.00000000000000000, 102.0186397125481506 ) ) ;
#88143=CARTESIAN_POINT ( 'NONE',  ( 88.84533078683669771, -57.60264346193348928, 203.6993548357257851 ) ) ;
#88144=CARTESIAN_POINT ( 'NONE',  ( 73.91531349502166393, -47.40886024016416656, -22.31105010388982279 ) ) ;
#88145=DIRECTION ( 'NONE',  ( 0.000000000000000000, 0.000000000000000000, 1.000000000000000000 ) ) ;
#88148=CARTESIAN_POINT ( 'NONE',  ( -75.41707018382817296, -60.00000000000002132, 184.0048572794236179 ) ) ;
#88152=CARTESIAN_POINT ( 'NONE',  ( -85.41682882701736901, -42.92406899005316490, 186.8839715543561510 ) ) ;
#88165=CARTESIAN_POINT ( 'NONE',  ( 2.723397405354400211E-15, -8.673617379884035472E-16, 22.23822744035697241 ) ) ;
#88167=CARTESIAN_POINT ( 'NONE',  ( 89.90448154148772630, -29.99999999999993605, -11.15250327688899645 ) ) ;
#88168=CARTESIAN_POINT ( 'NONE',  ( -80.36800950332954585, -29.09175213282752992, 137.3191375394279419 ) ) ;
#88170=CARTESIAN_POINT ( 'NONE',  ( 28.47648766833107103, -14.21045842199436926, 36.49840447651481412 ) ) ;
#88172=CARTESIAN_POINT ( 'NONE',  ( 103.6548915283567993, -57.63783869900026247, 202.5245876488449426 ) ) ;
#88181=CARTESIAN_POINT ( 'NONE',  ( -106.5035232221163426, -60.15522548674435654, 170.5901316164547836 ) ) ;
#88193=CARTESIAN_POINT ( 'NONE',  ( -25.54656159126955117, -59.99999999999990763, 43.65498583421084788 ) ) ;
#88194=CARTESIAN_POINT ( 'NONE',  ( 27.18233788174618937, -36.00292342176191340, 31.66508634081275630 ) ) ;
#88202=CARTESIAN_POINT ( 'NONE',  ( -113.4247593822225042, -60.00000000000000000, 152.6440057603899447 ) ) ;
#88209=CARTESIAN_POINT ( 'NONE',  ( 63.72657953987652490, -30.00000000000000000, 76.60532204191858341 ) ) ;
#88214=CARTESIAN_POINT ( 'NONE',  ( 0.000000000000000000, 0.000000000000000000, -8.000000000000000000 ) ) ;
#88236=CARTESIAN_POINT ( 'NONE',  ( 63.81288939447262010, -42.95796419212698680, 84.51729907025924149 ) ) ;
#88241=CARTESIAN_POINT ( 'NONE',  ( -14.05937931246655026, -57.67120694556813731, -44.20476115079929258 ) ) ;
#88245=CARTESIAN_POINT ( 'NONE',  ( -1.780747208277499993, -60.00000000000000000, -36.88202602987092860 ) ) ;
#88251=CARTESIAN_POINT ( 'NONE',  ( 86.84945405509184013, -28.04156739919917385, 186.3543369133316503 ) ) ;
#88261=CARTESIAN_POINT ( 'NONE',  ( 39.15529195327606971, -60.00000000000000000, 50.94776041160520208 ) ) ;
#88262=CARTESIAN_POINT ( 'NONE',  ( -99.14678559174451777, -29.99999999999999645, 146.1870180612345109 ) ) ;
#88264=EDGE_CURVE ( 'NONE', #87422, #53391, #70511, .T. ) ;
#88267=CARTESIAN_POINT ( 'NONE',  ( 35.66404283213154258, -57.69580505578924345, 49.84151983041640932 ) ) ;
#88274=CARTESIAN_POINT ( 'NONE',  ( -16.78325067526352044, -60.00000000000000711, 39.90621369170523991 ) ) ;
#88276=CARTESIAN_POINT ( 'NONE',  ( -86.87673661167058015, -20.64820290907504940, 186.0011859003656980 ) ) ;
#88280=CARTESIAN_POINT ( 'NONE',  ( -14.55865618082035873, -39.47623590528959880, 30.59058187625803527 ) ) ;
#88282=CARTESIAN_POINT ( 'NONE',  ( -105.0711731827093018, -60.00000000000000711, 187.5141690426402192 ) ) ;
#88293=CARTESIAN_POINT ( 'NONE',  ( 68.86877790052056980, -60.00000000000000711, 135.3615938647542407 ) ) ;
#88299=CARTESIAN_POINT ( 'NONE',  ( 12.83322425571993186, -59.99999999999995737, 42.04720346242444151 ) ) ;
#88313=CARTESIAN_POINT ( 'NONE',  ( -112.8182474800815243, -59.99999999999511147, 189.9060221141766931 ) ) ;
#88315=CARTESIAN_POINT ( 'NONE',  ( 76.54505153461919065, -60.00000000000001421, 189.0643905970971446 ) ) ;
#88318=CARTESIAN_POINT ( 'NONE',  ( -104.7861223705664599, -14.21045842199442433, 190.1679628257406875 ) ) ;
#88319=CARTESIAN_POINT ( 'NONE',  ( 10.41105519390918843, -53.39685824552639559, 32.80285974031103535 ) ) ;
#88321=CARTESIAN_POINT ( 'NONE',  ( 102.6780276613828278, -38.00000000000000711, 166.4682704798183295 ) ) ;
#88323=ADVANCED_FACE ( 'NONE', ( #79127 ), #3347, .T. ) ;
#88324=CARTESIAN_POINT ( 'NONE',  ( -45.67848460884854944, -56.80937477045559802, 49.30617761660595022 ) ) ;
#88335=CARTESIAN_POINT ( 'NONE',  ( 105.3833277626438871, -29.99999999999387157, 194.8351416830720666 ) ) ;
#88341=CARTESIAN_POINT ( 'NONE',  ( 92.39057177564670553, -30.00000000000000355, 102.4589548229546949 ) ) ;
#88343=DIRECTION ( 'NONE',  ( 0.000000000000000000, 0.000000000000000000, 1.000000000000000000 ) ) ;
#88355=CARTESIAN_POINT ( 'NONE',  ( 88.77998102494933619, -38.53862295708325547, 200.2196504074838117 ) ) ;
#88357=CARTESIAN_POINT ( 'NONE',  ( 87.03565217808413479, -60.19692735285366325, -7.183757740799211255 ) ) ;
#88358=CARTESIAN_POINT ( 'NONE',  ( 77.65976466551792612, -37.99999999999995737, 131.2189903408646785 ) ) ;
#88360=CARTESIAN_POINT ( 'NONE',  ( 0.000000000000000000, 30.00000000000000000, 0.000000000000000000 ) ) ;
#88377=CARTESIAN_POINT ( 'NONE',  ( 41.33631551152040373, -29.05874733539805632, 49.05523552014034294 ) ) ;
#88381=CARTESIAN_POINT ( 'NONE',  ( 85.30112616295713224, -35.74003604604289563, 182.5928498885529052 ) ) ;
#88386=CARTESIAN_POINT ( 'NONE',  ( 95.59699575574133235, -57.67169082706072913, 38.02165857417077177 ) ) ;
#88398=CARTESIAN_POINT ( 'NONE',  ( -9.858548355958978604, -23.16810237002645678, -30.52285683705125052 ) ) ;
#88402=CARTESIAN_POINT ( 'NONE',  ( -102.2211543079583294, -38.00000000000004974, 182.8469250058557805 ) ) ;
#88408=CARTESIAN_POINT ( 'NONE',  ( -23.91971553424620112, -19.70479182448596589, -33.18013212959203173 ) ) ;
#88410=CARTESIAN_POINT ( 'NONE',  ( -57.64009741160396061, -60.22830627530903058, -30.33965759735865575 ) ) ;
#88417=CARTESIAN_POINT ( 'NONE',  ( -92.53465222392649991, -60.00000000000000711, -1.764304992001874517 ) ) ;
#88421=CARTESIAN_POINT ( 'NONE',  ( 100.4533534623010098, -60.28154197531982561, 195.5193666514165614 ) ) ;
#88424=CARTESIAN_POINT ( 'NONE',  ( -79.90040665909508277, -60.36515567690381090, 174.0697010744071065 ) ) ;
#88437=CARTESIAN_POINT ( 'NONE',  ( -96.25446706653225704, -57.62198180035323247, 204.5564252943773340 ) ) ;
#88443=CARTESIAN_POINT ( 'NONE',  ( 95.18118770502717041, -60.00000000000013500, -7.509903379402337542 ) ) ;
#88445=CARTESIAN_POINT ( 'NONE',  ( -64.23299091672136285, -59.99999999999999289, 125.0187485388276656 ) ) ;
#88447=CARTESIAN_POINT ( 'NONE',  ( -53.32813900909374638, -53.37880559940036562, 62.19817634995050781 ) ) ;
#88451=CARTESIAN_POINT ( 'NONE',  ( -99.57148504860369087, -37.80425350881786528, 191.2424562810986686 ) ) ;
#88455=CARTESIAN_POINT ( 'NONE',  ( 80.35317488720673396, -38.35617844620870187, -26.29242304138821851 ) ) ;
#88462=CARTESIAN_POINT ( 'NONE',  ( 63.00516225510686752, -29.99999999999999289, 74.69021731496640371 ) ) ;
#88470=CARTESIAN_POINT ( 'NONE',  ( 49.15655608998503112, -29.13270878632327054, 46.07185368943500237 ) ) ;
#88473=CARTESIAN_POINT ( 'NONE',  ( -102.1566426654864301, -38.44188724825352210, 199.6156023558743584 ) ) ;
#88475=CARTESIAN_POINT ( 'NONE',  ( 91.29669025949715433, -38.40056992187813734, -10.42823402827028190 ) ) ;
#88479=CARTESIAN_POINT ( 'NONE',  ( 105.6700157783516829, -60.15124779082972140, 156.3737876120203794 ) ) ;
#88485=CARTESIAN_POINT ( 'NONE',  ( 78.99695195452900975, -60.00000000000000000, 194.6422132151330118 ) ) ;
#88489=CARTESIAN_POINT ( 'NONE',  ( 55.72842314015646537, -56.85053476136143757, 69.22857699785234331 ) ) ;
#88494=CARTESIAN_POINT ( 'NONE',  ( -100.3096506332310014, -38.46452049353877101, 200.4061333699972920 ) ) ;
#88504=VERTEX_POINT ( 'NONE', #85961 ) ;
#88505=CARTESIAN_POINT ( 'NONE',  ( 84.74071589511709135, -28.95261022299601095, 169.9338770228943076 ) ) ;
#88542=CARTESIAN_POINT ( 'NONE',  ( -106.5419819426516881, -60.00000000000000711, 119.7747142723297742 ) ) ;
#88548=CARTESIAN_POINT ( 'NONE',  ( -82.82730212088782196, -46.49498115257645736, 178.5359483646249998 ) ) ;
#88555=CARTESIAN_POINT ( 'NONE',  ( -86.56691879974580672, -60.14943795851970521, 24.17102811031225684 ) ) ;
#88561=CARTESIAN_POINT ( 'NONE',  ( 106.6028846201213440, -30.00000000000002487, 192.6838848496860521 ) ) ;
#88562=CARTESIAN_POINT ( 'NONE',  ( -90.56108803656626094, -30.00000000000000711, 34.47189148671483849 ) ) ;
#88563=CARTESIAN_POINT ( 'NONE',  ( -61.04315145770602413, -42.96496502653089067, 76.66717857525411262 ) ) ;
#88566=CARTESIAN_POINT ( 'NONE',  ( 82.32787579396226363, -60.00000000001609379, 201.4521251157181325 ) ) ;
#88568=CARTESIAN_POINT ( 'NONE',  ( 3.050709723766003911, -46.43461503410409819, 31.62373175404598769 ) ) ;
#88576=CARTESIAN_POINT ( 'NONE',  ( -94.73029569914376680, -59.99999999999997868, 47.21885834219733624 ) ) ;
#88582=DIRECTION ( 'NONE',  ( 0.000000000000000000, -1.000000000000000000, 0.000000000000000000 ) ) ;
#88589=CARTESIAN_POINT ( 'NONE',  ( -36.22558170428006719, -46.43489304307155408, 37.39699883427675076 ) ) ;
#88592=CARTESIAN_POINT ( 'NONE',  ( 40.62864974475749591, -25.69507913308015645, 36.04227385710505160 ) ) ;
#88593=CARTESIAN_POINT ( 'NONE',  ( -10.45706415777859455, -1.734723475976807094E-15, 13.60704923275178935 ) ) ;
#88596=CARTESIAN_POINT ( 'NONE',  ( -66.69118985233596675, -38.33596727070246146, 120.0288781097716537 ) ) ;
#88606=CARTESIAN_POINT ( 'NONE',  ( 100.7656204750565649, -60.00000000000001421, 85.52486764147262477 ) ) ;
#88611=CARTESIAN_POINT ( 'NONE',  ( -65.15920822928832479, -30.00000000000001066, 80.64472866489825265 ) ) ;
#88626=CARTESIAN_POINT ( 'NONE',  ( 78.92104432068852304, -56.84203907387598775, 159.0975971619027121 ) ) ;
#88634=CARTESIAN_POINT ( 'NONE',  ( -53.52971897118871425, -57.67555505732850207, 87.03092276603273092 ) ) ;
#88656=CARTESIAN_POINT ( 'NONE',  ( -6.206025854132298569, -21.79809244015144998, -38.54595585258209667 ) ) ;
#88657=CARTESIAN_POINT ( 'NONE',  ( -59.07834085828424264, -30.00000000000000711, 64.72383880810683365 ) ) ;
#88663=CARTESIAN_POINT ( 'NONE',  ( 91.70293005516124651, -57.61487155903986945, 204.2876863399782508 ) ) ;
#88670=CARTESIAN_POINT ( 'NONE',  ( -72.48404470694545410, -60.00000000000001421, 158.0047739593530309 ) ) ;
#88675=CARTESIAN_POINT ( 'NONE',  ( -86.18651039905068956, -24.72797755481551363, 181.0558452470112911 ) ) ;
#88688=CARTESIAN_POINT ( 'NONE',  ( 10.45706415778036025, -1.734723475976807094E-15, -13.60704923275195455 ) ) ;
#88690=CARTESIAN_POINT ( 'NONE',  ( 61.70037527280209844, -30.00000000000006040, -32.45262418874342103 ) ) ;
#88691=CARTESIAN_POINT ( 'NONE',  ( -79.30432945941426226, -39.49937122350303298, 141.5529580233551883 ) ) ;
#88694=CARTESIAN_POINT ( 'NONE',  ( 43.57856552656106430, -59.99999999999991473, 62.86110226080823793 ) ) ;
#88696=CARTESIAN_POINT ( 'NONE',  ( 101.4167185739037649, -57.63043782431127227, 203.4936600526360451 ) ) ;
#88708=CARTESIAN_POINT ( 'NONE',  ( -103.1762899285966881, -45.26535789155201428, 156.3495666460457585 ) ) ;
#88720=CARTESIAN_POINT ( 'NONE',  ( 31.88784071051081170, -56.84613636546770721, 36.98492141617447260 ) ) ;
#88733=CARTESIAN_POINT ( 'NONE',  ( 61.59314311649531248, -60.00000000000001421, -35.21162133311354125 ) ) ;
#88757=CARTESIAN_POINT ( 'NONE',  ( 65.35202525436315568, -49.90957767371891407, 92.77620802272491574 ) ) ;
#88759=ORIENTED_EDGE ( 'NONE', *, *, #9063, .T. ) ;
#88762=CARTESIAN_POINT ( 'NONE',  ( -11.25758791135831594, -57.67118876967119689, -44.34807234721190383 ) ) ;
#88776=CARTESIAN_POINT ( 'NONE',  ( 86.51826356133454965, -17.01126878319249869, 184.3016907190141467 ) ) ;
#88785=CARTESIAN_POINT ( 'NONE',  ( 33.19169623717888129, -60.00000000000000711, 44.98076713291913364 ) ) ;
#88786=CARTESIAN_POINT ( 'NONE',  ( -99.80277137147388089, -29.99999999999998934, 186.4011847855257997 ) ) ;
#88789=CARTESIAN_POINT ( 'NONE',  ( 45.09405268356402985, -57.68306127209417156, 65.36625235151646507 ) ) ;
#88796=CARTESIAN_POINT ( 'NONE',  ( -22.96940955295018583, -60.00000000000001421, 40.68925847043787059 ) ) ;
#88798=CARTESIAN_POINT ( 'NONE',  ( -86.68948599710770964, -20.67461466719461072, 184.9450686744756638 ) ) ;
#88804=CARTESIAN_POINT ( 'NONE',  ( -10.44718778294642547, -56.88425898734509190, 33.38460417480683873 ) ) ;
#88805=CARTESIAN_POINT ( 'NONE',  ( -86.31506357673099217, -59.99999999999993605, 20.26404540652117348 ) ) ;
#88812=CARTESIAN_POINT ( 'NONE',  ( 68.03985042304489639, -60.00000000000000000, 131.2812129801127128 ) ) ;
#88817=CARTESIAN_POINT ( 'NONE',  ( 8.309829428344436053, -30.00000000000008527, 36.98670151680749996 ) ) ;
#88833=CARTESIAN_POINT ( 'NONE',  ( -84.07952891099454007, -59.99999999997081090, 202.4448410950529933 ) ) ;
#88835=CARTESIAN_POINT ( 'NONE',  ( 50.14918825808751990, -59.99999999999997158, 72.16795998310614380 ) ) ;
#88838=CARTESIAN_POINT ( 'NONE',  ( -109.4365443207511390, -30.00000000000002487, 178.4890703142130519 ) ) ;
#88839=CARTESIAN_POINT ( 'NONE',  ( 13.61911990997247912, -49.91571610495643796, 32.29718510433961853 ) ) ;
#88840=CARTESIAN_POINT ( 'NONE',  ( 82.95080249199725131, -37.99999999999999289, 0.1906324524714007318 ) ) ;
#88843=CARTESIAN_POINT ( 'NONE',  ( -47.01998836181715546, -32.61244973267624658, 44.20308275279673182 ) ) ;
#88859=CARTESIAN_POINT ( 'NONE',  ( 85.40235745944882240, -30.00000000001180567, 197.3970878040293258 ) ) ;
#88864=CARTESIAN_POINT ( 'NONE',  ( 97.89651928708440209, -30.00000000000000355, 136.8046996854560291 ) ) ;
#88877=CARTESIAN_POINT ( 'NONE',  ( 77.57546568842502666, -38.52226549919825516, 186.7529093661793240 ) ) ;
#88879=CARTESIAN_POINT ( 'NONE',  ( 85.72732811624759108, -52.73815978549392014, -5.088828352706781466 ) ) ;
#88880=CARTESIAN_POINT ( 'NONE',  ( 54.54809302485524114, -37.99999999999998579, 58.67176596216953044 ) ) ;
#88896=CARTESIAN_POINT ( 'NONE',  ( -17.95542721193044144, -24.37817513870772146, 36.37955489103553930 ) ) ;
#88899=CARTESIAN_POINT ( 'NONE',  ( 85.97695406691678954, -24.93193571675475084, 178.6345212492455516 ) ) ;
#88904=CARTESIAN_POINT ( 'NONE',  ( 94.18556020815232444, -57.67258279061592674, 22.45562361954496922 ) ) ;
#88905=CARTESIAN_POINT ( 'NONE',  ( -71.17284327374473207, -38.00000000000000711, -21.88481141223168436 ) ) ;
#88912=CARTESIAN_POINT ( 'NONE',  ( -67.05072968586063098, -37.99999999999999289, 91.59218951166944578 ) ) ;
#88928=CARTESIAN_POINT ( 'NONE',  ( -82.80614267855605704, -38.00000000000003553, -11.81022639143571062 ) ) ;
#88932=CARTESIAN_POINT ( 'NONE',  ( -7.488027283362990616, -15.86055150849546891, -34.99201987073333697 ) ) ;
#88935=CARTESIAN_POINT ( 'NONE',  ( -60.68503947009055821, -60.22838572110379829, -29.53389179007121612 ) ) ;
#88940=CARTESIAN_POINT ( 'NONE',  ( -92.38535695020712524, -60.00000000000000711, 0.3501147898381914425 ) ) ;
#88943=CARTESIAN_POINT ( 'NONE',  ( 100.1607552341765626, -52.76472588658410245, 194.0887023229978752 ) ) ;
#88947=AXIS2_PLACEMENT_3D ( 'NONE', #90991, #58621, #91521 ) ;
#88948=CARTESIAN_POINT ( 'NONE',  ( -79.60123751058100083, -60.34287689035896562, 171.0025021070919138 ) ) ;
#88960=CARTESIAN_POINT ( 'NONE',  ( -102.4013124767651135, -57.63331223797548120, 203.1247769353137755 ) ) ;
#88965=CARTESIAN_POINT ( 'NONE',  ( -2.770043159915164477, -30.00000000000000355, -40.00000000000000000 ) ) ;
#88967=CARTESIAN_POINT ( 'NONE',  ( -12.83279097724939000, -59.99999999999996447, 42.04727692947117390 ) ) ;
#88969=CARTESIAN_POINT ( 'NONE',  ( -51.33271646286868872, -56.84205495537675290, 59.27433511503952701 ) ) ;
#88972=CARTESIAN_POINT ( 'NONE',  ( -97.77229920577525490, -60.35143482894316236, 196.6193423550709838 ) ) ;
#88978=CARTESIAN_POINT ( 'NONE',  ( 86.54967306013999462, -38.36251286152597828, -21.34969726277113722 ) ) ;
#88983=CARTESIAN_POINT ( 'NONE',  ( 84.65080674787581927, -30.00000000000000355, 167.0029673134147572 ) ) ;
#88992=CARTESIAN_POINT ( 'NONE',  ( 48.79736262066600005, -53.36142271290932371, 53.26804720879731292 ) ) ;
#88999=CARTESIAN_POINT ( 'NONE',  ( -110.5647867906232307, -38.35612385186053075, 181.7710796630721006 ) ) ;
#89001=CARTESIAN_POINT ( 'NONE',  ( 110.0387909984985839, -38.35604073266033254, 155.0741904860052784 ) ) ;
#89006=CARTESIAN_POINT ( 'NONE',  ( 95.18346684494451893, -45.28272192646301164, 101.5333130734479710 ) ) ;
#89011=CARTESIAN_POINT ( 'NONE',  ( 83.36324000638602172, -60.00000000000000711, 199.0841329743253141 ) ) ;
#89015=CARTESIAN_POINT ( 'NONE',  ( 58.31012229776316502, -22.13292565276272583, 60.29346654336805500 ) ) ;
#89017=CARTESIAN_POINT ( 'NONE',  ( 80.00000000000000000, -52.00000000000000000, -19.09707704303353282 ) ) ;
#89020=CARTESIAN_POINT ( 'NONE',  ( -108.5122601155575381, -38.35613504444431499, 141.2758010726541613 ) ) ;
#89024=DIRECTION ( 'NONE',  ( -0.000000000000000000, -1.000000000000000000, -0.000000000000000000 ) ) ;
#89029=CARTESIAN_POINT ( 'NONE',  ( 83.65262599924042775, -39.46245688817372610, 175.6971847891388165 ) ) ;
#89066=CARTESIAN_POINT ( 'NONE',  ( -2.499999999999944933, -22.55587783588024919, 27.64562232041509304 ) ) ;
#89070=CARTESIAN_POINT ( 'NONE',  ( -112.0871042065531498, -59.99999999999998579, 178.2000521787075229 ) ) ;
#89079=CARTESIAN_POINT ( 'NONE',  ( -84.83620007791539308, -28.93200143582290096, 170.9445379179137490 ) ) ;
#89091=CARTESIAN_POINT ( 'NONE',  ( 105.9102621261374253, -29.99999999999996803, 132.9887338302407898 ) ) ;
#89093=CARTESIAN_POINT ( 'NONE',  ( -94.62342829788488530, -14.21045842199438525, 80.85070941463327188 ) ) ;
#89094=CARTESIAN_POINT ( 'NONE',  ( -61.54080906459579836, -46.44072477553419986, 79.75972302785436341 ) ) ;
#89098=CARTESIAN_POINT ( 'NONE',  ( 94.27018399449993069, -60.00000000003408474, 15.95119456387866563 ) ) ;
#89105=DIRECTION ( 'NONE',  ( 0.000000000000000000, 0.000000000000000000, 1.000000000000000000 ) ) ;
#89109=CARTESIAN_POINT ( 'NONE',  ( -85.86322845308646379, -59.99999999999998579, 200.5221374670101682 ) ) ;
#89118=CARTESIAN_POINT ( 'NONE',  ( 98.58269965288447167, -59.99999999999997158, 196.3309157176815631 ) ) ;
#89119=CARTESIAN_POINT ( 'NONE',  ( -33.64918128699429190, -60.31113787621708155, 38.51426646422538624 ) ) ;
#89122=CARTESIAN_POINT ( 'NONE',  ( 37.92194407314020310, -36.05154521609172491, 36.40098896805632478 ) ) ;
#89123=CARTESIAN_POINT ( 'NONE',  ( 8.569529079650926917, -1.734723475976807094E-15, 14.86825985027943808 ) ) ;
#89126=CARTESIAN_POINT ( 'NONE',  ( -57.80876175898364266, -38.34424999602565975, 89.67284400224633600 ) ) ;
#89138=CARTESIAN_POINT ( 'NONE',  ( 93.33649174705706741, -60.00000000000001421, 35.53938046925307503 ) ) ;
#89144=CARTESIAN_POINT ( 'NONE',  ( -89.88506759848812067, -30.00000000010622259, 28.44306712582588048 ) ) ;
#89148=CARTESIAN_POINT ( 'NONE',  ( 0.000000000000000000, -15.00000000000000000, -8.000000000000000000 ) ) ;
#89159=CARTESIAN_POINT ( 'NONE',  ( 81.28744592092785126, -36.02883678850789551, 150.3977081706462968 ) ) ;
#89167=CARTESIAN_POINT ( 'NONE',  ( -26.05015581842503991, -57.67603816461070920, 43.50693983564572420 ) ) ;
#89180=CARTESIAN_POINT ( 'NONE',  ( -31.39072542170150015, -22.34702334173443816, 32.41690302228272458 ) ) ;
#89193=CARTESIAN_POINT ( 'NONE',  ( -59.29073024543932036, -37.24633815747250765, -34.34540174141172741 ) ) ;
#89197=VECTOR ( 'NONE', #48709, 1000.000000000000000 ) ;
#89199=CARTESIAN_POINT ( 'NONE',  ( 91.22868010984630871, -57.61353597378020197, 204.2121190900673184 ) ) ;
#89204=CARTESIAN_POINT ( 'NONE',  ( -72.77643868140833661, -60.00000000000000000, 160.4837882257039041 ) ) ;
#89210=CARTESIAN_POINT ( 'NONE',  ( -85.02917054920756357, -46.57021548746553208, 187.6139099441489577 ) ) ;
#89216=CARTESIAN_POINT ( 'NONE',  ( -83.87577431657142313, -52.72623505988846659, -15.45652431476665889 ) ) ;
#89225=CARTESIAN_POINT ( 'NONE',  ( -2.227375807149027054, -1.734723475976807094E-15, 17.01589776168603407 ) ) ;
#89227=EDGE_CURVE ( 'NONE', #93158, #8148, #23778, .T. ) ;
#89228=CARTESIAN_POINT ( 'NONE',  ( 79.45700042099618088, -60.00000000000000711, -30.99979279722015590 ) ) ;
#89229=CARTESIAN_POINT ( 'NONE',  ( -79.84541195356943888, -22.14834539919765177, 128.4737088173135646 ) ) ;
#89231=CARTESIAN_POINT ( 'NONE',  ( 49.67137106584178241, -60.00000000000004263, 77.31490210218785819 ) ) ;
#89233=CARTESIAN_POINT ( 'NONE',  ( 80.72171367857396262, -57.51083543166566159, 199.5255592465300936 ) ) ;
#89251=CARTESIAN_POINT ( 'NONE',  ( -1.363517047694020823, -14.21045842199434794, 34.36840973699905533 ) ) ;
#89252=CARTESIAN_POINT ( 'NONE',  ( 29.17198231074005577, -39.48311188039721031, 32.84881695570470583 ) ) ;
#89255=B_SPLINE_CURVE_WITH_KNOTS ( 'NONE', 3,
 ( #104284, #77905, #28319, #78420 ),
 .UNSPECIFIED., .F., .F.,
 ( 4, 4 ),
 ( 0.0009108016474575763048, 0.009022848917173635630 ),
 .UNSPECIFIED. ) ;
#89267=CARTESIAN_POINT ( 'NONE',  ( 19.49680244870894441, -59.99999999999999289, -41.87632309024431976 ) ) ;
#89295=CARTESIAN_POINT ( 'NONE',  ( -55.25757206493887708, -60.00000000000000711, 69.43508648390772464 ) ) ;
#89296=CARTESIAN_POINT ( 'NONE',  ( 65.80721811158888102, -22.10268982855930631, 79.50398025642166999 ) ) ;
#89297=EDGE_CURVE ( 'NONE', #84319, #72232, #36144, .T. ) ;
#89302=CARTESIAN_POINT ( 'NONE',  ( -5.647684535521968918, -57.67118449236373579, -44.55142524122563685 ) ) ;
#89309=AXIS2_PLACEMENT_3D ( 'NONE', #68070, #44876, #27121 ) ;
#89315=VERTEX_POINT ( 'NONE', #81957 ) ;
#89318=CARTESIAN_POINT ( 'NONE',  ( 8.537483284794495475, -60.00000000000000000, 39.63655399926129519 ) ) ;
#89319=CARTESIAN_POINT ( 'NONE',  ( -93.75466218594513634, -30.00000000000000355, 191.2470980862353542 ) ) ;
#89324=CARTESIAN_POINT ( 'NONE',  ( 39.85978143129780449, -57.69245178989500999, 55.45386101768630738 ) ) ;
#89329=CARTESIAN_POINT ( 'NONE',  ( 10.14997255787597297, -22.66085254118687331, -38.54259180169733412 ) ) ;
#89332=CARTESIAN_POINT ( 'NONE',  ( -4.079827781214096838, -60.00000000000000000, 39.63120119151885490 ) ) ;
#89337=CARTESIAN_POINT ( 'NONE',  ( -86.39639614912320553, -50.14485074065887460, 191.2668530642233975 ) ) ;
#89341=CARTESIAN_POINT ( 'NONE',  ( -11.48823353272537240, -53.40259021410059859, 32.82079992462674056 ) ) ;
#89353=CARTESIAN_POINT ( 'NONE',  ( 65.96454949761043451, -60.00000000000000000, 122.2396239898068018 ) ) ;
#89359=CARTESIAN_POINT ( 'NONE',  ( 37.54937173058232247, -29.99999999999994671, 45.10736187702755018 ) ) ;
#89375=CARTESIAN_POINT ( 'NONE',  ( -96.27974869280906489, -60.00000000000978417, 205.0145893238625092 ) ) ;
#89377=CARTESIAN_POINT ( 'NONE',  ( 75.01455921003739036, -59.99999999999997868, 181.4220384249936444 ) ) ;
#89380=CARTESIAN_POINT ( 'NONE',  ( -104.4188068117427264, -29.99999999999997868, 196.2181340123987923 ) ) ;
#89381=CARTESIAN_POINT ( 'NONE',  ( 17.60034620493656377, -25.55031154538487215, 28.43495793658222581 ) ) ;
#89383=CARTESIAN_POINT ( 'NONE',  ( 83.27655652115849705, -38.00000000000000711, -5.287797665593598317 ) ) ;
#89385=CARTESIAN_POINT ( 'NONE',  ( -44.69002865036945593, -36.07507680361931079, 42.37332714719177318 ) ) ;
#89398=CARTESIAN_POINT ( 'NONE',  ( 96.49954056570551586, -29.99999999997318767, 199.8705361785111450 ) ) ;
#89401=CARTESIAN_POINT ( 'NONE',  ( 100.2850625226886621, -30.00000000000001066, 156.5047868331033385 ) ) ;
#89406=ORIENTED_EDGE ( 'NONE', *, *, #40555, .F. ) ;
#89418=CARTESIAN_POINT ( 'NONE',  ( 83.66693253132321217, -38.78100776230738234, 197.5407986867839725 ) ) ;
#89420=CARTESIAN_POINT ( 'NONE',  ( 86.80186013151742941, -38.00000000000003553, 188.4282799762682998 ) ) ;
#89430=( LENGTH_UNIT ( ) NAMED_UNIT ( * ) SI_UNIT ( .MILLI., .METRE. ) );
#89435=CARTESIAN_POINT ( 'NONE',  ( -6.118049227779695620, -18.82936832617644640, 35.12770106459590380 ) ) ;
#89439=( BOUNDED_SURFACE ( )  B_SPLINE_SURFACE ( 2, 3, ( 
 ( #78266, #59992, #86389, #44314, #82780, #100946, #77208, #28698, #2776, #93404, #69656, #43776, #85857, #35726, #12456, #52390, #10856, #85302, #94470, #36267, #8882, #102547, #11388, #35184, #41787, #92852, #45385, #61042, #52931, #101489, #19018, #74669, #4378, #37318, #70180, #93929, #11930, #25101, #3320, #57957, #27641, #69134, #90882, #28166, #16997, #49874, #51859, #22720, #23240, #30270, #4919, #55558, #14572, #38367, #88494, #30813, #96055, #47478, #31347, #95517, #37851, #71231, #80376, #70714, #103604, #71752, #95007, #12982, #56078, #96586, #63159, #22183, #64227, #7022, #97099, #62117, #104661, #6488, #38883, #72294, #79326, #39419, #55034, #79850, #29755, #53973, #105201, #63699, #89020, #62629, #87966, #104127, #48003, #14046, #15116, #46950, #5959, #78786, #21658, #80911, #39939, #103086, #29236, #21142, #86912, #45910, #54494, #87439, #13516, #46436, #5445, #64740, #7542, #90608, #56629, #33452, #24831, #65268, #99210, #57160, #72810, #16717, #97616, #89550, #83046, #82513, #8086, #40991, #91159, #1019, #17265, #31860, #49606, #66327, #57685, #25374 ),
 ( #81428, #23781, #8616, #41519, #74406, #48537, #73880, #49065, #42049, #106775, #483, #81960, #98677, #15646, #40458, #9138, #74933, #32926, #65800, #58230, #50138, #105717, #24313, #90072, #16179, #73338, #106236, #32395, #98158, #2367, #78391, #76261, #76790, #20212, #29353, #69263, #77872, #35312, #86520, #68176, #4507, #37444, #69782, #62245, #20753, #27770, #70313, #2895, #53066, #102674, #85985, #101072, #10985, #53591, #12057, #95129, #10458, #45517, #44986, #94605, #61713, #27232, #36913, #12583, #44444, #51981, #103208, #60645, #92983, #68731, #21261, #11514, #54098, #60118, #43377, #77338, #19144, #52516, #84898, #28836, #43902, #85432, #35855, #102135, #3449, #101615, #93531, #19677, #36396, #3984, #28289, #61164, #94050, #7145, #78920, #54619, #89144, #64860, #48132, #55160, #14701, #5562, #5044, #72421, #38491, #97743, #104251, #23368, #95650, #79451, #96185, #47073, #80497, #39008, #31468, #30399, #22845, #105842, #96708, #46557, #104791, #23910, #79973, #6618, #6090, #87042, #87561, #37978, #81029, #46037, #71352, #55678, #31986, #71887, #47602, #70839 ),
 ( #39544, #13110, #97220, #63285, #40057, #22314, #88611, #105325, #64351, #103731, #13644, #56206, #15245, #29877, #62754, #72934, #21785, #88089, #14169, #30940, #63818, #67001, #90737, #98288, #34127, #74004, #32526, #8212, #1706, #57814, #1154, #81543, #17925, #16853, #40584, #98805, #15776, #75061, #58910, #24960, #50777, #8742, #49734, #7666, #83169, #24446, #90202, #25506, #41650, #73466, #99882, #83690, #48659, #57279, #91804, #34661, #9796, #82641, #91284, #82093, #106361, #42174, #41121, #67533, #87, #26054, #65396, #74536, #16302, #613, #49193, #17392, #33056, #33576, #100413, #56750, #89678, #65926, #42712, #66455, #99331, #75607, #58363, #50267, #9267, #28164, #44857, #76133, #20085, #92313, #11386, #2233, #101487, #27102, #27638, #60517, #61577, #35182, #52388, #4376, #70178, #37316, #92850, #77746, #10854, #77206, #69654, #19551, #93402, #26578, #61040, #3857, #68048, #52929, #18464, #44312, #100944, #85300, #59990, #3318, #36263, #94468, #19015, #35724, #69132, #85855, #102005, #36788, #76662, #93927, #45383, #11928, #51857, #102545, #59446, #28696 ) ),
 .UNSPECIFIED., .F., .F., .F. ) 
 B_SPLINE_SURFACE_WITH_KNOTS ( ( 3, 3 ),
 ( 4, 2, 2, 2, 2, 2, 2, 2, 2, 2, 2, 2, 2, 2, 2, 2, 2, 2, 2, 2, 2, 2, 2, 2, 2, 2, 2, 2, 2, 2, 2, 2, 2, 2, 2, 2, 2, 2, 2, 2, 2, 2, 2, 2, 2, 2, 2, 2, 2, 2, 2, 2, 2, 2, 2, 2, 2, 2, 2, 2, 2, 2, 2, 2, 2, 2, 2, 4 ),
 ( 0.000000000000000000, 1.000000000000000000 ),
 ( 0.000000000000000000, 0.01154064568618346810, 0.02308129137236693620, 0.03462193705855040604, 0.04616258274473387241, 0.06924387411710081208, 0.09232516548946774482, 0.1038658111756512181, 0.1154064568618346776, 0.1211767797049264211, 0.1269471025480181647, 0.1327174253911098945, 0.1356025868126557454, 0.1384877482342016242, 0.1399303289449745635, 0.1413729096557475029, 0.1420942000111339587, 0.1428154903665204145, 0.1431761355442136563, 0.1435367807219068981, 0.1442580710772933539, 0.1457006517880662932, 0.1464219421434527491, 0.1471432324988392049, 0.1485858132096121442, 0.1493071035649986000, 0.1500283939203850836, 0.1503890390980783254, 0.1507496842757715672, 0.1509300068646181880, 0.1511103294534648089, 0.1512004907478881055, 0.1512906520423114021, 0.1514709746311580230, 0.1518316198088512370, 0.1521922649865444788, 0.1529135553419309623, 0.1543561360527038739, 0.1557987167634768133, 0.1586838781850226643, 0.1615690396065685430, 0.1673393624496602727, 0.1731096852927520025, 0.1846503309789354896, 0.2077316223513024362, 0.2308129137236693551, 0.2769754964684032483, 0.3000567878407701672, 0.3231380792131370860, 0.3346787248993205455, 0.3404490477424122474, 0.3462193705855040049, 0.3491045320070498836, 0.3519896934285957624, 0.3534322741393687295, 0.3548748548501416411, 0.3563174355609145527, 0.3570387259163010363, 0.3573993710939942781, 0.3577600162716875198, 0.3581206614493807616, 0.3584813066270740034, 0.3592025969824604870, 0.3606451776932333986, 0.3620877584040063102, 0.3635303391147792773, 0.3664155005363251005, 0.3693006619578709793 ),
 .UNSPECIFIED. ) 
 GEOMETRIC_REPRESENTATION_ITEM ( )  RATIONAL_B_SPLINE_SURFACE ( (
 ( 1.000000000000000000, 1.000000000000000000, 1.000000000000000000, 1.000000000000000000, 1.000000000000000000, 1.000000000000000000, 1.000000000000000000, 1.000000000000000000, 1.000000000000000000, 1.000000000000000000, 1.000000000000000000, 1.000000000000000000, 1.000000000000000000, 1.000000000000000000, 1.000000000000000000, 1.000000000000000000, 1.000000000000000000, 1.000000000000000000, 1.000000000000000000, 1.000000000000000000, 1.000000000000000000, 1.000000000000000000, 1.000000000000000000, 1.000000000000000000, 1.000000000000000000, 1.000000000000000000, 1.000000000000000000, 1.000000000000000000, 1.000000000000000000, 1.000000000000000000, 1.000000000000000000, 1.000000000000000000, 1.000000000000000000, 1.000000000000000000, 1.000000000000000000, 1.000000000000000000, 1.000000000000000000, 1.000000000000000000, 1.000000000000000000, 1.000000000000000000, 1.000000000000000000, 1.000000000000000000, 1.000000000000000000, 1.000000000000000000, 1.000000000000000000, 1.000000000000000000, 1.000000000000000000, 1.000000000000000000, 1.000000000000000000, 1.000000000000000000, 1.000000000000000000, 1.000000000000000000, 1.000000000000000000, 1.000000000000000000, 1.000000000000000000, 1.000000000000000000, 1.000000000000000000, 1.000000000000000000, 1.000000000000000000, 1.000000000000000000, 1.000000000000000000, 1.000000000000000000, 1.000000000000000000, 1.000000000000000000, 1.000000000000000000, 1.000000000000000000, 1.000000000000000000, 1.000000000000000000, 1.000000000000000000, 1.000000000000000000, 1.000000000000000000, 1.000000000000000000, 1.000000000000000000, 1.000000000000000000, 1.000000000000000000, 1.000000000000000000, 1.000000000000000000, 1.000000000000000000, 1.000000000000000000, 1.000000000000000000, 1.000000000000000000, 1.000000000000000000, 1.000000000000000000, 1.000000000000000000, 1.000000000000000000, 1.000000000000000000, 1.000000000000000000, 1.000000000000000000, 1.000000000000000000, 1.000000000000000000, 1.000000000000000000, 1.000000000000000000, 1.000000000000000000, 1.000000000000000000, 1.000000000000000000, 1.000000000000000000, 1.000000000000000000, 1.000000000000000000, 1.000000000000000000, 1.000000000000000000, 1.000000000000000000, 1.000000000000000000, 1.000000000000000000, 1.000000000000000000, 1.000000000000000000, 1.000000000000000000, 1.000000000000000000, 1.000000000000000000, 1.000000000000000000, 1.000000000000000000, 1.000000000000000000, 1.000000000000000000, 1.000000000000000000, 1.000000000000000000, 1.000000000000000000, 1.000000000000000000, 1.000000000000000000, 1.000000000000000000, 1.000000000000000000, 1.000000000000000000, 1.000000000000000000, 1.000000000000000000, 1.000000000000000000, 1.000000000000000000, 1.000000000000000000, 1.000000000000000000, 1.000000000000000000, 1.000000000000000000, 1.000000000000000000, 1.000000000000000000, 1.000000000000000000, 1.000000000000000000, 1.000000000000000000, 1.000000000000000000, 1.000000000000000000, 1.000000000000000000),
 ( 1.857142857142858317, 1.857142857142858317, 1.857142857142858317, 1.857142857142858317, 1.857142857142858317, 1.857142857142858317, 1.857142857142858317, 1.857142857142858317, 1.857142857142858317, 1.857142857142858317, 1.857142857142858317, 1.857142857142858317, 1.857142857142858317, 1.857142857142858317, 1.857142857142858317, 1.857142857142858317, 1.857142857142858317, 1.857142857142858317, 1.857142857142858317, 1.857142857142858317, 1.857142857142858317, 1.857142857142858317, 1.857142857142858317, 1.857142857142858317, 1.857142857142858317, 1.857142857142858317, 1.857142857142858317, 1.857142857142858317, 1.857142857142858317, 1.857142857142858317, 1.857142857142858317, 1.857142857142858317, 1.857142857142858317, 1.857142857142858317, 1.857142857142858317, 1.857142857142858317, 1.857142857142858317, 1.857142857142858317, 1.857142857142858317, 1.857142857142858317, 1.857142857142858317, 1.857142857142858317, 1.857142857142858317, 1.857142857142858317, 1.857142857142858317, 1.857142857142858317, 1.857142857142858317, 1.857142857142858317, 1.857142857142858317, 1.857142857142858317, 1.857142857142858317, 1.857142857142858317, 1.857142857142858317, 1.857142857142858317, 1.857142857142858317, 1.857142857142858317, 1.857142857142858317, 1.857142857142858317, 1.857142857142858317, 1.857142857142858317, 1.857142857142858317, 1.857142857142858317, 1.857142857142858317, 1.857142857142858317, 1.857142857142858317, 1.857142857142858317, 1.857142857142858317, 1.857142857142858317, 1.857142857142858317, 1.857142857142858317, 1.857142857142858317, 1.857142857142858317, 1.857142857142858317, 1.857142857142858317, 1.857142857142858317, 1.857142857142858317, 1.857142857142858317, 1.857142857142858317, 1.857142857142858317, 1.857142857142858317, 1.857142857142858317, 1.857142857142858317, 1.857142857142858317, 1.857142857142858317, 1.857142857142858317, 1.857142857142858317, 1.857142857142858317, 1.857142857142858317, 1.857142857142858317, 1.857142857142858317, 1.857142857142858317, 1.857142857142858317, 1.857142857142858317, 1.857142857142858317, 1.857142857142858317, 1.857142857142858317, 1.857142857142859205, 1.857142857142859205, 1.857142857142857428, 1.857142857142857428, 1.857142857142855430, 1.857142857142855430, 1.857142857142858317, 1.857142857142858317, 1.857142857142858317, 1.857142857142858317, 1.857142857142858317, 1.857142857142858317, 1.857142857142858317, 1.857142857142858317, 1.857142857142858317, 1.857142857142858317, 1.857142857142858317, 1.857142857142858317, 1.857142857142858317, 1.857142857142858317, 1.857142857142860981, 1.857142857142860981, 1.857142857142858317, 1.857142857142858317, 1.857142857142858317, 1.857142857142858317, 1.857142857142858317, 1.857142857142858317, 1.857142857142858317, 1.857142857142858317, 1.857142857142858317, 1.857142857142858317, 1.857142857142858317, 1.857142857142858317, 1.857142857142858317, 1.857142857142858317, 1.857142857142858317, 1.857142857142858317, 1.857142857142858317, 1.857142857142858317),
 ( 1.000000000000000000, 1.000000000000000000, 1.000000000000000000, 1.000000000000000000, 1.000000000000000000, 1.000000000000000000, 1.000000000000000000, 1.000000000000000000, 1.000000000000000000, 1.000000000000000000, 1.000000000000000000, 1.000000000000000000, 1.000000000000000000, 1.000000000000000000, 1.000000000000000000, 1.000000000000000000, 1.000000000000000000, 1.000000000000000000, 1.000000000000000000, 1.000000000000000000, 1.000000000000000000, 1.000000000000000000, 1.000000000000000000, 1.000000000000000000, 1.000000000000000000, 1.000000000000000000, 1.000000000000000000, 1.000000000000000000, 1.000000000000000000, 1.000000000000000000, 1.000000000000000000, 1.000000000000000000, 1.000000000000000000, 1.000000000000000000, 1.000000000000000000, 1.000000000000000000, 1.000000000000000000, 1.000000000000000000, 1.000000000000000000, 1.000000000000000000, 1.000000000000000000, 1.000000000000000000, 1.000000000000000000, 1.000000000000000000, 1.000000000000000000, 1.000000000000000000, 1.000000000000000000, 1.000000000000000000, 1.000000000000000000, 1.000000000000000000, 1.000000000000000000, 1.000000000000000000, 1.000000000000000000, 1.000000000000000000, 1.000000000000000000, 1.000000000000000000, 1.000000000000000000, 1.000000000000000000, 1.000000000000000000, 1.000000000000000000, 1.000000000000000000, 1.000000000000000000, 1.000000000000000000, 1.000000000000000000, 1.000000000000000000, 1.000000000000000000, 1.000000000000000000, 1.000000000000000000, 1.000000000000000000, 1.000000000000000000, 1.000000000000000000, 1.000000000000000000, 1.000000000000000000, 1.000000000000000000, 1.000000000000000000, 1.000000000000000000, 1.000000000000000000, 1.000000000000000000, 1.000000000000000000, 1.000000000000000000, 1.000000000000000000, 1.000000000000000000, 1.000000000000000000, 1.000000000000000000, 1.000000000000000000, 1.000000000000000000, 1.000000000000000000, 1.000000000000000000, 1.000000000000000000, 1.000000000000000000, 1.000000000000000000, 1.000000000000000000, 1.000000000000000000, 1.000000000000000000, 1.000000000000000000, 1.000000000000000000, 1.000000000000000000, 1.000000000000000000, 1.000000000000000000, 1.000000000000000000, 1.000000000000000000, 1.000000000000000000, 1.000000000000000000, 1.000000000000000000, 1.000000000000000000, 1.000000000000000000, 1.000000000000000000, 1.000000000000000000, 1.000000000000000000, 1.000000000000000000, 1.000000000000000000, 1.000000000000000000, 1.000000000000000000, 1.000000000000000000, 1.000000000000000000, 1.000000000000000000, 1.000000000000000000, 1.000000000000000000, 1.000000000000000000, 1.000000000000000000, 1.000000000000000000, 1.000000000000000000, 1.000000000000000000, 1.000000000000000000, 1.000000000000000000, 1.000000000000000000, 1.000000000000000000, 1.000000000000000000, 1.000000000000000000, 1.000000000000000000, 1.000000000000000000, 1.000000000000000000, 1.000000000000000000, 1.000000000000000000, 1.000000000000000000, 1.000000000000000000) ) ) 
 REPRESENTATION_ITEM ( '' )  SURFACE ( )  );
#89441=CARTESIAN_POINT ( 'NONE',  ( 85.78618341410623316, -28.50839767291424565, 180.2823363360693918 ) ) ;
#89445=CARTESIAN_POINT ( 'NONE',  ( 95.27829797562213798, -57.67182506141622866, 35.15692822873978685 ) ) ;
#89463=CARTESIAN_POINT ( 'NONE',  ( -102.0620737423919593, -38.00000000000000711, 183.9277168086509846 ) ) ;
#89467=CARTESIAN_POINT ( 'NONE',  ( -6.557141181177008171, -15.75010798306612081, -35.04602174276683257 ) ) ;
#89469=CARTESIAN_POINT ( 'NONE',  ( -56.97006370568202982, -21.76999005371631313, -23.90107951094816485 ) ) ;
#89477=CARTESIAN_POINT ( 'NONE',  ( -92.65990761677430498, -60.00000000000002132, -3.893849931707503043 ) ) ;
#89481=CARTESIAN_POINT ( 'NONE',  ( 97.77191385463773088, -60.34768693918523041, 196.6186543819742383 ) ) ;
#89485=CARTESIAN_POINT ( 'NONE',  ( -84.31906800682108383, -22.12972036364938333, 154.7647679128914433 ) ) ;
#89495=CARTESIAN_POINT ( 'NONE',  ( -103.1324900820093262, -57.63586870064128931, 202.7914362107620434 ) ) ;
#89501=CARTESIAN_POINT ( 'NONE',  ( -34.13564290404001156, -60.00000000000002132, -42.84076297484070039 ) ) ;
#89503=CARTESIAN_POINT ( 'NONE',  ( -52.60481344042765528, -60.31495398866518087, 63.32391407137016870 ) ) ;
#89507=CARTESIAN_POINT ( 'NONE',  ( -99.46713752920656759, -52.77532478499336577, 194.5109139038963235 ) ) ;
#89512=CARTESIAN_POINT ( 'NONE',  ( 98.76629783378818672, -38.35591045133333665, 81.67967853887255103 ) ) ;
#89518=CARTESIAN_POINT ( 'NONE',  ( 85.25533141069878695, -30.00000000000000355, 172.6891169115829996 ) ) ;
#89526=CARTESIAN_POINT ( 'NONE',  ( 50.43109628883428286, -53.36716467480742665, 56.24163232349562946 ) ) ;
#89533=CARTESIAN_POINT ( 'NONE',  ( -91.98980923544721122, -38.35482474950386944, 34.70844003865646954 ) ) ;
#89536=CARTESIAN_POINT ( 'NONE',  ( 92.03920658769411034, -38.35407107957195905, 35.11563712653246228 ) ) ;
#89538=CARTESIAN_POINT ( 'NONE',  ( 101.1120282019177239, -52.71709064890642082, 130.0501827644169452 ) ) ;
#89541=CARTESIAN_POINT ( 'NONE',  ( 80.42679257503434087, -59.99999999999999289, 196.4953341280405539 ) ) ;
#89545=CARTESIAN_POINT ( 'NONE',  ( 56.34713570575822672, -25.61535964347525152, 57.53183839505768304 ) ) ;
#89550=CARTESIAN_POINT ( 'NONE',  ( -88.28902640317532757, -38.37280356866271092, -19.18740266668778460 ) ) ;
#89560=CARTESIAN_POINT ( 'NONE',  ( 85.20513743252166705, -25.43210005301644472, 169.0098029066481331 ) ) ;
#89580=CARTESIAN_POINT ( 'NONE',  ( -22.57777066253796505, -27.40074420488135942, 37.49751158013248897 ) ) ;
#89602=CARTESIAN_POINT ( 'NONE',  ( -112.2163655317416868, -59.99999999999998579, 171.0452993802184096 ) ) ;
#89610=CARTESIAN_POINT ( 'NONE',  ( -81.66238495618624427, -57.04855356713849091, 183.2407446992486086 ) ) ;
#89623=CARTESIAN_POINT ( 'NONE',  ( 114.4521715241705664, -60.00000000000002842, 166.3966616003652348 ) ) ;
#89624=CARTESIAN_POINT ( 'NONE',  ( -108.8241353627135055, -30.00000000000001421, 157.0475095860343515 ) ) ;
#89625=CARTESIAN_POINT ( 'NONE',  ( -62.49919243722554540, -18.63627675925726734, 68.78216434012247760 ) ) ;
#89628=CARTESIAN_POINT ( 'NONE',  ( 112.7800843278198073, -59.99999999999997158, 146.3612206852396014 ) ) ;
#89630=CARTESIAN_POINT ( 'NONE',  ( 2.033923692053578591, -49.91572940536237013, 32.20638245996861571 ) ) ;
#89638=CARTESIAN_POINT ( 'NONE',  ( -91.91408097602798932, -60.00000000000000000, 202.3452444908770929 ) ) ;
#89641=AXIS2_PLACEMENT_3D ( 'NONE', #62890, #46687, #62365 ) ;
#89648=CARTESIAN_POINT ( 'NONE',  ( 86.71109173531407066, -60.00000000000004974, -11.42213278536460486 ) ) ;
#89649=CARTESIAN_POINT ( 'NONE',  ( -31.31696575628595269, -22.13776733473083169, 30.43610477315223406 ) ) ;
#89653=CARTESIAN_POINT ( 'NONE',  ( 39.81835848735108385, -53.34354282573661976, 41.56692554013707763 ) ) ;
#89660=CARTESIAN_POINT ( 'NONE',  ( -59.09117307917458106, -38.34357130299601835, 93.55555875830225432 ) ) ;
#89672=CARTESIAN_POINT ( 'NONE',  ( 100.7785506732187883, -59.99999999999999289, 85.60081394660342369 ) ) ;
#89678=CARTESIAN_POINT ( 'NONE',  ( -99.67836086284214048, -30.00000000000002132, 186.8797784846947252 ) ) ;
#89692=CARTESIAN_POINT ( 'NONE',  ( 83.58678869323294691, -18.68415770015456090, 145.1632175728272784 ) ) ;
#89700=CARTESIAN_POINT ( 'NONE',  ( -69.72050231116651275, -57.68271840123205862, 152.1212729744891590 ) ) ;
#89713=CARTESIAN_POINT ( 'NONE',  ( -33.70810140226702600, -23.45504108715438107, 33.05596252965560211 ) ) ;
#89732=CARTESIAN_POINT ( 'NONE',  ( 106.6191002599640143, -57.65239554408994138, 200.4187991428152600 ) ) ;
#89739=CARTESIAN_POINT ( 'NONE',  ( -74.01186676100478223, -60.00000000000000000, 172.3432513155285619 ) ) ;
#89743=CARTESIAN_POINT ( 'NONE',  ( -85.91487385093410012, -32.00067969521617783, 183.3906813362126798 ) ) ;
#89749=CARTESIAN_POINT ( 'NONE',  ( -87.01158373004948032, -60.18652252783364531, -5.598645846854314101 ) ) ;
#89757=CARTESIAN_POINT ( 'NONE',  ( 22.23822744035697241, -8.673617379884035472E-16, -2.910977163136222678 ) ) ;
#89759=CARTESIAN_POINT ( 'NONE',  ( 47.46761990717632784, -14.21045842199427511, -33.06011575854734730 ) ) ;
#89761=CARTESIAN_POINT ( 'NONE',  ( -80.60696305975868370, -18.68079635666938643, 129.0832030291728927 ) ) ;
#89763=CARTESIAN_POINT ( 'NONE',  ( 52.56736687853028656, -59.99999999999993605, 85.36620364727897936 ) ) ;
#89765=CARTESIAN_POINT ( 'NONE',  ( 88.05830098754434232, -57.66964593057830513, -24.45951718257569496 ) ) ;
#89779=CARTESIAN_POINT ( 'NONE',  ( -8.555246586836847911, -60.00000000000005684, 41.98716887921269603 ) ) ;
#89780=CARTESIAN_POINT ( 'NONE',  ( 29.78856322856827177, -39.48450492069009954, 33.06000570913132464 ) ) ;
#89794=CARTESIAN_POINT ( 'NONE',  ( 8.249451541537798249, -60.00000000000000000, -42.48302917854579164 ) ) ;
#89821=CARTESIAN_POINT ( 'NONE',  ( -38.04320146006180181, -60.00000000000000711, 41.36025795104787051 ) ) ;
#89822=CARTESIAN_POINT ( 'NONE',  ( 65.58602450514189286, -25.57852054671029762, 80.66737998054381364 ) ) ;
#89826=CARTESIAN_POINT ( 'NONE',  ( -28.02803974396783815, -57.67115643259209889, -43.15031372974605972 ) ) ;
#89834=CIRCLE ( 'NONE', #62289, 74.46152422706630603 ) ;
#89845=CARTESIAN_POINT ( 'NONE',  ( 12.16851236901548461, -60.00000000000000000, 39.68953834586075402 ) ) ;
#89846=CARTESIAN_POINT ( 'NONE',  ( -96.88846608153241391, -29.99999999999999289, 191.1171794686087537 ) ) ;
#89849=CARTESIAN_POINT ( 'NONE',  ( 46.38270258108293120, -57.68171275033647305, 68.22110787291272516 ) ) ;
#89852=CARTESIAN_POINT ( 'NONE',  ( 14.73658302030201916, -23.99622960207933176, -38.53156179264232151 ) ) ;
#89853=CARTESIAN_POINT ( 'NONE',  ( -21.12363372865564770, -60.00000000000000000, 40.37864402363731386 ) ) ;
#89857=CARTESIAN_POINT ( 'NONE',  ( -86.95901752989097133, -39.09618168350279177, 189.0029776537705004 ) ) ;
#89859=VERTEX_POINT ( 'NONE', #82915 ) ;
#89862=CARTESIAN_POINT ( 'NONE',  ( -10.30264850706973334, -42.95776240863717277, 31.06144808585462158 ) ) ;
#89876=CARTESIAN_POINT ( 'NONE',  ( 73.51917576782351205, -60.00000000000002132, 167.3794919118397502 ) ) ;
#89893=CARTESIAN_POINT ( 'NONE',  ( -46.26700095126739853, -60.00000000001953282, 68.87414247443797422 ) ) ;
#89895=CARTESIAN_POINT ( 'NONE',  ( 80.47396527936437849, -59.99999999999998579, 196.5700788117762272 ) ) ;
#89897=CARTESIAN_POINT ( 'NONE',  ( -106.9542266815933829, -14.21045842199434084, 174.0135369018153995 ) ) ;
#89898=CARTESIAN_POINT ( 'NONE',  ( 14.88179425905683040, -60.35850697746405302, 34.08740321138691343 ) ) ;
#89900=CARTESIAN_POINT ( 'NONE',  ( 82.51400834001795204, -38.00000000000000000, 7.859624698400971887 ) ) ;
#89902=CARTESIAN_POINT ( 'NONE',  ( -45.40034815561197235, -29.15988752944468132, 41.32649748755925856 ) ) ;
#89915=CARTESIAN_POINT ( 'NONE',  ( 55.77201978694041884, -30.00000000000000000, 79.48271800460260295 ) ) ;
#89920=CARTESIAN_POINT ( 'NONE',  ( 97.88837943941081221, -30.00000000000000000, 136.7472917770585070 ) ) ;
#89934=CARTESIAN_POINT ( 'NONE',  ( 81.59556071043041925, -38.84188875790712103, 195.3954600456527260 ) ) ;
#89952=CARTESIAN_POINT ( 'NONE',  ( -11.19867756180316576, -20.63762499452760579, 35.45502084197963200 ) ) ;
#89959=CARTESIAN_POINT ( 'NONE',  ( 86.22304159983994509, -21.27469319544424664, 177.9707522126931565 ) ) ;
#89964=CARTESIAN_POINT ( 'NONE',  ( 91.18366750016291178, -57.66344145994273873, -20.65528270058285543 ) ) ;
#89968=CARTESIAN_POINT ( 'NONE',  ( -80.85862215050043744, -29.99999999999999645, 6.799607089790798753 ) ) ;
#89972=CARTESIAN_POINT ( 'NONE',  ( -77.67718612014897417, -38.00000000000005684, 131.3029103090800049 ) ) ;
#89982=CARTESIAN_POINT ( 'NONE',  ( -100.3203616992955602, -38.00000000000001421, 190.0301232681506178 ) ) ;
#89987=CARTESIAN_POINT ( 'NONE',  ( -32.71804766712359935, -22.58455031971449500, -31.71287671542873809 ) ) ;
#89990=CARTESIAN_POINT ( 'NONE',  ( -53.90259159284356372, -47.40884937127464127, -29.08431734911702193 ) ) ;
#89997=CARTESIAN_POINT ( 'NONE',  ( -49.90941830484705832, -60.00000000000000711, -37.92245557729972205 ) ) ;
#90000=CARTESIAN_POINT ( 'NONE',  ( 51.09436811768170372, -36.01308660601653600, -27.73089587904936693 ) ) ;
#90002=CARTESIAN_POINT ( 'NONE',  ( 97.64984543025403241, -37.74050600311834103, 192.6344482948218513 ) ) ;
#90015=DIRECTION ( 'NONE',  ( 0.000000000000000000, 1.000000000000000000, 0.000000000000000000 ) ) ;
#90017=CARTESIAN_POINT ( 'NONE',  ( -44.31189620312834876, -57.68384900168454976, 63.67342368891909388 ) ) ;
#90022=CARTESIAN_POINT ( 'NONE',  ( -71.63495682827519317, -59.99999999999997868, -34.46936934826943855 ) ) ;
#90024=CARTESIAN_POINT ( 'NONE',  ( -51.98423175508690974, -36.04436685186517053, 52.98251616644076023 ) ) ;
#90028=CARTESIAN_POINT ( 'NONE',  ( -98.77881222975014452, -45.25002549436672439, 193.4356104138574608 ) ) ;
#90032=CARTESIAN_POINT ( 'NONE',  ( 90.65106265292511978, -38.40367301679646772, -14.05939008884039687 ) ) ;
#90036=CARTESIAN_POINT ( 'NONE',  ( 83.83835625336350006, -30.00000000000001066, 159.6014582805543114 ) ) ;
#90043=ORIENTED_EDGE ( 'NONE', *, *, #100975, .T. ) ;
#90045=CARTESIAN_POINT ( 'NONE',  ( 50.66589989479253830, -18.73013578598424544, 44.89221390001991807 ) ) ;
#90052=CARTESIAN_POINT ( 'NONE',  ( -99.13475156731828974, -38.35568229781205218, 83.36745941595933118 ) ) ;
#90055=CARTESIAN_POINT ( 'NONE',  ( 90.93190340128646199, -38.35213422126950888, 22.02682049786888996 ) ) ;
#90058=CARTESIAN_POINT ( 'NONE',  ( 98.39798496753780910, -60.15124137177372887, 105.6244202628760291 ) ) ;
#90064=CARTESIAN_POINT ( 'NONE',  ( 75.57301170064098983, -60.00000000000000711, 184.8856015330856906 ) ) ;
#90067=CARTESIAN_POINT ( 'NONE',  ( 58.13224282022872558, -25.60471780380888163, 61.38686201737864678 ) ) ;
#90072=CARTESIAN_POINT ( 'NONE',  ( -78.09727535895957828, -30.00000000009066170, 183.0935977092201483 ) ) ;
#90084=CARTESIAN_POINT ( 'NONE',  ( 81.58455456068359979, -57.02865422085555025, 182.7966820730144377 ) ) ;
#90100=CARTESIAN_POINT ( 'NONE',  ( -9.350002378314655971, -19.95346413354524628, 35.32894845137520434 ) ) ;
#90105=ORIENTED_EDGE ( 'NONE', *, *, #32326, .F. ) ;
#90113=CARTESIAN_POINT ( 'NONE',  ( 2.499999999999973799, -24.66556253578214708, -30.98417860745333741 ) ) ;
#90125=CARTESIAN_POINT ( 'NONE',  ( -98.42509890393606042, -59.99999999999997868, 71.54236955077431048 ) ) ;
#90132=CARTESIAN_POINT ( 'NONE',  ( -84.52672161841623222, -32.42574458993667719, 173.3582839768502311 ) ) ;
#90147=CARTESIAN_POINT ( 'NONE',  ( 107.0562500300223974, -29.99999999999996803, 141.2193814890308374 ) ) ;
#90148=CARTESIAN_POINT ( 'NONE',  ( -110.6385074381434066, -60.00000000000007816, 195.8055798097608147 ) ) ;
#90149=CARTESIAN_POINT ( 'NONE',  ( -62.81242157416450311, -25.58369064279834504, 72.96567011718758522 ) ) ;
#90152=CARTESIAN_POINT ( 'NONE',  ( 94.28611985541716933, -59.99999999997079669, 7.686723608328764890 ) ) ;
#90163=CARTESIAN_POINT ( 'NONE',  ( -111.9086460000415144, -59.99999999999997158, 180.9596613643843455 ) ) ;
#90175=CARTESIAN_POINT ( 'NONE',  ( 106.4219938862113821, -60.00000000000001421, 168.4123002066837955 ) ) ;
#90176=CARTESIAN_POINT ( 'NONE',  ( -32.29403280988383784, -29.08578870323540499, 32.09562443352605499 ) ) ;
#90179=CARTESIAN_POINT ( 'NONE',  ( 38.96479555484809509, -56.80366364879377272, 41.53497084807919748 ) ) ;
#90184=CARTESIAN_POINT ( 'NONE',  ( -84.12347576869696297, -38.75549085414967010, 197.8715174774602588 ) ) ;
#90195=CARTESIAN_POINT ( 'NONE',  ( 110.4910188636535935, -59.99999999999997868, 147.4617906836925272 ) ) ;
#90202=CARTESIAN_POINT ( 'NONE',  ( -93.75210457069380254, -29.99999999999987210, 191.2467940272817657 ) ) ;
#90210=ADVANCED_FACE ( 'NONE', ( #106522 ), #96344, .F. ) ;
#90215=CARTESIAN_POINT ( 'NONE',  ( 81.03589328419950277, -42.96753771842250558, 157.4344923703873746 ) ) ;
#90222=CARTESIAN_POINT ( 'NONE',  ( 61.66664358393324363, -59.99999999999998579, -29.25180319347440516 ) ) ;
#90235=CARTESIAN_POINT ( 'NONE',  ( 24.39419124516655657, -28.62692427288619257, 38.06577721013648130 ) ) ;
#90253=CARTESIAN_POINT ( 'NONE',  ( 110.8284296095286408, -57.67014611720160389, 194.4637431536222607 ) ) ;
#90259=CARTESIAN_POINT ( 'NONE',  ( -75.39763943359314169, -59.99999999999999289, 183.8902267106653596 ) ) ;
#90262=CARTESIAN_POINT ( 'NONE',  ( -83.43770954620740099, -60.98761413718671065, 191.4432686340473140 ) ) ;
#90266=EDGE_CURVE ( 'NONE', #32321, #35136, #31535, .T. ) ;
#90272=CARTESIAN_POINT ( 'NONE',  ( -83.09759193211895933, -37.81164733650378196, -2.431872990241325638 ) ) ;
#90278=CARTESIAN_POINT ( 'NONE',  ( 17.01589776168603407, -1.734723475976807094E-15, 2.227375807149028386 ) ) ;
#90280=CARTESIAN_POINT ( 'NONE',  ( -24.89493309229959195, -29.99999999999998934, -38.80368402536839056 ) ) ;
#90281=CARTESIAN_POINT ( 'NONE',  ( -76.96556261419941336, -39.49594249891509889, 129.2692312102975905 ) ) ;
#90283=CARTESIAN_POINT ( 'NONE',  ( 37.39695856105412730, -59.99999999999995737, 52.44754946039245880 ) ) ;
#90285=CARTESIAN_POINT ( 'NONE',  ( 93.86154337525294977, -57.67558731759218205, 9.050589446141858119 ) ) ;
#90302=CARTESIAN_POINT ( 'NONE',  ( -12.83279097724939000, -59.99999999999996447, 42.04727692947117390 ) ) ;
#90303=CARTESIAN_POINT ( 'NONE',  ( 31.08139726357473975, -53.37705209072197476, 36.01296622256593594 ) ) ;
#90313=DIRECTION ( 'NONE',  ( 0.000000000000000000, 0.000000000000000000, 1.000000000000000000 ) ) ;
#90317=CARTESIAN_POINT ( 'NONE',  ( 32.98329542059315855, -60.00000000000001421, -40.55872363790090418 ) ) ;
#90344=CARTESIAN_POINT ( 'NONE',  ( -50.19342719663330143, -60.00000000000001421, 58.08342307450251241 ) ) ;
#90345=CARTESIAN_POINT ( 'NONE',  ( 64.36790054385453175, -39.48203839976437735, 84.34053321678844384 ) ) ;
#90350=CARTESIAN_POINT ( 'NONE',  ( -39.15148982810983824, -57.67118160050520004, -41.75192649668374401 ) ) ;
#90369=CARTESIAN_POINT ( 'NONE',  ( 12.79681648763941304, -60.00000000000000711, 39.70851819966105012 ) ) ;
#90370=CARTESIAN_POINT ( 'NONE',  ( -94.85800629167543718, -30.00000000000000711, 191.3397425934319642 ) ) ;
#90374=CARTESIAN_POINT ( 'NONE',  ( 72.46120011609563960, -57.66624515346453705, 176.5848336718106850 ) ) ;
#90379=CARTESIAN_POINT ( 'NONE',  ( 23.61215506847839407, -27.18552302756052086, -38.41032867837353137 ) ) ;
#90384=CARTESIAN_POINT ( 'NONE',  ( -8.449011944071282088, -59.99999999999999289, 39.63593633568572017 ) ) ;
#90390=CARTESIAN_POINT ( 'NONE',  ( -87.22177126902033706, -35.38517059622223115, 188.6312149666980531 ) ) ;
#90394=CARTESIAN_POINT ( 'NONE',  ( -7.280080666583438997, -60.36582059539835399, 33.94095750819536761 ) ) ;
#90399=CARTESIAN_POINT ( 'NONE',  ( -97.47674776263787066, -60.00000000000000000, 196.6139650356533934 ) ) ;
#90409=CARTESIAN_POINT ( 'NONE',  ( 106.7878191156923293, -14.21045842199435150, 165.8358245669431597 ) ) ;
#90429=CARTESIAN_POINT ( 'NONE',  ( -72.28463938464267358, -59.99999999997559286, 178.7115098145620777 ) ) ;
#90432=CARTESIAN_POINT ( 'NONE',  ( 91.86097484301993177, -60.00000000000001421, 13.21028115448139317 ) ) ;
#90433=CARTESIAN_POINT ( 'NONE',  ( -106.4855387602377732, -14.21045842199444564, 182.1782270149441558 ) ) ;
#90434=CARTESIAN_POINT ( 'NONE',  ( 17.88298539565740342, -39.47322924647534848, 30.78448731433081420 ) ) ;
#90436=CARTESIAN_POINT ( 'NONE',  ( -39.33899073937549673, -42.97721915985697194, 38.92032525959593414 ) ) ;
#90448=CARTESIAN_POINT ( 'NONE',  ( 77.53488771745220731, -30.00000000000000711, -16.24820434784860979 ) ) ;
#90453=CARTESIAN_POINT ( 'NONE',  ( 98.41709237619858186, -30.00000000000000000, 140.5531095731581956 ) ) ;
#90466=CARTESIAN_POINT ( 'NONE',  ( 84.35232594345727364, -38.74306589926045774, 198.0791177174846496 ) ) ;
#90486=( NAMED_UNIT ( * ) PLANE_ANGLE_UNIT ( ) SI_UNIT ( $, .RADIAN. ) );
#90488=CARTESIAN_POINT ( 'NONE',  ( 2.333519804815400889, -18.10848410825153110, 35.01514424201566555 ) ) ;
#90492=CARTESIAN_POINT ( 'NONE',  ( 85.31123991943051976, -46.55852039550524779, 188.2316344986979004 ) ) ;
#90496=CARTESIAN_POINT ( 'NONE',  ( 94.51265451826158426, -57.66905794854115186, -1.775134423264453698 ) ) ;
#90500=CARTESIAN_POINT ( 'NONE',  ( -81.59220867401275257, -30.00000000000000355, -7.144273055932939265 ) ) ;
#90501=CARTESIAN_POINT ( 'NONE',  ( -61.30120358801738689, -38.00000000000001421, 74.93692602774881095 ) ) ;
#90521=CARTESIAN_POINT ( 'NONE',  ( -73.58024007755891205, -60.22810801993039576, -24.87566229692106390 ) ) ;
#90530=CARTESIAN_POINT ( 'NONE',  ( -33.44424537694998634, -59.99999999999999289, -40.50270220663588105 ) ) ;
#90536=CARTESIAN_POINT ( 'NONE',  ( 96.46995715361335044, -52.82112724768406053, 195.4050685382941595 ) ) ;
#90543=VERTEX_POINT ( 'NONE', #8502 ) ;
#90551=CARTESIAN_POINT ( 'NONE',  ( -15.40724846713353813, -57.67135988443339301, 41.78154393163084279 ) ) ;
#90556=CARTESIAN_POINT ( 'NONE',  ( 24.50706706878033359, -14.21045842199442077, -36.19515235953155496 ) ) ;
#90557=CARTESIAN_POINT ( 'NONE',  ( -1.363517047694020823, -14.21045842199434794, 34.36840973699905533 ) ) ;
#90559=CARTESIAN_POINT ( 'NONE',  ( -51.69204177676629541, -60.31069149989181000, 61.32316516767149039 ) ) ;
#90562=CARTESIAN_POINT ( 'NONE',  ( -98.44269825977914934, -37.74221500662412865, 192.2764363897139219 ) ) ;
#90567=CARTESIAN_POINT ( 'NONE',  ( 72.31813523599501536, -38.32585783385900413, 147.7857233425339132 ) ) ;
#90574=CARTESIAN_POINT ( 'NONE',  ( 85.25619601544318016, -29.99999999999999645, 172.6969293775904077 ) ) ;
#90582=CARTESIAN_POINT ( 'NONE',  ( 52.65259415171738766, -46.43731922596889206, 58.09906300711125482 ) ) ;
#90587=CARTESIAN_POINT ( 'NONE',  ( -92.83006309950484081, -38.35493895758955318, 42.01425766727841449 ) ) ;
#90590=CARTESIAN_POINT ( 'NONE',  ( 90.85051015719332668, -38.35148808657510955, 20.42926060149419243 ) ) ;
#90592=CARTESIAN_POINT ( 'NONE',  ( 96.80527538515720209, -45.28275837559359474, 111.1125581287882227 ) ) ;
#90593=DIRECTION ( 'NONE',  ( 0.000000000000000000, -0.000000000000000000, 1.000000000000000000 ) ) ;
#90597=CARTESIAN_POINT ( 'NONE',  ( 74.84954895605289948, -60.00000000000000000, 180.1045722148651862 ) ) ;
#90602=CARTESIAN_POINT ( 'NONE',  ( 62.08318622917204266, -25.58606428081736439, 71.03334541717022432 ) ) ;
#90608=CARTESIAN_POINT ( 'NONE',  ( -90.56781767776030279, -38.40338341477720974, -14.35555322263740585 ) ) ;
#90622=CARTESIAN_POINT ( 'NONE',  ( 85.50308900661609357, -25.30960514552327112, 172.5786385089847386 ) ) ;
#90635=CARTESIAN_POINT ( 'NONE',  ( -22.05550015032907041, -27.05256809874309099, 37.35158853590624517 ) ) ;
#90649=CARTESIAN_POINT ( 'NONE',  ( 49.54707403498029805, -21.77003194717852352, -25.65727647574667714 ) ) ;
#90658=CARTESIAN_POINT ( 'NONE',  ( -95.68557296049533534, -59.99999999999999289, 53.88884937414592002 ) ) ;
#90665=CARTESIAN_POINT ( 'NONE',  ( -84.11688277119964141, -32.48829956650884299, 169.3662770803418027 ) ) ;
#90684=CARTESIAN_POINT ( 'NONE',  ( 106.2140667560022536, -14.21045842199435860, 184.2067176257025380 ) ) ;
#90685=CARTESIAN_POINT ( 'NONE',  ( -111.5324017304388207, -60.00000000000003553, 193.8614060841614730 ) ) ;
#90687=CARTESIAN_POINT ( 'NONE',  ( -62.08384294452462626, -25.58717909351559072, 71.03563272662908901 ) ) ;
#90690=CARTESIAN_POINT ( 'NONE',  ( 94.50843613628299522, -59.99999999999023714, -13.93139703282171382 ) ) ;
#90694=CARTESIAN_POINT ( 'NONE',  ( 3.009920775786005365, -32.51036453576112706, 29.30336538357065379 ) ) ;
#90695=CARTESIAN_POINT ( 'NONE',  ( -103.1107698907982666, -52.71038489674184291, 144.4341237230532329 ) ) ;
#90702=CARTESIAN_POINT ( 'NONE',  ( -75.65743859592900833, -59.99999999999997868, 185.4139711062220783 ) ) ;
#90712=EDGE_CURVE ( 'NONE', #16098, #91737, #56783, .T. ) ;
#90715=CARTESIAN_POINT ( 'NONE',  ( -32.98079388240127230, -53.37464682946390582, 36.89136972320321917 ) ) ;
#90717=CARTESIAN_POINT ( 'NONE',  ( 41.71345372385450645, -53.34109301277966608, 43.41992601474273528 ) ) ;
#90720=CARTESIAN_POINT ( 'NONE',  ( -78.97285025244843837, -38.69040606023478546, 190.9764379862736803 ) ) ;
#90724=CARTESIAN_POINT ( 'NONE',  ( 42.36833565741010688, -59.99999999999995026, 45.73954733928472649 ) ) ;
#90732=CARTESIAN_POINT ( 'NONE',  ( 110.9494655861507937, -60.00000000000000711, 151.6493514595819647 ) ) ;
#90737=CARTESIAN_POINT ( 'NONE',  ( -85.97253845739234634, -30.00000000000002132, 178.5979368392352455 ) ) ;
#90751=CARTESIAN_POINT ( 'NONE',  ( 83.35798400553088072, -25.61440315765044673, 152.1571764916998006 ) ) ;
#90761=CARTESIAN_POINT ( 'NONE',  ( -2.567709512550288231, -59.99999999999997158, -36.87296048416308736 ) ) ;
#90767=DIRECTION ( 'NONE',  ( 0.000000000000000000, 1.000000000000000000, 0.000000000000000000 ) ) ;
#90769=CARTESIAN_POINT ( 'NONE',  ( 86.97298709575052555, -42.77486660283044984, 189.9043035977022100 ) ) ;
#90772=CARTESIAN_POINT ( 'NONE',  ( 32.17570300886618639, -33.85735722696470873, 41.96334411972644318 ) ) ;
#90783=CARTESIAN_POINT ( 'NONE',  ( 0.000000000000000000, -30.00000000000000000, 0.000000000000000000 ) ) ;
#90792=CARTESIAN_POINT ( 'NONE',  ( 100.6493391994169713, -57.67098493463386433, 72.97180361904253232 ) ) ;
#90798=CARTESIAN_POINT ( 'NONE',  ( -76.39489477947479656, -59.99999999999998579, 188.5198920997321181 ) ) ;
#90802=CARTESIAN_POINT ( 'NONE',  ( -86.28510748321916424, -21.13358643084282562, 179.4914488576992539 ) ) ;
#90803=ORIENTED_EDGE ( 'NONE', *, *, #3549, .F. ) ;
#90810=CARTESIAN_POINT ( 'NONE',  ( -82.83571923027355410, -37.76998749466422822, -11.56981727052722952 ) ) ;
#90816=CARTESIAN_POINT ( 'NONE',  ( -14.86825985027621755, -1.734723475976807094E-15, 8.569529079659670145 ) ) ;
#90819=CARTESIAN_POINT ( 'NONE',  ( 2.851859124854637884, -60.00000000000000711, -45.00000000000000711 ) ) ;
#90820=CARTESIAN_POINT ( 'NONE',  ( -80.26835608370822683, -22.15024438636563531, 130.4779458602490081 ) ) ;
#90822=CARTESIAN_POINT ( 'NONE',  ( 61.00101809772601769, -14.21045842199439591, 86.19763211990357377 ) ) ;
#90824=CARTESIAN_POINT ( 'NONE',  ( 113.9092013170919984, -57.67115667734820050, 163.3307494887165205 ) ) ;
#90842=CARTESIAN_POINT ( 'NONE',  ( 30.66882219077799121, -32.54285829269771568, 32.11411510472900233 ) ) ;
#90858=CARTESIAN_POINT ( 'NONE',  ( 92.74063705008857994, -60.00000000000000000, -6.517803209784806207 ) ) ;
#90873=CARTESIAN_POINT ( 'NONE',  ( 82.69522727347742830, -37.85838301434696973, 3.610110074265372226 ) ) ;
#90882=CARTESIAN_POINT ( 'NONE',  ( -89.32918359285039855, -38.52324389788776671, 200.4084188219295868 ) ) ;
#90887=CARTESIAN_POINT ( 'NONE',  ( 64.03519573087221772, -49.91008808719962531, 88.80839993703304458 ) ) ;
#90892=CARTESIAN_POINT ( 'NONE',  ( -81.27538057784241232, -57.67119034933180188, -29.50368748078413361 ) ) ;
#90895=CARTESIAN_POINT ( 'NONE',  ( -10.00000000000000178, 0.000000000000000000, -9.999999999999998224 ) ) ;
#90901=CARTESIAN_POINT ( 'NONE',  ( -10.00000000000000178, -15.00000000000000000, -9.999999999999998224 ) ) ;
#90914=CARTESIAN_POINT ( 'NONE',  ( -91.28316960610226261, -30.00000000000000000, 190.6086971429253651 ) ) ;
#90918=CARTESIAN_POINT ( 'NONE',  ( 63.16835690643451784, -57.67863152263677051, 119.1560271867259928 ) ) ;
#90923=CARTESIAN_POINT ( 'NONE',  ( 23.78672531768528842, -27.25131086482705456, -38.40582345290683008 ) ) ;
#90925=CARTESIAN_POINT ( 'NONE',  ( -43.37962327791924366, -60.00000000000000711, 57.54474475887785445 ) ) ;
#90931=CARTESIAN_POINT ( 'NONE',  ( -86.66824802271996475, -46.47689432800410003, 190.4879100785292394 ) ) ;
#90935=CARTESIAN_POINT ( 'NONE',  ( -9.314508772266908210, -49.92099836516761258, 32.21320177879483282 ) ) ;
#90952=CARTESIAN_POINT ( 'NONE',  ( 114.4521715241705664, -60.00000000000002842, 166.3966616003652348 ) ) ;
#90970=CARTESIAN_POINT ( 'NONE',  ( -72.81278058970477218, -59.99999999999997868, 182.9869454968206526 ) ) ;
#90972=CARTESIAN_POINT ( 'NONE',  ( 91.85330244269961497, -59.99999999999997158, 11.80756330073621818 ) ) ;
#90973=CARTESIAN_POINT ( 'NONE',  ( -74.10870907870054225, -60.00000000000004974, 189.8079394841834073 ) ) ;
#90974=CARTESIAN_POINT ( 'NONE',  ( 14.66643285550703268, -46.43468913974415813, 31.75579674561490506 ) ) ;
#90976=CARTESIAN_POINT ( 'NONE',  ( 82.45602942012469327, -37.99999999999996447, -12.86876314179797731 ) ) ;
#90979=CARTESIAN_POINT ( 'NONE',  ( -40.91703361344463730, -32.61193104857954239, 37.87439492575138900 ) ) ;
#90991=CARTESIAN_POINT ( 'NONE',  ( 9.999999999999998224, -15.00000000000000000, -9.999999999999998224 ) ) ;
#90993=CARTESIAN_POINT ( 'NONE',  ( 77.15469530005194088, -30.00000000000000711, -16.53926888306029852 ) ) ;
#90997=CARTESIAN_POINT ( 'NONE',  ( 80.76008078732601803, -30.00000000000000355, 12.10041964063638531 ) ) ;
#91020=CARTESIAN_POINT ( 'NONE',  ( 85.38575775096529696, -38.67724262594119011, 198.7153968702330928 ) ) ;
#91042=CARTESIAN_POINT ( 'NONE',  ( 86.18625139326670137, -24.72646195496230703, 181.0545054023034481 ) ) ;
#91047=CARTESIAN_POINT ( 'NONE',  ( 93.58048534552796127, -57.65383078522462057, -15.61220460149725575 ) ) ;
#91049=DIRECTION ( 'NONE',  ( -3.673940397442057649E-17, 0.000000000000000000, -1.000000000000000000 ) ) ;
#91051=CARTESIAN_POINT ( 'NONE',  ( -81.58955636323381100, -30.00000000000000711, -7.351077512096740207 ) ) ;
#91052=B_SPLINE_CURVE_WITH_KNOTS ( 'NONE', 3,
 ( #24360, #23288, #89066, #14618 ),
 .UNSPECIFIED., .F., .F.,
 ( 4, 4 ),
 ( 0.000000000000000000, 0.01132017942645960167 ),
 .UNSPECIFIED. ) ;
#91072=CARTESIAN_POINT ( 'NONE',  ( -55.69463391236389782, -28.61016029938631533, -26.37040716894560077 ) ) ;
#91075=CARTESIAN_POINT ( 'NONE',  ( -68.19771576902743959, -21.77019576768154252, -20.22133746935010024 ) ) ;
#91082=CARTESIAN_POINT ( 'NONE',  ( -67.48012074439532171, -60.00000000000000000, -33.40833613135792035 ) ) ;
#91084=CARTESIAN_POINT ( 'NONE',  ( 65.56157315575767086, -37.85303547496034327, -24.10004436282220297 ) ) ;
#91087=CARTESIAN_POINT ( 'NONE',  ( 102.5332414093125379, -60.18420180869041047, 193.5345815919327492 ) ) ;
#91088=CARTESIAN_POINT ( 'NONE',  ( 31.43263229211846266, -31.27596996767818993, 32.16362705870713512 ) ) ;
#91101=CARTESIAN_POINT ( 'NONE',  ( -47.68231610104891871, -57.68007204195236426, 71.30078553503261674 ) ) ;
#91107=CARTESIAN_POINT ( 'NONE',  ( 34.13661050418165388, -59.99999999999998579, -42.84071489294807122 ) ) ;
#91110=CARTESIAN_POINT ( 'NONE',  ( -51.42996021425486219, -36.04690667729754949, 52.01100956484014404 ) ) ;
#91114=CARTESIAN_POINT ( 'NONE',  ( -97.51575089595564805, -45.25067345593495105, 193.9083865710881014 ) ) ;
#91121=CARTESIAN_POINT ( 'NONE',  ( 85.87629844180868588, -38.64549821753008985, 199.0215093646828279 ) ) ;
#91126=CARTESIAN_POINT ( 'NONE',  ( 84.03161318001124869, -30.00000000000000000, 161.2884451932859520 ) ) ;
#91133=CARTESIAN_POINT ( 'NONE',  ( 52.51395162811751050, -36.03863491630684024, 53.95531543791132378 ) ) ;
#91138=CARTESIAN_POINT ( 'NONE',  ( -90.66024329338046073, -38.34389756899053481, 8.992944879562799088 ) ) ;
#91141=CARTESIAN_POINT ( 'NONE',  ( 105.3748507632057283, -38.35594986074055157, 120.2417250538963884 ) ) ;
#91143=CARTESIAN_POINT ( 'NONE',  ( 85.09281517647455928, -52.71298583903853796, 20.05580076196299899 ) ) ;
#91149=CARTESIAN_POINT ( 'NONE',  ( 74.36297015317659032, -59.99999999999999289, 175.8144878597308889 ) ) ;
#91154=CARTESIAN_POINT ( 'NONE',  ( 61.58695439658515625, -56.86329823613085210, 85.14614063634395791 ) ) ;
#91159=CARTESIAN_POINT ( 'NONE',  ( -84.69403854917420915, -38.35848897778367217, -23.12898730350110554 ) ) ;
#91167=AXIS2_PLACEMENT_3D ( 'NONE', #24060, #64498, #14322 ) ;
#91172=CARTESIAN_POINT ( 'NONE',  ( 85.02604456486491813, -28.87707945974564794, 172.9526225289325509 ) ) ;
#91180=CARTESIAN_POINT ( 'NONE',  ( -34.74080303120308599, -31.24499895687540274, -37.89147051442173364 ) ) ;
#91183=CARTESIAN_POINT ( 'NONE',  ( 53.65548343568850242, -60.00000000000000711, 81.46444441885545018 ) ) ;
#91186=CARTESIAN_POINT ( 'NONE',  ( 28.19983488487488188, -20.81563479387831350, 31.87448879475714136 ) ) ;
#91187=CARTESIAN_POINT ( 'NONE',  ( -15.78206918482793952, -23.13227408766112347, 36.04868682780729472 ) ) ;
#91200=CARTESIAN_POINT ( 'NONE',  ( 56.92553280862420451, -47.40888104890370869, -28.31668682213464550 ) ) ;
#91210=CARTESIAN_POINT ( 'NONE',  ( -103.7767948193627490, -59.99999999999998579, 103.1325596424688058 ) ) ;
#91219=CARTESIAN_POINT ( 'NONE',  ( -80.54720188594731667, -60.43838022186359638, 180.0448206866681176 ) ) ;
#91235=CARTESIAN_POINT ( 'NONE',  ( 114.5290872765719570, -59.99999999999999289, 168.5341745518089738 ) ) ;
#91236=CARTESIAN_POINT ( 'NONE',  ( -106.6793529335496515, -14.21045842199435860, 163.7930604915816559 ) ) ;
#91237=CARTESIAN_POINT ( 'NONE',  ( -58.43140080053613161, -49.91469830724326329, 72.99038015592236661 ) ) ;
#91240=CARTESIAN_POINT ( 'NONE',  ( 103.8610105594060826, -59.99999999999504752, 202.9082511799323640 ) ) ;
#91242=CARTESIAN_POINT ( 'NONE',  ( 8.168457008275577635, -39.47263446743016857, 30.46165443850678756 ) ) ;
#91244=CARTESIAN_POINT ( 'NONE',  ( -104.0415063169905210, -60.15505986368567193, 141.9492927151964068 ) ) ;
#91250=CARTESIAN_POINT ( 'NONE',  ( -34.12482747856847709, -60.00000000000001421, 45.63882276711500907 ) ) ;
#91254=CARTESIAN_POINT ( 'NONE',  ( 4.418206560264961169, 0.000000000000000000, -16.46930219881951629 ) ) ;
#91259=CARTESIAN_POINT ( 'NONE',  ( 106.4812587873048386, -60.00000000000000711, 170.6759392298722844 ) ) ;
#91260=CARTESIAN_POINT ( 'NONE',  ( -32.30208268559946561, -18.68134237623966243, 30.13613988364853569 ) ) ;
#91261=CARTESIAN_POINT ( 'NONE',  ( 43.31019682569796458, -49.88810819673993535, 44.39210588798376023 ) ) ;
#91266=CARTESIAN_POINT ( 'NONE',  ( -78.45100946094439109, -38.62822479361768302, 189.5449468668735449 ) ) ;
#91270=CARTESIAN_POINT ( 'NONE',  ( 41.33432493934709129, -60.00000000000001421, 44.56932545367675402 ) ) ;
#91277=CARTESIAN_POINT ( 'NONE',  ( 108.6217454145117074, -59.99999999999999289, 133.3216537659859000 ) ) ;
#91284=CARTESIAN_POINT ( 'NONE',  ( -97.66629619665867779, -29.99999999999996447, 190.7960662493706536 ) ) ;
#91294=CARTESIAN_POINT ( 'NONE',  ( 81.74723224102429242, -42.96870066486594908, 163.6216033774333880 ) ) ;
#91310=CARTESIAN_POINT ( 'NONE',  ( 86.99289245865087139, -28.01648969556236679, 186.8500900893037340 ) ) ;
#91312=EDGE_CURVE ( 'NONE', #86629, #8148, #22424, .T. ) ;
#91324=EDGE_CURVE ( 'NONE', #59127, #27380, #10977, .T. ) ;
#91331=CARTESIAN_POINT ( 'NONE',  ( 112.4379523079562375, -57.67145323133323132, 146.7647033902477745 ) ) ;
#91336=CARTESIAN_POINT ( 'NONE',  ( -76.22964667330261079, -60.00000000000000000, 187.8941157857488520 ) ) ;
#91340=CARTESIAN_POINT ( 'NONE',  ( -85.56701186126900893, -28.63696673469639364, 178.3758072176077860 ) ) ;
#91349=CARTESIAN_POINT ( 'NONE',  ( -83.25979992438379895, -37.78815355357362193, -6.773437407079532235 ) ) ;
#91357=CARTESIAN_POINT ( 'NONE',  ( 34.13661050418165388, -59.99999999999998579, -42.84071489294807122 ) ) ;
#91358=CARTESIAN_POINT ( 'NONE',  ( -79.51372813587923361, -25.61810700385877126, 129.8594159933582830 ) ) ;
#91360=CARTESIAN_POINT ( 'NONE',  ( 58.28796150060976089, -14.21045842199433729, 78.47796032183087789 ) ) ;
#91362=CARTESIAN_POINT ( 'NONE',  ( 113.6418193360469928, -57.67116734740694994, 183.3658933255892123 ) ) ;
#91372=FACE_OUTER_BOUND ( 'NONE', #68069, .T. ) ;
#91380=CARTESIAN_POINT ( 'NONE',  ( 31.80301772498203405, -25.61137255198223883, 31.25798125024838114 ) ) ;
#91389=CARTESIAN_POINT ( 'NONE',  ( 6.026974479199131350E-05, -59.99999999999998579, 33.88964995960238014 ) ) ;
#91396=CARTESIAN_POINT ( 'NONE',  ( 92.74004866154591298, -60.00000000000000711, -6.457183730990628590 ) ) ;
#91411=CARTESIAN_POINT ( 'NONE',  ( 85.67969062639832600, -52.73321948659197034, -3.978974129479640354 ) ) ;
#91424=CARTESIAN_POINT ( 'NONE',  ( 76.02982832201053043, -49.90348184441494084, 133.3415602174417529 ) ) ;
#91427=CIRCLE ( 'NONE', #89641, 1.999999999999998224 ) ;
#91431=CARTESIAN_POINT ( 'NONE',  ( -114.1029252960232725, -57.67113437255621022, 166.8310794691209367 ) ) ;
#91435=CARTESIAN_POINT ( 'NONE',  ( 103.8300117340547644, -45.28274633995925313, 179.3923655754059610 ) ) ;
#91440=CARTESIAN_POINT ( 'NONE',  ( -89.99999999999997158, 500000.0000000000582, 196.0238439516549818 ) ) ;
#91448=CARTESIAN_POINT ( 'NONE',  ( 12.86962311105386370, -60.00000000000000711, 39.71074230895528245 ) ) ;
#91449=CARTESIAN_POINT ( 'NONE',  ( -91.56480674067756809, -29.99999999999999645, 190.7188212141660699 ) ) ;
#91455=CARTESIAN_POINT ( 'NONE',  ( 69.37660719181492652, -57.68221287598195346, 149.8084875684434110 ) ) ;
#91457=CARTESIAN_POINT ( 'NONE',  ( 21.80423302458568102, -26.50636464758302324, -38.45223598383380192 ) ) ;
#91461=CARTESIAN_POINT ( 'NONE',  ( -38.99971751517416152, -60.00000000000000000, 50.74464281562639911 ) ) ;
#91464=CARTESIAN_POINT ( 'NONE',  ( -85.18066487451336855, -53.84498426936280424, 190.9692991790889778 ) ) ;
#91467=CARTESIAN_POINT ( 'NONE',  ( -6.184616894767937190, -53.40250187758704925, 32.78001493188074988 ) ) ;
#91469=CARTESIAN_POINT ( 'NONE',  ( 84.44642999311443532, -56.38380764954431612, 190.8905981808263448 ) ) ;
#91474=VERTEX_POINT ( 'NONE', #16892 ) ;
#91483=CARTESIAN_POINT ( 'NONE',  ( 106.4854190881680154, -14.21045842199434439, 182.1792229330528983 ) ) ;
#91484=CARTESIAN_POINT ( 'NONE',  ( -85.11433041153968304, -18.62775704286118739, 156.3534888976464572 ) ) ;
#91504=EDGE_LOOP ( 'NONE', ( #63237, #50508, #17776, #1658, #73164, #44987 ) ) ;
#91505=CARTESIAN_POINT ( 'NONE',  ( 92.16359607964912470, -59.99999999999998579, 3.391195432473796068 ) ) ;
#91506=CARTESIAN_POINT ( 'NONE',  ( -72.11328378729270128, -60.00000000000007816, 177.1367255069332316 ) ) ;
#91507=CARTESIAN_POINT ( 'NONE',  ( 15.54306593367750722, -32.51112372676959694, 29.48007834858285037 ) ) ;
#91510=CARTESIAN_POINT ( 'NONE',  ( -39.97149089181551318, -56.80599509476397202, 42.45399057685605015 ) ) ;
#91521=DIRECTION ( 'NONE',  ( -8.673617379884035472E-17, 0.000000000000000000, -1.000000000000000000 ) ) ;
#91523=CARTESIAN_POINT ( 'NONE',  ( 81.11895617840627892, -30.00000000000015987, -11.48067823770064244 ) ) ;
#91528=CARTESIAN_POINT ( 'NONE',  ( 86.67015649070671657, -30.00000000000000355, 68.44422152834891904 ) ) ;
#91548=CARTESIAN_POINT ( 'NONE',  ( 75.52049878556597662, -38.35346467193087250, 174.3913471852752082 ) ) ;
#91562=UNCERTAINTY_MEASURE_WITH_UNIT (LENGTH_MEASURE( 1.000000000000000082E-05 ), #103295, 'distance_accuracy_value', 'NONE');
#91569=CARTESIAN_POINT ( 'NONE',  ( 83.83731836935660908, -61.02556977702034402, 192.0768483181223019 ) ) ;
#91573=CARTESIAN_POINT ( 'NONE',  ( 83.90317718560991977, -57.67099787064372407, -27.79890540918554365 ) ) ;
#91574=CARTESIAN_POINT ( 'NONE',  ( -71.61946902996672293, -38.00000000000000711, -21.68294473311254578 ) ) ;
#91578=CARTESIAN_POINT ( 'NONE',  ( -80.78937829594153186, -29.99999999999999645, 9.273401272670504625 ) ) ;
#91591=CARTESIAN_POINT ( 'NONE',  ( 68.29510937182399744, -29.93295853997381073, -21.58228327437667460 ) ) ;
#91596=CARTESIAN_POINT ( 'NONE',  ( -38.83077474420895214, -24.51455171004923983, -30.53465071944147979 ) ) ;
#91609=CARTESIAN_POINT ( 'NONE',  ( -66.17813322318392011, -60.00000000000000000, -33.83408426857283757 ) ) ;
#91613=CARTESIAN_POINT ( 'NONE',  ( 98.44230880729132593, -37.77081898374070335, 192.2818622570195259 ) ) ;
#91627=CARTESIAN_POINT ( 'NONE',  ( -19.49904798085934843, -57.67182591607114261, 42.12704350231687300 ) ) ;
#91632=CARTESIAN_POINT ( 'NONE',  ( -94.98233504546384154, -60.00000000000004263, -11.07720828487985720 ) ) ;
#91634=CARTESIAN_POINT ( 'NONE',  ( -49.26216918836951209, -42.98127006318125609, 50.67504490609899648 ) ) ;
#91642=CARTESIAN_POINT ( 'NONE',  ( 106.1546576866561225, -38.37411319834205869, 196.1368700578019002 ) ) ;
#91647=CARTESIAN_POINT ( 'NONE',  ( 92.29684323675850521, -29.99999999999999645, 190.9540310920743309 ) ) ;
#91654=CARTESIAN_POINT ( 'NONE',  ( 52.28277805137703638, -42.97149545941184812, 56.06074786058347570 ) ) ;
#91661=CARTESIAN_POINT ( 'NONE',  ( -90.67172824033494294, -38.34345381613530179, 8.532772670937511350 ) ) ;
#91664=CARTESIAN_POINT ( 'NONE',  ( 110.2491435845926588, -38.35601175776276506, 184.3373205914413120 ) ) ;
#91666=CARTESIAN_POINT ( 'NONE',  ( 85.41402076159042167, -45.28278736550084460, 38.51236139168902639 ) ) ;
#91670=CARTESIAN_POINT ( 'NONE',  ( 74.84030112959139558, -60.00000000000000711, 180.0309485043998450 ) ) ;
#91674=CARTESIAN_POINT ( 'NONE',  ( 60.17165906010207976, -32.54078018923782167, 69.39975707695209906 ) ) ;
#91685=CARTESIAN_POINT ( 'NONE',  ( -24.73976553408828138, -19.17417380900784352, 31.50158786446911208 ) ) ;
#91690=CARTESIAN_POINT ( 'NONE',  ( 82.97048537381988353, -53.65713580650503189, 186.0269519114637831 ) ) ;
#91694=VERTEX_POINT ( 'NONE', #37352 ) ;
#91700=CARTESIAN_POINT ( 'NONE',  ( -38.75976230197111505, -32.56425988891942325, -37.56949155413147423 ) ) ;
#91702=CARTESIAN_POINT ( 'NONE',  ( 56.51238540776725472, -60.00000000000000000, 89.69717995302688962 ) ) ;
#91704=CARTESIAN_POINT ( 'NONE',  ( 4.445870512337758207, -12.80577256473136671, 32.12328779665543266 ) ) ;
#91705=CARTESIAN_POINT ( 'NONE',  ( -16.06393304193705873, -23.29483378636053814, 36.09226395465890391 ) ) ;
#91712=CARTESIAN_POINT ( 'NONE',  ( -74.38258808346769513, -38.35603007024654687, -29.43386503283010214 ) ) ;
#91718=CARTESIAN_POINT ( 'NONE',  ( 19.42798308777478056, -60.22819309317802805, -36.14118300158362018 ) ) ;
#91730=CARTESIAN_POINT ( 'NONE',  ( -100.8717445597720399, -60.00000000000000000, 86.14780900159736632 ) ) ;
#91736=CARTESIAN_POINT ( 'NONE',  ( -82.63399304676930512, -46.48556652261747502, 177.1140125195145743 ) ) ;
#91737=VERTEX_POINT ( 'NONE', #23818 ) ;
#91746=CARTESIAN_POINT ( 'NONE',  ( -51.62523913740291448, -57.67116585372185966, -39.59675499642695939 ) ) ;
#91753=CARTESIAN_POINT ( 'NONE',  ( 102.6948251682922404, -14.21045842199434084, 129.2649694714442035 ) ) ;
#91754=CARTESIAN_POINT ( 'NONE',  ( -106.6847104835838564, -14.21045842199429288, 180.1424598013736329 ) ) ;
#91755=CARTESIAN_POINT ( 'NONE',  ( -61.52905154805608134, -22.11594851545532237, 67.98467379429274615 ) ) ;
#91758=CARTESIAN_POINT ( 'NONE',  ( 15.62220340632255500, -60.00000000000000000, 39.81715212526117398 ) ) ;
#91760=CARTESIAN_POINT ( 'NONE',  ( 6.184718825718106494, -53.39673701277134654, 32.77909904936606011 ) ) ;
#91761=CARTESIAN_POINT ( 'NONE',  ( -103.7347427267881699, -52.71028617885053080, 187.7480353013368699 ) ) ;
#91767=CARTESIAN_POINT ( 'NONE',  ( -74.64324676806940317, -60.00000000000002132, 178.4426176709596632 ) ) ;
#91779=CARTESIAN_POINT ( 'NONE',  ( -30.72484781686770816, -22.13132935070668950, 30.23765891460996968 ) ) ;
#91782=CARTESIAN_POINT ( 'NONE',  ( 42.93374039441252421, -36.07034193160639290, 40.55194211749969924 ) ) ;
#91787=CARTESIAN_POINT ( 'NONE',  ( -80.66978632760687162, -38.82151610998087676, 194.1105594702565611 ) ) ;
#91790=CARTESIAN_POINT ( 'NONE',  ( 66.68617954663659475, -59.99999999999999289, 102.5125723375521716 ) ) ;
#91798=CARTESIAN_POINT ( 'NONE',  ( 108.8962094583731215, -60.00000000000000711, 135.2403837889553415 ) ) ;
#91803=ORIENTED_EDGE ( 'NONE', *, *, #45660, .T. ) ;
#91804=CARTESIAN_POINT ( 'NONE',  ( -97.11318458300092971, -29.99999999999995026, 191.0494389299799991 ) ) ;
#91817=CARTESIAN_POINT ( 'NONE',  ( 83.63424747110293822, -25.60960768623118256, 154.1967841724264190 ) ) ;
#91831=CARTESIAN_POINT ( 'NONE',  ( 87.38076970993836312, -46.41592001660386302, 191.3361042550797890 ) ) ;
#91844=CARTESIAN_POINT ( 'NONE',  ( 106.1565704622439483, -57.67112875917140968, 105.3532823125157591 ) ) ;
#91850=CARTESIAN_POINT ( 'NONE',  ( -76.29703970935240420, -59.99999999999999289, 188.1515592608628253 ) ) ;
#91855=CARTESIAN_POINT ( 'NONE',  ( -86.40763381868782744, -17.66018640161714615, 176.8075989531612322 ) ) ;
#91864=CARTESIAN_POINT ( 'NONE',  ( -83.22986503187559038, -37.77933018691697953, -8.240303472404791663 ) ) ;
#91871=CARTESIAN_POINT ( 'NONE',  ( 1.384974311275041225, -30.00000000000000000, 37.00000000000000711 ) ) ;
#91873=CARTESIAN_POINT ( 'NONE',  ( -33.15890210479862787, -30.00000000000000711, -37.92163678030271967 ) ) ;
#91874=CARTESIAN_POINT ( 'NONE',  ( -71.46856667809383623, -32.54058556944256253, 102.5544078860655333 ) ) ;
#91876=CARTESIAN_POINT ( 'NONE',  ( 78.68869634200761709, -14.21045842199439591, 170.0117969751115652 ) ) ;
#91878=CARTESIAN_POINT ( 'NONE',  ( 113.4549893713481055, -57.67117437226071530, 184.8066837110240783 ) ) ;
#91899=CARTESIAN_POINT ( 'NONE',  ( 33.23707082931593249, -46.42958337853537643, 35.74295623557356549 ) ) ;
#91909=CARTESIAN_POINT ( 'NONE',  ( -89.99999999999997158, -38.00000000001091394, 196.0238439516549818 ) ) ;
#91911=ORIENTED_EDGE ( 'NONE', *, *, #81811, .F. ) ;
#91912=CARTESIAN_POINT ( 'NONE',  ( 81.11655526126887139, -60.00000000000000000, -27.26544461796351371 ) ) ;
#91927=CARTESIAN_POINT ( 'NONE',  ( 83.52925484045992732, -45.27642508538186661, -13.37253514952393552 ) ) ;
#91937=CARTESIAN_POINT ( 'NONE',  ( 75.71757240347274376, -53.37388941686415222, 134.6993321033900486 ) ) ;
#91944=CARTESIAN_POINT ( 'NONE',  ( -109.3314759607053759, -57.67120315069445269, 124.6891463060778165 ) ) ;
#91948=CARTESIAN_POINT ( 'NONE',  ( 103.5970710204898779, -45.28273151134633423, 181.5168165621360572 ) ) ;
#91966=CARTESIAN_POINT ( 'NONE',  ( -84.91616747946434884, -29.99999999999999289, 169.5307764630179008 ) ) ;
#91970=CARTESIAN_POINT ( 'NONE',  ( 73.61960571407516341, -57.62828218540514769, 185.1312174396749413 ) ) ;
#91973=CARTESIAN_POINT ( 'NONE',  ( 28.41704268849491299, -28.98892241734421660, -38.24770077405835877 ) ) ;
#91975=CARTESIAN_POINT ( 'NONE',  ( -41.38414514539831401, -60.00000000000000000, 54.16917059837041393 ) ) ;
#91977=CARTESIAN_POINT ( 'NONE',  ( -85.53935049295719750, -53.83736247170576661, 191.4365733638258291 ) ) ;
#91980=CARTESIAN_POINT ( 'NONE',  ( -6.121071711750540878, -42.95758222298059081, 31.03938273056196806 ) ) ;
#91983=B_SPLINE_SURFACE_WITH_KNOTS ( 'NONE', 3, 3, ( 
 ( #70503, #30589, #95836, #79111, #12243, #62414, #55346, #21967, #79634, #103392, #6264, #29542, #87751 ),
 ( #21440, #54275, #38160, #64015, #63480, #13297, #45175, #46224, #46743, #5750, #96378, #88276, #39202 ),
 ( #72079, #23027, #78053, #800, #58006, #32712, #74717, #90390, #23557, #15429, #56402, #66108, #33769 ),
 ( #8924, #40238, #73114, #48843, #106019, #66644, #16495, #56936, #81736, #49379, #97944, #14889, #57466 ),
 ( #32165, #81210, #65047, #98987, #24094, #99528, #89857, #41830, #33234, #25150, #25705, #15965, #7859 ),
 ( #74188, #40766, #73657, #98465, #90931, #64531, #48317, #17043, #106560, #49918, #97396, #88798, #65581 ),
 ( #24619, #47784, #82287, #89337, #266, #8399, #41301, #82825, #7326, #80687, #6807, #39725, #72602 ),
 ( #105507, #31647, #2431, #101674, #27832, #19738, #50970, #67714, #43967, #52575, #60702, #93585, #35378 ),
 ( #50440, #101139, #83352, #36454, #102197, #76856, #43439, #100599, #76318, #69318, #67190, #34844, #9449 ),
 ( #26760, #3513, #2963, #10523, #19212, #59632, #68245, #59095, #85499, #27299, #83884, #58567, #51515 ),
 ( #60182, #44508, #91977, #92506, #18661, #93050, #9998, #84433, #18115, #52044, #11581, #84958, #11045 ),
 ( #35920, #77397, #91464, #68791, #42363, #34313, #17578, #75250, #42903, #1891, #1351, #100067, #75797 ),
 ( #26233, #29931, #77932, #28899, #6146, #54690, #62817, #30464, #70899, #53127, #45574, #103788, #46100 ),
 ( #22382, #104314, #54155, #96257, #39077, #71413, #5107, #87097, #69841, #47139, #20814, #45049, #20276 ),
 ( #38038, #71958, #61772, #63358, #53648, #95187, #95710, #87624, #4040, #21849, #62296, #86044, #13173 ),
 ( #55227, #78983, #94110, #13708, #46618, #88152, #14233, #36973, #79515, #28345, #86578, #80033, #94669 ),
 ( #12119, #102738, #61225, #5627, #12642, #78453, #4574, #37511, #38548, #70374, #103269, #29419, #21318 ),
 ( #63885, #82158, #98859, #24507, #89210, #32588, #32050, #96775, #89743, #8271, #41184, #56820, #22904 ),
 ( #98352, #25022, #33117, #47667, #49255, #104861, #97282, #16919, #105388, #65984, #88675, #14765, #57877 ),
 ( #80562, #56272, #72481, #82698, #74061, #57341, #150, #40119, #8804, #15308, #6682, #90802, #81097 ),
 ( #90262, #39608, #16365, #15838, #64928, #41712, #48196, #49795, #48720, #65460, #31528, #31003, #64409 ),
 ( #81608, #55741, #72994, #7735, #23434, #7210, #40645, #105899, #97814, #23979, #73527, #106430, #60575 ),
 ( #42770, #9857, #10390, #26113, #34718, #75120, #76191, #35788, #51382, #84297, #83749, #34184, #91855 ),
 ( #67060, #101546, #58970, #17980, #67592, #50842, #52443, #2291, #75661, #100470, #35239, #1761, #671 ),
 ( #11450, #26630, #99937, #59502, #51915, #92374, #85361, #18522, #27699, #19075, #84831, #93466, #43308 ),
 ( #68105, #60054, #101004, #27162, #92910, #76720, #50320, #1215, #10911, #43830, #68667, #83226, #19614 ),
 ( #9320, #2833, #74594, #33635, #42231, #66516, #99389, #25573, #58431, #91340, #17454, #38425, #79382 ),
 ( #95580, #44374, #36848, #63219, #44919, #5501, #28223, #61095, #71289, #29813, #20143, #102607, #11989 ),
 ( #54557, #103662, #87495, #86453, #22244, #61644, #93983, #104182, #20685, #52996, #70767, #85916, #62688 ),
 ( #4435, #88021, #94535, #13576, #103143, #4979, #77804, #46492, #3916, #54028, #96110, #69714, #102065 ),
 ( #30326, #21715, #28764, #77271, #12514, #45444, #21198, #78320, #53524, #37380, #55091, #3382, #29290 ),
 ( #36325, #95063, #69194, #45970, #70241, #62173, #86971, #13039, #78848, #37907, #56688, #6015, #96638 ),
 ( #106294, #39476, #64282, #30872, #63751, #80433, #32457, #40517, #15704, #22774, #14626, #98733, #73394 ),
 ( #16234, #89610, #38939, #31404, #48592, #31917, #17, #8145, #90132, #39995, #82019, #24889, #57213 ),
 ( #72868, #55611, #32984, #6543, #88548, #71816, #104719, #97677, #57741, #47538, #49119, #72354, #80963 ),
 ( #65329, #105257, #81481, #48065, #97151, #105778, #98217, #23299, #56134, #89079, #41051, #15176, #73935 ),
 ( #7079, #64794, #23843, #14101, #7598, #24370, #65855, #47007, #79905, #16775, #59378, #27574, #42105 ),
 ( #74989, #67985, #66931, #101423, #91736, #10785, #35117, #100871, #2707, #99812, #17855, #51246, #76062 ),
 ( #50708, #100343, #92785, #66381, #17323, #27033, #83620, #51788, #99261, #43705, #9724, #25438, #34592 ),
 ( #42640, #58292, #2164, #84173, #26506, #92239, #83100, #43181, #1082, #68534, #25983, #67465, #8676 ),
 ( #18394, #59918, #18946, #84700, #9194, #58843, #76596, #35655, #90665, #49664, #10269, #82572, #41578 ),
 ( #91219, #74464, #544, #33507, #50198, #75538, #34057, #1633, #44247, #54422, #36726, #77139, #86843 ),
 ( #12917, #45316, #20565, #104057, #3790, #103538, #12388, #21075, #3256, #62558, #28098, #70110, #79258 ),
 ( #11318, #53404, #46368, #45840, #20018, #60453, #102483, #61510, #37248, #94403, #36197, #69065, #29686 ),
 ( #103019, #11862, #86322, #60973, #62050, #21590, #29174, #94939, #37783, #87367, #78712, #44792, #93328 ),
 ( #78198, #69592, #4312, #71162, #101938, #28627, #85231, #95444, #53911, #5382, #4849, #70644, #13447 ),
 ( #38302, #93859, #19482, #52319, #85789, #52861, #77681, #6954, #15043, #17599, #63630, #105133, #72230 ),
 ( #88424, #97030, #30744, #31788, #99549, #39871, #72743, #39353, #96520, #47410, #58583, #22651, #91484 ),
 ( #14497, #23170, #80302, #9468, #64671, #31274, #56014, #97544, #64158, #63085, #105647, #75271, #6414 ),
 ( #88948, #7470, #47933, #42380, #80841, #50461, #81360, #40387, #83371, #23705, #56558, #89485, #15579 ),
 ( #48470, #73269, #32327, #5885, #55487, #106167, #66664, #25725, #38815, #30198, #95985, #71681, #22111 ),
 ( #54965, #87894, #104588, #13976, #46881, #79785, #93069, #85521, #44530, #60200, #67210, #43986, #101693 ),
 ( #36472, #50989, #52594, #1369, #100617, #20298, #1911, #69341, #91997, #18133, #102220, #93609, #83903 ),
 ( #75816, #86067, #11599, #60722, #77418, #43461, #12138, #18680, #10017, #28368, #51536, #3534, #19235 ),
 ( #42924, #61246, #34864, #11062, #53149, #67733, #59117, #101158, #94130, #19760, #26780, #45067, #76337 ),
 ( #84980, #2450, #59649, #92525, #34335, #100084, #52065, #84450, #26254, #10543, #76873, #35397, #2985 ),
 ( #68265, #27320, #35940, #68811, #27853, #13727, #69862, #53665, #14787, #63377, #103293, #21337, #94687 ),
 ( #37529, #96274, #104330, #79531, #20835, #78471, #55760, #30478, #5644, #80052, #46634, #102756, #95205 ),
 ( #22400, #96791, #54174, #79006, #38568, #55244, #29952, #5126, #87644, #6163, #86599, #4595, #14252 ),
 ( #39095, #12663, #104885, #38059, #45594, #21867, #88691, #62835, #70394, #88168, #71428, #47157, #71975 ),
 ( #31024, #29439, #77949, #13190, #54707, #28917, #63905, #22923, #4064, #36992, #61793, #62312, #87116 ),
 ( #46121, #70915, #103807, #95726, #33132, #23455, #105916, #15327, #25591, #57896, #169, #90820, #89761 ),
 ( #64943, #31548, #41727, #23996, #64430, #74083, #56291, #66002, #32607, #7752, #91358, #89229, #56837 ),
 ( #16936, #15858, #99409, #98879, #106449, #8291, #48736, #57362, #48213, #49814, #65480, #73012, #47682 ),
 ( #24522, #98369, #33656, #81118, #81629, #40662, #90281, #32069, #73545, #7225, #49271, #8823, #16384 ),
 ( #82175, #40135, #97835, #74611, #41197, #691, #25039, #82719, #66535, #58449, #80580, #6701, #39629 ),
 ( #72500, #105405, #97300, #92930, #61111, #75682, #9878, #1781, #101562, #100488, #28241, #18539, #44392 ),
 ( #68681, #36342, #26645, #51404, #84845, #2849, #76208, #84315, #27177, #19630, #99959, #50861, #60593 ),
 ( #85381, #26132, #77288, #10412, #58986, #68126, #17473, #2313, #91874, #35803, #10928, #60067, #19092 ),
 ( #76739, #34738, #102079, #59520, #101023, #42248, #11465, #51933, #93481, #52463, #3400, #42789, #92391 ),
 ( #69213, #50336, #83245, #43849, #9338, #75139, #27719, #1234, #34204, #67076, #18001, #83767, #67609 ),
 ( #35259, #43327, #71306, #88040, #13591, #78336, #30887, #5517, #78867, #103159, #4994, #104737, #93998 ),
 ( #70787, #45987, #28780, #6032, #86472, #3932, #85934, #12005, #103683, #20160, #94551, #30342, #12528 ),
 ( #95595, #46505, #69731, #21732, #21212, #44938, #37925, #104199, #63236, #29827, #53010, #62704, #87511 ),
 ( #22261, #36863, #38440, #77822, #45463, #38954, #20703, #55110, #102622, #61662, #14120, #79401, #53541 ),
 ( #4453, #71831, #96128, #47021, #79923, #29304, #37397, #70258, #62194, #95080, #54041, #86988, #13055 ),
 ( #54572, #48610, #23858, #560, #7096, #35, #15725, #24392, #47553, #65874, #31420, #73412, #82589 ),
 ( #14644, #56702, #49683, #49139, #23314, #63768, #105794, #64811, #40533, #97693, #80449, #6560, #33007 ),
 ( #81495, #39493, #8694, #98753, #7615, #41602, #65345, #105274, #97167, #64295, #41070, #74485, #24907 ),
 ( #55626, #72368, #96656, #82039, #89094, #40011, #56150, #15189, #48078, #8163, #90149, #98236, #80980 ),
 ( #22791, #16254, #57231, #57761, #106309, #88563, #72883, #32474, #73954, #31933, #90687, #16796, #89625 ),
 ( #42123, #84192, #44269, #92259, #1104, #51809, #27056, #43200, #2185, #26002, #92806, #91755, #11337 ),
 ( #10288, #58312, #27593, #76085, #76615, #2727, #101440, #58865, #42659, #18965, #60475, #35678, #68554 ),
 ( #93354, #25459, #35135, #91237, #77161, #33528, #75009, #17344, #59940, #66400, #34078, #51270, #99281 ),
 ( #19506, #84722, #17875, #50219, #10807, #18413, #75559, #68005, #83120, #66951, #9743, #9215, #52340 ),
 ( #100890, #85253, #99830, #50728, #26525, #83638, #43724, #1654, #34612, #67483, #100362, #59398, #4334 ),
 ( #52884, #46388, #5401, #62071, #93879, #22131, #79279, #53931, #96006, #4868, #44812, #36748, #77699 ),
 ( #54983, #38322, #45859, #101958, #85809, #46904, #95465, #28647, #53425, #20038, #11884, #69610, #21612 ),
 ( #37805, #3811, #102504, #87913, #29708, #70667, #71184, #78733, #28118, #20586, #103558, #21097, #13995 ),
 ( #104077, #29196, #30219, #3277, #63105, #86863, #94960, #61531, #36217, #94424, #86343, #60993, #12409 ),
 ( #69085, #45340, #62582, #78218, #37268, #70132, #103038, #12938, #54442, #87392, #13467, #97565, #38836 ),
 ( #63648, #106186, #88447, #32348, #64695, #39890, #16667, #23191, #16130, #31805, #40407, #96538, #81914 ),
 ( #89503, #98635, #6433, #30762, #72764, #65754, #65220, #39371, #79807, #15066, #80860, #56580, #6972 ),
 ( #22669, #49014, #8031, #23729, #55507, #24785, #40943, #15598, #57634, #81383, #14519, #72248, #47431 ),
 ( #90559, #73835, #48488, #71699, #80321, #5906, #98113, #105150, #56036, #31293, #64179, #97049, #24262 ),
 ( #7493, #88969, #47953, #104611, #57111, #73289, #106730, #90024, #105670, #32879, #18290, #67359, #35549 ),
 ( #18838, #75432, #10684, #60344, #92682, #26404, #1524, #91110, #68422, #42002, #66277, #41471, #74359 ),
 ( #93220, #50092, #51682, #74882, #9621, #51145, #75965, #25323, #84063, #83518, #437, #34490, #26930 ),
 ( #100238, #8568, #92142, #43078, #43600, #84602, #99165, #100764, #49558, #969, #101317, #82999, #76491 ),
 ( #59270, #2598, #66820, #27467, #9094, #82467, #33951, #99709, #42530, #25879, #33408, #10164, #17747 ),
 ( #2063, #58738, #58183, #35013, #17219, #91634, #50603, #67878, #59803, #102369, #30098, #20456, #46267 ),
 ( #5279, #13341, #95347, #45218, #87263, #62984, #62455, #102907, #78093, #60866, #38202, #11750, #36091 ),
 ( #44142, #29074, #19383, #19908, #21483, #44684, #86216, #20978, #45730, #101833, #53811, #53297, #11211 ),
 ( #103434, #54318, #4211, #85126, #61941, #12815, #79152, #71063, #68962, #70546, #52214, #77571, #103954 ),
 ( #77030, #3147, #27997, #93754, #4743, #52752, #3688, #85673, #36618, #29585, #78611, #69483, #61399 ),
 ( #28516, #94291, #12288, #37141, #70006, #37683, #94833, #86742, #80734, #55906, #32758, #39249, #32214 ),
 ( #56453, #79682, #97990, #63522, #105551, #7906, #22552, #46790, #88843, #81783, #81261, #55393, #95884 ),
 ( #96932, #72651, #23068, #5793, #38714, #65094, #24144, #47830, #71579, #40812, #56986, #39775, #73706 ),
 ( #30634, #88324, #96421, #104484, #87792, #13874, #31690, #22009, #14396, #89902, #47309, #14936, #97442 ),
 ( #80203, #23604, #6852, #6308, #64577, #73162, #16011, #89385, #54864, #15477, #48368, #48890, #106608 ),
 ( #40287, #72123, #105033, #31174, #64057, #7374, #106065, #49430, #100645, #51018, #41348, #17090, #33281 ),
 ( #74239, #82339, #92024, #43486, #66152, #83398, #24662, #42952, #59676, #18159, #49967, #2475, #83932 ),
 ( #65631, #8970, #1939, #17625, #26280, #8446, #67757, #99034, #75301, #84477, #25200, #16543, #58610 ),
 ( #10045, #58056, #98514, #843, #66693, #42407, #99575, #316, #90979, #34891, #26803, #50485, #82874 ),
 ( #92556, #9495, #51561, #67238, #41875, #74764, #33817, #75844, #10569, #18706, #1397, #57515, #25751 ),
 ( #76362, #91510, #34363, #100115, #59142, #90436, #22287, #61820, #37021, #85005, #35968, #14669, #96154 ),
 ( #38983, #77975, #60227, #52621, #4092, #53177, #22817, #30912, #6057, #61271, #104762, #47578, #79947 ),
 ( #94162, #76904, #55651, #27883, #63794, #55135, #19787, #80473, #88064, #20330, #44559, #86093, #35423 ),
 ( #11629, #93095, #71858, #3560, #88589, #14144, #12164, #102784, #36498, #45095, #68838, #96679, #69889 ),
 ( #68294, #28398, #28947, #47048, #101188, #101716, #69366, #77446, #27349, #93637, #102246, #60749, #19267 ),
 ( #52095, #11089, #44014, #85548, #3015, #33554, #72909, #66425, #64840, #97718, #73442, #23884, #91260 ),
 ( #23340, #105819, #98781, #33031, #8189, #56179, #7119, #17370, #65898, #41097, #8718, #49164, #31443 ),
 ( #82070, #24417, #99309, #588, #82616, #32500, #74511, #50242, #49710, #90176, #65371, #48104, #25481 ),
 ( #89119, #105298, #64323, #16280, #6586, #40034, #41626, #31960, #106336, #73977, #24936, #15216, #60 ),
 ( #97195, #98263, #90715, #58337, #57255, #72394, #57787, #16825, #39518, #81005, #56727, #89649, #15750 ),
 ( #48634, #81518, #7643, #40559, #66976, #11362, #68577, #58888, #34638, #50754, #61017, #93376, #35702 ),
 ( #93904, #83661, #100914, #42149, #60496, #9772, #44289, #99856, #26029, #77184, #101462, #91779, #67506 ),
 ( #20059, #19527, #27613, #52363, #18439, #83145, #100387, #17902, #3295, #59421, #42687, #2749, #75583 ),
 ( #68024, #43225, #9242, #26549, #85275, #35157, #43748, #1681, #36238, #92284, #92826, #101980, #51294 ),
 ( #76108, #69107, #28140, #84214, #75033, #10309, #2208, #59963, #27080, #18987, #51831, #1131, #34104 ),
 ( #84744, #10828, #76640, #45879, #30238, #70687, #28669, #94449, #61554, #87413, #96027, #5418, #4892 ),
 ( #12430, #62088, #45360, #22152, #103577, #103060, #94980, #29727, #37290, #52908, #62601, #85830, #78241 ),
 ( #4354, #46411, #70156, #11906, #21117, #55003, #79297, #38342, #87934, #29216, #53949, #21631, #13488 ),
 ( #86884, #95486, #71203, #20606, #12957, #104098, #78758, #63127, #53444, #44835, #37825, #86365, #54462 ),
 ( #77721, #3832, #36767, #69633, #102525, #11172, #34972, #101793, #100724, #20411, #84560, #93176, #67317 ),
 ( #19344, #85631, #11706, #3643, #67836, #51642, #27960, #101276, #3103, #26364, #44643, #10126, #52173 ),
 ( #75923, #100199, #35502, #28476, #60823, #2024, #86173, #10643, #43560, #85088, #76446, #59227, #92101 ),
 ( #77527, #27427, #18244, #61357, #36579, #44099, #94250, #76987, #84020, #26887, #43035, #19868, #53255 ),
 ( #36048, #34448, #51101, #42490, #93715, #59760, #92638, #18796, #2555, #68381, #52704, #68919, #69445 ),
 ( #60304, #75386, #102327, #1484, #2559, #85637, #60827, #61901, #86177, #12249, #53775, #11175, #36052 ),
 ( #45694, #78056, #11710, #93719, #76450, #86705, #27431, #51645, #26891, #59766, #44647, #78574, #35507 ),
 ( #34976, #19872, #68386, #53259, #28480, #77531, #3648, #60308, #94254, #93182, #12776, #76994, #36582 ),
 ( #29035, #69449, #4174, #37105, #102870, #19348, #44103, #20415, #94796, #69968, #20939, #102331, #67838 ),
 ( #61361, #92642, #100729, #18800, #43564, #84566, #45179, #10647, #101280, #52708, #52177, #85091, #3106 ),
 ( #68922, #101796, #27964, #96382, #13836, #22511, #15433, #71023, #37643, #72607, #48321, #80164, #55351 ),
 ( #105510, #80691, #30594, #31651, #4709, #47787, #88280, #63483, #46227, #23562, #103914, #21444, #103395 ),
 ( #14356, #70507, #5238, #6811, #30062, #71540, #6268, #31132, #87222, #39206, #38675, #29547, #47268 ),
 ( #39729, #72082, #62418, #104990, #64021, #64535, #97400, #54279, #55865, #95312, #62944, #56406, #38164 ),
 ( #13302, #79115, #89341, #96897, #95840, #21971, #54825, #87755, #14893, #23031, #46748, #79638, #5755 ),
 ( #104443, #88804, #57471, #65052, #803, #89862, #33772, #66112, #41306, #18118, #24623, #17583, #33238 ),
 ( #97948, #83355, #48847, #90935, #100070, #7863, #32169, #74192, #67193, #66647, #40770, #81215, #16498 ),
 ( #58010, #98991, #26237, #73661, #49383, #82291, #17046, #32716, #271, #81740, #82830, #42366, #49922 ),
 ( #90394, #106565, #98470, #1354, #65585, #34316, #8403, #25154, #8929, #41833, #59099, #74720, #99531 ),
 ( #25708, #58570, #91467, #24098, #50443, #91980, #9452, #75253, #15969, #7330, #40242, #56940, #73118 ),
 ( #106023, #94672, #51518, #94113, #43443, #11048, #52578, #77400, #26763, #85502, #84962, #42906, #35923 ),
 ( #20279, #2966, #10001, #93589, #44511, #45051, #86047, #100602, #102201, #50973, #76321, #69844, #84436 ),
 ( #34848, #67717, #12122, #36457, #59634, #2434, #18664, #28902, #61228, #3516, #53130, #93053, #61775 ),
 ( #92509, #77936, #27302, #10526, #69323, #35381, #28348, #68794, #43970, #83887, #101142, #4044, #101677 ),
 ( #68248, #36976, #60185, #60705, #102741, #19216, #1894, #76859, #75800, #52047, #27835, #19741, #11584 ),
 ( #105771, #23293, #37514, #70377, #65323, #24364, #80959, #4577, #41046, #98211, #72863, #8138, #23837 ) ),
 .UNSPECIFIED., .F., .F., .F.,
 ( 4, 3, 3, 3, 3, 3, 3, 3, 3, 3, 3, 3, 3, 3, 3, 3, 3, 3, 3, 3, 3, 3, 3, 3, 3, 3, 3, 3, 3, 3, 3, 3, 3, 3, 3, 3, 3, 3, 3, 3, 3, 3, 3, 3, 3, 3, 3, 3, 3, 3, 3, 3, 3, 4 ),
 ( 4, 3, 3, 3, 4 ),
 ( 0.8179795923582280359, 0.8194016267929293829, 0.8201126440102800563, 0.8208236612276307298, 0.8236677300970334237, 0.8243787473143840971, 0.8250897645317347706, 0.8265117989664361176, 0.8279338334011374645, 0.8293558678358388114, 0.8321999367052415053, 0.8350440055746441992, 0.8364660400093455461, 0.8378880744440468931, 0.8407321433134495869, 0.8435762121828522808, 0.8464202810522549747, 0.8521084187910603625, 0.8577965565298657502, 0.8634846942686710269, 0.8691728320074763037, 0.8748609697462816914, 0.8862372452238924669, 0.9089897961791140180, 0.9203660716567247935, 0.9232101405261274873, 0.9260542093955301812, 0.9317423471343355690, 0.9374304848731409567, 0.9431186226119463445, 0.9459626914813490384, 0.9488067603507517322, 0.9516508292201544261, 0.9544948980895570090, 0.9559169325242582449, 0.9573389669589595918, 0.9601830358283622857, 0.9630271046977649796, 0.9658711735671676735, 0.9687152424365703673, 0.9715593113059730612, 0.9722703285233237347, 0.9729813457406744082, 0.9744033801753757551, 0.9758254146100771020, 0.9772474490447784490, 0.9800915179141811429, 0.9829355867835838367, 0.9857796556529865306, 0.9886237245223892245, 0.9914677933917919184, 0.9943118622611946122, 0.9971559311305973061, 1.000000000000000000 ),
 ( 0.03164164694831613639, 0.3798059082496895167, 0.7279701695510628623, 1.076134430852436319, 1.424298692153809665 ),
 .UNSPECIFIED. ) ;
#91988=MECHANICAL_DESIGN_GEOMETRIC_PRESENTATION_REPRESENTATION('',(#54097),#36981);
#91991=CARTESIAN_POINT ( 'NONE',  ( 81.98192093697382177, -38.00000000001091394, -13.86368299876859567 ) ) ;
#91996=CARTESIAN_POINT ( 'NONE',  ( 114.5290872765719570, -59.99999999999999289, 168.5341745518089738 ) ) ;
#91997=CARTESIAN_POINT ( 'NONE',  ( -82.26374899041833544, -32.56066175956263464, 153.0468411736874259 ) ) ;
#92018=CARTESIAN_POINT ( 'NONE',  ( 111.9602503973177647, -59.99999999999997868, 180.3351832281744578 ) ) ;
#92019=CARTESIAN_POINT ( 'NONE',  ( -79.87726071770381964, -29.99999999999996092, 191.0765191543576407 ) ) ;
#92020=CARTESIAN_POINT ( 'NONE',  ( 18.63452250350944084, -22.07072144282664183, 27.94029182146244494 ) ) ;
#92024=CARTESIAN_POINT ( 'NONE',  ( -43.39865720172556962, -53.34764174391096958, 45.35594569590636382 ) ) ;
#92036=CARTESIAN_POINT ( 'NONE',  ( -48.35517769068118099, -38.32756362620095558, 64.77550779848442630 ) ) ;
#92038=CARTESIAN_POINT ( 'NONE',  ( 81.53245238598010758, -30.00000000000000000, -8.829371841663466114 ) ) ;
#92043=CARTESIAN_POINT ( 'NONE',  ( 80.76588975746719257, -30.00000000000000355, 10.92248678019670471 ) ) ;
#92058=CARTESIAN_POINT ( 'NONE',  ( 74.29104448979910558, -38.32825804840491202, 162.8965795265015402 ) ) ;
#92078=CARTESIAN_POINT ( 'NONE',  ( 86.31765247549246567, -21.06018481759237559, 180.2375958646254901 ) ) ;
#92083=CARTESIAN_POINT ( 'NONE',  ( 90.46448577880153152, -57.66543568833093758, -21.68132792077462057 ) ) ;
#92089=CARTESIAN_POINT ( 'NONE',  ( -94.06182321730192086, -30.00000000000000000, 112.3371401795816240 ) ) ;
#92098=CARTESIAN_POINT ( 'NONE',  ( -65.54168109996004432, -37.85200263902478923, -24.10684023409089605 ) ) ;
#92100=CARTESIAN_POINT ( 'NONE',  ( 56.97675734779401324, -28.82016638348090609, -25.97335252889095258 ) ) ;
#92101=CARTESIAN_POINT ( 'NONE',  ( -24.15655977932474485, -18.60408373216753475, 28.02082033799254646 ) ) ;
#92106=CARTESIAN_POINT ( 'NONE',  ( -67.63677907206896123, -29.90539320196331374, -21.89490774697042497 ) ) ;
#92117=CARTESIAN_POINT ( 'NONE',  ( -87.95683113949989718, -59.99999999999999289, -21.63131309512601419 ) ) ;
#92121=CARTESIAN_POINT ( 'NONE',  ( 100.7680253952265019, -52.74798219828765866, 193.5988501864534328 ) ) ;
#92135=CARTESIAN_POINT ( 'NONE',  ( -72.53004918620850106, -57.66488672193313647, 177.2532351053191348 ) ) ;
#92140=CARTESIAN_POINT ( 'NONE',  ( -87.68152309050471160, -14.21045842199426801, 32.26861779447729361 ) ) ;
#92142=CARTESIAN_POINT ( 'NONE',  ( -49.90681345140622938, -53.37058229338229154, 55.25435010867053620 ) ) ;
#92146=CARTESIAN_POINT ( 'NONE',  ( -95.20579108050159789, -45.25313649919430503, 194.1753725634821990 ) ) ;
#92153=CARTESIAN_POINT ( 'NONE',  ( 81.99224433430156012, -38.84286317575919867, 195.8945477241109927 ) ) ;
#92158=CARTESIAN_POINT ( 'NONE',  ( 94.36600822773108632, -30.00000000000000711, 191.3092720282738242 ) ) ;
#92162=EDGE_LOOP ( 'NONE', ( #8000, #100786 ) ) ;
#92164=CARTESIAN_POINT ( 'NONE',  ( 53.40199480540213983, -39.50120367549543943, 56.96464640269142166 ) ) ;
#92168=CARTESIAN_POINT ( 'NONE',  ( -88.09014624656468584, -38.37178535084554198, -19.45122215882188854 ) ) ;
#92170=CARTESIAN_POINT ( 'NONE',  ( 108.2573416289480406, -38.35772023760677740, 192.2552001511533888 ) ) ;
#92172=CARTESIAN_POINT ( 'NONE',  ( 84.65144155607768539, -45.28281508045545678, 31.07819321620053188 ) ) ;
#92180=CARTESIAN_POINT ( 'NONE',  ( 59.39647789081419660, -32.54350338366015194, 67.45545659301726005 ) ) ;
#92183=CARTESIAN_POINT ( 'NONE',  ( 89.99999999999997158, -52.00000000000000000, 198.0238439516549818 ) ) ;
#92189=CARTESIAN_POINT ( 'NONE',  ( -41.85571157551820676, -27.12375206088530533, 37.13791425116489364 ) ) ;
#92193=CARTESIAN_POINT ( 'NONE',  ( 81.59403609548893144, -60.63023761752385354, 186.3572134667889770 ) ) ;
#92202=CARTESIAN_POINT ( 'NONE',  ( -18.51720514346013502, -25.29809392112008481, -38.50248889867572899 ) ) ;
#92204=CARTESIAN_POINT ( 'NONE',  ( 47.62749844892509543, -59.99999999999999289, 66.18161539844986407 ) ) ;
#92206=CARTESIAN_POINT ( 'NONE',  ( -27.49835752312068848, -30.75254570659940256, 39.28988535020603479 ) ) ;
#92211=AXIS2_PLACEMENT_3D ( 'NONE', #49844, #82750, #8852 ) ;
#92222=CARTESIAN_POINT ( 'NONE',  ( 22.67313198859957168, -60.22830976074993714, -35.89781762293466016 ) ) ;
#92232=CARTESIAN_POINT ( 'NONE',  ( -104.6395680266647332, -59.99999999999999289, 108.2291619832981695 ) ) ;
#92239=CARTESIAN_POINT ( 'NONE',  ( -82.93997213326217377, -42.97867824148965354, 174.7049767036717185 ) ) ;
#92256=CARTESIAN_POINT ( 'NONE',  ( 89.21217950020245269, -30.00000000000004974, 13.74488734703711934 ) ) ;
#92258=CARTESIAN_POINT ( 'NONE',  ( -73.20331151331558317, -59.99999999999998579, 185.6225630369678470 ) ) ;
#92259=CARTESIAN_POINT ( 'NONE',  ( -59.90188342519598308, -49.91569465878361456, 76.94345777252618745 ) ) ;
#92262=CARTESIAN_POINT ( 'NONE',  ( 87.20415626912121354, -59.99999999999998579, -25.76356015432472901 ) ) ;
#92264=CARTESIAN_POINT ( 'NONE',  ( 7.005973654531714168, -22.06726470602710677, 27.55784255609015077 ) ) ;
#92265=CARTESIAN_POINT ( 'NONE',  ( -101.5318813598352676, -45.26482616480781473, 190.2983095272828962 ) ) ;
#92273=CARTESIAN_POINT ( 'NONE',  ( -80.72759035304791553, -59.99999999999998579, 196.8484650859923875 ) ) ;
#92277=CARTESIAN_POINT ( 'NONE',  ( 11.24494283604391498, -0.000000000000000000, -12.81923949848203570 ) ) ;
#92284=CARTESIAN_POINT ( 'NONE',  ( -29.88958479793361889, -29.06775393404062058, 31.22462154783213961 ) ) ;
#92286=CARTESIAN_POINT ( 'NONE',  ( 42.62262948205808044, -25.70207388102151569, 37.69155540254526215 ) ) ;
#92291=CARTESIAN_POINT ( 'NONE',  ( -80.10895284081995271, -38.78997264253702326, 193.1831740812525595 ) ) ;
#92295=CARTESIAN_POINT ( 'NONE',  ( 49.17729069842651768, -59.99999999999997868, 56.10385161243137020 ) ) ;
#92305=CARTESIAN_POINT ( 'NONE',  ( 102.1815710810213318, -60.00000000000000000, 93.80444312277987251 ) ) ;
#92313=CARTESIAN_POINT ( 'NONE',  ( -96.54523544995177531, -29.99999999999999645, 127.4433644037409294 ) ) ;
#92328=CARTESIAN_POINT ( 'NONE',  ( 83.21183222637840515, -29.08118594051771311, 155.6702613005863611 ) ) ;
#92343=CARTESIAN_POINT ( 'NONE',  ( 86.71928054816494580, -53.76640798283146694, 192.6448558597238048 ) ) ;
#92362=ADVANCED_FACE ( 'NONE', ( #104341 ), #87655, .F. ) ;
#92368=CARTESIAN_POINT ( 'NONE',  ( -89.32677887001227646, -60.00000000000000000, 201.7918933705177551 ) ) ;
#92374=CARTESIAN_POINT ( 'NONE',  ( -84.53343285826699116, -42.97347055893645518, 184.1442894847539264 ) ) ;
#92378=ORIENTED_EDGE ( 'NONE', *, *, #48546, .F. ) ;
#92382=CARTESIAN_POINT ( 'NONE',  ( -86.34385121660355367, -60.13442145805939987, 4.656109867693190907 ) ) ;
#92389=CARTESIAN_POINT ( 'NONE',  ( 71.37437158690347871, -14.21045842199427156, 121.5198118854055451 ) ) ;
#92390=CARTESIAN_POINT ( 'NONE',  ( -90.08857655234534434, -29.99999999999997158, -9.079940112750868764 ) ) ;
#92391=CARTESIAN_POINT ( 'NONE',  ( -69.94854193131207865, -18.63627970369213216, 89.84632296843932409 ) ) ;
#92393=CARTESIAN_POINT ( 'NONE',  ( 60.31460910868286618, -60.00000000000004263, 109.8329304423809702 ) ) ;
#92395=CARTESIAN_POINT ( 'NONE',  ( 71.84765068926689935, -57.67113087382353598, -33.99244728326649323 ) ) ;
#92416=CARTESIAN_POINT ( 'NONE',  ( 32.74417656138047761, -42.96070844271284273, 34.86843745313173315 ) ) ;
#92429=CARTESIAN_POINT ( 'NONE',  ( 89.81584424423061819, -59.99999999999999289, -19.13689436224120044 ) ) ;
#92443=CARTESIAN_POINT ( 'NONE',  ( 85.70736671412652186, -60.21256416796455824, -14.76746838438766574 ) ) ;
#92448=ORIENTED_EDGE ( 'NONE', *, *, #34650, .T. ) ;
#92460=CARTESIAN_POINT ( 'NONE',  ( 76.96578608493661022, -39.49246347046180006, 129.2675137813639878 ) ) ;
#92464=AXIS2_PLACEMENT_3D ( 'NONE', #37904, #54554, #87493 ) ;
#92469=CARTESIAN_POINT ( 'NONE',  ( -93.88160267686131988, -57.67344353738141649, 16.36278552810739839 ) ) ;
#92473=CARTESIAN_POINT ( 'NONE',  ( 105.2955105692893767, -60.15122319160084885, 186.5850414784887903 ) ) ;
#92490=CARTESIAN_POINT ( 'NONE',  ( -85.61137192986321054, -30.00000000000000000, 175.7392374104872772 ) ) ;
#92494=CARTESIAN_POINT ( 'NONE',  ( 72.49335252660162610, -57.66551810483609586, 176.8856597097985457 ) ) ;
#92498=CARTESIAN_POINT ( 'NONE',  ( 37.56709637062468232, -32.17750619218406882, -37.66840575663092494 ) ) ;
#92502=CARTESIAN_POINT ( 'NONE',  ( -29.01163664099933825, -59.99999999999997868, 42.57063036807574719 ) ) ;
#92506=CARTESIAN_POINT ( 'NONE',  ( -85.76695094951085707, -50.18274658732842397, 190.4785943899394738 ) ) ;
#92509=CARTESIAN_POINT ( 'NONE',  ( -2.053642860964516981, -60.36585557917648970, 33.94789663158027793 ) ) ;
#92524=CARTESIAN_POINT ( 'NONE',  ( 110.2448519957423940, -60.00000000000004974, 128.1456905595833575 ) ) ;
#92525=CARTESIAN_POINT ( 'NONE',  ( -79.44753746119148730, -49.90808891599596819, 154.1174546483202903 ) ) ;
#92530=CARTESIAN_POINT ( 'NONE',  ( 22.32272541537730604, -57.67282817906140480, 42.57846511115439370 ) ) ;
#92551=CARTESIAN_POINT ( 'NONE',  ( 100.7596044958396106, -60.00000000000001421, 201.6406045078230136 ) ) ;
#92552=CARTESIAN_POINT ( 'NONE',  ( -81.10703223160209063, -14.21045842199456288, 192.6080781080067652 ) ) ;
#92553=CARTESIAN_POINT ( 'NONE',  ( 21.78139057835771553, -56.87475540586999756, 34.12209627113270471 ) ) ;
#92554=CARTESIAN_POINT ( 'NONE',  ( 83.10779110695617078, -38.00000000000002842, -10.21842127791309274 ) ) ;
#92556=CARTESIAN_POINT ( 'NONE',  ( -41.03595122651036320, -60.25878796785968206, 44.31288513920497252 ) ) ;
#92570=CARTESIAN_POINT ( 'NONE',  ( 97.20601475542966341, -29.99999999999981171, 191.0240291480905910 ) ) ;
#92574=CARTESIAN_POINT ( 'NONE',  ( 86.61511892060461548, -30.00000000000000355, 68.09894758470834120 ) ) ;
#92590=CARTESIAN_POINT ( 'NONE',  ( 75.54928104856406890, -38.35460038409268435, 174.6471884719728394 ) ) ;
#92612=CARTESIAN_POINT ( 'NONE',  ( 86.06184277206247657, -28.35162415433135763, 182.3406178006961227 ) ) ;
#92621=CARTESIAN_POINT ( 'NONE',  ( -90.12656837431330814, -29.99999999999999645, 89.23295766621065184 ) ) ;
#92635=CARTESIAN_POINT ( 'NONE',  ( 64.05557409813005165, -29.67380080880776561, -23.45134551522981425 ) ) ;
#92638=CARTESIAN_POINT ( 'NONE',  ( -22.50258514725704373, -39.47840698168496942, 31.31635883088512884 ) ) ;
#92642=CARTESIAN_POINT ( 'NONE',  ( -17.08789101759687767, -56.88345495196291779, 33.63599213401663945 ) ) ;
#92643=CARTESIAN_POINT ( 'NONE',  ( -38.36866069078110542, -24.37386123566381713, -30.62827207695247012 ) ) ;
#92653=CARTESIAN_POINT ( 'NONE',  ( -13.21548557454697281, -60.00000000000000000, -42.26782324170446259 ) ) ;
#92656=CARTESIAN_POINT ( 'NONE',  ( 101.3229910990397968, -52.73391794366923335, 193.0151051031019449 ) ) ;
#92658=CARTESIAN_POINT ( 'NONE',  ( 7.676252702269514394, -19.86679654487617341, 27.19205508634107460 ) ) ;
#92673=CARTESIAN_POINT ( 'NONE',  ( -93.13590452085961147, -60.00000000000967049, -17.97697602678234574 ) ) ;
#92679=CARTESIAN_POINT ( 'NONE',  ( -82.45890327043613865, -29.99999999999992184, -23.17447414549992146 ) ) ;
#92682=CARTESIAN_POINT ( 'NONE',  ( -51.13654845188015230, -46.44342577944571104, 55.14519627722154382 ) ) ;
#92692=CARTESIAN_POINT ( 'NONE',  ( 84.40671846796894329, -38.73973353392212005, 198.0806718234546508 ) ) ;
#92695=CARTESIAN_POINT ( 'NONE',  ( 87.41401970320464443, -30.00000000000000000, 185.1823391226513422 ) ) ;
#92701=CARTESIAN_POINT ( 'NONE',  ( 52.14939519039409532, -60.30582305101183493, 62.32281964044140921 ) ) ;
#92705=CARTESIAN_POINT ( 'NONE',  ( -85.43458966979623881, -38.35985982854320042, -22.44720385632372128 ) ) ;
#92709=CARTESIAN_POINT ( 'NONE',  ( 106.8991994874582190, -38.36537085630794053, 195.0165758976116308 ) ) ;
#92711=CARTESIAN_POINT ( 'NONE',  ( 84.42372515681569212, -45.28278671564551416, 28.58935177623963853 ) ) ;
#92714=SURFACE_SIDE_STYLE ('',( #59843 ) ) ;
#92731=CARTESIAN_POINT ( 'NONE',  ( 28.90468586868453471, -21.14203283741673545, 31.90548891044728919 ) ) ;
#92738=CARTESIAN_POINT ( 'NONE',  ( 83.57408830821859169, -42.98028180361450978, 179.4502539513921988 ) ) ;
#92743=CARTESIAN_POINT ( 'NONE',  ( -94.80169991939609986, -37.82085344593683374, 106.6770961138861367 ) ) ;
#92747=CARTESIAN_POINT ( 'NONE',  ( -23.24548731573063165, -27.04727666617280235, -38.41943903429619667 ) ) ;
#92749=CARTESIAN_POINT ( 'NONE',  ( 42.15184130795574902, -60.00000000000000000, 55.41083953232990211 ) ) ;
#92750=CARTESIAN_POINT ( 'NONE',  ( 27.02674341509898781, -30.42927322169125404, 39.08002995295369431 ) ) ;
#92755=CARTESIAN_POINT ( 'NONE',  ( -28.18961936475973573, -31.22569484158471909, 39.61244384221697601 ) ) ;
#92767=CARTESIAN_POINT ( 'NONE',  ( 57.64153548184016529, -60.22831400432175286, -30.33932336446891753 ) ) ;
#92778=CARTESIAN_POINT ( 'NONE',  ( -92.23564407392396447, -60.00000000000000000, 2.399895685214207930 ) ) ;
#92785=CARTESIAN_POINT ( 'NONE',  ( -81.72239385450473037, -53.48791114501855049, 179.5194371415524870 ) ) ;
#92795=CARTESIAN_POINT ( 'NONE',  ( -72.50181434431193850, -38.00000000001091394, -21.26203725901419261 ) ) ;
#92800=PRESENTATION_STYLE_ASSIGNMENT (( #9738 ) ) ;
#92803=CARTESIAN_POINT ( 'NONE',  ( 105.2982900294548614, -30.00000000000001066, 128.8790101386541096 ) ) ;
#92805=CARTESIAN_POINT ( 'NONE',  ( -71.69513722905418263, -59.99999999999990763, 172.8795092261717912 ) ) ;
#92806=CARTESIAN_POINT ( 'NONE',  ( -61.32617096396685952, -25.59081373081079747, 69.10494924817277251 ) ) ;
#92810=CARTESIAN_POINT ( 'NONE',  ( -102.7692820952204045, -45.26544015360205009, 186.5759103958386333 ) ) ;
#92811=PRESENTATION_STYLE_ASSIGNMENT (( #84727 ) ) ;
#92817=CARTESIAN_POINT ( 'NONE',  ( -76.66120007774280509, -59.99999999999997868, 189.5221980919927489 ) ) ;
#92826=CARTESIAN_POINT ( 'NONE',  ( -29.71626147859926448, -25.59364090554883120, 30.54361049305994058 ) ) ;
#92828=CARTESIAN_POINT ( 'NONE',  ( 45.67906931825459793, -56.80297510144281858, 49.30526560711538053 ) ) ;
#92832=CARTESIAN_POINT ( 'NONE',  ( -95.43172166446088056, -38.48744210534112398, 201.2268467534914862 ) ) ;
#92836=CARTESIAN_POINT ( 'NONE',  ( 62.91912717164011326, -60.00000000000000000, 90.67547237248358272 ) ) ;
#92844=CARTESIAN_POINT ( 'NONE',  ( 112.0489445181305683, -60.00000000000000000, 179.0880007768037103 ) ) ;
#92850=CARTESIAN_POINT ( 'NONE',  ( -81.23169817918467572, -30.00000000000000000, 0.5271219704189816779 ) ) ;
#92852=CARTESIAN_POINT ( 'NONE',  ( -77.60330327168814790, -38.52455064180648492, 186.9244840374806813 ) ) ;
#92863=CARTESIAN_POINT ( 'NONE',  ( 80.46043862466507335, -53.38907585616056650, 168.0494285789779383 ) ) ;
#92904=CARTESIAN_POINT ( 'NONE',  ( -108.2689893803878363, -60.00000000000000000, 195.1503591843108723 ) ) ;
#92910=CARTESIAN_POINT ( 'NONE',  ( -84.10481117900889103, -46.56341232157270582, 184.9836422536479006 ) ) ;
#92916=CARTESIAN_POINT ( 'NONE',  ( -82.45168481354632206, -37.83267541790726796, 9.374888728109986857 ) ) ;
#92925=CARTESIAN_POINT ( 'NONE',  ( 66.35352848486118660, -59.99999999999995737, 134.7740243497364645 ) ) ;
#92929=CARTESIAN_POINT ( 'NONE',  ( -87.61621634008581339, -14.21045842199436571, -10.69165924380367372 ) ) ;
#92930=CARTESIAN_POINT ( 'NONE',  ( -74.24509999404291705, -49.90998642872604307, 125.1187655734622126 ) ) ;
#92932=CARTESIAN_POINT ( 'NONE',  ( 74.93436731647082638, -29.99999999999996803, 156.1785850212263824 ) ) ;
#92934=CARTESIAN_POINT ( 'NONE',  ( 84.62951063988832345, -57.67093676639928645, -27.31841214351725355 ) ) ;
#92946=CARTESIAN_POINT ( 'NONE',  ( -53.16843670460360016, -59.99999999999020872, 87.15546671691542713 ) ) ;
#92961=CARTESIAN_POINT ( 'NONE',  ( 32.12746647248193455, -42.96020264381913734, 34.58970033397424260 ) ) ;
#92962=CARTESIAN_POINT ( 'NONE',  ( -5.820808985964939453, -8.673617379884035472E-16, 21.65942590380532451 ) ) ;
#92975=CARTESIAN_POINT ( 'NONE',  ( 92.55954463226689199, -60.00000000000000000, -10.73077478005948926 ) ) ;
#92983=CARTESIAN_POINT ( 'NONE',  ( -105.2209555712209976, -30.00000000000275691, 195.0728638946999638 ) ) ;
#92989=CARTESIAN_POINT ( 'NONE',  ( 84.67034172243197077, -52.74716631599819294, -13.90098049673125047 ) ) ;
#92999=SURFACE_STYLE_USAGE ( .BOTH. , #27249 ) ;
#93004=CARTESIAN_POINT ( 'NONE',  ( 71.58615475096345904, -60.32492746567568531, 120.7698757878210500 ) ) ;
#93009=CARTESIAN_POINT ( 'NONE',  ( -94.01586347659660703, -57.67588051021766660, 5.310313041227479935 ) ) ;
#93014=CARTESIAN_POINT ( 'NONE',  ( 101.7586560006743213, -37.84847941927726822, 185.3643445841708797 ) ) ;
#93019=CARTESIAN_POINT ( 'NONE',  ( -51.68662921661150023, -29.93083927907686004, 49.51763535396641913 ) ) ;
#93033=CARTESIAN_POINT ( 'NONE',  ( -89.02983586496698365, -30.00000000000000355, 188.7461324850866902 ) ) ;
#93038=CARTESIAN_POINT ( 'NONE',  ( 86.13252104161762190, -57.57606074614650993, 202.7608471217752140 ) ) ;
#93042=CARTESIAN_POINT ( 'NONE',  ( 38.01963658391477452, -32.32223440244047197, -37.62936076183553524 ) ) ;
#93045=CARTESIAN_POINT ( 'NONE',  ( -35.97666713092540647, -60.00000000000000711, 47.32977935146745097 ) ) ;
#93050=CARTESIAN_POINT ( 'NONE',  ( -86.18659369993858377, -42.85476313570202933, 188.6125987248406659 ) ) ;
#93053=CARTESIAN_POINT ( 'NONE',  ( -2.979541785652459751, -22.06772564117152058, 27.56319171407887936 ) ) ;
#93068=CARTESIAN_POINT ( 'NONE',  ( 104.6654747121523030, -30.00000000000000000, 124.7724495044359116 ) ) ;
#93069=CARTESIAN_POINT ( 'NONE',  ( -81.69435353299347469, -39.50040572665027128, 158.0323826615473592 ) ) ;
#93090=CARTESIAN_POINT ( 'NONE',  ( -94.89844962927027439, -60.00000000000001421, 205.0338773334991060 ) ) ;
#93091=CARTESIAN_POINT ( 'NONE',  ( 21.87256311572295076, -60.35484851998849365, 34.71956232952695842 ) ) ;
#93095=CARTESIAN_POINT ( 'NONE',  ( -36.77948966406264475, -56.82339243700149467, 39.80873089715750268 ) ) ;
#93107=CARTESIAN_POINT ( 'NONE',  ( 97.69330145236169471, -30.00000000000014921, 190.7792052488607908 ) ) ;
#93111=CARTESIAN_POINT ( 'NONE',  ( 84.99074402005219042, -30.00000000000000711, 57.64709464612924705 ) ) ;
#93130=CARTESIAN_POINT ( 'NONE',  ( 71.86920016943035705, -38.32705086600410027, 145.1004257776124291 ) ) ;
#93153=CARTESIAN_POINT ( 'NONE',  ( 86.60070351626397667, -39.13477975523821328, 188.3070256512509104 ) ) ;
#93158=VERTEX_POINT ( 'NONE', #7501 ) ;
#93164=CARTESIAN_POINT ( 'NONE',  ( -81.86398423121568158, -29.99999999999999645, 32.54976024431884696 ) ) ;
#93168=CARTESIAN_POINT ( 'NONE',  ( 32.58266151836870250, -57.69062872889872295, 46.99190750165519859 ) ) ;
#93171=CARTESIAN_POINT ( 'NONE',  ( -43.37300451664871304, -36.38839727959540937, 41.06639963762513190 ) ) ;
#93175=CARTESIAN_POINT ( 'NONE',  ( 48.74245842222025260, -27.20503387118322181, -28.29543663440009738 ) ) ;
#93176=CARTESIAN_POINT ( 'NONE',  ( -26.01996383795994205, -22.09242311380402057, 28.98075328728764788 ) ) ;
#93182=CARTESIAN_POINT ( 'NONE',  ( -18.79090678414550908, -29.03354218681774412, 29.12109915567513596 ) ) ;
#93194=CARTESIAN_POINT ( 'NONE',  ( 1.405425595346621037E-06, -60.00000000000000000, -42.63907915653317104 ) ) ;
#93196=CARTESIAN_POINT ( 'NONE',  ( 99.03177814179444738, -37.80525585742561390, 191.8580698190465625 ) ) ;
#93204=EDGE_CURVE ( 'NONE', #93532, #71278, #39381, .T. ) ;
#93212=CARTESIAN_POINT ( 'NONE',  ( -85.79013029828182368, -59.99999999998781419, -26.89979960300323469 ) ) ;
#93218=CARTESIAN_POINT ( 'NONE',  ( -86.58264346576902426, -59.99999999999995737, -26.28034805200384838 ) ) ;
#93220=CARTESIAN_POINT ( 'NONE',  ( -50.24583591853911457, -60.30222183590655050, 58.32363953540177448 ) ) ;
#93230=CARTESIAN_POINT ( 'NONE',  ( 75.51533756583152979, -30.00000000000000000, -27.33238513093788669 ) ) ;
#93235=CARTESIAN_POINT ( 'NONE',  ( 90.25683128961706814, -29.99999999999999645, 190.0668461241068030 ) ) ;
#93241=CARTESIAN_POINT ( 'NONE',  ( 54.51536369449565456, -46.43638089579248174, 62.03764367210229835 ) ) ;
#93245=CARTESIAN_POINT ( 'NONE',  ( -86.94600573690735246, -38.36377377443699288, -20.89387357848544369 ) ) ;
#93249=CARTESIAN_POINT ( 'NONE',  ( 110.3745256113219284, -38.35605052074757282, 158.9612946903319823 ) ) ;
#93251=CARTESIAN_POINT ( 'NONE',  ( 86.42351163725670915, -60.14453129240431650, 21.61429144264777946 ) ) ;
#93273=CARTESIAN_POINT ( 'NONE',  ( -7.749805355827879438, -13.26271386457699997, 32.00645959793580886 ) ) ;
#93279=CARTESIAN_POINT ( 'NONE',  ( 86.15856653264481224, -21.41364612637495668, 176.4187449916978210 ) ) ;
#93285=CARTESIAN_POINT ( 'NONE',  ( -98.00753366316151016, -52.71031723798989077, 110.7941533929202507 ) ) ;
#93289=CARTESIAN_POINT ( 'NONE',  ( -18.69161154690413795, -25.36093076282173087, -38.50044509632451906 ) ) ;
#93292=CARTESIAN_POINT ( 'NONE',  ( 40.53591651757645309, -60.00000000000000000, 52.85790476262030779 ) ) ;
#93294=CARTESIAN_POINT ( 'NONE',  ( 33.80992109950155111, -34.85164080663998476, 43.18581089266367457 ) ) ;
#93297=CARTESIAN_POINT ( 'NONE',  ( -37.27179927782982816, -36.61903506054549240, 46.51218512112991021 ) ) ;
#93307=CARTESIAN_POINT ( 'NONE',  ( -2.090939542649697280, -60.00000000000000711, 39.63613289865730849 ) ) ;
#93312=CARTESIAN_POINT ( 'NONE',  ( 3.211837540737783936, -60.22813567888628938, -36.90749154621568096 ) ) ;
#93320=CARTESIAN_POINT ( 'NONE',  ( -92.28312636555040172, -59.99999999999999289, 23.72048675611388546 ) ) ;
#93328=CARTESIAN_POINT ( 'NONE',  ( -85.45028039093672589, -18.58812102731535632, 159.4271763632907835 ) ) ;
#93334=( BOUNDED_SURFACE ( )  B_SPLINE_SURFACE ( 2, 3, ( 
 ( #44534, #86603, #102224, #68269, #27324, #60204, #77953, #12668, #28922, #36476, #92530, #76341, #100622, #12142, #19239, #43990, #43465, #52069, #84984, #4068, #20303, #28373, #11066, #76877, #78475, #53153, #61250, #2990, #26784, #94691, #59653, #94134, #77422, #45598, #53669, #69866, #3538, #18684, #51540, #84454, #35944, #68814, #101697, #27857, #93613, #87120, #62316, #95209, #47160, #7229, #70919, #6706, #62840, #30483, #71978, #96795, #46124, #104888, #104334, #21341, #55248, #47686, #39633, #22404, #29443, #6167, #63909, #64433, #105409, #13194, #14791, #70398, #95731, #89233, #103811, #31550, #54179, #79010, #97304, #55763, #5130, #21871, #38063, #48217, #80584, #22927, #72504, #5648, #81120, #87648, #29956, #23459, #54711, #103297, #13730, #46638, #79535, #88696, #38572, #71433, #88172, #63381, #56294, #15330, #96278, #14256, #80057, #39098, #31028, #49275, #57900, #50866, #48740, #16389, #64947, #83249, #8295, #91878, #91362, #98883, #695, #41201, #49818, #40665, #42252, #90824, #65484, #40139, #33136, #16940, #25044, #26135, #73549, #74087, #82179, #82723, #98373, #173, #106453, #41731, #1238, #8827, #74615, #66006, #32611, #57366, #67080, #24526, #99963, #90285, #33660, #66539, #99413, #18005, #25595, #58453, #17477, #50339, #9342, #73016, #75143, #83771, #34208, #58990, #105921, #81633, #7757, #32073, #97839, #24000, #56840, #89765, #15862, #92934, #10932, #77292, #102084, #68686, #43853, #19634, #12009, #92395, #43331, #53014, #76743, #77826, #18544, #36867, #2853, #51408, #60597, #20707, #101566, #84320, #28245, #3404, #52467, #85385, #2318, #69217, #68131, #94556 ),
 ( #61115, #9882, #35263, #28784, #10416, #44942, #100492, #26649, #3935, #94002, #76212, #101027, #53545, #51936, #35807, #93485, #27724, #59526, #27181, #85938, #69735, #11468, #60072, #61666, #102626, #44396, #42793, #36347, #19096, #84849, #20164, #75686, #1785, #34742, #67613, #78340, #62198, #23317, #71834, #4997, #29830, #103163, #29308, #45990, #104740, #6035, #88043, #95084, #86991, #64298, #38958, #14123, #78870, #12532, #47556, #86476, #55113, #104202, #72371, #80452, #55629, #5520, #6563, #97170, #22794, #63239, #38443, #21216, #105277, #37928, #54046, #4458, #37401, #96131, #45467, #13059, #88566, #70790, #46508, #47024, #30890, #103686, #79926, #13594, #70262, #71309, #63771, #14647, #30346, #62707, #22264, #96659, #39496, #31423, #95598, #21736, #54575, #87514, #79404, #56705, #91240, #40014, #72886, #17347, #41605, #31936, #7618, #23861, #34082, #66403, #8697, #99284, #98239, #66954, #73416, #105797, #50222, #32477, #64816, #82592, #97697, #74488, #41073, #16257, #99833, #106313, #25463, #8167, #16800, #89628, #58315, #15728, #65877, #75012, #48613, #7099, #49142, #42126, #563, #81498, #40536, #56154, #83123, #33531, #9218, #24395, #89098, #65348, #57234, #1106, #90152, #82043, #15192, #73957, #48081, #38, #33010, #80983, #98756, #24910, #57764, #49686, #90690, #29577, #100364, #37134, #46259, #59401, #83641, #20447, #13333, #12809, #92262, #71056, #69477, #28509, #4205, #61393, #42663, #75562, #70537, #62449, #86210, #9746, #79145, #103428, #78086, #5271, #29065, #67485, #18416, #26528, #4736, #38196, #95340, #70000, #17877, #1657, #26005, #45723, #52744, #77565 ),
 ( #34615, #85667, #58868, #53805, #61935, #11740, #91758, #21476, #50731, #102901, #45212, #44678, #54311, #87258, #53289, #3680, #36612, #102362, #94825, #12282, #94282, #20971, #86734, #78605, #37675, #22002, #80725, #40806, #104480, #40279, #96413, #64050, #105544, #23596, #79676, #31682, #31165, #95878, #88835, #81252, #73155, #55900, #62976, #39767, #97435, #97983, #32208, #46782, #48360, #103947, #22544, #16007, #30626, #65086, #87785, #13868, #24138, #89377, #5786, #55385, #72642, #88315, #96925, #63514, #64568, #56981, #6843, #56444, #6301, #14390, #47301, #89895, #80197, #48883, #39241, #72115, #23061, #105025, #81777, #15467, #14929, #47821, #7367, #106056, #30093, #7900, #54855, #38708, #71572, #25192, #82330, #41341, #17618, #99568, #100639, #18154, #51010, #92551, #49960, #74758, #34356, #59136, #25747, #838, #83392, #75836, #49426, #310, #10038, #33810, #34884, #8440, #26799, #66687, #74233, #50480, #84469, #58602, #33277, #92018, #67231, #9489, #42400, #66147, #26273, #58050, #51555, #8964, #75296, #98507, #67752, #1389, #42945, #1933, #59669, #99029, #82868, #83927, #18699, #10564, #73700, #100108, #106602, #65625, #32752, #24657, #57509, #90432, #90972, #16535, #17083, #41870, #91505, #61266, #2469, #20857, #37551, #69883, #27878, #87139, #61815, #28393, #52616, #94155, #54200, #52088, #19783, #68287, #86622, #11624, #95228, #94708, #102241, #4087, #44554, #53171, #44010, #45618, #20326, #68833, #43479, #36494, #86088, #12160, #29463, #76897, #77441, #85543, #3556, #3011, #60743, #70419, #35963, #103315, #101712, #93632, #69362, #45090, #21360, #77969, #37015, #102777 ) ),
 .UNSPECIFIED., .F., .F., .T. ) 
 B_SPLINE_SURFACE_WITH_KNOTS ( ( 3, 3 ),
 ( 4, 2, 2, 2, 2, 2, 2, 2, 2, 2, 2, 2, 2, 2, 2, 2, 2, 2, 2, 2, 2, 2, 2, 2, 2, 2, 2, 2, 2, 2, 2, 2, 2, 2, 2, 2, 2, 2, 2, 2, 2, 2, 2, 2, 2, 2, 2, 2, 2, 2, 2, 2, 2, 2, 2, 2, 2, 2, 2, 2, 2, 2, 2, 2, 2, 2, 2, 2, 2, 2, 2, 2, 2, 2, 2, 2, 2, 2, 2, 2, 2, 2, 2, 2, 2, 2, 2, 2, 2, 2, 2, 2, 2, 2, 2, 2, 2, 2, 2, 2, 4 ),
 ( 0.000000000000000000, 1.000000000000000000 ),
 ( 0.000000000000000000, 0.008518889176590353426, 0.01277833376488552927, 0.01703777835318070685, 0.02129722294147588096, 0.02342694523562346975, 0.02555666752977105854, 0.02981611211806623613, 0.03088097326514003052, 0.03194583441221382492, 0.03407555670636141371, 0.03833500129465658435, 0.04046472358880417314, 0.04259444588295176193, 0.04685389047124693951, 0.05111333505954211709, 0.05537277964783729467, 0.05963222423613247225, 0.06389166882442764983, 0.06815111341272282741, 0.07667000258931316869, 0.08518889176590352386, 0.1022266701190842342, 0.1363022268254456548, 0.1533400051786263374, 0.1618588943552166926, 0.1703777835318070477, 0.1746372281201022392, 0.1788966727083974029, 0.1831561172966925666, 0.1874155618849877580, 0.1895452841791353538, 0.1916750064732829495, 0.1938047287674305452, 0.1948695899145043153, 0.1959344510615781132, 0.1980641733557256812, 0.2001938956498732769, 0.2012587567969470748, 0.2023236179440208726, 0.2044533402381684684, 0.2065830625323160641, 0.2087127848264636598, 0.2108425071206112555, 0.2129722294147588235, 0.2140370905618326214, 0.2151019517089063915, 0.2172316740030539872, 0.2182965351501277851, 0.2193613962972015830, 0.2214911185913491787, 0.2225559797384229765, 0.2236208408854967744, 0.2257505631796443701, 0.2278802854737919659, 0.2300100077679395338, 0.2342694523562346975, 0.2363991746503822933, 0.2385288969445298890, 0.2427883415328250805, 0.2470477861211202442, 0.2555666752977105993, 0.2598261198860057908, 0.2640855644743009822, 0.2726044536508913096, 0.2896422320040720200, 0.3066800103572526748, 0.3407555670636140954, 0.3577933454167948057, 0.3748311237699755161, 0.3918689021231562264, 0.4003877912997465538, 0.4089066804763369367, 0.4131661250646321282, 0.4174255696529273196, 0.4216850142412225111, 0.4259444588295176470, 0.4302039034178127830, 0.4344633480061079744, 0.4365930703002555702, 0.4387227925944031659, 0.4429822371826983574, 0.4440470983297721830, 0.4451119594768459531, 0.4472416817709935488, 0.4515011263592887403, 0.4557605709475839317, 0.4600200155358790677, 0.4621497378300266634, 0.4642794601241742036, 0.4685389047124693951, 0.4770577938890597780, 0.4855766830656501609, 0.4898361276539453524, 0.4940955722422404883, 0.5026144614188308157, 0.5111333505954211986, 0.5196522397720115816, 0.5281711289486019645, 0.5366900181251923474, 0.5452089073017826193 ),
 .UNSPECIFIED. ) 
 GEOMETRIC_REPRESENTATION_ITEM ( )  RATIONAL_B_SPLINE_SURFACE ( (
 ( 1.000000000000000000, 1.000000000000000000, 1.000000000000000000, 1.000000000000000000, 1.000000000000000000, 1.000000000000000000, 1.000000000000000000, 1.000000000000000000, 1.000000000000000000, 1.000000000000000000, 1.000000000000000000, 1.000000000000000000, 1.000000000000000000, 1.000000000000000000, 1.000000000000000000, 1.000000000000000000, 1.000000000000000000, 1.000000000000000000, 1.000000000000000000, 1.000000000000000000, 1.000000000000000000, 1.000000000000000000, 1.000000000000000000, 1.000000000000000000, 1.000000000000000000, 1.000000000000000000, 1.000000000000000000, 1.000000000000000000, 1.000000000000000000, 1.000000000000000000, 1.000000000000000000, 1.000000000000000000, 1.000000000000000000, 1.000000000000000000, 1.000000000000000000, 1.000000000000000000, 1.000000000000000000, 1.000000000000000000, 1.000000000000000000, 1.000000000000000000, 1.000000000000000000, 1.000000000000000000, 1.000000000000000000, 1.000000000000000000, 1.000000000000000000, 1.000000000000000000, 1.000000000000000000, 1.000000000000000000, 1.000000000000000000, 1.000000000000000000, 1.000000000000000000, 1.000000000000000000, 1.000000000000000000, 1.000000000000000000, 1.000000000000000000, 1.000000000000000000, 1.000000000000000000, 1.000000000000000000, 1.000000000000000000, 1.000000000000000000, 1.000000000000000000, 1.000000000000000000, 1.000000000000000000, 1.000000000000000000, 1.000000000000000000, 1.000000000000000000, 1.000000000000000000, 1.000000000000000000, 1.000000000000000000, 1.000000000000000000, 1.000000000000000000, 1.000000000000000000, 1.000000000000000000, 1.000000000000000000, 1.000000000000000000, 1.000000000000000000, 1.000000000000000000, 1.000000000000000000, 1.000000000000000000, 1.000000000000000000, 1.000000000000000000, 1.000000000000000000, 1.000000000000000000, 1.000000000000000000, 1.000000000000000000, 1.000000000000000000, 1.000000000000000000, 1.000000000000000000, 1.000000000000000000, 1.000000000000000000, 1.000000000000000000, 1.000000000000000000, 1.000000000000000000, 1.000000000000000000, 1.000000000000000000, 1.000000000000000000, 1.000000000000000000, 1.000000000000000000, 1.000000000000000000, 1.000000000000000000, 1.000000000000000000, 1.000000000000000000, 1.000000000000000000, 1.000000000000000000, 1.000000000000000000, 1.000000000000000000, 1.000000000000000000, 1.000000000000000000, 1.000000000000000000, 1.000000000000000000, 1.000000000000000000, 1.000000000000000000, 1.000000000000000000, 1.000000000000000000, 1.000000000000000000, 1.000000000000000000, 1.000000000000000000, 1.000000000000000000, 1.000000000000000000, 1.000000000000000000, 1.000000000000000000, 1.000000000000000000, 1.000000000000000000, 1.000000000000000000, 1.000000000000000000, 1.000000000000000000, 1.000000000000000000, 1.000000000000000000, 1.000000000000000000, 1.000000000000000000, 1.000000000000000000, 1.000000000000000000, 1.000000000000000000, 1.000000000000000000, 1.000000000000000000, 1.000000000000000000, 1.000000000000000000, 1.000000000000000000, 1.000000000000000000, 1.000000000000000000, 1.000000000000000000, 1.000000000000000000, 1.000000000000000000, 1.000000000000000000, 1.000000000000000000, 1.000000000000000000, 1.000000000000000000, 1.000000000000000000, 1.000000000000000000, 1.000000000000000000, 1.000000000000000000, 1.000000000000000000, 1.000000000000000000, 1.000000000000000000, 1.000000000000000000, 1.000000000000000000, 1.000000000000000000, 1.000000000000000000, 1.000000000000000000, 1.000000000000000000, 1.000000000000000000, 1.000000000000000000, 1.000000000000000000, 1.000000000000000000, 1.000000000000000000, 1.000000000000000000, 1.000000000000000000, 1.000000000000000000, 1.000000000000000000, 1.000000000000000000, 1.000000000000000000, 1.000000000000000000, 1.000000000000000000, 1.000000000000000000, 1.000000000000000000, 1.000000000000000000, 1.000000000000000000, 1.000000000000000000, 1.000000000000000000, 1.000000000000000000, 1.000000000000000000, 1.000000000000000000, 1.000000000000000000, 1.000000000000000000, 1.000000000000000000, 1.000000000000000000, 1.000000000000000000, 1.000000000000000000, 1.000000000000000000, 1.000000000000000000, 1.000000000000000000, 1.000000000000000000, 1.000000000000000000, 1.000000000000000000, 1.000000000000000000, 1.000000000000000000, 1.000000000000000000, 1.000000000000000000, 1.000000000000000000, 1.000000000000000000, 1.000000000000000000, 1.000000000000000000),
 ( 1.857142857142858317, 1.857142857142858317, 1.857142857142858317, 1.857142857142858317, 1.857142857142858317, 1.857142857142858317, 1.857142857142858317, 1.857142857142858317, 1.857142857142858317, 1.857142857142858317, 1.857142857142858317, 1.857142857142858317, 1.857142857142858317, 1.857142857142858317, 1.857142857142858317, 1.857142857142858317, 1.857142857142858317, 1.857142857142858317, 1.857142857142858317, 1.857142857142858317, 1.857142857142858317, 1.857142857142858317, 1.857142857142859205, 1.857142857142859205, 1.857142857142858317, 1.857142857142858317, 1.857142857142858317, 1.857142857142858317, 1.857142857142858317, 1.857142857142858317, 1.857142857142858317, 1.857142857142858317, 1.857142857142858317, 1.857142857142858317, 1.857142857142858317, 1.857142857142858317, 1.857142857142858317, 1.857142857142858317, 1.857142857142858317, 1.857142857142858317, 1.857142857142858317, 1.857142857142858317, 1.857142857142858317, 1.857142857142858317, 1.857142857142858317, 1.857142857142858317, 1.857142857142858317, 1.857142857142858317, 1.857142857142858317, 1.857142857142858317, 1.857142857142858317, 1.857142857142858317, 1.857142857142858317, 1.857142857142858317, 1.857142857142858317, 1.857142857142858317, 1.857142857142858317, 1.857142857142858317, 1.857142857142858317, 1.857142857142858317, 1.857142857142858317, 1.857142857142858317, 1.857142857142858317, 1.857142857142858317, 1.857142857142858317, 1.857142857142858317, 1.857142857142858317, 1.857142857142858317, 1.857142857142858317, 1.857142857142858317, 1.857142857142858317, 1.857142857142858317, 1.857142857142858317, 1.857142857142858317, 1.857142857142858317, 1.857142857142858317, 1.857142857142858317, 1.857142857142858317, 1.857142857142858317, 1.857142857142858317, 1.857142857142858317, 1.857142857142858317, 1.857142857142858317, 1.857142857142858317, 1.857142857142858317, 1.857142857142858317, 1.857142857142858317, 1.857142857142858317, 1.857142857142858317, 1.857142857142858317, 1.857142857142858317, 1.857142857142858317, 1.857142857142858317, 1.857142857142858317, 1.857142857142858317, 1.857142857142858317, 1.857142857142858317, 1.857142857142858317, 1.857142857142858317, 1.857142857142858317, 1.857142857142858317, 1.857142857142858317, 1.857142857142858317, 1.857142857142858317, 1.857142857142858317, 1.857142857142858317, 1.857142857142858317, 1.857142857142858317, 1.857142857142858317, 1.857142857142858317, 1.857142857142858317, 1.857142857142858317, 1.857142857142858317, 1.857142857142858317, 1.857142857142858317, 1.857142857142858317, 1.857142857142858317, 1.857142857142858317, 1.857142857142858317, 1.857142857142858317, 1.857142857142858317, 1.857142857142858317, 1.857142857142858317, 1.857142857142858317, 1.857142857142858317, 1.857142857142858317, 1.857142857142858317, 1.857142857142858317, 1.857142857142858317, 1.857142857142858317, 1.857142857142858317, 1.857142857142858317, 1.857142857142858317, 1.857142857142858317, 1.857142857142858317, 1.857142857142858317, 1.857142857142858317, 1.857142857142858317, 1.857142857142858317, 1.857142857142858317, 1.857142857142858317, 1.857142857142858317, 1.857142857142858317, 1.857142857142858317, 1.857142857142858317, 1.857142857142858317, 1.857142857142858317, 1.857142857142858317, 1.857142857142858317, 1.857142857142858317, 1.857142857142858317, 1.857142857142858317, 1.857142857142858317, 1.857142857142858317, 1.857142857142858317, 1.857142857142858317, 1.857142857142858317, 1.857142857142858317, 1.857142857142858317, 1.857142857142858317, 1.857142857142858317, 1.857142857142858317, 1.857142857142859205, 1.857142857142859205, 1.857142857142858317, 1.857142857142858317, 1.857142857142858317, 1.857142857142858317, 1.857142857142858317, 1.857142857142858317, 1.857142857142858317, 1.857142857142858317, 1.857142857142858317, 1.857142857142858317, 1.857142857142858317, 1.857142857142858317, 1.857142857142858317, 1.857142857142858317, 1.857142857142858317, 1.857142857142858317, 1.857142857142857428, 1.857142857142857428, 1.857142857142858317, 1.857142857142858317, 1.857142857142858317, 1.857142857142858317, 1.857142857142856318, 1.857142857142856318, 1.857142857142858317, 1.857142857142858317, 1.857142857142858317, 1.857142857142858317, 1.857142857142858317, 1.857142857142858317, 1.857142857142858317, 1.857142857142858317, 1.857142857142858317, 1.857142857142858317, 1.857142857142858317, 1.857142857142858317, 1.857142857142858317, 1.857142857142858317),
 ( 1.000000000000000000, 1.000000000000000000, 1.000000000000000000, 1.000000000000000000, 1.000000000000000000, 1.000000000000000000, 1.000000000000000000, 1.000000000000000000, 1.000000000000000000, 1.000000000000000000, 1.000000000000000000, 1.000000000000000000, 1.000000000000000000, 1.000000000000000000, 1.000000000000000000, 1.000000000000000000, 1.000000000000000000, 1.000000000000000000, 1.000000000000000000, 1.000000000000000000, 1.000000000000000000, 1.000000000000000000, 1.000000000000000000, 1.000000000000000000, 1.000000000000000000, 1.000000000000000000, 1.000000000000000000, 1.000000000000000000, 1.000000000000000000, 1.000000000000000000, 1.000000000000000000, 1.000000000000000000, 1.000000000000000000, 1.000000000000000000, 1.000000000000000000, 1.000000000000000000, 1.000000000000000000, 1.000000000000000000, 1.000000000000000000, 1.000000000000000000, 1.000000000000000000, 1.000000000000000000, 1.000000000000000000, 1.000000000000000000, 1.000000000000000000, 1.000000000000000000, 1.000000000000000000, 1.000000000000000000, 1.000000000000000000, 1.000000000000000000, 1.000000000000000000, 1.000000000000000000, 1.000000000000000000, 1.000000000000000000, 1.000000000000000000, 1.000000000000000000, 1.000000000000000000, 1.000000000000000000, 1.000000000000000000, 1.000000000000000000, 1.000000000000000000, 1.000000000000000000, 1.000000000000000000, 1.000000000000000000, 1.000000000000000000, 1.000000000000000000, 1.000000000000000000, 1.000000000000000000, 1.000000000000000000, 1.000000000000000000, 1.000000000000000000, 1.000000000000000000, 1.000000000000000000, 1.000000000000000000, 1.000000000000000000, 1.000000000000000000, 1.000000000000000000, 1.000000000000000000, 1.000000000000000000, 1.000000000000000000, 1.000000000000000000, 1.000000000000000000, 1.000000000000000000, 1.000000000000000000, 1.000000000000000000, 1.000000000000000000, 1.000000000000000000, 1.000000000000000000, 1.000000000000000000, 1.000000000000000000, 1.000000000000000000, 1.000000000000000000, 1.000000000000000000, 1.000000000000000000, 1.000000000000000000, 1.000000000000000000, 1.000000000000000000, 1.000000000000000000, 1.000000000000000000, 1.000000000000000000, 1.000000000000000000, 1.000000000000000000, 1.000000000000000000, 1.000000000000000000, 1.000000000000000000, 1.000000000000000000, 1.000000000000000000, 1.000000000000000000, 1.000000000000000000, 1.000000000000000000, 1.000000000000000000, 1.000000000000000000, 1.000000000000000000, 1.000000000000000000, 1.000000000000000000, 1.000000000000000000, 1.000000000000000000, 1.000000000000000000, 1.000000000000000000, 1.000000000000000000, 1.000000000000000000, 1.000000000000000000, 1.000000000000000000, 1.000000000000000000, 1.000000000000000000, 1.000000000000000000, 1.000000000000000000, 1.000000000000000000, 1.000000000000000000, 1.000000000000000000, 1.000000000000000000, 1.000000000000000000, 1.000000000000000000, 1.000000000000000000, 1.000000000000000000, 1.000000000000000000, 1.000000000000000000, 1.000000000000000000, 1.000000000000000000, 1.000000000000000000, 1.000000000000000000, 1.000000000000000000, 1.000000000000000000, 1.000000000000000000, 1.000000000000000000, 1.000000000000000000, 1.000000000000000000, 1.000000000000000000, 1.000000000000000000, 1.000000000000000000, 1.000000000000000000, 1.000000000000000000, 1.000000000000000000, 1.000000000000000000, 1.000000000000000000, 1.000000000000000000, 1.000000000000000000, 1.000000000000000000, 1.000000000000000000, 1.000000000000000000, 1.000000000000000000, 1.000000000000000000, 1.000000000000000000, 1.000000000000000000, 1.000000000000000000, 1.000000000000000000, 1.000000000000000000, 1.000000000000000000, 1.000000000000000000, 1.000000000000000000, 1.000000000000000000, 1.000000000000000000, 1.000000000000000000, 1.000000000000000000, 1.000000000000000000, 1.000000000000000000, 1.000000000000000000, 1.000000000000000000, 1.000000000000000000, 1.000000000000000000, 1.000000000000000000, 1.000000000000000000, 1.000000000000000000, 1.000000000000000000, 1.000000000000000000, 1.000000000000000000, 1.000000000000000000, 1.000000000000000000, 1.000000000000000000, 1.000000000000000000, 1.000000000000000000, 1.000000000000000000, 1.000000000000000000, 1.000000000000000000, 1.000000000000000000, 1.000000000000000000, 1.000000000000000000, 1.000000000000000000, 1.000000000000000000, 1.000000000000000000, 1.000000000000000000, 1.000000000000000000) ) ) 
 REPRESENTATION_ITEM ( '' )  SURFACE ( )  );
#93342=ORIENTED_EDGE ( 'NONE', *, *, #95943, .T. ) ;
#93344=CARTESIAN_POINT ( 'NONE',  ( -83.74719587345013849, -57.67098913794580994, -27.91190304260424071 ) ) ;
#93352=CARTESIAN_POINT ( 'NONE',  ( 101.2959083255158390, -29.99999999999995026, 104.2725399938968707 ) ) ;
#93353=CARTESIAN_POINT ( 'NONE',  ( -79.87726071770381964, -29.99999999999996092, 191.0765191543576407 ) ) ;
#93354=CARTESIAN_POINT ( 'NONE',  ( -57.84996654388071846, -60.33641506065911386, 76.30861162968490419 ) ) ;
#93358=CARTESIAN_POINT ( 'NONE',  ( -104.9459564440097381, -60.15519249609457830, 188.0231784350408475 ) ) ;
#93369=CARTESIAN_POINT ( 'NONE',  ( 11.24487389204834997, 0.000000000000000000, 12.81917055448515619 ) ) ;
#93376=CARTESIAN_POINT ( 'NONE',  ( -31.02080448264273826, -22.13447804649420547, 30.33493143269389947 ) ) ;
#93379=CARTESIAN_POINT ( 'NONE',  ( 44.56484537913603106, -29.16031456794998888, 40.40432702718549507 ) ) ;
#93385=CARTESIAN_POINT ( 'NONE',  ( -89.02571210877493968, -38.53235496327626919, 200.2987166445973344 ) ) ;
#93397=CARTESIAN_POINT ( 'NONE',  ( 112.2015293769591580, -60.00000000000000711, 175.2242769347896569 ) ) ;
#93402=CARTESIAN_POINT ( 'NONE',  ( -81.57395695671810643, -30.00000000000003908, -8.068917339165949443 ) ) ;
#93404=CARTESIAN_POINT ( 'NONE',  ( -62.80366873856288379, -38.34034637481484253, 105.3709165728642603 ) ) ;
#93413=CARTESIAN_POINT ( 'NONE',  ( 79.80183204735519098, -60.35092112530382025, 173.0457402211850138 ) ) ;
#93460=CARTESIAN_POINT ( 'NONE',  ( -101.8030891146729289, -60.00000000000000000, 201.2278047307587201 ) ) ;
#93466=CARTESIAN_POINT ( 'NONE',  ( -86.18086450786695707, -21.36838705098882230, 176.9395935000053441 ) ) ;
#93471=CARTESIAN_POINT ( 'NONE',  ( -85.33252481412877444, -52.70932741134135568, 1.350972571353141971 ) ) ;
#93478=CARTESIAN_POINT ( 'NONE',  ( 62.54367487775790124, -59.99999999999994316, 118.0935059193921575 ) ) ;
#93480=CARTESIAN_POINT ( 'NONE',  ( -82.45890327043613865, -29.99999999999992184, -23.17447414549992146 ) ) ;
#93481=CARTESIAN_POINT ( 'NONE',  ( -69.00208524908248364, -32.53704488351955604, 94.70596908067794573 ) ) ;
#93483=CARTESIAN_POINT ( 'NONE',  ( 78.95048871113250755, -29.99999999999999645, 188.4614743794136871 ) ) ;
#93485=CARTESIAN_POINT ( 'NONE',  ( 28.72931389660035251, -59.99999999999750599, 45.02702490174896610 ) ) ;
#93498=CARTESIAN_POINT ( 'NONE',  ( -75.70276281760169468, -59.99999999999019451, 193.8926945017304888 ) ) ;
#93503=CARTESIAN_POINT ( 'NONE',  ( 11.17734400176826171, -4.285714285714296246, -22.67073868809949033 ) ) ;
#93512=CARTESIAN_POINT ( 'NONE',  ( 31.39243574302858519, -29.07687128735913618, 31.74798812421044403 ) ) ;
#93523=CARTESIAN_POINT ( 'NONE',  ( 92.01402115998416775, -60.00000000000000000, 5.925301312853033409 ) ) ;
#93531=CARTESIAN_POINT ( 'NONE',  ( -109.1611028234465692, -29.99999999994022559, 160.9843952204544735 ) ) ;
#93532=VERTEX_POINT ( 'NONE', #36628 ) ;
#93537=CARTESIAN_POINT ( 'NONE',  ( 86.24207113919420920, -60.22626128449206107, -13.36701399825027181 ) ) ;
#93550=CARTESIAN_POINT ( 'NONE',  ( 70.97006384286886771, -39.48593960573443695, 105.0516801013103105 ) ) ;
#93554=CARTESIAN_POINT ( 'NONE',  ( -84.33710589588049800, -57.55216090540037044, 201.9444809301270141 ) ) ;
#93558=CARTESIAN_POINT ( 'NONE',  ( 103.4806006637074489, -45.28272409703987478, 182.5790420555011053 ) ) ;
#93563=CARTESIAN_POINT ( 'NONE',  ( -49.78251962175088607, -29.64715986801754610, 46.26550681513847252 ) ) ;
#93575=CARTESIAN_POINT ( 'NONE',  ( -85.49392800990823105, -30.00000000000000355, 174.7729343606026475 ) ) ;
#93579=CARTESIAN_POINT ( 'NONE',  ( 81.11165248383676385, -57.51401271914193813, 199.8270164379141249 ) ) ;
#93581=CARTESIAN_POINT ( 'NONE',  ( 37.51403724872147194, -32.16046718318631292, -37.67293210278931781 ) ) ;
#93584=CARTESIAN_POINT ( 'NONE',  ( -66.45734036689610491, -60.00000000000001421, 124.2522409290889271 ) ) ;
#93585=CARTESIAN_POINT ( 'NONE',  ( -86.63543225537370063, -20.69559410499708818, 184.5538921392410430 ) ) ;
#93589=CARTESIAN_POINT ( 'NONE',  ( -4.087803312211714335, -49.92081496441304012, 32.20210259524810681 ) ) ;
#93598=AXIS2_PLACEMENT_3D ( 'NONE', #43946, #42881, #34830 ) ;
#93608=CARTESIAN_POINT ( 'NONE',  ( 92.59918368926680898, -29.99999999999998224, 50.96418643717338881 ) ) ;
#93609=CARTESIAN_POINT ( 'NONE',  ( -83.49067641280694829, -22.15006867442743754, 148.6564140083872303 ) ) ;
#93612=DIRECTION ( 'NONE',  ( -0.000000000000000000, -1.000000000000000000, -0.000000000000000000 ) ) ;
#93613=CARTESIAN_POINT ( 'NONE',  ( 57.99551341713360841, -57.67649500090644210, 100.6097491013691609 ) ) ;
#93632=CARTESIAN_POINT ( 'NONE',  ( 22.21354712676404830, -60.00000000000001421, -41.66341169407889566 ) ) ;
#93633=CARTESIAN_POINT ( 'NONE',  ( -43.57786082180619047, -59.99999999999987921, 62.86006299602857439 ) ) ;
#93634=CARTESIAN_POINT ( 'NONE',  ( 23.00510670403769709, -56.87329948538524604, 34.33241275911512247 ) ) ;
#93637=CARTESIAN_POINT ( 'NONE',  ( -34.08206426064871408, -29.10158233164262853, 32.84525425997023973 ) ) ;
#93650=CARTESIAN_POINT ( 'NONE',  ( 98.69640391454856854, -29.99999999999997868, 189.4887148491113180 ) ) ;
#93654=CARTESIAN_POINT ( 'NONE',  ( 81.33220965908822109, -30.00000000000000000, -0.9688136936568159108 ) ) ;
#93670=CARTESIAN_POINT ( 'NONE',  ( 75.46173676908961170, -38.35133497314376427, 173.8617030787818578 ) ) ;
#93680=( BOUNDED_CURVE ( )  B_SPLINE_CURVE ( 2, ( #20666, #68647, #52973 ),
 .UNSPECIFIED., .F., .F. ) 
 B_SPLINE_CURVE_WITH_KNOTS ( ( 3, 3 ),
 ( 0.000000000000000000, 1.000000000000000000 ),
 .UNSPECIFIED. ) 
 CURVE ( )  GEOMETRIC_REPRESENTATION_ITEM ( )  RATIONAL_B_SPLINE_CURVE ( ( 1.000000000000000000, 1.857142857142858317, 1.000000000000000000 ) ) 
 REPRESENTATION_ITEM ( '' )  );
#93693=CARTESIAN_POINT ( 'NONE',  ( 86.67109623895983361, -39.12583655368941749, 188.4524350337027840 ) ) ;
#93702=CARTESIAN_POINT ( 'NONE',  ( -92.95396129993294210, -30.00000000000000711, 105.7524778981976823 ) ) ;
#93705=CARTESIAN_POINT ( 'NONE',  ( 31.99970601987291019, -57.68905111566994748, 46.55696586113492685 ) ) ;
#93709=CARTESIAN_POINT ( 'NONE',  ( -12.62509669329198481, -21.71534459113969717, 27.56286583360048326 ) ) ;
#93713=CARTESIAN_POINT ( 'NONE',  ( 47.70175436633333987, -26.95658883994271449, -28.55419944461410608 ) ) ;
#93715=CARTESIAN_POINT ( 'NONE',  ( -22.70419453045296265, -46.43894835127135678, 32.52296259171259862 ) ) ;
#93719=CARTESIAN_POINT ( 'NONE',  ( -20.41567380225452766, -49.92006620171714815, 32.77936002969759954 ) ) ;
#93731=CARTESIAN_POINT ( 'NONE',  ( 103.3943054737346046, -60.16143074633508547, 192.1485504246914786 ) ) ;
#93732=FILL_AREA_STYLE_COLOUR ( '', #38893 ) ;
#93748=CARTESIAN_POINT ( 'NONE',  ( -64.13648978638106257, -59.99999999998060929, -36.96743988013938775 ) ) ;
#93752=CARTESIAN_POINT ( 'NONE',  ( -89.21220262753612928, -29.99999999999994316, 13.74661749290507906 ) ) ;
#93754=CARTESIAN_POINT ( 'NONE',  ( -47.95171403034644442, -49.90426566354960158, 50.75745535836532696 ) ) ;
#93766=CARTESIAN_POINT ( 'NONE',  ( 54.45238581501602937, -38.34104842573536587, 79.96003652838339804 ) ) ;
#93771=CARTESIAN_POINT ( 'NONE',  ( 90.89870986292757493, -29.99999999999999645, 190.4476607199382272 ) ) ;
#93776=CARTESIAN_POINT ( 'NONE',  ( 54.21244330743853368, -53.37526703652106619, 64.17922940371380491 ) ) ;
#93780=CARTESIAN_POINT ( 'NONE',  ( -85.43770264849763407, -38.35986594992170495, -22.44427725120138106 ) ) ;
#93783=CARTESIAN_POINT ( 'NONE',  ( 110.8167341139307069, -38.35606656894265143, 179.0010575348368889 ) ) ;
#93786=CARTESIAN_POINT ( 'NONE',  ( 86.18168139896047819, -60.14160201014042428, 16.47270778115648326 ) ) ;
#93805=CARTESIAN_POINT ( 'NONE',  ( -14.09593269997207088, -14.81306030174825317, 31.68409824573272004 ) ) ;
#93809=CARTESIAN_POINT ( 'NONE',  ( 86.40550120089977781, -17.76515147996571642, 175.7347892468938539 ) ) ;
#93814=CARTESIAN_POINT ( 'NONE',  ( -89.89106403992835226, -52.70984408041336167, 62.30226075620301884 ) ) ;
#93819=CARTESIAN_POINT ( 'NONE',  ( -8.675203801466720321, -22.30999872138366413, -38.54374433678079015 ) ) ;
#93824=CARTESIAN_POINT ( 'NONE',  ( 17.12293775459222545, -60.00000000000000711, 39.93182275144659599 ) ) ;
#93825=CARTESIAN_POINT ( 'NONE',  ( 36.21953432627893932, -36.13225097047772749, 45.40297091003908037 ) ) ;
#93827=CARTESIAN_POINT ( 'NONE',  ( 35.66921402495393068, -24.37933129301127977, 33.74266031588260972 ) ) ;
#93828=CARTESIAN_POINT ( 'NONE',  ( -32.31175092299783103, -33.94243246659586788, 42.05989758142741408 ) ) ;
#93840=CARTESIAN_POINT ( 'NONE',  ( -0.001453451169200235555, -21.77031582776994512, -30.51803592518467312 ) ) ;
#93851=CARTESIAN_POINT ( 'NONE',  ( -91.86405410517724590, -60.00000000000002132, 11.09660898435537035 ) ) ;
#93855=CARTESIAN_POINT ( 'NONE',  ( 89.99999999999997158, -60.00000000000000000, 196.0238439516549818 ) ) ;
#93859=CARTESIAN_POINT ( 'NONE',  ( -80.43703877261472712, -56.89382256290284801, 173.6098779234407345 ) ) ;
#93871=CARTESIAN_POINT ( 'NONE',  ( -94.10527518209565301, -57.67545334945994995, 3.926124123639501029 ) ) ;
#93877=CARTESIAN_POINT ( 'NONE',  ( 100.7779335074592524, -14.21045842199434084, 117.1442511085924565 ) ) ;
#93878=CARTESIAN_POINT ( 'NONE',  ( -100.0713701506240767, -14.21045842199444209, 196.7486061734171585 ) ) ;
#93879=CARTESIAN_POINT ( 'NONE',  ( -56.24379992063114031, -46.44138396924517309, 65.97396921761240662 ) ) ;
#93883=CARTESIAN_POINT ( 'NONE',  ( -104.8207464962321041, -52.71021621793995848, 181.7139379092529623 ) ) ;
#93890=CARTESIAN_POINT ( 'NONE',  ( 78.22378191117061874, -38.35599095560626637, -27.52319075166474960 ) ) ;
#93904=CARTESIAN_POINT ( 'NONE',  ( -32.69584145684933674, -60.31921410685050944, 38.00927738129874456 ) ) ;
#93906=CARTESIAN_POINT ( 'NONE',  ( 47.98400582330030062, -46.44011229906595872, 49.73359105907310607 ) ) ;
#93909=CARTESIAN_POINT ( 'NONE',  ( -87.79946780904923287, -38.56465307817885702, 199.8815181703243127 ) ) ;
#93910=ORIENTED_EDGE ( 'NONE', *, *, #71262, .F. ) ;
#93919=CARTESIAN_POINT ( 'NONE',  ( 105.3430580151378848, -60.00000000000000000, 198.9623513283988814 ) ) ;
#93927=CARTESIAN_POINT ( 'NONE',  ( -77.49146788675471953, -30.00000000000003197, -16.28211930504271976 ) ) ;
#93929=CARTESIAN_POINT ( 'NONE',  ( -83.77510898144794282, -38.77500651307043711, 197.6085426658710844 ) ) ;
#93943=CARTESIAN_POINT ( 'NONE',  ( 80.80464672076368515, -60.47367659752207913, 181.9382789710017789 ) ) ;
#93980=CARTESIAN_POINT ( 'NONE',  ( -102.8080736368318924, -60.00000000000000711, 200.7218921456022542 ) ) ;
#93983=CARTESIAN_POINT ( 'NONE',  ( -84.39678327578025119, -39.41870918651168409, 180.8096083365613822 ) ) ;
#93991=CARTESIAN_POINT ( 'NONE',  ( -83.82575208384432131, -45.26788530597328020, 5.651614345716667209 ) ) ;
#93996=CARTESIAN_POINT ( 'NONE',  ( 71.28669324481667502, -60.00000000000002132, 168.6228882893990715 ) ) ;
#93997=CARTESIAN_POINT ( 'NONE',  ( -93.94019401501873290, -59.99999999999992895, -15.95863606727341022 ) ) ;
#93998=CARTESIAN_POINT ( 'NONE',  ( -67.38458195274520790, -18.62889978042072059, 82.16052029329225093 ) ) ;
#94000=CARTESIAN_POINT ( 'NONE',  ( 97.80297141475710987, -14.21045842199415432, 197.6895799465713708 ) ) ;
#94002=CARTESIAN_POINT ( 'NONE',  ( 21.58919157199202843, -60.00000000000991207, 42.83841619683437330 ) ) ;
#94016=CARTESIAN_POINT ( 'NONE',  ( -27.82884491182329612, -60.00000000000002132, -41.18721216356012604 ) ) ;
#94019=CARTESIAN_POINT ( 'NONE',  ( -80.00000000000000000, -60.00000000000000000, -19.09707704303353282 ) ) ;
#94028=CARTESIAN_POINT ( 'NONE',  ( 32.69486656708485128, -25.62054887169689010, 31.60347500623590733 ) ) ;
#94030=EDGE_CURVE ( 'NONE', #40814, #87422, #63331, .T. ) ;
#94041=CARTESIAN_POINT ( 'NONE',  ( 92.00108026731086852, -60.00000000000000711, 6.185581164671163812 ) ) ;
#94050=CARTESIAN_POINT ( 'NONE',  ( -97.19700283461635593, -30.00000000007960921, 80.76470468910331135 ) ) ;
#94056=CARTESIAN_POINT ( 'NONE',  ( 84.92072808231688441, -52.75190680617863137, -13.22419148268572719 ) ) ;
#94059=CARTESIAN_POINT ( 'NONE',  ( 73.19785846594415091, -56.33009803196139842, -24.31540027847616869 ) ) ;
#94068=CARTESIAN_POINT ( 'NONE',  ( 82.56818838668320382, -18.68756746491115095, 139.1075167907083596 ) ) ;
#94073=CARTESIAN_POINT ( 'NONE',  ( -94.30950767697063952, -57.61975185784459086, 204.5257163505249309 ) ) ;
#94085=CARTESIAN_POINT ( 'NONE',  ( -39.97223656545506287, -26.31402483469310027, 35.94295830377559042 ) ) ;
#94097=CARTESIAN_POINT ( 'NONE',  ( 51.30196405314951846, -28.81598073202483690, -34.78016533206015737 ) ) ;
#94098=CARTESIAN_POINT ( 'NONE',  ( -62.55748708953316850, -29.99999999999999289, 73.50292915578185671 ) ) ;
#94101=CARTESIAN_POINT ( 'NONE',  ( 75.17713619727400953, -57.57008159638389344, 191.1469172435081987 ) ) ;
#94103=CARTESIAN_POINT ( 'NONE',  ( 48.07208864154289785, -35.12482717350385997, -36.45831645058230919 ) ) ;
#94106=CARTESIAN_POINT ( 'NONE',  ( -53.29227158861940694, -60.00000000000000711, 80.45665323453354745 ) ) ;
#94110=CARTESIAN_POINT ( 'NONE',  ( -84.61722220583241949, -53.82794903670232856, 190.0724395252715340 ) ) ;
#94113=CARTESIAN_POINT ( 'NONE',  ( -5.121394014575314735, -49.92081713162068723, 32.19947040910868452 ) ) ;
#94126=CARTESIAN_POINT ( 'NONE',  ( -2.910977163136218682, -8.673617379884035472E-16, 22.23822744035697241 ) ) ;
#94129=CARTESIAN_POINT ( 'NONE',  ( 88.56622727954015772, -14.21045842199445630, 40.39835639566682346 ) ) ;
#94130=CARTESIAN_POINT ( 'NONE',  ( -81.68110744402518719, -32.56240651117416007, 148.9491915846473660 ) ) ;
#94134=CARTESIAN_POINT ( 'NONE',  ( 42.58655652176065587, -57.68666533375992600, 60.21381296430073604 ) ) ;
#94155=CARTESIAN_POINT ( 'NONE',  ( 91.67460378421274925, -59.99999999999997868, -15.10447286846676107 ) ) ;
#94157=CARTESIAN_POINT ( 'NONE',  ( -36.05833693101251214, -60.00000000000004263, 50.77755985414292184 ) ) ;
#94158=CARTESIAN_POINT ( 'NONE',  ( 22.60328433090425904, -42.95462652055326913, 31.91884077397672570 ) ) ;
#94162=CARTESIAN_POINT ( 'NONE',  ( -38.04192487099758324, -60.27676763154023121, 41.50750820892533000 ) ) ;
#94175=CARTESIAN_POINT ( 'NONE',  ( -64.25342926545496880, -38.33908962693352152, 110.6569961331102121 ) ) ;
#94177=CARTESIAN_POINT ( 'NONE',  ( 99.84195935041229575, -29.99999999999997868, 186.2662609802098075 ) ) ;
#94183=CARTESIAN_POINT ( 'NONE',  ( 81.59412300828947195, -30.00000000000000000, -6.883953906076696327 ) ) ;
#94203=CARTESIAN_POINT ( 'NONE',  ( 59.97286723080061677, -22.12426351543174619, 64.13356965173628055 ) ) ;
#94221=CARTESIAN_POINT ( 'NONE',  ( 86.37779416861748416, -20.93961008912989286, 181.4651759308039232 ) ) ;
#94231=CARTESIAN_POINT ( 'NONE',  ( -85.32909183395112507, -29.99999999999999645, 59.83043280556380950 ) ) ;
#94236=CARTESIAN_POINT ( 'NONE',  ( 14.56780743600302586, -57.67141137934046924, 41.74351479442032087 ) ) ;
#94248=CARTESIAN_POINT ( 'NONE',  ( 22.09068723947702395, -19.16686062785725753, -33.43374534816550891 ) ) ;
#94250=CARTESIAN_POINT ( 'NONE',  ( -23.68218076818291706, -39.47912890587980428, 31.49652407728643055 ) ) ;
#94253=CARTESIAN_POINT ( 'NONE',  ( 76.12557658274099026, -38.35599704320051018, -28.58424740099938077 ) ) ;
#94254=CARTESIAN_POINT ( 'NONE',  ( -18.86856976124040486, -32.51467859884330380, 29.71142835944370830 ) ) ;
#94266=CARTESIAN_POINT ( 'NONE',  ( 100.4946997161162443, -37.84604486669937984, 189.5797555323898962 ) ) ;
#94267=CARTESIAN_POINT ( 'NONE',  ( 49.18359670589789090, -37.81820580435596213, 48.86208063644627941 ) ) ;
#94280=CARTESIAN_POINT ( 'NONE',  ( -94.91350004442121246, -59.99999999999032951, -11.18889123746408920 ) ) ;
#94282=CARTESIAN_POINT ( 'NONE',  ( 32.54749815468527885, -60.00000000000002132, 44.51763105449811064 ) ) ;
#94285=CARTESIAN_POINT ( 'NONE',  ( -94.62342829788488530, -14.21045842199438525, 80.85070941463327188 ) ) ;
#94286=CARTESIAN_POINT ( 'NONE',  ( 6.227159620205909185, -60.35885591111542681, 33.93934178768890320 ) ) ;
#94291=CARTESIAN_POINT ( 'NONE',  ( -47.58650698943795021, -56.82114114556742379, 52.30438436347986908 ) ) ;
#94303=CARTESIAN_POINT ( 'NONE',  ( 92.64207125262521458, -29.99999999987929655, 51.61815748969144124 ) ) ;
#94307=EDGE_CURVE ( 'NONE', #51964, #102392, #65793, .T. ) ;
#94309=CARTESIAN_POINT ( 'NONE',  ( 98.19688506443435472, -30.00000000000000355, 190.3059900313137689 ) ) ;
#94316=CARTESIAN_POINT ( 'NONE',  ( 54.63781606259024670, -32.56084225145857403, 56.78402738445370090 ) ) ;
#94322=CARTESIAN_POINT ( 'NONE',  ( -91.32775393698508992, -38.36579091124441021, -2.591198299663252325 ) ) ;
#94325=CARTESIAN_POINT ( 'NONE',  ( 94.69161108849048958, -38.49000774377354617, 201.2185778078309113 ) ) ;
#94328=CARTESIAN_POINT ( 'NONE',  ( 83.72129867378865242, -45.28294897705733035, 15.97319318370404773 ) ) ;
#94347=CARTESIAN_POINT ( 'NONE',  ( 14.68095810428979853, -17.65437676951217227, 35.02762473332876425 ) ) ;
#94352=CARTESIAN_POINT ( 'NONE',  ( 85.48291297220137608, -32.15055455726690070, 180.9890288920893511 ) ) ;
#94357=CARTESIAN_POINT ( 'NONE',  ( -92.21955131628659785, -52.71021242866512324, 76.94161136100676401 ) ) ;
#94363=CARTESIAN_POINT ( 'NONE',  ( 21.30699193799562252, -60.00000000000000711, 40.40681636397585663 ) ) ;
#94364=CARTESIAN_POINT ( 'NONE',  ( -86.78976035038994041, -38.00000000000004974, 188.4439161865618644 ) ) ;
#94365=CARTESIAN_POINT ( 'NONE',  ( 39.79890337217759821, -26.23938249810791845, 35.83377390011310126 ) ) ;
#94367=CARTESIAN_POINT ( 'NONE',  ( -29.55526716209243077, -32.15409974475024768, 40.32020078543521180 ) ) ;
#94384=CARTESIAN_POINT ( 'NONE',  ( -4.829386694092057120, -60.22815139279438057, -36.87030747315908030 ) ) ;
#94393=CARTESIAN_POINT ( 'NONE',  ( -94.46259299136239918, -59.99999999999999289, 45.00074042340703784 ) ) ;
#94403=CARTESIAN_POINT ( 'NONE',  ( -84.24477676735598664, -29.03027281900111589, 164.8630760665813284 ) ) ;
#94415=CARTESIAN_POINT ( 'NONE',  ( -94.70367724826090239, -57.65721615037961811, -8.919493359160306056 ) ) ;
#94421=CARTESIAN_POINT ( 'NONE',  ( 71.63670194497801447, -60.00000000000009948, -34.46961289685300045 ) ) ;
#94423=CARTESIAN_POINT ( 'NONE',  ( -39.49898250731507687, -29.99999999999994316, 47.07929020003657428 ) ) ;
#94424=CARTESIAN_POINT ( 'NONE',  ( -55.26582361395064424, -29.09120361102063157, 56.68308257653641391 ) ) ;
#94429=CARTESIAN_POINT ( 'NONE',  ( -101.7716104940794537, -52.71911127419147647, 192.4179177423009151 ) ) ;
#94430=CARTESIAN_POINT ( 'NONE',  ( 99.81081141497985243, -37.99999999999998579, 138.1205616140921961 ) ) ;
#94435=PRESENTATION_STYLE_ASSIGNMENT (( #79287 ) ) ;
#94449=CARTESIAN_POINT ( 'NONE',  ( -29.01219337864047532, -36.01131291592842842, 32.18479342621510852 ) ) ;
#94452=CARTESIAN_POINT ( 'NONE',  ( 47.63708399370681690, -49.89836957298526698, 50.26224229957048095 ) ) ;
#94455=CARTESIAN_POINT ( 'NONE',  ( -89.60598034427661673, -38.52158010613944583, 200.4661439829993697 ) ) ;
#94464=CARTESIAN_POINT ( 'NONE',  ( 112.1444936845196594, -59.99999999999999289, 176.9640175347291233 ) ) ;
#94466=EDGE_LOOP ( 'NONE', ( #84573, #52203 ) ) ;
#94468=CARTESIAN_POINT ( 'NONE',  ( -80.42593251586281156, -30.00000000000000000, -13.16377588536598786 ) ) ;
#94469=VERTEX_POINT ( 'NONE', #78008 ) ;
#94470=CARTESIAN_POINT ( 'NONE',  ( -74.84880931779602520, -38.33446659060637529, 168.0768817207809036 ) ) ;
#94486=CARTESIAN_POINT ( 'NONE',  ( 81.53291621683337098, -53.45972034811280338, 178.0932871262222079 ) ) ;
#94529=CARTESIAN_POINT ( 'NONE',  ( -96.53420287613388950, -59.99999999999998579, 202.5374593177585325 ) ) ;
#94535=CARTESIAN_POINT ( 'NONE',  ( -82.76397134495906016, -53.63233267313180619, 185.2452585357339103 ) ) ;
#94538=ORIENTED_EDGE ( 'NONE', *, *, #80652, .F. ) ;
#94541=CARTESIAN_POINT ( 'NONE',  ( -84.30425635789666217, -45.26998071672124979, -1.773480528068236417 ) ) ;
#94548=CARTESIAN_POINT ( 'NONE',  ( 78.42589391212746364, -14.21045842199428222, 185.4806485215488010 ) ) ;
#94550=CARTESIAN_POINT ( 'NONE',  ( -94.33288967953484416, -60.00000000000004263, 18.12646456170910625 ) ) ;
#94551=CARTESIAN_POINT ( 'NONE',  ( -65.58664656726918452, -25.57963682766552438, 80.66977220019482786 ) ) ;
#94553=CARTESIAN_POINT ( 'NONE',  ( 105.0775402602081954, -59.99999999999994316, 202.2121962084956976 ) ) ;
#94556=CARTESIAN_POINT ( 'NONE',  ( 2.435348427764908250E-07, -57.67120202539301488, -44.61186700419774098 ) ) ;
#94567=CARTESIAN_POINT ( 'NONE',  ( -89.41502101575679262, -59.99999999999998579, -19.75460450551653224 ) ) ;
#94578=CIRCLE ( 'NONE', #104957, 60.00000000000000000 ) ;
#94583=CARTESIAN_POINT ( 'NONE',  ( 33.88146361334444379, -25.63312173870950517, 32.08093021307823989 ) ) ;
#94584=CARTESIAN_POINT ( 'NONE',  ( -12.70248734012553804, -4.285714285715715555, -22.03900363279001340 ) ) ;
#94598=CARTESIAN_POINT ( 'NONE',  ( 92.66631810923314561, -60.00000000000001421, -4.015254816811776983 ) ) ;
#94605=CARTESIAN_POINT ( 'NONE',  ( -102.6614301708703181, -29.99999999999975486, 197.7212064138423386 ) ) ;
#94610=CARTESIAN_POINT ( 'NONE',  ( 83.97033530527313872, -52.73435016161096911, -15.30432209802549437 ) ) ;
#94617=ADVANCED_FACE ( 'NONE', ( #14312 ), #89439, .T. ) ;
#94622=CARTESIAN_POINT ( 'NONE',  ( 79.26994885458404383, -32.55667777107090188, 134.6539744698178538 ) ) ;
#94629=CARTESIAN_POINT ( 'NONE',  ( -70.79351044798765713, -57.68242073007258597, 160.4532249112098157 ) ) ;
#94637=CARTESIAN_POINT ( 'NONE',  ( -52.01488423272231643, -29.95943715781152505, 50.12585609927782571 ) ) ;
#94651=CARTESIAN_POINT ( 'NONE',  ( -33.19001599143121695, -22.73732675021535954, -31.63514692089995606 ) ) ;
#94652=CARTESIAN_POINT ( 'NONE',  ( -66.43834448911053414, -30.00000000000000000, 84.40165359335730955 ) ) ;
#94657=CARTESIAN_POINT ( 'NONE',  ( 78.25717990118528178, -57.50986624554720805, 196.9151558317045385 ) ) ;
#94663=CARTESIAN_POINT ( 'NONE',  ( -53.46014380037404834, -59.99999999999999289, 80.92137724076353322 ) ) ;
#94669=CARTESIAN_POINT ( 'NONE',  ( -86.39277916084785147, -17.36997147719805668, 179.6821819924676333 ) ) ;
#94672=CARTESIAN_POINT ( 'NONE',  ( -5.156364120415605434, -56.88410093696714398, 33.35976719709237415 ) ) ;
#94677=VECTOR ( 'NONE', #44203, 1000.000000000000000 ) ;
#94683=CARTESIAN_POINT ( 'NONE',  ( -22.03900363279597840, -4.285714285713229543, -12.70248734010661451 ) ) ;
#94686=CARTESIAN_POINT ( 'NONE',  ( 101.2959083255158390, -29.99999999999995026, 104.2725399938968707 ) ) ;
#94687=CARTESIAN_POINT ( 'NONE',  ( -82.56867337363084403, -18.68741499447245502, 139.1104154598086495 ) ) ;
#94691=CARTESIAN_POINT ( 'NONE',  ( 40.58563001615174670, -57.69103653720686253, 56.61367073664153793 ) ) ;
#94708=CARTESIAN_POINT ( 'NONE',  ( 86.68221780050056680, -59.99999999999997868, -23.04089234932559549 ) ) ;
#94709=CARTESIAN_POINT ( 'NONE',  ( -69.35428882245668092, -14.21045842199431064, 113.5922931172439263 ) ) ;
#94710=CARTESIAN_POINT ( 'NONE',  ( 26.29730120201151067, -29.04676451314565711, 30.24640415352105549 ) ) ;
#94717=CARTESIAN_POINT ( 'NONE',  ( -24.41571844174603001, -4.285714285714296246, -6.539732759932831208 ) ) ;
#94724=CARTESIAN_POINT ( 'NONE',  ( -54.49732025174689909, -38.34336403967661511, 80.08277365667782988 ) ) ;
#94726=CARTESIAN_POINT ( 'NONE',  ( 100.1751865587538646, -29.99999999999997868, 184.8388631958245583 ) ) ;
#94729=CARTESIAN_POINT ( 'NONE',  ( 81.33861762675972784, -30.00000000000000711, -1.059591593001759868 ) ) ;
#94751=CARTESIAN_POINT ( 'NONE',  ( 65.34791356701451548, -18.62574154944152838, 76.43348303465126037 ) ) ;
#94754=CARTESIAN_POINT ( 'NONE',  ( -52.11024624342783795, -36.01363760906497902, -35.80679646664415117 ) ) ;
#94768=CARTESIAN_POINT ( 'NONE',  ( 85.99512895147944391, -46.52335532650928940, 189.5191995827347284 ) ) ;
#94774=CARTESIAN_POINT ( 'NONE',  ( -17.80527173634003191, -17.90131026958873406, -34.03118370072504462 ) ) ;
#94778=CARTESIAN_POINT ( 'NONE',  ( -100.7719193891408338, -30.00000000000000000, 180.5683480488255270 ) ) ;
#94782=CARTESIAN_POINT ( 'NONE',  ( 28.28340439371653048, -57.67994101532651285, 44.40698028540107600 ) ) ;
#94790=CARTESIAN_POINT ( 'NONE',  ( 7.575153643621726829, -15.84894062807185122, -34.99671955924535638 ) ) ;
#94796=CARTESIAN_POINT ( 'NONE',  ( -17.74239981412279832, -32.51404901966539995, 29.61011661303510323 ) ) ;
#94809=CARTESIAN_POINT ( 'NONE',  ( 104.0800975233037775, -60.15442106764426455, 190.6471068656633747 ) ) ;
#94810=CARTESIAN_POINT ( 'NONE',  ( 39.19831989819565621, -34.84122234843880506, 37.04583787359052849 ) ) ;
#94822=CARTESIAN_POINT ( 'NONE',  ( -98.65929570741894850, -59.99999999996092015, 58.00980118487002102 ) ) ;
#94825=CARTESIAN_POINT ( 'NONE',  ( 31.02726165664941860, -59.99999999999998579, 43.58380924251923716 ) ) ;
#94828=CARTESIAN_POINT ( 'NONE',  ( -91.01385585952614576, -29.99999999999999289, 38.60219201899132457 ) ) ;
#94829=CARTESIAN_POINT ( 'NONE',  ( 9.022935735952771097, -18.58636217958399328, 26.98789801028366142 ) ) ;
#94833=CARTESIAN_POINT ( 'NONE',  ( -47.70095744468055443, -39.52629137943383597, 47.20404219366211152 ) ) ;
#94843=CARTESIAN_POINT ( 'NONE',  ( 59.26090642338721182, -38.34351558597094112, 94.03560012898597620 ) ) ;
#94847=CARTESIAN_POINT ( 'NONE',  ( 98.45347978416359069, -30.00000000000000000, 189.9177565486554613 ) ) ;
#94853=CARTESIAN_POINT ( 'NONE',  ( 54.32622272398685226, -60.31656904070205627, 67.31739225095211054 ) ) ;
#94858=VERTEX_POINT ( 'NONE', #34533 ) ;
#94863=CARTESIAN_POINT ( 'NONE',  ( 92.73232662571349749, -38.49779465622716401, 201.0880014169763115 ) ) ;
#94865=CARTESIAN_POINT ( 'NONE',  ( 82.42441318170639875, -37.85770433546145597, 11.94012267114784187 ) ) ;
#94885=CARTESIAN_POINT ( 'NONE',  ( -42.02846191695555689, -38.14260630011440867, 52.77835525687510199 ) ) ;
#94888=CARTESIAN_POINT ( 'NONE',  ( 84.96975805255164005, -35.80893149064998227, 180.8542816627177956 ) ) ;
#94892=CARTESIAN_POINT ( 'NONE',  ( -88.26195796627457923, -60.15288368548232967, 41.81127973269768461 ) ) ;
#94900=CARTESIAN_POINT ( 'NONE',  ( 17.26102777918536546, -23.99532633086393574, 36.28153977239290384 ) ) ;
#94903=CARTESIAN_POINT ( 'NONE',  ( 49.50347019672712889, -29.59020143643714817, 45.82998437115109169 ) ) ;
#94915=CARTESIAN_POINT ( 'NONE',  ( -83.25840715934710090, -38.00000000000002842, -8.522864994567452612 ) ) ;
#94921=CARTESIAN_POINT ( 'NONE',  ( -9.688912271943010524, -60.22816138548923703, -36.71155112804019183 ) ) ;
#94931=CARTESIAN_POINT ( 'NONE',  ( -93.39135768774528401, -60.00000000000000000, 36.04682483438401164 ) ) ;
#94939=CARTESIAN_POINT ( 'NONE',  ( -83.26671734593782048, -36.00732091460121609, 166.7895401501197057 ) ) ;
#94951=CARTESIAN_POINT ( 'NONE',  ( -94.41147650277389403, -57.65372982601817853, -11.88746169270405773 ) ) ;
#94956=CARTESIAN_POINT ( 'NONE',  ( 59.37626172009473180, -60.00000000000000000, -38.24869620007160620 ) ) ;
#94958=CARTESIAN_POINT ( 'NONE',  ( -68.63253095932553549, -60.00000000000002842, 147.4008728361381486 ) ) ;
#94960=CARTESIAN_POINT ( 'NONE',  ( -54.81653371739410119, -39.50102972048344441, 59.89691189185823106 ) ) ;
#94963=CARTESIAN_POINT ( 'NONE',  ( -99.71594338102195820, -37.80910377345113460, 191.0446671273005279 ) ) ;
#94975=CARTESIAN_POINT ( 'NONE',  ( 65.65137904215926312, -29.99999999999999645, 82.10676440717566038 ) ) ;
#94980=CARTESIAN_POINT ( 'NONE',  ( -28.55605187411735457, -39.48529133943618064, 32.65731791215971214 ) ) ;
#94983=CARTESIAN_POINT ( 'NONE',  ( 48.29725937789723389, -46.43994943433606437, 50.22590090644417415 ) ) ;
#94988=CARTESIAN_POINT ( 'NONE',  ( -92.77767653423819638, -38.49725484616736537, 201.0877250123326974 ) ) ;
#94990=CARTESIAN_POINT ( 'NONE',  ( 91.35834606489962084, -38.36978471520085776, -3.221837418575325795 ) ) ;
#94998=EDGE_CURVE ( 'NONE', #24767, #91737, #44727, .T. ) ;
#94999=CARTESIAN_POINT ( 'NONE',  ( 112.1772628306614052, -59.99999999999999289, 169.0755217369682555 ) ) ;
#95007=CARTESIAN_POINT ( 'NONE',  ( -105.5261409709756748, -38.38483589435347199, 196.9266904464792844 ) ) ;
#95019=CARTESIAN_POINT ( 'NONE',  ( 84.88150630316555123, -25.51212071581490193, 165.4351799496252795 ) ) ;
#95031=CARTESIAN_POINT ( 'NONE',  ( -76.57718945954728440, -29.99999999999999645, -16.95318723146485951 ) ) ;
#95058=CARTESIAN_POINT ( 'NONE',  ( -109.8703831905171739, -60.00000000000000000, 191.6706218040895351 ) ) ;
#95063=CARTESIAN_POINT ( 'NONE',  ( -81.99317651741259283, -57.10874830205603558, 184.9732242174657131 ) ) ;
#95068=CARTESIAN_POINT ( 'NONE',  ( -82.58338653627937731, -37.82595221992723111, 19.55788899699552985 ) ) ;
#95075=CARTESIAN_POINT ( 'NONE',  ( 91.59609553898350498, -30.00000000000011013, 199.7677339052814602 ) ) ;
#95078=CARTESIAN_POINT ( 'NONE',  ( -103.3502313461265771, -29.99999999999994671, 116.5677832811329893 ) ) ;
#95080=CARTESIAN_POINT ( 'NONE',  ( -64.34807526719896487, -29.05564722728329841, 78.93431987242449566 ) ) ;
#95082=CARTESIAN_POINT ( 'NONE',  ( 107.5269304809499431, -60.00000000000002132, 200.1385401206229062 ) ) ;
#95084=CARTESIAN_POINT ( 'NONE',  ( 68.10881077269327477, -59.99999999992211741, 143.9720702942270805 ) ) ;
#95092=CARTESIAN_POINT ( 'NONE',  ( -22.28694302522780646, -60.00000000000000000, -41.69514407324499672 ) ) ;
#95096=CARTESIAN_POINT ( 'NONE',  ( 20.05453516056601870, -4.285714285714295357, 15.38541618194247462 ) ) ;
#95106=CARTESIAN_POINT ( 'NONE',  ( 35.25614048150857371, -29.11149068573612197, 33.41673982746184635 ) ) ;
#95107=CARTESIAN_POINT ( 'NONE',  ( -22.23822744035697241, -8.673617379884035472E-16, 2.910977163147204116 ) ) ;
#95121=CARTESIAN_POINT ( 'NONE',  ( 92.42130671373989514, -59.99999999999999289, -0.1412969037266383898 ) ) ;
#95129=CARTESIAN_POINT ( 'NONE',  ( -100.6754568013630546, -30.00000000001534417, 198.8498281808039110 ) ) ;
#95143=CARTESIAN_POINT ( 'NONE',  ( 80.28596508060884673, -22.14989292550031408, 130.4700177602690303 ) ) ;
#95148=CARTESIAN_POINT ( 'NONE',  ( -79.30961931381874308, -57.50609382800362823, 198.1725500959836666 ) ) ;
#95157=CARTESIAN_POINT ( 'NONE',  ( -44.27626259443545109, -28.04480004288071271, 39.31746864059538638 ) ) ;
#95170=CARTESIAN_POINT ( 'NONE',  ( 36.34975922649171309, -25.58885759170347285, -36.75400926445155392 ) ) ;
#95171=CARTESIAN_POINT ( 'NONE',  ( -70.50465783075846105, -30.00000000000000000, 96.95367432551131515 ) ) ;
#95177=CARTESIAN_POINT ( 'NONE',  ( 83.82547419363363872, -57.54511867887681120, 201.6526650243154961 ) ) ;
#95178=CARTESIAN_POINT ( 'NONE',  ( 66.35709354130753468, -34.58960992778622057, -23.23728143668597212 ) ) ;
#95182=CARTESIAN_POINT ( 'NONE',  ( -65.73763923497537576, -59.99999999999999289, 121.3057691148710546 ) ) ;
#95187=CARTESIAN_POINT ( 'NONE',  ( -85.48259689372021342, -42.91901377629291403, 187.0514599090093668 ) ) ;
#95195=CARTESIAN_POINT ( 'NONE',  ( -82.19473257060306537, -37.78714006915895141, -13.37952554880742539 ) ) ;
#95202=CARTESIAN_POINT ( 'NONE',  ( -20.16952962162825358, -4.285714285714285587, -15.50035291838207741 ) ) ;
#95204=CARTESIAN_POINT ( 'NONE',  ( 81.17508142137076277, -14.21045842199431952, -20.85096179708197184 ) ) ;
#95205=CARTESIAN_POINT ( 'NONE',  ( -82.19555188958855751, -18.68685282153844440, 137.0995853282088888 ) ) ;
#95209=CARTESIAN_POINT ( 'NONE',  ( 68.47697457713316282, -57.68192611185578755, 143.9093171085472136 ) ) ;
#95211=UNCERTAINTY_MEASURE_WITH_UNIT (LENGTH_MEASURE( 1.000000000000000082E-05 ), #21106, 'distance_accuracy_value', 'NONE');
#95228=CARTESIAN_POINT ( 'NONE',  ( 88.58376342546317517, -59.99999999999997868, -20.95051356008556454 ) ) ;
#95230=CARTESIAN_POINT ( 'NONE',  ( -67.93243969554674777, -60.00000000000000711, 143.1807200622937728 ) ) ;
#95231=CARTESIAN_POINT ( 'NONE',  ( 24.15507690844725275, -18.60410174432488617, 28.02059554046051204 ) ) ;
#95243=CARTESIAN_POINT ( 'NONE',  ( 90.02747032318434606, -29.99999999999950617, 189.8937112016718913 ) ) ;
#95246=CARTESIAN_POINT ( 'NONE',  ( 81.42671810001343147, -30.00000000000000355, -2.306699052306097730 ) ) ;
#95249=LINE ( 'NONE', #88214, #84619 ) ;
#95266=CARTESIAN_POINT ( 'NONE',  ( 61.07682198875333768, -38.34186034985221170, 99.84630197542874441 ) ) ;
#95269=CARTESIAN_POINT ( 'NONE',  ( -81.20402667235619276, -59.99999999999999289, 183.8840203063076615 ) ) ;
#95270=CARTESIAN_POINT ( 'NONE',  ( 64.65535091061465778, -18.62627765022782711, 74.52426303803912333 ) ) ;
#95282=CARTESIAN_POINT ( 'NONE',  ( -67.80574261165853045, -59.99999999999996447, -27.21884045395757923 ) ) ;
#95286=CARTESIAN_POINT ( 'NONE',  ( 84.25898199574321268, -61.06033809349827379, 192.6519333314404321 ) ) ;
#95293=CARTESIAN_POINT ( 'NONE',  ( -97.63826302307023752, -29.99999999999999289, 135.0012949887297964 ) ) ;
#95298=CARTESIAN_POINT ( 'NONE',  ( 18.63861866008372914, -57.67172055977938072, 42.04919199611194358 ) ) ;
#95306=CARTESIAN_POINT ( 'NONE',  ( 8.061685236282825271E-09, -15.39512265162600535, -35.22781471665102515 ) ) ;
#95312=CARTESIAN_POINT ( 'NONE',  ( -12.26548772233443607, -29.03140120957289483, 28.77903004484144844 ) ) ;
#95313=CARTESIAN_POINT ( 'NONE',  ( -85.18896233714281152, -59.99999999999995737, -15.68185129854840554 ) ) ;
#95338=CARTESIAN_POINT ( 'NONE',  ( -81.99131086603355811, -60.00000000001472245, 201.2528149072493591 ) ) ;
#95340=CARTESIAN_POINT ( 'NONE',  ( 27.99111733527702128, -59.99999999998071587, -43.50173535898519361 ) ) ;
#95344=CARTESIAN_POINT ( 'NONE',  ( -93.27866288726950472, -14.21045842199433373, 72.78127944122930160 ) ) ;
#95345=CARTESIAN_POINT ( 'NONE',  ( 10.33868530926878293, -46.43477040252509624, 31.64147147909017477 ) ) ;
#95347=CARTESIAN_POINT ( 'NONE',  ( -48.79702489733374193, -53.36716363833840404, 53.26924858186875156 ) ) ;
#95356=CARTESIAN_POINT ( 'NONE',  ( 109.5302677101368971, -30.00000000002007638, 167.0734019624199220 ) ) ;
#95361=CARTESIAN_POINT ( 'NONE',  ( 98.45048472303585640, -29.99999999999998934, 189.9226899209341752 ) ) ;
#95376=CARTESIAN_POINT ( 'NONE',  ( 90.18666349947973515, -38.51691557554957512, 200.6227239373147029 ) ) ;
#95378=CARTESIAN_POINT ( 'NONE',  ( 82.58786548269614514, -37.85377812443031331, 19.55393185633859687 ) ) ;
#95395=CARTESIAN_POINT ( 'NONE',  ( 19.80240316827772418, -19.66620075454853023, 35.71518255902564931 ) ) ;
#95398=CARTESIAN_POINT ( 'NONE',  ( 83.08287465949443629, -57.29649053352386545, 188.7195907736446259 ) ) ;
#95403=CARTESIAN_POINT ( 'NONE',  ( 94.19135992194647145, -57.67257302826786258, 22.54914657329851124 ) ) ;
#95410=CARTESIAN_POINT ( 'NONE',  ( 11.50153144591023135, -20.88508670642358567, 35.51598441719492882 ) ) ;
#95412=CARTESIAN_POINT ( 'NONE',  ( 45.73666261138588851, -28.54726377660503189, 40.86505474274270711 ) ) ;
#95428=CARTESIAN_POINT ( 'NONE',  ( -9.445484387178764152, -34.58962642155982792, -32.44472896259313188 ) ) ;
#95430=ORIENTED_EDGE ( 'NONE', *, *, #12903, .F. ) ;
#95437=CARTESIAN_POINT ( 'NONE',  ( -92.69104981119035358, -60.00000000000001421, -9.101021654975044228 ) ) ;
#95444=CARTESIAN_POINT ( 'NONE',  ( -83.15922951428930787, -36.01117145647910434, 165.7727490414225997 ) ) ;
#95446=CARTESIAN_POINT ( 'NONE',  ( -12.81923949848597566, -0.000000000000000000, -11.24494283603735667 ) ) ;
#95457=CARTESIAN_POINT ( 'NONE',  ( -91.87475470944771416, -57.66094841159801376, -19.53952869114660373 ) ) ;
#95463=CARTESIAN_POINT ( 'NONE',  ( 88.04031092259528180, -30.00000000000002842, -17.07720529721093072 ) ) ;
#95464=CARTESIAN_POINT ( 'NONE',  ( -69.27297328317253289, -60.00000000000002132, 151.6304908672517513 ) ) ;
#95465=CARTESIAN_POINT ( 'NONE',  ( -55.70695580102734112, -39.49968801934875984, 61.84876187497510358 ) ) ;
#95469=CARTESIAN_POINT ( 'NONE',  ( -103.0193768792050122, -60.17265108286817821, 192.8001605453025888 ) ) ;
#95473=VERTEX_POINT ( 'NONE', #24977 ) ;
#95486=CARTESIAN_POINT ( 'NONE',  ( -28.03643574868016941, -56.86872177355682112, 35.51725734821072678 ) ) ;
#95490=CARTESIAN_POINT ( 'NONE',  ( 47.55815791837702022, -60.27279555562992641, 53.32434900433165126 ) ) ;
#95494=CARTESIAN_POINT ( 'NONE',  ( -108.8780014184540050, -38.35654192929601436, 190.5193283876913881 ) ) ;
#95496=CARTESIAN_POINT ( 'NONE',  ( 90.93050292392858580, -38.34431075332760486, 3.015154126244044441 ) ) ;
#95505=CARTESIAN_POINT ( 'NONE',  ( 87.01852956366043657, -60.00000000000000711, 201.0108315922142879 ) ) ;
#95517=CARTESIAN_POINT ( 'NONE',  ( -103.4331137144314141, -38.42286339601668743, 198.8239305193790472 ) ) ;
#95527=CARTESIAN_POINT ( 'NONE',  ( 81.72320301993624980, -53.48224605584718461, 179.5177899479337214 ) ) ;
#95553=B_SPLINE_CURVE_WITH_KNOTS ( 'NONE', 3,
 ( #101581, #27741, #67628, #99974, #17487, #93503, #50350, #51422, #19649, #9897, #11485, #44411, #26145, #3420, #42265, #83262, #75158, #1249, #59001, #77839, #38458, #78885, #54061, #95096, #21755, #36362, #37415, #28801, #12024, #21233, #45486, #29322, #62213, #61683 ),
 .UNSPECIFIED., .F., .F.,
 ( 4, 2, 2, 2, 2, 2, 2, 2, 2, 2, 2, 2, 2, 2, 2, 2, 4 ),
 ( 0.5000000000000000000, 0.5312500000000000000, 0.5625000000000000000, 0.5937500000000000000, 0.6250000000000000000, 0.6562500000000000000, 0.6875000000000000000, 0.7187500000000000000, 0.7500000000000000000, 0.7812500000000000000, 0.8125000000000000000, 0.8437500000000000000, 0.8750000000000000000, 0.9062500000000000000, 0.9375000000000000000, 0.9687500000000000000, 1.000000000000000000 ),
 .UNSPECIFIED. ) ;
#95574=CARTESIAN_POINT ( 'NONE',  ( -109.2006123233502137, -59.99999999999999289, 137.4141054976637975 ) ) ;
#95580=CARTESIAN_POINT ( 'NONE',  ( -82.47186679091046813, -60.82202273473512122, 189.3326345159165953 ) ) ;
#95587=CARTESIAN_POINT ( 'NONE',  ( -83.90290634939050562, -45.26542921300821831, 21.05896802600032913 ) ) ;
#95593=CARTESIAN_POINT ( 'NONE',  ( 82.63356161194110427, -60.00000000000014921, 201.7055385233423976 ) ) ;
#95594=CARTESIAN_POINT ( 'NONE',  ( -103.2977232915219048, -14.21045842199428577, 133.3115090881459253 ) ) ;
#95595=CARTESIAN_POINT ( 'NONE',  ( -63.04233670341422169, -60.34557740310773966, 91.29213200275268036 ) ) ;
#95598=CARTESIAN_POINT ( 'NONE',  ( 99.19415962822883159, -60.00000000000739675, 204.5929917445554338 ) ) ;
#95607=CARTESIAN_POINT ( 'NONE',  ( -63.47509362114410436, -60.00000000000000000, -34.70012741899613218 ) ) ;
#95618=CARTESIAN_POINT ( 'NONE',  ( 101.1017039263183221, -60.00000000000007816, 195.0041137791595531 ) ) ;
#95621=CARTESIAN_POINT ( 'NONE',  ( 35.65037063887645274, -36.04038755283193041, 35.00118258462216403 ) ) ;
#95623=CARTESIAN_POINT ( 'NONE',  ( -21.65942590380950605, 4.828984019150144164E-12, 5.820808985950977288 ) ) ;
#95641=CARTESIAN_POINT ( 'NONE',  ( 100.7204764832770536, -60.00000000000001421, 85.25963890312766580 ) ) ;
#95650=CARTESIAN_POINT ( 'NONE',  ( -90.07223913452511965, -30.00000000002903988, -8.398832610232158657 ) ) ;
#95662=CARTESIAN_POINT ( 'NONE',  ( 80.34687235150721563, -36.02841022270869331, 144.2383497923063658 ) ) ;
#95668=CARTESIAN_POINT ( 'NONE',  ( -74.02244645645996002, -57.61166141858229395, 187.2311674206319765 ) ) ;
#95684=ORIENTED_EDGE ( 'NONE', *, *, #36235, .T. ) ;
#95688=CARTESIAN_POINT ( 'NONE',  ( -27.26849945976038114, -20.79577116979002227, -32.65558008730316431 ) ) ;
#95689=CARTESIAN_POINT ( 'NONE',  ( -82.88436837210520025, -29.99999999999999645, 152.0600583881144132 ) ) ;
#95695=CARTESIAN_POINT ( 'NONE',  ( 91.17736083037920025, -57.61337127814945802, 204.2034886438755166 ) ) ;
#95697=CARTESIAN_POINT ( 'NONE',  ( 59.86708669470515787, -21.77003396638972532, -23.08968796104069909 ) ) ;
#95703=CARTESIAN_POINT ( 'NONE',  ( -53.48817481113404426, -59.99999999999999289, 80.99915126202921556 ) ) ;
#95710=CARTESIAN_POINT ( 'NONE',  ( -85.68467769695706693, -39.26620762603923254, 186.0355029637988480 ) ) ;
#95711=ORIENTED_EDGE ( 'NONE', *, *, #90266, .F. ) ;
#95718=CARTESIAN_POINT ( 'NONE',  ( -84.35224106894892770, -60.17954417897186659, -17.01416247631696166 ) ) ;
#95723=CARTESIAN_POINT ( 'NONE',  ( 3.088855081073062209E-15, -4.285714285714286476, 25.22241582816893413 ) ) ;
#95725=CARTESIAN_POINT ( 'NONE',  ( 86.58362542449755495, -60.00000000000002132, -26.27920600484676683 ) ) ;
#95726=CARTESIAN_POINT ( 'NONE',  ( -77.55089032165899710, -49.90769110663840991, 141.6289234985631538 ) ) ;
#95729=FILL_AREA_STYLE ('',( #36995 ) ) ;
#95731=CARTESIAN_POINT ( 'NONE',  ( 79.56404080552624691, -57.50631293715987624, 198.4392659916153150 ) ) ;
#95750=CARTESIAN_POINT ( 'NONE',  ( -66.01875947964627755, -14.21045842199442077, 101.7785962432973292 ) ) ;
#95751=CARTESIAN_POINT ( 'NONE',  ( 26.10287486467459317, -39.47800315929696779, 32.00527294968382819 ) ) ;
#95756=UNCERTAINTY_MEASURE_WITH_UNIT (LENGTH_MEASURE( 1.000000000000000082E-05 ), #21727, 'distance_accuracy_value', 'NONE');
#95758=CARTESIAN_POINT ( 'NONE',  ( -21.88880945939638067, -4.285714285714295357, -12.64023069600375138 ) ) ;
#95768=CARTESIAN_POINT ( 'NONE',  ( 53.08934989192468379, -29.99999999999999289, 52.21148837440650681 ) ) ;
#95772=CARTESIAN_POINT ( 'NONE',  ( 81.13063282006866928, -30.00000000000000711, 1.952550465599699470 ) ) ;
#95794=AXIS2_PLACEMENT_3D ( 'NONE', #41080, #56163, #89105 ) ;
#95797=PRODUCT_DEFINITION_SHAPE ( 'NONE', 'NONE',  #17933 ) ;
#95798=CARTESIAN_POINT ( 'NONE',  ( 63.73364275548575364, -22.10444409302240132, 73.75141016224915802 ) ) ;
#95809=CARTESIAN_POINT ( 'NONE',  ( 40.03204023273700329, -60.00000000000002842, -33.82007831649015372 ) ) ;
#95815=CARTESIAN_POINT ( 'NONE',  ( 86.66175704258623114, -20.68399464850984870, 184.7485519202856210 ) ) ;
#95824=CARTESIAN_POINT ( 'NONE',  ( -99.07703161370366729, -30.00000000000000000, 145.6223805078784324 ) ) ;
#95827=CARTESIAN_POINT ( 'NONE',  ( 42.44169098129961526, -57.68683908594360332, 59.94108253702619749 ) ) ;
#95836=CARTESIAN_POINT ( 'NONE',  ( -87.15677342750342405, -53.73642251599375896, 193.0054991913189042 ) ) ;
#95840=CARTESIAN_POINT ( 'NONE',  ( -11.40776449738530474, -46.43936320564299081, 31.65861530297792825 ) ) ;
#95842=CARTESIAN_POINT ( 'NONE',  ( -101.2984257039321818, -59.99999999999997868, 123.3486402982567398 ) ) ;
#95850=CARTESIAN_POINT ( 'NONE',  ( 73.51678032629719439, -60.00000000000000000, 167.3558390227925088 ) ) ;
#95875=CARTESIAN_POINT ( 'NONE',  ( -94.29423131824410120, -59.99999999999747757, 204.9864844129882044 ) ) ;
#95878=CARTESIAN_POINT ( 'NONE',  ( 49.62012381316495890, -59.99999999999997868, 70.85806097636194067 ) ) ;
#95881=CARTESIAN_POINT ( 'NONE',  ( -102.6949714452557885, -14.21045842199446518, 129.2658233771313974 ) ) ;
#95882=CARTESIAN_POINT ( 'NONE',  ( 12.44414058928305344, -42.95372205198454196, 31.10491182296270196 ) ) ;
#95884=CARTESIAN_POINT ( 'NONE',  ( -46.99575457356646524, -18.77608308516024849, 40.16000815951232283 ) ) ;
#95893=CARTESIAN_POINT ( 'NONE',  ( 84.89073916653602225, -30.00000000000001776, 197.0696916040373026 ) ) ;
#95897=CARTESIAN_POINT ( 'NONE',  ( 94.82639388037442529, -30.00000000000000355, 191.3365978075416933 ) ) ;
#95909=CARTESIAN_POINT ( 'NONE',  ( -76.12537862032631608, -38.35598417008158378, -28.58435412235099804 ) ) ;
#95912=CARTESIAN_POINT ( 'NONE',  ( 102.3932405693164611, -38.43728085762052160, 199.4716403674687513 ) ) ;
#95914=CARTESIAN_POINT ( 'NONE',  ( 83.78544372828790188, -45.28299759132907099, 18.52600201645970657 ) ) ;
#95934=CARTESIAN_POINT ( 'NONE',  ( -36.76540882621739570, -27.25414842009635663, 43.58040692005798888 ) ) ;
#95941=CARTESIAN_POINT ( 'NONE',  ( 85.45182810718637256, -39.29543685595842106, 185.3021898051531196 ) ) ;
#95943=EDGE_CURVE ( 'NONE', #72232, #77351, #8646, .T. ) ;
#95946=CARTESIAN_POINT ( 'NONE',  ( 94.01656501709089753, -57.67294275299069284, 19.38523437918474102 ) ) ;
#95953=CARTESIAN_POINT ( 'NONE',  ( 15.09797279524721425, -22.74424748559674470, 35.94748513521482636 ) ) ;
#95954=CARTESIAN_POINT ( 'NONE',  ( 48.75403305889158645, -29.43289434049833986, 44.67303107480096003 ) ) ;
#95960=CARTESIAN_POINT ( 'NONE',  ( -39.51997949802257182, -33.17322444800073811, -29.37170241217619449 ) ) ;
#95962=CARTESIAN_POINT ( 'NONE',  ( -95.03937034330597555, -38.00000000000000000, 107.8039155741109738 ) ) ;
#95964=ORIENTED_EDGE ( 'NONE', *, *, #32326, .T. ) ;
#95970=CARTESIAN_POINT ( 'NONE',  ( -41.98950613031892942, -60.22824704085319780, -33.55409513438841174 ) ) ;
#95977=CARTESIAN_POINT ( 'NONE',  ( -92.53812791416793004, -60.00000000000000711, -1.816796087269537008 ) ) ;
#95985=CARTESIAN_POINT ( 'NONE',  ( -83.63428025110276565, -25.61067944322265433, 154.1989751819577634 ) ) ;
#95988=CARTESIAN_POINT ( 'NONE',  ( -16.14668631625900019, -0.000000000000000000, -5.483261958887230669 ) ) ;
#95998=CARTESIAN_POINT ( 'NONE',  ( -94.30950767697063952, -57.61975185784459086, 204.5257163505249309 ) ) ;
#96004=CARTESIAN_POINT ( 'NONE',  ( 79.45700042099618088, -60.00000000000000711, -30.99979279722015590 ) ) ;
#96005=CARTESIAN_POINT ( 'NONE',  ( -61.00210428163805432, -14.21045842199449005, 86.20094954650318186 ) ) ;
#96006=CARTESIAN_POINT ( 'NONE',  ( -56.92782483176372921, -32.55445101946592246, 61.63125569926470604 ) ) ;
#96011=CARTESIAN_POINT ( 'NONE',  ( -101.3713891769874778, -45.26458131978182564, 190.6351527844882980 ) ) ;
#96015=CARTESIAN_POINT ( 'NONE',  ( 110.7700795740980197, -38.35618397565083626, 179.7263034240603474 ) ) ;
#96027=CARTESIAN_POINT ( 'NONE',  ( -28.52589013025375664, -25.58464632904579261, 30.19568687849871935 ) ) ;
#96030=CARTESIAN_POINT ( 'NONE',  ( 48.17486088641305741, -56.81898877664855974, 53.29977222331121567 ) ) ;
#96034=CARTESIAN_POINT ( 'NONE',  ( -110.7787815506858209, -38.35615617498751106, 165.0880282141192765 ) ) ;
#96037=CARTESIAN_POINT ( 'NONE',  ( 87.50928707171397036, -38.36873170751620421, -20.25758776273239903 ) ) ;
#96046=CARTESIAN_POINT ( 'NONE',  ( 84.12166230012984158, -60.00000000000000711, 199.5799458206678878 ) ) ;
#96050=CARTESIAN_POINT ( 'NONE',  ( 55.38483915043129002, -46.43683086870206012, 64.00419006234304220 ) ) ;
#96055=CARTESIAN_POINT ( 'NONE',  ( -101.6643687224884616, -38.44986872770192576, 199.8638131606589923 ) ) ;
#96064=CARTESIAN_POINT ( 'NONE',  ( 82.08679795893965547, -49.97481940385915067, 177.5961885972273251 ) ) ;
#96078=CARTESIAN_POINT ( 'NONE',  ( -81.02657573093092935, -30.00000000000000000, 21.43806085364088077 ) ) ;
#96104=CARTESIAN_POINT ( 'NONE',  ( -112.1392827011767537, -60.00000000000000000, 167.2709583566187916 ) ) ;
#96110=CARTESIAN_POINT ( 'NONE',  ( -85.66377476482907127, -25.20926228141058800, 174.6162987478353728 ) ) ;
#96118=CARTESIAN_POINT ( 'NONE',  ( -86.12765991300337021, -60.14013167474347199, 11.25586421641007284 ) ) ;
#96126=CARTESIAN_POINT ( 'NONE',  ( 78.95048871113250755, -29.99999999999999645, 188.4614743794136871 ) ) ;
#96127=CARTESIAN_POINT ( 'NONE',  ( -108.2372990039095271, -60.00000000000000000, 115.4700740038245499 ) ) ;
#96128=CARTESIAN_POINT ( 'NONE',  ( -62.81791404775724175, -53.39247542489125919, 86.98738384603005613 ) ) ;
#96131=CARTESIAN_POINT ( 'NONE',  ( 80.31347780062725406, -60.00000000002691536, 200.0034699237392601 ) ) ;
#96143=CARTESIAN_POINT ( 'NONE',  ( -86.98208477778736381, -60.00000000000001421, -22.74275743632538749 ) ) ;
#96148=DIRECTION ( 'NONE',  ( 0.000000000000000000, 0.000000000000000000, -1.000000000000000000 ) ) ;
#96154=CARTESIAN_POINT ( 'NONE',  ( -38.12989804336692146, -18.75727802424759361, 32.82810357043974392 ) ) ;
#96160=CARTESIAN_POINT ( 'NONE',  ( 35.82070543335183288, -18.72939031532795440, 31.62416683920327287 ) ) ;
#96161=CARTESIAN_POINT ( 'NONE',  ( 21.65942590380565491, 2.899645552008857721E-12, 5.820808985964478488 ) ) ;
#96178=CARTESIAN_POINT ( 'NONE',  ( 94.32096871168523933, -60.00000000000000711, 43.89811362915176574 ) ) ;
#96182=ORIENTED_EDGE ( 'NONE', *, *, #30939, .F. ) ;
#96185=CARTESIAN_POINT ( 'NONE',  ( -89.94601218680125498, -30.00000000001251266, -10.37167675054645066 ) ) ;
#96202=CARTESIAN_POINT ( 'NONE',  ( 78.40831120363421292, -56.84011713593565673, 154.9006849491204036 ) ) ;
#96209=CARTESIAN_POINT ( 'NONE',  ( -29.91071955673133687, -57.68399870184025247, 45.22199076326395328 ) ) ;
#96220=CARTESIAN_POINT ( 'NONE',  ( -10.70060044141619215, -13.94213797727864623, 31.85821448878728290 ) ) ;
#96234=CARTESIAN_POINT ( 'NONE',  ( 60.33857676659169300, -29.90340425700747673, -32.82934671700747487 ) ) ;
#96235=CARTESIAN_POINT ( 'NONE',  ( -81.32146438466961058, -29.99999999999999645, 141.8559041851008828 ) ) ;
#96241=CARTESIAN_POINT ( 'NONE',  ( 96.78308981908668329, -57.62245937922295980, 204.4637576706275581 ) ) ;
#96243=CARTESIAN_POINT ( 'NONE',  ( 66.87521826036821437, -21.77028756581515623, -20.76402545033162284 ) ) ;
#96251=CARTESIAN_POINT ( 'NONE',  ( -72.04520221236295185, -60.00000000000000711, 154.6154111227524766 ) ) ;
#96257=CARTESIAN_POINT ( 'NONE',  ( -85.04220142028198381, -50.19910149378929276, 189.2836192048938244 ) ) ;
#96269=CARTESIAN_POINT ( 'NONE',  ( -24.56594385547996140, -4.285714285713227767, 6.601913983196856073 ) ) ;
#96273=CARTESIAN_POINT ( 'NONE',  ( 84.17695284478443796, -14.21045842199441367, -18.06956050794424584 ) ) ;
#96274=CARTESIAN_POINT ( 'NONE',  ( -78.12100248001522118, -56.84623792800805120, 152.8030804558065938 ) ) ;
#96276=CARTESIAN_POINT ( 'NONE',  ( 24.48575568784926304, -14.21045842199439946, 35.52093559979998361 ) ) ;
#96278=CARTESIAN_POINT ( 'NONE',  ( 106.0311746394521037, -57.64931060779116478, 200.9292066482266534 ) ) ;
#96287=CARTESIAN_POINT ( 'NONE',  ( -103.3976274097190071, -52.71035023079828363, 146.8235736524452193 ) ) ;
#96299=CARTESIAN_POINT ( 'NONE',  ( 24.76367760800922113, -35.99787462728398424, 31.10278417371337767 ) ) ;
#96304=FACE_BOUND ( 'NONE', #70330, .T. ) ;
#96311=CARTESIAN_POINT ( 'NONE',  ( 49.72939441809057115, -60.00000000000001421, -37.95769542429952281 ) ) ;
#96338=CARTESIAN_POINT ( 'NONE',  ( -80.12203077669109064, -60.00000000000006395, 175.6696548227984351 ) ) ;
#96339=CARTESIAN_POINT ( 'NONE',  ( 62.81860187692696229, -53.38668648289181107, 86.98641772761070001 ) ) ;
#96344=CYLINDRICAL_SURFACE ( 'NONE', #91167, 2.000000000000001776 ) ;
#96345=ORIENTED_EDGE ( 'NONE', *, *, #17173, .F. ) ;
#96348=CARTESIAN_POINT ( 'NONE',  ( 72.07940662483305516, -59.99999999999998579, -25.51851818892304635 ) ) ;
#96352=CARTESIAN_POINT ( 'NONE',  ( 86.50032125490628232, -17.01892177610816859, 184.1023120340136359 ) ) ;
#96358=( LENGTH_UNIT ( ) NAMED_UNIT ( * ) SI_UNIT ( .MILLI., .METRE. ) );
#96362=CARTESIAN_POINT ( 'NONE',  ( 29.59573307755961480, -59.99999999999998579, 42.83999512026873902 ) ) ;
#96363=CARTESIAN_POINT ( 'NONE',  ( -99.16875731687827056, -30.00000000000000000, 146.3660697992883968 ) ) ;
#96367=CARTESIAN_POINT ( 'NONE',  ( 44.76088533861224761, -57.68343184253352263, 64.64529994903629984 ) ) ;
#96376=CARTESIAN_POINT ( 'NONE',  ( -15.78091564468949848, -59.99999999999999289, 39.83881286635372732 ) ) ;
#96378=CARTESIAN_POINT ( 'NONE',  ( -87.07081158247649455, -24.31846254880739266, 186.7358293699816727 ) ) ;
#96382=CARTESIAN_POINT ( 'NONE',  ( -15.83958888108630703, -49.92074823066483447, 32.40208527561495089 ) ) ;
#96384=CARTESIAN_POINT ( 'NONE',  ( -87.01178792140694895, -60.00000000000005684, -6.909150771205774255 ) ) ;
#96391=CARTESIAN_POINT ( 'NONE',  ( 72.07854270695700905, -60.00000000000000000, 154.8658330893785546 ) ) ;
#96396=CARTESIAN_POINT ( 'NONE',  ( 48.80991865481109215, -14.21045842199436215, 55.83985330155353921 ) ) ;
#96409=MECHANICAL_DESIGN_GEOMETRIC_PRESENTATION_REPRESENTATION('',(#36157),#58528);
#96410=CARTESIAN_POINT ( 'NONE',  ( -109.0008218237458379, -59.99999999999387512, 198.3904110863214498 ) ) ;
#96413=CARTESIAN_POINT ( 'NONE',  ( 42.98998915891669981, -59.99999999999998579, 56.82525478121357310 ) ) ;
#96416=CARTESIAN_POINT ( 'NONE',  ( -109.0818456041877766, -30.00000000000003908, 182.6288557207085148 ) ) ;
#96417=CARTESIAN_POINT ( 'NONE',  ( 12.26502348511670171, -29.02967927662671599, 28.77873360239995648 ) ) ;
#96418=CARTESIAN_POINT ( 'NONE',  ( 84.67820983338387464, -37.99999999999997158, 42.84007939968466161 ) ) ;
#96421=CARTESIAN_POINT ( 'NONE',  ( -45.65210561564843772, -53.35409427601360477, 48.30568668782035502 ) ) ;
#96431=CARTESIAN_POINT ( 'NONE',  ( 79.03822195096249459, -29.99999999999494804, 187.3972024871379176 ) ) ;
#96433=CARTESIAN_POINT ( 'NONE',  ( 100.3334076089338112, -30.00000000000000000, 183.9054159315834909 ) ) ;
#96448=CARTESIAN_POINT ( 'NONE',  ( 100.3166457666017237, -38.46339582723162920, 200.4016571423995856 ) ) ;
#96450=CARTESIAN_POINT ( 'NONE',  ( 84.45185607837281339, -45.28786482119996748, -4.595507990911970708 ) ) ;
#96451=CARTESIAN_POINT ( 'NONE',  ( 61.29076810083007842, -38.00000000000000711, 74.90883847999660361 ) ) ;
#96469=CARTESIAN_POINT ( 'NONE',  ( -41.97394556256499953, -29.24123356747789160, 50.03082711761693702 ) ) ;
#96473=CARTESIAN_POINT ( 'NONE',  ( 84.97747700260335080, -42.94964189027161439, 185.6624707830199554 ) ) ;
#96477=CARTESIAN_POINT ( 'NONE',  ( 94.40184081913845660, -57.67114072026561900, -0.1777694819485469147 ) ) ;
#96492=CARTESIAN_POINT ( 'NONE',  ( -90.58776433791602756, -37.99999999999997158, 81.87422108073580773 ) ) ;
#96497=ADVANCED_FACE ( 'NONE', ( #50675 ), #7182, .F. ) ;
#96503=CARTESIAN_POINT ( 'NONE',  ( -58.42930312626833711, -21.77003758643937203, -23.50835556100766510 ) ) ;
#96512=CARTESIAN_POINT ( 'NONE',  ( -92.62061861149213371, -60.00000000000000711, -10.08911953426519403 ) ) ;
#96516=CARTESIAN_POINT ( 'NONE',  ( 99.29740484581111559, -45.26881857393725994, 193.1476703519705893 ) ) ;
#96520=CARTESIAN_POINT ( 'NONE',  ( -83.37668499989145232, -32.53985942674935927, 162.2598532935533626 ) ) ;
#96529=CARTESIAN_POINT ( 'NONE',  ( -82.98668029349501296, -57.53378708018315280, 201.1759417985833238 ) ) ;
#96535=CARTESIAN_POINT ( 'NONE',  ( 94.49477393579812201, -60.00000000000003553, -13.88944369105108301 ) ) ;
#96536=CARTESIAN_POINT ( 'NONE',  ( -69.92584042677506773, -30.00000000000002842, 127.5397447585766599 ) ) ;
#96538=CARTESIAN_POINT ( 'NONE',  ( -54.56892480951270841, -22.15834078237627480, 52.62495691221676708 ) ) ;
#96542=CARTESIAN_POINT ( 'NONE',  ( -102.9241234416141282, -60.17493127080694393, 192.9570147602996144 ) ) ;
#96546=CARTESIAN_POINT ( 'NONE',  ( 110.9944082960603140, -38.35619069247599100, 173.2626205915072717 ) ) ;
#96551=CARTESIAN_POINT ( 'NONE',  ( 54.58541135956112100, -30.00000000000001066, 54.90165979975594013 ) ) ;
#96561=CARTESIAN_POINT ( 'NONE',  ( 48.92534730531904330, -18.75215370966537520, 42.51723731469244427 ) ) ;
#96564=CARTESIAN_POINT ( 'NONE',  ( -104.4412629575702738, -38.40429514389773402, 198.0193396095312437 ) ) ;
#96566=CARTESIAN_POINT ( 'NONE',  ( 88.37099315902020180, -38.37563564094526214, -19.06208899794795997 ) ) ;
#96570=CARTESIAN_POINT ( 'NONE',  ( 94.36110561261105545, -45.28273083012499001, 96.73308552606165733 ) ) ;
#96575=CARTESIAN_POINT ( 'NONE',  ( 99.43937970958685924, -59.99999999999999289, 202.0376968176740888 ) ) ;
#96580=CARTESIAN_POINT ( 'NONE',  ( 56.69983827852902891, -53.38006274212794722, 70.12899238981250960 ) ) ;
#96586=CARTESIAN_POINT ( 'NONE',  ( -106.7662800213460628, -38.36637556396474480, 195.2415563008339348 ) ) ;
#96597=CARTESIAN_POINT ( 'NONE',  ( 84.83629015364854808, -28.93020097267356050, 170.9427086118279817 ) ) ;
#96633=CARTESIAN_POINT ( 'NONE',  ( -108.0975085614644513, -60.00000000000000000, 129.7140120509529595 ) ) ;
#96634=DIRECTION ( 'NONE',  ( 1.000000000000000000, 0.000000000000000000, 0.000000000000000000 ) ) ;
#96638=CARTESIAN_POINT ( 'NONE',  ( -86.25780443371026251, -18.23629696712657022, 169.8396338056661534 ) ) ;
#96646=CARTESIAN_POINT ( 'NONE',  ( -83.66830488457027570, -45.26507799069083404, 12.12265221865681042 ) ) ;
#96652=CARTESIAN_POINT ( 'NONE',  ( 88.35660587733796945, -14.21045842199459486, 197.0604887900697122 ) ) ;
#96654=CARTESIAN_POINT ( 'NONE',  ( -91.50803816462422446, -30.00000000000001776, 42.72771024551138908 ) ) ;
#96656=CARTESIAN_POINT ( 'NONE',  ( -61.11614492808612908, -53.39328282429821826, 82.02358402482038002 ) ) ;
#96659=CARTESIAN_POINT ( 'NONE',  ( 96.79493678139994017, -59.99999999999132427, 204.9247966883611980 ) ) ;
#96661=CARTESIAN_POINT ( 'NONE',  ( 3.081314264678424397, -56.87780286871037561, 33.36400653726988708 ) ) ;
#96669=CARTESIAN_POINT ( 'NONE',  ( -93.08565485029603792, -60.00000000000000000, 33.23478458921270828 ) ) ;
#96679=CARTESIAN_POINT ( 'NONE',  ( -34.85857064921750492, -22.18165287194634416, 31.84054876490759156 ) ) ;
#96683=CARTESIAN_POINT ( 'NONE',  ( 40.48137601666525853, -22.23684450456674710, 35.13079649809134963 ) ) ;
#96685=CARTESIAN_POINT ( 'NONE',  ( -14.86825985027621755, -1.734723475976807094E-15, 8.569529079659670145 ) ) ;
#96689=CARTESIAN_POINT ( 'NONE',  ( -75.45914410051923937, -38.35135203049976838, 173.8682629998443758 ) ) ;
#96700=CARTESIAN_POINT ( 'NONE',  ( 95.10565317760159587, -60.00000000000000711, 49.79938089396723200 ) ) ;
#96705=EDGE_CURVE ( 'NONE', #45904, #102350, #47234, .T. ) ;
#96708=CARTESIAN_POINT ( 'NONE',  ( -88.42496338177498671, -30.00000000000168399, -16.19662829210094301 ) ) ;
#96723=CARTESIAN_POINT ( 'NONE',  ( 80.44587350599928754, -49.90936352864175518, 162.4342867686268903 ) ) ;
#96734=CARTESIAN_POINT ( 'NONE',  ( -23.49283269198559765, -57.67355083020559192, 42.82390242447587525 ) ) ;
#96745=CARTESIAN_POINT ( 'NONE',  ( -7.127421841361177179, -13.18528672947971891, 32.02679007952325918 ) ) ;
#96756=CARTESIAN_POINT ( 'NONE',  ( -57.63211173758740813, -37.00413535841546775, -34.72254536230725819 ) ) ;
#96763=CARTESIAN_POINT ( 'NONE',  ( 100.5645707510053626, -57.62842971074093157, 203.7695601258284057 ) ) ;
#96765=CARTESIAN_POINT ( 'NONE',  ( 58.43705451886171431, -47.40890191778955653, -27.93287016854851501 ) ) ;
#96770=CARTESIAN_POINT ( 'NONE',  ( -73.50277685114647852, -59.99999999999999289, 167.2174948213626351 ) ) ;
#96775=CARTESIAN_POINT ( 'NONE',  ( -85.72959342069100330, -35.64893082154279824, 184.4343426154862584 ) ) ;
#96788=CARTESIAN_POINT ( 'NONE',  ( 2.723397405354400211E-15, -8.673617379884035472E-16, 22.23822744035697241 ) ) ;
#96790=CARTESIAN_POINT ( 'NONE',  ( 95.02194560458454475, -59.99999999999987210, -3.233414228271875857 ) ) ;
#96791=CARTESIAN_POINT ( 'NONE',  ( -77.83469039265052913, -56.84582962964739750, 150.7048350401225889 ) ) ;
#96793=CARTESIAN_POINT ( 'NONE',  ( 41.69321614992608716, -29.99999999999995737, 49.76314934024226488 ) ) ;
#96795=CARTESIAN_POINT ( 'NONE',  ( 72.54833963118097984, -57.66457796962676952, 177.4209049984457636 ) ) ;
#96804=CARTESIAN_POINT ( 'NONE',  ( -101.6938598978349262, -37.82055728416436580, 153.9927469340554183 ) ) ;
#96807=AXIS2_PLACEMENT_3D ( 'NONE', #52674, #18218, #51069 ) ;
#96816=CARTESIAN_POINT ( 'NONE',  ( 26.23477066092984700, -42.95572057826144885, 32.63390350353837022 ) ) ;
#96830=CARTESIAN_POINT ( 'NONE',  ( 15.26350624587492000, -59.99999999999998579, -42.14653362384034807 ) ) ;
#96831=CARTESIAN_POINT ( 'NONE',  ( 54.95194601437927417, -29.99999999999999289, 55.56075107115263734 ) ) ;
#96858=CARTESIAN_POINT ( 'NONE',  ( 63.00956775988831993, -39.48292126951590575, 80.42806493650408584 ) ) ;
#96868=CARTESIAN_POINT ( 'NONE',  ( 86.83143111513136603, -35.42916943998449142, 187.7786419653708094 ) ) ;
#96876=CARTESIAN_POINT ( 'NONE',  ( 25.76161585170470403, -60.00000000000001421, 41.38317439764583128 ) ) ;
#96877=CARTESIAN_POINT ( 'NONE',  ( -98.98182216182540571, -30.00000000000000711, 144.8605357131832534 ) ) ;
#96881=CARTESIAN_POINT ( 'NONE',  ( 52.17267667566792255, -57.67659005738761380, 83.18092912029068486 ) ) ;
#96890=CARTESIAN_POINT ( 'NONE',  ( -8.202091538805017734, -59.99999999999997868, 39.63445737841648508 ) ) ;
#96892=CARTESIAN_POINT ( 'NONE',  ( 1.911035399909858157, -15.42382690385200306, -35.21246151727765294 ) ) ;
#96897=CARTESIAN_POINT ( 'NONE',  ( -11.44799901505533946, -49.92097670987179470, 32.23970761380233796 ) ) ;
#96899=CARTESIAN_POINT ( 'NONE',  ( -88.95083730581535519, -60.00000000000000711, 47.31616727603900330 ) ) ;
#96909=CARTESIAN_POINT ( 'NONE',  ( 72.66458305811862317, -60.00000000000000711, 159.4996536347722156 ) ) ;
#96923=CARTESIAN_POINT ( 'NONE',  ( -104.7668148436344495, -60.00000000001475797, 202.3575108280591337 ) ) ;
#96925=CARTESIAN_POINT ( 'NONE',  ( 76.75507714372903934, -60.00000000000002132, 189.7492337977039654 ) ) ;
#96928=CARTESIAN_POINT ( 'NONE',  ( -108.5047409391136455, -30.00000000000001776, 153.5997188701533105 ) ) ;
#96929=CARTESIAN_POINT ( 'NONE',  ( 13.71723278984751815, -56.87769479953498575, 33.46138947822615251 ) ) ;
#96930=CARTESIAN_POINT ( 'NONE',  ( 82.72479378746378131, -37.99999999999997868, 3.475805411804568923 ) ) ;
#96932=CARTESIAN_POINT ( 'NONE',  ( -46.36168458591362196, -60.26899542073847726, 51.31494294901810349 ) ) ;
#96936=DIRECTION ( 'NONE',  ( 0.000000000000000000, 0.000000000000000000, 1.000000000000000000 ) ) ;
#96946=CARTESIAN_POINT ( 'NONE',  ( 91.10875621309618566, -29.99999999996073896, 199.5150240557169354 ) ) ;
#96950=CARTESIAN_POINT ( 'NONE',  ( 99.76087090034495475, -30.00000000000000355, 151.2002837684392489 ) ) ;
#96966=CARTESIAN_POINT ( 'NONE',  ( 79.25291760674103614, -38.71628596270740985, 191.5093671535432520 ) ) ;
#96968=CARTESIAN_POINT ( 'NONE',  ( 82.98893668538087809, -37.84625678214262479, -0.6931496944285937545 ) ) ;
#96969=CARTESIAN_POINT ( 'NONE',  ( 80.69144941626747425, -37.99999999999993605, 148.5548834094500137 ) ) ;
#96988=VECTOR ( 'NONE', #11257, 1000.000000000000000 ) ;
#96993=CARTESIAN_POINT ( 'NONE',  ( 85.70847550465963138, -32.07071322668284807, 182.3195111745817769 ) ) ;
#96996=CARTESIAN_POINT ( 'NONE',  ( 94.76232204274911908, -57.67206613426113648, 30.20201912920926901 ) ) ;
#97007=CARTESIAN_POINT ( 'NONE',  ( -31.04749644452845914, -30.39921546070477731, -30.04532190092515620 ) ) ;
#97016=CARTESIAN_POINT ( 'NONE',  ( -48.31675829002472256, -60.22826300482149975, -32.41392416354486983 ) ) ;
#97022=CARTESIAN_POINT ( 'NONE',  ( -91.89520039571972632, -60.00000000000000711, -14.34466715436823492 ) ) ;
#97026=CARTESIAN_POINT ( 'NONE',  ( 98.08802719723102825, -37.75359325362526874, 192.4663707679745244 ) ) ;
#97030=CARTESIAN_POINT ( 'NONE',  ( -80.33501531167325993, -56.88691000900035988, 172.5936903209407660 ) ) ;
#97041=CARTESIAN_POINT ( 'NONE',  ( -77.81697554521740301, -57.51284286114859157, 196.3444844341304929 ) ) ;
#97047=CARTESIAN_POINT ( 'NONE',  ( -75.59778980771257295, -60.00000000000000711, -32.85486631586996253 ) ) ;
#97048=CARTESIAN_POINT ( 'NONE',  ( -32.49743750560201505, -59.99999999999998579, 47.28107978972537495 ) ) ;
#97049=CARTESIAN_POINT ( 'NONE',  ( -52.96930251354979902, -22.17327373329827722, 49.74579268807322308 ) ) ;
#97053=CARTESIAN_POINT ( 'NONE',  ( -99.57258923306162046, -45.25279128809092555, 192.9568983376553035 ) ) ;
#97055=ORIENTED_EDGE ( 'NONE', *, *, #91312, .T. ) ;
#97057=CARTESIAN_POINT ( 'NONE',  ( 109.2343739603617507, -38.35611523210522478, 189.3471561603757038 ) ) ;
#97063=CARTESIAN_POINT ( 'NONE',  ( 85.00342762049730538, -29.99999999999999289, 170.3482649358438152 ) ) ;
#97065=FACE_OUTER_BOUND ( 'NONE', #81687, .T. ) ;
#97071=CARTESIAN_POINT ( 'NONE',  ( 49.74709343585908528, -32.58936152964536603, 48.06759981570923657 ) ) ;
#97072=DIRECTION ( 'NONE',  ( -0.000000000000000000, 1.000000000000000000, -0.000000000000000000 ) ) ;
#97076=CARTESIAN_POINT ( 'NONE',  ( -110.4642460645833637, -38.35610247955116137, 182.6975338912728262 ) ) ;
#97078=CARTESIAN_POINT ( 'NONE',  ( 89.17615470242493814, -38.38424890164885284, -17.73986973391627231 ) ) ;
#97082=CARTESIAN_POINT ( 'NONE',  ( 101.2421465956972355, -45.28276229600517411, 139.7551188333355014 ) ) ;
#97086=CIRCLE ( 'NONE', #102252, 1.999999999999998224 ) ;
#97088=CARTESIAN_POINT ( 'NONE',  ( 83.18737980040994273, -60.00000000000000000, 198.9619646874331522 ) ) ;
#97093=CARTESIAN_POINT ( 'NONE',  ( 54.89891884253371757, -56.84790269950949693, 67.23841002115719334 ) ) ;
#97099=CARTESIAN_POINT ( 'NONE',  ( -108.4974870776933216, -38.35706132716640582, 191.6606617528426852 ) ) ;
#97108=CARTESIAN_POINT ( 'NONE',  ( 84.37186861624395817, -32.45071114265312673, 171.8667827280741562 ) ) ;
#97144=CARTESIAN_POINT ( 'NONE',  ( -109.9681397012935378, -60.00000000000001421, 143.1854525654455870 ) ) ;
#97151=CARTESIAN_POINT ( 'NONE',  ( -82.76128424870692868, -46.49188429553897350, 178.0646004425870501 ) ) ;
#97165=CARTESIAN_POINT ( 'NONE',  ( 109.0818019194042847, -30.00000000000000355, 182.6293461004923131 ) ) ;
#97166=CARTESIAN_POINT ( 'NONE',  ( -104.6655502547336738, -29.99999999999993250, 124.7729330896767408 ) ) ;
#97167=CARTESIAN_POINT ( 'NONE',  ( -63.09091515402169392, -32.53411138963832627, 77.17286524773658130 ) ) ;
#97170=CARTESIAN_POINT ( 'NONE',  ( 74.89656030667543973, -59.99999999998028244, 191.9882623802560317 ) ) ;
#97172=FACE_OUTER_BOUND ( 'NONE', #65582, .T. ) ;
#97183=CARTESIAN_POINT ( 'NONE',  ( -106.6622389571683129, -60.00000000000001421, 197.5332747654210266 ) ) ;
#97195=CARTESIAN_POINT ( 'NONE',  ( -33.33496386269368372, -60.31377368949035400, 38.34004965045540558 ) ) ;
#97198=CARTESIAN_POINT ( 'NONE',  ( 41.52545057012824969, -22.24250618979461791, 35.91399818572732983 ) ) ;
#97199=CARTESIAN_POINT ( 'NONE',  ( 13.60704923275372202, -1.734723475976807094E-15, 10.45706415777666365 ) ) ;
#97202=CARTESIAN_POINT ( 'NONE',  ( -57.79103112299724643, -38.34425813298624064, 89.61988761945933391 ) ) ;
#97212=CARTESIAN_POINT ( 'NONE',  ( 95.41688625546588298, -60.00000000000000711, 52.01396517246381279 ) ) ;
#97220=CARTESIAN_POINT ( 'NONE',  ( -56.65595402317139673, -29.99999999999999289, 59.14054006920170536 ) ) ;
#97238=CARTESIAN_POINT ( 'NONE',  ( 78.52592673875363971, -60.31111541565864798, 160.5468623774698926 ) ) ;
#97246=CARTESIAN_POINT ( 'NONE',  ( -66.37944403907447111, -57.68041551771388953, 132.8370836190597686 ) ) ;
#97258=CARTESIAN_POINT ( 'NONE',  ( -34.55953967696941476, -23.85835632124947736, 33.33342719774777407 ) ) ;
#97269=CARTESIAN_POINT ( 'NONE',  ( -56.61081697993206774, -29.99999999999999289, 59.00319635214307112 ) ) ;
#97274=CARTESIAN_POINT ( 'NONE',  ( 101.8386296196878504, -57.63167174066484932, 203.3325908020501913 ) ) ;
#97278=CARTESIAN_POINT ( 'NONE',  ( -75.06267738998585060, -60.00000000000000000, 181.7393887267853074 ) ) ;
#97282=CARTESIAN_POINT ( 'NONE',  ( -85.45145498079543245, -39.29912314789010708, 185.3035127737040000 ) ) ;
#97290=CARTESIAN_POINT ( 'NONE',  ( -82.31759468112190348, -37.78304723879290350, -13.10579271544666824 ) ) ;
#97297=CARTESIAN_POINT ( 'NONE',  ( 17.78317311658683408, 9.642355526980000143E-13, 13.66642973271509831 ) ) ;
#97299=CARTESIAN_POINT ( 'NONE',  ( 86.47489896066092285, -14.21045842199428932, -14.67047700064687987 ) ) ;
#97300=CARTESIAN_POINT ( 'NONE',  ( -73.95641269737396328, -53.38221346759030439, 126.4400680314501386 ) ) ;
#97302=CARTESIAN_POINT ( 'NONE',  ( 34.32456002071940304, -30.00000000000004263, 42.48759634994703305 ) ) ;
#97304=CARTESIAN_POINT ( 'NONE',  ( 83.66466658337685658, -57.54292938958637649, 201.5661420244404098 ) ) ;
#97324=CARTESIAN_POINT ( 'NONE',  ( -28.47812542966827110, -14.21045842199436926, 36.49899343628653270 ) ) ;
#97325=CARTESIAN_POINT ( 'NONE',  ( 30.12050400343885670, -60.32946261704295665, 36.84871485504820754 ) ) ;
#97336=CARTESIAN_POINT ( 'NONE',  ( 8.020137790548009349, -59.99999999999997868, -42.49116362023697491 ) ) ;
#97337=CARTESIAN_POINT ( 'NONE',  ( 84.45351475738571878, -30.00000000000000711, 165.1268496781745228 ) ) ;
#97362=CARTESIAN_POINT ( 'NONE',  ( 67.81700998233858968, -49.90853710843107649, 100.7767112817635962 ) ) ;
#97384=CARTESIAN_POINT ( 'NONE',  ( 18.35737871519194897, -59.99999999999998579, 40.03727238643882202 ) ) ;
#97385=CARTESIAN_POINT ( 'NONE',  ( -97.91306529131917102, -30.00000000000001066, 190.6200330007610830 ) ) ;
#97387=CARTESIAN_POINT ( 'NONE',  ( 51.82355698883625195, -57.67687465298720184, 82.20230154831503455 ) ) ;
#97390=CARTESIAN_POINT ( 'NONE',  ( 5.094487508937581843, -21.66492762252005733, -38.54749912668833645 ) ) ;
#97394=CARTESIAN_POINT ( 'NONE',  ( -25.28100474081467297, -60.00000000000000000, 41.24667794035808299 ) ) ;
#97396=CARTESIAN_POINT ( 'NONE',  ( -86.82857037991892923, -24.34865412473423874, 185.7447558296186116 ) ) ;
#97400=CARTESIAN_POINT ( 'NONE',  ( -12.39957699862355867, -39.47617499352052306, 30.52395290649034720 ) ) ;
#97402=CARTESIAN_POINT ( 'NONE',  ( -102.8242071241121494, -60.00000000000002132, 193.0618602036044251 ) ) ;
#97413=CARTESIAN_POINT ( 'NONE',  ( 73.19597753742192481, -59.99999999999999289, 164.2624391722602581 ) ) ;
#97419=CARTESIAN_POINT ( 'NONE',  ( 17.10696384799877379, -59.99999999999999289, 42.25337809451749393 ) ) ;
#97431=AXIS2_PLACEMENT_3D ( 'NONE', #32917, #33446, #49057 ) ;
#97433=CARTESIAN_POINT ( 'NONE',  ( -114.3713164436567808, -59.99999999998046718, 179.7174110124658171 ) ) ;
#97435=CARTESIAN_POINT ( 'NONE',  ( 59.88169702972975017, -60.00000000000000000, 100.0279864558745970 ) ) ;
#97438=CARTESIAN_POINT ( 'NONE',  ( -109.3240689110004524, -30.00000000000000355, 163.9542341103382057 ) ) ;
#97439=CARTESIAN_POINT ( 'NONE',  ( 17.67110049161424001, -29.03104148580605681, 29.02232790898393944 ) ) ;
#97440=CARTESIAN_POINT ( 'NONE',  ( 82.65902591454842252, -38.00000000000001421, 4.571707806879225622 ) ) ;
#97442=CARTESIAN_POINT ( 'NONE',  ( -45.26055152525536585, -18.78576083745453573, 38.35371795687179741 ) ) ;
#97459=CARTESIAN_POINT ( 'NONE',  ( 102.8143635727166725, -29.99999999998916778, 197.6080321013283196 ) ) ;
#97463=CARTESIAN_POINT ( 'NONE',  ( 92.40083123715065483, -30.00000000000000000, 102.5190540915925794 ) ) ;
#97476=CARTESIAN_POINT ( 'NONE',  ( 77.82015756661967032, -38.55211276278178900, 187.6246246428004554 ) ) ;
#97478=CARTESIAN_POINT ( 'NONE',  ( 60.26117253150567876, -38.00000000000000711, 72.16388681341805977 ) ) ;
#97497=CARTESIAN_POINT ( 'NONE',  ( 85.84491179312431086, -28.47452358815500872, 180.7459189754015085 ) ) ;
#97500=CARTESIAN_POINT ( 'NONE',  ( 95.55007516758162467, -57.67170984176614468, 37.60999171965882937 ) ) ;
#97507=CARTESIAN_POINT ( 'NONE',  ( -68.81967529573854847, -38.00000000000000711, 97.19646116308891237 ) ) ;
#97509=CARTESIAN_POINT ( 'NONE',  ( 52.75515435479064763, -30.00000000000000355, 51.54203667234443031 ) ) ;
#97522=CARTESIAN_POINT ( 'NONE',  ( 66.64570889441912982, -29.85741638960125144, -22.35595166279332346 ) ) ;
#97529=CARTESIAN_POINT ( 'NONE',  ( -53.22631969426956999, -34.58940849159185404, -27.04708426754712036 ) ) ;
#97537=CARTESIAN_POINT ( 'NONE',  ( -92.42151101069008234, -60.00000000000004263, -0.1434650216276215917 ) ) ;
#97540=CARTESIAN_POINT ( 'NONE',  ( 95.56019984581097049, -45.27097885572743508, 194.1693090572786957 ) ) ;
#97544=CARTESIAN_POINT ( 'NONE',  ( -82.82964344457306538, -36.02023518659409262, 162.7145647415955239 ) ) ;
#97558=CARTESIAN_POINT ( 'NONE',  ( -105.5530292394789882, -57.64680470462099038, 201.3003284212183246 ) ) ;
#97563=CARTESIAN_POINT ( 'NONE',  ( -24.50860473033056053, -14.21045842199433018, -36.19504829128915446 ) ) ;
#97564=CARTESIAN_POINT ( 'NONE',  ( -35.95074892501450847, -14.21045842199431242, 40.03088108345822604 ) ) ;
#97565=CARTESIAN_POINT ( 'NONE',  ( -55.06617873199689228, -22.15486436616988186, 53.58246572885349224 ) ) ;
#97568=CARTESIAN_POINT ( 'NONE',  ( -94.99629163939333409, -37.68183183142493675, 193.0097866583948587 ) ) ;
#97573=CARTESIAN_POINT ( 'NONE',  ( 89.79343125311589802, -38.39299482666958596, -16.49077915764583224 ) ) ;
#97578=CARTESIAN_POINT ( 'NONE',  ( 80.71650499981790006, -30.00000000000000000, 138.4101816275387762 ) ) ;
#97579=PLANE ( 'NONE',  #88947 ) ;
#97585=CARTESIAN_POINT ( 'NONE',  ( 49.07992270265078361, -53.36225572876357148, 53.76467797184545105 ) ) ;
#97593=CARTESIAN_POINT ( 'NONE',  ( -103.1838665334889811, -38.42661002002991211, 199.0052621351852622 ) ) ;
#97596=CARTESIAN_POINT ( 'NONE',  ( 110.3407746192199710, -38.35604946154091266, 158.5393008408863693 ) ) ;
#97600=CARTESIAN_POINT ( 'NONE',  ( 99.88553850844114379, -45.28285284022323509, 130.2282180348674956 ) ) ;
#97605=CARTESIAN_POINT ( 'NONE',  ( 98.72690313425520969, -60.00000000000001421, 202.2179184582266203 ) ) ;
#97611=CARTESIAN_POINT ( 'NONE',  ( 57.41795923026059967, -39.49217349359543761, 65.75899213438894719 ) ) ;
#97616=CARTESIAN_POINT ( 'NONE',  ( -88.77003120989235185, -38.37858000208290576, -18.43781038091345081 ) ) ;
#97626=CARTESIAN_POINT ( 'NONE',  ( 81.99978726385299410, -53.51631961905815160, 181.3751107682264490 ) ) ;
#97643=CARTESIAN_POINT ( 'NONE',  ( -22.00283802693145674, -27.01760079402097503, 37.33722609614333265 ) ) ;
#97667=CARTESIAN_POINT ( 'NONE',  ( -108.6743357863307011, -60.00000000000000711, 133.6544377956901997 ) ) ;
#97677=CARTESIAN_POINT ( 'NONE',  ( -84.06399816896501420, -35.95112890273957618, 174.2808740462292576 ) ) ;
#97691=CARTESIAN_POINT ( 'NONE',  ( 113.3390500081078613, -59.99999999999998579, 187.7085336688584221 ) ) ;
#97692=CARTESIAN_POINT ( 'NONE',  ( -105.8602000712061368, -14.21045842199440656, 153.6005699772977096 ) ) ;
#97693=CARTESIAN_POINT ( 'NONE',  ( -63.65786723876805553, -29.05667524070321761, 77.00078859873751469 ) ) ;
#97697=CARTESIAN_POINT ( 'NONE',  ( 114.4128415685117517, -60.00000000000000000, 179.0782004262347868 ) ) ;
#97699=CARTESIAN_POINT ( 'NONE',  ( 1.492275824608998712E-05, -32.51050348448658411, 29.30806720701680845 ) ) ;
#97708=CARTESIAN_POINT ( 'NONE',  ( -111.6036597322333392, -59.99999999999998579, 158.4792128661873107 ) ) ;
#97717=CARTESIAN_POINT ( 'NONE',  ( 97.58930920902680839, -60.00000000000000711, 101.0550937258192903 ) ) ;
#97718=CARTESIAN_POINT ( 'NONE',  ( -32.89073344312465252, -29.09100879441119147, 32.34260077112399756 ) ) ;
#97721=CARTESIAN_POINT ( 'NONE',  ( 38.48534256757758953, -25.67948113044661085, 34.55249355692391333 ) ) ;
#97725=CARTESIAN_POINT ( 'NONE',  ( -61.07287120190940044, -38.34218409855068899, 99.79094347136515353 ) ) ;
#97735=CARTESIAN_POINT ( 'NONE',  ( 100.7731613570876448, -59.99999999999998579, 85.56916059977524469 ) ) ;
#97740=CARTESIAN_POINT ( 'NONE',  ( -2.499999999999999556, -8.000000000000000000, 17.89626171146327493 ) ) ;
#97743=CARTESIAN_POINT ( 'NONE',  ( -90.05569471966944661, -29.99999999998339106, -4.911636287503251985 ) ) ;
#97751=DIRECTION ( 'NONE',  ( 0.000000000000000000, -1.000000000000000000, 0.000000000000000000 ) ) ;
#97760=CARTESIAN_POINT ( 'NONE',  ( 79.40570566424929666, -60.32724123763684787, 168.9258148112880349 ) ) ;
#97768=CIRCLE ( 'NONE', #65054, 7.499999999992679633 ) ;
#97769=CARTESIAN_POINT ( 'NONE',  ( -61.06992298392258078, -57.67755795743399716, 111.0944920020532862 ) ) ;
#97782=CARTESIAN_POINT ( 'NONE',  ( -10.95918059713568837, -14.00797954113551747, 31.84498254503383663 ) ) ;
#97795=CARTESIAN_POINT ( 'NONE',  ( -15.58318277380108263, -24.24093616901115311, -38.53689649557993846 ) ) ;
#97801=CARTESIAN_POINT ( 'NONE',  ( 101.9220456111045507, -57.63191952442775801, 203.3003234520283513 ) ) ;
#97808=CARTESIAN_POINT ( 'NONE',  ( -73.84812816836441129, -60.00000000000000000, 170.6796079630115912 ) ) ;
#97814=CARTESIAN_POINT ( 'NONE',  ( -85.63198936259853156, -32.10030600112477828, 181.8800658012134477 ) ) ;
#97823=CARTESIAN_POINT ( 'NONE',  ( -87.02619266019526378, -60.19139343833020206, -6.136718658578977248 ) ) ;
#97833=CARTESIAN_POINT ( 'NONE',  ( -2.910977163135976653, -8.673617379884035472E-16, -22.23822744035697241 ) ) ;
#97834=CARTESIAN_POINT ( 'NONE',  ( -71.63495682827519317, -59.99999999999997868, -34.46936934826943855 ) ) ;
#97835=CARTESIAN_POINT ( 'NONE',  ( -74.87526142751326574, -53.38099747595546773, 130.5593691470315605 ) ) ;
#97837=CARTESIAN_POINT ( 'NONE',  ( 52.32017852953563164, -14.21045842199431242, 63.23906622249963760 ) ) ;
#97839=CARTESIAN_POINT ( 'NONE',  ( 92.21232009249456496, -57.65949651113772489, -18.94920474166798385 ) ) ;
#97855=ORIENTED_EDGE ( 'NONE', *, *, #74554, .T. ) ;
#97858=CARTESIAN_POINT ( 'NONE',  ( 29.88845415383573823, -29.06604919746129667, 31.22394821666031817 ) ) ;
#97875=CARTESIAN_POINT ( 'NONE',  ( 65.84150895268908243, -60.00000000000000000, -33.94149391649602165 ) ) ;
#97899=CARTESIAN_POINT ( 'NONE',  ( 63.59140386760513053, -56.86218274724328126, 91.13360387561940001 ) ) ;
#97904=CARTESIAN_POINT ( 'NONE',  ( -64.02773510654475331, -57.67113784069211135, -36.59462343474526591 ) ) ;
#97921=( NAMED_UNIT ( * ) SI_UNIT ( $, .STERADIAN. ) SOLID_ANGLE_UNIT ( ) );
#97927=CARTESIAN_POINT ( 'NONE',  ( -94.21191784372652478, -30.00000000000000355, 191.2965387815471843 ) ) ;
#97930=CARTESIAN_POINT ( 'NONE',  ( 35.43536369062855584, -57.69560819355115910, 49.59754854414701697 ) ) ;
#97936=CARTESIAN_POINT ( 'NONE',  ( 9.997272199965776096, -22.62240898069702411, -38.54272479879313806 ) ) ;
#97940=CARTESIAN_POINT ( 'NONE',  ( -21.06506537777876531, -59.99999999999999289, 40.36978327349123674 ) ) ;
#97944=CARTESIAN_POINT ( 'NONE',  ( -86.90711792063859775, -24.33407301245372523, 186.0904578520139978 ) ) ;
#97948=CARTESIAN_POINT ( 'NONE',  ( -9.411392529996735590, -60.36588867045908557, 33.95496757082129591 ) ) ;
#97961=CARTESIAN_POINT ( 'NONE',  ( 61.46887122245544077, -60.00000000000000000, 105.4469840523393458 ) ) ;
#97963=ORIENTED_EDGE ( 'NONE', *, *, #31638, .T. ) ;
#97964=DIRECTION ( 'NONE',  ( -1.000000000000000000, 0.000000000000000000, 0.000000000000000000 ) ) ;
#97968=CARTESIAN_POINT ( 'NONE',  ( 44.75958163560274272, -30.00000000000001776, 54.38364795613178870 ) ) ;
#97981=CARTESIAN_POINT ( 'NONE',  ( -73.56062074102059967, -60.00000000001949019, 187.3333967129919131 ) ) ;
#97983=CARTESIAN_POINT ( 'NONE',  ( 64.60710420547525246, -60.00000000000000000, 116.1616718869901632 ) ) ;
#97985=CARTESIAN_POINT ( 'NONE',  ( -112.8607363433238930, -60.00000000000000000, 189.7948125560051551 ) ) ;
#97986=CARTESIAN_POINT ( 'NONE',  ( 15.66189778777191854, -39.47289686819183174, 30.64853919330023402 ) ) ;
#97988=CARTESIAN_POINT ( 'NONE',  ( 82.45244879800553406, -37.99999999999995737, 11.14743738424387764 ) ) ;
#97990=CARTESIAN_POINT ( 'NONE',  ( -47.00008757630948253, -53.35960851535460137, 50.29090797156688097 ) ) ;
#98003=CARTESIAN_POINT ( 'NONE',  ( 88.03191322166020427, -30.00000000001757883, 198.6467012898908138 ) ) ;
#98007=CARTESIAN_POINT ( 'NONE',  ( 100.5443587151843587, -29.99999999999998934, 159.7778150890727034 ) ) ;
#98023=CARTESIAN_POINT ( 'NONE',  ( 85.15092372543439581, -38.69193916550122481, 198.5729534848597950 ) ) ;
#98037=FILL_AREA_STYLE ('',( #98559 ) ) ;
#98046=ORIENTED_EDGE ( 'NONE', *, *, #106672, .F. ) ;
#98047=CARTESIAN_POINT ( 'NONE',  ( 85.12736371515951816, -39.33789070826465206, 184.1504447524897046 ) ) ;
#98051=CARTESIAN_POINT ( 'NONE',  ( 82.54125890550720612, -57.67110014045612587, -28.70085741798137846 ) ) ;
#98054=CARTESIAN_POINT ( 'NONE',  ( -81.57465289304622047, -30.00000000000000711, -5.224175191359936576 ) ) ;
#98055=CARTESIAN_POINT ( 'NONE',  ( -85.74343386013892143, -37.99999999999996447, 185.6815049747404487 ) ) ;
#98069=CARTESIAN_POINT ( 'NONE',  ( 71.30924092933392444, -30.00000000000000711, -20.00752902790307530 ) ) ;
#98073=CARTESIAN_POINT ( 'NONE',  ( -26.77005346869424329, -20.63395408316250723, -32.73886166069684123 ) ) ;
#98075=CARTESIAN_POINT ( 'NONE',  ( -32.37202873548481818, -60.22819029308026728, -34.89880865881568894 ) ) ;
#98077=VERTEX_POINT ( 'NONE', #9285 ) ;
#98085=CARTESIAN_POINT ( 'NONE',  ( -87.91029806970415450, -60.00000000000000000, -21.68455642860508448 ) ) ;
#98089=CARTESIAN_POINT ( 'NONE',  ( 93.93808739026684407, -37.70322700098001434, 192.9552561637989925 ) ) ;
#98104=CARTESIAN_POINT ( 'NONE',  ( -90.87004379432312362, -57.61277171722555579, 204.1615020926832358 ) ) ;
#98110=CARTESIAN_POINT ( 'NONE',  ( -64.67113474307254251, -14.21045842199435505, -28.81208810413780697 ) ) ;
#98112=CARTESIAN_POINT ( 'NONE',  ( -36.05833693101251214, -60.00000000000004263, 50.77755985414292184 ) ) ;
#98113=CARTESIAN_POINT ( 'NONE',  ( -52.39849268324191200, -39.50851378549550930, 55.00951463007811526 ) ) ;
#98117=CARTESIAN_POINT ( 'NONE',  ( -100.2666838828567677, -52.75501491069231719, 194.0125142992028202 ) ) ;
#98122=CARTESIAN_POINT ( 'NONE',  ( 90.99775346010591193, -38.40525435722307179, -12.64124594595937090 ) ) ;
#98127=CARTESIAN_POINT ( 'NONE',  ( 84.03711676261723085, -30.00000000000000000, 161.3372059342742943 ) ) ;
#98134=CARTESIAN_POINT ( 'NONE',  ( 49.98497805703834729, -18.73844719463555819, 43.94240058066204568 ) ) ;
#98137=ORIENTED_EDGE ( 'NONE', *, *, #40286, .T. ) ;
#98138=CARTESIAN_POINT ( 'NONE',  ( -108.1787983003200395, -38.35626379967903432, 139.1432696700099143 ) ) ;
#98141=CARTESIAN_POINT ( 'NONE',  ( 90.86182427071091183, -38.35175685699187653, 20.64787121975910367 ) ) ;
#98144=CARTESIAN_POINT ( 'NONE',  ( 98.81654218035373560, -52.71701439775952025, 115.6172114277043050 ) ) ;
#98149=CARTESIAN_POINT ( 'NONE',  ( 74.92543916372812873, -60.00000000000000711, 180.6976430414843833 ) ) ;
#98152=CARTESIAN_POINT ( 'NONE',  ( 56.07231050077595569, -49.90802284892470908, 67.05805815868586706 ) ) ;
#98158=CARTESIAN_POINT ( 'NONE',  ( -80.04809061299876305, -30.00000000001593392, 190.5044041146019538 ) ) ;
#98170=CARTESIAN_POINT ( 'NONE',  ( 82.89656108765285580, -46.49426597450035104, 178.9984722453477275 ) ) ;
#98186=CARTESIAN_POINT ( 'NONE',  ( -8.717155287858316726, -19.71234147751727761, 35.28392597056648583 ) ) ;
#98206=B_SPLINE_CURVE_WITH_KNOTS ( 'NONE', 3,
 ( #24216, #15016, #6390, #23147, #48964, #88398, #57066, #16084, #54939, #72204, #81862, #7987, #105108, #97007, #104029, #95960, #22084, #46861, #66773, #920, #58137, #43031, #34444, #66228, #92098, #74317, #99661, #42485 ),
 .UNSPECIFIED., .F., .F.,
 ( 4, 2, 2, 2, 2, 2, 2, 2, 2, 2, 2, 2, 2, 4 ),
 ( 0.07710222747882937433, 0.08159137518423913160, 0.08383594903694401024, 0.08608052288964888887, 0.09056967059505866002, 0.09505881830046841729, 0.1040371137112879457, 0.1130154091221074741, 0.1219937045329270164, 0.1309719999437465587, 0.1354611476491563160, 0.1399502953545660733, 0.1444394430599758306, 0.1489285907653855878 ),
 .UNSPECIFIED. ) ;
#98209=CARTESIAN_POINT ( 'NONE',  ( -99.55134491157069476, -60.00000000000000000, 78.35702824496748065 ) ) ;
#98211=CARTESIAN_POINT ( 'NONE',  ( 9.183192031130861521E-06, -29.03115897286976832, 28.72817645508066775 ) ) ;
#98217=CARTESIAN_POINT ( 'NONE',  ( -83.59314024080309480, -39.46891138312180658, 175.2148047660766679 ) ) ;
#98218=ORIENTED_EDGE ( 'NONE', *, *, #45381, .F. ) ;
#98232=CARTESIAN_POINT ( 'NONE',  ( 104.4271199315001013, -14.21045842199428932, 141.4133776126798523 ) ) ;
#98235=CARTESIAN_POINT ( 'NONE',  ( -104.7861223705664599, -14.21045842199442433, 190.1679628257406875 ) ) ;
#98236=CARTESIAN_POINT ( 'NONE',  ( -63.02399650324780112, -22.10761227753726743, 71.83296306885770832 ) ) ;
#98239=CARTESIAN_POINT ( 'NONE',  ( 112.1647626997707192, -60.00000000000001421, 192.1852754171339654 ) ) ;
#98242=CARTESIAN_POINT ( 'NONE',  ( -2.304441091496778042E-06, -22.06731698597467428, 27.56753612393148956 ) ) ;
#98248=ORIENTED_EDGE ( 'NONE', *, *, #104320, .T. ) ;
#98251=CARTESIAN_POINT ( 'NONE',  ( -107.0982019125352593, -60.00000000000001421, 196.9758988471260182 ) ) ;
#98262=CARTESIAN_POINT ( 'NONE',  ( 106.1377881480577088, -60.00000000000000000, 180.8750096036389436 ) ) ;
#98263=CARTESIAN_POINT ( 'NONE',  ( -33.15903214888006545, -56.84432955689586464, 37.61496284774349874 ) ) ;
#98265=AXIS2_PLACEMENT_3D ( 'NONE', #25692, #84421, #45951 ) ;
#98266=CARTESIAN_POINT ( 'NONE',  ( 40.03051666693097133, -36.06173267250149905, 37.97872145570595137 ) ) ;
#98271=CARTESIAN_POINT ( 'NONE',  ( -81.56573377466280306, -38.84171562881364537, 195.3582572410830096 ) ) ;
#98284=CARTESIAN_POINT ( 'NONE',  ( 110.0488610262806048, -60.00000000000001421, 143.8402947968523904 ) ) ;
#98288=CARTESIAN_POINT ( 'NONE',  ( -86.48208369142494689, -30.00000000000002132, 181.4558340259839895 ) ) ;
#98306=CARTESIAN_POINT ( 'NONE',  ( 82.86123803554382050, -22.15437991950470931, 144.5942242259914394 ) ) ;
#98319=CIRCLE ( 'NONE', #84547, 7.500000000001509015 ) ;
#98326=CARTESIAN_POINT ( 'NONE',  ( 29.70662014929110839, -32.25496426234150249, 40.40754308457954380 ) ) ;
#98328=DIRECTION ( 'NONE',  ( 0.000000000000000000, -1.000000000000000000, 0.000000000000000000 ) ) ;
#98341=CARTESIAN_POINT ( 'NONE',  ( 102.6741165558615450, -57.67098198743860138, 85.02274040594497251 ) ) ;
#98349=CARTESIAN_POINT ( 'NONE',  ( -73.88487227173887106, -60.00000000000001421, 171.0524701157142999 ) ) ;
#98352=CARTESIAN_POINT ( 'NONE',  ( -83.75545966347903004, -61.02389094001022585, 191.9544639385318590 ) ) ;
#98353=ORIENTED_EDGE ( 'NONE', *, *, #51386, .T. ) ;
#98359=CARTESIAN_POINT ( 'NONE',  ( -83.25986436703819038, -37.78524753907071698, -7.278281021959687180 ) ) ;
#98365=CARTESIAN_POINT ( 'NONE',  ( 17.01589776168603407, -1.734723475976807094E-15, -2.227375807149030162 ) ) ;
#98367=CARTESIAN_POINT ( 'NONE',  ( -16.35184830034500791, -14.21045842199432663, -36.83529024868766300 ) ) ;
#98369=CARTESIAN_POINT ( 'NONE',  ( -75.40408572285984690, -56.85084406233583110, 136.0574973080508983 ) ) ;
#98371=CARTESIAN_POINT ( 'NONE',  ( 37.62958953315902022, -14.21045842199429288, 41.24408864243086015 ) ) ;
#98373=CARTESIAN_POINT ( 'NONE',  ( 100.8522003986677475, -57.67122939875248022, 74.21107199178662484 ) ) ;
#98392=CARTESIAN_POINT ( 'NONE',  ( 29.36420834963063342, -18.64469661114391030, 29.18565830806650752 ) ) ;
#98400=CARTESIAN_POINT ( 'NONE',  ( 89.99999999999997158, -52.00000000000000000, 196.0238439516549818 ) ) ;
#98431=CARTESIAN_POINT ( 'NONE',  ( 64.89962780002818477, -56.86111594249680934, 95.13482168274560991 ) ) ;
#98453=CARTESIAN_POINT ( 'NONE',  ( -95.67697799131535419, -30.00000000000000355, 191.3169455322079671 ) ) ;
#98455=CARTESIAN_POINT ( 'NONE',  ( 72.46540426577622895, -57.66615126196867180, 176.6242912695971370 ) ) ;
#98459=CARTESIAN_POINT ( 'NONE',  ( 19.32975784459248203, -25.59227486960913467, -38.49241694374236289 ) ) ;
#98462=CARTESIAN_POINT ( 'NONE',  ( -4.212150072450890903, -59.99999999999999289, 39.63086106002882048 ) ) ;
#98465=CARTESIAN_POINT ( 'NONE',  ( -86.48841333095882078, -50.13869857804851193, 191.3748143931806283 ) ) ;
#98470=CARTESIAN_POINT ( 'NONE',  ( -7.230353591503060784, -53.40254472460676283, 32.78041106468180743 ) ) ;
#98471=LINE ( 'NONE', #105511, #29039 ) ;
#98484=CARTESIAN_POINT ( 'NONE',  ( 107.5810510768942549, -30.00000000000001066, 145.3411688640341879 ) ) ;
#98505=CARTESIAN_POINT ( 'NONE',  ( -11.24474098223441665, -60.00000000000000711, 42.02457686618004828 ) ) ;
#98507=CARTESIAN_POINT ( 'NONE',  ( 110.4355216320049635, -59.99999999999998579, 146.6424206039912121 ) ) ;
#98509=CARTESIAN_POINT ( 'NONE',  ( -105.8602000712061368, -14.21045842199440656, 153.6005699772977096 ) ) ;
#98510=CARTESIAN_POINT ( 'NONE',  ( 14.72031451962790172, -49.91564338959982905, 32.33869626530814401 ) ) ;
#98514=CARTESIAN_POINT ( 'NONE',  ( -41.71313970803240778, -53.34689749798402403, 43.42087845691148829 ) ) ;
#98528=CARTESIAN_POINT ( 'NONE',  ( 75.85296913857929724, -29.99999999993386623, 164.1495175436531895 ) ) ;
#98533=CARTESIAN_POINT ( 'NONE',  ( 90.44129752230823271, -29.99999999999999645, 91.07386086299301553 ) ) ;
#98545=CARTESIAN_POINT ( 'NONE',  ( 79.97203214341874400, -38.78014282313012728, 192.9381993355203804 ) ) ;
#98559=FILL_AREA_STYLE_COLOUR ( '', #71028 ) ;
#98562=( LENGTH_UNIT ( ) NAMED_UNIT ( * ) SI_UNIT ( .MILLI., .METRE. ) );
#98572=CARTESIAN_POINT ( 'NONE',  ( 85.04290646969892009, -50.19384762663964494, 189.2821407580086088 ) ) ;
#98576=CARTESIAN_POINT ( 'NONE',  ( 94.47643939734095397, -57.66978673744599604, -1.231856577211943637 ) ) ;
#98581=CARTESIAN_POINT ( 'NONE',  ( -80.98454112480462186, -30.00000000000000355, 4.285213993873024485 ) ) ;
#98586=CARTESIAN_POINT ( 'NONE',  ( 52.44308130789431033, -29.98757490428321759, 50.93680095260226182 ) ) ;
#98595=CARTESIAN_POINT ( 'NONE',  ( -99.16883851872213995, -37.99999999999991473, 191.7725159787542282 ) ) ;
#98608=CARTESIAN_POINT ( 'NONE',  ( -33.99305469949648284, -60.00000000000000000, -40.43516885408138961 ) ) ;
#98612=CARTESIAN_POINT ( 'NONE',  ( 96.81084219511998867, -52.81891926509837276, 195.3532482584386969 ) ) ;
#98627=CARTESIAN_POINT ( 'NONE',  ( -29.04643245788701122, -57.68166065953202093, 44.76603692081018693 ) ) ;
#98632=CARTESIAN_POINT ( 'NONE',  ( 32.64290048136811606, -14.21045842199427867, -35.33280650708731230 ) ) ;
#98635=CARTESIAN_POINT ( 'NONE',  ( -52.73927720795784069, -56.84651578577485509, 62.26472032949996560 ) ) ;
#98638=CARTESIAN_POINT ( 'NONE',  ( -98.60539400174438640, -37.75072670319377011, 192.1773030902787980 ) ) ;
#98643=CARTESIAN_POINT ( 'NONE',  ( 84.23062891746764080, -38.75005706687972662, 197.9527241322343230 ) ) ;
#98646=EDGE_CURVE ( 'NONE', #18895, #44460, #6018, .T. ) ;
#98649=CARTESIAN_POINT ( 'NONE',  ( 84.63983498852250875, -30.00000000000000355, 166.8986807930797340 ) ) ;
#98656=CARTESIAN_POINT ( 'NONE',  ( 49.01680650270304795, -56.82380834871364783, 54.79513700058014081 ) ) ;
#98657=MECHANICAL_DESIGN_GEOMETRIC_PRESENTATION_REPRESENTATION('',(#40086),#10801);
#98661=CARTESIAN_POINT ( 'NONE',  ( -97.41561983528457347, -38.35525745205964654, 73.11340283102843784 ) ) ;
#98663=CARTESIAN_POINT ( 'NONE',  ( 91.87323331309748653, -38.35385193510057178, 33.51482854396223132 ) ) ;
#98665=CARTESIAN_POINT ( 'NONE',  ( 104.4246528305459378, -52.71695562033825411, 156.3626540467217865 ) ) ;
#98669=CARTESIAN_POINT ( 'NONE',  ( 74.36230277464828475, -60.00000000000001421, 175.8080994144255840 ) ) ;
#98672=CARTESIAN_POINT ( 'NONE',  ( 60.90451431562469509, -56.86322954724349898, 83.15454531713724862 ) ) ;
#98677=CARTESIAN_POINT ( 'NONE',  ( -71.41185097590582131, -30.00000000016128965, 134.2290320126720928 ) ) ;
#98687=CARTESIAN_POINT ( 'NONE',  ( 85.24943635772166317, -25.41792041905209842, 169.5202013333633033 ) ) ;
#98703=CARTESIAN_POINT ( 'NONE',  ( -10.71489332182602361, -20.52239476129827267, 35.44028641706174199 ) ) ;
#98717=CARTESIAN_POINT ( 'NONE',  ( 64.34530734380760464, -47.40884564742954410, -26.19147373469116502 ) ) ;
#98726=CARTESIAN_POINT ( 'NONE',  ( -98.09259472220433906, -59.99999999999999289, 69.49854301730701422 ) ) ;
#98733=CARTESIAN_POINT ( 'NONE',  ( -85.81337131230007742, -21.82407471985175818, 170.1709790121419985 ) ) ;
#98744=CARTESIAN_POINT ( 'NONE',  ( 0.000000000000000000, -15.00000000000000000, 0.000000000000000000 ) ) ;
#98750=CARTESIAN_POINT ( 'NONE',  ( 108.8241408383580193, -29.99999999999998224, 157.0475695436092565 ) ) ;
#98752=CARTESIAN_POINT ( 'NONE',  ( -106.1779193982466580, -14.21045842199435860, 156.9944278011976451 ) ) ;
#98753=CARTESIAN_POINT ( 'NONE',  ( -62.01645086870617973, -49.91653808238077517, 82.86907591662273376 ) ) ;
#98756=CARTESIAN_POINT ( 'NONE',  ( 95.11636133611268917, -59.99999999998292566, -7.883470413377934527 ) ) ;
#98758=CARTESIAN_POINT ( 'NONE',  ( 1.013586109042279082, -49.91581433662842926, 32.20895234904045168 ) ) ;
#98759=CARTESIAN_POINT ( 'NONE',  ( -97.91261498135648367, -37.82064874998170723, 125.6660091448068073 ) ) ;
#98768=CARTESIAN_POINT ( 'NONE',  ( -94.01890188198808573, -59.99999999999997158, 202.5480236000225034 ) ) ;
#98774=AXIS2_PLACEMENT_3D ( 'NONE', #83906, #93612, #84983 ) ;
#98780=CARTESIAN_POINT ( 'NONE',  ( 105.5007349313588634, -60.00000000000002842, 154.8517593642223744 ) ) ;
#98781=CARTESIAN_POINT ( 'NONE',  ( -33.91206465489236876, -53.37053416063930200, 37.37971910314460189 ) ) ;
#98783=CARTESIAN_POINT ( 'NONE',  ( 42.79026094202129116, -60.24709657765144755, 46.28082913036630686 ) ) ;
#98786=CARTESIAN_POINT ( 'NONE',  ( -81.60022401860847197, -38.84181500998843006, 195.4017998612470137 ) ) ;
#98788=CARTESIAN_POINT ( 'NONE',  ( 2.499999999999999556, -8.000000000000000000, 17.89626171146327138 ) ) ;
#98797=CARTESIAN_POINT ( 'NONE',  ( 110.7605312682850780, -60.00000000000000711, 149.8757700383887936 ) ) ;
#98802=CARTESIAN_POINT ( 'NONE',  ( -44.47534256803313468, -38.31161230092084224, 57.00189278798902137 ) ) ;
#98803=ORIENTED_EDGE ( 'NONE', *, *, #4191, .F. ) ;
#98805=CARTESIAN_POINT ( 'NONE',  ( -90.04282506516243245, -29.99999999999963407, 189.9068615740519590 ) ) ;
#98819=ORIENTED_EDGE ( 'NONE', *, *, #89297, .F. ) ;
#98820=CARTESIAN_POINT ( 'NONE',  ( 79.31590203019780461, -53.37304251699236346, 157.6480627266177805 ) ) ;
#98833=CARTESIAN_POINT ( 'NONE',  ( 86.51326442782708170, -53.78086573019226080, 192.4535467407390570 ) ) ;
#98836=CARTESIAN_POINT ( 'NONE',  ( 21.62698502147047819, -26.76882475084324042, 37.23665029981403052 ) ) ;
#98851=CARTESIAN_POINT ( 'NONE',  ( 112.9101767622411643, -57.67113815742245464, 187.8873526033939640 ) ) ;
#98853=LINE ( 'NONE', #41705, #58775 ) ;
#98856=CARTESIAN_POINT ( 'NONE',  ( -77.66702251434536208, -59.99999999999999289, 192.1189785543494963 ) ) ;
#98859=CARTESIAN_POINT ( 'NONE',  ( -84.46326382266198607, -53.81991241739247300, 189.8031309934812327 ) ) ;
#98864=EDGE_LOOP ( 'NONE', ( #45003, #40860, #7383, #26514 ) ) ;
#98869=CARTESIAN_POINT ( 'NONE',  ( -87.03135510228767657, -60.19613468631837350, -6.661356676301259050 ) ) ;
#98875=CARTESIAN_POINT ( 'NONE',  ( 21.65942590380180022, -2.602085213965209853E-15, -5.820808985962528936 ) ) ;
#98878=CARTESIAN_POINT ( 'NONE',  ( -8.180708021844917965, -14.21045842199436926, -37.25108655295423432 ) ) ;
#98879=CARTESIAN_POINT ( 'NONE',  ( -76.80044675745622840, -49.90808875740508910, 137.4838826220702401 ) ) ;
#98881=CARTESIAN_POINT ( 'NONE',  ( 78.54417320222145804, -14.21045842199432307, 165.9036888455924270 ) ) ;
#98883=CARTESIAN_POINT ( 'NONE',  ( 113.9274098329656084, -57.67114099918555326, 180.4894649156854598 ) ) ;
#98885=LINE ( 'NONE', #16393, #104317 ) ;
#98904=CARTESIAN_POINT ( 'NONE',  ( 31.54446617496518712, -49.90305043662050366, 35.58892852745655233 ) ) ;
#98911=PLANE ( 'NONE',  #92211 ) ;
#98918=CARTESIAN_POINT ( 'NONE',  ( 92.74135359634635734, -60.00000000000000000, -6.602453662847219462 ) ) ;
#98932=CARTESIAN_POINT ( 'NONE',  ( 83.10245286683164068, -37.83958788250053829, -2.435592654216626851 ) ) ;
#98943=CARTESIAN_POINT ( 'NONE',  ( -14.60449729785899464, -60.00000000000003553, 34.00514524257540927 ) ) ;
#98945=CARTESIAN_POINT ( 'NONE',  ( 70.22185649915901706, -49.90760283489759530, 108.7999883389251181 ) ) ;
#98951=CARTESIAN_POINT ( 'NONE',  ( -94.70367724826090239, -57.65721615037961811, -8.919493359160306056 ) ) ;
#98969=CARTESIAN_POINT ( 'NONE',  ( 4.633946686836865503, -60.00000000000000000, 39.63006500553967726 ) ) ;
#98970=CARTESIAN_POINT ( 'NONE',  ( -91.23729876660307525, -30.00000000000000355, 190.5897172708922369 ) ) ;
#98973=CARTESIAN_POINT ( 'NONE',  ( 73.86186822093814897, -57.61872494714916115, 186.3625796096756915 ) ) ;
#98976=CARTESIAN_POINT ( 'NONE',  ( 9.893172293432595410, -22.59654125385418766, -38.54281256708559766 ) ) ;
#98981=CARTESIAN_POINT ( 'NONE',  ( -32.82504303899613518, -60.00000000000001421, 44.72063024855318503 ) ) ;
#98987=CARTESIAN_POINT ( 'NONE',  ( -86.58206345380148150, -50.13197549991983237, 191.4801916809975637 ) ) ;
#98991=CARTESIAN_POINT ( 'NONE',  ( -8.311032557564669077, -56.88425799153385753, 33.36415341410724977 ) ) ;
#99004=CARTESIAN_POINT ( 'NONE',  ( 104.9451034742319706, -14.21045842199432663, 145.4709692194043669 ) ) ;
#99026=CARTESIAN_POINT ( 'NONE',  ( -68.94556730486883112, -59.99999999997069722, 149.4068084800686904 ) ) ;
#99029=CARTESIAN_POINT ( 'NONE',  ( 99.83762202063759617, -60.00000000000000000, 80.07466358523365102 ) ) ;
#99030=CARTESIAN_POINT ( 'NONE',  ( -78.26172670240529783, -14.21045842199445275, 161.8221046207387985 ) ) ;
#99031=CARTESIAN_POINT ( 'NONE',  ( 17.45845221745307541, -18.58884928908958400, 27.26027009539929935 ) ) ;
#99032=CARTESIAN_POINT ( 'NONE',  ( 82.55061241810440720, -37.99999999999995026, -12.61180328641926174 ) ) ;
#99034=CARTESIAN_POINT ( 'NONE',  ( -42.02556652957100880, -36.07178335321912499, 39.65759594440722680 ) ) ;
#99047=CARTESIAN_POINT ( 'NONE',  ( 80.09155444759548459, -30.00000000000000000, -13.68037423625693627 ) ) ;
#99052=CARTESIAN_POINT ( 'NONE',  ( 97.89039143310566260, -30.00000000000000000, 136.7614787515506691 ) ) ;
#99056=ORIENTED_EDGE ( 'NONE', *, *, #5854, .T. ) ;
#99069=CARTESIAN_POINT ( 'NONE',  ( 79.61952492946029736, -38.75123715105880962, 192.2766210044055981 ) ) ;
#99092=CARTESIAN_POINT ( 'NONE',  ( 84.96757647266667846, -50.19333676378905551, 189.1419654610012628 ) ) ;
#99097=CARTESIAN_POINT ( 'NONE',  ( 93.07912069066024685, -57.65568903999214001, -17.02304421024389924 ) ) ;
#99104=CARTESIAN_POINT ( 'NONE',  ( -81.36966163465557145, -30.00000000000000000, -1.517807414885295580 ) ) ;
#99117=EDGE_CURVE ( 'NONE', #60981, #27380, #89255, .T. ) ;
#99122=CARTESIAN_POINT ( 'NONE',  ( -46.15551534976521708, -26.57306916659460683, -28.92868944221968164 ) ) ;
#99124=CARTESIAN_POINT ( 'NONE',  ( -69.47170429735781738, -60.22820986096264306, -26.63212845803639084 ) ) ;
#99134=CARTESIAN_POINT ( 'NONE',  ( -49.88581133959984726, -60.00000000000000711, -37.92708229162208511 ) ) ;
#99140=CARTESIAN_POINT ( 'NONE',  ( 101.2319675162309807, -52.73591760636113435, 193.1241288170249959 ) ) ;
#99142=CARTESIAN_POINT ( 'NONE',  ( 26.44954341376113049, -28.72239887604681385, 30.17119393485961609 ) ) ;
#99157=CARTESIAN_POINT ( 'NONE',  ( -72.23603530542938245, -57.67079283669161782, 174.4370243615865661 ) ) ;
#99163=CARTESIAN_POINT ( 'NONE',  ( -48.21571607899795708, -30.00000000000001066, -35.59733477200444440 ) ) ;
#99164=CARTESIAN_POINT ( 'NONE',  ( -28.47812542966827110, -14.21045842199436926, 36.49899343628653270 ) ) ;
#99165=CARTESIAN_POINT ( 'NONE',  ( -50.22257761704449308, -39.51501898924006895, 51.10941894695140775 ) ) ;
#99168=CARTESIAN_POINT ( 'NONE',  ( -100.3692683177832947, -52.75229974785736431, 193.9353176766608726 ) ) ;
#99173=CARTESIAN_POINT ( 'NONE',  ( 93.05610975779491412, -38.49596479831048157, 201.1399583442435528 ) ) ;
#99177=CARTESIAN_POINT ( 'NONE',  ( 85.25411052359936548, -29.99999999999999645, 172.6780782422512743 ) ) ;
#99183=CARTESIAN_POINT ( 'NONE',  ( 53.26745199980564394, -29.10185247891099891, 52.81664263156634576 ) ) ;
#99187=CARTESIAN_POINT ( 'NONE',  ( -106.3081487713218394, -38.35654553538349631, 126.0309737019096303 ) ) ;
#99191=CARTESIAN_POINT ( 'NONE',  ( 99.83938914365424466, -38.35585918022645302, 87.51053804860399055 ) ) ;
#99194=CARTESIAN_POINT ( 'NONE',  ( 85.81162101844391543, -52.71496586455459976, 30.16212271239476905 ) ) ;
#99199=CARTESIAN_POINT ( 'NONE',  ( 75.45779768849573088, -60.00000000000001421, 184.2411573433691672 ) ) ;
#99204=CARTESIAN_POINT ( 'NONE',  ( 62.38864196659469741, -32.53364364072947268, 75.22878982978467377 ) ) ;
#99210=CARTESIAN_POINT ( 'NONE',  ( -89.66675816820549016, -38.39121966713390322, -16.77064573778548962 ) ) ;
#99220=CARTESIAN_POINT ( 'NONE',  ( 82.39197520823663012, -53.57314957911707864, 183.5891899450602409 ) ) ;
#99231=CARTESIAN_POINT ( 'NONE',  ( 52.36387915676058924, -60.00000000000000000, 77.90990540846810575 ) ) ;
#99233=CARTESIAN_POINT ( 'NONE',  ( 19.31324592808787699, -16.82044274283948226, 31.48938567249289733 ) ) ;
#99235=CARTESIAN_POINT ( 'NONE',  ( -15.48955457585431184, -22.96514382653771236, 36.00456892657421548 ) ) ;
#99247=CARTESIAN_POINT ( 'NONE',  ( 41.46650182939242058, -47.40888185850945291, -31.47352802185152854 ) ) ;
#99254=CARTESIAN_POINT ( 'NONE',  ( -95.52932323723678110, -60.00000000000000000, 52.80250551557467276 ) ) ;
#99261=CARTESIAN_POINT ( 'NONE',  ( -84.26947212678977905, -32.46855681540231586, 170.8702711660567104 ) ) ;
#99271=CARTESIAN_POINT ( 'NONE',  ( -22.45002021702217121, -57.67118433041228798, -43.66150106997372404 ) ) ;
#99279=CARTESIAN_POINT ( 'NONE',  ( 106.4976671120242173, -30.00000000000003553, 137.1020467228335349 ) ) ;
#99280=CARTESIAN_POINT ( 'NONE',  ( -106.4855387602377732, -14.21045842199444564, 182.1782270149441558 ) ) ;
#99281=CARTESIAN_POINT ( 'NONE',  ( -60.16549379149508070, -18.65118697126286662, 63.02844734512476066 ) ) ;
#99284=CARTESIAN_POINT ( 'NONE',  ( 111.6472127090487731, -60.00000000002953016, 193.6361861217306455 ) ) ;
#99288=CARTESIAN_POINT ( 'NONE',  ( 7.055885070595124375, -29.02937926490056952, 28.71821008264055664 ) ) ;
#99290=CARTESIAN_POINT ( 'NONE',  ( -101.4585684387344173, -37.82058770419944693, 151.6467883671373897 ) ) ;
#99296=CARTESIAN_POINT ( 'NONE',  ( -69.88467371534370898, -59.99999999999997868, 140.7241876569264605 ) ) ;
#99307=EDGE_CURVE ( 'NONE', #85478, #35775, #75638, .T. ) ;
#99308=CARTESIAN_POINT ( 'NONE',  ( 86.30257998548809439, -60.00000000000005684, -13.06867930585625714 ) ) ;
#99309=CARTESIAN_POINT ( 'NONE',  ( -33.60394201097540190, -53.37182691420839120, 37.21343069149457961 ) ) ;
#99311=CARTESIAN_POINT ( 'NONE',  ( 45.62230598746199917, -49.89328325408317966, 47.30517501752983378 ) ) ;
#99315=CARTESIAN_POINT ( 'NONE',  ( -76.45337711124132341, -38.40897008212451880, 181.4709146294509594 ) ) ;
#99319=CARTESIAN_POINT ( 'NONE',  ( 6.026974479199131350E-05, -59.99999999999998579, 33.88964995960238014 ) ) ;
#99326=CARTESIAN_POINT ( 'NONE',  ( 102.0663143730366897, -60.00000000000000711, 93.13200012967355690 ) ) ;
#99331=CARTESIAN_POINT ( 'NONE',  ( -100.6601205862880306, -29.99999999999999289, 181.6786300687315077 ) ) ;
#99342=CARTESIAN_POINT ( 'NONE',  ( 83.70516314075617004, -32.52322900293838615, 165.3182127895680935 ) ) ;
#99358=CARTESIAN_POINT ( 'NONE',  ( 86.75617746412517306, -28.06358367585517755, 186.0038586487513896 ) ) ;
#99379=CARTESIAN_POINT ( 'NONE',  ( 109.7502093377535886, -57.66773119830670424, 196.5356198408315436 ) ) ;
#99381=DIRECTION ( 'NONE',  ( -8.673617379884035472E-17, -0.000000000000000000, -1.000000000000000000 ) ) ;
#99385=CARTESIAN_POINT ( 'NONE',  ( -76.54204534339102395, -60.00000000000000000, 189.0398269527300386 ) ) ;
#99389=CARTESIAN_POINT ( 'NONE',  ( -84.65018232938496112, -39.39540612587336454, 182.1018301571575080 ) ) ;
#99397=CARTESIAN_POINT ( 'NONE',  ( -83.87309315678267296, -45.26105613303531783, -12.39373611433831002 ) ) ;
#99408=CARTESIAN_POINT ( 'NONE',  ( -42.61015704936735915, -60.00000000000002842, -41.65925318937349431 ) ) ;
#99409=CARTESIAN_POINT ( 'NONE',  ( -76.47417906005152588, -53.37849902404385460, 138.8593508845263500 ) ) ;
#99411=CARTESIAN_POINT ( 'NONE',  ( 74.10901235487826000, -60.00000000000013500, 189.8092491115571647 ) ) ;
#99413=CARTESIAN_POINT ( 'NONE',  ( 94.13231147061260629, -57.67516424662597530, 3.527862659130869716 ) ) ;
#99438=CARTESIAN_POINT ( 'NONE',  ( 29.64987082370327443, -49.90670958807863400, 34.84601124182362497 ) ) ;
#99456=CARTESIAN_POINT ( 'NONE',  ( 92.63360815464589848, -60.00000000000000711, -10.02160836745851924 ) ) ;
#99469=CARTESIAN_POINT ( 'NONE',  ( 85.75696656807998863, -52.74486970128089069, -6.687712918687570784 ) ) ;
#99481=CARTESIAN_POINT ( 'NONE',  ( 78.21122318075710211, -25.61170846490405140, 123.8332679187113570 ) ) ;
#99486=CARTESIAN_POINT ( 'NONE',  ( -112.9456993887476415, -57.67119592114509175, 187.6412086615824535 ) ) ;
#99491=CARTESIAN_POINT ( 'NONE',  ( 106.3494858034724473, -60.15152210362587226, 165.8936471126561116 ) ) ;
#99510=CARTESIAN_POINT ( 'NONE',  ( 5.699273591081692736, -60.00000000000000711, 39.62882889116424678 ) ) ;
#99511=CARTESIAN_POINT ( 'NONE',  ( -95.90249117390003164, -30.00000000000000000, 191.2992004980491458 ) ) ;
#99516=CARTESIAN_POINT ( 'NONE',  ( 71.48874846803950334, -57.67964410071327563, 166.9188931464234429 ) ) ;
#99517=PLANE ( 'NONE',  #98265 ) ;
#99519=CARTESIAN_POINT ( 'NONE',  ( 5.356817479642971058, -21.70158312131658107, -38.54714666297098091 ) ) ;
#99522=CARTESIAN_POINT ( 'NONE',  ( -47.13330949325234087, -60.00000000000000000, 65.07896732603337853 ) ) ;
#99528=CARTESIAN_POINT ( 'NONE',  ( -86.89203889042968854, -42.78634412649035568, 189.7867230391053113 ) ) ;
#99531=CARTESIAN_POINT ( 'NONE',  ( -6.981413442716312368, -18.58616681457634812, 26.97768225704258782 ) ) ;
#99546=CARTESIAN_POINT ( 'NONE',  ( -2.499999999999998668, -30.00000000000000000, 14.79019945774903988 ) ) ;
#99548=CARTESIAN_POINT ( 'NONE',  ( 106.9545358495978036, -14.21045842199422715, 174.0142581296349249 ) ) ;
#99549=CARTESIAN_POINT ( 'NONE',  ( -81.63870341442944323, -46.45233036171202201, 168.1652440659686647 ) ) ;
#99568=CARTESIAN_POINT ( 'NONE',  ( 98.00949598672239915, -60.00000000000002132, 202.3503918769513348 ) ) ;
#99569=CARTESIAN_POINT ( 'NONE',  ( -75.88739805180117060, -29.99999999999992895, 164.4352692622292409 ) ) ;
#99570=CARTESIAN_POINT ( 'NONE',  ( 14.82802221756835337, -56.87755216349057719, 33.50449817620127391 ) ) ;
#99575=CARTESIAN_POINT ( 'NONE',  ( -41.19266119959871020, -39.52519630628623304, 39.71623854401850906 ) ) ;
#99589=CARTESIAN_POINT ( 'NONE',  ( 80.60035871062690660, -30.00000000000002132, -12.85408025116223030 ) ) ;
#99593=CARTESIAN_POINT ( 'NONE',  ( 83.37423355587279161, -30.00000000000000711, 45.87345500807001741 ) ) ;
#99613=CARTESIAN_POINT ( 'NONE',  ( 71.17493717688701338, -38.32825970135854732, 141.0574813979111752 ) ) ;
#99639=CARTESIAN_POINT ( 'NONE',  ( 86.00260977355637237, -31.96737194753035993, 183.8078381457158628 ) ) ;
#99643=CARTESIAN_POINT ( 'NONE',  ( 94.59607722009114639, -57.65580962601410420, -10.11045476332422233 ) ) ;
#99644=CARTESIAN_POINT ( 'NONE',  ( -72.06260621993654070, -38.00000000000000711, -21.47558456850402209 ) ) ;
#99649=CARTESIAN_POINT ( 'NONE',  ( -81.29614434187884342, -30.00000000000000355, -0.4277737793982985259 ) ) ;
#99661=CARTESIAN_POINT ( 'NONE',  ( -69.78524612388557102, -37.99999999999998579, -22.51197996374267163 ) ) ;
#99664=CARTESIAN_POINT ( 'NONE',  ( -99.77890780064966236, -38.00000000000000000, 191.0086380629846872 ) ) ;
#99670=CARTESIAN_POINT ( 'NONE',  ( -55.63384620081478005, -28.59984222904408924, -26.38889157063913515 ) ) ;
#99681=CARTESIAN_POINT ( 'NONE',  ( -81.60080408399453233, -60.00000000000000711, -26.95971957032864097 ) ) ;
#99686=CARTESIAN_POINT ( 'NONE',  ( 100.3941749304550228, -45.27673104686710559, 192.1863761042158103 ) ) ;
#99701=CARTESIAN_POINT ( 'NONE',  ( -70.79351044798765713, -57.68242073007258597, 160.4532249112098157 ) ) ;
#99706=CARTESIAN_POINT ( 'NONE',  ( -86.58068678654640848, -14.21045842199428932, 15.94391106889438525 ) ) ;
#99709=CARTESIAN_POINT ( 'NONE',  ( -49.68514091287890011, -36.05463875348423386, 49.10112299445400907 ) ) ;
#99721=CARTESIAN_POINT ( 'NONE',  ( 102.6639770615377358, -38.43513029337811560, 199.3197935500999449 ) ) ;
#99725=CARTESIAN_POINT ( 'NONE',  ( 91.72323227205116325, -30.00000000000000355, 190.7728913354281133 ) ) ;
#99733=CARTESIAN_POINT ( 'NONE',  ( 52.90017982257470663, -39.50313443167738825, 55.98633902596940715 ) ) ;
#99737=CARTESIAN_POINT ( 'NONE',  ( -90.94353020372604135, -38.35252991750218143, 22.60780205736431370 ) ) ;
#99740=CARTESIAN_POINT ( 'NONE',  ( 107.3311760226882399, -38.36199077526415380, 194.2594862871855810 ) ) ;
#99742=CARTESIAN_POINT ( 'NONE',  ( 91.04242074902893478, -60.15067329966424126, 61.63544511148911909 ) ) ;
#99748=CARTESIAN_POINT ( 'NONE',  ( 73.94230384998250827, -60.00000000000001421, 171.6353201340098167 ) ) ;
#99752=CARTESIAN_POINT ( 'NONE',  ( 59.58870697170010544, -29.07040874811379538, 66.34822725558861123 ) ) ;
#99767=CARTESIAN_POINT ( 'NONE',  ( 84.96427950620631009, -32.31981596804619983, 177.2606859094109666 ) ) ;
#99776=CARTESIAN_POINT ( 'NONE',  ( -12.91373906194155730, -23.42439430174764325, -38.53824115500798086 ) ) ;
#99780=CARTESIAN_POINT ( 'NONE',  ( 47.42216474123039660, -60.00000000000000000, 65.72069959097976266 ) ) ;
#99782=CARTESIAN_POINT ( 'NONE',  ( 19.45299894497249227, -16.87718219434115952, 31.48667012707523938 ) ) ;
#99783=CARTESIAN_POINT ( 'NONE',  ( -16.40833728792867419, -23.49546845913443605, 36.14695687728993789 ) ) ;
#99791=CARTESIAN_POINT ( 'NONE',  ( -12.50707228786319547, -23.21292011592133164, -38.54089711067194912 ) ) ;
#99796=CARTESIAN_POINT ( 'NONE',  ( 15.97931424437294723, -47.40880484825536456, -34.25640142802624410 ) ) ;
#99805=CARTESIAN_POINT ( 'NONE',  ( -106.1131432879537044, -60.00000000000000711, 117.1109480045180078 ) ) ;
#99812=CARTESIAN_POINT ( 'NONE',  ( -84.74062074580929504, -28.95439361776484333, 169.9357238595956971 ) ) ;
#99828=CARTESIAN_POINT ( 'NONE',  ( 102.4475954893556633, -30.00000000000004263, 111.1011446524310742 ) ) ;
#99829=CARTESIAN_POINT ( 'NONE',  ( -106.8727010878311745, -14.21045842199433373, 167.8788319932906461 ) ) ;
#99830=CARTESIAN_POINT ( 'NONE',  ( -56.69927050699357807, -53.38582612393514637, 70.13001638502136359 ) ) ;
#99833=CARTESIAN_POINT ( 'NONE',  ( 114.4431422422120619, -60.00000000000976286, 166.1592868538951393 ) ) ;
#99835=CARTESIAN_POINT ( 'NONE',  ( 2.999727326758741430, -29.02930189954776807, 28.72327379294769401 ) ) ;
#99836=CARTESIAN_POINT ( 'NONE',  ( -105.1952383919716425, -60.15502232595932242, 151.5760161608686758 ) ) ;
#99839=EDGE_CURVE ( 'NONE', #60981, #100031, #98206, .T. ) ;
#99842=LINE ( 'NONE', #58874, #37252 ) ;
#99843=CARTESIAN_POINT ( 'NONE',  ( -73.64671352647415858, -60.00000000000000000, 168.6311605301084455 ) ) ;
#99847=DIRECTION ( 'NONE',  ( 0.000000000000000000, 0.000000000000000000, 1.000000000000000000 ) ) ;
#99854=CARTESIAN_POINT ( 'NONE',  ( 86.10036459384876650, -60.00000000000004263, 13.51756007424883599 ) ) ;
#99856=CARTESIAN_POINT ( 'NONE',  ( -31.45780706891997269, -36.02065666347889561, 33.04706042998527238 ) ) ;
#99859=CARTESIAN_POINT ( 'NONE',  ( 43.48316998106664499, -56.79513185587920532, 46.31952888274560109 ) ) ;
#99864=CARTESIAN_POINT ( 'NONE',  ( -80.06624740215067959, -38.78696431783050258, 193.1076717199356665 ) ) ;
#99868=CARTESIAN_POINT ( 'NONE',  ( 79.70884519849728633, -60.00000000000013500, 171.5327084686719274 ) ) ;
#99876=CARTESIAN_POINT ( 'NONE',  ( 103.6221050402626105, -59.99999999999999289, 102.2249670950544527 ) ) ;
#99882=CARTESIAN_POINT ( 'NONE',  ( -95.93003187330748460, -29.99999999999981526, 191.2983833983815032 ) ) ;
#99890=DIRECTION ( 'NONE',  ( 0.000000000000000000, 0.000000000000000000, -1.000000000000000000 ) ) ;
#99894=CARTESIAN_POINT ( 'NONE',  ( 80.64106222537829183, -56.90139274204167918, 175.6386766945464046 ) ) ;
#99911=CARTESIAN_POINT ( 'NONE',  ( 87.19800390447835525, -46.42919513289680822, 191.1394352392929932 ) ) ;
#99926=CARTESIAN_POINT ( 'NONE',  ( 112.0387186725491091, -57.67108335773423278, 191.1994195377486108 ) ) ;
#99933=CARTESIAN_POINT ( 'NONE',  ( -90.45134624145916291, -60.00000000000001421, 202.0642490602653538 ) ) ;
#99937=CARTESIAN_POINT ( 'NONE',  ( -83.55671512945748702, -53.74164608449824954, 187.8046252073974358 ) ) ;
#99947=CARTESIAN_POINT ( 'NONE',  ( -85.13337042228866380, -52.74891044688261843, -12.49663770922077255 ) ) ;
#99957=CARTESIAN_POINT ( 'NONE',  ( 59.37626172009473180, -60.00000000000000000, -38.24869620007160620 ) ) ;
#99959=CARTESIAN_POINT ( 'NONE',  ( -74.24640087699403068, -25.59795120301134830, 107.9182274487227602 ) ) ;
#99961=CARTESIAN_POINT ( 'NONE',  ( 75.52921836606891759, -59.99999999999984368, 193.8580410961210134 ) ) ;
#99963=CARTESIAN_POINT ( 'NONE',  ( 93.82677057603169146, -57.67444542026858301, 11.80858161689750752 ) ) ;
#99974=CARTESIAN_POINT ( 'NONE',  ( 6.539732759932831208, -4.285714285714297134, -24.41571844174604067 ) ) ;
#99982=CARTESIAN_POINT ( 'NONE',  ( 32.67496446562977752, -36.02319022030835072, 33.54900523351410868 ) ) ;
#99992=CARTESIAN_POINT ( 'NONE',  ( 1.078140322363270668E-05, -30.00000000000000000, 28.88964995960238014 ) ) ;
#99998=CARTESIAN_POINT ( 'NONE',  ( 65.89753327251730752, -60.00000000000000000, -33.92370292367453288 ) ) ;
#100012=CARTESIAN_POINT ( 'NONE',  ( 84.49694251429671965, -45.28645896664576043, -6.726666319064526611 ) ) ;
#100023=CARTESIAN_POINT ( 'NONE',  ( 72.91780076713102687, -42.96040658466132101, 114.3445280546203122 ) ) ;
#100029=CARTESIAN_POINT ( 'NONE',  ( -114.2271649293462445, -57.67113267762195505, 172.5270642037310722 ) ) ;
#100031=VERTEX_POINT ( 'NONE', #39639 ) ;
#100035=CARTESIAN_POINT ( 'NONE',  ( 102.1162378120948802, -37.84850780196365605, 183.3995072184255548 ) ) ;
#100052=CARTESIAN_POINT ( 'NONE',  ( -87.82931391962068801, -30.00000000000000000, 186.3420930804710736 ) ) ;
#100057=CARTESIAN_POINT ( 'NONE',  ( 70.41249110440050174, -57.68249115096489987, 157.3832962191312674 ) ) ;
#100061=CARTESIAN_POINT ( 'NONE',  ( 59.52453317996337745, -37.26894803123993682, -34.27940060143461665 ) ) ;
#100065=CARTESIAN_POINT ( 'NONE',  ( -36.68252776495059919, -60.00000000000001421, 48.02914264494187080 ) ) ;
#100067=CARTESIAN_POINT ( 'NONE',  ( -86.42980866402069751, -20.84916326163546429, 182.4270226805664663 ) ) ;
#100070=CARTESIAN_POINT ( 'NONE',  ( -9.282201836941181838, -46.43936834299204719, 31.63261336507683552 ) ) ;
#100083=CARTESIAN_POINT ( 'NONE',  ( 113.0845476695725864, -59.99999999999993605, 149.3435440849930842 ) ) ;
#100084=CARTESIAN_POINT ( 'NONE',  ( -80.22109857244845443, -42.96982832339585201, 151.2315873428279076 ) ) ;
#100108=CARTESIAN_POINT ( 'NONE',  ( 93.04510679386291372, -60.00000000000001421, 32.83262320753426877 ) ) ;
#100110=CARTESIAN_POINT ( 'NONE',  ( -89.23267494088513274, -59.99999999999987921, 204.3671292578742680 ) ) ;
#100111=CARTESIAN_POINT ( 'NONE',  ( 24.01072772857711968, -49.91340150330263725, 33.32366789474293967 ) ) ;
#100115=CARTESIAN_POINT ( 'NONE',  ( -39.65982915714113233, -49.89218387423591139, 40.68439334530297202 ) ) ;
#100118=ORIENTED_EDGE ( 'NONE', *, *, #94998, .T. ) ;
#100126=CARTESIAN_POINT ( 'NONE',  ( -44.47534256803313468, -38.31161230092084224, 57.00189278798902137 ) ) ;
#100128=CARTESIAN_POINT ( 'NONE',  ( 81.40593295988355749, -29.99999999999995026, -2.043119297071557039 ) ) ;
#100133=CARTESIAN_POINT ( 'NONE',  ( 86.61543636280471503, -29.99999999999999645, 68.10094066095521725 ) ) ;
#100152=CARTESIAN_POINT ( 'NONE',  ( 62.23204737827733624, -38.34071032238272636, 103.6626538615274313 ) ) ;
#100154=B_SPLINE_CURVE_WITH_KNOTS ( 'NONE', 3,
 ( #55278, #22439, #47193, #30521, #14289, #23491, #97336, #57402, #89794, #32100, #48776, #73585, #16425, #6198, #96830, #15363, #56335, #89267, #81668, #104369, #5683, #104926, #14824, #90317, #6741, #24556, #39136, #32646, #72536, #63419, #48249, #63943, #72014, #64981, #31066, #22960, #81150, #7790, #96311, #65517, #55796, #105444, #88733, #7261, #40172, #73046, #79570, #105956, #97875, #24030, #56871, #99998, #35303, #50902, #101064, #41763, #33698, #75179, #100528, #18043, #60111, #9376, #1819, #91912, #67649, #26689, #18585, #25630, #68170, #66572, #34775, #42290, #84361, #10452, #8329, #83285, #59025, #82756, #59563, #41233, #92429, #49306, #51447, #58492, #43367, #76254, #57936, #83811, #16974, #42830, #74119, #67113, #75726, #2360, #33169, #8857, #49851, #27224, #9922, #26166, #92975, #74648, #206, #82215, #99456, #17511, #66041, #732, #1278, #98918, #90858, #25078, #91396, #50373, #34243, #86514, #20202, #13102, #28281, #27762, #102125, #53058, #70306, #94598, #78383, #19670, #62238, #43891, #29348, #103722, #19137, #60636, #2887, #20745, #36904, #68725, #37970, #69774, #44979, #37437, #95121, #84888, #51972, #10976, #12049, #102666, #3443, #54090, #69252, #21253, #46030, #87032, #78912, #61155, #101607, #93523, #77330, #5038, #45511, #70832, #94041, #29869, #36386, #12574, #4500, #62747, #28826, #77860, #11507, #76783, #85423, #35846, #85978, #52507, #53584, #44435, #103202, #3974, #61705, #40579, #7660, #64342, #106357, #79966, #105318, #15238, #104245, #40051, #87554, #89138, #80491, #31460, #63813, #81535, #14692, #48125, #22308, #72415, #6611, #30934, #96178, #56199, #55154, #88083, #47596, #96700, #81023, #22837, #97212, #71880, #13636, #105836, #104784, #38481, #46551, #7140, #14161, #79443, #73460, #6082, #55669, #71347, #30392, #63279, #5554, #47064, #39538, #23362, #32519, #31979, #72926, #64855, #56744, #95641, #39002, #88606, #97735, #23904, #89672, #15769, #54612, #48651, #21777, #606, #43243, #99326, #84233, #82, #92305, #66448, #57273, #50262, #49728, #41116, #50771, #73998, #33051, #83165, #34656, #49185, #18457, #99876, #58358, #16296, #66995, #65919, #9259, #67525, #75602, #26048, #16847, #100406, #42168, #51311, #58907, #10328, #57809, #82635, #91277, #9790, #34122, #91798, #25500, #17918, #1149, #83683, #42705, #26568, #41646, #76128, #8737, #1701, #17388, #65393, #59440, #2225, #98284, #24441, #75052, #90195, #98797, #24954, #90732, #82088, #8206, #74529, #33570, #78257, #103077, #43764, #44850, #2770, #28688, #27096, #52924, #61570, #70172, #19007, #101480, #35719, #94999, #77202, #84763, #76656, #93397, #29231, #94464, #4370, #11381, #100938, #68596, #69646, #28157, #92844, #36782, #27631, #20077, #37308, #45376, #102539, #19544, #60512, #20621, #62107, #86382, #12449, #53963, #86901, #12974, #52380, #59983, #53462, #102000, #21135, #77741, #45900, #78777, #35174, #44306, #68041, #85291, #51851, #61033, #10846, #3312, #36257, #69126, #93919, #85849, #11923, #3852, #87432, #13507, #37841, #4911, #56070, #14036, #47993, #72801, #46429, #14559, #96575, #46942, #97605, #6478, #64218, #70704, #79314, #5437, #104651, #5947, #47469, #22174, #55023, #29746, #87954, #72285, #38359, #71221, #63689, #79842, #38873, #39409, #71740, #62619, #15106, #30803, #54485, #95505, #105189, #104114, #21648, #56619, #96046, #22710, #89011, #80364, #97088, #30259, #80901, #63148, #55548, #89541, #7010, #23231, #39929, #105707, #48527, #88485, #31335, #31849, #64731, #23772, #15634, #103595, #7529, #40447, #16707, #74396, #73873, #33989, #57150, #25917, #57674, #73327, #8607, #42040, #50636, #81418, #49054, #90064, #17258, #66317, #16168, #106226, #99199, #475, #66859, #58773, #33444, #32388, #98149, #25363, #58223, #90597, #17786, #49597, #91670, #9655, #83554, #65259, #41509, #40984, #106768, #82505, #24301, #81950, #8075, #91149, #98669, #50128, #32914, #65792, #24822, #83038, #9129, #74922, #1005, #99748, #30071, #31143, #71550, #72621, #32182, #15444, #48335, #89876, #15983, #48860, #63493, #95850, #55364, #80703, #97413, #79652, #81230, #62954, #64547, #55877, #6820, #39218, #56955, #96909, #23573, #104455, #30603, #5763, #96391, #81753, #105001, #103924, #21980, #7347, #73131, #72093, #7875, #40256, #54835, #56420, #65064, #88293, #88812, #6279, #71033, #105523, #89353, #87763, #46758, #38685, #64031, #23040, #47798, #14906, #39740, #22521, #13845, #106035, #14368, #31663, #97961, #47277, #24111, #80175, #5369, #9160, #17291, #91702, #58256, #33474, #2126, #1047, #50165, #17817, #67430, #76030, #91183, #83067, #42071, #66346, #74956, #99231, #67950, #2666, #25949, #100307, #50670, #101381, #10231, #100831, #74430, #34021, #66893, #68493, #84133, #92204, #26467, #83583, #99780, #506, #26997, #58809, #9692, #35617, #42602, #59338, #18358, #75497, #1594, #25399, #34557, #59876, #51211, #35080, #43147, #92749, #60415, #18907, #51752, #84666, #10752, #43667, #76556, #27536, #93292, #19449, #52283, #8640, #41542, #69030, #88261, #104425, #19976, #102442, #22494, #71523, #30571, #23010, #44213, #11280, #77100, #79619, #63467, #69552, #14877, #28586, #55845, #6792, #88785, #47767, #20525, #28062, #72064, #60934, #52822, #96362, #80671, #101902, #39712, #61471, #47246, #80149, #96876, #55332, #5732, #77639, #36158, #44753, #3217, #46727, #85749, #14339, #6249, #31628, #3757, #94363, #38657, #31114, #39184, #97384, #53361, #104973, #64002, #93824, #72586, #11820, #105493, #64515, #23544, #86282, #85195, #36689, #13815, #91448, #17563, #15414, #90369, #66091, #89845, #41813, #48301, #66626, #58548, #57450, #1330, #781, #32152, #89318, #56385, #33754, #65564, #99510, #65029, #98969, #24077, #49902, #81198, #74174, #82810, #50425, #40223, #15950, #56920 ),
 .UNSPECIFIED., .F., .F.,
 ( 4, 1, 1, 1, 1, 1, 1, 2, 2, 1, 1, 2, 2, 1, 1, 1, 1, 1, 1, 1, 2, 2, 1, 1, 1, 1, 1, 1, 1, 1, 2, 2, 1, 1, 1, 1, 1, 1, 1, 1, 1, 2, 2, 1, 1, 1, 1, 1, 1, 1, 1, 1, 2, 2, 1, 1, 1, 1, 1, 1, 1, 2, 2, 1, 1, 1, 1, 2, 2, 1, 1, 1, 1, 1, 2, 2, 1, 1, 1, 1, 1, 1, 2, 2, 1, 1, 1, 1, 1, 1, 2, 2, 1, 1, 1, 1, 1, 2, 2, 1, 1, 1, 1, 1, 1, 2, 2, 1, 1, 1, 1, 1, 2, 2, 1, 1, 1, 1, 1, 2, 2, 1, 1, 1, 1, 1, 1, 2, 2, 1, 1, 1, 1, 1, 2, 2, 1, 1, 1, 1, 1, 1, 1, 2, 2, 1, 1, 1, 1, 1, 1, 1, 1, 2, 2, 1, 1, 1, 1, 1, 1, 2, 2, 1, 1, 1, 1, 1, 1, 1, 2, 2, 1, 1, 1, 1, 1, 1, 1, 1, 1, 2, 2, 1, 1, 1, 1, 1, 1, 1, 1, 1, 1, 2, 2, 1, 1, 1, 1, 2, 2, 1, 1, 1, 1, 1, 1, 1, 1, 1, 2, 2, 1, 1, 1, 1, 1, 1, 1, 1, 1, 2, 2, 1, 1, 1, 1, 1, 1, 1, 1, 2, 2, 1, 1, 1, 1, 1, 1, 1, 2, 2, 1, 1, 1, 1, 1, 1, 1, 2, 2, 1, 1, 1, 1, 1, 1, 1, 1, 1, 2, 2, 1, 1, 1, 1, 1, 1, 1, 2, 2, 1, 1, 1, 1, 1, 1, 1, 1, 2, 2, 1, 1, 1, 1, 1, 1, 1, 1, 2, 2, 1, 1, 1, 1, 1, 2, 2, 1, 1, 1, 1, 2, 2, 1, 1, 1, 1, 1, 2, 2, 1, 1, 1, 1, 1, 2, 2, 1, 1, 2, 2, 1, 2, 2, 1, 1, 1, 1, 2, 2, 1, 1, 1, 1, 2, 2, 1, 1, 1, 1, 2, 2, 1, 1, 1, 1, 1, 1, 2, 2, 1, 1, 1, 1, 1, 1, 2, 2, 1, 1, 1, 1, 1, 1, 1, 2, 2, 1, 1, 1, 1, 1, 1, 1, 2, 2, 1, 1, 1, 1, 1, 1, 1, 1, 2, 2, 1, 1, 1, 1, 2, 2, 1, 1, 1, 1, 1, 1, 1, 1, 2, 2, 1, 1, 1, 1, 1, 1, 2, 2, 1, 1, 1, 1, 1, 1, 2, 2, 1, 1, 1, 1, 1, 2, 2, 1, 1, 1, 1, 1, 1, 2, 2, 1, 1, 1, 1, 1, 1, 2, 2, 1, 1, 1, 1, 2, 2, 1, 1, 1, 1, 1, 1, 1, 2, 2, 1, 1, 1, 1, 1, 1, 1, 2, 2, 1, 1, 1, 1, 1, 1, 1, 2, 2, 1, 1, 1, 1, 1, 1, 1, 2, 2, 1, 1, 1, 1, 1, 1, 2, 2, 1, 1, 1, 1, 1, 1, 2, 2, 1, 1, 1, 1, 1, 2, 2, 1, 1, 1, 1, 2, 2, 1, 1, 1, 1, 2, 2, 1, 1, 1, 1, 1, 2, 2, 1, 1, 1, 1, 1, 1, 2, 2, 1, 1, 1, 1, 1, 1, 2, 2, 1, 1, 1, 1, 1, 1, 1, 2, 2, 1, 1, 1, 1, 1, 1, 1, 2, 2, 1, 1, 1, 1, 1, 1, 1, 2, 2, 4 ),
 ( 0.000000000000000000, 0.007812499999935031136, 0.01171874999990254497, 0.01367187499988630275, 0.01464843749987818251, 0.01513671874987412153, 0.01538085937487209190, 0.01550292968737107362, 0.01562499999987005533, 0.02343749999980482279, 0.02734374999977220652, 0.02929687499975590359, 0.03124999999973960760, 0.04687499999960928476, 0.05468749999954413549, 0.05859374999951156432, 0.06054687499949527874, 0.06152343749948713247, 0.06201171874948303853, 0.06225585937448099155, 0.06237792968697994378, 0.06249999999947890295, 0.07812499999934767458, 0.08593749999928204653, 0.08984374999924922556, 0.09179687499923282201, 0.09277343749922460636, 0.09326171874922049854, 0.09350585937421843075, 0.09362792968671740379, 0.09368896484296690419, 0.09374999999921639071, 0.1093749999990826505, 0.1171874999990158012, 0.1210937499989824112, 0.1230468749989657024, 0.1240234374989573618, 0.1245117187489531985, 0.1247558593739510890, 0.1248779296864500898, 0.1249389648426995902, 0.1249694824208242849, 0.1249999999989489935, 0.1406249999988075927, 0.1484374999987368993, 0.1523437499987015387, 0.1542968749986838584, 0.1552734374986749766, 0.1557617187486705079, 0.1560058593736682875, 0.1561279296861672328, 0.1561889648424166777, 0.1562194824205414556, 0.1562499999986662336, 0.1640624999986147747, 0.1679687499985890731, 0.1699218749985761945, 0.1708984374985696997, 0.1713867187485664523, 0.1716308593735648147, 0.1717529296860639820, 0.1718139648423135935, 0.1718749999985632049, 0.1757812499985364207, 0.1777343749985230148, 0.1787109374985162979, 0.1791992187485129118, 0.1794433593735112187, 0.1796874999985095256, 0.1835937499984822696, 0.1855468749984686416, 0.1865234374984618415, 0.1870117187484584276, 0.1872558593734567345, 0.1873779296859559018, 0.1874999999984550414, 0.1914062499984279242, 0.1933593749984143517, 0.1943359374984076071, 0.1948242187484042209, 0.1950683593734025001, 0.1951904296859016674, 0.1952514648421512511, 0.1953124999984008070, 0.1992187499983747445, 0.2011718749983617271, 0.2021484374983552046, 0.2026367187483519572, 0.2028808593733503196, 0.2030029296858494869, 0.2030639648420990984, 0.2031249999983486820, 0.2050781249983356369, 0.2060546874983291421, 0.2065429687483258669, 0.2067871093733242571, 0.2069091796858234522, 0.2069702148420730359, 0.2070312499983226473, 0.2089843749983096299, 0.2099609374983031074, 0.2104492187482998600, 0.2106933593732982501, 0.2108154296857974175, 0.2108764648420470289, 0.2109069824201718346, 0.2109374999982966403, 0.2128906249982839838, 0.2138671874982776555, 0.2143554687482744914, 0.2145996093732729093, 0.2147216796857721044, 0.2147827148420217158, 0.2148437499982712995, 0.2167968749982587262, 0.2177734374982524534, 0.2182617187482492893, 0.2185058593732477072, 0.2186279296857469301, 0.2186889648419965138, 0.2187499999982461252, 0.2226562499982208121, 0.2246093749982081278, 0.2255859374982018273, 0.2260742187481986631, 0.2263183593731970533, 0.2264404296856962762, 0.2265014648419458876, 0.2265624999981954713, 0.2304687499981701582, 0.2324218749981575016, 0.2333984374981511456, 0.2338867187481479815, 0.2341308593731463994, 0.2342529296856455945, 0.2343749999981447896, 0.2421874999980942467, 0.2460937499980689613, 0.2480468749980563326, 0.2490234374980500320, 0.2495117187480468679, 0.2497558593730452858, 0.2498779296855445087, 0.2499389648417940923, 0.2499999999980437315, 0.2656249999979469201, 0.2734374999978985699, 0.2773437499978743670, 0.2792968749978622656, 0.2802734374978562149, 0.2807617187478532172, 0.2810058593728517184, 0.2811279296853509968, 0.2811889648416006082, 0.2812499999978501641, 0.2890624999978015919, 0.2929687499977773335, 0.2949218749977651766, 0.2958984374977591258, 0.2963867187477561282, 0.2966308593727545739, 0.2967529296852537968, 0.2968749999977530196, 0.3046874999977027820, 0.3085937499976776355, 0.3105468749976650900, 0.3115234374976587617, 0.3120117187476556531, 0.3122558593726540987, 0.3123779296851532661, 0.3124389648414028775, 0.3124999999976524889, 0.3281249999975477394, 0.3359374999974953924, 0.3398437499974692466, 0.3417968749974561460, 0.3427734374974495957, 0.3432617187474463205, 0.3435058593724447107, 0.3436279296849438780, 0.3436889648411934894, 0.3437194824193182674, 0.3437499999974430454, 0.3593749999973815390, 0.3671874999973507303, 0.3710937499973353537, 0.3730468749973276932, 0.3740234374973238074, 0.3745117187473219200, 0.3747558593723210318, 0.3748779296848205322, 0.3749389648410703102, 0.3749694824191952547, 0.3749847412082576437, 0.3749999999973200882, 0.3828124999973044340, 0.3867187499972965514, 0.3886718749972926656, 0.3896484374972907783, 0.3901367187472897791, 0.3906249999972888354, 0.3984374999972733478, 0.4023437499972656317, 0.4042968749972616904, 0.4052734374972596920, 0.4057617187472586373, 0.4060058593722580267, 0.4061279296847577491, 0.4061889648410076936, 0.4062194824191325826, 0.4062347412081950271, 0.4062499999972574161, 0.4218749999971741493, 0.4296874999971324605, 0.4335937499971116438, 0.4355468749971012632, 0.4365234374970959896, 0.4370117187470933806, 0.4372558593720921039, 0.4373779296845914377, 0.4374389648408411602, 0.4374694824189659936, 0.4374999999970907716, 0.4531249999970035636, 0.4609374999969600428, 0.4648437499969382825, 0.4667968749969272912, 0.4677734374969217956, 0.4682617187469190756, 0.4685058593719177433, 0.4686279296844170217, 0.4686889648406666886, 0.4687499999969163000, 0.4765624999968729458, 0.4804687499968512410, 0.4824218749968403608, 0.4833984374968350317, 0.4838867187468323117, 0.4841308593718309794, 0.4842529296843304243, 0.4843139648405801467, 0.4843749999968298692, 0.4921874999968056663, 0.4960937499967935094, 0.4980468749967875697, 0.4990234374967845166, 0.4995117187467830178, 0.4997558593717822961, 0.4998779296842817965, 0.4999389648405315745, 0.4999999999967813524, 0.5156249999967325026, 0.5234374999967079667, 0.5273437499966957542, 0.5292968749966897590, 0.5302734374966865394, 0.5307617187466850961, 0.5310058593716844300, 0.5311279296841838748, 0.5311889648404337638, 0.5312194824185586528, 0.5312499999966834308, 0.5390624999966778796, 0.5429687499966751041, 0.5449218749966738828, 0.5458984374966732167, 0.5463867187466728836, 0.5466308593716726616, 0.5467529296841725506, 0.5468139648404225506, 0.5468749999966726616, 0.5546874999966865394, 0.5585937499966934228, 0.5605468749966969755, 0.5615234374966986408, 0.5620117187466993069, 0.5622558593716997510, 0.5623779296842000841, 0.5624389648404501951, 0.5624694824185751951, 0.5624999999967000841, 0.5703124999967056352, 0.5742187499967084108, 0.5761718749967096320, 0.5771484374967102982, 0.5776367187467107422, 0.5778808593717107422, 0.5780029296842108533, 0.5780639648404610753, 0.5780944824185860753, 0.5781249999967111863, 0.5820312499967029707, 0.5839843749966986408, 0.5849609374966965314, 0.5854492187466955322, 0.5856933593716948661, 0.5858154296841946440, 0.5859374999966944220, 0.5898437499966880937, 0.5917968749966850961, 0.5927734374966835418, 0.5932617187466827646, 0.5935058593716823205, 0.5937499999966818764, 0.5976562499966756592, 0.5996093749966725506, 0.6005859374966709963, 0.6010742187466702191, 0.6013183593716697750, 0.6014404296841695530, 0.6015624999966693309, 0.6054687499966613373, 0.6074218749966574515, 0.6083984374966554531, 0.6088867187466544539, 0.6091308593716540098, 0.6092529296841537878, 0.6093749999966534547, 0.6113281249966494579, 0.6123046874966474595, 0.6127929687466464603, 0.6132812499966455722, 0.6152343749966416864, 0.6162109374966397990, 0.6171874999966379116, 0.6210937499966301401, 0.6230468749966260322, 0.6240234374966240338, 0.6245117187466230346, 0.6247558593716224795, 0.6249999999966220354, 0.6289062499966131536, 0.6308593749966087127, 0.6318359374966064923, 0.6323242187466053821, 0.6325683593716049380, 0.6328124999966044939, 0.6367187499965958342, 0.6386718749965916153, 0.6396484374965893949, 0.6401367187465882846, 0.6403808593715877295, 0.6406249999965871744, 0.6445312499965771824, 0.6464843749965721864, 0.6474609374965697439, 0.6479492187465684117, 0.6481933593715677455, 0.6483154296840674125, 0.6483764648403171904, 0.6484374999965669684, 0.6523437499965499820, 0.6542968749965414332, 0.6552734374965371034, 0.6557617187465351050, 0.6560058593715341058, 0.6561279296840334396, 0.6561889648402831066, 0.6562499999965326625, 0.6601562499965086817, 0.6621093749964966912, 0.6630859374964906960, 0.6635742187464878095, 0.6638183593714862551, 0.6639404296839854780, 0.6640014648402351449, 0.6640319824183599229, 0.6640624999964848119, 0.6679687499964853670, 0.6699218749964857000, 0.6708984374964859221, 0.6713867187464859221, 0.6716308593714860331, 0.6717529296839860331, 0.6718139648402359221, 0.6718444824183610331, 0.6718749999964861441, 0.6757812499964886976, 0.6777343749964900299, 0.6787109374964906960, 0.6791992187464910291, 0.6794433593714912512, 0.6795654296839913622, 0.6796264648402413622, 0.6796569824183664732, 0.6796722412074290842, 0.6796874999964916952, 0.6835937499964956920, 0.6855468749964976904, 0.6865234374964988007, 0.6870117187464992448, 0.6872558593714994668, 0.6874999999964995778, 0.6914062499965030195, 0.6933593749965047959, 0.6943359374965056841, 0.6948242187465063502, 0.6950683593715065722, 0.6951904296840065722, 0.6952514648402567943, 0.6952819824183820163, 0.6952972412074446273, 0.6953124999965073494, 0.6992187499965401010, 0.7011718749965563102, 0.7021484374965644149, 0.7026367187465686337, 0.7028808593715706321, 0.7030029296840717423, 0.7030639648403224085, 0.7031249999965729636, 0.7109374999966618924, 0.7148437499967063014, 0.7167968749967285058, 0.7177734374967396080, 0.7182617187467451592, 0.7185058593717480457, 0.7186279296842494890, 0.7187499999967509323, 0.7343749999969289011, 0.7421874999970180520, 0.7460937499970626829, 0.7480468749970848874, 0.7490234374970959896, 0.7495117187471016518, 0.7499999999971072029, 0.7656249999972888354, 0.7734374999973796516, 0.7773437499974250597, 0.7792968749974478193, 0.7802734374974590326, 0.7807617187474648057, 0.7810058593724676923, 0.7812499999974704679, 0.7968749999976542098, 0.8046874999977460252, 0.8085937499977918774, 0.8105468749978148590, 0.8115234374978262943, 0.8120117187478319565, 0.8122558593728348431, 0.8124999999978376186, 0.8281249999980183629, 0.8359374999981087351, 0.8398437499981539212, 0.8417968749981765697, 0.8427734374981878940, 0.8437499999981992183, 0.8515624999982897014, 0.8554687499983348875, 0.8574218749983575361, 0.8583984374983688603, 0.8588867187483744114, 0.8591308593733772980, 0.8592529296858787413, 0.8593139648421294075, 0.8593749999983800736, 0.8671874999984743315, 0.8710937499985214050, 0.8730468749985448307, 0.8740234374985565990, 0.8745117187485624832, 0.8747558593735652588, 0.8748779296860667021, 0.8749389648423174792, 0.8749999999985681454, 0.8828124999986611821, 0.8867187499987075894, 0.8886718749987307930, 0.8896484374987423394, 0.8901367187487481125, 0.8903808593737511101, 0.8905029296862526644, 0.8905639648425033306, 0.8906249999987541077, 0.8984374999988422594, 0.9023437499988864463, 0.9042968749989085397, 0.9052734374989195310, 0.9057617187489251931, 0.9060058593739279686, 0.9061279296864293009, 0.9061889648426800781, 0.9062499999989307442, 0.9101562499989760413, 0.9121093749989985788, 0.9130859374990099031, 0.9135742187490156763, 0.9138183593740184518, 0.9139404296865198951, 0.9140014648427706723, 0.9140624999990213384, 0.9179687499990665245, 0.9199218749990891730, 0.9208984374991004973, 0.9213867187491061594, 0.9216308593741090460, 0.9217529296866104893, 0.9218139648428611554, 0.9218749999991119326, 0.9257812499991567856, 0.9277343749991792121, 0.9287109374991904254, 0.9291992187491959765, 0.9294433593741987520, 0.9295654296867001953, 0.9296874999992016386, 0.9335937499992466027, 0.9355468749992691402, 0.9365234374992804645, 0.9370117187492860156, 0.9372558593742889022, 0.9374999999992916777, 0.9414062499993371969, 0.9433593749993599564, 0.9443359374993711697, 0.9448242187493769428, 0.9450683593743798294, 0.9453124999993826050, 0.9492187499994281241, 0.9511718749994507727, 0.9521484374994620969, 0.9526367187494678701, 0.9528808593744706457, 0.9530029296869720890, 0.9531249999994735322, 0.9570312499995189404, 0.9589843749995415889, 0.9599609374995529132, 0.9604492187495586863, 0.9606933593745614619, 0.9608154296870629052, 0.9608764648433136824, 0.9609374999995643485, 0.9648437499996087574, 0.9667968749996310729, 0.9677734374996421751, 0.9682617187496477262, 0.9685058593746505018, 0.9686279296871519451, 0.9686889648434026112, 0.9687499999996533884, 0.9726562499996975752, 0.9746093749997197797, 0.9755859374997308819, 0.9760742187497363220, 0.9763183593747390976, 0.9764404296872405409, 0.9765014648434912070, 0.9765319824216165401, 0.9765624999997418731, 0.9804687499997850608, 0.9824218749998067102, 0.9833984374998175904, 0.9838867187498229194, 0.9841308593748256950, 0.9842529296873270273, 0.9843139648435776934, 0.9843444824217030265, 0.9843749999998282485, 0.9882812499998713252, 0.9902343749998927525, 0.9912109374999035216, 0.9916992187499089617, 0.9919433593749116262, 0.9920654296874129585, 0.9921264648436637357, 0.9921569824217889577, 0.9921874999999142908, 1.000000000000000000 ),
 .UNSPECIFIED. ) ;
#100172=CARTESIAN_POINT ( 'NONE',  ( 86.23189122538319396, -24.68366007135474760, 181.5277984381359886 ) ) ;
#100176=CARTESIAN_POINT ( 'NONE',  ( 93.00281210641563234, -57.65601615028951699, -17.21362402452485441 ) ) ;
#100179=CARTESIAN_POINT ( 'NONE',  ( 0.000000000000000000, -30.00000000000000000, 0.000000000000000000 ) ) ;
#100183=CARTESIAN_POINT ( 'NONE',  ( -93.99531654986856211, -30.00000000000000355, 111.9393279711768798 ) ) ;
#100198=CARTESIAN_POINT ( 'NONE',  ( 13.04985325050550315, -16.80601421349662417, -34.54123526020268997 ) ) ;
#100199=CARTESIAN_POINT ( 'NONE',  ( -25.48234102807342083, -56.87598310890427200, 34.80864869422586594 ) ) ;
#100203=CARTESIAN_POINT ( 'NONE',  ( -50.03090904413763695, -27.50677130059942854, -27.97160039159090772 ) ) ;
#100213=CARTESIAN_POINT ( 'NONE',  ( -82.58075912419870690, -59.99999999999999289, -26.31469373492660679 ) ) ;
#100216=CARTESIAN_POINT ( 'NONE',  ( 101.5064089130223692, -60.23311196733765627, 194.7041288308016931 ) ) ;
#100230=CARTESIAN_POINT ( 'NONE',  ( -11.25203090971146302, -57.67122638729478723, 41.63652355756774881 ) ) ;
#100234=CARTESIAN_POINT ( 'NONE',  ( -87.78075539319912934, -14.21045842199443499, -8.620330001511526063 ) ) ;
#100238=CARTESIAN_POINT ( 'NONE',  ( -49.74225373137043960, -60.29818990586195326, 57.32659193509455520 ) ) ;
#100247=CARTESIAN_POINT ( 'NONE',  ( 87.56679391027844872, -38.57208170489048626, 199.7935100241939210 ) ) ;
#100254=CARTESIAN_POINT ( 'NONE',  ( 93.38388337575746334, -30.00000000000000711, 191.1906521887401311 ) ) ;
#100261=CARTESIAN_POINT ( 'NONE',  ( 53.27090504139580673, -42.96895588525129739, 58.02480099802018287 ) ) ;
#100267=CARTESIAN_POINT ( 'NONE',  ( -91.44302139157441900, -38.39068403194840329, -8.132174192228589504 ) ) ;
#100271=CARTESIAN_POINT ( 'NONE',  ( 110.3727171012441488, -38.35605046350913483, 158.9384829488004982 ) ) ;
#100273=CARTESIAN_POINT ( 'NONE',  ( 86.56429641673445019, -52.71572802512593370, 37.65660418523465580 ) ) ;
#100281=CARTESIAN_POINT ( 'NONE',  ( 59.17824404644323266, -49.90990980372215091, 74.96678020754490035 ) ) ;
#100294=CARTESIAN_POINT ( 'NONE',  ( 84.73811181637501022, -32.38007879023361824, 175.3238245508336206 ) ) ;
#100303=CARTESIAN_POINT ( 'NONE',  ( -20.17834448772858380, -25.90226919805355266, -38.48103527270688318 ) ) ;
#100307=CARTESIAN_POINT ( 'NONE',  ( 50.76975585573665484, -60.00000000000000711, 73.74697247292149882 ) ) ;
#100309=CARTESIAN_POINT ( 'NONE',  ( -27.57469521172910376, -30.80484053261712774, 39.32463195004949341 ) ) ;
#100324=CARTESIAN_POINT ( 'NONE',  ( 54.58014935078251284, -60.22827346522726799, -31.12123911173822677 ) ) ;
#100326=B_SPLINE_CURVE_WITH_KNOTS ( 'NONE', 3,
 ( #53492, #29260, #11954, #52957, #69679, #5469, #95031, #61607, #62141, #70733, #102576, #21686, #37875, #103629, #62660, #71256, #45416, #78288, #60542, #52411, #11415, #36293, #4406, #44341, #3352, #83464, #5980, #106671, #82407, #58674, #9565, #50549, #58125, #74305, #65696, #73772, #41942, #49501, #91051, #42471, #22209, #90500, #55060, #32288, #17160, #65156, #98054, #48955, #24203, #75369, #8509, #99104, #9035, #106129, #82937, #57052, #99649, #81852, #30295, #380, #50031, #40886, #74828, #909, #98581, #33887, #89968, #25822, #91578, #17685, #41410, #66762, #25263, #63184, #24727, #57578, #32820, #46977, #16610, #16075, #7973, #96078, #87988, #33348, #14068, #66216, #79875, #38910, #71775, #18779, #93164, #2008, #51082, #27413, #18229, #60291, #68906, #84002, #101779, #85616, #59743, #59210, #36563, #12228, #34955, #43550, #19331, #34432, #53239, #52161, #94231, #67824, #85073, #61342, #102313, #69433, #11157, #27948, #51628, #28465, #44086, #10631, #10110, #3087, #101261, #76969, #20396, #43019, #92621, #100707, #2547, #45159, #86162, #44627, #60810, #76430, #1468, #36032, #93702, #35489, #75908, #26874, #100183, #84546, #67301, #19854, #68365, #92089, #52689, #11691, #77515, #3628, #26350, #78039, #79095, #70486, #53759, #80150, #86687, #64003, #47247, #95293, #12757, #63468, #79620, #96877, #95824, #13816, #88262, #14341, #54804, #71524, #4158, #96363, #37089, #21953, #21423, #45681, #69955, #102851, #46211, #78559, #72065, #4691, #55846, #37623, #30041, #104426, #29018, #22495, #61884, #87737, #54264, #103381, #94778, #20925, #5218, #62401, #29528, #104974, #87207, #13281, #30572, #14878, #55333, #38148, #6250, #71005, #31115, #23012, #88786, #46729, #39186, #38658, #103898, #62931, #5734, #15951, #64516, #56921, #32153, #254, #6793, #39713, #24078, #66627, #57452, #106007, #82270, #81720, #65030, #32698, #48302, #97385, #73639, #23545, #106543, #8382, #56386, #41285, #25135, #33221, #105494, #82811, #58550, #81199, #89846, #65565, #80672, #99511, #98453, #33755, #7311, #24603, #782, #41814, #8912, #90370, #74175, #97927, #74702, #15415, #48827, #89319, #49363, #40752, #16485, #25685, #40225, #7845, #73093, #66093, #91449, #47768, #90914, #98970, #57994, #72587, #17027, #49903, #31631, #27284, #42884, #9428, #34296, #52560, #60165, #84415, #1331, #35360, #93033, #68230, #76305, #2948, #17564, #18640, #9981, #100052, #19723, #26220, #3499, #44495, #34833, #59079, #35903, #19192, #36438, #101123, #52032, #27818, #60687, #84943, #43424, #69308, #85484, #26744, #75782, #68779, #83336, #92490, #1875, #11032, #101660, #67702, #100584, #93575, #102183, #59620, #11564, #2417, #51500, #10510, #91966, #43949, #77383, #76841, #28332, #42348, #61208, #50426, #75235, #67171, #18095, #50956, #83870, #13155, #102721, #79499, #62802, #62282, #5610, #55211, #38535, #38022, #86031, #95689, #87609, #70357, #54141, #22365, #103253, #5089, #29399, #61754, #96235, #36955, #47122, #71941, #70881, #21304, #29915, #12625, #86565, #28884, #88136, #21833, #95171, #103775, #104296, #20798, #14218, #69823, #80019, #63341, #87081, #46084, #54672, #71397, #13690, #46602, #94652, #78965, #4557, #53630, #39061, #45562, #30447, #6130, #104845, #30986, #94098, #20262, #53108, #12103, #78431, #37494, #45033, #77918, #4027, #72466, #15824, #88657, #64395, #16351, #97269, #23415, #81082 ),
 .UNSPECIFIED., .F., .F.,
 ( 4, 1, 1, 1, 1, 1, 1, 1, 1, 2, 2, 1, 1, 1, 1, 1, 1, 2, 2, 1, 1, 1, 1, 1, 1, 1, 2, 2, 1, 1, 1, 1, 1, 1, 1, 2, 2, 1, 1, 1, 1, 1, 1, 1, 2, 2, 2, 1, 1, 1, 2, 2, 1, 1, 1, 1, 1, 2, 2, 1, 1, 1, 1, 1, 1, 1, 2, 2, 1, 1, 1, 1, 1, 1, 1, 2, 2, 1, 1, 1, 1, 1, 1, 1, 1, 2, 2, 1, 1, 1, 1, 1, 1, 1, 1, 1, 1, 2, 2, 1, 1, 1, 1, 1, 1, 1, 1, 1, 2, 2, 2, 1, 1, 1, 1, 1, 1, 1, 1, 2, 2, 1, 1, 1, 1, 1, 1, 1, 1, 1, 2, 2, 1, 1, 1, 1, 1, 1, 1, 1, 2, 2, 1, 1, 1, 1, 1, 1, 1, 1, 1, 2, 2, 1, 1, 1, 1, 1, 1, 1, 1, 1, 1, 2, 2, 1, 1, 1, 1, 1, 1, 1, 2, 2, 1, 1, 1, 1, 1, 1, 1, 2, 2, 1, 1, 1, 1, 1, 2, 2, 1, 1, 1, 2, 2, 1, 1, 1, 1, 2, 2, 1, 1, 1, 1, 1, 2, 2, 1, 1, 1, 2, 2, 1, 1, 1, 2, 2, 1, 1, 1, 1, 1, 2, 2, 1, 2, 2, 1, 1, 1, 1, 1, 2, 2, 1, 1, 1, 1, 1, 1, 1, 2, 2, 1, 1, 1, 1, 1, 1, 1, 1, 2, 2, 1, 1, 1, 1, 1, 1, 1, 1, 2, 2, 1, 1, 1, 1, 1, 1, 2, 2, 1, 1, 1, 1, 1, 1, 1, 1, 2, 2, 1, 1, 1, 1, 1, 1, 1, 2, 2, 1, 1, 1, 1, 1, 1, 2, 2, 1, 1, 1, 1, 1, 1, 1, 1, 2, 2, 1, 1, 1, 1, 1, 1, 2, 2, 1, 1, 1, 1, 1, 1, 1, 1, 2, 2, 1, 1, 1, 2, 2, 1, 1, 4 ),
 ( 0.000000000000000000, 0.007812499999918122787, 0.01171874999987713474, 0.01367187499985664072, 0.01464843749984634166, 0.01513671874984119300, 0.01538085937483866031, 0.01550292968733738355, 0.01556396484358680936, 0.01559448242171157170, 0.01562499999983633578, 0.02343749999978248996, 0.02734374999975560522, 0.02929687499974212295, 0.03027343749973534712, 0.03076171874973193318, 0.03100585937473019152, 0.03112792968722936579, 0.03124999999972853659, 0.03515624999970040632, 0.03710937499968632036, 0.03808593749967928432, 0.03857421874967577324, 0.03881835937467401770, 0.03894042968717313646, 0.03900146484342268544, 0.03903198242154746339, 0.03906249999967224135, 0.04296874999964340330, 0.04492187499962898428, 0.04589843749962177477, 0.04638671874961817349, 0.04663085937461636937, 0.04675292968711546732, 0.04681396484336501629, 0.04684448242148979424, 0.04687499999961456526, 0.05468749999955686836, 0.05859374999952800950, 0.06054687499951358354, 0.06152343749950636709, 0.06201171874950275886, 0.06225585937450096169, 0.06237792968700005963, 0.06243896484324961554, 0.06249999999949916452, 0.07031249999944196027, 0.07421874999941335815, 0.07617187499939906403, 0.07714843749939191697, 0.07763671874938833650, 0.07812499999938475603, 0.08593749999932762118, 0.08984374999929904682, 0.09179687499928476657, 0.09277343749927764727, 0.09326171874927406680, 0.09350585937427229044, 0.09374999999927050021, 0.1093749999991570909, 0.1171874999991003585, 0.1210937499990720062, 0.1230468749990578231, 0.1240234374990507316, 0.1245117187490471927, 0.1247558593740454302, 0.1248779296865445559, 0.1249999999990436816, 0.1406249999989302724, 0.1484374999988735677, 0.1523437499988452293, 0.1542968749988310739, 0.1552734374988239685, 0.1557617187488203880, 0.1560058593738185839, 0.1561279296863176957, 0.1562499999988168076, 0.1718749999987017885, 0.1796874999986442512, 0.1835937499986154964, 0.1855468749986011190, 0.1865234374985939025, 0.1870117187485903221, 0.1872558593735885457, 0.1873779296860876853, 0.1874389648423372412, 0.1874999999985867694, 0.2187499999983521515, 0.2343749999982348287, 0.2421874999981761811, 0.2460937499981468435, 0.2480468749981321608, 0.2490234374981249166, 0.2495117187481212251, 0.2497558593731193932, 0.2498779296856184773, 0.2499389648418680054, 0.2499694824199928389, 0.2499999999981176169, 0.2812499999979674037, 0.2968749999978922416, 0.3046874999978547160, 0.3085937499978359533, 0.3105468749978264609, 0.3115234374978217979, 0.3120117187478193554, 0.3122558593728181897, 0.3123779296853176346, 0.3124389648415674126, 0.3124999999978171350, 0.3437499999976899590, 0.3593749999976263987, 0.3671874999975946463, 0.3710937499975788256, 0.3730468749975709430, 0.3740234374975669462, 0.3745117187475650034, 0.3747558593725640597, 0.3748779296850636156, 0.3749389648413133380, 0.3749999999975630605, 0.4062499999974437670, 0.4218749999973840370, 0.4296874999973542830, 0.4335937499973393505, 0.4355468749973320230, 0.4365234374973284148, 0.4370117187473264719, 0.4372558593723253617, 0.4373779296848246956, 0.4374389648410741960, 0.4374999999973237519, 0.4531249999971969644, 0.4609374999971336817, 0.4648437499971019848, 0.4667968749970862197, 0.4677734374970783926, 0.4682617187470746178, 0.4685058593720728415, 0.4686279296845718423, 0.4686889648408214537, 0.4687499999970711206, 0.4843749999969746978, 0.4921874999969265141, 0.4960937499969023667, 0.4980468749968904874, 0.4990234374968843811, 0.4995117187468814390, 0.4997558593718801068, 0.4998779296843793296, 0.4999389648406289410, 0.4999694824187537190, 0.4999999999968784969, 0.5312499999966507902, 0.5468749999965369923, 0.5546874999964801489, 0.5585937499964518382, 0.5605468749964376274, 0.5615234374964305220, 0.5620117187464269692, 0.5622558593714250819, 0.5623779296839241937, 0.5624389648401738606, 0.5624694824182986386, 0.5624999999964234165, 0.5703124999963722352, 0.5742187499963464781, 0.5761718749963338215, 0.5771484374963274933, 0.5776367187463243846, 0.5778808593713228303, 0.5780029296838220532, 0.5780639648400717201, 0.5781249999963213870, 0.5820312499963147257, 0.5839843749963113950, 0.5849609374963098407, 0.5854492187463090636, 0.5856933593713085084, 0.5858154296838082864, 0.5858764648400581754, 0.5859069824181831754, 0.5859374999963080644, 0.5878906249962998487, 0.5888671874962957409, 0.5893554687462938535, 0.5895996093712928543, 0.5897216796837922992, 0.5897827148400422992, 0.5898437499962921882, 0.5908203124962911890, 0.5913085937462908559, 0.5915527343712906339, 0.5916748046837905228, 0.5917968749962905228, 0.5927734374962895236, 0.5932617187462891906, 0.5935058593712889685, 0.5936279296837888575, 0.5936889648400387465, 0.5937499999962886355, 0.5957031249962814190, 0.5966796874962778663, 0.5971679687462759789, 0.5974121093712749797, 0.5975341796837745356, 0.5975952148400242026, 0.5976562499962738695, 0.5996093749962628783, 0.6005859374962573272, 0.6010742187462545516, 0.6013183593712531083, 0.6015624999962516650, 0.6035156249962393415, 0.6044921874962332353, 0.6049804687462301267, 0.6052246093712285724, 0.6054687499962270181, 0.6074218749962153607, 0.6083984374962094765, 0.6088867187462065900, 0.6091308593712051467, 0.6092529296837044805, 0.6093139648399541475, 0.6093749999962038144, 0.6113281249961912689, 0.6123046874961850516, 0.6132812499961787234, 0.6152343749961661779, 0.6162109374961598496, 0.6166992187461567410, 0.6169433593711552977, 0.6170654296836544095, 0.6171264648399039654, 0.6171874999961536323, 0.6210937499961349806, 0.6230468749961256547, 0.6240234374961208808, 0.6245117187461185493, 0.6247558593711173280, 0.6248779296836167729, 0.6249389648398665509, 0.6249694824179915509, 0.6249999999961165509, 0.6328124999961596275, 0.6367187499961810548, 0.6386718749961918240, 0.6396484374961970421, 0.6401367187461998176, 0.6403808593712011499, 0.6405029296837018160, 0.6405639648399520381, 0.6405944824180771491, 0.6406249999962022601, 0.6484374999962930763, 0.6523437499963383734, 0.6542968749963610220, 0.6552734374963723463, 0.6557617187463781194, 0.6560058593713808950, 0.6561279296838822273, 0.6561889648401328934, 0.6562194824182582265, 0.6562499999963835595, 0.6640624999964694908, 0.6679687499965123454, 0.6699218749965338837, 0.6708984374965446529, 0.6713867187465498709, 0.6716308593715525355, 0.6717529296840539788, 0.6718749999965553110, 0.6796874999966473485, 0.6835937499966934228, 0.6855468749967164044, 0.6865234374967280617, 0.6870117187467337239, 0.6872558593717364994, 0.6873779296842381648, 0.6874389648404887199, 0.6874694824186140529, 0.6874999999967393860, 0.7031249999969233500, 0.7109374999970154985, 0.7148437499970615727, 0.7167968749970846654, 0.7177734374970963227, 0.7182617187471022069, 0.7185058593721050935, 0.7186279296846065368, 0.7187499999971078690, 0.7343749999972727371, 0.7421874999973553377, 0.7460937499973965270, 0.7480468749974170661, 0.7490234374974272802, 0.7495117187474323872, 0.7497558593724349407, 0.7499999999974373832, 0.8124999999980522247, 0.8437499999983595345, 0.8593749999985131893, 0.8671874999985900168, 0.8710937499986284305, 0.8730468749986476373, 0.8740234374986571853, 0.8745117187486619592, 0.8747558593736642907, 0.8749999999986666221, 0.8906249999988182786, 0.8984374999988939958, 0.9023437499989319655, 0.9042968749989508392, 0.9052734374989602761, 0.9057617187489650501, 0.9060058593739673816, 0.9062499999989697130, 0.9218749999991281419, 0.9296874999992073008, 0.9335937499992469357, 0.9355468749992666977, 0.9365234374992766897, 0.9370117187492815747, 0.9372558593742840172, 0.9373779296867852384, 0.9374389648430360156, 0.9374999999992866817, 0.9531249999994668709, 0.9609374999995567990, 0.9619140624995680122, 0.9624023437495735633, 0.9628906249995791145, 0.9648437499996014299, 0.9687499999996457278, 1.000000000000000000 ),
 .UNSPECIFIED. ) ;
#100335=CARTESIAN_POINT ( 'NONE',  ( -102.4273698138863722, -60.00000000000000000, 95.23766053874160775 ) ) ;
#100343=CARTESIAN_POINT ( 'NONE',  ( -81.29675584934015831, -56.99031933536476657, 180.9625569273741519 ) ) ;
#100357=FILL_AREA_STYLE ('',( #10803 ) ) ;
#100359=CARTESIAN_POINT ( 'NONE',  ( 103.3501304845727873, -29.99999999999998579, 116.5671668536019610 ) ) ;
#100361=CARTESIAN_POINT ( 'NONE',  ( -76.30486425386099825, -30.00000000000004619, 168.5691345232379206 ) ) ;
#100362=CARTESIAN_POINT ( 'NONE',  ( -58.13295120765930335, -25.60580355849098311, 61.38901395099644986 ) ) ;
#100364=CARTESIAN_POINT ( 'NONE',  ( 93.82195685172136734, -59.99999999999752731, -16.20128001769883497 ) ) ;
#100366=CARTESIAN_POINT ( 'NONE',  ( 7.105781327744331577, -35.99149389464556492, 29.87857778648328733 ) ) ;
#100367=CARTESIAN_POINT ( 'NONE',  ( -102.7248202937925612, -52.71211498143689766, 190.6735650292727087 ) ) ;
#100368=PLANE ( 'NONE',  #36912 ) ;
#100374=CARTESIAN_POINT ( 'NONE',  ( -77.82043145825072372, -60.00000000000001421, 192.4616265064402114 ) ) ;
#100387=CARTESIAN_POINT ( 'NONE',  ( -31.02242612524658938, -39.49085496570000942, 33.50213709495920966 ) ) ;
#100390=CARTESIAN_POINT ( 'NONE',  ( 46.23384880443906297, -29.15623005253502598, 42.24550313519566203 ) ) ;
#100394=CARTESIAN_POINT ( 'NONE',  ( -78.26226481065664586, -38.60566898501981825, 189.0129437702546511 ) ) ;
#100398=CARTESIAN_POINT ( 'NONE',  ( 23.93832669066742724, -60.00000000000001421, 35.01784081144786853 ) ) ;
#100405=DIRECTION ( 'NONE',  ( 0.000000000000000000, -0.000000000000000000, 1.000000000000000000 ) ) ;
#100406=CARTESIAN_POINT ( 'NONE',  ( 106.3883173979913437, -60.00000000000000711, 118.8213136657173266 ) ) ;
#100410=CARTESIAN_POINT ( 'NONE',  ( -53.08935917470201815, -30.00000000000000000, 52.21147893555080799 ) ) ;
#100413=CARTESIAN_POINT ( 'NONE',  ( -99.23654757740681021, -30.00000000000000711, 188.2532938818355319 ) ) ;
#100424=CARTESIAN_POINT ( 'NONE',  ( 82.17599174339494539, -39.49534644509261483, 162.1453621538301775 ) ) ;
#100445=CARTESIAN_POINT ( 'NONE',  ( 86.86885569288263298, -50.10510242869298736, 191.7877947622934585 ) ) ;
#100448=DIRECTION ( 'NONE',  ( -1.000000000000000000, -0.000000000000000000, -0.000000000000000000 ) ) ;
#100466=CARTESIAN_POINT ( 'NONE',  ( -91.39810932065459781, -60.00000000000001421, 202.2552732027076274 ) ) ;
#100470=CARTESIAN_POINT ( 'NONE',  ( -85.72996169165566016, -28.54324383439242752, 179.8132596535202197 ) ) ;
#100477=CARTESIAN_POINT ( 'NONE',  ( -86.87225386170726438, -60.16560806864642075, -2.785716167088986506 ) ) ;
#100485=CARTESIAN_POINT ( 'NONE',  ( 52.32017852953563164, -14.21045842199431242, 63.23906622249963760 ) ) ;
#100487=CARTESIAN_POINT ( 'NONE',  ( -93.17098673813583787, -59.99999999999997158, -17.95829132299026298 ) ) ;
#100488=CARTESIAN_POINT ( 'NONE',  ( -75.97434538570179541, -29.07737278147254756, 117.1882777120721073 ) ) ;
#100489=B_SPLINE_CURVE_WITH_KNOTS ( 'NONE', 3,
 ( #29386, #77370, #19182, #94637, #103241, #93019, #52020, #3486, #36942, #27806, #13141, #11020, #102705, #43938, #37481, #35890, #36426, #76827, #68768, #93563, #62272, #20248, #4540, #19710, #28318, #70344, #45547, #12089, #53096, #21289, #101649, #69295, #102169, #77904, #52547, #61195, #60676, #69809, #95157, #45022, #4012, #85469, #87068, #46070, #78953, #28870, #94085, #86018, #20783, #35350, #53618, #86553, #68216, #21819, #71383, #97258, #31501, #6653, #54657, #5597, #89713, #63325, #89180, #88124, #15812, #6117, #32019, #56243, #15281, #23948, #14204, #39043, #72454, #23401, #64896, #40093, #105362, #38520, #47106, #104283, #7179, #48166, #87593, #30973, #13678, #81067, #72968, #30432, #71928, #39580, #104829, #105876, #97782, #56788, #63854, #96220, #80008, #64381, #22351, #96745, #46588, #48693, #5075, #22878, #38010, #70872, #103764, #79487, #29901, #55713 ),
 .UNSPECIFIED., .F., .F.,
 ( 4, 2, 2, 1, 1, 1, 1, 2, 2, 1, 2, 2, 1, 1, 1, 2, 2, 1, 2, 2, 1, 1, 1, 2, 2, 1, 2, 2, 1, 1, 1, 2, 2, 1, 2, 2, 1, 1, 2, 2, 1, 2, 2, 1, 2, 2, 1, 2, 2, 1, 1, 2, 2, 1, 2, 2, 2, 1, 1, 2, 2, 1, 1, 2, 2, 2, 2, 1, 2, 4 ),
 ( 0.000000000000000000, 0.01574254035199997015, 0.02361381052799983032, 0.02754944561599962510, 0.02951726315999962311, 0.03050117193199966895, 0.03099312631799969187, 0.03123910351099974669, 0.03136209210749976717, 0.03148508070399978764, 0.04722762105598653920, 0.05509889123197986988, 0.05903452631997656297, 0.06100234386397482278, 0.06198625263597389717, 0.06247820702197335457, 0.06272418421497306940, 0.06297016140797279116, 0.09445524211193562225, 0.1101977824639170656, 0.1180690526399078705, 0.1220046877279032521, 0.1239725052719010123, 0.1249564140438999132, 0.1254483684298993706, 0.1259403228158987864, 0.1574254035198680290, 0.1731679438718526365, 0.1810392140478448708, 0.1849748491358410019, 0.1869426666798391368, 0.1874346210658384970, 0.1879265754518378295, 0.1889104842238366333, 0.2203955649278004358, 0.2361381052797823232, 0.2440093754557732808, 0.2479450105437687457, 0.2499128280877664643, 0.2508967368597653236, 0.2518806456317641551, 0.2833657263357283740, 0.2991082666877105667, 0.3069795368637016075, 0.3109151719516971002, 0.3128829894956948743, 0.3148508070396926484, 0.3463358877436555350, 0.3620784280956369505, 0.3699496982716277138, 0.3738853333596230399, 0.3748692421316219270, 0.3753611965176212872, 0.3758531509036206475, 0.3778209684476182550, 0.4093060491515793098, 0.4250485895035597816, 0.4329198596795500453, 0.4368554947675451494, 0.4373474491535445652, 0.4378394035395440365, 0.4388233123115429235, 0.4407911298555406421, 0.4565336702075227238, 0.4644049403835138201, 0.4683405754715093128, 0.4703083930155070869, 0.4722762105595048610, 0.4880187509114868871, 0.5037612912634689133 ),
 .UNSPECIFIED. ) ;
#100491=CARTESIAN_POINT ( 'NONE',  ( 70.80389978121282013, -30.00000000000000711, 131.5992258684728995 ) ) ;
#100492=CARTESIAN_POINT ( 'NONE',  ( 15.48885350034982089, -60.00000000000000000, 42.17456718879848410 ) ) ;
#100515=CARTESIAN_POINT ( 'NONE',  ( 31.81754536830298008, -42.95997511258514834, 34.45836456846625850 ) ) ;
#100528=CARTESIAN_POINT ( 'NONE',  ( 80.69099499396966735, -59.99999999999997868, -27.52696420757851214 ) ) ;
#100540=CARTESIAN_POINT ( 'NONE',  ( 10.00000000000000000, -15.00000000000000000, 10.00000000000000178 ) ) ;
#100541=CARTESIAN_POINT ( 'NONE',  ( 83.23442963069594214, -37.80756990166215559, -8.243152359157335241 ) ) ;
#100554=CARTESIAN_POINT ( 'NONE',  ( 74.82255457991739434, -42.96157133918497095, 122.4742354992479108 ) ) ;
#100562=CARTESIAN_POINT ( 'NONE',  ( -96.68549010014578471, -57.67144976548149771, 46.95518404347522079 ) ) ;
#100566=CARTESIAN_POINT ( 'NONE',  ( 104.8217955542264548, -52.71705407144827404, 181.7153123444907692 ) ) ;
#100570=CARTESIAN_POINT ( 'NONE',  ( -81.98196232622828461, -37.99999999999996447, -13.86369433938586582 ) ) ;
#100584=CARTESIAN_POINT ( 'NONE',  ( -85.49552939016024311, -30.00000000000000000, 174.7863823751660846 ) ) ;
#100588=CARTESIAN_POINT ( 'NONE',  ( 70.14605380316399419, -57.68253419882464073, 155.2985699437752771 ) ) ;
#100592=CARTESIAN_POINT ( 'NONE',  ( 29.61882069994729960, -29.43158534365355550, -38.19371325218018853 ) ) ;
#100595=CARTESIAN_POINT ( 'NONE',  ( -37.39234250541336024, -60.00000000000002132, 48.78642601381413613 ) ) ;
#100599=CARTESIAN_POINT ( 'NONE',  ( -86.76683669320412662, -35.44260230858979099, 187.6259941901972752 ) ) ;
#100602=CARTESIAN_POINT ( 'NONE',  ( -4.032884956273577792, -35.99424295969529197, 29.88149843471951073 ) ) ;
#100614=SURFACE_STYLE_FILL_AREA ( #83900 ) ;
#100616=CARTESIAN_POINT ( 'NONE',  ( 114.4011996162234510, -59.99999999999997158, 179.2244502532067827 ) ) ;
#100617=CARTESIAN_POINT ( 'NONE',  ( -80.62560537530049487, -46.44214533936248301, 158.8984127742610895 ) ) ;
#100622=CARTESIAN_POINT ( 'NONE',  ( 24.28208867544860183, -57.67420315891946103, 43.01449209020211839 ) ) ;
#100639=CARTESIAN_POINT ( 'NONE',  ( 98.70648322990193435, -59.99999999999998579, 202.2230572402837367 ) ) ;
#100640=CARTESIAN_POINT ( 'NONE',  ( -88.35884389454342625, -14.21045842199434794, 197.0605769606054594 ) ) ;
#100641=CARTESIAN_POINT ( 'NONE',  ( 24.11997513724847408, -53.39263269948676083, 33.93311544977419913 ) ) ;
#100644=EDGE_CURVE ( 'NONE', #16368, #40837, #99842, .T. ) ;
#100645=CARTESIAN_POINT ( 'NONE',  ( -43.76208095016959732, -32.61856360751036021, 40.47694461062264537 ) ) ;
#100657=CARTESIAN_POINT ( 'NONE',  ( 76.63262662268121517, -30.00000000002306422, 171.6915798261921395 ) ) ;
#100661=CARTESIAN_POINT ( 'NONE',  ( 84.07723708129948648, -30.00000000000000000, 51.17427913239208692 ) ) ;
#100678=CARTESIAN_POINT ( 'NONE',  ( 76.58278636061123734, -38.42162667129784381, 182.2336444325641480 ) ) ;
#100689=CARTESIAN_POINT ( 'NONE',  ( 9.118906730430985774E-15, 30.00000000000000000, -74.46152422706630603 ) ) ;
#100696=CARTESIAN_POINT ( 'NONE',  ( 84.81970466459384284, -50.19123916470319813, 188.8545982504039102 ) ) ;
#100703=CARTESIAN_POINT ( 'NONE',  ( -72.50181434431193850, -38.00000000001091394, -21.26203725901419261 ) ) ;
#100707=CARTESIAN_POINT ( 'NONE',  ( -90.16919950005070916, -30.00000000000000000, 89.48266059237039372 ) ) ;
#100723=CARTESIAN_POINT ( 'NONE',  ( 40.40045996829983466, -24.98508198468909924, -30.21120896785051002 ) ) ;
#100724=CARTESIAN_POINT ( 'NONE',  ( -26.43713145984708746, -32.52648158339238904, 30.88029666580395727 ) ) ;
#100729=CARTESIAN_POINT ( 'NONE',  ( -17.02355309802323191, -53.40205467437851894, 33.05030794773703207 ) ) ;
#100730=CARTESIAN_POINT ( 'NONE',  ( -63.60144037357603963, -29.63473796242592684, -23.63298369914019759 ) ) ;
#100733=CARTESIAN_POINT ( 'NONE',  ( -69.08272651081071558, -34.58952494725262738, -22.16738816901018438 ) ) ;
#100742=CARTESIAN_POINT ( 'NONE',  ( 98.76119375271832723, -37.78714592256793736, 192.0742751786086160 ) ) ;
#100755=CARTESIAN_POINT ( 'NONE',  ( -94.23463998755006799, -59.99999999999511147, 9.458815458491475425 ) ) ;
#100759=AXIS2_PLACEMENT_3D ( 'NONE', #5814, #30117, #47331 ) ;
#100760=CARTESIAN_POINT ( 'NONE',  ( -90.56108803656626094, -30.00000000000000711, 34.47189148671483849 ) ) ;
#100764=CARTESIAN_POINT ( 'NONE',  ( -50.29965373618113489, -36.05105100340624347, 50.07322630481903758 ) ) ;
#100776=CARTESIAN_POINT ( 'NONE',  ( 94.50952691389738902, -38.49070133904758251, 201.2196195639374707 ) ) ;
#100781=CARTESIAN_POINT ( 'NONE',  ( 94.51288522389913282, -30.00000000000000711, 191.3190572542347354 ) ) ;
#100786=ORIENTED_EDGE ( 'NONE', *, *, #50996, .T. ) ;
#100787=CARTESIAN_POINT ( 'NONE',  ( 50.73443445076901526, -60.29831178159185612, 59.32218280885512485 ) ) ;
#100792=CARTESIAN_POINT ( 'NONE',  ( -91.44668068905532721, -38.39006247391498050, -8.007462388528333364 ) ) ;
#100795=CARTESIAN_POINT ( 'NONE',  ( 106.9049990251340034, -38.36531872114127140, 195.0069650757791067 ) ) ;
#100797=CARTESIAN_POINT ( 'NONE',  ( 88.36089431529551064, -37.84864422464463019, 68.44789249334731096 ) ) ;
#100815=CARTESIAN_POINT ( 'NONE',  ( 43.34664592991014587, -27.69598330275180231, 38.46056262246474944 ) ) ;
#100818=CARTESIAN_POINT ( 'NONE',  ( 82.22591555319118584, -60.76466039185579859, 188.6612029719528039 ) ) ;
#100823=CARTESIAN_POINT ( 'NONE',  ( -98.38802680873801876, -45.26535420428151468, 120.6788969241506209 ) ) ;
#100827=CARTESIAN_POINT ( 'NONE',  ( -27.61666142601160701, -28.69133200283256713, -38.28075806456551788 ) ) ;
#100831=CARTESIAN_POINT ( 'NONE',  ( 50.67286391799485301, -60.00000000000000000, 73.50007806226966522 ) ) ;
#100833=CARTESIAN_POINT ( 'NONE',  ( 24.28708600688997166, -28.55405093416178630, 38.02957352212126096 ) ) ;
#100835=CARTESIAN_POINT ( 'NONE',  ( 27.01661562657338678, -20.25300179656017008, 31.73816561356836274 ) ) ;
#100837=CARTESIAN_POINT ( 'NONE',  ( -42.01420664154974105, -38.13943564830498190, 52.75245923061931563 ) ) ;
#100857=CARTESIAN_POINT ( 'NONE',  ( 15.57243583339607618, -21.77026072153822156, -30.00009859734665696 ) ) ;
#100865=CARTESIAN_POINT ( 'NONE',  ( -91.97968714158955095, -60.00000000000003553, 6.646224270140889345 ) ) ;
#100871=CARTESIAN_POINT ( 'NONE',  ( -83.89944615507195635, -35.96775995157042871, 172.8053575196213671 ) ) ;
#100887=CARTESIAN_POINT ( 'NONE',  ( 96.14436826854903018, -60.00000000000009237, 39.43554979140174765 ) ) ;
#100889=CARTESIAN_POINT ( 'NONE',  ( -92.04690998902847809, -60.00000000000008527, 204.8849370891594219 ) ) ;
#100890=CARTESIAN_POINT ( 'NONE',  ( -56.33823149440868150, -60.33114724083395686, 72.31374845339159663 ) ) ;
#100893=CARTESIAN_POINT ( 'NONE',  ( -103.5943349152434791, -45.26536037131153023, 181.5148655901820973 ) ) ;
#100900=CARTESIAN_POINT ( 'NONE',  ( -82.28682622294347482, -60.00000000000002132, 198.2874724176148789 ) ) ;
#100914=CARTESIAN_POINT ( 'NONE',  ( -32.34892057383476072, -53.37767965076007215, 36.58595348072790188 ) ) ;
#100918=CARTESIAN_POINT ( 'NONE',  ( 44.50089742215685362, -25.70400728066517715, 39.42175729867503264 ) ) ;
#100923=CARTESIAN_POINT ( 'NONE',  ( -94.07850901117426190, -38.49210041709851282, 201.1960849539863432 ) ) ;
#100928=CARTESIAN_POINT ( 'NONE',  ( 58.87759684000966587, -59.99999999999999289, 78.92660630072694516 ) ) ;
#100938=CARTESIAN_POINT ( 'NONE',  ( 112.1232886518557308, -60.00000000000000000, 177.4603685517026577 ) ) ;
#100944=CARTESIAN_POINT ( 'NONE',  ( -80.84769301060788393, -30.00000000000003197, -12.29708576950179655 ) ) ;
#100946=CARTESIAN_POINT ( 'NONE',  ( -54.59759563194740650, -38.34127430065652931, 80.36034406101917682 ) ) ;
#100956=CARTESIAN_POINT ( 'NONE',  ( 81.09842540489270846, -46.43962613874821699, 163.0359359564797046 ) ) ;
#100974=CARTESIAN_POINT ( 'NONE',  ( 86.53796551356465727, -57.40570272851905997, 193.5699017834150197 ) ) ;
#100975=EDGE_CURVE ( 'NONE', #30000, #44460, #102377, .T. ) ;
#101000=CARTESIAN_POINT ( 'NONE',  ( -77.61630265161984710, -60.00000000000000711, 192.0045729689810514 ) ) ;
#101004=CARTESIAN_POINT ( 'NONE',  ( -83.43097235363796926, -53.72644085999411345, 187.4685730767253915 ) ) ;
#101011=CARTESIAN_POINT ( 'NONE',  ( -82.48223426280006265, -37.83324084028321010, 8.085024656640488416 ) ) ;
#101019=CARTESIAN_POINT ( 'NONE',  ( 64.23331706704713895, -60.00000000000004263, 125.0204823638418361 ) ) ;
#101022=CARTESIAN_POINT ( 'NONE',  ( -72.33650272884364085, -14.21045842199437992, -25.95337777301578797 ) ) ;
#101023=CARTESIAN_POINT ( 'NONE',  ( -68.05384738583532567, -46.43832317692169909, 99.56375534947220274 ) ) ;
#101025=CARTESIAN_POINT ( 'NONE',  ( 68.63284294399571195, -59.99999999999999289, 147.4025539660169954 ) ) ;
#101027=CARTESIAN_POINT ( 'NONE',  ( 23.54848554166952823, -59.99999999999506173, 43.23155359999935143 ) ) ;
#101037=CARTESIAN_POINT ( 'NONE',  ( -71.30636318066278534, -59.99999999991200639, 168.8601541835865305 ) ) ;
#101051=CARTESIAN_POINT ( 'NONE',  ( 32.25262845956538627, -39.49034541401320553, 34.00867910329044719 ) ) ;
#101052=CARTESIAN_POINT ( 'NONE',  ( 2.723397405354400211E-15, -8.673617379884035472E-16, 22.23822744035697241 ) ) ;
#101055=EDGE_LOOP ( 'NONE', ( #6527, #87280, #29235, #52153 ) ) ;
#101064=CARTESIAN_POINT ( 'NONE',  ( 73.19133291941243158, -60.00000000000002842, -31.37687942255105966 ) ) ;
#101072=CARTESIAN_POINT ( 'NONE',  ( -97.92030896840019238, -29.99999999999134914, 199.6821230727564114 ) ) ;
#101080=CARTESIAN_POINT ( 'NONE',  ( 85.63808483343134981, -52.75639776242220336, -9.610134456905338851 ) ) ;
#101090=FILL_AREA_STYLE ('',( #43393 ) ) ;
#101095=CARTESIAN_POINT ( 'NONE',  ( 75.17581571613058600, -49.90415678964559731, 129.2185576746167897 ) ) ;
#101102=CARTESIAN_POINT ( 'NONE',  ( -93.89056551065039002, -57.67583025180931600, 8.072597750090290347 ) ) ;
#101106=CARTESIAN_POINT ( 'NONE',  ( 105.1873821515111018, -60.15126481720113816, 187.0774076014252785 ) ) ;
#101123=CARTESIAN_POINT ( 'NONE',  ( -86.49196759552401659, -29.99999999999999289, 181.4671144795470639 ) ) ;
#101127=CARTESIAN_POINT ( 'NONE',  ( 83.50137569068580490, -57.54076335939706155, 201.4680290845222999 ) ) ;
#101131=CARTESIAN_POINT ( 'NONE',  ( 70.17982293570671004, -38.22781381422611702, -31.10776116069777331 ) ) ;
#101134=CARTESIAN_POINT ( 'NONE',  ( -39.40759530360957541, -59.99999999999999289, 51.27385300903834775 ) ) ;
#101139=CARTESIAN_POINT ( 'NONE',  ( -85.78283469545968387, -57.45526895688682600, 192.9326975944933054 ) ) ;
#101142=CARTESIAN_POINT ( 'NONE',  ( -1.987691155308321189, -25.54942359938841889, 28.14570803181489822 ) ) ;
#101156=EDGE_CURVE ( 'NONE', #31749, #90543, #41588, .T. ) ;
#101157=CARTESIAN_POINT ( 'NONE',  ( 90.94603201905546541, -14.21045842199432663, 57.96280492189741551 ) ) ;
#101158=CARTESIAN_POINT ( 'NONE',  ( -81.28725701646312984, -36.03165964993199566, 150.3997114263125070 ) ) ;
#101160=DIRECTION ( 'NONE',  ( 0.000000000000000000, -1.000000000000000000, 0.000000000000000000 ) ) ;
#101184=CARTESIAN_POINT ( 'NONE',  ( -92.04690998902847809, -60.00000000000008527, 204.8849370891594219 ) ) ;
#101185=CARTESIAN_POINT ( 'NONE',  ( 20.76647212221055483, -18.59340802667270864, 27.55324192485566570 ) ) ;
#101188=CARTESIAN_POINT ( 'NONE',  ( -35.05813823911775984, -46.43391309501947717, 36.68683573906173478 ) ) ;
#101202=CARTESIAN_POINT ( 'NONE',  ( 98.58235770902466300, -29.99999999999995737, 189.7049926379953888 ) ) ;
#101207=CARTESIAN_POINT ( 'NONE',  ( 81.06425680110626786, -30.00000000000000000, 22.12711938399802847 ) ) ;
#101226=CARTESIAN_POINT ( 'NONE',  ( 75.26362525057788844, -38.34453862111913480, 172.0622010566955851 ) ) ;
#101232=AXIS2_PLACEMENT_3D ( 'NONE', #19179, #67153, #28314 ) ;
#101253=CARTESIAN_POINT ( 'NONE',  ( 86.57521083124422034, -42.81237575202452916, 189.2799081440977602 ) ) ;
#101257=CARTESIAN_POINT ( 'NONE',  ( 69.25544739171029107, -57.67106767548779089, -34.92408972481134555 ) ) ;
#101261=CARTESIAN_POINT ( 'NONE',  ( -88.91012085090163453, -30.00000000000000355, 82.06472925106058369 ) ) ;
#101274=CARTESIAN_POINT ( 'NONE',  ( 61.09210413872295931, -29.38834330421657270, -24.58964298202642595 ) ) ;
#101276=CARTESIAN_POINT ( 'NONE',  ( -25.97158367243803667, -36.00318411789499606, 31.37728892077313603 ) ) ;
#101280=CARTESIAN_POINT ( 'NONE',  ( -16.63618056918942045, -32.51365049520764217, 29.53634284231671714 ) ) ;
#101294=CARTESIAN_POINT ( 'NONE',  ( 100.9578779286414800, -52.74261186640906374, 193.4183224279464071 ) ) ;
#101309=CARTESIAN_POINT ( 'NONE',  ( -83.96692933907711165, -60.00000000000971312, -28.23229891493929600 ) ) ;
#101315=CARTESIAN_POINT ( 'NONE',  ( -87.76943268072510307, -14.21045842199432307, -6.547605000374890238 ) ) ;
#101317=CARTESIAN_POINT ( 'NONE',  ( -50.52341832492433582, -25.65870449059931957, 46.96528990739796683 ) ) ;
#101326=CARTESIAN_POINT ( 'NONE',  ( 109.5798523967376497, -30.00000000001343992, 175.3446974936682068 ) ) ;
#101331=CARTESIAN_POINT ( 'NONE',  ( 87.06498138213956395, -30.00000000000000355, 183.9578833979254568 ) ) ;
#101337=CARTESIAN_POINT ( 'NONE',  ( 51.03706583455220880, -49.90368789440714892, 56.18858338209947334 ) ) ;
#101338=LINE ( 'NONE', #77053, #38732 ) ;
#101342=CARTESIAN_POINT ( 'NONE',  ( -90.37755454089685259, -38.40153146471335788, -14.95169647791086653 ) ) ;
#101345=CARTESIAN_POINT ( 'NONE',  ( 108.2541020591300907, -38.35772930560278127, 192.2632853830203032 ) ) ;
#101347=CARTESIAN_POINT ( 'NONE',  ( 83.25917025631360957, -37.85102771844027814, 29.52673368758545536 ) ) ;
#101349=FILL_AREA_STYLE ('',( #35049 ) ) ;
#101363=CARTESIAN_POINT ( 'NONE',  ( 1.666670260708756013, -30.00000000000001066, 28.88807923168612746 ) ) ;
#101366=CARTESIAN_POINT ( 'NONE',  ( -52.00049474763441992, -30.00000000000002132, 50.03028121960383601 ) ) ;
#101371=CARTESIAN_POINT ( 'NONE',  ( 84.21780330469050568, -46.56204000551604594, 185.3552051814339166 ) ) ;
#101375=CARTESIAN_POINT ( 'NONE',  ( -85.41117724271114753, -45.26541568431846230, 38.51296887745267128 ) ) ;
#101379=CARTESIAN_POINT ( 'NONE',  ( -14.01098147192283783, -23.76418724810895000, -38.53464035791351705 ) ) ;
#101381=CARTESIAN_POINT ( 'NONE',  ( 50.69148081940352313, -60.00000000000004263, 73.54746023732971594 ) ) ;
#101383=CARTESIAN_POINT ( 'NONE',  ( 29.74370370787013584, -32.27977560020801207, 40.42837052529171871 ) ) ;
#101386=CARTESIAN_POINT ( 'NONE',  ( 10.53029844143175531, -13.89981288703387641, 31.86682902241898319 ) ) ;
#101389=CARTESIAN_POINT ( 'NONE',  ( -2.499999999999996447, -17.75175104828353057, -25.82778608236962015 ) ) ;
#101403=CARTESIAN_POINT ( 'NONE',  ( 25.91305494270541843, -60.22838175289183482, -35.60186180949625623 ) ) ;
#101416=CARTESIAN_POINT ( 'NONE',  ( -94.39869318582654500, -60.00000000000000711, 44.50543556059614048 ) ) ;
#101423=CARTESIAN_POINT ( 'NONE',  ( -82.21114147848552989, -49.99081894097567158, 178.5515362787500635 ) ) ;
#101432=CARTESIAN_POINT ( 'NONE',  ( -113.9602498558271719, -57.67115345197749576, 163.9892394128282262 ) ) ;
#101438=CARTESIAN_POINT ( 'NONE',  ( 95.66379843407523254, -59.99999999999997158, 35.18487050012404893 ) ) ;
#101439=CARTESIAN_POINT ( 'NONE',  ( -82.63253876390992048, -60.00000000000011369, 201.7050754921980911 ) ) ;
#101440=CARTESIAN_POINT ( 'NONE',  ( -59.77475626106946294, -39.49178998087817405, 71.62854156836660025 ) ) ;
#101444=CARTESIAN_POINT ( 'NONE',  ( -104.7020446980512958, -52.71019846712929535, 182.7859787390149222 ) ) ;
#101451=CARTESIAN_POINT ( 'NONE',  ( -40.66005888438434823, -59.99999999999998579, 53.02551035700262361 ) ) ;
#101456=CARTESIAN_POINT ( 'NONE',  ( 2.220657265734799157, -0.000000000000000000, -16.90652009647985565 ) ) ;
#101462=CARTESIAN_POINT ( 'NONE',  ( -30.90958803885418504, -25.60400391790700425, 30.93804380000945287 ) ) ;
#101464=CARTESIAN_POINT ( 'NONE',  ( 44.68940265413235835, -36.07226461998735090, 42.37193160774957335 ) ) ;
#101468=CARTESIAN_POINT ( 'NONE',  ( -89.65333812297674854, -38.52081078200126285, 200.4790887592579054 ) ) ;
#101472=CARTESIAN_POINT ( 'NONE',  ( 14.61174433364459802, -59.99999999999999289, 34.00541122474304245 ) ) ;
#101480=CARTESIAN_POINT ( 'NONE',  ( 112.1766375600363403, -60.00000000000000711, 169.0515973596464221 ) ) ;
#101487=CARTESIAN_POINT ( 'NONE',  ( -88.84843115600412489, -30.00000000000000711, 82.20554073122355021 ) ) ;
#101489=CARTESIAN_POINT ( 'NONE',  ( -79.70867639164802654, -38.76023424625122260, 192.4775466185992627 ) ) ;
#101498=AXIS2_PLACEMENT_3D ( 'NONE', #18147, #52607, #26267 ) ;
#101500=CARTESIAN_POINT ( 'NONE',  ( 84.80004317470192632, -22.09711215687178765, 158.8498095341223859 ) ) ;
#101513=CARTESIAN_POINT ( 'NONE',  ( 87.03219043533479748, -39.08529333260427308, 189.1299867071195422 ) ) ;
#101540=CARTESIAN_POINT ( 'NONE',  ( -102.3495297225788931, -60.00000000000001421, 200.9636531052911721 ) ) ;
#101546=CARTESIAN_POINT ( 'NONE',  ( -83.34365347161629245, -57.34364429206465275, 189.3595448663711807 ) ) ;
#101551=CARTESIAN_POINT ( 'NONE',  ( -86.30673588546420660, -60.13456697820941343, 5.314161181627422792 ) ) ;
#101558=CARTESIAN_POINT ( 'NONE',  ( 74.04755006654457361, -14.21045842199432307, 133.5027151116648838 ) ) ;
#101561=CARTESIAN_POINT ( 'NONE',  ( -95.18184656059791848, -59.99999999999997158, -7.511930356246473650 ) ) ;
#101562=CARTESIAN_POINT ( 'NONE',  ( -75.68663096329835582, -32.54935148169148817, 118.5104710783690791 ) ) ;
#101564=CARTESIAN_POINT ( 'NONE',  ( 83.90815637317848541, -29.99999999999993605, 196.6622986253035208 ) ) ;
#101566=CARTESIAN_POINT ( 'NONE',  ( 36.29725819348360716, -57.67119622293918013, -42.14310373887633432 ) ) ;
#101577=CARTESIAN_POINT ( 'NONE',  ( -74.75441323975938701, -60.00000000000489564, 191.7171422206980367 ) ) ;
#101580=CARTESIAN_POINT ( 'NONE',  ( 80.00000000000000000, -60.00000000000000000, -21.09707704303352926 ) ) ;
#101581=CARTESIAN_POINT ( 'NONE',  ( 1.544427540536530710E-15, -4.285714285714290916, -25.22241582816893057 ) ) ;
#101592=CARTESIAN_POINT ( 'NONE',  ( 33.33570294487471841, -60.30676322309119541, 38.33902022564197409 ) ) ;
#101593=CARTESIAN_POINT ( 'NONE',  ( -12.70248734011669356, -4.285714285715063632, 22.03900363279318597 ) ) ;
#101607=CARTESIAN_POINT ( 'NONE',  ( 92.02827674427864224, -60.00000000000000000, 5.649209357253974773 ) ) ;
#101615=CARTESIAN_POINT ( 'NONE',  ( -109.4266139821181838, -29.99999999998669153, 164.9709206702354152 ) ) ;
#101621=CARTESIAN_POINT ( 'NONE',  ( 85.03385216039647787, -52.75405561412956246, -12.86923322555876581 ) ) ;
#101630=PRESENTATION_STYLE_ASSIGNMENT (( #92999 ) ) ;
#101634=CARTESIAN_POINT ( 'NONE',  ( 75.82183472299138316, -60.31256542882874072, 141.6087927635422830 ) ) ;
#101639=CARTESIAN_POINT ( 'NONE',  ( -72.53004918620850106, -57.66488672193313647, 177.2532351053191348 ) ) ;
#101643=CARTESIAN_POINT ( 'NONE',  ( 104.0197026221604659, -45.28274691081462322, 170.3665903025353430 ) ) ;
#101649=CARTESIAN_POINT ( 'NONE',  ( -46.03754588423731064, -28.64604925653195977, 41.20450600710818634 ) ) ;
#101652=CARTESIAN_POINT ( 'NONE',  ( 97.24367771952604755, -45.35429863921569904, 193.9807169920567560 ) ) ;
#101660=CARTESIAN_POINT ( 'NONE',  ( -85.50673915265689118, -30.00000000000000000, 174.8803046632957034 ) ) ;
#101663=CARTESIAN_POINT ( 'NONE',  ( 83.69418490561940871, -57.54334727501766622, 201.5786063079811186 ) ) ;
#101666=CARTESIAN_POINT ( 'NONE',  ( 28.38348711115560263, -28.97649890655438654, -38.24913939007272745 ) ) ;
#101669=CARTESIAN_POINT ( 'NONE',  ( -53.06927891376064821, -60.00000000000000711, 79.84214154986403855 ) ) ;
#101674=CARTESIAN_POINT ( 'NONE',  ( -86.30437896728759029, -50.15100290326923016, 191.1588917352661383 ) ) ;
#101677=CARTESIAN_POINT ( 'NONE',  ( -1.974527876150213856, -18.58613712976008614, 26.98527037229319347 ) ) ;
#101691=CARTESIAN_POINT ( 'NONE',  ( 92.03798523278891253, -30.00000000000002842, 46.84723268580137301 ) ) ;
#101693=CARTESIAN_POINT ( 'NONE',  ( -84.18899188864789096, -18.67328967961437414, 149.2220349266904407 ) ) ;
#101697=CARTESIAN_POINT ( 'NONE',  ( 53.63544537906832232, -57.67554562530587958, 87.33806224458429313 ) ) ;
#101712=CARTESIAN_POINT ( 'NONE',  ( 27.75240500599559113, -60.00000000000001421, -41.15272815132448869 ) ) ;
#101713=CARTESIAN_POINT ( 'NONE',  ( -51.40736910322219444, -29.99999999999990052, 68.09419600167673536 ) ) ;
#101714=CARTESIAN_POINT ( 'NONE',  ( 22.40106687016081111, -35.99523339415899414, 30.71253893013516745 ) ) ;
#101716=CARTESIAN_POINT ( 'NONE',  ( -34.86660559149834171, -42.96819926141629509, 35.91443906510038175 ) ) ;
#101727=CARTESIAN_POINT ( 'NONE',  ( 92.67046874064129725, -29.99999999999975486, 191.0464373490836749 ) ) ;
#101732=CARTESIAN_POINT ( 'NONE',  ( 80.38962007328909465, -30.00000000000000000, -13.30899004357461912 ) ) ;
#101741=LINE ( 'NONE', #82501, #4563 ) ;
#101748=CARTESIAN_POINT ( 'NONE',  ( 75.47013347569310326, -38.35162841314899396, 173.9377833191998661 ) ) ;
#101771=CARTESIAN_POINT ( 'NONE',  ( 86.39827197653144708, -17.11905348657290915, 182.3887232808949932 ) ) ;
#101779=CARTESIAN_POINT ( 'NONE',  ( -82.75356297445279097, -30.00000000000000711, 40.85445903543622137 ) ) ;
#101784=CARTESIAN_POINT ( 'NONE',  ( 16.75933443583691584, -57.67153105735553709, 41.87489785921763996 ) ) ;
#101788=CARTESIAN_POINT ( 'NONE',  ( -36.26183010482215252, -33.57661459365222356, 34.86165481847040581 ) ) ;
#101791=CARTESIAN_POINT ( 'NONE',  ( 47.78548586219075389, -26.97685489492021205, -28.53356913460428856 ) ) ;
#101793=CARTESIAN_POINT ( 'NONE',  ( -26.57524688902023868, -36.00438821441548498, 31.51423073511094941 ) ) ;
#101796=CARTESIAN_POINT ( 'NONE',  ( -15.95769171998673919, -56.88368443177520106, 33.57075391308669765 ) ) ;
#101812=CARTESIAN_POINT ( 'NONE',  ( 101.3166947854019924, -37.84832686624076103, 187.1998071382763271 ) ) ;
#101826=CARTESIAN_POINT ( 'NONE',  ( -80.19169983686356318, -59.99999999999025846, -30.56219965566434738 ) ) ;
#101831=CARTESIAN_POINT ( 'NONE',  ( -93.17098673813583787, -59.99999999999997158, -17.95829132299026298 ) ) ;
#101833=CARTESIAN_POINT ( 'NONE',  ( -48.81468002507525483, -29.13763464560829419, 45.59164195770564021 ) ) ;
#101839=CARTESIAN_POINT ( 'NONE',  ( -93.93607513590077929, -37.67500921297137495, 192.9510021341835966 ) ) ;
#101845=CARTESIAN_POINT ( 'NONE',  ( 89.66286304382025207, -29.99999999999339195, -12.38401627152031637 ) ) ;
#101850=CARTESIAN_POINT ( 'NONE',  ( 87.02385573829870680, -30.00000000000000000, 183.8029085475771183 ) ) ;
#101858=CARTESIAN_POINT ( 'NONE',  ( 54.05082700138242302, -22.16248697930777567, 51.66267588704993585 ) ) ;
#101863=CARTESIAN_POINT ( 'NONE',  ( -91.44417391070038548, -38.39049349820264467, -8.093955909943030491 ) ) ;
#101866=CARTESIAN_POINT ( 'NONE',  ( 109.9455632978033890, -38.35592182039783182, 186.4162405044224613 ) ) ;
#101868=CARTESIAN_POINT ( 'NONE',  ( 85.24673747113007494, -52.71308823531107635, 2.599026173514388471 ) ) ;
#101892=CARTESIAN_POINT ( 'NONE',  ( 84.33144613566925329, -42.97469618036930683, 183.3463168981145657 ) ) ;
#101895=CARTESIAN_POINT ( 'NONE',  ( -98.81514710444544392, -52.71022382344329316, 115.6151661280325840 ) ) ;
#101899=CARTESIAN_POINT ( 'NONE',  ( -8.929954440217160894, -22.36709864391503544, -38.54354848803745170 ) ) ;
#101902=CARTESIAN_POINT ( 'NONE',  ( 29.47384080531130124, -60.00000000000000711, 42.78219204235330153 ) ) ;
#101904=CARTESIAN_POINT ( 'NONE',  ( 33.03637614824300073, -34.39509796229107508, 42.57305433018176188 ) ) ;
#101906=CARTESIAN_POINT ( 'NONE',  ( 52.01278122997629794, -29.95930541098613631, 50.12252116197368679 ) ) ;
#101907=CARTESIAN_POINT ( 'NONE',  ( -34.19577669012690535, -35.06686992932695546, 43.52267011995650137 ) ) ;
#101921=CARTESIAN_POINT ( 'NONE',  ( 1.540719842239331561, -21.77031602692093060, -30.51804812785477594 ) ) ;
#101930=CARTESIAN_POINT ( 'NONE',  ( -91.95502790194899490, -60.00000000000000000, 7.220182617842619166 ) ) ;
#101938=CARTESIAN_POINT ( 'NONE',  ( -81.85053211555002406, -46.45651121556473839, 170.1952362726539150 ) ) ;
#101940=CARTESIAN_POINT ( 'NONE',  ( -7.540179673743359068, -0.000000000000000000, -15.29468310208057602 ) ) ;
#101944=AXIS2_PLACEMENT_3D ( 'NONE', #17400, #97751, #99890 ) ;
#101950=CARTESIAN_POINT ( 'NONE',  ( -57.15598917327103834, -57.67115757216583205, -38.38010944898898202 ) ) ;
#101955=CARTESIAN_POINT ( 'NONE',  ( 90.56091889802806350, -29.99999999999993960, 34.47026654395114775 ) ) ;
#101957=CARTESIAN_POINT ( 'NONE',  ( -81.96434049221993234, -29.99999999999993250, 194.6677479149438454 ) ) ;
#101958=CARTESIAN_POINT ( 'NONE',  ( -55.22263546528215272, -49.91236510178273988, 65.08345786281854828 ) ) ;
#101962=CARTESIAN_POINT ( 'NONE',  ( -102.3679167227413700, -37.82050009904918397, 181.3159907740166830 ) ) ;
#101980=CARTESIAN_POINT ( 'NONE',  ( -29.54167733814598407, -22.11927707116958075, 29.86409302364821627 ) ) ;
#101983=CARTESIAN_POINT ( 'NONE',  ( 48.50725277660750834, -53.36040862114389682, 52.77151552700934189 ) ) ;
#101988=CARTESIAN_POINT ( 'NONE',  ( -100.6822085231046344, -38.46011006933861864, 200.2742388691330291 ) ) ;
#102000=CARTESIAN_POINT ( 'NONE',  ( 108.8655680065974423, -60.00000000000000711, 193.9842112700635539 ) ) ;
#102005=CARTESIAN_POINT ( 'NONE',  ( -79.26773016923658588, -29.99999999999997868, -14.68326225543056829 ) ) ;
#102007=SURFACE_SIDE_STYLE ('',( #20629 ) ) ;
#102016=CARTESIAN_POINT ( 'NONE',  ( 81.30317062471358724, -53.43848046224103143, 176.1350280067906624 ) ) ;
#102061=CARTESIAN_POINT ( 'NONE',  ( -111.3761741217465300, -60.00000000000000711, 185.3197500022033068 ) ) ;
#102065=CARTESIAN_POINT ( 'NONE',  ( -86.34263362178202783, -18.09246414803421033, 171.9745557676415615 ) ) ;
#102071=CARTESIAN_POINT ( 'NONE',  ( -83.93095737769149878, -45.26970912266205005, 3.740156994664543877 ) ) ;
#102076=CARTESIAN_POINT ( 'NONE',  ( 66.64731328016637235, -30.00000000000005684, 114.0820693445010363 ) ) ;
#102078=CARTESIAN_POINT ( 'NONE',  ( -73.46108764834735894, -30.00000000000002132, -28.33320811291743269 ) ) ;
#102079=CARTESIAN_POINT ( 'NONE',  ( -67.57911227637399065, -53.38914766505263998, 101.9919822544095638 ) ) ;
#102081=CARTESIAN_POINT ( 'NONE',  ( 97.75109942996037660, -59.99999999999985789, 204.9114775063931120 ) ) ;
#102084=CARTESIAN_POINT ( 'NONE',  ( 80.91739486121119285, -57.67116913187329885, -29.69084684708537125 ) ) ;
#102096=CARTESIAN_POINT ( 'NONE',  ( -92.21698522519400854, -60.00000000000001421, -12.99394316321618703 ) ) ;
#102111=CARTESIAN_POINT ( 'NONE',  ( 33.78548833840188337, -56.83387574824190835, 37.94913980780508211 ) ) ;
#102125=CARTESIAN_POINT ( 'NONE',  ( 92.68197952148119612, -59.99999999999999289, -4.372387793708037762 ) ) ;
#102135=CARTESIAN_POINT ( 'NONE',  ( -109.6056691518176649, -30.00000000000000000, 173.1093856131147959 ) ) ;
#102141=CARTESIAN_POINT ( 'NONE',  ( 85.09962800393060434, -60.19390250260627084, -15.90040431203298255 ) ) ;
#102156=CARTESIAN_POINT ( 'NONE',  ( 79.60872795848992212, -29.08772644578209210, 133.2594084639777634 ) ) ;
#102161=CARTESIAN_POINT ( 'NONE',  ( -111.5786317092108533, -57.67087409935591324, 192.6842770035980834 ) ) ;
#102169=CARTESIAN_POINT ( 'NONE',  ( -45.45765750525109183, -28.45291710252894646, 40.56146669681922390 ) ) ;
#102182=CARTESIAN_POINT ( 'NONE',  ( -23.46280628704403171, -21.90278913687860651, -37.56245478017753214 ) ) ;
#102183=CARTESIAN_POINT ( 'NONE',  ( -85.49286042444410327, -30.00000000000000711, 174.7639661085288481 ) ) ;
#102187=AXIS2_PLACEMENT_3D ( 'NONE', #88360, #29109, #39284 ) ;
#102188=CARTESIAN_POINT ( 'NONE',  ( 75.44058859636598413, -57.56160405487426601, 191.8524245654686240 ) ) ;
#102189=LINE ( 'NONE', #84950, #34540 ) ;
#102192=CARTESIAN_POINT ( 'NONE',  ( 39.31863996099055214, -32.72901781786905673, -37.51093992367277963 ) ) ;
#102195=CARTESIAN_POINT ( 'NONE',  ( -64.60151486236289031, -60.00000000000001421, 116.7762116740196063 ) ) ;
#102197=CARTESIAN_POINT ( 'NONE',  ( -86.41237560483617131, -46.49691307358666137, 190.1354165495773714 ) ) ;
#102201=CARTESIAN_POINT ( 'NONE',  ( -4.019156803245598653, -32.51259995193562702, 29.30134738771553415 ) ) ;
#102203=EDGE_CURVE ( 'NONE', #30000, #81108, #30616, .T. ) ;
#102217=CARTESIAN_POINT ( 'NONE',  ( 15.50035291838848472, -4.285714285715568117, -20.16952962162309859 ) ) ;
#102219=CARTESIAN_POINT ( 'NONE',  ( 94.42187179517443951, -29.99999999999998934, 63.29523499578382228 ) ) ;
#102220=CARTESIAN_POINT ( 'NONE',  ( -83.08186369656709758, -25.62021722390013068, 150.1200563151912775 ) ) ;
#102224=CARTESIAN_POINT ( 'NONE',  ( 5.689865212206615119, -57.67123513422165360, 41.59068566848854687 ) ) ;
#102241=CARTESIAN_POINT ( 'NONE',  ( 85.64840212452983792, -60.00000000000000000, -23.98298676833077181 ) ) ;
#102242=CARTESIAN_POINT ( 'NONE',  ( -59.93215762506982713, -30.00000000000009592, 91.51900601851320971 ) ) ;
#102243=CARTESIAN_POINT ( 'NONE',  ( 22.70406402036928739, -46.43430815227275588, 32.52211750540141111 ) ) ;
#102246=CARTESIAN_POINT ( 'NONE',  ( -33.88291765572438408, -25.63420728696120676, 32.08181795506389733 ) ) ;
#102249=CARTESIAN_POINT ( 'NONE',  ( -23.93420880016848074, -4.285714285714295357, -8.127057321558261549 ) ) ;
#102252=AXIS2_PLACEMENT_3D ( 'NONE', #71949, #28891, #88145 ) ;
#102257=CARTESIAN_POINT ( 'NONE',  ( -73.92728128053286696, -38.32663353633068226, 159.7396587626866449 ) ) ;
#102259=CARTESIAN_POINT ( 'NONE',  ( 97.91342610505886057, -29.99999999999999289, 190.6140529371372452 ) ) ;
#102263=CARTESIAN_POINT ( 'NONE',  ( 81.33594675399758955, -30.00000000000000355, -1.021767529535129171 ) ) ;
#102285=CARTESIAN_POINT ( 'NONE',  ( 59.69857829083183987, -53.38500049141745052, 78.06181712156276831 ) ) ;
#102304=CARTESIAN_POINT ( 'NONE',  ( 85.92109966458600923, -53.81464801703884149, 191.8547092607505817 ) ) ;
#102309=CARTESIAN_POINT ( 'NONE',  ( 65.37306859926557934, -29.78427825893012582, -22.92028099111634631 ) ) ;
#102313=CARTESIAN_POINT ( 'NONE',  ( -86.38235237773579911, -29.99999999999999645, 66.63133496844396575 ) ) ;
#102315=CARTESIAN_POINT ( 'NONE',  ( 28.07782961039620417, -57.67952082435122918, 44.31659357402789823 ) ) ;
#102325=CARTESIAN_POINT ( 'NONE',  ( 39.39455998684030646, -24.68490879047467956, -30.41947531785933734 ) ) ;
#102327=CARTESIAN_POINT ( 'NONE',  ( -21.68992718180131618, -53.40044820062799857, 33.52570783747689376 ) ) ;
#102331=CARTESIAN_POINT ( 'NONE',  ( -17.53032627728494575, -22.07011661811088032, 27.84778146757210138 ) ) ;
#102343=CARTESIAN_POINT ( 'NONE',  ( -10.78860715609207865, -60.00000000000000000, -42.38218987242183289 ) ) ;
#102346=CARTESIAN_POINT ( 'NONE',  ( 102.6487958908516589, -45.28275320593341036, 187.0266445405623017 ) ) ;
#102350=VERTEX_POINT ( 'NONE', #9206 ) ;
#102360=CARTESIAN_POINT ( 'NONE',  ( -57.24587099102581078, -60.00000000000970601, -38.75777265976601882 ) ) ;
#102362=CARTESIAN_POINT ( 'NONE',  ( 30.71235692075721602, -60.00000000000002132, 43.40817750810721520 ) ) ;
#102365=CARTESIAN_POINT ( 'NONE',  ( -113.0839934364197887, -60.00000000000005684, 149.3435297534686299 ) ) ;
#102366=CARTESIAN_POINT ( 'NONE',  ( 3.991493828809749456, -25.54818830820175890, 28.14084830479718491 ) ) ;
#102368=ADVANCED_FACE ( 'NONE', ( #84183 ), #79034, .T. ) ;
#102369=CARTESIAN_POINT ( 'NONE',  ( -49.48822239264870859, -29.13117794537824423, 46.55600149492851614 ) ) ;
#102377=LINE ( 'NONE', #52763, #8015 ) ;
#102379=CARTESIAN_POINT ( 'NONE',  ( 90.09087589920459038, -29.99999999999832667, -7.510710023258664769 ) ) ;
#102384=CARTESIAN_POINT ( 'NONE',  ( 97.54756622113360720, -30.00000000000000711, 190.8661322625956700 ) ) ;
#102392=VERTEX_POINT ( 'NONE', #78228 ) ;
#102393=CARTESIAN_POINT ( 'NONE',  ( 53.04775056965937807, -60.30987783887891851, 64.32335167159055800 ) ) ;
#102397=CARTESIAN_POINT ( 'NONE',  ( -90.43472293642049920, -38.40210348684055219, -14.77404530433802243 ) ) ;
#102400=CARTESIAN_POINT ( 'NONE',  ( 89.10629083803385697, -38.53219886314418829, 200.3222450649632833 ) ) ;
#102403=CARTESIAN_POINT ( 'NONE',  ( 83.77118831961728063, -45.28417051351964773, 6.938750227302574736 ) ) ;
#102410=ADVANCED_FACE ( 'NONE', ( #71192 ), #61086, .T. ) ;
#102427=CARTESIAN_POINT ( 'NONE',  ( -31.60541874544299645, -33.50245859134227544, 41.55280622130048584 ) ) ;
#102430=CARTESIAN_POINT ( 'NONE',  ( 84.53399812488744658, -42.96929415438898303, 184.1428513560889542 ) ) ;
#102435=CARTESIAN_POINT ( 'NONE',  ( -86.84743696432029481, -37.82102094881744847, 58.81972901610166815 ) ) ;
#102441=CARTESIAN_POINT ( 'NONE',  ( 81.92741076442609938, -53.50746804662570355, 180.9159421606091200 ) ) ;
#102442=CARTESIAN_POINT ( 'NONE',  ( 38.67627001412847676, -59.99999999999999289, 50.31928010676779195 ) ) ;
#102443=CARTESIAN_POINT ( 'NONE',  ( 16.26197166262537763, -23.40186626609153109, 36.11761830283866459 ) ) ;
#102445=CARTESIAN_POINT ( 'NONE',  ( 51.42506870373882322, -29.90362599224476980, 49.04348699933098032 ) ) ;
#102464=CARTESIAN_POINT ( 'NONE',  ( 4.765530066358713235, -47.40889156923955028, -34.73460941772712118 ) ) ;
#102473=CARTESIAN_POINT ( 'NONE',  ( -91.96800439629041080, -60.00000000000000000, 6.911253661384300528 ) ) ;
#102483=CARTESIAN_POINT ( 'NONE',  ( -82.93554783337889091, -39.48948165585812831, 169.2715108827067354 ) ) ;
#102486=CARTESIAN_POINT ( 'NONE',  ( -8.521464936451071281, -0.000000000000000000, 14.76977913854606506 ) ) ;
#102495=CARTESIAN_POINT ( 'NONE',  ( -94.14808112328414325, -57.65316219711669987, -13.38331396264917394 ) ) ;
#102501=CARTESIAN_POINT ( 'NONE',  ( 82.73925898424661796, -14.21045842199433373, -19.52984640694043250 ) ) ;
#102502=CARTESIAN_POINT ( 'NONE',  ( -74.10870907870054225, -60.00000000000004974, 189.8079394841834073 ) ) ;
#102504=CARTESIAN_POINT ( 'NONE',  ( -54.64099352351128402, -53.38243350366994378, 65.16998337476768199 ) ) ;
#102508=CARTESIAN_POINT ( 'NONE',  ( -103.9834764852472517, -52.71019089480785880, 186.8325922579311680 ) ) ;
#102513=FILL_AREA_STYLE ('',( #45349 ) ) ;
#102520=CARTESIAN_POINT ( 'NONE',  ( 66.85002385057480012, -29.99999999999999645, 85.60483471394741173 ) ) ;
#102525=CARTESIAN_POINT ( 'NONE',  ( -26.98668602709024356, -46.43780309524522210, 33.41811407250219901 ) ) ;
#102526=CARTESIAN_POINT ( 'NONE',  ( 47.78329097220170496, -18.76695584851968235, 41.09799256819893287 ) ) ;
#102530=CARTESIAN_POINT ( 'NONE',  ( -93.74606775496390298, -38.49331479316243332, 201.1767005034121780 ) ) ;
#102539=CARTESIAN_POINT ( 'NONE',  ( 111.2827313485384479, -60.00000000000000000, 185.7785520166476090 ) ) ;
#102545=CARTESIAN_POINT ( 'NONE',  ( -73.50846916961513955, -30.00000000000000711, -18.85481956966018302 ) ) ;
#102547=CARTESIAN_POINT ( 'NONE',  ( -75.93393509941148523, -38.37291240018149097, 177.9364027747577381 ) ) ;
#102562=CARTESIAN_POINT ( 'NONE',  ( 84.54726099131491424, -28.98982865470740933, 167.9107454418049770 ) ) ;
#102576=CARTESIAN_POINT ( 'NONE',  ( -76.71780263312517434, -30.00000000000000355, -16.85326244919820482 ) ) ;
#102586=ORIENTED_EDGE ( 'NONE', *, *, #93204, .T. ) ;
#102587=B_SPLINE_CURVE_WITH_KNOTS ( 'NONE', 3,
 ( #63809, #14158, #45507, #21249 ),
 .UNSPECIFIED., .F., .F.,
 ( 4, 4 ),
 ( 0.000000000000000000, 0.01132019266528281470 ),
 .UNSPECIFIED. ) ;
#102602=CARTESIAN_POINT ( 'NONE',  ( -112.0514578880708285, -59.99999999999998579, 178.8323363711955665 ) ) ;
#102607=CARTESIAN_POINT ( 'NONE',  ( -86.11088107305231176, -21.49943172053022522, 175.3779314699612542 ) ) ;
#102614=CARTESIAN_POINT ( 'NONE',  ( -86.74535326754120490, -60.15511608754272288, -0.9989608454956866446 ) ) ;
#102619=CARTESIAN_POINT ( 'NONE',  ( 72.58683006904378487, -60.00000000000011369, 181.3898877100950244 ) ) ;
#102620=CARTESIAN_POINT ( 'NONE',  ( -89.32121524059635931, -30.00000000000006750, 17.90039431539770121 ) ) ;
#102622=CARTESIAN_POINT ( 'NONE',  ( -64.47158722768480743, -32.53199268566179825, 81.05542600198782566 ) ) ;
#102624=CARTESIAN_POINT ( 'NONE',  ( 80.78816237064734196, -29.99999999999997513, 192.9482874834278903 ) ) ;
#102626=CARTESIAN_POINT ( 'NONE',  ( 35.58387498457056353, -60.00000000000000000, 50.27079091460490901 ) ) ;
#102639=CARTESIAN_POINT ( 'NONE',  ( -82.04894669109339134, -60.00000000000000000, -26.67549837306723504 ) ) ;
#102653=CARTESIAN_POINT ( 'NONE',  ( 35.62089395783882395, -56.82290754243824438, 39.01274798168336133 ) ) ;
#102654=CARTESIAN_POINT ( 'NONE',  ( -24.56594385547996140, -4.285714285713227767, 6.601913983196856073 ) ) ;
#102666=CARTESIAN_POINT ( 'NONE',  ( 92.28783886427984839, -60.00000000000001421, 1.681624045158784719 ) ) ;
#102674=CARTESIAN_POINT ( 'NONE',  ( -96.30420021061665636, -29.99999999998855316, 199.8843319236383138 ) ) ;
#102691=CARTESIAN_POINT ( 'NONE',  ( 79.60604231873648473, -42.96535285804148430, 147.0936545434987579 ) ) ;
#102697=CARTESIAN_POINT ( 'NONE',  ( -75.26480569136067800, -57.56533996972894585, 191.5310976926263322 ) ) ;
#102705=CARTESIAN_POINT ( 'NONE',  ( -51.39279124642569485, -29.89994363668846589, 48.98449833262483821 ) ) ;
#102720=CARTESIAN_POINT ( 'NONE',  ( -44.85365888377566534, -27.62284328472143002, -35.79871730042521705 ) ) ;
#102721=CARTESIAN_POINT ( 'NONE',  ( -84.24606464348262591, -30.00000000000000000, 163.2190891219070465 ) ) ;
#102727=CARTESIAN_POINT ( 'NONE',  ( 77.69090662619261423, -57.51539192374901432, 196.1345721221005931 ) ) ;
#102735=CARTESIAN_POINT ( 'NONE',  ( -53.51261712237818813, -59.99999999999999289, 81.06700852216475539 ) ) ;
#102738=CARTESIAN_POINT ( 'NONE',  ( -84.23439574659690265, -57.43960185101178695, 191.0516973466356490 ) ) ;
#102741=CARTESIAN_POINT ( 'NONE',  ( -1.010379499472258136, -46.43937201709040608, 31.62954529578411567 ) ) ;
#102753=CARTESIAN_POINT ( 'NONE',  ( -12.70248734011669356, -4.285714285715063632, 22.03900363279318597 ) ) ;
#102755=CARTESIAN_POINT ( 'NONE',  ( 101.8005042720997864, -59.99999999999995026, 77.51357286062189189 ) ) ;
#102756=CARTESIAN_POINT ( 'NONE',  ( -81.82631429444417392, -22.15562358550804589, 138.5281546227773504 ) ) ;
#102758=SURFACE_STYLE_FILL_AREA ( #95729 ) ;
#102777=CARTESIAN_POINT ( 'NONE',  ( 1.405425598185054066E-06, -60.00000000000000711, -42.63907915653317104 ) ) ;
#102780=CARTESIAN_POINT ( 'NONE',  ( -72.31573431813527009, -14.21045842199431064, 125.5062215401438266 ) ) ;
#102781=CARTESIAN_POINT ( 'NONE',  ( 29.17015437932591126, -53.38279045855296090, 35.28568588006530860 ) ) ;
#102784=CARTESIAN_POINT ( 'NONE',  ( -35.65114319003946264, -36.04324675791306021, 35.00216631688633129 ) ) ;
#102797=CARTESIAN_POINT ( 'NONE',  ( -69.38341510186705818, -38.33187031249859444, 131.7580717154634726 ) ) ;
#102798=CARTESIAN_POINT ( 'NONE',  ( 101.1080780491627991, -29.99999999999998224, 175.1557127305151198 ) ) ;
#102802=CARTESIAN_POINT ( 'NONE',  ( 80.98407313594076129, -30.00000000000000355, -11.93458638676729144 ) ) ;
#102822=CARTESIAN_POINT ( 'NONE',  ( 60.44875679912436084, -38.34244523237531155, 97.82314019685307471 ) ) ;
#102826=CARTESIAN_POINT ( 'NONE',  ( 62.38096262930346114, -60.33914173519230673, 89.28673981057380615 ) ) ;
#102840=CARTESIAN_POINT ( 'NONE',  ( 86.43023946451208417, -24.51488847468812793, 183.3687221833509966 ) ) ;
#102847=CARTESIAN_POINT ( 'NONE',  ( 36.58860353225821882, -23.84130847726161662, -30.99593518099760558 ) ) ;
#102851=CARTESIAN_POINT ( 'NONE',  ( -100.3439110779055312, -29.99999999999999645, 157.3914886282430246 ) ) ;
#102855=CARTESIAN_POINT ( 'NONE',  ( 19.65360057920942438, -57.67192277060839700, 42.16630265707282632 ) ) ;
#102870=CARTESIAN_POINT ( 'NONE',  ( -18.02399320543497296, -46.43928582069488442, 31.96005001963083458 ) ) ;
#102871=CARTESIAN_POINT ( 'NONE',  ( -86.66579604520306646, -60.00000000000000711, -0.1178683406456105670 ) ) ;
#102879=AXIS2_PLACEMENT_3D ( 'NONE', #18325, #68458, #26439 ) ;
#102880=CARTESIAN_POINT ( 'NONE',  ( -5.422877198588844649, -59.99999999999999289, -42.58549929937262135 ) ) ;
#102884=CARTESIAN_POINT ( 'NONE',  ( 102.0397306347427104, -52.72302187501731652, 192.0072258283632323 ) ) ;
#102899=CARTESIAN_POINT ( 'NONE',  ( -94.80066220543719169, -60.00000000000000000, -0.2464906575786718901 ) ) ;
#102901=CARTESIAN_POINT ( 'NONE',  ( 21.98983231224196544, -60.00000000000000000, 40.51305684052432809 ) ) ;
#102904=CARTESIAN_POINT ( 'NONE',  ( -104.9451182028910239, -14.21045842199441367, 145.4712626202903323 ) ) ;
#102905=CARTESIAN_POINT ( 'NONE',  ( 13.57004255533479942, -46.43472687649081365, 31.71508379387893228 ) ) ;
#102907=CARTESIAN_POINT ( 'NONE',  ( -49.06124572357285984, -36.05852591224155645, 48.12833458416420029 ) ) ;
#102908=VERTEX_POINT ( 'NONE', #75461 ) ;
#102918=CARTESIAN_POINT ( 'NONE',  ( 89.86244880932272849, -29.99999999998984990, -1.486525042624827986 ) ) ;
#102921=CARTESIAN_POINT ( 'NONE',  ( 100.8396476006763578, -29.99999999999999645, 163.9396555014752437 ) ) ;
#102927=CARTESIAN_POINT ( 'NONE',  ( 55.41416639835406954, -25.62021389884816358, 55.60954475568744471 ) ) ;
#102938=CARTESIAN_POINT ( 'NONE',  ( 101.5779485941844626, -38.45071526406401574, 199.8867405208796981 ) ) ;
#102941=CARTESIAN_POINT ( 'NONE',  ( 83.72785699625647737, -45.28390520765234584, 8.237543405220815629 ) ) ;
#102961=CARTESIAN_POINT ( 'NONE',  ( -2.229368152238511147, -14.88154708191588504, 34.47882516350917825 ) ) ;
#102964=CARTESIAN_POINT ( 'NONE',  ( 85.34274748661711385, -32.19989682491620897, 180.0761885193842886 ) ) ;
#102969=CARTESIAN_POINT ( 'NONE',  ( -96.73191789133785790, -60.15505594016180169, 95.88985520306968624 ) ) ;
#102977=CARTESIAN_POINT ( 'NONE',  ( 7.804325080931074687, -19.38637389769215957, 35.22465547960180743 ) ) ;
#102979=CARTESIAN_POINT ( 'NONE',  ( 50.24570806728828387, -29.73392352015472540, 47.01200513134826764 ) ) ;
#102990=CARTESIAN_POINT ( 'NONE',  ( -82.45001613080906111, -38.00000000000001421, 10.13691710915257183 ) ) ;
#102997=CARTESIAN_POINT ( 'NONE',  ( -7.964568475979583617, -47.40891111626400800, -34.64478426194994398 ) ) ;
#103007=CARTESIAN_POINT ( 'NONE',  ( -93.39459019562438868, -60.00000000000000000, 36.07653886588029479 ) ) ;
#103019=CARTESIAN_POINT ( 'NONE',  ( -80.20997988972960968, -60.39356314814814652, 177.0984289422948734 ) ) ;
#103030=CARTESIAN_POINT ( 'NONE',  ( -92.76317396897962908, -57.65703681568646743, -17.81073576277876569 ) ) ;
#103036=CARTESIAN_POINT ( 'NONE',  ( 63.50796903478703115, -60.00000000000007816, -37.13796669901890368 ) ) ;
#103037=CARTESIAN_POINT ( 'NONE',  ( -62.54317499552948334, -60.00000000000000711, 118.0918133646953976 ) ) ;
#103038=CARTESIAN_POINT ( 'NONE',  ( -54.35042906398516038, -39.50198214953601195, 58.92073034776293383 ) ) ;
#103042=ORIENTED_EDGE ( 'NONE', *, *, #75605, .F. ) ;
#103043=CARTESIAN_POINT ( 'NONE',  ( -100.6300002315544901, -45.26144706321691302, 191.8785347955782754 ) ) ;
#103055=CARTESIAN_POINT ( 'NONE',  ( 62.21186031149353113, -30.00000000000000355, 72.58540792779400874 ) ) ;
#103060=CARTESIAN_POINT ( 'NONE',  ( -28.71080020290498780, -42.96128409593538322, 33.31360371976838053 ) ) ;
#103063=CARTESIAN_POINT ( 'NONE',  ( 46.99059970337066261, -56.81049650515272020, 51.30630512147487821 ) ) ;
#103066=CARTESIAN_POINT ( 'NONE',  ( -87.32597803086463273, -38.58248733736562031, 199.6835492166326560 ) ) ;
#103068=CARTESIAN_POINT ( 'NONE',  ( 89.40823501132422280, -38.38738139504339841, -17.29573669771441047 ) ) ;
#103077=CARTESIAN_POINT ( 'NONE',  ( 111.0086579293828493, -60.00000000000002842, 152.2211401378526148 ) ) ;
#103086=CARTESIAN_POINT ( 'NONE',  ( -90.92816914291333319, -38.34532242824909787, 3.098464593803623046 ) ) ;
#103099=CARTESIAN_POINT ( 'NONE',  ( 83.25611969625570907, -39.47771237622612261, 172.2730610428070008 ) ) ;
#103137=CARTESIAN_POINT ( 'NONE',  ( -94.55424737603695462, -60.00000000000000711, 202.5650574291949511 ) ) ;
#103143=CARTESIAN_POINT ( 'NONE',  ( -83.51272355743553533, -46.53462533077923524, 182.5745365089843801 ) ) ;
#103149=CARTESIAN_POINT ( 'NONE',  ( -82.43943121196362256, -37.82767094664968255, 14.49479528845560417 ) ) ;
#103153=DIRECTION ( 'NONE',  ( 1.871721906610600077E-16, 0.000000000000000000, -1.000000000000000000 ) ) ;
#103156=CARTESIAN_POINT ( 'NONE',  ( 78.42622819757743002, -14.21045842199428932, 178.5071270543957951 ) ) ;
#103158=CARTESIAN_POINT ( 'NONE',  ( -95.73631051900581213, -30.00000000000000000, 71.50198832723137343 ) ) ;
#103159=CARTESIAN_POINT ( 'NONE',  ( -66.70770666932376969, -29.05727726843131720, 85.70037747262490768 ) ) ;
#103161=CARTESIAN_POINT ( 'NONE',  ( 112.2652136917531465, -60.00000000000000000, 191.8488956690686962 ) ) ;
#103163=CARTESIAN_POINT ( 'NONE',  ( 52.35809470648487007, -60.00000000002930278, 84.81990995266937716 ) ) ;
#103174=CARTESIAN_POINT ( 'NONE',  ( -90.16357200789421711, -59.99999999999997868, -18.56049759532515253 ) ) ;
#103188=CARTESIAN_POINT ( 'NONE',  ( 33.54291075367279973, -46.42946800168273569, 35.89603996142585629 ) ) ;
#103189=CARTESIAN_POINT ( 'NONE',  ( -22.03900363279597840, -4.285714285713229543, -12.70248734010661451 ) ) ;
#103190=ORIENTED_EDGE ( 'NONE', *, *, #9058, .F. ) ;
#103202=CARTESIAN_POINT ( 'NONE',  ( 92.01104092861777417, -60.00000000000000000, 18.65600228545548589 ) ) ;
#103208=CARTESIAN_POINT ( 'NONE',  ( -104.4911618787428438, -30.00000000000223466, 196.0249069884481514 ) ) ;
#103214=CARTESIAN_POINT ( 'NONE',  ( 82.06366534565165693, -37.81903932946467961, -13.65071145180755430 ) ) ;
#103225=CARTESIAN_POINT ( 'NONE',  ( 77.23229261623454533, -53.37152101417233041, 143.0171963300477103 ) ) ;
#103231=CARTESIAN_POINT ( 'NONE',  ( -100.8911947370258844, -57.62911827813870502, 203.6698938757279223 ) ) ;
#103241=CARTESIAN_POINT ( 'NONE',  ( -51.87932953685692894, -29.94853046243735406, 49.87283498340130450 ) ) ;
#103252=CARTESIAN_POINT ( 'NONE',  ( -13.71949818509876629, -19.30456015386723223, -37.82957963845891669 ) ) ;
#103253=CARTESIAN_POINT ( 'NONE',  ( -82.83350497009941193, -30.00000000000000355, 151.6907841967885417 ) ) ;
#103258=CARTESIAN_POINT ( 'NONE',  ( 83.70865895686264935, -57.54354250294924356, 201.5867987658908760 ) ) ;
#103259=CARTESIAN_POINT ( 'NONE',  ( 73.58146070047708065, -60.22809872142786958, -24.87506665778998638 ) ) ;
#103264=CARTESIAN_POINT ( 'NONE',  ( -62.19705368951759539, -60.00000000000000000, 107.9267807310001643 ) ) ;
#103269=CARTESIAN_POINT ( 'NONE',  ( -86.23216682740927297, -24.68519757505537626, 181.5290854991648359 ) ) ;
#103289=CARTESIAN_POINT ( 'NONE',  ( 15.50035291838412199, -4.285714285712356464, 20.16952962162429941 ) ) ;
#103292=CARTESIAN_POINT ( 'NONE',  ( 105.2982900294548614, -30.00000000000001066, 128.8790101386541096 ) ) ;
#103293=CARTESIAN_POINT ( 'NONE',  ( -81.81404306141678262, -25.62499348290805301, 141.9831859399797054 ) ) ;
#103295=( LENGTH_UNIT ( ) NAMED_UNIT ( * ) SI_UNIT ( .MILLI., .METRE. ) );
#103297=CARTESIAN_POINT ( 'NONE',  ( 98.32443960344940592, -57.62441092855549840, 204.2909859055558286 ) ) ;
#103315=CARTESIAN_POINT ( 'NONE',  ( 30.52000010178268496, -60.00000000000000000, -40.85847840406977127 ) ) ;
#103316=CARTESIAN_POINT ( 'NONE',  ( -39.49898250731507687, -29.99999999999994316, 47.07929020003657428 ) ) ;
#103317=CARTESIAN_POINT ( 'NONE',  ( 26.43631887545773651, -32.52417025399565631, 30.87970515157304519 ) ) ;
#103330=CARTESIAN_POINT ( 'NONE',  ( 97.48148763265582772, -29.99999999999981171, 190.8966502933984657 ) ) ;
#103333=CARTESIAN_POINT ( 'NONE',  ( 81.12250922778763140, -30.00000000000000355, 2.073590792126307480 ) ) ;
#103357=CARTESIAN_POINT ( 'NONE',  ( -83.59931608698744299, -60.00000000000002132, 191.2519107553881383 ) ) ;
#103358=CARTESIAN_POINT ( 'NONE',  ( 63.26434788449935809, -56.86244944842989213, 90.13329942383785465 ) ) ;
#103374=CARTESIAN_POINT ( 'NONE',  ( 86.68178608655959749, -24.39358399406027900, 184.9913743671155260 ) ) ;
#103381=CARTESIAN_POINT ( 'NONE',  ( -100.7873380846828724, -30.00000000000000355, 180.4097680941990234 ) ) ;
#103383=CARTESIAN_POINT ( 'NONE',  ( 25.95016476712096321, -57.67607197499474836, 43.50018178531507829 ) ) ;
#103392=CARTESIAN_POINT ( 'NONE',  ( -87.29218671470692925, -28.00333867647982800, 187.7165209339487717 ) ) ;
#103395=CARTESIAN_POINT ( 'NONE',  ( -14.23481919006072616, -18.58702783338264908, 27.09272798716932940 ) ) ;
#103396=CARTESIAN_POINT ( 'NONE',  ( -86.89501302346295120, -60.00000000000000711, -9.734508581877785005 ) ) ;
#103418=CARTESIAN_POINT ( 'NONE',  ( 2.500000000000000000, -8.000000000000000000, 14.79019945774903988 ) ) ;
#103419=( BOUNDED_SURFACE ( )  B_SPLINE_SURFACE ( 2, 3, ( 
 ( #35598, #101366, #25932, #36671, #27519, #60396, #59318, #26451, #92189, #51195, #69535, #59860, #58789, #34539, #18341, #91685, #50650, #77083, #93805, #19435, #93273, #52265, #42583, #60919, #52805, #85731, #85179, #11264, #11803, #75484, #3200, #77623, #84115, #92731, #36143, #10214, #44735, #43127, #76012, #3740, #2112, #100815, #35062, #67930, #26977, #84652, #12864, #37735 ),
 ( #13926, #63034, #103486, #96469, #4795, #4264, #78659, #54368, #95934, #78142, #45266, #70057, #53345, #37192, #46315, #87313, #80252, #5841, #54917, #38767, #63579, #39300, #102961, #45783, #38252, #13394, #79207, #71632, #61452, #28568, #94347, #95395, #86265, #22059, #47365, #12339, #104538, #22607, #30691, #55442, #70594, #29124, #61993, #53865, #88377, #87843, #14451, #29634 ),
 ( #30150, #21535, #94885, #104003, #21025, #5329, #6361, #71116, #86793, #102427, #20509, #46836, #62510, #79738, #56505, #40338, #88896, #8497, #89952, #16060, #89435, #7423, #14991, #64111, #90488, #32806, #73218, #66204, #81309, #80791, #48418, #24192, #65680, #47883, #6903, #39825, #23123, #72701, #48941, #57038, #50018, #82389, #24716, #41399, #33338, #9020, #105600, #15525 ) ),
 .UNSPECIFIED., .F., .F., .F. ) 
 B_SPLINE_SURFACE_WITH_KNOTS ( ( 3, 3 ),
 ( 4, 2, 2, 2, 2, 2, 2, 2, 2, 2, 2, 2, 2, 2, 2, 2, 2, 2, 2, 2, 2, 2, 2, 4 ),
 ( 0.000000000000000000, 1.000000000000000000 ),
 ( 0.000000000000000000, 0.008322629228191371839, 0.01248394384228705689, 0.01664525845638274368, 0.02496788768457411378, 0.02912920229866980057, 0.03329051691276548736, 0.04161314614095686093, 0.04993577536914822756, 0.05825840459733960114, 0.06241971921143528446, 0.06658103382553097471, 0.07074234843962665109, 0.07282300574667449622, 0.07490366305372234135, 0.08322629228191372186, 0.09154892151010508849, 0.09987155073829645513, 0.1040328653523921454, 0.1081941799664878356, 0.1123554945805835259, 0.1165168091946792023, 0.1248394384228705689, 0.1331620676510619494 ),
 .UNSPECIFIED. ) 
 GEOMETRIC_REPRESENTATION_ITEM ( )  RATIONAL_B_SPLINE_SURFACE ( (
 ( 1.000000000000000000, 1.000000000000000000, 1.000000000000000000, 1.000000000000000000, 1.000000000000000000, 1.000000000000000000, 1.000000000000000000, 1.000000000000000000, 1.000000000000000000, 1.000000000000000000, 1.000000000000000000, 1.000000000000000000, 1.000000000000000000, 1.000000000000000000, 1.000000000000000000, 1.000000000000000000, 1.000000000000000000, 1.000000000000000000, 1.000000000000000000, 1.000000000000000000, 1.000000000000000000, 1.000000000000000000, 1.000000000000000000, 1.000000000000000000, 1.000000000000000000, 1.000000000000000000, 1.000000000000000000, 1.000000000000000000, 1.000000000000000000, 1.000000000000000000, 1.000000000000000000, 1.000000000000000000, 1.000000000000000000, 1.000000000000000000, 1.000000000000000000, 1.000000000000000000, 1.000000000000000000, 1.000000000000000000, 1.000000000000000000, 1.000000000000000000, 1.000000000000000000, 1.000000000000000000, 1.000000000000000000, 1.000000000000000000, 1.000000000000000000, 1.000000000000000000, 1.000000000000000000, 1.000000000000000000),
 ( 1.857142857142858317, 1.857142857142858317, 1.857142857142858317, 1.857142857142858317, 1.857142857142858317, 1.857142857142858317, 1.857142857142858317, 1.857142857142858317, 1.857142857142858317, 1.857142857142858317, 1.857142857142858317, 1.857142857142858317, 1.857142857142858317, 1.857142857142858317, 1.857142857142858317, 1.857142857142858317, 1.857142857142858317, 1.857142857142858317, 1.857142857142858317, 1.857142857142858317, 1.857142857142858317, 1.857142857142858317, 1.857142857142858317, 1.857142857142858317, 1.857142857142858317, 1.857142857142858317, 1.857142857142858317, 1.857142857142858317, 1.857142857142858317, 1.857142857142858317, 1.857142857142858317, 1.857142857142858317, 1.857142857142858317, 1.857142857142858317, 1.857142857142858317, 1.857142857142858317, 1.857142857142859205, 1.857142857142859205, 1.857142857142858317, 1.857142857142858317, 1.857142857142857428, 1.857142857142857428, 1.857142857142858317, 1.857142857142858317, 1.857142857142858317, 1.857142857142858317, 1.857142857142858317, 1.857142857142858317),
 ( 1.000000000000000000, 1.000000000000000000, 1.000000000000000000, 1.000000000000000000, 1.000000000000000000, 1.000000000000000000, 1.000000000000000000, 1.000000000000000000, 1.000000000000000000, 1.000000000000000000, 1.000000000000000000, 1.000000000000000000, 1.000000000000000000, 1.000000000000000000, 1.000000000000000000, 1.000000000000000000, 1.000000000000000000, 1.000000000000000000, 1.000000000000000000, 1.000000000000000000, 1.000000000000000000, 1.000000000000000000, 1.000000000000000000, 1.000000000000000000, 1.000000000000000000, 1.000000000000000000, 1.000000000000000000, 1.000000000000000000, 1.000000000000000000, 1.000000000000000000, 1.000000000000000000, 1.000000000000000000, 1.000000000000000000, 1.000000000000000000, 1.000000000000000000, 1.000000000000000000, 1.000000000000000000, 1.000000000000000000, 1.000000000000000000, 1.000000000000000000, 1.000000000000000000, 1.000000000000000000, 1.000000000000000000, 1.000000000000000000, 1.000000000000000000, 1.000000000000000000, 1.000000000000000000, 1.000000000000000000) ) ) 
 REPRESENTATION_ITEM ( '' )  SURFACE ( )  );
#103425=CARTESIAN_POINT ( 'NONE',  ( -91.55378440295650933, -59.99999999999023714, 204.7501500527700671 ) ) ;
#103428=CARTESIAN_POINT ( 'NONE',  ( 57.09504128153807301, -59.99999999999997868, -38.79348205093937452 ) ) ;
#103431=CARTESIAN_POINT ( 'NONE',  ( -94.42208465491292202, -30.00000000000002132, 63.29659460224121403 ) ) ;
#103432=CARTESIAN_POINT ( 'NONE',  ( 8.054255350734946362, -25.54841287528824623, 28.14046425560073317 ) ) ;
#103434=CARTESIAN_POINT ( 'NONE',  ( -48.12968807026369689, -60.28544049161936158, 54.32557363639672587 ) ) ;
#103444=CARTESIAN_POINT ( 'NONE',  ( 109.3019642819107418, -29.99999999999331379, 163.0555205557570559 ) ) ;
#103448=CARTESIAN_POINT ( 'NONE',  ( 95.19895599661560937, -29.99999999999999645, 191.3423363543731455 ) ) ;
#103454=CARTESIAN_POINT ( 'NONE',  ( 54.20624670247494237, -42.96740642929500353, 59.98673961352833572 ) ) ;
#103464=CARTESIAN_POINT ( 'NONE',  ( 88.58302811347638794, -38.54321962364008414, 200.1547288739133990 ) ) ;
#103466=CARTESIAN_POINT ( 'NONE',  ( 83.89778286979191080, -45.28641516711167014, 4.373900399497115288 ) ) ;
#103482=AXIS2_PLACEMENT_3D ( 'NONE', #98400, #14819, #16421 ) ;
#103486=CARTESIAN_POINT ( 'NONE',  ( -43.59233498779423854, -29.69447325614249067, 52.52981076111234415 ) ) ;
#103490=CARTESIAN_POINT ( 'NONE',  ( 86.39767885033103312, -17.86857175737891978, 174.6560174384326842 ) ) ;
#103495=CARTESIAN_POINT ( 'NONE',  ( 93.84014446886344274, -57.67487048525376991, 10.77052861846502907 ) ) ;
#103500=CARTESIAN_POINT ( 'NONE',  ( -8.066564334389425994, -22.17767452351848689, -38.54423803581626373 ) ) ;
#103503=CARTESIAN_POINT ( 'NONE',  ( 34.50342751135733010, -23.83194123643590245, 33.31419988176715918 ) ) ;
#103511=CARTESIAN_POINT ( 'NONE',  ( -82.46191414289508259, -38.00000000000002842, 16.70185672408629785 ) ) ;
#103517=CARTESIAN_POINT ( 'NONE',  ( 7.758608792424636746, -21.77038665610601598, -30.37594175526581708 ) ) ;
#103524=AXIS2_PLACEMENT_3D ( 'NONE', #30490, #23466, #79019 ) ;
#103530=CARTESIAN_POINT ( 'NONE',  ( -92.73406948728150212, -59.99999999999998579, -6.025074217602045756 ) ) ;
#103538=CARTESIAN_POINT ( 'NONE',  ( -82.60715075437619248, -42.97642582163322800, 171.7397776580246500 ) ) ;
#103550=CARTESIAN_POINT ( 'NONE',  ( -69.44743540119901581, -57.67117814800237596, -34.85819734733303221 ) ) ;
#103556=CARTESIAN_POINT ( 'NONE',  ( 94.38107034336813683, -59.99999999999990763, 5.298252861571447703 ) ) ;
#103557=CARTESIAN_POINT ( 'NONE',  ( -68.01705929348101165, -29.99999999999997158, 119.4519777144086703 ) ) ;
#103558=CARTESIAN_POINT ( 'NONE',  ( -55.88782504570332321, -25.61907991660268280, 56.57138212751718953 ) ) ;
#103559=EDGE_LOOP ( 'NONE', ( #28648, #100118, #55529, #86833 ) ) ;
#103562=CARTESIAN_POINT ( 'NONE',  ( -101.5044452224088047, -52.72315398099703998, 192.7887324484784699 ) ) ;
#103577=CARTESIAN_POINT ( 'NONE',  ( -28.86452025935745880, -46.43714135143746091, 33.97076303928542984 ) ) ;
#103580=CARTESIAN_POINT ( 'NONE',  ( 47.01442997823554748, -46.44001080992690333, 48.25839572838238922 ) ) ;
#103586=CARTESIAN_POINT ( 'NONE',  ( -104.4730387931192581, -38.40368207287023239, 197.9910534897900902 ) ) ;
#103588=CARTESIAN_POINT ( 'NONE',  ( 90.73652762505595604, -38.34866151637469045, 17.91778245446875317 ) ) ;
#103589=CARTESIAN_POINT ( 'NONE',  ( 81.38975290692940234, -59.99999999999997158, 184.8793320046452777 ) ) ;
#103595=CARTESIAN_POINT ( 'NONE',  ( 77.81167547839096699, -60.00000000000001421, 192.4355787521637922 ) ) ;
#103604=CARTESIAN_POINT ( 'NONE',  ( -104.9207578273651364, -38.39526174885175180, 197.5709644312131559 ) ) ;
#103616=CARTESIAN_POINT ( 'NONE',  ( 84.78132171091615987, -25.52741569763149698, 164.4133495432128882 ) ) ;
#103629=CARTESIAN_POINT ( 'NONE',  ( -77.71356797093831403, -30.00000000000000355, -16.14039426699441648 ) ) ;
#103657=CARTESIAN_POINT ( 'NONE',  ( -107.9499919529012431, -60.00000000000000000, 195.7098482030020250 ) ) ;
#103662=CARTESIAN_POINT ( 'NONE',  ( -82.60006740705316020, -57.21883819474334842, 187.3423846480518762 ) ) ;
#103670=CARTESIAN_POINT ( 'NONE',  ( -83.71921483055798774, -37.82245684421392440, 34.46557360337037323 ) ) ;
#103676=DIRECTION ( 'NONE',  ( 0.000000000000000000, -0.000000000000000000, 1.000000000000000000 ) ) ;
#103678=CARTESIAN_POINT ( 'NONE',  ( 94.36203364593035303, -29.99999999999990763, 200.0833959884570845 ) ) ;
#103680=CARTESIAN_POINT ( 'NONE',  ( -104.6757555735165113, -59.99999999999997158, 94.38003174760403624 ) ) ;
#103683=CARTESIAN_POINT ( 'NONE',  ( -65.14366692970418171, -32.53254546774595468, 82.99592137394043334 ) ) ;
#103686=CARTESIAN_POINT ( 'NONE',  ( 86.64996127643055956, -59.99999999999018740, 203.5283718990660304 ) ) ;
#103695=CARTESIAN_POINT ( 'NONE',  ( -56.69921514847198551, -59.99999999999997868, -36.46084757427505707 ) ) ;
#103708=CARTESIAN_POINT ( 'NONE',  ( 36.21250698581494731, -25.65782209074169629, 33.24609087713096756 ) ) ;
#103709=CARTESIAN_POINT ( 'NONE',  ( 2.227375807149031495, -1.734723475976807094E-15, 17.01589776168603407 ) ) ;
#103722=CARTESIAN_POINT ( 'NONE',  ( 92.56714293118520231, -60.00000000000000711, -2.262852274558210475 ) ) ;
#103731=CARTESIAN_POINT ( 'NONE',  ( -72.27031706507756326, -30.00000000000000711, 102.6033500751135108 ) ) ;
#103737=CARTESIAN_POINT ( 'NONE',  ( 82.42550243480754091, -45.27952612892028839, -15.39413152779067495 ) ) ;
#103746=CARTESIAN_POINT ( 'NONE',  ( 79.16640897475440397, -49.90285545602715445, 152.0307613521693213 ) ) ;
#103754=CARTESIAN_POINT ( 'NONE',  ( -96.25446706653225704, -57.62198180035323247, 204.5564252943773340 ) ) ;
#103758=( GEOMETRIC_REPRESENTATION_CONTEXT ( 3 ) GLOBAL_UNCERTAINTY_ASSIGNED_CONTEXT ( ( #2142 ) ) GLOBAL_UNIT_ASSIGNED_CONTEXT ( ( #89430, #55959, #32261 ) ) REPRESENTATION_CONTEXT ( 'NONE', 'WORKASPACE' ) );
#103764=CARTESIAN_POINT ( 'NONE',  ( -3.619505474376166987, -12.72493135072700809, 32.14504651205703567 ) ) ;
#103772=FACE_OUTER_BOUND ( 'NONE', #19739, .T. ) ;
#103774=CARTESIAN_POINT ( 'NONE',  ( 2.261098177828874789, -17.79480199333886148, -37.95484528153015447 ) ) ;
#103775=CARTESIAN_POINT ( 'NONE',  ( -70.24286758344388204, -29.99999999999999645, 96.10628421054605042 ) ) ;
#103779=CARTESIAN_POINT ( 'NONE',  ( 106.6288915411791436, -57.65244875278279579, 200.4099561371844516 ) ) ;
#103780=CARTESIAN_POINT ( 'NONE',  ( 61.30676048588166083, -21.77000062380585632, -22.67053275276132140 ) ) ;
#103784=CARTESIAN_POINT ( 'NONE',  ( -55.48269212579123888, -60.00000000000000711, 86.66456991474446170 ) ) ;
#103788=CARTESIAN_POINT ( 'NONE',  ( -86.37828719965159507, -20.94065575718939698, 181.4663392420019363 ) ) ;
#103797=CARTESIAN_POINT ( 'NONE',  ( -82.42414396666261212, -45.26226855185817044, -15.39094701099094387 ) ) ;
#103801=ORIENTED_EDGE ( 'NONE', *, *, #45141, .F. ) ;
#103806=CARTESIAN_POINT ( 'NONE',  ( 86.74683449613482367, -14.21045842199431242, 20.02856677177719646 ) ) ;
#103807=CARTESIAN_POINT ( 'NONE',  ( -77.21040881692944424, -53.37756037490176908, 143.0221096505717071 ) ) ;
#103811=CARTESIAN_POINT ( 'NONE',  ( 81.34140718358432309, -57.51511421472552144, 200.0314531987298210 ) ) ;
#103832=CARTESIAN_POINT ( 'NONE',  ( -67.91869938964059372, -14.21045842199436571, 108.3284777829519214 ) ) ;
#103833=CARTESIAN_POINT ( 'NONE',  ( 27.75406281153830435, -49.90938140761433317, 34.23113296838447894 ) ) ;
#103838=CARTESIAN_POINT ( 'NONE',  ( -22.67073868809948678, -4.285714285714296246, -11.17734400176827769 ) ) ;
#103846=CARTESIAN_POINT ( 'NONE',  ( 85.46602935900409648, -29.99999999999995026, 174.5920392183242029 ) ) ;
#103848=CARTESIAN_POINT ( 'NONE',  ( 2.377971153322278042E-07, -60.00000000000000000, 39.63907915656436387 ) ) ;
#103849=CARTESIAN_POINT ( 'NONE',  ( 81.59427637599597460, -29.99999999999999645, -6.810622583152962761 ) ) ;
#103863=CARTESIAN_POINT ( 'NONE',  ( 60.67466929282835508, -38.34223859905504384, 98.54665191328351170 ) ) ;
#103867=CARTESIAN_POINT ( 'NONE',  ( 64.12946791427296489, -32.52996445180959029, 80.08306847456309185 ) ) ;
#103871=CARTESIAN_POINT ( 'NONE',  ( -63.92463504160575383, -37.78188829957583295, -33.13005288218677435 ) ) ;
#103879=CARTESIAN_POINT ( 'NONE',  ( 30.62829732754926582, -60.00000000000002842, -35.06421439060901690 ) ) ;
#103885=CARTESIAN_POINT ( 'NONE',  ( 86.89257692234927788, -42.78194120415572144, 189.7856798060613528 ) ) ;
#103890=CARTESIAN_POINT ( 'NONE',  ( 27.88494491742561721, -20.99829245791718790, -32.55451976490055443 ) ) ;
#103894=EDGE_LOOP ( 'NONE', ( #87898, #72668, #62956, #58065, #24811, #45995, #64299, #76263, #12502, #84527, #70554 ) ) ;
#103898=CARTESIAN_POINT ( 'NONE',  ( -99.15767263151849420, -29.99999999999998934, 188.4520339999081671 ) ) ;
#103901=CARTESIAN_POINT ( 'NONE',  ( 32.03033611666798919, -57.68913864069202191, 46.57911711074292782 ) ) ;
#103914=CARTESIAN_POINT ( 'NONE',  ( -14.34294123642693997, -25.55009647558605224, 28.25866928844338588 ) ) ;
#103915=CARTESIAN_POINT ( 'NONE',  ( -106.1474143027046324, -59.99999999999999289, 180.7708242920181476 ) ) ;
#103922=EDGE_CURVE ( 'NONE', #39827, #53391, #89834, .T. ) ;
#103924=CARTESIAN_POINT ( 'NONE',  ( 72.06213202562246067, -59.99999999999999289, 154.7422713602608724 ) ) ;
#103930=CARTESIAN_POINT ( 'NONE',  ( 51.84565611112584804, -38.00000000000000711, 53.44666998630373911 ) ) ;
#103945=CARTESIAN_POINT ( 'NONE',  ( -90.78562293538325889, -60.00000000002675904, 204.6252288958342263 ) ) ;
#103947=CARTESIAN_POINT ( 'NONE',  ( 72.43113064393337197, -59.99999999999998579, 157.5155133769252416 ) ) ;
#103951=CARTESIAN_POINT ( 'NONE',  ( -99.89444227931625164, -30.00000000000003197, 96.08249125629401988 ) ) ;
#103952=CARTESIAN_POINT ( 'NONE',  ( 11.24629686663563888, -32.51060762582239505, 29.33386000569823793 ) ) ;
#103954=CARTESIAN_POINT ( 'NONE',  ( -48.56021830926045624, -18.75688510409356979, 42.04449221851854901 ) ) ;
#103963=CARTESIAN_POINT ( 'NONE',  ( 90.70307972239879746, -30.00000000003412381, 199.4269904992890758 ) ) ;
#103968=CARTESIAN_POINT ( 'NONE',  ( 99.07418092138790655, -30.00000000000000000, 188.6523126474757532 ) ) ;
#103984=CARTESIAN_POINT ( 'NONE',  ( 105.2440405677593276, -38.38944072604935798, 197.2348950601119668 ) ) ;
#103986=CARTESIAN_POINT ( 'NONE',  ( 85.00044501559656851, -52.70739042385801554, 7.105829972696751540 ) ) ;
#104003=CARTESIAN_POINT ( 'NONE',  ( -40.11045082424308816, -37.66163030632180408, 50.00889850192834274 ) ) ;
#104008=CARTESIAN_POINT ( 'NONE',  ( 84.74745017207317233, -42.96139324155009831, 184.9190875993280656 ) ) ;
#104013=CARTESIAN_POINT ( 'NONE',  ( 94.19019775188388621, -57.67257497933957922, 22.53043024018837315 ) ) ;
#104023=CARTESIAN_POINT ( 'NONE',  ( 36.18613319579441878, -24.61962019850594885, 33.95388689007886285 ) ) ;
#104029=CARTESIAN_POINT ( 'NONE',  ( -33.85941220253381800, -31.37761359142308137, -29.86486766534904902 ) ) ;
#104031=CARTESIAN_POINT ( 'NONE',  ( -83.17519967775672285, -38.00000000000002132, -9.623065349217405640 ) ) ;
#104039=CARTESIAN_POINT ( 'NONE',  ( -34.26200826892031870, -21.77016632158549569, -28.20174604461301016 ) ) ;
#104040=ADVANCED_FACE ( 'NONE', ( #51998 ), #48762, .T. ) ;
#104050=CARTESIAN_POINT ( 'NONE',  ( -92.65510230062061225, -60.00000000000000000, -3.796815982375457477 ) ) ;
#104057=CARTESIAN_POINT ( 'NONE',  ( -81.73723767783293681, -49.95509653891984669, 174.6705688511061396 ) ) ;
#104059=CARTESIAN_POINT ( 'NONE',  ( -16.90652009647373077, -0.000000000000000000, -2.220657265743024134 ) ) ;
#104069=CARTESIAN_POINT ( 'NONE',  ( -82.32950074003311158, -57.52534511946047502, 200.7509962287250573 ) ) ;
#104074=CARTESIAN_POINT ( 'NONE',  ( 86.55961277372783513, -14.21045842199431597, 7.754469001180375187 ) ) ;
#104076=CARTESIAN_POINT ( 'NONE',  ( -55.44100834966593538, -14.21045842199449361, 70.81055559928208254 ) ) ;
#104077=CARTESIAN_POINT ( 'NONE',  ( -53.90679042101523777, -60.32124336610769433, 66.32078629646572665 ) ) ;
#104082=CARTESIAN_POINT ( 'NONE',  ( -99.83212472546227900, -45.25428798288277221, 192.7520070752582626 ) ) ;
#104088=CARTESIAN_POINT ( 'NONE',  ( 108.5726971398995886, -38.35682900653360150, 191.4692688943128474 ) ) ;
#104098=CARTESIAN_POINT ( 'NONE',  ( -27.46968486408479393, -42.96035443980599666, 32.94799843992185373 ) ) ;
#104101=CARTESIAN_POINT ( 'NONE',  ( 47.91978359059700665, -53.35808289020361883, 51.77896845157469841 ) ) ;
#104104=CARTESIAN_POINT ( 'NONE',  ( -110.8309764612567818, -38.35617722019826203, 166.2611764703423489 ) ) ;
#104106=CARTESIAN_POINT ( 'NONE',  ( 91.36700694265483946, -38.39761548113196454, -9.638155343660422147 ) ) ;
#104114=CARTESIAN_POINT ( 'NONE',  ( 86.89686805065835529, -59.99999999999999289, 200.9617660479750896 ) ) ;
#104119=CARTESIAN_POINT ( 'NONE',  ( 55.54612012703360335, -42.96652821328475369, 62.92581338446308337 ) ) ;
#104127=CARTESIAN_POINT ( 'NONE',  ( -101.2596523789430734, -38.35544838490221053, 95.56470404527684082 ) ) ;
#104138=CARTESIAN_POINT ( 'NONE',  ( 85.21594557227290068, -22.03823677191263997, 162.9487912823339002 ) ) ;
#104154=CARTESIAN_POINT ( 'NONE',  ( -0.3592832422766795153, -18.03253741398754428, 35.00534045900273128 ) ) ;
#104178=CARTESIAN_POINT ( 'NONE',  ( -106.7033407227921771, -60.00000000000000711, 120.7809815305387815 ) ) ;
#104182=CARTESIAN_POINT ( 'NONE',  ( -84.74376759734492737, -35.85438675842900835, 179.5104609505815745 ) ) ;
#104190=CARTESIAN_POINT ( 'NONE',  ( -84.91794694852686121, -52.70031527363017432, 9.720178435334927869 ) ) ;
#104194=SURFACE_STYLE_FILL_AREA ( #38950 ) ;
#104196=CARTESIAN_POINT ( 'NONE',  ( 78.64960161195060095, -14.21045842199435860, 174.1843170503133251 ) ) ;
#104197=ADVANCED_FACE ( 'NONE', ( #52835 ), #77754, .T. ) ;
#104198=CARTESIAN_POINT ( 'NONE',  ( -112.5893510171550105, -59.99999999999995026, 145.0943965991558002 ) ) ;
#104199=CARTESIAN_POINT ( 'NONE',  ( -64.58854662160332794, -36.00888594457155989, 83.18360510322872869 ) ) ;
#104202=CARTESIAN_POINT ( 'NONE',  ( 72.64833377984137996, -60.00000000001470113, 181.7429652714145334 ) ) ;
#104214=CARTESIAN_POINT ( 'NONE',  ( -38.87179246869587246, -59.99999999999997868, -39.79893131892280422 ) ) ;
#104223=CARTESIAN_POINT ( 'NONE',  ( 103.5194293720434047, -60.00000000000000000, 191.8575224287939136 ) ) ;
#104227=CARTESIAN_POINT ( 'NONE',  ( 37.15806814115364176, -42.96900667323284040, 37.34969296406126915 ) ) ;
#104229=CARTESIAN_POINT ( 'NONE',  ( 2.910977163135976653, -8.673617379884035472E-16, -22.23822744035697241 ) ) ;
#104245=CARTESIAN_POINT ( 'NONE',  ( 93.27314801925561483, -59.99999999999999289, 34.94592296014532451 ) ) ;
#104251=CARTESIAN_POINT ( 'NONE',  ( -90.09582030224672167, -29.99999999995693400, -6.009880044648006958 ) ) ;
#104258=CARTESIAN_POINT ( 'NONE',  ( 84.35043940098535131, -60.17546792520573007, -17.01487635743571758 ) ) ;
#104268=CARTESIAN_POINT ( 'NONE',  ( 78.86428744248468092, -49.90252285640023899, 149.9481409427032474 ) ) ;
#104269=B_SPLINE_CURVE_WITH_KNOTS ( 'NONE', 3,
 ( #54240, #78018, #71501, #46185, #87711, #13793, #5196, #5712, #4134, #103871, #62382, #86667, #30550, #12736, #45658, #30020, #69931, #78539, #61858, #79077, #63447, #94754, #20903, #53738, #4668, #37602, #70464, #87184, #29508, #38127, #62906, #21932, #2124, #35077, #34552, #91700, #42599, #52279, #17813, #85191, #51747, #67946, #44211, #91180, #51209, #36154, #18356, #58804, #75495, #76552, #77097, #11276, #59874, #25396, #68491, #58252, #27532, #100827, #50160, #1591, #26996, #2664, #3216, #67426, #26464, #92747, #10750, #69026, #60410, #18903, #50664, #83580, #100303, #59331, #84129, #17285, #93289, #10228, #9689, #34017, #76026, #92202, #84665, #43144, #83065, #9158, #42066, #43664, #25945, #35615, #101379, #19448, #74953, #1044, #66889, #99776, #13937, #70606, #69549, #78156, #4808, #87856, #29137, #101899, #93819, #103500, #22072, #19974, #37746, #52821, #79748, #28059, #3754, #85747, #54930, #13407, #11817, #70073 ),
 .UNSPECIFIED., .F., .F.,
 ( 4, 2, 2, 2, 1, 2, 2, 2, 2, 1, 1, 2, 2, 2, 2, 2, 1, 1, 1, 1, 2, 2, 2, 2, 1, 1, 1, 2, 2, 1, 2, 2, 1, 1, 1, 1, 2, 2, 2, 1, 2, 2, 1, 1, 1, 2, 2, 1, 1, 2, 2, 1, 1, 1, 2, 2, 2, 2, 1, 1, 1, 1, 1, 2, 2, 2, 1, 2, 2, 2, 2, 2, 1, 1, 4 ),
 ( 0.000000000000000000, 0.03109947195041606882, 0.06219894390083216540, 0.06608637789463417400, 0.06997381188843615485, 0.07774867987604017205, 0.09329841585124813708, 0.1243978878016639561, 0.1263416047985648771, 0.1282853217954657843, 0.1321727557892676541, 0.1399476237768715048, 0.1554973597520793449, 0.1865968317024948031, 0.1870827609517200507, 0.1875686902009452983, 0.1885405486993957380, 0.1904842656962965064, 0.1943716996900981542, 0.2021465676777013665, 0.2176963036529078188, 0.2487957756033205292, 0.2497676341017708856, 0.2507394926002212143, 0.2526832095971218162, 0.2565706435909231309, 0.2643455115785259824, 0.2798952475537313522, 0.3109947195041422030, 0.3119665780025925317, 0.3124525072518176683, 0.3125132484079708450, 0.3125739895641240218, 0.3126954718764308749, 0.3129384365010439151, 0.3148821534979506787, 0.3187695874917642058, 0.3265444554793912602, 0.3420941914546455909, 0.3430660499530990282, 0.3435519792023257746, 0.3437949438269390368, 0.3440379084515524100, 0.3459816254484592846, 0.3498690594422732003, 0.3576439274299010873, 0.3731936634051568613, 0.3741655219036103541, 0.3746514511528371005, 0.3748944157774504737, 0.3750158980897572714, 0.3751373804020640135, 0.3770810973989722759, 0.3809685313927887451, 0.3887433993804217947, 0.4042931353556878937, 0.4062368523525962116, 0.4064798169772098069, 0.4067227816018233466, 0.4072087108510503706, 0.4081805693495044740, 0.4120680033433208878, 0.4198428713309536042, 0.4353926073062189817, 0.4373363243031271330, 0.4383081828015812365, 0.4392800413000353399, 0.4431674752938518091, 0.4509423432814846366, 0.4664920792567503471, 0.4684357962536586095, 0.4703795132505668164, 0.4742669472443832301, 0.4820418152320161131, 0.4975915512072818236 ),
 .UNSPECIFIED. ) ;
#104277=CARTESIAN_POINT ( 'NONE',  ( 4.154708322984369194E-08, -57.67120202538961138, 41.61186700422869933 ) ) ;
#104283=CARTESIAN_POINT ( 'NONE',  ( -19.58630244784536956, -16.93174034405112494, 31.48444303673279165 ) ) ;
#104284=CARTESIAN_POINT ( 'NONE',  ( -2.499999999981197707, -21.99834632368703069, -30.53960193249073640 ) ) ;
#104285=CARTESIAN_POINT ( 'NONE',  ( -0.8333333325078958742, -30.00000000000000355, -31.89470688134987597 ) ) ;
#104295=CARTESIAN_POINT ( 'NONE',  ( -73.92168396121962815, -30.09624395831016841, -28.12708220521432878 ) ) ;
#104296=CARTESIAN_POINT ( 'NONE',  ( -70.11123173094190975, -29.99999999999999645, 95.68224316551422248 ) ) ;
#104301=CARTESIAN_POINT ( 'NONE',  ( 107.1778406945288822, -57.65541713316640937, 199.8906253976937251 ) ) ;
#104302=CARTESIAN_POINT ( 'NONE',  ( 72.01055813165709196, -21.77032294813915314, -18.48580111295489914 ) ) ;
#104308=CARTESIAN_POINT ( 'NONE',  ( -75.40897020374366377, -60.00000000000000711, 183.9572039174722988 ) ) ;
#104314=CARTESIAN_POINT ( 'NONE',  ( -84.47662886974657681, -57.45685610910329899, 191.4181384606809218 ) ) ;
#104317=VECTOR ( 'NONE', #56295, 1000.000000000000000 ) ;
#104320=EDGE_CURVE ( 'NONE', #74273, #34458, #72143, .T. ) ;
#104322=CARTESIAN_POINT ( 'NONE',  ( -82.37491455164230558, -37.78085970200692145, -12.96758841603934798 ) ) ;
#104329=CARTESIAN_POINT ( 'NONE',  ( 89.66801957890137942, -59.99999999999992895, -23.31517609469964469 ) ) ;
#104330=CARTESIAN_POINT ( 'NONE',  ( -78.49245547457638850, -53.37694864719454557, 151.3764068736151955 ) ) ;
#104332=CARTESIAN_POINT ( 'NONE',  ( 12.27067942234224418, -14.21045842199423959, 34.40196113412964962 ) ) ;
#104334=CARTESIAN_POINT ( 'NONE',  ( 73.26562775815939688, -57.64134225645462806, 183.1174502722914781 ) ) ;
#104341=FACE_OUTER_BOUND ( 'NONE', #71842, .T. ) ;
#104342=CARTESIAN_POINT ( 'NONE',  ( -101.1105981715984683, -52.71026112637824923, 130.0485633398400864 ) ) ;
#104344=( BOUNDED_CURVE ( )  B_SPLINE_CURVE ( 2, ( #8720, #106337, #1132 ),
 .UNSPECIFIED., .F., .F. ) 
 B_SPLINE_CURVE_WITH_KNOTS ( ( 3, 3 ),
 ( 0.000000000000000000, 1.000000000000000000 ),
 .UNSPECIFIED. ) 
 CURVE ( )  GEOMETRIC_REPRESENTATION_ITEM ( )  RATIONAL_B_SPLINE_CURVE ( ( 1.000000000000000000, 1.857142857142858317, 1.000000000000000000 ) ) 
 REPRESENTATION_ITEM ( '' )  );
#104357=CARTESIAN_POINT ( 'NONE',  ( 27.61218054589077298, -46.43287580142983728, 33.58888037689876427 ) ) ;
#104369=CARTESIAN_POINT ( 'NONE',  ( 28.51326288413663690, -59.99999999999999289, -41.06723538131018358 ) ) ;
#104371=CARTESIAN_POINT ( 'NONE',  ( 84.25108322389057491, -29.99999999999987566, 163.2339291413038609 ) ) ;
#104396=CARTESIAN_POINT ( 'NONE',  ( -81.39518705382832309, -59.99999999999992184, 184.9064298456866879 ) ) ;
#104397=CARTESIAN_POINT ( 'NONE',  ( 62.26579310671900203, -56.86312895564053349, 87.13878417979945823 ) ) ;
#104409=CARTESIAN_POINT ( 'NONE',  ( -31.68901581506993637, -60.00000000000002132, -34.94011393958808753 ) ) ;
#104411=EDGE_CURVE ( 'NONE', #26612, #105449, #56652, .T. ) ;
#104415=CARTESIAN_POINT ( 'NONE',  ( 86.81478249919962309, -39.10848448064970029, 188.7318862069557781 ) ) ;
#104421=ORIENTED_EDGE ( 'NONE', *, *, #54806, .T. ) ;
#104425=CARTESIAN_POINT ( 'NONE',  ( 39.14272297605699436, -60.00000000000003553, 50.93124313437822082 ) ) ;
#104426=CARTESIAN_POINT ( 'NONE',  ( -100.7945030569529479, -30.00000000000000355, 162.5532351115364236 ) ) ;
#104428=CARTESIAN_POINT ( 'NONE',  ( 35.32811641198794206, -57.69550348741336876, 49.48441236252082831 ) ) ;
#104435=CARTESIAN_POINT ( 'NONE',  ( -1.413758147757360861, -60.00000000000000711, 39.63760611331755257 ) ) ;
#104436=CARTESIAN_POINT ( 'NONE',  ( 11.47105347311152634, -16.49375446481005270, -34.68891165858038761 ) ) ;
#104443=CARTESIAN_POINT ( 'NONE',  ( -10.48329054730247556, -60.36588335206413092, 33.96539373894616176 ) ) ;
#104444=CARTESIAN_POINT ( 'NONE',  ( -87.60448404220831264, -59.99999999999997158, 36.07240305281307258 ) ) ;
#104455=CARTESIAN_POINT ( 'NONE',  ( 72.21310543845304153, -60.00000000000000000, 155.8912871955335788 ) ) ;
#104463=STYLED_ITEM ( 'NONE', ( #45981 ), #36850 ) ;
#104478=CARTESIAN_POINT ( 'NONE',  ( -114.4908978873841647, -60.00000000000980549, 166.8152118193485194 ) ) ;
#104480=CARTESIAN_POINT ( 'NONE',  ( 40.78730011461682636, -60.00000000000002132, 53.21614385487430354 ) ) ;
#104481=CARTESIAN_POINT ( 'NONE',  ( 85.18902050349326771, -60.00000000000000000, -15.68190703514374107 ) ) ;
#104482=CARTESIAN_POINT ( 'NONE',  ( -91.50803816462422446, -30.00000000000001776, 42.72771024551138908 ) ) ;
#104483=CARTESIAN_POINT ( 'NONE',  ( 12.35463245259948906, -35.99170037105584896, 29.94182087016703875 ) ) ;
#104484=CARTESIAN_POINT ( 'NONE',  ( -45.62210685601630900, -49.89848660444781814, 47.30625596735477956 ) ) ;
#104498=CARTESIAN_POINT ( 'NONE',  ( 103.5655738155463581, -30.00000000000023093, 196.9807721782169097 ) ) ;
#104503=CARTESIAN_POINT ( 'NONE',  ( 97.34229447618668019, -30.00000000000000000, 190.9596792136885597 ) ) ;
#104512=CARTESIAN_POINT ( 'NONE',  ( -79.35676939654273099, -38.35606429531669903, -26.89919366358169128 ) ) ;
#104515=CARTESIAN_POINT ( 'NONE',  ( 91.60420904625036087, -38.50451920916797377, 200.9222943262674050 ) ) ;
#104517=CARTESIAN_POINT ( 'NONE',  ( 82.73356237690738624, -37.85693543688039142, 2.979072353819682828 ) ) ;
#104518=CARTESIAN_POINT ( 'NONE',  ( 84.34874083255445498, -38.00000000000004974, 179.1776475100507184 ) ) ;
#104538=CARTESIAN_POINT ( 'NONE',  ( 32.10152049993604351, -25.19009005012509306, 40.01174804926688466 ) ) ;
#104545=CARTESIAN_POINT ( 'NONE',  ( 85.96484678228922860, -28.40575032613359951, 181.6661039577698773 ) ) ;
#104549=CARTESIAN_POINT ( 'NONE',  ( 94.28774462368049569, -57.67244037246990729, 24.05690785289403522 ) ) ;
#104565=CARTESIAN_POINT ( 'NONE',  ( -102.0812981579065735, -37.99999999999997868, 157.7097999441383251 ) ) ;
#104571=CARTESIAN_POINT ( 'NONE',  ( -10.35119932786764174, -16.29280028192038898, -34.78455815056601352 ) ) ;
#104573=CARTESIAN_POINT ( 'NONE',  ( -37.82507325719418390, -34.58951407227882413, -29.84568773776970474 ) ) ;
#104581=CARTESIAN_POINT ( 'NONE',  ( -92.68008335882309723, -60.00000000000002132, -4.308470193755781885 ) ) ;
#104585=CARTESIAN_POINT ( 'NONE',  ( 99.94675357384078040, -52.77032261955505277, 194.2389869445230772 ) ) ;
#104588=CARTESIAN_POINT ( 'NONE',  ( -80.02865028407020986, -53.38608073763546713, 163.9029365645991163 ) ) ;
#104600=CARTESIAN_POINT ( 'NONE',  ( -93.14832842661381562, -57.61817439972283239, 204.4570750068989469 ) ) ;
#104608=CARTESIAN_POINT ( 'NONE',  ( 87.24803233485737053, -14.21045842199430709, -0.3983294879921217557 ) ) ;
#104610=CARTESIAN_POINT ( 'NONE',  ( -40.90223414571102012, -60.00000000000005684, 57.82070650035302606 ) ) ;
#104611=CARTESIAN_POINT ( 'NONE',  ( -51.55243906946975585, -49.90950515671671184, 57.17738528615195293 ) ) ;
#104617=CARTESIAN_POINT ( 'NONE',  ( -102.1345869732698191, -60.20522555469838011, 194.0426171803833029 ) ) ;
#104622=CARTESIAN_POINT ( 'NONE',  ( 88.43115089625497660, -38.37427755674787022, -18.98099822564858385 ) ) ;
#104635=CARTESIAN_POINT ( 'NONE',  ( 49.49069524382411345, -46.43876033542694159, 52.19611476058279464 ) ) ;
#104638=CARTESIAN_POINT ( 'NONE',  ( -110.9980754224539368, -38.35624728847308518, 173.2928619168303896 ) ) ;
#104641=CARTESIAN_POINT ( 'NONE',  ( 91.20265291891645631, -38.35752600691088077, -0.7216000038766476887 ) ) ;
#104644=CARTESIAN_POINT ( 'NONE',  ( 96.73119497196310590, -60.15121125156788651, 95.89194316550425867 ) ) ;
#104651=CARTESIAN_POINT ( 'NONE',  ( 95.26165383619279226, -60.00000000000000711, 202.5694694144836205 ) ) ;
#104655=CARTESIAN_POINT ( 'NONE',  ( 56.58617729883268765, -39.49445358650807947, 63.80126640809557870 ) ) ;
#104661=CARTESIAN_POINT ( 'NONE',  ( -109.1755639416890773, -38.35617105290818074, 189.5517844986839293 ) ) ;
#104673=CARTESIAN_POINT ( 'NONE',  ( 81.50921258790607737, -57.01699942316916747, 182.3434811776381252 ) ) ;
#104712=CARTESIAN_POINT ( 'NONE',  ( -112.1936433325827522, -60.00000000000000000, 169.7638481750816197 ) ) ;
#104713=PLANE ( 'NONE',  #104870 ) ;
#104719=CARTESIAN_POINT ( 'NONE',  ( -83.65218577006966427, -39.46595630469712290, 175.6988558114236980 ) ) ;
#104726=CARTESIAN_POINT ( 'NONE',  ( -86.28082192411680751, -60.14685432405564569, 19.04948843146160442 ) ) ;
#104734=CARTESIAN_POINT ( 'NONE',  ( 96.06638400950703272, -14.21045842199450426, 198.0643409056117434 ) ) ;
#104736=CARTESIAN_POINT ( 'NONE',  ( -91.97835729869039767, -14.21045842199439591, 64.70454208516892436 ) ) ;
#104737=CARTESIAN_POINT ( 'NONE',  ( -67.15909898532748912, -22.10498377052748964, 83.34062656716834283 ) ) ;
#104740=CARTESIAN_POINT ( 'NONE',  ( 57.63154298134735853, -59.99999999998056666, 100.7219984684233367 ) ) ;
#104742=CARTESIAN_POINT ( 'NONE',  ( 1.980960943318600176, -22.06722745478349168, 27.56539235055124948 ) ) ;
#104751=CARTESIAN_POINT ( 'NONE',  ( -104.6983220124084397, -60.00000000000001421, 108.3235972286209261 ) ) ;
#104762=CARTESIAN_POINT ( 'NONE',  ( -37.36874049225535543, -25.67000572301214945, 33.86699708943749698 ) ) ;
#104767=CARTESIAN_POINT ( 'NONE',  ( 41.58657417432790737, -49.88673011520329936, 42.49169459770972423 ) ) ;
#104768=CARTESIAN_POINT ( 'NONE',  ( -10.45706415777455689, -1.734723475976807094E-15, -13.60704923275582701 ) ) ;
#104773=CARTESIAN_POINT ( 'NONE',  ( -73.67975493303866585, -38.32615326775285780, 157.6922298713693067 ) ) ;
#104784=CARTESIAN_POINT ( 'NONE',  ( 95.45921739354632507, -60.00000000000001421, 52.31160816427112792 ) ) ;
#104791=CARTESIAN_POINT ( 'NONE',  ( -88.03351418313572196, -29.99999999999498002, -16.96970854458511724 ) ) ;
#104808=CARTESIAN_POINT ( 'NONE',  ( 80.62625263358452798, -46.43735505546275988, 158.8973765016157813 ) ) ;
#104815=CARTESIAN_POINT ( 'NONE',  ( -57.91314980999670325, -57.67646044164155228, 100.3416927154360536 ) ) ;
#104816=B_SPLINE_SURFACE_WITH_KNOTS ( 'NONE', 3, 3, ( 
 ( #70364, #88144, #87087, #104302 ),
 ( #103259, #47657, #63346, #55733 ),
 ( #73916, #14224, #32966, #78973 ),
 ( #38540, #106785, #24870, #79506 ),
 ( #12633, #21839, #6138, #96243 ),
 ( #62287, #22373, #95178, #8123 ),
 ( #21309, #13162, #62808, #65837 ),
 ( #70888, #98717, #41035, #46090 ),
 ( #54678, #39066, #86570, #103780 ),
 ( #29922, #55217, #71947, #95697 ),
 ( #87615, #104851, #30994, #63876 ),
 ( #45567, #96765, #78439, #49646 ),
 ( #92767, #91200, #51227, #82554 ),
 ( #100324, #75519, #9710, #43165 ),
 ( #524, #35100, #34039, #90649 ),
 ( #84153, #33487, #68511, #42620 ),
 ( #16755, #2148, #9173, #83086 ),
 ( #66365, #99247, #1613, #27016 ),
 ( #84684, #74975, #18376, #10252 ),
 ( #34575, #50686, #8655, #76046 ),
 ( #67448, #17839, #58273, #59360 ),
 ( #2690, #50180, #42086, #83604 ),
 ( #101403, #26485, #74445, #41562 ),
 ( #92222, #58826, #25415, #59895 ),
 ( #91718, #17307, #67966, #1065 ),
 ( #66912, #99796, #18928, #100857 ),
 ( #51770, #10769, #25967, #43687 ),
 ( #76575, #35641, #57727, #12896 ),
 ( #45300, #12374, #53385, #103517 ),
 ( #78180, #45825, #29156, #38285 ),
 ( #78697, #102464, #13429, #60955 ),
 ( #93312, #77662, #4829, #3775 ),
 ( #86302, #4297, #21566, #101921 ),
 ( #69047, #5367, #62541, #93840 ),
 ( #71149, #36710, #28611, #62028 ),
 ( #60436, #46350, #70093, #70627 ),
 ( #94384, #37232, #79240, #53897 ),
 ( #27557, #21058, #37764, #61494 ),
 ( #20003, #102997, #87352, #29671 ),
 ( #94921, #86827, #95428, #54407 ),
 ( #28081, #69574, #19468, #20546 ),
 ( #52304, #85213, #11303, #44232 ),
 ( #52844, #77122, #3235, #36179 ),
 ( #85768, #11842, #44773, #6400 ),
 ( #106153, #46869, #57075, #81873 ),
 ( #105633, #38796, #32309, #56538 ),
 ( #98075, #31774, #72216, #47916 ),
 ( #7999, #40908, #63070, #104039 ),
 ( #105118, #30178, #104573, #23158 ),
 ( #95970, #31260, #64146, #22094 ),
 ( #23693, #40371, #80287, #54949 ),
 ( #97016, #87877, #64654, #30727 ),
 ( #47394, #13959, #65182, #80824 ),
 ( #6937, #89990, #97529, #48978 ),
 ( #88410, #55994, #16097, #79767 ),
 ( #5872, #71666, #39335, #89469 ),
 ( #88935, #63614, #15026, #96503 ),
 ( #15563, #22638, #55473, #39858 ),
 ( #72731, #14481, #48452, #81345 ),
 ( #7457, #73250, #24227, #73795 ),
 ( #51648, #32842, #84572, #41965 ),
 ( #25842, #34454, #106692, #18251 ),
 ( #99124, #65719, #49521, #8529 ),
 ( #43044, #57598, #100733, #91075 ),
 ( #24751, #75395, #74326, #58700 ),
 ( #90521, #34979, #17709, #75932 ),
 ( #59769, #1492, #18804, #66241 ) ),
 .UNSPECIFIED., .F., .F., .F.,
 ( 4, 3, 3, 3, 3, 3, 3, 3, 3, 3, 3, 3, 3, 3, 3, 3, 3, 3, 3, 3, 3, 3, 4 ),
 ( 4, 4 ),
 ( 0.4267139204576358424, 0.4312935645218702874, 0.4358732085861046768, 0.4404528526503390662, 0.4450324967145734556, 0.4541917848430422344, 0.4633510729715110132, 0.4725103610999797921, 0.4816696492284485709, 0.4908289373569173497, 0.4954085814211517391, 0.4999882254853861285, 0.5045678695496205179, 0.5091475136138550184, 0.5183068017423237972, 0.5274660898707925760, 0.5366253779992613548, 0.5457846661277301337, 0.5549439542561989125, 0.5595235983204333019, 0.5641032423846676913, 0.5686828864489020807, 0.5732625305131364701 ),
 ( 0.03623606276729821052, 1.318162535682649183 ),
 .UNSPECIFIED. ) ;
#104829=CARTESIAN_POINT ( 'NONE',  ( -11.21238143379541619, -14.07322973648245856, 31.83197821777864078 ) ) ;
#104845=CARTESIAN_POINT ( 'NONE',  ( -62.66006049324404614, -30.00000000000001066, 73.77690815432163163 ) ) ;
#104849=CARTESIAN_POINT ( 'NONE',  ( 92.90827380281179160, -57.61735079984537578, 204.4405232865525477 ) ) ;
#104851=CARTESIAN_POINT ( 'NONE',  ( 59.93292360988266410, -47.40898519424397506, -27.52549038968009043 ) ) ;
#104856=CARTESIAN_POINT ( 'NONE',  ( -72.92009701100754171, -59.99999999999999289, 161.7471689223172007 ) ) ;
#104861=CARTESIAN_POINT ( 'NONE',  ( -85.22359929980800075, -42.93809111955054192, 186.3718570108496237 ) ) ;
#104870=AXIS2_PLACEMENT_3D ( 'NONE', #21711, #13035, #96634 ) ;
#104884=CARTESIAN_POINT ( 'NONE',  ( 92.19440588371723777, -59.99999999999994316, -19.86251273113072102 ) ) ;
#104885=CARTESIAN_POINT ( 'NONE',  ( -77.88326922906453831, -53.37685894332580716, 147.1956358302255410 ) ) ;
#104887=CARTESIAN_POINT ( 'NONE',  ( 35.98705420554111356, -30.00000000000000355, 43.73599804831894033 ) ) ;
#104888=CARTESIAN_POINT ( 'NONE',  ( 73.06332208692298025, -57.64923196330578037, 181.6867478007702630 ) ) ;
#104898=CARTESIAN_POINT ( 'NONE',  ( -103.0586439431804564, -60.15481352663451986, 134.7074848548440400 ) ) ;
#104910=CARTESIAN_POINT ( 'NONE',  ( -21.36131896786188378, -60.00000000000002132, 42.72829597934922674 ) ) ;
#104911=CARTESIAN_POINT ( 'NONE',  ( 27.49024895849569106, -29.05222164557826758, 30.53773838945769725 ) ) ;
#104926=CARTESIAN_POINT ( 'NONE',  ( 32.09297087671797755, -60.00000000000002132, -40.66494470579936404 ) ) ;
#104927=CARTESIAN_POINT ( 'NONE',  ( 88.81459683227794244, -29.99999999999995737, 188.4117534872304418 ) ) ;
#104946=FILL_AREA_STYLE_COLOUR ( '', #69434 ) ;
#104951=CARTESIAN_POINT ( 'NONE',  ( 64.69054239873878487, -29.05368727968382458, 79.89853205579872508 ) ) ;
#104957=AXIS2_PLACEMENT_3D ( 'NONE', #64034, #97964, #56424 ) ;
#104959=AXIS2_PLACEMENT_3D ( 'NONE', #50634, #18872, #66314 ) ;
#104962=CARTESIAN_POINT ( 'NONE',  ( 86.68877158589015153, -20.67351136403616962, 184.9441422176963385 ) ) ;
#104973=CARTESIAN_POINT ( 'NONE',  ( 17.37359531700059634, -60.00000000000000711, 39.95162597743414068 ) ) ;
#104974=CARTESIAN_POINT ( 'NONE',  ( -100.7567655553329757, -29.99999999999999645, 180.7204987279467048 ) ) ;
#104977=CARTESIAN_POINT ( 'NONE',  ( 36.41245709655431284, -57.69609435492582605, 50.68243955302485659 ) ) ;
#104984=CARTESIAN_POINT ( 'NONE',  ( -20.99456667357952000, -60.00000000000000000, 40.35920817678867678 ) ) ;
#104985=CARTESIAN_POINT ( 'NONE',  ( 0.4783642039767228016, -15.39516892388123637, -35.22788256086853664 ) ) ;
#104990=CARTESIAN_POINT ( 'NONE',  ( -12.53346734362791359, -49.92094994888364567, 32.26888292110559320 ) ) ;
#104991=CARTESIAN_POINT ( 'NONE',  ( -86.83940835675045378, -60.00000000000007105, -10.29891589400428309 ) ) ;
#105001=CARTESIAN_POINT ( 'NONE',  ( 72.06473877601102629, -59.99999999999999289, 154.7618788949081932 ) ) ;
#105006=CARTESIAN_POINT ( 'NONE',  ( 1.363418823244991529, -14.21045842199435150, 34.36840973699906954 ) ) ;
#105022=CARTESIAN_POINT ( 'NONE',  ( -108.4957846533182675, -60.00000000000615330, 199.0410807392527772 ) ) ;
#105025=CARTESIAN_POINT ( 'NONE',  ( 84.31499252833064872, -60.00000000000002132, 199.6929933629102152 ) ) ;
#105028=CARTESIAN_POINT ( 'NONE',  ( -109.4306967521916221, -29.99999999999999645, 166.0290040158848797 ) ) ;
#105029=CARTESIAN_POINT ( 'NONE',  ( 13.76622771894575514, -60.35868451098616561, 34.04349415497945586 ) ) ;
#105030=CARTESIAN_POINT ( 'NONE',  ( 82.55399726781115533, -38.00000000000001421, 6.763662827364390395 ) ) ;
#105033=CARTESIAN_POINT ( 'NONE',  ( -44.20937707563757613, -53.34858502187538676, 46.33038334879231712 ) ) ;
#105045=CARTESIAN_POINT ( 'NONE',  ( 106.6412839208548036, -30.00000000000165912, 192.5192194241506627 ) ) ;
#105049=CARTESIAN_POINT ( 'NONE',  ( 87.55810224661499319, -30.00000000000000711, 73.94386861778465914 ) ) ;
#105065=CARTESIAN_POINT ( 'NONE',  ( 78.47953390179775113, -38.63294422717142851, 189.6624935433154349 ) ) ;
#105067=CARTESIAN_POINT ( 'NONE',  ( 84.14018061964620188, -45.28747372694517281, 0.6296579836999579571 ) ) ;
#105068=CARTESIAN_POINT ( 'NONE',  ( 84.14737378976931836, -37.99999999999996447, 177.7231074054740532 ) ) ;
#105084=PRESENTATION_STYLE_ASSIGNMENT (( #41397 ) ) ;
#105090=CARTESIAN_POINT ( 'NONE',  ( 86.24358644654743955, -21.22751543189874468, 178.4789263468928766 ) ) ;
#105095=CARTESIAN_POINT ( 'NONE',  ( 93.83744002707871346, -57.67473800415772445, 11.12884359937129730 ) ) ;
#105108=CARTESIAN_POINT ( 'NONE',  ( -25.43785777808176718, -28.36737569912000367, -30.30737543915739707 ) ) ;
#105110=CARTESIAN_POINT ( 'NONE',  ( -101.4594870179214894, -37.99999999999997868, 151.1679595334590260 ) ) ;
#105115=CARTESIAN_POINT ( 'NONE',  ( -19.58115073825180374, -18.43134085946331169, -33.78044860928109472 ) ) ;
#105118=CARTESIAN_POINT ( 'NONE',  ( -38.79060871343663308, -60.22819976177238743, -34.02320779555699914 ) ) ;
#105126=CARTESIAN_POINT ( 'NONE',  ( -92.63321420215758906, -60.00000000000000711, -3.375781646321903029 ) ) ;
#105128=CARTESIAN_POINT ( 'NONE',  ( 59.83737978852683881, -37.40166281318659003, -25.85311039118933962 ) ) ;
#105129=CARTESIAN_POINT ( 'NONE',  ( 101.3985084166410218, -60.23849521171775478, 194.8049258406955175 ) ) ;
#105133=CARTESIAN_POINT ( 'NONE',  ( -84.79477645726274204, -22.09607886015096767, 158.8527075901939156 ) ) ;
#105142=CARTESIAN_POINT ( 'NONE',  ( -73.72791963761318357, -57.62431822613736898, 185.7849209195708227 ) ) ;
#105148=CARTESIAN_POINT ( 'NONE',  ( -16.35184830034500791, -14.21045842199432663, -36.83529024868766300 ) ) ;
#105149=CARTESIAN_POINT ( 'NONE',  ( -51.40736910322219444, -29.99999999999990052, 68.09419600167673536 ) ) ;
#105150=CARTESIAN_POINT ( 'NONE',  ( -52.51426326109795895, -36.04149165182834480, 53.95691964957212861 ) ) ;
#105155=CARTESIAN_POINT ( 'NONE',  ( -98.11506906225089608, -60.34699860078747236, 196.5395051151577093 ) ) ;
#105159=CARTESIAN_POINT ( 'NONE',  ( 107.2300937431054990, -38.36237930411618180, 194.4693520903244348 ) ) ;
#105164=CARTESIAN_POINT ( 'NONE',  ( 84.60172713863487104, -30.00000000000000355, 166.5370262984466763 ) ) ;
#105173=ORIENTED_EDGE ( 'NONE', *, *, #3409, .T. ) ;
#105174=CARTESIAN_POINT ( 'NONE',  ( 50.22232791766091253, -39.51160255249801878, 51.10789571635989859 ) ) ;
#105178=CARTESIAN_POINT ( 'NONE',  ( -104.7053668603516599, -38.39921602607821427, 197.7787533616209430 ) ) ;
#105181=CARTESIAN_POINT ( 'NONE',  ( 90.74466543776695460, -38.34261519167259991, 6.545665434262897264 ) ) ;
#105184=CARTESIAN_POINT ( 'NONE',  ( 95.60192313703464606, -37.84851270224621800, 111.4288484754221713 ) ) ;
#105189=CARTESIAN_POINT ( 'NONE',  ( 86.93613143775358765, -59.99999999999999289, 200.9776908624942280 ) ) ;
#105190=AXIS2_PLACEMENT_3D ( 'NONE', #22451, #55296, #32659 ) ;
#105194=CARTESIAN_POINT ( 'NONE',  ( 57.77568988088241753, -32.54838333112581239, 63.57324009296404199 ) ) ;
#105201=CARTESIAN_POINT ( 'NONE',  ( -110.5502611048591177, -38.35605075777012019, 160.8838554956551832 ) ) ;
#105212=CARTESIAN_POINT ( 'NONE',  ( 84.00887293287516400, -35.95423091463445076, 173.7886553935154268 ) ) ;
#105252=CARTESIAN_POINT ( 'NONE',  ( -112.1932564010748763, -60.00000000000000711, 169.7459552627697121 ) ) ;
#105257=CARTESIAN_POINT ( 'NONE',  ( -81.50822721619086053, -57.02328051233624961, 182.3449969974295755 ) ) ;
#105271=CARTESIAN_POINT ( 'NONE',  ( 83.90815637317848541, -29.99999999999993605, 196.6622986253035208 ) ) ;
#105273=CARTESIAN_POINT ( 'NONE',  ( -108.9224886339666085, -60.00000000000004263, 119.6925845435806650 ) ) ;
#105274=CARTESIAN_POINT ( 'NONE',  ( -62.87621289667217894, -36.01054220196925115, 78.31231431900522466 ) ) ;
#105277=CARTESIAN_POINT ( 'NONE',  ( 77.05631773205139723, -60.00000000000989075, 196.3100209729188919 ) ) ;
#105279=CARTESIAN_POINT ( 'NONE',  ( 3.020116147952439434, -35.99142716605504688, 29.88345697530386502 ) ) ;
#105287=CARTESIAN_POINT ( 'NONE',  ( -85.23168696672351530, -60.00000000000006395, 200.2110442732997910 ) ) ;
#105298=CARTESIAN_POINT ( 'NONE',  ( -33.47199527190278445, -56.84231303533334057, 37.78255240090093992 ) ) ;
#105302=CARTESIAN_POINT ( 'NONE',  ( 40.33337910916750957, -42.97531841030273370, 39.77847369127800192 ) ) ;
#105304=CARTESIAN_POINT ( 'NONE',  ( -13.66642973270730010, -3.469446951953614189E-15, -17.78317311658304689 ) ) ;
#105307=CARTESIAN_POINT ( 'NONE',  ( -74.85312537499551411, -38.33503454998542992, 168.0912832715343086 ) ) ;
#105318=CARTESIAN_POINT ( 'NONE',  ( 93.06500352313815938, -60.00000000000000000, 32.93591750832660381 ) ) ;
#105325=CARTESIAN_POINT ( 'NONE',  ( -67.63917399235995731, -30.00000000000001066, 87.92849407231595649 ) ) ;
#105338=CARTESIAN_POINT ( 'NONE',  ( 82.67279699970272588, -29.08879217702658337, 151.5812038771563550 ) ) ;
#105348=CARTESIAN_POINT ( 'NONE',  ( -52.60809588292248407, -57.67627119646954981, 84.38067992663381744 ) ) ;
#105362=CARTESIAN_POINT ( 'NONE',  ( -20.36232553423073810, -17.25202226850461784, 31.47323143012087954 ) ) ;
#105379=CARTESIAN_POINT ( 'NONE',  ( 101.9849436419454491, -57.63211355776580547, 203.2755632733008042 ) ) ;
#105384=CARTESIAN_POINT ( 'NONE',  ( -74.81262360460598870, -59.99999999999999289, 179.8084771762270293 ) ) ;
#105388=CARTESIAN_POINT ( 'NONE',  ( -85.87270434792566220, -32.01548043290308243, 183.1783680013945741 ) ) ;
#105395=CARTESIAN_POINT ( 'NONE',  ( -84.13922450232199424, -52.73021857188881967, -15.00297300780911947 ) ) ;
#105404=CARTESIAN_POINT ( 'NONE',  ( 94.69963775048552179, -60.00000000000009948, 1.032162584924374293 ) ) ;
#105405=CARTESIAN_POINT ( 'NONE',  ( -73.66749217889153556, -56.85450343998585510, 127.7611477684293391 ) ) ;
#105407=CARTESIAN_POINT ( 'NONE',  ( 48.02079947780210745, -30.00000000000000711, 60.50169175835635826 ) ) ;
#105409=CARTESIAN_POINT ( 'NONE',  ( 77.56974481787175080, -57.51673336786241464, 195.9651212718508475 ) ) ;
#105418=CARTESIAN_POINT ( 'NONE',  ( -99.35947654427663167, -37.82049538106502951, 135.1392028905823111 ) ) ;
#105431=CARTESIAN_POINT ( 'NONE',  ( 29.45595439878422184, -32.53657559208932071, 31.71262922621859204 ) ) ;
#105444=CARTESIAN_POINT ( 'NONE',  ( 57.01351239614803745, -60.00000000000001421, -36.42612028841926275 ) ) ;
#105449=VERTEX_POINT ( 'NONE', #80173 ) ;
#105467=CARTESIAN_POINT ( 'NONE',  ( -54.47640052782665521, -60.00000000000000000, 67.52253231662828625 ) ) ;
#105468=CARTESIAN_POINT ( 'NONE',  ( 65.92109651114007818, -60.33495006274211647, 100.3550901629334362 ) ) ;
#105474=ORIENTED_EDGE ( 'NONE', *, *, #55213, .F. ) ;
#105478=ADVANCED_FACE ( 'NONE', ( #86320 ), #72617, .F. ) ;
#105493=CARTESIAN_POINT ( 'NONE',  ( 17.04897055569503905, -60.00000000000000711, 39.92612883515686661 ) ) ;
#105494=CARTESIAN_POINT ( 'NONE',  ( -96.99361400851853432, -30.00000000000001066, 191.0864438644175891 ) ) ;
#105497=CARTESIAN_POINT ( 'NONE',  ( 52.36026450593488590, -57.67644934183336147, 83.70945018486365541 ) ) ;
#105505=CARTESIAN_POINT ( 'NONE',  ( -12.42807525731150164, -60.00000000000000711, 39.69786023814224762 ) ) ;
#105507=CARTESIAN_POINT ( 'NONE',  ( -85.66156584027689291, -61.06605174068531028, 194.0559517944926995 ) ) ;
#105510=CARTESIAN_POINT ( 'NONE',  ( -14.88112861571068279, -60.36545018808638474, 34.08850901830101066 ) ) ;
#105511=CARTESIAN_POINT ( 'NONE',  ( -2.499999999999997780, -30.00000000000000000, 14.79019945774903810 ) ) ;
#105523=CARTESIAN_POINT ( 'NONE',  ( 66.11079172910912405, -60.00000000000000000, 122.8458817101759308 ) ) ;
#105528=( NAMED_UNIT ( * ) PLANE_ANGLE_UNIT ( ) SI_UNIT ( $, .RADIAN. ) );
#105541=CARTESIAN_POINT ( 'NONE',  ( -77.30691964702137398, -59.99999999999513989, 196.7061328158951596 ) ) ;
#105544=CARTESIAN_POINT ( 'NONE',  ( 44.97999590490915978, -60.00000000000000000, 60.55235333090226391 ) ) ;
#105547=CARTESIAN_POINT ( 'NONE',  ( -114.5930292407900879, -59.99999999999997868, 172.8116974628616163 ) ) ;
#105548=CARTESIAN_POINT ( 'NONE',  ( 16.37553332807584994, -18.58809198569462495, 27.19376126714132624 ) ) ;
#105550=PLANE ( 'NONE',  #13840 ) ;
#105551=CARTESIAN_POINT ( 'NONE',  ( -47.01439492264584885, -46.44460756023540426, 48.25956263889609232 ) ) ;
#105561=CARTESIAN_POINT ( 'NONE',  ( 103.9866713306733743, -29.99999999999896616, 196.5747536251343206 ) ) ;
#105566=CARTESIAN_POINT ( 'NONE',  ( 100.5837132263118292, -30.00000000000000000, 160.2813360046134505 ) ) ;
#105580=CARTESIAN_POINT ( 'NONE',  ( 82.02875481936112578, -38.83883151105103337, 195.9167761120497460 ) ) ;
#105600=CARTESIAN_POINT ( 'NONE',  ( 43.23783249438958620, -38.30607820824091903, 54.77471611439175092 ) ) ;
#105601=EDGE_CURVE ( 'NONE', #81108, #30000, #60516, .T. ) ;
#105604=CARTESIAN_POINT ( 'NONE',  ( 84.53280797509962952, -50.18428614998399695, 188.2537912682702768 ) ) ;
#105608=CARTESIAN_POINT ( 'NONE',  ( 94.41737687008979663, -57.67086643237934851, -0.3944160041198634947 ) ) ;
#105616=CARTESIAN_POINT ( 'NONE',  ( -83.62938647969347983, -37.99999999999996447, 173.4280063321390060 ) ) ;
#105626=CARTESIAN_POINT ( 'NONE',  ( 67.97786962772167385, -29.92019613139300205, -21.73453229204871207 ) ) ;
#105631=CARTESIAN_POINT ( 'NONE',  ( -1.895665647442401625, -15.39481678902619244, -35.22747512624398780 ) ) ;
#105633=CARTESIAN_POINT ( 'NONE',  ( -29.14298834304714703, -60.22827824258391871, -35.25025982252484624 ) ) ;
#105640=CARTESIAN_POINT ( 'NONE',  ( -92.53829303969855857, -60.00000000000000711, -1.819294454048275167 ) ) ;
#105642=CARTESIAN_POINT ( 'NONE',  ( 6.211901734583654466, -22.42181773049501814, -30.53157825004622694 ) ) ;
#105644=CARTESIAN_POINT ( 'NONE',  ( 99.00120839754166013, -45.26735151141791391, 193.3245999471389212 ) ) ;
#105647=CARTESIAN_POINT ( 'NONE',  ( -84.12721481491040265, -25.59031489470379483, 158.2850513293658423 ) ) ;
#105662=CARTESIAN_POINT ( 'NONE',  ( -112.9456993887476415, -57.67119592114509175, 187.6412086615824535 ) ) ;
#105668=CARTESIAN_POINT ( 'NONE',  ( -60.75193363616918418, -14.21045842199437281, -29.98592940458554779 ) ) ;
#105670=CARTESIAN_POINT ( 'NONE',  ( -52.09024895363909735, -32.57805271825053950, 51.93362379009405316 ) ) ;
#105673=CARTESIAN_POINT ( 'NONE',  ( -96.81022089726320701, -52.81206184454612895, 195.3521687869499601 ) ) ;
#105678=CARTESIAN_POINT ( 'NONE',  ( 110.9724741510028991, -38.35616282069194938, 175.3757637281809423 ) ) ;
#105683=CARTESIAN_POINT ( 'NONE',  ( 85.25163243476666253, -30.00000000000000355, 172.6556488447312177 ) ) ;
#105691=CARTESIAN_POINT ( 'NONE',  ( 50.37465153049131317, -32.58476194434919648, 49.03543699400612610 ) ) ;
#105695=CARTESIAN_POINT ( 'NONE',  ( -110.8996023805193545, -38.35620705874759295, 168.0205389799528461 ) ) ;
#105698=CARTESIAN_POINT ( 'NONE',  ( 92.29851316895251045, -38.35437613414789126, 37.52047800107067133 ) ) ;
#105701=CARTESIAN_POINT ( 'NONE',  ( 100.5956480701022144, -45.28263325919924398, 134.9964452043381016 ) ) ;
#105707=CARTESIAN_POINT ( 'NONE',  ( 80.05528450392095863, -60.00000000000001421, 196.0545680023233501 ) ) ;
#105712=CARTESIAN_POINT ( 'NONE',  ( 58.02861234676127822, -42.96355013425112190, 68.81395379777194421 ) ) ;
#105717=CARTESIAN_POINT ( 'NONE',  ( -77.30345793199742843, -30.00000000002674838, 177.7601236066231536 ) ) ;
#105726=CARTESIAN_POINT ( 'NONE',  ( 82.63461646052759590, -46.48100528357909411, 177.1123106745573637 ) ) ;
#105748=CARTESIAN_POINT ( 'NONE',  ( -19.42089550010631172, -25.33333743194299359, 36.70181951355001360 ) ) ;
#105763=ORIENTED_EDGE ( 'NONE', *, *, #54901, .F. ) ;
#105769=CARTESIAN_POINT ( 'NONE',  ( -112.0884059626418860, -60.00000000000000711, 178.1755789913165984 ) ) ;
#105771=CARTESIAN_POINT ( 'NONE',  ( 6.087340769098095516E-05, -60.36594248999337964, 33.95064037460127793 ) ) ;
#105778=CARTESIAN_POINT ( 'NONE',  ( -83.17772658434090260, -42.98067204979764000, 176.6392034412271528 ) ) ;
#105792=CARTESIAN_POINT ( 'NONE',  ( 114.0746655879125200, -59.99999999999997158, 159.9914145889356121 ) ) ;
#105793=CARTESIAN_POINT ( 'NONE',  ( -113.8519240760089133, -60.00000000000002842, 157.1483645435538108 ) ) ;
#105794=CARTESIAN_POINT ( 'NONE',  ( -63.00954343448449180, -39.48637485122225144, 80.42972209915033943 ) ) ;
#105797=CARTESIAN_POINT ( 'NONE',  ( 113.3142912537098539, -60.00000000000000000, 187.7786430344451674 ) ) ;
#105799=CARTESIAN_POINT ( 'NONE',  ( 4.363475717344336561E-05, -49.91581431533978019, 32.20895234549234232 ) ) ;
#105808=CARTESIAN_POINT ( 'NONE',  ( -87.83100605766939850, -59.99999999999994316, 201.3292211320413401 ) ) ;
#105818=CARTESIAN_POINT ( 'NONE',  ( 103.2567985417785650, -60.00000000000000000, 192.3623435299448090 ) ) ;
#105819=CARTESIAN_POINT ( 'NONE',  ( -34.09410029386582863, -56.83839777928749015, 38.12311633126902422 ) ) ;
#105821=CARTESIAN_POINT ( 'NONE',  ( 39.17175573955607604, -39.51526351848063001, 38.04212958671963207 ) ) ;
#105822=CARTESIAN_POINT ( 'NONE',  ( 2.083846472846741813E-15, -1.734723475976807094E-15, 17.01589776168603407 ) ) ;
#105825=CARTESIAN_POINT ( 'NONE',  ( -73.89011895107292105, -38.32652016529552697, 159.4283385861867259 ) ) ;
#105826=VERTEX_POINT ( 'NONE', #82170 ) ;
#105836=CARTESIAN_POINT ( 'NONE',  ( 95.45595281539657151, -60.00000000000001421, 52.28868166623287550 ) ) ;
#105842=CARTESIAN_POINT ( 'NONE',  ( -88.54670987746852973, -29.99999999999983302, -15.93061657816609333 ) ) ;
#105858=CARTESIAN_POINT ( 'NONE',  ( 83.89881790786340332, -18.68023142264728520, 147.1895477365627585 ) ) ;
#105866=CARTESIAN_POINT ( 'NONE',  ( -42.46252528007325111, -57.68686955033432895, 59.97785686028149854 ) ) ;
#105876=CARTESIAN_POINT ( 'NONE',  ( -11.00522668414577154, -14.01981851350334018, 31.84261960800534297 ) ) ;
#105878=CARTESIAN_POINT ( 'NONE',  ( -2.500000000000011990, -30.00000000000000000, -31.87333704504306908 ) ) ;
#105886=CARTESIAN_POINT ( 'NONE',  ( -62.60825180612043539, -37.65708592411966293, -33.50786494313757657 ) ) ;
#105891=CARTESIAN_POINT ( 'NONE',  ( 106.3456735113185374, -57.65092651592087236, 200.6602391493835285 ) ) ;
#105896=CARTESIAN_POINT ( 'NONE',  ( -74.34434612437654266, -60.00000000000000000, 175.6378450051794573 ) ) ;
#105899=CARTESIAN_POINT ( 'NONE',  ( -85.39200440104596623, -35.72338773939898715, 183.0114852614501331 ) ) ;
#105913=CARTESIAN_POINT ( 'NONE',  ( 2.910977163136224011, -8.673617379884035472E-16, 22.23822744035697241 ) ) ;
#105915=CARTESIAN_POINT ( 'NONE',  ( 88.04031092259528180, -30.00000000000002842, -17.07720529721093072 ) ) ;
#105916=CARTESIAN_POINT ( 'NONE',  ( -78.57144265810380546, -39.49830219292440603, 137.4485770626870362 ) ) ;
#105919=CARTESIAN_POINT ( 'NONE',  ( 34.60434289261801410, -60.00000000000002842, 49.20687062438629056 ) ) ;
#105921=CARTESIAN_POINT ( 'NONE',  ( 93.43194010991950904, -57.65434931037806621, -16.06956276475861145 ) ) ;
#105924=CARTESIAN_POINT ( 'NONE',  ( 0.000000000000000000, -30.00000000000000000, 0.000000000000000000 ) ) ;
#105944=CARTESIAN_POINT ( 'NONE',  ( 29.28785219392642603, -29.06229949932505363, 31.04084042630147877 ) ) ;
#105950=FACE_BOUND ( 'NONE', #41340, .T. ) ;
#105956=CARTESIAN_POINT ( 'NONE',  ( 65.77608706097059610, -60.00000000000001421, -33.96223278568422899 ) ) ;
#105979=CARTESIAN_POINT ( 'NONE',  ( -10.43488688844078993, -60.00000000000002132, 33.89243132277722736 ) ) ;
#105980=CARTESIAN_POINT ( 'NONE',  ( 65.36469853637363769, -29.05439105967825952, 81.83063248125246503 ) ) ;
#105985=CARTESIAN_POINT ( 'NONE',  ( -57.15598917327103834, -57.67115757216583205, -38.38010944898898202 ) ) ;
#106007=CARTESIAN_POINT ( 'NONE',  ( -98.17474337771899684, -29.99999999999999645, 190.3296048190805152 ) ) ;
#106010=CARTESIAN_POINT ( 'NONE',  ( 53.89377858532357379, -57.67595397426320147, 88.10897076158549623 ) ) ;
#106014=CARTESIAN_POINT ( 'NONE',  ( 22.63357787059576864, -26.81694554740444048, -38.43512209275669278 ) ) ;
#106016=CARTESIAN_POINT ( 'NONE',  ( -16.88293466221169581, -60.00000000000001421, 39.91355644712231765 ) ) ;
#106019=CARTESIAN_POINT ( 'NONE',  ( -86.84244699270934120, -46.46287268932884018, 190.7113349457623883 ) ) ;
#106023=CARTESIAN_POINT ( 'NONE',  ( -5.173845848792242741, -60.36574285059159450, 33.93991560295228282 ) ) ;
#106035=CARTESIAN_POINT ( 'NONE',  ( 61.54478197300144160, -59.99999999999999289, 105.7065446260163526 ) ) ;
#106040=CARTESIAN_POINT ( 'NONE',  ( 36.05900422978820075, -60.00000000000002132, 50.77828662454974307 ) ) ;
#106054=CARTESIAN_POINT ( 'NONE',  ( -36.75617418030669370, -59.99999999999754152, 51.65163013687570981 ) ) ;
#106056=CARTESIAN_POINT ( 'NONE',  ( 89.54885025292163903, -60.00000000000002132, 201.8582137258730143 ) ) ;
#106059=CARTESIAN_POINT ( 'NONE',  ( -108.2763249159406769, -59.99999999999986500, 199.3718883026843116 ) ) ;
#106060=CARTESIAN_POINT ( 'NONE',  ( 17.02384506383146245, -53.39628896086755816, 33.04942014297441943 ) ) ;
#106062=CARTESIAN_POINT ( 'NONE',  ( 100.9474370845066176, -38.00000000000000711, 146.8126285005432408 ) ) ;
#106065=CARTESIAN_POINT ( 'NONE',  ( -43.92060318859008561, -39.52985988317308141, 42.42323198190868538 ) ) ;
#106078=CARTESIAN_POINT ( 'NONE',  ( 92.35295832812823846, -30.00000000007834089, 199.7455495689326312 ) ) ;
#106084=CARTESIAN_POINT ( 'NONE',  ( 97.43685538820150782, -30.00000000000000000, 133.5638869304015088 ) ) ;
#106097=CARTESIAN_POINT ( 'NONE',  ( 85.26653421436701308, -38.68462227007306353, 198.6437487644617761 ) ) ;
#106100=CARTESIAN_POINT ( 'NONE',  ( 86.49569524121002928, -38.00000000000003553, 187.7518329194348894 ) ) ;
#106121=CARTESIAN_POINT ( 'NONE',  ( 83.75659386667784645, -61.01700501349375116, 191.9530215260792829 ) ) ;
#106126=CARTESIAN_POINT ( 'NONE',  ( 83.06228876499081082, -57.67107222564732893, -28.36318629505660738 ) ) ;
#106129=CARTESIAN_POINT ( 'NONE',  ( -81.36319491956838590, -30.00000000000000711, -1.421388179323267220 ) ) ;
#106151=CARTESIAN_POINT ( 'NONE',  ( -17.87520619753193429, -17.95932086966949015, -34.00109537085095468 ) ) ;
#106153=CARTESIAN_POINT ( 'NONE',  ( -25.91394795060947942, -60.22836619208757014, -35.60171098623400354 ) ) ;
#106159=CARTESIAN_POINT ( 'NONE',  ( -66.81167781205434153, -60.00000000000000711, -33.62895559939038037 ) ) ;
#106161=CARTESIAN_POINT ( 'NONE',  ( 25.47402648759802446, -28.38081445280734982, -30.30612721234350815 ) ) ;
#106163=CARTESIAN_POINT ( 'NONE',  ( 98.11478003982226426, -60.34325407385573214, 196.5388644659511783 ) ) ;
#106167=CARTESIAN_POINT ( 'NONE',  ( -81.52096736789169995, -42.97176952543888717, 161.5648495392605923 ) ) ;
#106177=CARTESIAN_POINT ( 'NONE',  ( -111.5786317092108533, -57.67087409935591324, 192.6842770035980834 ) ) ;
#106182=CARTESIAN_POINT ( 'NONE',  ( 8.309465130445103043, -30.00000000000003197, -39.88086614825118659 ) ) ;
#106183=EDGE_CURVE ( 'NONE', #65536, #34458, #5092, .T. ) ;
#106184=CARTESIAN_POINT ( 'NONE',  ( -4.155049527179308200, -30.00000000000002842, 36.99135516471767460 ) ) ;
#106186=CARTESIAN_POINT ( 'NONE',  ( -53.18781749681305371, -56.84782064553103709, 63.26121515912522142 ) ) ;
#106189=CARTESIAN_POINT ( 'NONE',  ( -97.18938212093779327, -37.69980210926051001, 192.7882013891335191 ) ) ;
#106194=CARTESIAN_POINT ( 'NONE',  ( 91.24927989895878966, -38.36004604005931640, -1.395253234482411786 ) ) ;
#106200=CARTESIAN_POINT ( 'NONE',  ( 83.93844488845637386, -29.99999999999999645, 160.4690723128815932 ) ) ;
#106206=CARTESIAN_POINT ( 'NONE',  ( 49.59389593497978410, -22.20511380567462112, 44.49589264220691831 ) ) ;
#106212=CARTESIAN_POINT ( 'NONE',  ( -98.34829155932973777, -38.35547239742750492, 78.70912769862152913 ) ) ;
#106215=CARTESIAN_POINT ( 'NONE',  ( 110.3578795809912094, -38.35604999599375020, 158.7521924589690627 ) ) ;
#106219=CARTESIAN_POINT ( 'NONE',  ( 101.8269878747205723, -52.71687279565823303, 134.8528526430313832 ) ) ;
#106226=CARTESIAN_POINT ( 'NONE',  ( 75.46095339194756946, -60.00000000000001421, 184.2592822936660184 ) ) ;
#106231=CARTESIAN_POINT ( 'NONE',  ( 55.73253904170881157, -29.08777573428741547, 57.64467041135599601 ) ) ;
#106233=DIRECTION ( 'NONE',  ( -0.000000000000000000, -1.000000000000000000, -0.000000000000000000 ) ) ;
#106236=CARTESIAN_POINT ( 'NONE',  ( -79.13986484937814225, -29.99999999996501998, 187.8162035005837254 ) ) ;
#106247=CARTESIAN_POINT ( 'NONE',  ( 85.70055246076826450, -21.88621194787217306, 168.6156743441144954 ) ) ;
#106263=CARTESIAN_POINT ( 'NONE',  ( -5.931024892954755323, -18.81772794593000953, 35.12675206171071807 ) ) ;
#106275=CARTESIAN_POINT ( 'NONE',  ( 2.499999999999970690, -27.33278124259516773, -31.42875788144166549 ) ) ;
#106283=CARTESIAN_POINT ( 'NONE',  ( -106.4944820610378855, -60.00000000000000711, 119.4794274787003161 ) ) ;
#106294=CARTESIAN_POINT ( 'NONE',  ( -81.41272853779376817, -60.59700324890057033, 185.5284586587616502 ) ) ;
#106307=CARTESIAN_POINT ( 'NONE',  ( 107.5810510768942549, -30.00000000000001066, 145.3411688640341879 ) ) ;
#106308=CARTESIAN_POINT ( 'NONE',  ( -104.0091953780157752, -14.21045842199432663, 192.0632730704776066 ) ) ;
#106309=CARTESIAN_POINT ( 'NONE',  ( -60.83465437253532571, -46.44060695584406062, 77.79315034241348314 ) ) ;
#106313=CARTESIAN_POINT ( 'NONE',  ( 114.2967361943732953, -59.99999999999019451, 163.3079217394894727 ) ) ;
#106315=CARTESIAN_POINT ( 'NONE',  ( 1.010365562846486931, -46.43475217007103595, 31.62877532128088731 ) ) ;
#106321=CARTESIAN_POINT ( 'NONE',  ( 80.00000000000000000, -52.00000000000000000, -23.09707704303352926 ) ) ;
#106322=CARTESIAN_POINT ( 'NONE',  ( -108.2569967048411002, -60.00000000000000000, 195.1947638852328168 ) ) ;
#106335=CARTESIAN_POINT ( 'NONE',  ( 106.3131009653180001, -59.99999999999999289, 178.6139974719857832 ) ) ;
#106336=CARTESIAN_POINT ( 'NONE',  ( -32.18409987042326037, -32.55419226210070605, 32.69844470122687596 ) ) ;
#106337=CARTESIAN_POINT ( 'NONE',  ( 2.723397405354400211E-15, -8.673617379884035472E-16, 22.23822744035697241 ) ) ;
#106339=CARTESIAN_POINT ( 'NONE',  ( 41.05623627240671425, -36.06612582573725234, 38.79247790458893519 ) ) ;
#106346=CARTESIAN_POINT ( 'NONE',  ( -76.87893151430891692, -38.44669289976816628, 183.7668099329592906 ) ) ;
#106357=CARTESIAN_POINT ( 'NONE',  ( 92.37230681663571374, -60.00000000000000711, 25.27844034073237012 ) ) ;
#106361=CARTESIAN_POINT ( 'NONE',  ( -97.81687375994280842, -30.00000000000000711, 190.6942671029864016 ) ) ;
#106378=CARTESIAN_POINT ( 'NONE',  ( 81.68119091632517836, -32.56014869712902993, 148.9471023736466861 ) ) ;
#106387=CARTESIAN_POINT ( 'NONE',  ( -41.14701979708251400, -57.68941641447864299, 57.58229189354211286 ) ) ;
#106399=CARTESIAN_POINT ( 'NONE',  ( 25.33765615706812824, -29.26986317732292875, 38.39381496285782447 ) ) ;
#106410=CARTESIAN_POINT ( 'NONE',  ( 34.43512893958828869, -31.17098412693171738, -37.93505368340076700 ) ) ;
#106417=CARTESIAN_POINT ( 'NONE',  ( 98.12606319475514738, -57.67113334830845162, 57.02791250460963823 ) ) ;
#106423=CARTESIAN_POINT ( 'NONE',  ( -73.46981879484900446, -60.00000000000000711, 166.8934759688809493 ) ) ;
#106430=CARTESIAN_POINT ( 'NONE',  ( -86.24395819885462799, -21.22842368464919360, 178.4804303958884191 ) ) ;
#106434=ORIENTED_EDGE ( 'NONE', *, *, #6254, .F. ) ;
#106437=CARTESIAN_POINT ( 'NONE',  ( -84.47593557506488082, -45.26840861548302541, -7.721260587021224531 ) ) ;
#106446=CARTESIAN_POINT ( 'NONE',  ( 14.86825985028009711, -3.469446951953614189E-15, -8.569529079650944681 ) ) ;
#106448=CARTESIAN_POINT ( 'NONE',  ( 56.79302105626919683, -14.21045842199427867, -31.02814365720875500 ) ) ;
#106449=CARTESIAN_POINT ( 'NONE',  ( -77.12671445486094512, -46.43767849076631649, 136.1084143596141018 ) ) ;
#106451=CARTESIAN_POINT ( 'NONE',  ( 39.04758850296788353, -59.99999999999992184, 54.77506993285218329 ) ) ;
#106453=CARTESIAN_POINT ( 'NONE',  ( 98.20513577084435042, -57.67132909654652906, 57.59918237178697353 ) ) ;
#106471=CARTESIAN_POINT ( 'NONE',  ( -29.53202096672922039, -60.00000000000010658, 45.26681583358117678 ) ) ;
#106472=CARTESIAN_POINT ( 'NONE',  ( 30.76658144297569208, -60.32562095059588358, 37.11897213549833907 ) ) ;
#106492=CARTESIAN_POINT ( 'NONE',  ( 76.77425057322363955, -30.00000000000000355, -16.81280392441903615 ) ) ;
#106517=CARTESIAN_POINT ( 'NONE',  ( 67.10493487639952548, -60.33315822119670457, 104.4191278749690213 ) ) ;
#106522=FACE_OUTER_BOUND ( 'NONE', #98864, .T. ) ;
#106543=CARTESIAN_POINT ( 'NONE',  ( -97.61356772442498198, -30.00000000000000000, 190.8259052030175837 ) ) ;
#106548=CARTESIAN_POINT ( 'NONE',  ( 73.67851877562725349, -57.62598256385592776, 185.4460714352483137 ) ) ;
#106556=CARTESIAN_POINT ( 'NONE',  ( -3.616699737053585828, -60.00000000000002132, 39.63238166876963930 ) ) ;
#106560=CARTESIAN_POINT ( 'NONE',  ( -86.96504166901752342, -31.71858355094692072, 187.3098402634578861 ) ) ;
#106565=CARTESIAN_POINT ( 'NONE',  ( -7.255220592255878564, -56.88418264328358021, 33.36068424955863065 ) ) ;
#106579=CARTESIAN_POINT ( 'NONE',  ( 114.2391797980453276, -59.99999999999998579, 181.3573912910646015 ) ) ;
#106600=CARTESIAN_POINT ( 'NONE',  ( -28.88003843141569149, -59.99999999999504752, 45.10078281693999003 ) ) ;
#106602=CARTESIAN_POINT ( 'NONE',  ( 92.77553358407693906, -60.00000000000002132, 30.03680362789697611 ) ) ;
#106603=CARTESIAN_POINT ( 'NONE',  ( -109.5675793427969040, -29.99999999999999289, 170.1817020036065742 ) ) ;
#106604=CARTESIAN_POINT ( 'NONE',  ( 16.44069842872639597, -22.06891279552154472, 27.77928941714268518 ) ) ;
#106608=CARTESIAN_POINT ( 'NONE',  ( -44.36511314976974063, -18.78910562120168137, 37.46626611847334942 ) ) ;
#106615=CARTESIAN_POINT ( 'NONE',  ( 2.500000000000001776, -13.08383851101123163, -21.61544523615733482 ) ) ;
#106621=CARTESIAN_POINT ( 'NONE',  ( 74.76569601199581427, -30.00000000009216805, 154.8922564148840877 ) ) ;
#106625=CARTESIAN_POINT ( 'NONE',  ( 92.05506390259360217, -30.00000000000000355, 100.4937872494486015 ) ) ;
#106640=CARTESIAN_POINT ( 'NONE',  ( 87.39133433791327832, -38.57836354491904274, 199.7233327510910499 ) ) ;
#106662=CARTESIAN_POINT ( 'NONE',  ( 84.17059686059378976, -61.05527343651194627, 192.5408628639999051 ) ) ;
#106667=CARTESIAN_POINT ( 'NONE',  ( 79.56493839289275627, -57.67121238173562148, -30.45972677269765327 ) ) ;
#106671=CARTESIAN_POINT ( 'NONE',  ( -81.37744105750925883, -30.00000000000000711, -10.21548990795500522 ) ) ;
#106672=EDGE_CURVE ( 'NONE', #71545, #91694, #76175, .T. ) ;
#106674=CARTESIAN_POINT ( 'NONE',  ( -83.79209681126675946, -37.99999999999999289, 174.8870184814763036 ) ) ;
#106686=CARTESIAN_POINT ( 'NONE',  ( -99.45001380552274384, -38.00000000000004974, 191.4583679090391684 ) ) ;
#106692=CARTESIAN_POINT ( 'NONE',  ( -66.35739722136700891, -34.58948124108970745, -23.23708708512139509 ) ) ;
#106701=CARTESIAN_POINT ( 'NONE',  ( -66.14035079976200393, -60.00000000000000000, -33.84619808995684309 ) ) ;
#106705=CARTESIAN_POINT ( 'NONE',  ( 99.19867269638797325, -45.26832955309748030, 193.2066468836933382 ) ) ;
#106721=CARTESIAN_POINT ( 'NONE',  ( -61.06992298392258078, -57.67755795743399716, 111.0944920020532862 ) ) ;
#106726=CARTESIAN_POINT ( 'NONE',  ( 8.180134260905338905, -14.21045842199436926, -37.25106736021741227 ) ) ;
#106730=CARTESIAN_POINT ( 'NONE',  ( -51.87710858498652300, -39.51066125304492260, 54.03131810460910600 ) ) ;
#106733=CARTESIAN_POINT ( 'NONE',  ( -98.99772353281480264, -45.25013960604325547, 193.3232175602864231 ) ) ;
#106739=CARTESIAN_POINT ( 'NONE',  ( 89.50843841616533325, -38.52256170111905220, 200.4442316066328260 ) ) ;
#106744=CARTESIAN_POINT ( 'NONE',  ( 82.54044539369691336, -30.00000000000000355, 149.6189146675613415 ) ) ;
#106751=CARTESIAN_POINT ( 'NONE',  ( 49.43331438854296778, -32.59166132229344726, 47.58368122656079890 ) ) ;
#106757=CARTESIAN_POINT ( 'NONE',  ( -92.64360711281031513, -38.35495908042472024, 40.47194345170088070 ) ) ;
#106760=CARTESIAN_POINT ( 'NONE',  ( 98.46909904549914927, -38.35583610091571671, 79.42329170081190171 ) ) ;
#106762=CARTESIAN_POINT ( 'NONE',  ( 103.0583287818154048, -60.15111231639958334, 134.7092673011946147 ) ) ;
#106768=CARTESIAN_POINT ( 'NONE',  ( 74.39885652900197499, -60.00000000000000000, 176.1565043745205230 ) ) ;
#106771=CARTESIAN_POINT ( 'NONE',  ( 60.51310404470154225, -39.48713381824052959, 73.58315150410720662 ) ) ;
#106775=CARTESIAN_POINT ( 'NONE',  ( -64.15115902790869029, -29.99999999991991828, 104.9769517853171976 ) ) ;
#106785=CARTESIAN_POINT ( 'NONE',  ( 69.96852216794175661, -47.40896019409530027, -24.11339453208464434 ) ) ;
ENDSEC;
END-ISO-10303-21;
